ISO-10303-21;
HEADER;
/* Generated by software containing ST-Developer
 * from STEP Tools, Inc. (www.steptools.com) 
 */

FILE_DESCRIPTION(
/* description */ (''),
/* implementation_level */ '2;1');

FILE_NAME(
/* name */ 'Precision Feed Screw D5 Lead 2.step',
/* time_stamp */ '2026-10-15T12:29:06-07:00',
/* author */ (''),
/* organization */ (''),
/* preprocessor_version */ 'ST-DEVELOPER v20.2',
/* originating_system */ 'Autodesk Translation Framework v15.15.0.0',
/* authorisation */ '');

FILE_SCHEMA (('AUTOMOTIVE_DESIGN { 1 0 10303 214 3 1 1 }'));
ENDSEC;

DATA;
#10=MECHANICAL_DESIGN_GEOMETRIC_PRESENTATION_REPRESENTATION('',(#1742),#135282);
#304=B_SPLINE_SURFACE_WITH_KNOTS('',3,3,((#48705,#48706,#48707,#48708,#48709,
#48710,#48711,#48712,#48713,#48714,#48715,#48716,#48717,#48718,#48719,#48720,
#48721,#48722,#48723,#48724,#48725,#48726,#48727,#48728,#48729,#48730,#48731,
#48732,#48733,#48734,#48735,#48736,#48737,#48738,#48739),(#48740,#48741,
#48742,#48743,#48744,#48745,#48746,#48747,#48748,#48749,#48750,#48751,#48752,
#48753,#48754,#48755,#48756,#48757,#48758,#48759,#48760,#48761,#48762,#48763,
#48764,#48765,#48766,#48767,#48768,#48769,#48770,#48771,#48772,#48773,#48774),
(#48775,#48776,#48777,#48778,#48779,#48780,#48781,#48782,#48783,#48784,
#48785,#48786,#48787,#48788,#48789,#48790,#48791,#48792,#48793,#48794,#48795,
#48796,#48797,#48798,#48799,#48800,#48801,#48802,#48803,#48804,#48805,#48806,
#48807,#48808,#48809),(#48810,#48811,#48812,#48813,#48814,#48815,#48816,
#48817,#48818,#48819,#48820,#48821,#48822,#48823,#48824,#48825,#48826,#48827,
#48828,#48829,#48830,#48831,#48832,#48833,#48834,#48835,#48836,#48837,#48838,
#48839,#48840,#48841,#48842,#48843,#48844)),.UNSPECIFIED.,.F.,.F.,.F.,(4,
4),(4,1,1,1,1,1,1,1,1,1,1,1,1,1,1,1,1,1,1,1,1,1,1,1,1,1,1,1,1,1,1,1,4),
(0.,0.0601216701678314),(0.958497295273323,0.960061197080218,0.961540412003173,
0.964498841849082,0.967457271694992,0.970415701540902,0.970600603406271,
0.970785505271641,0.971155309002379,0.971894916463857,0.973374131386812,
0.974113738848289,0.974853346309767,0.976332561232722,0.977811776155676,
0.979290991078631,0.980770206001586,0.982249420924541,0.984221707488481,
0.986193994052421,0.988166280616361,0.989152423898331,0.989645495539316,
0.989892031359808,0.990015299270054,0.990076933225178,0.990138567180301,
0.99211085374424,0.99408314030818,0.995562355231135,0.99704157015409,0.998520785077045,
1.00008475653519),.UNSPECIFIED.);
#305=B_SPLINE_SURFACE_WITH_KNOTS('',3,3,((#49300,#49301,#49302,#49303,#49304,
#49305,#49306,#49307,#49308,#49309,#49310,#49311,#49312,#49313,#49314,#49315,
#49316,#49317,#49318,#49319,#49320,#49321,#49322,#49323,#49324,#49325,#49326,
#49327,#49328,#49329,#49330,#49331,#49332,#49333,#49334,#49335,#49336),
(#49337,#49338,#49339,#49340,#49341,#49342,#49343,#49344,#49345,#49346,
#49347,#49348,#49349,#49350,#49351,#49352,#49353,#49354,#49355,#49356,#49357,
#49358,#49359,#49360,#49361,#49362,#49363,#49364,#49365,#49366,#49367,#49368,
#49369,#49370,#49371,#49372,#49373),(#49374,#49375,#49376,#49377,#49378,
#49379,#49380,#49381,#49382,#49383,#49384,#49385,#49386,#49387,#49388,#49389,
#49390,#49391,#49392,#49393,#49394,#49395,#49396,#49397,#49398,#49399,#49400,
#49401,#49402,#49403,#49404,#49405,#49406,#49407,#49408,#49409,#49410),
(#49411,#49412,#49413,#49414,#49415,#49416,#49417,#49418,#49419,#49420,
#49421,#49422,#49423,#49424,#49425,#49426,#49427,#49428,#49429,#49430,#49431,
#49432,#49433,#49434,#49435,#49436,#49437,#49438,#49439,#49440,#49441,#49442,
#49443,#49444,#49445,#49446,#49447)),.UNSPECIFIED.,.F.,.F.,.F.,(4,4),(4,
1,1,1,1,1,1,1,1,1,1,1,1,1,1,1,1,1,1,1,1,1,1,1,1,1,1,1,1,1,1,1,1,1,4),(-0.0004131206956421,
0.0600746011189307),(-0.000245952479762335,0.0018432399144214,0.00368647982884281,
0.00552971974326421,0.00737295965768562,0.00983061287691415,0.0122882660961427,
0.013517092705757,0.0141315060105641,0.0144387126629677,0.0147459193153712,
0.0172035725345998,0.0196612257538283,0.0221188789730568,0.0245765321922854,
0.0258053588018997,0.0270341854115139,0.0294918386307425,0.0307206652403567,
0.031949491849971,0.0344071450691995,0.0352263628089424,0.0368647982884281,
0.0393224515076566,0.0399368648124638,0.0405512781172709,0.0417801047268852,
0.0430089313364994,0.0436233446413066,0.0439305512937101,0.0442377579461137,
0.0460809978605351,0.0479242377749565,0.0497674776893779,0.0518564147280488),
 .UNSPECIFIED.);
#306=B_SPLINE_SURFACE_WITH_KNOTS('',3,3,((#49706,#49707,#49708,#49709,#49710,
#49711,#49712,#49713,#49714,#49715,#49716,#49717,#49718,#49719,#49720,#49721,
#49722,#49723,#49724,#49725,#49726,#49727,#49728,#49729,#49730,#49731,#49732,
#49733,#49734,#49735,#49736,#49737,#49738,#49739,#49740,#49741,#49742,#49743,
#49744,#49745,#49746,#49747,#49748,#49749,#49750,#49751,#49752,#49753,#49754,
#49755,#49756,#49757,#49758,#49759,#49760,#49761,#49762,#49763,#49764,#49765,
#49766,#49767),(#49768,#49769,#49770,#49771,#49772,#49773,#49774,#49775,
#49776,#49777,#49778,#49779,#49780,#49781,#49782,#49783,#49784,#49785,#49786,
#49787,#49788,#49789,#49790,#49791,#49792,#49793,#49794,#49795,#49796,#49797,
#49798,#49799,#49800,#49801,#49802,#49803,#49804,#49805,#49806,#49807,#49808,
#49809,#49810,#49811,#49812,#49813,#49814,#49815,#49816,#49817,#49818,#49819,
#49820,#49821,#49822,#49823,#49824,#49825,#49826,#49827,#49828,#49829),
(#49830,#49831,#49832,#49833,#49834,#49835,#49836,#49837,#49838,#49839,
#49840,#49841,#49842,#49843,#49844,#49845,#49846,#49847,#49848,#49849,#49850,
#49851,#49852,#49853,#49854,#49855,#49856,#49857,#49858,#49859,#49860,#49861,
#49862,#49863,#49864,#49865,#49866,#49867,#49868,#49869,#49870,#49871,#49872,
#49873,#49874,#49875,#49876,#49877,#49878,#49879,#49880,#49881,#49882,#49883,
#49884,#49885,#49886,#49887,#49888,#49889,#49890,#49891),(#49892,#49893,
#49894,#49895,#49896,#49897,#49898,#49899,#49900,#49901,#49902,#49903,#49904,
#49905,#49906,#49907,#49908,#49909,#49910,#49911,#49912,#49913,#49914,#49915,
#49916,#49917,#49918,#49919,#49920,#49921,#49922,#49923,#49924,#49925,#49926,
#49927,#49928,#49929,#49930,#49931,#49932,#49933,#49934,#49935,#49936,#49937,
#49938,#49939,#49940,#49941,#49942,#49943,#49944,#49945,#49946,#49947,#49948,
#49949,#49950,#49951,#49952,#49953)),.UNSPECIFIED.,.F.,.F.,.F.,(4,4),(4,
1,1,1,1,1,1,1,1,1,1,1,1,1,1,1,1,1,1,1,1,1,1,1,1,1,1,1,1,1,1,1,1,1,1,1,1,
1,1,1,1,1,1,1,1,1,1,1,1,1,1,1,1,1,1,1,1,1,1,4),(-0.000719064234915953,0.0600510031832868),
(0.116699315494241,0.118587303856748,0.120430777434874,0.122274251012999,
0.124117724591124,0.125961198169249,0.127804671747374,0.1296481453255,0.131491618903625,
0.133949583674458,0.134564074867167,0.135178566059875,0.136407548445292,
0.138865513216126,0.141323477986959,0.143781442757793,0.146239407528626,
0.148082881106752,0.149926354684877,0.151769828263002,0.153613301841127,
0.155456775419252,0.157300248997378,0.159143722575503,0.160987196153628,
0.162830669731753,0.164674143309878,0.166517616888004,0.168361090466129,
0.170204564044254,0.172048037622379,0.173891511200504,0.17573498477863,
0.178192949549463,0.180650914320297,0.18310887909113,0.185566843861964,
0.186795826247381,0.188024808632798,0.190482773403631,0.191711755789048,
0.192940738174465,0.193247983770819,0.193555229367173,0.194169720559882,
0.19478421175259,0.195398702945298,0.197856667716132,0.200314632486966,
0.201953275667521,0.205230562028633,0.205691430423164,0.207074035606758,
0.208917509184883,0.210760982763008,0.212604456341134,0.214447929919259,
0.216291403497384,0.218134877075509,0.220431769292195),.UNSPECIFIED.);
#307=B_SPLINE_SURFACE_WITH_KNOTS('',3,3,((#50568,#50569,#50570,#50571,#50572,
#50573,#50574,#50575,#50576,#50577,#50578,#50579,#50580,#50581,#50582,#50583,
#50584,#50585,#50586,#50587,#50588,#50589,#50590,#50591,#50592,#50593,#50594,
#50595,#50596,#50597,#50598,#50599,#50600,#50601,#50602,#50603,#50604,#50605,
#50606,#50607,#50608,#50609,#50610,#50611,#50612,#50613,#50614,#50615,#50616,
#50617,#50618,#50619,#50620,#50621,#50622,#50623,#50624,#50625,#50626,#50627,
#50628,#50629,#50630,#50631,#50632,#50633,#50634,#50635,#50636),(#50637,
#50638,#50639,#50640,#50641,#50642,#50643,#50644,#50645,#50646,#50647,#50648,
#50649,#50650,#50651,#50652,#50653,#50654,#50655,#50656,#50657,#50658,#50659,
#50660,#50661,#50662,#50663,#50664,#50665,#50666,#50667,#50668,#50669,#50670,
#50671,#50672,#50673,#50674,#50675,#50676,#50677,#50678,#50679,#50680,#50681,
#50682,#50683,#50684,#50685,#50686,#50687,#50688,#50689,#50690,#50691,#50692,
#50693,#50694,#50695,#50696,#50697,#50698,#50699,#50700,#50701,#50702,#50703,
#50704,#50705),(#50706,#50707,#50708,#50709,#50710,#50711,#50712,#50713,
#50714,#50715,#50716,#50717,#50718,#50719,#50720,#50721,#50722,#50723,#50724,
#50725,#50726,#50727,#50728,#50729,#50730,#50731,#50732,#50733,#50734,#50735,
#50736,#50737,#50738,#50739,#50740,#50741,#50742,#50743,#50744,#50745,#50746,
#50747,#50748,#50749,#50750,#50751,#50752,#50753,#50754,#50755,#50756,#50757,
#50758,#50759,#50760,#50761,#50762,#50763,#50764,#50765,#50766,#50767,#50768,
#50769,#50770,#50771,#50772,#50773,#50774),(#50775,#50776,#50777,#50778,
#50779,#50780,#50781,#50782,#50783,#50784,#50785,#50786,#50787,#50788,#50789,
#50790,#50791,#50792,#50793,#50794,#50795,#50796,#50797,#50798,#50799,#50800,
#50801,#50802,#50803,#50804,#50805,#50806,#50807,#50808,#50809,#50810,#50811,
#50812,#50813,#50814,#50815,#50816,#50817,#50818,#50819,#50820,#50821,#50822,
#50823,#50824,#50825,#50826,#50827,#50828,#50829,#50830,#50831,#50832,#50833,
#50834,#50835,#50836,#50837,#50838,#50839,#50840,#50841,#50842,#50843)),
 .UNSPECIFIED.,.F.,.F.,.F.,(4,4),(4,1,1,1,1,1,1,1,1,1,1,1,1,1,1,1,1,1,1,
1,1,1,1,1,1,1,1,1,1,1,1,1,1,1,1,1,1,1,1,1,1,1,1,1,1,1,1,1,1,1,1,1,1,1,1,
1,1,1,1,1,1,1,1,1,1,1,4),(-0.000304659761922948,0.0600640983517747),(0.285071931319951,
0.286954925748233,0.288798399656758,0.290641873565284,0.292485347473809,
0.294328821382334,0.296172295290859,0.298015769199385,0.29985924310791,
0.302317208319277,0.304775173530644,0.307233138742011,0.309076612650536,
0.310920086559061,0.312763560467587,0.314607034376112,0.316450508284637,
0.318293982193163,0.319215719147425,0.320137456101688,0.320828758817385,
0.32105919305595,0.321520061533082,0.321750495771647,0.321980930010213,
0.32428527239587,0.325667877827264,0.328433088690051,0.329354825644314,
0.331198299552839,0.333041773461365,0.33488524736989,0.336728721278415,
0.337189589755546,0.337650458232678,0.33857219518694,0.339493932141203,
0.340415669095466,0.342259143003991,0.344102616912516,0.345946090821041,
0.347789564729567,0.349633038638092,0.351476512546617,0.352091003849459,
0.35239824950088,0.352705495152301,0.353934477757984,0.356392442969351,
0.357621425575035,0.358235916877876,0.358850408180718,0.361308373392085,
0.363766338603452,0.366224303814819,0.368682269026186,0.370320912500431,
0.371959555974676,0.37359819944892,0.375441673357445,0.377285147265971,
0.379128621174496,0.380972095083021,0.382815568991547,0.384659042900072,
0.386502516808597,0.388345990717122),.UNSPECIFIED.);
#308=B_SPLINE_SURFACE_WITH_KNOTS('',3,3,((#52114,#52115,#52116,#52117,#52118,
#52119,#52120,#52121,#52122,#52123,#52124,#52125,#52126,#52127,#52128,#52129,
#52130,#52131,#52132,#52133,#52134,#52135,#52136,#52137,#52138,#52139,#52140,
#52141,#52142,#52143,#52144,#52145,#52146,#52147,#52148,#52149,#52150,#52151,
#52152,#52153,#52154,#52155,#52156,#52157,#52158,#52159,#52160,#52161,#52162,
#52163,#52164,#52165,#52166,#52167,#52168,#52169,#52170,#52171,#52172,#52173,
#52174,#52175,#52176),(#52177,#52178,#52179,#52180,#52181,#52182,#52183,
#52184,#52185,#52186,#52187,#52188,#52189,#52190,#52191,#52192,#52193,#52194,
#52195,#52196,#52197,#52198,#52199,#52200,#52201,#52202,#52203,#52204,#52205,
#52206,#52207,#52208,#52209,#52210,#52211,#52212,#52213,#52214,#52215,#52216,
#52217,#52218,#52219,#52220,#52221,#52222,#52223,#52224,#52225,#52226,#52227,
#52228,#52229,#52230,#52231,#52232,#52233,#52234,#52235,#52236,#52237,#52238,
#52239),(#52240,#52241,#52242,#52243,#52244,#52245,#52246,#52247,#52248,
#52249,#52250,#52251,#52252,#52253,#52254,#52255,#52256,#52257,#52258,#52259,
#52260,#52261,#52262,#52263,#52264,#52265,#52266,#52267,#52268,#52269,#52270,
#52271,#52272,#52273,#52274,#52275,#52276,#52277,#52278,#52279,#52280,#52281,
#52282,#52283,#52284,#52285,#52286,#52287,#52288,#52289,#52290,#52291,#52292,
#52293,#52294,#52295,#52296,#52297,#52298,#52299,#52300,#52301,#52302),
(#52303,#52304,#52305,#52306,#52307,#52308,#52309,#52310,#52311,#52312,
#52313,#52314,#52315,#52316,#52317,#52318,#52319,#52320,#52321,#52322,#52323,
#52324,#52325,#52326,#52327,#52328,#52329,#52330,#52331,#52332,#52333,#52334,
#52335,#52336,#52337,#52338,#52339,#52340,#52341,#52342,#52343,#52344,#52345,
#52346,#52347,#52348,#52349,#52350,#52351,#52352,#52353,#52354,#52355,#52356,
#52357,#52358,#52359,#52360,#52361,#52362,#52363,#52364,#52365)),
 .UNSPECIFIED.,.F.,.F.,.F.,(4,4),(4,1,1,1,1,1,1,1,1,1,1,1,1,1,1,1,1,1,1,
1,1,1,1,1,1,1,1,1,1,1,1,1,1,1,1,1,1,1,1,1,1,1,1,1,1,1,1,1,1,1,1,1,1,1,1,
1,1,1,1,1,4),(-0.000669329015107292,0.0600896068960631),(0.453390084310778,
0.45532256751791,0.457166041104501,0.459009514691093,0.460852988277684,
0.462696461864275,0.464539935450866,0.466383409037458,0.468226882624049,
0.470684847406171,0.473142812188293,0.475600776970414,0.478058741752536,
0.480516706534658,0.48297467131678,0.484818144903371,0.486661618489962,
0.488505092076554,0.490348565663145,0.492192039249736,0.494035512836328,
0.495878986422919,0.49772246000951,0.498183328406158,0.498644196802806,
0.499565933596102,0.501409407182693,0.503252880769284,0.505096354355876,
0.506939827942467,0.507400696339115,0.508783301529058,0.510626775115649,
0.512470248702241,0.514928213484362,0.517386178266484,0.519844143048606,
0.522302107830728,0.52476007261285,0.527218037394971,0.529676002177093,
0.530290493372624,0.530904984568154,0.531519475763684,0.532133966959215,
0.534591931741337,0.535820914132398,0.537049896523458,0.53868853971154,
0.540327182899621,0.541965826087702,0.542887562880998,0.543809299674293,
0.544731036467589,0.545652773260885,0.547496246847476,0.549339720434067,
0.551183194020659,0.55302666760725,0.554870141193841,0.55716859910234),
 .UNSPECIFIED.);
#309=B_SPLINE_SURFACE_WITH_KNOTS('',3,3,((#53368,#53369,#53370,#53371,#53372,
#53373,#53374,#53375,#53376,#53377,#53378,#53379,#53380,#53381,#53382,#53383,
#53384,#53385,#53386,#53387,#53388,#53389,#53390,#53391,#53392,#53393,#53394,
#53395,#53396,#53397,#53398,#53399,#53400,#53401,#53402,#53403,#53404,#53405,
#53406,#53407,#53408,#53409,#53410,#53411,#53412,#53413,#53414,#53415,#53416,
#53417,#53418,#53419,#53420,#53421,#53422,#53423,#53424),(#53425,#53426,
#53427,#53428,#53429,#53430,#53431,#53432,#53433,#53434,#53435,#53436,#53437,
#53438,#53439,#53440,#53441,#53442,#53443,#53444,#53445,#53446,#53447,#53448,
#53449,#53450,#53451,#53452,#53453,#53454,#53455,#53456,#53457,#53458,#53459,
#53460,#53461,#53462,#53463,#53464,#53465,#53466,#53467,#53468,#53469,#53470,
#53471,#53472,#53473,#53474,#53475,#53476,#53477,#53478,#53479,#53480,#53481),
(#53482,#53483,#53484,#53485,#53486,#53487,#53488,#53489,#53490,#53491,
#53492,#53493,#53494,#53495,#53496,#53497,#53498,#53499,#53500,#53501,#53502,
#53503,#53504,#53505,#53506,#53507,#53508,#53509,#53510,#53511,#53512,#53513,
#53514,#53515,#53516,#53517,#53518,#53519,#53520,#53521,#53522,#53523,#53524,
#53525,#53526,#53527,#53528,#53529,#53530,#53531,#53532,#53533,#53534,#53535,
#53536,#53537,#53538),(#53539,#53540,#53541,#53542,#53543,#53544,#53545,
#53546,#53547,#53548,#53549,#53550,#53551,#53552,#53553,#53554,#53555,#53556,
#53557,#53558,#53559,#53560,#53561,#53562,#53563,#53564,#53565,#53566,#53567,
#53568,#53569,#53570,#53571,#53572,#53573,#53574,#53575,#53576,#53577,#53578,
#53579,#53580,#53581,#53582,#53583,#53584,#53585,#53586,#53587,#53588,#53589,
#53590,#53591,#53592,#53593,#53594,#53595)),.UNSPECIFIED.,.F.,.F.,.F.,(4,
4),(4,1,1,1,1,1,1,1,1,1,1,1,1,1,1,1,1,1,1,1,1,1,1,1,1,1,1,1,1,1,1,1,1,1,
1,1,1,1,1,1,1,1,1,1,1,1,1,1,1,1,1,1,1,1,4),(-0.000398179937811476,0.0600544212357538),
(0.621792488306161,0.623690199736931,0.625533673395834,0.627377147054738,
0.629220620713642,0.631064094372546,0.63290756803145,0.634751041690353,
0.636594515349257,0.639052480227795,0.641510445106334,0.643968409984872,
0.646426374863411,0.648884339741949,0.651342304620487,0.653185778279391,
0.655029251938295,0.657333594011925,0.658716199256103,0.660559672915006,
0.66240314657391,0.663324883403362,0.666090093891718,0.667933567550621,
0.669777041209525,0.671620514868429,0.673463988527333,0.674846593771511,
0.675307462186237,0.677150935845141,0.678994409504044,0.680837883162948,
0.683295848041487,0.685753812920025,0.688211777798563,0.690669742677102,
0.69312770755564,0.695585672434178,0.698043637312717,0.700501602191255,
0.701730584630524,0.702959567069794,0.703574058289428,0.705417531948332,
0.707056175200691,0.710333461705409,0.711716066949587,0.712176935364313,
0.714020409023216,0.71586388268212,0.717707356341024,0.719550829999928,
0.721394303658832,0.723237777317735,0.725081250976639),.UNSPECIFIED.);
#310=B_SPLINE_SURFACE_WITH_KNOTS('',3,3,((#55419,#55420,#55421,#55422,#55423,
#55424,#55425,#55426,#55427,#55428,#55429,#55430,#55431,#55432,#55433,#55434,
#55435,#55436,#55437,#55438,#55439,#55440,#55441,#55442,#55443,#55444,#55445,
#55446,#55447,#55448,#55449,#55450,#55451,#55452,#55453,#55454,#55455,#55456,
#55457,#55458,#55459,#55460,#55461,#55462,#55463,#55464,#55465,#55466,#55467,
#55468,#55469,#55470,#55471,#55472,#55473,#55474,#55475,#55476),(#55477,
#55478,#55479,#55480,#55481,#55482,#55483,#55484,#55485,#55486,#55487,#55488,
#55489,#55490,#55491,#55492,#55493,#55494,#55495,#55496,#55497,#55498,#55499,
#55500,#55501,#55502,#55503,#55504,#55505,#55506,#55507,#55508,#55509,#55510,
#55511,#55512,#55513,#55514,#55515,#55516,#55517,#55518,#55519,#55520,#55521,
#55522,#55523,#55524,#55525,#55526,#55527,#55528,#55529,#55530,#55531,#55532,
#55533,#55534),(#55535,#55536,#55537,#55538,#55539,#55540,#55541,#55542,
#55543,#55544,#55545,#55546,#55547,#55548,#55549,#55550,#55551,#55552,#55553,
#55554,#55555,#55556,#55557,#55558,#55559,#55560,#55561,#55562,#55563,#55564,
#55565,#55566,#55567,#55568,#55569,#55570,#55571,#55572,#55573,#55574,#55575,
#55576,#55577,#55578,#55579,#55580,#55581,#55582,#55583,#55584,#55585,#55586,
#55587,#55588,#55589,#55590,#55591,#55592),(#55593,#55594,#55595,#55596,
#55597,#55598,#55599,#55600,#55601,#55602,#55603,#55604,#55605,#55606,#55607,
#55608,#55609,#55610,#55611,#55612,#55613,#55614,#55615,#55616,#55617,#55618,
#55619,#55620,#55621,#55622,#55623,#55624,#55625,#55626,#55627,#55628,#55629,
#55630,#55631,#55632,#55633,#55634,#55635,#55636,#55637,#55638,#55639,#55640,
#55641,#55642,#55643,#55644,#55645,#55646,#55647,#55648,#55649,#55650)),
 .UNSPECIFIED.,.F.,.F.,.F.,(4,4),(4,1,1,1,1,1,1,1,1,1,1,1,1,1,1,1,1,1,1,
1,1,1,1,1,1,1,1,1,1,1,1,1,1,1,1,1,1,1,1,1,1,1,1,1,1,1,1,1,1,1,1,1,1,1,1,
4),(-4.02403031655857E-6,0.09969297120439),(0.91568008989925,0.918757739489292,
0.9217667121008,0.924775684712307,0.927784657323815,0.92979063906482,0.931796620805825,
0.93380260254683,0.935307088852584,0.936811575158338,0.939820547769846,
0.940071295487471,0.940322043205097,0.940823538640348,0.940948912499161,
0.941074286357974,0.9413250340756,0.941575781793225,0.941701155652038,0.941826529510851,
0.942495190091186,0.943832511251856,0.944166841542024,0.944501171832191,
0.945169832412526,0.945838492992861,0.946507153573196,0.947844474733866,
0.949850456474872,0.951856438215877,0.953862419956882,0.955868401697887,
0.957874383438892,0.959880365179897,0.9608833560504,0.961886346920902,0.962889337791405,
0.963892328661908,0.966901301273415,0.969910273884923,0.972919246496431,
0.975928219107938,0.977432705413692,0.978937191719446,0.9804416780252,0.981946164330954,
0.983450650636708,0.984955136942461,0.986459623248215,0.987964109553969,
0.989468595859723,0.990973082165477,0.993982054776985,0.996991027388492,
0.998495513694246,1.00000605975256),.UNSPECIFIED.);
#311=B_SPLINE_SURFACE_WITH_KNOTS('',3,3,((#56234,#56235,#56236,#56237,#56238,
#56239,#56240,#56241,#56242,#56243,#56244,#56245,#56246,#56247,#56248,#56249,
#56250,#56251,#56252,#56253,#56254,#56255,#56256,#56257,#56258,#56259),
(#56260,#56261,#56262,#56263,#56264,#56265,#56266,#56267,#56268,#56269,
#56270,#56271,#56272,#56273,#56274,#56275,#56276,#56277,#56278,#56279,#56280,
#56281,#56282,#56283,#56284,#56285),(#56286,#56287,#56288,#56289,#56290,
#56291,#56292,#56293,#56294,#56295,#56296,#56297,#56298,#56299,#56300,#56301,
#56302,#56303,#56304,#56305,#56306,#56307,#56308,#56309,#56310,#56311),
(#56312,#56313,#56314,#56315,#56316,#56317,#56318,#56319,#56320,#56321,
#56322,#56323,#56324,#56325,#56326,#56327,#56328,#56329,#56330,#56331,#56332,
#56333,#56334,#56335,#56336,#56337)),.UNSPECIFIED.,.F.,.F.,.F.,(4,4),(4,
1,1,1,1,1,1,1,1,1,1,1,1,1,1,1,1,1,1,1,1,1,1,4),(-0.000160794326669428,0.0629206068794883),
(-0.000160794326669428,0.00204857271922254,0.00409714543844508,0.00614571815766761,
0.00819429087689015,0.00827964807352442,0.0083650052701587,0.00853571966342724,
0.00887714844996433,0.00956000602303851,0.0109257211691869,0.0122914363153352,
0.0136571514614836,0.0150228666076319,0.0163885817537803,0.0174128681133916,
0.0184371544730028,0.0194614408326141,0.0199735840124197,0.0204857271922254,
0.0225342999114479,0.0245828726306705,0.026631445349893,0.0288407216756201),
 .UNSPECIFIED.);
#312=B_SPLINE_SURFACE_WITH_KNOTS('',3,3,((#56339,#56340,#56341,#56342,#56343,
#56344,#56345,#56346,#56347,#56348,#56349,#56350,#56351,#56352,#56353,#56354,
#56355,#56356,#56357,#56358,#56359,#56360,#56361,#56362,#56363,#56364,#56365,
#56366,#56367,#56368,#56369,#56370,#56371,#56372,#56373,#56374,#56375,#56376,
#56377,#56378,#56379,#56380,#56381,#56382,#56383,#56384,#56385,#56386,#56387,
#56388,#56389,#56390,#56391,#56392,#56393,#56394,#56395,#56396,#56397,#56398,
#56399,#56400,#56401,#56402),(#56403,#56404,#56405,#56406,#56407,#56408,
#56409,#56410,#56411,#56412,#56413,#56414,#56415,#56416,#56417,#56418,#56419,
#56420,#56421,#56422,#56423,#56424,#56425,#56426,#56427,#56428,#56429,#56430,
#56431,#56432,#56433,#56434,#56435,#56436,#56437,#56438,#56439,#56440,#56441,
#56442,#56443,#56444,#56445,#56446,#56447,#56448,#56449,#56450,#56451,#56452,
#56453,#56454,#56455,#56456,#56457,#56458,#56459,#56460,#56461,#56462,#56463,
#56464,#56465,#56466),(#56467,#56468,#56469,#56470,#56471,#56472,#56473,
#56474,#56475,#56476,#56477,#56478,#56479,#56480,#56481,#56482,#56483,#56484,
#56485,#56486,#56487,#56488,#56489,#56490,#56491,#56492,#56493,#56494,#56495,
#56496,#56497,#56498,#56499,#56500,#56501,#56502,#56503,#56504,#56505,#56506,
#56507,#56508,#56509,#56510,#56511,#56512,#56513,#56514,#56515,#56516,#56517,
#56518,#56519,#56520,#56521,#56522,#56523,#56524,#56525,#56526,#56527,#56528,
#56529,#56530),(#56531,#56532,#56533,#56534,#56535,#56536,#56537,#56538,
#56539,#56540,#56541,#56542,#56543,#56544,#56545,#56546,#56547,#56548,#56549,
#56550,#56551,#56552,#56553,#56554,#56555,#56556,#56557,#56558,#56559,#56560,
#56561,#56562,#56563,#56564,#56565,#56566,#56567,#56568,#56569,#56570,#56571,
#56572,#56573,#56574,#56575,#56576,#56577,#56578,#56579,#56580,#56581,#56582,
#56583,#56584,#56585,#56586,#56587,#56588,#56589,#56590,#56591,#56592,#56593,
#56594)),.UNSPECIFIED.,.F.,.F.,.F.,(4,4),(4,1,1,1,1,1,1,1,1,1,1,1,1,1,1,
1,1,1,1,1,1,1,1,1,1,1,1,1,1,1,1,1,1,1,1,1,1,1,1,1,1,1,1,1,1,1,1,1,1,1,1,
1,1,1,1,1,1,1,1,1,1,4),(-9.26332648532586E-5,0.0996768470183328),(0.0738580961833418,
0.076109515853017,0.0783083908329088,0.0805072658128007,0.0827061407926925,
0.0849050157725843,0.0871038907524762,0.089302765732368,0.0915016407122598,
0.0944334740187823,0.0958993906720435,0.0973653073253047,0.100297140631827,
0.10322897393835,0.106160807244872,0.109092640551394,0.111291515531286,
0.113490390511178,0.11568926549107,0.117888140470962,0.120087015450854,
0.122285890430745,0.124484765410637,0.126683640390529,0.128882515370421,
0.131081390350313,0.133280265330205,0.135479140310096,0.137678015289988,
0.13987689026988,0.142075765249772,0.144274640229664,0.145740556882925,
0.147206473536186,0.147939431862817,0.150138306842709,0.153070140149231,
0.156001973455754,0.158933806762276,0.161865640068798,0.162598598395429,
0.16333155672206,0.16406451504869,0.164797473375321,0.167729306681843,0.170661139988366,
0.172127056641627,0.172860014968258,0.173592973294888,0.17554752883257,
0.17603616771699,0.176524806601411,0.177502084370251,0.179456639907933,
0.181655514887825,0.183854389867717,0.186053264847609,0.1882521398275,0.190451014807392,
0.192649889787284,0.194848764767176,0.197140249031834),.UNSPECIFIED.);
#313=B_SPLINE_SURFACE_WITH_KNOTS('',3,3,((#57145,#57146,#57147,#57148,#57149,
#57150,#57151,#57152,#57153,#57154,#57155,#57156,#57157,#57158,#57159,#57160,
#57161,#57162,#57163,#57164,#57165,#57166,#57167,#57168,#57169,#57170,#57171,
#57172,#57173,#57174,#57175,#57176,#57177,#57178,#57179,#57180,#57181,#57182,
#57183,#57184,#57185,#57186,#57187,#57188,#57189,#57190,#57191,#57192,#57193,
#57194,#57195,#57196,#57197,#57198,#57199,#57200,#57201,#57202,#57203,#57204,
#57205,#57206,#57207,#57208,#57209,#57210,#57211,#57212,#57213),(#57214,
#57215,#57216,#57217,#57218,#57219,#57220,#57221,#57222,#57223,#57224,#57225,
#57226,#57227,#57228,#57229,#57230,#57231,#57232,#57233,#57234,#57235,#57236,
#57237,#57238,#57239,#57240,#57241,#57242,#57243,#57244,#57245,#57246,#57247,
#57248,#57249,#57250,#57251,#57252,#57253,#57254,#57255,#57256,#57257,#57258,
#57259,#57260,#57261,#57262,#57263,#57264,#57265,#57266,#57267,#57268,#57269,
#57270,#57271,#57272,#57273,#57274,#57275,#57276,#57277,#57278,#57279,#57280,
#57281,#57282),(#57283,#57284,#57285,#57286,#57287,#57288,#57289,#57290,
#57291,#57292,#57293,#57294,#57295,#57296,#57297,#57298,#57299,#57300,#57301,
#57302,#57303,#57304,#57305,#57306,#57307,#57308,#57309,#57310,#57311,#57312,
#57313,#57314,#57315,#57316,#57317,#57318,#57319,#57320,#57321,#57322,#57323,
#57324,#57325,#57326,#57327,#57328,#57329,#57330,#57331,#57332,#57333,#57334,
#57335,#57336,#57337,#57338,#57339,#57340,#57341,#57342,#57343,#57344,#57345,
#57346,#57347,#57348,#57349,#57350,#57351),(#57352,#57353,#57354,#57355,
#57356,#57357,#57358,#57359,#57360,#57361,#57362,#57363,#57364,#57365,#57366,
#57367,#57368,#57369,#57370,#57371,#57372,#57373,#57374,#57375,#57376,#57377,
#57378,#57379,#57380,#57381,#57382,#57383,#57384,#57385,#57386,#57387,#57388,
#57389,#57390,#57391,#57392,#57393,#57394,#57395,#57396,#57397,#57398,#57399,
#57400,#57401,#57402,#57403,#57404,#57405,#57406,#57407,#57408,#57409,#57410,
#57411,#57412,#57413,#57414,#57415,#57416,#57417,#57418,#57419,#57420)),
 .UNSPECIFIED.,.F.,.F.,.F.,(4,4),(4,1,1,1,1,1,1,1,1,1,1,1,1,1,1,1,1,1,1,
1,1,1,1,1,1,1,1,1,1,1,1,1,1,1,1,1,1,1,1,1,1,1,1,1,1,1,1,1,1,1,1,1,1,1,1,
1,1,1,1,1,1,1,1,1,1,1,4),(0.,0.0996711058249781),(0.242231595226055,0.244477134072873,
0.246676009090878,0.248874884108883,0.251073759126888,0.253272634144893,
0.255471509162898,0.257670384180903,0.259869259198908,0.262801092556248,
0.264267009234918,0.264999967574253,0.265732925913588,0.267198842592258,
0.268664759270928,0.270130675949598,0.271596592628268,0.274528425985608,
0.277460259342948,0.279659134360953,0.281858009378958,0.284056884396963,
0.286255759414968,0.288454634432973,0.290653509450978,0.29175294695998,
0.292852384468983,0.293951821977985,0.295051259486988,0.297250134504992,
0.299449009522997,0.301647884541002,0.303846759559007,0.306045634577012,
0.308244509595017,0.310443384613022,0.312642259631027,0.315574092988367,
0.318505926345707,0.321437759703047,0.324369593060387,0.327301426417727,
0.330233259775067,0.331699176453737,0.332432134793072,0.33279861396274,
0.333165093132407,0.336096926489747,0.337562843168417,0.339028759847087,
0.341960593204427,0.343915148775987,0.345869704347547,0.347824259919107,
0.348373978673608,0.348648838050859,0.348923697428109,0.349473416182611,
0.350023134937112,0.351122572446114,0.352222009955117,0.354420884973122,
0.356619759991127,0.358818635009132,0.361017510027137,0.363216385045142,
0.365415260063147),.UNSPECIFIED.);
#314=B_SPLINE_SURFACE_WITH_KNOTS('',3,3,((#57977,#57978,#57979,#57980,#57981,
#57982,#57983,#57984,#57985,#57986,#57987,#57988,#57989,#57990,#57991,#57992,
#57993,#57994,#57995,#57996,#57997,#57998,#57999,#58000,#58001,#58002,#58003,
#58004,#58005,#58006,#58007,#58008,#58009,#58010,#58011,#58012,#58013,#58014,
#58015,#58016,#58017,#58018,#58019,#58020,#58021,#58022,#58023,#58024,#58025,
#58026,#58027,#58028,#58029,#58030,#58031,#58032,#58033,#58034,#58035,#58036,
#58037,#58038,#58039,#58040),(#58041,#58042,#58043,#58044,#58045,#58046,
#58047,#58048,#58049,#58050,#58051,#58052,#58053,#58054,#58055,#58056,#58057,
#58058,#58059,#58060,#58061,#58062,#58063,#58064,#58065,#58066,#58067,#58068,
#58069,#58070,#58071,#58072,#58073,#58074,#58075,#58076,#58077,#58078,#58079,
#58080,#58081,#58082,#58083,#58084,#58085,#58086,#58087,#58088,#58089,#58090,
#58091,#58092,#58093,#58094,#58095,#58096,#58097,#58098,#58099,#58100,#58101,
#58102,#58103,#58104),(#58105,#58106,#58107,#58108,#58109,#58110,#58111,
#58112,#58113,#58114,#58115,#58116,#58117,#58118,#58119,#58120,#58121,#58122,
#58123,#58124,#58125,#58126,#58127,#58128,#58129,#58130,#58131,#58132,#58133,
#58134,#58135,#58136,#58137,#58138,#58139,#58140,#58141,#58142,#58143,#58144,
#58145,#58146,#58147,#58148,#58149,#58150,#58151,#58152,#58153,#58154,#58155,
#58156,#58157,#58158,#58159,#58160,#58161,#58162,#58163,#58164,#58165,#58166,
#58167,#58168),(#58169,#58170,#58171,#58172,#58173,#58174,#58175,#58176,
#58177,#58178,#58179,#58180,#58181,#58182,#58183,#58184,#58185,#58186,#58187,
#58188,#58189,#58190,#58191,#58192,#58193,#58194,#58195,#58196,#58197,#58198,
#58199,#58200,#58201,#58202,#58203,#58204,#58205,#58206,#58207,#58208,#58209,
#58210,#58211,#58212,#58213,#58214,#58215,#58216,#58217,#58218,#58219,#58220,
#58221,#58222,#58223,#58224,#58225,#58226,#58227,#58228,#58229,#58230,#58231,
#58232)),.UNSPECIFIED.,.F.,.F.,.F.,(4,4),(4,1,1,1,1,1,1,1,1,1,1,1,1,1,1,
1,1,1,1,1,1,1,1,1,1,1,1,1,1,1,1,1,1,1,1,1,1,1,1,1,1,1,1,1,1,1,1,1,1,1,1,
1,1,1,1,1,1,1,1,1,1,4),(-0.000238498840641111,0.099639560690363),(0.410645887791668,
0.412844762664804,0.415043637537941,0.417242512411078,0.419441387284215,
0.421640262157351,0.423839137030488,0.426038011903625,0.428236886776761,
0.43019144221955,0.431168719940944,0.434100553105126,0.437032386269308,
0.439964219433491,0.442896052597673,0.445827885761855,0.448759718926038,
0.45169155209022,0.454623385254402,0.457555218418585,0.460487051582767,
0.463418884746949,0.465617759620086,0.467816634493223,0.470015509366359,
0.472214384239496,0.474413259112633,0.47661213398577,0.478811008858906,
0.481009883732043,0.48320875860518,0.485407633478317,0.487606508351453,
0.48980538322459,0.491271299806681,0.491454539379443,0.491637778952204,
0.492004258097727,0.492737216388773,0.494203132970864,0.495669049552955,
0.496402007844,0.497134966135046,0.497318205707807,0.497501445280569,0.497867924426092,
0.498600882717137,0.50153271588132,0.504464549045502,0.507396382209684,
0.510328215373866,0.512282770816655,0.514237326259443,0.516191881702231,
0.518390756575368,0.520589631448505,0.522788506321641,0.524987381194778,
0.527186256067915,0.529385130941052,0.531584005814188,0.533782880687325),
 .UNSPECIFIED.);
#315=B_SPLINE_SURFACE_WITH_KNOTS('',3,3,((#58270,#58271,#58272,#58273,#58274,
#58275,#58276,#58277,#58278,#58279,#58280,#58281,#58282,#58283,#58284,#58285,
#58286,#58287,#58288,#58289,#58290,#58291,#58292,#58293,#58294,#58295,#58296,
#58297,#58298,#58299,#58300,#58301,#58302,#58303,#58304,#58305,#58306,#58307,
#58308,#58309,#58310,#58311,#58312,#58313,#58314,#58315,#58316,#58317,#58318,
#58319,#58320,#58321,#58322,#58323,#58324,#58325,#58326,#58327,#58328,#58329,
#58330,#58331,#58332),(#58333,#58334,#58335,#58336,#58337,#58338,#58339,
#58340,#58341,#58342,#58343,#58344,#58345,#58346,#58347,#58348,#58349,#58350,
#58351,#58352,#58353,#58354,#58355,#58356,#58357,#58358,#58359,#58360,#58361,
#58362,#58363,#58364,#58365,#58366,#58367,#58368,#58369,#58370,#58371,#58372,
#58373,#58374,#58375,#58376,#58377,#58378,#58379,#58380,#58381,#58382,#58383,
#58384,#58385,#58386,#58387,#58388,#58389,#58390,#58391,#58392,#58393,#58394,
#58395),(#58396,#58397,#58398,#58399,#58400,#58401,#58402,#58403,#58404,
#58405,#58406,#58407,#58408,#58409,#58410,#58411,#58412,#58413,#58414,#58415,
#58416,#58417,#58418,#58419,#58420,#58421,#58422,#58423,#58424,#58425,#58426,
#58427,#58428,#58429,#58430,#58431,#58432,#58433,#58434,#58435,#58436,#58437,
#58438,#58439,#58440,#58441,#58442,#58443,#58444,#58445,#58446,#58447,#58448,
#58449,#58450,#58451,#58452,#58453,#58454,#58455,#58456,#58457,#58458),
(#58459,#58460,#58461,#58462,#58463,#58464,#58465,#58466,#58467,#58468,
#58469,#58470,#58471,#58472,#58473,#58474,#58475,#58476,#58477,#58478,#58479,
#58480,#58481,#58482,#58483,#58484,#58485,#58486,#58487,#58488,#58489,#58490,
#58491,#58492,#58493,#58494,#58495,#58496,#58497,#58498,#58499,#58500,#58501,
#58502,#58503,#58504,#58505,#58506,#58507,#58508,#58509,#58510,#58511,#58512,
#58513,#58514,#58515,#58516,#58517,#58518,#58519,#58520,#58521)),
 .UNSPECIFIED.,.F.,.F.,.F.,(4,4),(4,1,1,1,1,1,1,1,1,1,1,1,1,1,1,1,1,1,1,
1,1,1,1,1,1,1,1,1,1,1,1,1,1,1,1,1,1,1,1,1,1,1,1,1,1,1,1,1,1,1,1,1,1,1,1,
1,1,1,1,1,4),(-0.000257012103592972,0.0996242942258564),(0.579013511076644,
0.581212386019991,0.583411260963338,0.585610135906685,0.587809010850032,
0.590007885793379,0.592206760736727,0.594405635680074,0.596604510623421,
0.599536343881217,0.602468177139013,0.605400010396809,0.605949729132646,
0.607598885340156,0.609797760283503,0.61199663522685,0.614195510170197,
0.616394385113544,0.618593260056891,0.620792135000238,0.621891572471912,
0.622991009943585,0.625922843201381,0.627388759830279,0.629587634773626,
0.631786509716973,0.633985384660321,0.636184259603668,0.637650176232566,
0.640582009490362,0.642780884433709,0.644979759377056,0.647178634320403,
0.64937750926375,0.651576384207097,0.653775259150444,0.655974134093791,
0.658173009037138,0.659638925666036,0.660371883980485,0.661104842294934,
0.662570758923832,0.66403667555273,0.665502592181628,0.666235550496078,
0.666968508810526,0.669900342068322,0.672832175326119,0.675764008583915,
0.678695841841711,0.680650397346908,0.682604952852106,0.684559508357303,
0.68675838330065,0.688957258243997,0.691156133187344,0.693355008130691,
0.695553883074038,0.697752758017385,0.699951632960732,0.702150507904079),
 .UNSPECIFIED.);
#316=B_SPLINE_SURFACE_WITH_KNOTS('',3,3,((#58563,#58564,#58565,#58566,#58567,
#58568,#58569,#58570,#58571,#58572,#58573,#58574,#58575,#58576,#58577,#58578,
#58579,#58580,#58581,#58582,#58583,#58584,#58585,#58586,#58587,#58588,#58589,
#58590,#58591,#58592,#58593,#58594,#58595,#58596,#58597,#58598,#58599,#58600,
#58601,#58602,#58603,#58604,#58605,#58606,#58607,#58608,#58609,#58610,#58611,
#58612,#58613,#58614,#58615,#58616,#58617,#58618,#58619),(#58620,#58621,
#58622,#58623,#58624,#58625,#58626,#58627,#58628,#58629,#58630,#58631,#58632,
#58633,#58634,#58635,#58636,#58637,#58638,#58639,#58640,#58641,#58642,#58643,
#58644,#58645,#58646,#58647,#58648,#58649,#58650,#58651,#58652,#58653,#58654,
#58655,#58656,#58657,#58658,#58659,#58660,#58661,#58662,#58663,#58664,#58665,
#58666,#58667,#58668,#58669,#58670,#58671,#58672,#58673,#58674,#58675,#58676),
(#58677,#58678,#58679,#58680,#58681,#58682,#58683,#58684,#58685,#58686,
#58687,#58688,#58689,#58690,#58691,#58692,#58693,#58694,#58695,#58696,#58697,
#58698,#58699,#58700,#58701,#58702,#58703,#58704,#58705,#58706,#58707,#58708,
#58709,#58710,#58711,#58712,#58713,#58714,#58715,#58716,#58717,#58718,#58719,
#58720,#58721,#58722,#58723,#58724,#58725,#58726,#58727,#58728,#58729,#58730,
#58731,#58732,#58733),(#58734,#58735,#58736,#58737,#58738,#58739,#58740,
#58741,#58742,#58743,#58744,#58745,#58746,#58747,#58748,#58749,#58750,#58751,
#58752,#58753,#58754,#58755,#58756,#58757,#58758,#58759,#58760,#58761,#58762,
#58763,#58764,#58765,#58766,#58767,#58768,#58769,#58770,#58771,#58772,#58773,
#58774,#58775,#58776,#58777,#58778,#58779,#58780,#58781,#58782,#58783,#58784,
#58785,#58786,#58787,#58788,#58789,#58790)),.UNSPECIFIED.,.F.,.F.,.F.,(4,
4),(4,1,1,1,1,1,1,1,1,1,1,1,1,1,1,1,1,1,1,1,1,1,1,1,1,1,1,1,1,1,1,1,1,1,
1,1,1,1,1,1,1,1,1,1,1,1,1,1,1,1,1,1,1,1,4),(-0.000347032421316872,0.099675803785384),
(0.747330707309962,0.749580010757179,0.751778885415099,0.753977760073019,
0.756176634730939,0.758375509388859,0.760574384046779,0.762773258704699,
0.764972133362619,0.767903966239845,0.769369882678459,0.770835799117072,
0.773767631994299,0.776699464871526,0.779631297748752,0.782563130625979,
0.784762005283899,0.786960879941819,0.789159754599739,0.791358629257659,
0.793557503915579,0.795756378573499,0.797955253231419,0.800154127889339,
0.802353002547259,0.804551877205179,0.806750751863099,0.808949626521019,
0.811148501178939,0.813347375836859,0.815546250494779,0.817745125152699,
0.819943999810619,0.822142874468539,0.823608790907153,0.826540623784379,
0.828739498442299,0.830938373100219,0.833137247758139,0.835336122416059,
0.837534997073979,0.8397338717319,0.84193274638982,0.84413162104774,0.847063453924966,
0.849995286802193,0.85292711967942,0.85512599433734,0.85732486899526,0.85952374365318,
0.8617226183111,0.86392149296902,0.86612036762694,0.86831924228486,0.87051811694278),
 .UNSPECIFIED.);
#317=B_SPLINE_SURFACE_WITH_KNOTS('',3,3,((#60620,#60621,#60622,#60623,#60624,
#60625,#60626,#60627,#60628,#60629,#60630,#60631,#60632,#60633,#60634,#60635,
#60636,#60637,#60638,#60639,#60640,#60641,#60642,#60643,#60644,#60645,#60646,
#60647,#60648,#60649,#60650,#60651,#60652,#60653,#60654,#60655,#60656,#60657,
#60658,#60659,#60660,#60661,#60662,#60663,#60664,#60665,#60666,#60667,#60668,
#60669,#60670,#60671,#60672,#60673,#60674,#60675,#60676,#60677,#60678,#60679,
#60680,#60681,#60682,#60683,#60684,#60685,#60686,#60687,#60688,#60689,#60690,
#60691,#60692,#60693,#60694,#60695,#60696,#60697,#60698,#60699,#60700,#60701,
#60702),(#60703,#60704,#60705,#60706,#60707,#60708,#60709,#60710,#60711,
#60712,#60713,#60714,#60715,#60716,#60717,#60718,#60719,#60720,#60721,#60722,
#60723,#60724,#60725,#60726,#60727,#60728,#60729,#60730,#60731,#60732,#60733,
#60734,#60735,#60736,#60737,#60738,#60739,#60740,#60741,#60742,#60743,#60744,
#60745,#60746,#60747,#60748,#60749,#60750,#60751,#60752,#60753,#60754,#60755,
#60756,#60757,#60758,#60759,#60760,#60761,#60762,#60763,#60764,#60765,#60766,
#60767,#60768,#60769,#60770,#60771,#60772,#60773,#60774,#60775,#60776,#60777,
#60778,#60779,#60780,#60781,#60782,#60783,#60784,#60785),(#60786,#60787,
#60788,#60789,#60790,#60791,#60792,#60793,#60794,#60795,#60796,#60797,#60798,
#60799,#60800,#60801,#60802,#60803,#60804,#60805,#60806,#60807,#60808,#60809,
#60810,#60811,#60812,#60813,#60814,#60815,#60816,#60817,#60818,#60819,#60820,
#60821,#60822,#60823,#60824,#60825,#60826,#60827,#60828,#60829,#60830,#60831,
#60832,#60833,#60834,#60835,#60836,#60837,#60838,#60839,#60840,#60841,#60842,
#60843,#60844,#60845,#60846,#60847,#60848,#60849,#60850,#60851,#60852,#60853,
#60854,#60855,#60856,#60857,#60858,#60859,#60860,#60861,#60862,#60863,#60864,
#60865,#60866,#60867,#60868),(#60869,#60870,#60871,#60872,#60873,#60874,
#60875,#60876,#60877,#60878,#60879,#60880,#60881,#60882,#60883,#60884,#60885,
#60886,#60887,#60888,#60889,#60890,#60891,#60892,#60893,#60894,#60895,#60896,
#60897,#60898,#60899,#60900,#60901,#60902,#60903,#60904,#60905,#60906,#60907,
#60908,#60909,#60910,#60911,#60912,#60913,#60914,#60915,#60916,#60917,#60918,
#60919,#60920,#60921,#60922,#60923,#60924,#60925,#60926,#60927,#60928,#60929,
#60930,#60931,#60932,#60933,#60934,#60935,#60936,#60937,#60938,#60939,#60940,
#60941,#60942,#60943,#60944,#60945,#60946,#60947,#60948,#60949,#60950,#60951)),
 .UNSPECIFIED.,.F.,.F.,.F.,(4,4),(4,1,1,1,1,1,1,1,1,1,1,1,1,1,1,1,1,1,1,
1,1,1,1,1,1,1,1,1,1,1,1,1,1,1,1,1,1,1,1,1,1,1,1,1,1,1,1,1,1,1,1,1,1,1,1,
1,1,1,1,1,1,1,1,1,1,1,1,1,1,1,1,1,1,1,1,1,1,1,1,1,4),(-0.000191727474006969,
0.120034558936103),(0.0144970658303938,0.0170193973464053,0.0195077183395957,
0.021996039332786,0.0244843603259764,0.0269726813191668,0.0294610023123572,
0.0319493233055476,0.034437644298738,0.0366494851815739,0.0388613260644098,
0.0410731669472457,0.0427320476093726,0.0443909282714996,0.0460498089336265,
0.0477086895957534,0.0493675702578804,0.0510264509200073,0.0526853315821342,
0.0535147719131977,0.0543442122442611,0.0560030929063881,0.057661973568515,
0.0593208542306419,0.0605650147272371,0.0609797348927689,0.0626386155548958,
0.0642974962170227,0.0659563768791496,0.0676152575412766,0.0680299777068083,
0.06844469787234,0.0692741382034035,0.0709330188655304,0.0725918995276573,
0.0742507801897843,0.0759096608519112,0.0775685415140381,0.0792274221761651,
0.080886302838292,0.0825451835004189,0.0842040641625458,0.0858629448246728,
0.0875218254867997,0.0891807061489266,0.0908395868110536,0.0924984674731805,
0.0941573481353074,0.0958162287974343,0.0974751094595613,0.0991339901216882,
0.100792870783815,0.102451751445942,0.104110632108069,0.105769512770196,
0.107428393432323,0.109640234315159,0.111852075197995,0.114063916080831,
0.114893356411894,0.115722796742957,0.117381677405084,0.119040558067211,
0.120699438729338,0.122358319391465,0.124017200053592,0.125676080715719,
0.127334961377846,0.128440881819264,0.129546802260682,0.131758643143518,
0.132864563584936,0.133970484026354,0.136458805019544,0.138947126012734,
0.141435447005925,0.143923767999115,0.146412088992306,0.148900409985496,
0.151388730978686,0.154068779445884),.UNSPECIFIED.);
#318=B_SPLINE_SURFACE_WITH_KNOTS('',3,3,((#61850,#61851,#61852,#61853,#61854,
#61855,#61856,#61857,#61858,#61859,#61860,#61861,#61862,#61863,#61864,#61865,
#61866,#61867,#61868,#61869,#61870,#61871,#61872,#61873,#61874,#61875,#61876,
#61877,#61878,#61879,#61880,#61881,#61882,#61883,#61884,#61885,#61886,#61887,
#61888,#61889,#61890,#61891,#61892,#61893,#61894,#61895,#61896,#61897,#61898,
#61899,#61900,#61901,#61902,#61903,#61904,#61905,#61906,#61907,#61908,#61909,
#61910,#61911,#61912,#61913,#61914,#61915,#61916,#61917,#61918,#61919,#61920,
#61921,#61922,#61923,#61924,#61925,#61926,#61927,#61928,#61929,#61930,#61931,
#61932,#61933,#61934,#61935,#61936,#61937,#61938),(#61939,#61940,#61941,
#61942,#61943,#61944,#61945,#61946,#61947,#61948,#61949,#61950,#61951,#61952,
#61953,#61954,#61955,#61956,#61957,#61958,#61959,#61960,#61961,#61962,#61963,
#61964,#61965,#61966,#61967,#61968,#61969,#61970,#61971,#61972,#61973,#61974,
#61975,#61976,#61977,#61978,#61979,#61980,#61981,#61982,#61983,#61984,#61985,
#61986,#61987,#61988,#61989,#61990,#61991,#61992,#61993,#61994,#61995,#61996,
#61997,#61998,#61999,#62000,#62001,#62002,#62003,#62004,#62005,#62006,#62007,
#62008,#62009,#62010,#62011,#62012,#62013,#62014,#62015,#62016,#62017,#62018,
#62019,#62020,#62021,#62022,#62023,#62024,#62025,#62026,#62027),(#62028,
#62029,#62030,#62031,#62032,#62033,#62034,#62035,#62036,#62037,#62038,#62039,
#62040,#62041,#62042,#62043,#62044,#62045,#62046,#62047,#62048,#62049,#62050,
#62051,#62052,#62053,#62054,#62055,#62056,#62057,#62058,#62059,#62060,#62061,
#62062,#62063,#62064,#62065,#62066,#62067,#62068,#62069,#62070,#62071,#62072,
#62073,#62074,#62075,#62076,#62077,#62078,#62079,#62080,#62081,#62082,#62083,
#62084,#62085,#62086,#62087,#62088,#62089,#62090,#62091,#62092,#62093,#62094,
#62095,#62096,#62097,#62098,#62099,#62100,#62101,#62102,#62103,#62104,#62105,
#62106,#62107,#62108,#62109,#62110,#62111,#62112,#62113,#62114,#62115,#62116),
(#62117,#62118,#62119,#62120,#62121,#62122,#62123,#62124,#62125,#62126,
#62127,#62128,#62129,#62130,#62131,#62132,#62133,#62134,#62135,#62136,#62137,
#62138,#62139,#62140,#62141,#62142,#62143,#62144,#62145,#62146,#62147,#62148,
#62149,#62150,#62151,#62152,#62153,#62154,#62155,#62156,#62157,#62158,#62159,
#62160,#62161,#62162,#62163,#62164,#62165,#62166,#62167,#62168,#62169,#62170,
#62171,#62172,#62173,#62174,#62175,#62176,#62177,#62178,#62179,#62180,#62181,
#62182,#62183,#62184,#62185,#62186,#62187,#62188,#62189,#62190,#62191,#62192,
#62193,#62194,#62195,#62196,#62197,#62198,#62199,#62200,#62201,#62202,#62203,
#62204,#62205)),.UNSPECIFIED.,.F.,.F.,.F.,(4,4),(4,1,1,1,1,1,1,1,1,1,1,
1,1,1,1,1,1,1,1,1,1,1,1,1,1,1,1,1,1,1,1,1,1,1,1,1,1,1,1,1,1,1,1,1,1,1,1,
1,1,1,1,1,1,1,1,1,1,1,1,1,1,1,1,1,1,1,1,1,1,1,1,1,1,1,1,1,1,1,1,1,1,1,1,
1,1,1,4),(-0.000343847952555671,0.120053031443545),(0.18284601578435,0.185387336016129,
0.187875651349888,0.190363966683647,0.192852282017407,0.194096439684286,
0.195340597351166,0.196584755018045,0.197828912684925,0.200317228018684,
0.201561385685564,0.202805543352443,0.204464420241616,0.206123297130789,
0.207782174019962,0.209441050909135,0.211099927798308,0.21275880468748,
0.214417681576653,0.21524712002124,0.215869198854679,0.216076558465826,
0.217735435354999,0.219394312244172,0.221053189133344,0.222712066022517,
0.22437094291169,0.226029819800863,0.227135737726978,0.229347573579209,
0.229900532542266,0.230453491505324,0.231559409431439,0.233771245283669,
0.2359830811359,0.237641958025073,0.239300834914246,0.240959711803418,0.242618588692591,
0.244277465581764,0.245936342470937,0.24759521936011,0.249254096249282,
0.250912973138455,0.252571850027628,0.254230726916801,0.255889603805974,
0.258101439658204,0.260313275510435,0.262525111362665,0.26363102928878,
0.264736947214895,0.266948783067126,0.269160618919356,0.270819495808529,
0.272478372697702,0.274966688031461,0.275796126476048,0.27745500336522,
0.279113880254393,0.280772757143566,0.282431634032739,0.284090510921912,
0.285749387811084,0.286578826255671,0.287408264700257,0.288237703144844,
0.28906714158943,0.291140737700896,0.292384895367776,0.294043772256949,
0.295702649146121,0.297914484998352,0.300126320850582,0.30067927981364,
0.302338156702813,0.302960235536253,0.303582314369692,0.304826472036572,
0.307314787370331,0.308558945037211,0.30980310270409,0.31229141803785,0.314779733371609,
0.317268048705368,0.319756364039127,0.322588480100517),.UNSPECIFIED.);
#319=B_SPLINE_SURFACE_WITH_KNOTS('',3,3,((#63143,#63144,#63145,#63146,#63147,
#63148,#63149,#63150,#63151,#63152,#63153,#63154,#63155,#63156,#63157,#63158,
#63159,#63160,#63161,#63162,#63163,#63164,#63165,#63166,#63167,#63168,#63169,
#63170,#63171,#63172,#63173,#63174,#63175,#63176,#63177,#63178,#63179,#63180,
#63181,#63182,#63183,#63184,#63185,#63186,#63187,#63188,#63189,#63190,#63191,
#63192,#63193,#63194,#63195,#63196,#63197,#63198,#63199,#63200,#63201,#63202,
#63203,#63204,#63205,#63206,#63207,#63208,#63209,#63210,#63211,#63212,#63213,
#63214,#63215,#63216,#63217,#63218,#63219,#63220,#63221,#63222,#63223,#63224,
#63225,#63226),(#63227,#63228,#63229,#63230,#63231,#63232,#63233,#63234,
#63235,#63236,#63237,#63238,#63239,#63240,#63241,#63242,#63243,#63244,#63245,
#63246,#63247,#63248,#63249,#63250,#63251,#63252,#63253,#63254,#63255,#63256,
#63257,#63258,#63259,#63260,#63261,#63262,#63263,#63264,#63265,#63266,#63267,
#63268,#63269,#63270,#63271,#63272,#63273,#63274,#63275,#63276,#63277,#63278,
#63279,#63280,#63281,#63282,#63283,#63284,#63285,#63286,#63287,#63288,#63289,
#63290,#63291,#63292,#63293,#63294,#63295,#63296,#63297,#63298,#63299,#63300,
#63301,#63302,#63303,#63304,#63305,#63306,#63307,#63308,#63309,#63310),
(#63311,#63312,#63313,#63314,#63315,#63316,#63317,#63318,#63319,#63320,
#63321,#63322,#63323,#63324,#63325,#63326,#63327,#63328,#63329,#63330,#63331,
#63332,#63333,#63334,#63335,#63336,#63337,#63338,#63339,#63340,#63341,#63342,
#63343,#63344,#63345,#63346,#63347,#63348,#63349,#63350,#63351,#63352,#63353,
#63354,#63355,#63356,#63357,#63358,#63359,#63360,#63361,#63362,#63363,#63364,
#63365,#63366,#63367,#63368,#63369,#63370,#63371,#63372,#63373,#63374,#63375,
#63376,#63377,#63378,#63379,#63380,#63381,#63382,#63383,#63384,#63385,#63386,
#63387,#63388,#63389,#63390,#63391,#63392,#63393,#63394),(#63395,#63396,
#63397,#63398,#63399,#63400,#63401,#63402,#63403,#63404,#63405,#63406,#63407,
#63408,#63409,#63410,#63411,#63412,#63413,#63414,#63415,#63416,#63417,#63418,
#63419,#63420,#63421,#63422,#63423,#63424,#63425,#63426,#63427,#63428,#63429,
#63430,#63431,#63432,#63433,#63434,#63435,#63436,#63437,#63438,#63439,#63440,
#63441,#63442,#63443,#63444,#63445,#63446,#63447,#63448,#63449,#63450,#63451,
#63452,#63453,#63454,#63455,#63456,#63457,#63458,#63459,#63460,#63461,#63462,
#63463,#63464,#63465,#63466,#63467,#63468,#63469,#63470,#63471,#63472,#63473,
#63474,#63475,#63476,#63477,#63478)),.UNSPECIFIED.,.F.,.F.,.F.,(4,4),(4,
1,1,1,1,1,1,1,1,1,1,1,1,1,1,1,1,1,1,1,1,1,1,1,1,1,1,1,1,1,1,1,1,1,1,1,1,
1,1,1,1,1,1,1,1,1,1,1,1,1,1,1,1,1,1,1,1,1,1,1,1,1,1,1,1,1,1,1,1,1,1,1,1,
1,1,1,1,1,1,1,1,4),(-0.000608094264401172,0.120053332327022),(0.35121353206522,
0.353754974599999,0.356243289735703,0.358731604871407,0.361219920007111,
0.363708235142815,0.364952392710666,0.366196550278518,0.368684865414222,
0.369929022982074,0.371173180549926,0.372832057307062,0.374490934064198,
0.376149810821334,0.37780868757847,0.379467564335606,0.381126441092742,
0.382785317849878,0.384444194607014,0.385273632985582,0.38610307136415,
0.387761948121286,0.389420824878422,0.391079701635558,0.392738578392693,
0.394397455149829,0.396056331906965,0.397715208664101,0.398821126502192,
0.399927044340283,0.402138880016464,0.404350715692645,0.406009592449781,
0.407668469206917,0.409327345964053,0.410986222721189,0.412645099478325,
0.414303976235461,0.415133414614029,0.415962852992597,0.416792291371165,
0.417621729749733,0.419280606506868,0.420939483264004,0.42259836002114,
0.424257236778276,0.426469072454458,0.428680908130639,0.43089274380682,
0.433104579483001,0.435316415159183,0.436422332997273,0.437528250835364,
0.4391871275925,0.440846004349636,0.442504881106772,0.444163757863908,0.445822634621044,
0.447481511378179,0.447896230567463,0.449140388135315,0.450799264892451,
0.452458141649587,0.454117018406723,0.455775895163859,0.457434771920995,
0.459093648678131,0.460752525435267,0.462411402192403,0.464070278949539,
0.46628211462572,0.468493950301901,0.470705785978083,0.471949943545935,
0.473194101113787,0.47568241624949,0.478170731385194,0.480659046520898,
0.483147361656602,0.485635676792306,0.48812399192801,0.491010307170531),
 .UNSPECIFIED.);
#320=B_SPLINE_SURFACE_WITH_KNOTS('',3,3,((#64056,#64057,#64058,#64059,#64060,
#64061,#64062,#64063,#64064,#64065,#64066,#64067,#64068,#64069,#64070,#64071,
#64072,#64073,#64074,#64075,#64076,#64077,#64078,#64079,#64080,#64081,#64082,
#64083,#64084,#64085,#64086,#64087,#64088,#64089,#64090,#64091,#64092,#64093,
#64094,#64095,#64096,#64097,#64098,#64099,#64100,#64101,#64102,#64103,#64104,
#64105,#64106,#64107,#64108,#64109,#64110,#64111,#64112,#64113,#64114,#64115,
#64116,#64117,#64118,#64119,#64120,#64121,#64122,#64123,#64124,#64125,#64126,
#64127,#64128,#64129,#64130,#64131,#64132,#64133,#64134,#64135,#64136,#64137,
#64138,#64139,#64140,#64141),(#64142,#64143,#64144,#64145,#64146,#64147,
#64148,#64149,#64150,#64151,#64152,#64153,#64154,#64155,#64156,#64157,#64158,
#64159,#64160,#64161,#64162,#64163,#64164,#64165,#64166,#64167,#64168,#64169,
#64170,#64171,#64172,#64173,#64174,#64175,#64176,#64177,#64178,#64179,#64180,
#64181,#64182,#64183,#64184,#64185,#64186,#64187,#64188,#64189,#64190,#64191,
#64192,#64193,#64194,#64195,#64196,#64197,#64198,#64199,#64200,#64201,#64202,
#64203,#64204,#64205,#64206,#64207,#64208,#64209,#64210,#64211,#64212,#64213,
#64214,#64215,#64216,#64217,#64218,#64219,#64220,#64221,#64222,#64223,#64224,
#64225,#64226,#64227),(#64228,#64229,#64230,#64231,#64232,#64233,#64234,
#64235,#64236,#64237,#64238,#64239,#64240,#64241,#64242,#64243,#64244,#64245,
#64246,#64247,#64248,#64249,#64250,#64251,#64252,#64253,#64254,#64255,#64256,
#64257,#64258,#64259,#64260,#64261,#64262,#64263,#64264,#64265,#64266,#64267,
#64268,#64269,#64270,#64271,#64272,#64273,#64274,#64275,#64276,#64277,#64278,
#64279,#64280,#64281,#64282,#64283,#64284,#64285,#64286,#64287,#64288,#64289,
#64290,#64291,#64292,#64293,#64294,#64295,#64296,#64297,#64298,#64299,#64300,
#64301,#64302,#64303,#64304,#64305,#64306,#64307,#64308,#64309,#64310,#64311,
#64312,#64313),(#64314,#64315,#64316,#64317,#64318,#64319,#64320,#64321,
#64322,#64323,#64324,#64325,#64326,#64327,#64328,#64329,#64330,#64331,#64332,
#64333,#64334,#64335,#64336,#64337,#64338,#64339,#64340,#64341,#64342,#64343,
#64344,#64345,#64346,#64347,#64348,#64349,#64350,#64351,#64352,#64353,#64354,
#64355,#64356,#64357,#64358,#64359,#64360,#64361,#64362,#64363,#64364,#64365,
#64366,#64367,#64368,#64369,#64370,#64371,#64372,#64373,#64374,#64375,#64376,
#64377,#64378,#64379,#64380,#64381,#64382,#64383,#64384,#64385,#64386,#64387,
#64388,#64389,#64390,#64391,#64392,#64393,#64394,#64395,#64396,#64397,#64398,
#64399)),.UNSPECIFIED.,.F.,.F.,.F.,(4,4),(4,1,1,1,1,1,1,1,1,1,1,1,1,1,1,
1,1,1,1,1,1,1,1,1,1,1,1,1,1,1,1,1,1,1,1,1,1,1,1,1,1,1,1,1,1,1,1,1,1,1,1,
1,1,1,1,1,1,1,1,1,1,1,1,1,1,1,1,1,1,1,1,1,1,1,1,1,1,1,1,1,1,1,1,4),(-0.0004813933155718,
0.120112165916443),(0.519522122356523,0.522122603429753,0.524610918586542,
0.527099233743331,0.52958754890012,0.532075864056908,0.534564179213697,
0.537052494370486,0.539540809527275,0.541199686298467,0.54285856306966,
0.544517439840852,0.546176316612045,0.547835193383237,0.548664631768834,
0.54949407015443,0.551152946925622,0.551982385311219,0.552397104504017,
0.552604464100416,0.552811823696815,0.5561295772392,0.559447330781585,0.561106207552778,
0.56276508432397,0.566082837866355,0.566290197462754,0.566497557059153,
0.566912276251951,0.567741714637548,0.568571153023144,0.56940059140874,
0.571059468179933,0.572718344951125,0.574377221722318,0.57603609849351,
0.577694975264703,0.579353852035895,0.581012728807088,0.58267160557828,
0.584330482349473,0.585989359120665,0.587648235891858,0.58930711266305,
0.590965989434243,0.592624866205435,0.594836701900359,0.597048537595282,
0.599260373290205,0.600366291137667,0.600919250061398,0.601472208985129,
0.604789962527514,0.605895880374975,0.607554757146168,0.60921363391736,
0.610872510688553,0.612531387459745,0.614190264230938,0.615849141002131,
0.616263860194929,0.616678579387727,0.617508017773323,0.619166894544516,
0.620825771315708,0.622484648086901,0.624143524858093,0.625802401629286,
0.627461278400478,0.629120155171671,0.630779031942863,0.632437908714056,
0.634649744408979,0.636861580103902,0.639073415798826,0.64031757337722,
0.641561730955615,0.644050046112403,0.646538361269192,0.649026676425981,
0.65151499158277,0.654003306739558,0.656491621896347,0.659296609515059),
 .UNSPECIFIED.);
#321=B_SPLINE_SURFACE_WITH_KNOTS('',3,3,((#65370,#65371,#65372,#65373,#65374,
#65375,#65376,#65377,#65378,#65379,#65380,#65381,#65382,#65383,#65384,#65385,
#65386,#65387,#65388,#65389,#65390,#65391,#65392,#65393,#65394,#65395,#65396,
#65397,#65398,#65399,#65400,#65401,#65402,#65403,#65404,#65405,#65406,#65407,
#65408,#65409,#65410,#65411,#65412,#65413,#65414,#65415,#65416,#65417,#65418,
#65419,#65420,#65421,#65422,#65423,#65424,#65425,#65426,#65427,#65428,#65429,
#65430,#65431,#65432,#65433,#65434,#65435,#65436,#65437,#65438,#65439,#65440,
#65441,#65442,#65443,#65444,#65445,#65446,#65447,#65448,#65449,#65450,#65451,
#65452,#65453,#65454,#65455,#65456,#65457,#65458,#65459,#65460),(#65461,
#65462,#65463,#65464,#65465,#65466,#65467,#65468,#65469,#65470,#65471,#65472,
#65473,#65474,#65475,#65476,#65477,#65478,#65479,#65480,#65481,#65482,#65483,
#65484,#65485,#65486,#65487,#65488,#65489,#65490,#65491,#65492,#65493,#65494,
#65495,#65496,#65497,#65498,#65499,#65500,#65501,#65502,#65503,#65504,#65505,
#65506,#65507,#65508,#65509,#65510,#65511,#65512,#65513,#65514,#65515,#65516,
#65517,#65518,#65519,#65520,#65521,#65522,#65523,#65524,#65525,#65526,#65527,
#65528,#65529,#65530,#65531,#65532,#65533,#65534,#65535,#65536,#65537,#65538,
#65539,#65540,#65541,#65542,#65543,#65544,#65545,#65546,#65547,#65548,#65549,
#65550,#65551),(#65552,#65553,#65554,#65555,#65556,#65557,#65558,#65559,
#65560,#65561,#65562,#65563,#65564,#65565,#65566,#65567,#65568,#65569,#65570,
#65571,#65572,#65573,#65574,#65575,#65576,#65577,#65578,#65579,#65580,#65581,
#65582,#65583,#65584,#65585,#65586,#65587,#65588,#65589,#65590,#65591,#65592,
#65593,#65594,#65595,#65596,#65597,#65598,#65599,#65600,#65601,#65602,#65603,
#65604,#65605,#65606,#65607,#65608,#65609,#65610,#65611,#65612,#65613,#65614,
#65615,#65616,#65617,#65618,#65619,#65620,#65621,#65622,#65623,#65624,#65625,
#65626,#65627,#65628,#65629,#65630,#65631,#65632,#65633,#65634,#65635,#65636,
#65637,#65638,#65639,#65640,#65641,#65642),(#65643,#65644,#65645,#65646,
#65647,#65648,#65649,#65650,#65651,#65652,#65653,#65654,#65655,#65656,#65657,
#65658,#65659,#65660,#65661,#65662,#65663,#65664,#65665,#65666,#65667,#65668,
#65669,#65670,#65671,#65672,#65673,#65674,#65675,#65676,#65677,#65678,#65679,
#65680,#65681,#65682,#65683,#65684,#65685,#65686,#65687,#65688,#65689,#65690,
#65691,#65692,#65693,#65694,#65695,#65696,#65697,#65698,#65699,#65700,#65701,
#65702,#65703,#65704,#65705,#65706,#65707,#65708,#65709,#65710,#65711,#65712,
#65713,#65714,#65715,#65716,#65717,#65718,#65719,#65720,#65721,#65722,#65723,
#65724,#65725,#65726,#65727,#65728,#65729,#65730,#65731,#65732,#65733)),
 .UNSPECIFIED.,.F.,.F.,.F.,(4,4),(4,1,1,1,1,1,1,1,1,1,1,1,1,1,1,1,1,1,1,
1,1,1,1,1,1,1,1,1,1,1,1,1,1,1,1,1,1,1,1,1,1,1,1,1,1,1,1,1,1,1,1,1,1,1,1,
1,1,1,1,1,1,1,1,1,1,1,1,1,1,1,1,1,1,1,1,1,1,1,1,1,1,1,1,1,1,1,1,1,4),(-0.000337432449522167,
0.120000000000001),(0.688001912782254,0.690490227769403,0.692978542756553,
0.695466857743702,0.697955172730851,0.700443487718,0.702931802705149,0.705420117692299,
0.707908432679448,0.710120268223581,0.712332103767713,0.714543939311846,
0.716202815969945,0.717861692628045,0.719520569286144,0.721179445944244,
0.722838322602343,0.724497199260443,0.726156075918542,0.727814952576642,
0.729473829234741,0.731132705892841,0.73279158255094,0.73445045920904,0.736109335867139,
0.737768212525239,0.739427089183338,0.741085965841438,0.742191883613504,
0.74329780138557,0.745509636929703,0.747721472473835,0.749933308017968,
0.752145143562101,0.753251061334167,0.7538040202202,0.754080499663217,0.754356979106233,
0.757674732422432,0.759333609080532,0.760992485738631,0.761407204903156,
0.761821924067681,0.762651362396731,0.763480800725781,0.76431023905483,
0.76513967738388,0.76596911571293,0.766798554041979,0.767627992371029,0.769286869029129,
0.770945745687228,0.772604622345328,0.774263499003427,0.775922375661527,
0.777581252319626,0.779240128977726,0.780899005635825,0.783110841179958,
0.78532267672409,0.787534512268223,0.789193388926323,0.790852265584422,
0.792511142242522,0.794170018900621,0.79582889555872,0.79748777221682,0.798731929710395,
0.800805525533019,0.802464402191118,0.804123278849218,0.804537998013743,
0.805782155507317,0.807441032165417,0.808063110912204,0.808685189658991,
0.809929347152566,0.811173504646141,0.812417662139715,0.814905977126865,
0.817394292114014,0.817705331487407,0.818638449607588,0.819882607101163,
0.821126764594738,0.822370922088312,0.8229930008351,0.824859237075461,0.827347552062611),
 .UNSPECIFIED.);
#322=B_SPLINE_SURFACE_WITH_KNOTS('',3,3,((#65787,#65788,#65789,#65790,#65791,
#65792,#65793,#65794,#65795,#65796,#65797),(#65798,#65799,#65800,#65801,
#65802,#65803,#65804,#65805,#65806,#65807,#65808),(#65809,#65810,#65811,
#65812,#65813,#65814,#65815,#65816,#65817,#65818,#65819),(#65820,#65821,
#65822,#65823,#65824,#65825,#65826,#65827,#65828,#65829,#65830)),
 .UNSPECIFIED.,.F.,.F.,.F.,(4,4),(4,1,1,1,1,1,1,1,4),(0.05527911728358,
0.0996900551293098),(0.981477459445449,0.984165788573041,0.986804823810868,
0.989443859048694,0.992082894286521,0.994721929524347,0.997360964762174,
0.998680482381087,1.00004977012262),.UNSPECIFIED.);
#323=B_SPLINE_SURFACE_WITH_KNOTS('',3,3,((#65831,#65832,#65833,#65834,#65835,
#65836,#65837,#65838,#65839,#65840,#65841,#65842,#65843,#65844,#65845,#65846,
#65847,#65848,#65849,#65850,#65851,#65852,#65853,#65854,#65855,#65856,#65857,
#65858,#65859,#65860,#65861,#65862,#65863,#65864,#65865,#65866,#65867,#65868,
#65869,#65870,#65871,#65872,#65873,#65874,#65875,#65876),(#65877,#65878,
#65879,#65880,#65881,#65882,#65883,#65884,#65885,#65886,#65887,#65888,#65889,
#65890,#65891,#65892,#65893,#65894,#65895,#65896,#65897,#65898,#65899,#65900,
#65901,#65902,#65903,#65904,#65905,#65906,#65907,#65908,#65909,#65910,#65911,
#65912,#65913,#65914,#65915,#65916,#65917,#65918,#65919,#65920,#65921,#65922),
(#65923,#65924,#65925,#65926,#65927,#65928,#65929,#65930,#65931,#65932,
#65933,#65934,#65935,#65936,#65937,#65938,#65939,#65940,#65941,#65942,#65943,
#65944,#65945,#65946,#65947,#65948,#65949,#65950,#65951,#65952,#65953,#65954,
#65955,#65956,#65957,#65958,#65959,#65960,#65961,#65962,#65963,#65964,#65965,
#65966,#65967,#65968),(#65969,#65970,#65971,#65972,#65973,#65974,#65975,
#65976,#65977,#65978,#65979,#65980,#65981,#65982,#65983,#65984,#65985,#65986,
#65987,#65988,#65989,#65990,#65991,#65992,#65993,#65994,#65995,#65996,#65997,
#65998,#65999,#66000,#66001,#66002,#66003,#66004,#66005,#66006,#66007,#66008,
#66009,#66010,#66011,#66012,#66013,#66014)),.UNSPECIFIED.,.F.,.F.,.F.,(4,
4),(4,1,1,1,1,1,1,1,1,1,1,1,1,1,1,1,1,1,1,1,1,1,1,1,1,1,1,1,1,1,1,1,1,1,
1,1,1,1,1,1,1,1,1,4),(-0.000533053460610251,0.0996242942258564),(0.,0.00168771915268776,
0.00337543830537552,0.00675087661075104,0.0101263149161266,0.0135017532215021,
0.0157520454250858,0.0180023376286695,0.0202526298322531,0.0219403489849409,
0.0236280681376287,0.0253157872903164,0.0270035064430042,0.0292537986465879,
0.0315040908501715,0.0337543830537552,0.0360046752573389,0.0382549674609226,
0.0405052596645063,0.0427555518680899,0.0450058440716736,0.0472561362752573,
0.049506428478841,0.0517567206824247,0.0540070128860084,0.0556947320386961,
0.0573824511913839,0.0590701703440716,0.0607578894967594,0.0641333278021349,
0.0658210469548227,0.0675087661075104,0.0691964852601982,0.070884204412886,
0.0725719235655737,0.0742596427182615,0.0765099349218452,0.0787602271254289,
0.0810105193290125,0.0843859576343881,0.0877613959397636,0.0911368342451391,
0.0928245533978269,0.0945122725505146),.UNSPECIFIED.);
#324=B_SPLINE_SURFACE_WITH_KNOTS('',3,3,((#66016,#66017,#66018,#66019,#66020,
#66021,#66022,#66023,#66024,#66025,#66026,#66027,#66028,#66029,#66030,#66031,
#66032,#66033,#66034,#66035,#66036,#66037,#66038,#66039,#66040,#66041,#66042,
#66043,#66044,#66045,#66046,#66047,#66048,#66049,#66050,#66051,#66052,#66053,
#66054,#66055,#66056,#66057,#66058,#66059,#66060,#66061,#66062,#66063,#66064,
#66065,#66066,#66067,#66068,#66069,#66070,#66071,#66072,#66073,#66074,#66075,
#66076,#66077,#66078),(#66079,#66080,#66081,#66082,#66083,#66084,#66085,
#66086,#66087,#66088,#66089,#66090,#66091,#66092,#66093,#66094,#66095,#66096,
#66097,#66098,#66099,#66100,#66101,#66102,#66103,#66104,#66105,#66106,#66107,
#66108,#66109,#66110,#66111,#66112,#66113,#66114,#66115,#66116,#66117,#66118,
#66119,#66120,#66121,#66122,#66123,#66124,#66125,#66126,#66127,#66128,#66129,
#66130,#66131,#66132,#66133,#66134,#66135,#66136,#66137,#66138,#66139,#66140,
#66141),(#66142,#66143,#66144,#66145,#66146,#66147,#66148,#66149,#66150,
#66151,#66152,#66153,#66154,#66155,#66156,#66157,#66158,#66159,#66160,#66161,
#66162,#66163,#66164,#66165,#66166,#66167,#66168,#66169,#66170,#66171,#66172,
#66173,#66174,#66175,#66176,#66177,#66178,#66179,#66180,#66181,#66182,#66183,
#66184,#66185,#66186,#66187,#66188,#66189,#66190,#66191,#66192,#66193,#66194,
#66195,#66196,#66197,#66198,#66199,#66200,#66201,#66202,#66203,#66204),
(#66205,#66206,#66207,#66208,#66209,#66210,#66211,#66212,#66213,#66214,
#66215,#66216,#66217,#66218,#66219,#66220,#66221,#66222,#66223,#66224,#66225,
#66226,#66227,#66228,#66229,#66230,#66231,#66232,#66233,#66234,#66235,#66236,
#66237,#66238,#66239,#66240,#66241,#66242,#66243,#66244,#66245,#66246,#66247,
#66248,#66249,#66250,#66251,#66252,#66253,#66254,#66255,#66256,#66257,#66258,
#66259,#66260,#66261,#66262,#66263,#66264,#66265,#66266,#66267)),
 .UNSPECIFIED.,.F.,.F.,.F.,(4,4),(4,1,1,1,1,1,1,1,1,1,1,1,1,1,1,1,1,1,1,
1,1,1,1,1,1,1,1,1,1,1,1,1,1,1,1,1,1,1,1,1,1,1,1,1,1,1,1,1,1,1,1,1,1,1,1,
1,1,1,1,1,4),(-0.000237162028320192,0.0996382913295698),(0.139688666527305,
0.141888509865,0.144088353202694,0.146288196540389,0.148488039878084,0.150687883215779,
0.152887726553474,0.155087569891169,0.157287413228864,0.160220537679124,
0.163153662129384,0.164620224354514,0.166086786579644,0.167553348804774,
0.169019911029903,0.171953035480163,0.174886159930423,0.177086003268118,
0.179285846605813,0.181485689943508,0.183685533281203,0.184235494115627,
0.18478545495005,0.185885376618898,0.188085219956593,0.190285063294288,
0.192484906631983,0.194684749969677,0.196884593307372,0.199084436645067,
0.200184358313915,0.200734319148339,0.201284279982762,0.203484123320457,
0.205683966658152,0.207883809995847,0.210083653333542,0.213016777783802,
0.215949902234062,0.218883026684322,0.221816151134581,0.224749275584841,
0.227682400035101,0.229148962260231,0.230615524485361,0.233548648935621,
0.236481773385881,0.239414897836141,0.241370314136314,0.243325730436487,
0.244303438586574,0.245281146736661,0.246381068405508,0.247480990074355,
0.24968083341205,0.251880676749745,0.25408052008744,0.256280363425135,0.25848020676283,
0.260680050100525,0.26287989343822),.UNSPECIFIED.);
#325=B_SPLINE_SURFACE_WITH_KNOTS('',3,3,((#66268,#66269,#66270,#66271,#66272,
#66273,#66274,#66275,#66276,#66277,#66278,#66279,#66280,#66281,#66282,#66283,
#66284,#66285,#66286,#66287,#66288,#66289,#66290,#66291,#66292,#66293,#66294,
#66295,#66296,#66297,#66298,#66299,#66300,#66301,#66302,#66303,#66304,#66305,
#66306,#66307,#66308,#66309,#66310,#66311,#66312,#66313,#66314,#66315,#66316,
#66317,#66318,#66319,#66320,#66321,#66322,#66323,#66324,#66325,#66326,#66327,
#66328,#66329,#66330,#66331),(#66332,#66333,#66334,#66335,#66336,#66337,
#66338,#66339,#66340,#66341,#66342,#66343,#66344,#66345,#66346,#66347,#66348,
#66349,#66350,#66351,#66352,#66353,#66354,#66355,#66356,#66357,#66358,#66359,
#66360,#66361,#66362,#66363,#66364,#66365,#66366,#66367,#66368,#66369,#66370,
#66371,#66372,#66373,#66374,#66375,#66376,#66377,#66378,#66379,#66380,#66381,
#66382,#66383,#66384,#66385,#66386,#66387,#66388,#66389,#66390,#66391,#66392,
#66393,#66394,#66395),(#66396,#66397,#66398,#66399,#66400,#66401,#66402,
#66403,#66404,#66405,#66406,#66407,#66408,#66409,#66410,#66411,#66412,#66413,
#66414,#66415,#66416,#66417,#66418,#66419,#66420,#66421,#66422,#66423,#66424,
#66425,#66426,#66427,#66428,#66429,#66430,#66431,#66432,#66433,#66434,#66435,
#66436,#66437,#66438,#66439,#66440,#66441,#66442,#66443,#66444,#66445,#66446,
#66447,#66448,#66449,#66450,#66451,#66452,#66453,#66454,#66455,#66456,#66457,
#66458,#66459),(#66460,#66461,#66462,#66463,#66464,#66465,#66466,#66467,
#66468,#66469,#66470,#66471,#66472,#66473,#66474,#66475,#66476,#66477,#66478,
#66479,#66480,#66481,#66482,#66483,#66484,#66485,#66486,#66487,#66488,#66489,
#66490,#66491,#66492,#66493,#66494,#66495,#66496,#66497,#66498,#66499,#66500,
#66501,#66502,#66503,#66504,#66505,#66506,#66507,#66508,#66509,#66510,#66511,
#66512,#66513,#66514,#66515,#66516,#66517,#66518,#66519,#66520,#66521,#66522,
#66523)),.UNSPECIFIED.,.F.,.F.,.F.,(4,4),(4,1,1,1,1,1,1,1,1,1,1,1,1,1,1,
1,1,1,1,1,1,1,1,1,1,1,1,1,1,1,1,1,1,1,1,1,1,1,1,1,1,1,1,1,1,1,1,1,1,1,1,
1,1,1,1,1,1,1,1,1,1,4),(-0.000173676366152087,0.0996748635808412),(0.308005718430657,
0.310256131102317,0.312455974418993,0.314655817735668,0.316855661052343,
0.319055504369019,0.321255347685694,0.323455191002369,0.325655034319044,
0.327610450600534,0.329565866882023,0.331521283163512,0.334454407585746,
0.337387532007979,0.340320656430213,0.343253780852447,0.343437101128836,
0.343620421405226,0.343987061958005,0.344353702510784,0.344720343063564,
0.346186905274681,0.349120029696914,0.352053154119148,0.354252997435823,
0.356452840752499,0.358652684069174,0.360852527385849,0.363052370702524,
0.3652522140192,0.367452057335875,0.36965190065255,0.371851743969226,0.374051587285901,
0.376251430602576,0.376801391431745,0.377351352260914,0.378451273919252,
0.381384398341485,0.384317522763719,0.387250647185953,0.390183771608187,
0.39311689603042,0.396050020452654,0.398983144874888,0.401916269297121,
0.404849393719355,0.406315955930472,0.407782518141589,0.409737934423078,
0.409982361458264,0.41022678849345,0.411693350704567,0.413648766986056,
0.415848610302732,0.418048453619407,0.420248296936082,0.422448140252758,
0.424647983569433,0.426847826886108,0.429047670202784,0.431421189885611),
 .UNSPECIFIED.);
#326=B_SPLINE_SURFACE_WITH_KNOTS('',3,3,((#66524,#66525,#66526,#66527,#66528,
#66529,#66530,#66531,#66532,#66533,#66534,#66535,#66536,#66537,#66538,#66539,
#66540,#66541,#66542,#66543,#66544,#66545,#66546,#66547,#66548,#66549,#66550,
#66551,#66552,#66553,#66554,#66555,#66556,#66557,#66558,#66559,#66560,#66561,
#66562,#66563,#66564,#66565,#66566,#66567,#66568,#66569,#66570,#66571,#66572,
#66573,#66574,#66575,#66576,#66577,#66578,#66579,#66580,#66581,#66582,#66583,
#66584,#66585),(#66586,#66587,#66588,#66589,#66590,#66591,#66592,#66593,
#66594,#66595,#66596,#66597,#66598,#66599,#66600,#66601,#66602,#66603,#66604,
#66605,#66606,#66607,#66608,#66609,#66610,#66611,#66612,#66613,#66614,#66615,
#66616,#66617,#66618,#66619,#66620,#66621,#66622,#66623,#66624,#66625,#66626,
#66627,#66628,#66629,#66630,#66631,#66632,#66633,#66634,#66635,#66636,#66637,
#66638,#66639,#66640,#66641,#66642,#66643,#66644,#66645,#66646,#66647),
(#66648,#66649,#66650,#66651,#66652,#66653,#66654,#66655,#66656,#66657,
#66658,#66659,#66660,#66661,#66662,#66663,#66664,#66665,#66666,#66667,#66668,
#66669,#66670,#66671,#66672,#66673,#66674,#66675,#66676,#66677,#66678,#66679,
#66680,#66681,#66682,#66683,#66684,#66685,#66686,#66687,#66688,#66689,#66690,
#66691,#66692,#66693,#66694,#66695,#66696,#66697,#66698,#66699,#66700,#66701,
#66702,#66703,#66704,#66705,#66706,#66707,#66708,#66709),(#66710,#66711,
#66712,#66713,#66714,#66715,#66716,#66717,#66718,#66719,#66720,#66721,#66722,
#66723,#66724,#66725,#66726,#66727,#66728,#66729,#66730,#66731,#66732,#66733,
#66734,#66735,#66736,#66737,#66738,#66739,#66740,#66741,#66742,#66743,#66744,
#66745,#66746,#66747,#66748,#66749,#66750,#66751,#66752,#66753,#66754,#66755,
#66756,#66757,#66758,#66759,#66760,#66761,#66762,#66763,#66764,#66765,#66766,
#66767,#66768,#66769,#66770,#66771)),.UNSPECIFIED.,.F.,.F.,.F.,(4,4),(4,
1,1,1,1,1,1,1,1,1,1,1,1,1,1,1,1,1,1,1,1,1,1,1,1,1,1,1,1,1,1,1,1,1,1,1,1,
1,1,1,1,1,1,1,1,1,1,1,1,1,1,1,1,1,1,1,1,1,1,4),(-0.000483778271071483,0.0996401519239673),
(0.476423916058673,0.478623759221241,0.480823602383808,0.483023445546375,
0.485223288708942,0.487423131871509,0.489622975034076,0.491822818196643,
0.49402266135921,0.495978077503714,0.497933493648219,0.499888909792723,
0.502822034009479,0.505755158226235,0.508688282442991,0.511621406659747,
0.514554530876503,0.51748765509326,0.518220936147449,0.518954217201638,
0.519687498255827,0.520420779310016,0.522620622472583,0.52482046563515,
0.527020308797717,0.529220151960284,0.531419995122852,0.533619838285419,
0.535819681447986,0.538019524610553,0.54021936777312,0.542419210935687,
0.544619054098254,0.546818897260821,0.549018740423388,0.551218583585956,
0.554151707802712,0.55561826991109,0.557818113073657,0.560017956236224,
0.562217799398791,0.564417642561358,0.566617485723925,0.568817328886493,
0.57101717204906,0.573217015211627,0.576150139428383,0.579083263645139,
0.582016387861895,0.583116309443179,0.583666270233821,0.584216231024462,
0.585316152605746,0.586416074187029,0.588615917349597,0.590815760512164,
0.593015603674731,0.595215446837298,0.597415289999865,0.599615133162432),
 .UNSPECIFIED.);
#327=B_SPLINE_SURFACE_WITH_KNOTS('',3,3,((#66772,#66773,#66774,#66775,#66776,
#66777,#66778,#66779,#66780,#66781,#66782,#66783,#66784,#66785,#66786,#66787,
#66788,#66789,#66790,#66791,#66792,#66793,#66794,#66795,#66796,#66797,#66798,
#66799,#66800,#66801,#66802,#66803,#66804,#66805,#66806,#66807,#66808,#66809,
#66810,#66811,#66812,#66813,#66814,#66815,#66816,#66817,#66818,#66819,#66820,
#66821,#66822,#66823,#66824,#66825,#66826,#66827,#66828),(#66829,#66830,
#66831,#66832,#66833,#66834,#66835,#66836,#66837,#66838,#66839,#66840,#66841,
#66842,#66843,#66844,#66845,#66846,#66847,#66848,#66849,#66850,#66851,#66852,
#66853,#66854,#66855,#66856,#66857,#66858,#66859,#66860,#66861,#66862,#66863,
#66864,#66865,#66866,#66867,#66868,#66869,#66870,#66871,#66872,#66873,#66874,
#66875,#66876,#66877,#66878,#66879,#66880,#66881,#66882,#66883,#66884,#66885),
(#66886,#66887,#66888,#66889,#66890,#66891,#66892,#66893,#66894,#66895,
#66896,#66897,#66898,#66899,#66900,#66901,#66902,#66903,#66904,#66905,#66906,
#66907,#66908,#66909,#66910,#66911,#66912,#66913,#66914,#66915,#66916,#66917,
#66918,#66919,#66920,#66921,#66922,#66923,#66924,#66925,#66926,#66927,#66928,
#66929,#66930,#66931,#66932,#66933,#66934,#66935,#66936,#66937,#66938,#66939,
#66940,#66941,#66942),(#66943,#66944,#66945,#66946,#66947,#66948,#66949,
#66950,#66951,#66952,#66953,#66954,#66955,#66956,#66957,#66958,#66959,#66960,
#66961,#66962,#66963,#66964,#66965,#66966,#66967,#66968,#66969,#66970,#66971,
#66972,#66973,#66974,#66975,#66976,#66977,#66978,#66979,#66980,#66981,#66982,
#66983,#66984,#66985,#66986,#66987,#66988,#66989,#66990,#66991,#66992,#66993,
#66994,#66995,#66996,#66997,#66998,#66999)),.UNSPECIFIED.,.F.,.F.,.F.,(4,
4),(4,1,1,1,1,1,1,1,1,1,1,1,1,1,1,1,1,1,1,1,1,1,1,1,1,1,1,1,1,1,1,1,1,1,
1,1,1,1,1,1,1,1,1,1,1,1,1,1,1,1,1,1,1,1,4),(-0.000295720647117127,0.0996668285717888),
(0.64474900998943,0.64699138736001,0.649191230384658,0.651391073409306,
0.653590916433954,0.655790759458603,0.657990602483251,0.660190445507899,
0.662390288532547,0.665323412565411,0.666789974581843,0.668256536598275,
0.67118966063114,0.674122784664004,0.677055908696868,0.679989032729732,
0.68218887575438,0.684388718779029,0.686588561803677,0.688788404828325,
0.690988247852973,0.693188090877621,0.695387933902269,0.697587776926917,
0.699787619951565,0.701987462976214,0.704187306000862,0.70638714902551,
0.708586992050158,0.710786835074806,0.712986678099454,0.715186521124103,
0.717386364148751,0.719586207173399,0.721052769189831,0.723985893222695,
0.726185736247343,0.728385579271991,0.730585422296639,0.732785265321288,
0.734985108345936,0.737184951370584,0.739384794395232,0.74158463741988,
0.744517761452744,0.747450885485609,0.750384009518473,0.752583852543121,
0.754783695567769,0.756983538592417,0.759183381617065,0.761383224641714,
0.763583067666362,0.76578291069101,0.768130417569294),.UNSPECIFIED.);
#328=B_SPLINE_SURFACE_WITH_KNOTS('',3,3,((#67000,#67001,#67002,#67003,#67004,
#67005,#67006,#67007,#67008,#67009,#67010,#67011,#67012,#67013,#67014,#67015,
#67016,#67017,#67018,#67019,#67020,#67021,#67022,#67023,#67024,#67025,#67026,
#67027,#67028,#67029,#67030,#67031,#67032,#67033,#67034,#67035,#67036,#67037,
#67038,#67039,#67040,#67041,#67042,#67043,#67044,#67045,#67046,#67047,#67048,
#67049,#67050,#67051,#67052,#67053,#67054,#67055,#67056,#67057,#67058,#67059,
#67060,#67061,#67062,#67063,#67064,#67065,#67066),(#67067,#67068,#67069,
#67070,#67071,#67072,#67073,#67074,#67075,#67076,#67077,#67078,#67079,#67080,
#67081,#67082,#67083,#67084,#67085,#67086,#67087,#67088,#67089,#67090,#67091,
#67092,#67093,#67094,#67095,#67096,#67097,#67098,#67099,#67100,#67101,#67102,
#67103,#67104,#67105,#67106,#67107,#67108,#67109,#67110,#67111,#67112,#67113,
#67114,#67115,#67116,#67117,#67118,#67119,#67120,#67121,#67122,#67123,#67124,
#67125,#67126,#67127,#67128,#67129,#67130,#67131,#67132,#67133),(#67134,
#67135,#67136,#67137,#67138,#67139,#67140,#67141,#67142,#67143,#67144,#67145,
#67146,#67147,#67148,#67149,#67150,#67151,#67152,#67153,#67154,#67155,#67156,
#67157,#67158,#67159,#67160,#67161,#67162,#67163,#67164,#67165,#67166,#67167,
#67168,#67169,#67170,#67171,#67172,#67173,#67174,#67175,#67176,#67177,#67178,
#67179,#67180,#67181,#67182,#67183,#67184,#67185,#67186,#67187,#67188,#67189,
#67190,#67191,#67192,#67193,#67194,#67195,#67196,#67197,#67198,#67199,#67200),
(#67201,#67202,#67203,#67204,#67205,#67206,#67207,#67208,#67209,#67210,
#67211,#67212,#67213,#67214,#67215,#67216,#67217,#67218,#67219,#67220,#67221,
#67222,#67223,#67224,#67225,#67226,#67227,#67228,#67229,#67230,#67231,#67232,
#67233,#67234,#67235,#67236,#67237,#67238,#67239,#67240,#67241,#67242,#67243,
#67244,#67245,#67246,#67247,#67248,#67249,#67250,#67251,#67252,#67253,#67254,
#67255,#67256,#67257,#67258,#67259,#67260,#67261,#67262,#67263,#67264,#67265,
#67266,#67267)),.UNSPECIFIED.,.F.,.F.,.F.,(4,4),(4,1,1,1,1,1,1,1,1,1,1,
1,1,1,1,1,1,1,1,1,1,1,1,1,1,1,1,1,1,1,1,1,1,1,1,1,1,1,1,1,1,1,1,1,1,1,1,
1,1,1,1,1,1,1,1,1,1,1,1,1,1,1,1,1,4),(-0.000370856902642016,0.0600414511958849),
(0.79017342904027,0.792057831484434,0.793901305088964,0.795744778693493,
0.797588252298022,0.799431725902551,0.800353462704815,0.801275199507079,
0.803118673111608,0.804962146716138,0.807420111522176,0.809878076328215,
0.812336041134254,0.814179514738783,0.816022988343312,0.817866461947841,
0.81970993555237,0.820631672354634,0.821553409156899,0.822475145959163,
0.823396882761428,0.825240356365957,0.827083829970486,0.828312812373505,
0.830770777179544,0.832614250784073,0.834457724388602,0.836301197993131,
0.83814467159766,0.839373654000679,0.841831618806718,0.842753355608982,
0.843675092411247,0.845518566015776,0.84644030281804,0.847362039620305,
0.849205513224834,0.851048986829363,0.852892460433892,0.854735934038421,
0.85657940764295,0.857808390045969,0.859037372448988,0.859651863650498,
0.860266354852008,0.861495337255027,0.862724319658047,0.863338810859556,
0.863953302061066,0.866411266867105,0.868869231673143,0.871327196479182,
0.872556178882201,0.873785161285221,0.875423804489247,0.877062447693272,
0.878701090897298,0.880544564501827,0.882388038106356,0.884231511710885,
0.886074985315414,0.887918458919943,0.889761932524472,0.891605406129001,
0.893665144683499),.UNSPECIFIED.);
#329=B_SPLINE_SURFACE_WITH_KNOTS('',3,3,((#67326,#67327,#67328,#67329,#67330,
#67331,#67332,#67333,#67334,#67335,#67336,#67337,#67338,#67339,#67340,#67341,
#67342,#67343,#67344,#67345,#67346,#67347,#67348,#67349,#67350,#67351,#67352,
#67353,#67354,#67355,#67356,#67357,#67358,#67359,#67360,#67361,#67362,#67363,
#67364,#67365,#67366,#67367,#67368,#67369,#67370,#67371,#67372,#67373,#67374,
#67375,#67376,#67377,#67378,#67379,#67380,#67381,#67382,#67383,#67384,#67385,
#67386,#67387,#67388,#67389,#67390,#67391,#67392,#67393,#67394,#67395,#67396,
#67397,#67398,#67399,#67400,#67401,#67402,#67403,#67404,#67405,#67406,#67407,
#67408,#67409,#67410,#67411,#67412,#67413),(#67414,#67415,#67416,#67417,
#67418,#67419,#67420,#67421,#67422,#67423,#67424,#67425,#67426,#67427,#67428,
#67429,#67430,#67431,#67432,#67433,#67434,#67435,#67436,#67437,#67438,#67439,
#67440,#67441,#67442,#67443,#67444,#67445,#67446,#67447,#67448,#67449,#67450,
#67451,#67452,#67453,#67454,#67455,#67456,#67457,#67458,#67459,#67460,#67461,
#67462,#67463,#67464,#67465,#67466,#67467,#67468,#67469,#67470,#67471,#67472,
#67473,#67474,#67475,#67476,#67477,#67478,#67479,#67480,#67481,#67482,#67483,
#67484,#67485,#67486,#67487,#67488,#67489,#67490,#67491,#67492,#67493,#67494,
#67495,#67496,#67497,#67498,#67499,#67500,#67501),(#67502,#67503,#67504,
#67505,#67506,#67507,#67508,#67509,#67510,#67511,#67512,#67513,#67514,#67515,
#67516,#67517,#67518,#67519,#67520,#67521,#67522,#67523,#67524,#67525,#67526,
#67527,#67528,#67529,#67530,#67531,#67532,#67533,#67534,#67535,#67536,#67537,
#67538,#67539,#67540,#67541,#67542,#67543,#67544,#67545,#67546,#67547,#67548,
#67549,#67550,#67551,#67552,#67553,#67554,#67555,#67556,#67557,#67558,#67559,
#67560,#67561,#67562,#67563,#67564,#67565,#67566,#67567,#67568,#67569,#67570,
#67571,#67572,#67573,#67574,#67575,#67576,#67577,#67578,#67579,#67580,#67581,
#67582,#67583,#67584,#67585,#67586,#67587,#67588,#67589),(#67590,#67591,
#67592,#67593,#67594,#67595,#67596,#67597,#67598,#67599,#67600,#67601,#67602,
#67603,#67604,#67605,#67606,#67607,#67608,#67609,#67610,#67611,#67612,#67613,
#67614,#67615,#67616,#67617,#67618,#67619,#67620,#67621,#67622,#67623,#67624,
#67625,#67626,#67627,#67628,#67629,#67630,#67631,#67632,#67633,#67634,#67635,
#67636,#67637,#67638,#67639,#67640,#67641,#67642,#67643,#67644,#67645,#67646,
#67647,#67648,#67649,#67650,#67651,#67652,#67653,#67654,#67655,#67656,#67657,
#67658,#67659,#67660,#67661,#67662,#67663,#67664,#67665,#67666,#67667,#67668,
#67669,#67670,#67671,#67672,#67673,#67674,#67675,#67676,#67677)),
 .UNSPECIFIED.,.F.,.F.,.F.,(4,4),(4,1,1,1,1,1,1,1,1,1,1,1,1,1,1,1,1,1,1,
1,1,1,1,1,1,1,1,1,1,1,1,1,1,1,1,1,1,1,1,1,1,1,1,1,1,1,1,1,1,1,1,1,1,1,1,
1,1,1,1,1,1,1,1,1,1,1,1,1,1,1,1,1,1,1,1,1,1,1,1,1,1,1,1,1,1,4),(-0.000543361608291823,
0.0996242942258564),(0.813159172043207,0.815359014876381,0.817558857709555,
0.819758700542729,0.821958543375904,0.824158386209078,0.826358229042252,
0.828558071875427,0.830757914708601,0.832224476597384,0.833691038486167,
0.83515760037495,0.835890881319341,0.836624162263733,0.837357443208124,
0.839557286041298,0.841757128874473,0.843956971707647,0.846156814540821,
0.848356657373996,0.85055650020717,0.852756343040344,0.853856264456931,
0.854956185873519,0.857156028706693,0.857889309651084,0.858622590595476,
0.859355871539867,0.860089152484259,0.86082243342865,0.861555714373042,
0.862655635789629,0.863755557206216,0.864855478622803,0.86595540003939,
0.868155242872565,0.870355085705739,0.871821647594522,0.874754771372088,
0.875854692788675,0.876954614205262,0.879154457038436,0.880254378455023,
0.880804339163317,0.881079319517464,0.881354299871611,0.883554142704785,
0.885753985537959,0.887953828371133,0.890153671204308,0.892353514037482,
0.89253683427358,0.892628494391629,0.892720154509678,0.893086794981873,
0.893820075926265,0.895286637815048,0.896753199703831,0.898219761592614,
0.898953042537005,0.899136362773103,0.899319683009201,0.899686323481397,
0.900052963953592,0.900419604425788,0.901152885370179,0.902619447258962,
0.904086009147745,0.905552571036528,0.907019132925311,0.908485694814094,
0.909952256702877,0.91141881859166,0.912885380480442,0.914840796332153,
0.916796212183863,0.917773920109719,0.918751628035574,0.920951470868748,
0.923151313701923,0.925351156535097,0.927550999368271,0.929750842201446,
0.93195068503462,0.934150527867794,0.936473459753071),.UNSPECIFIED.);
#330=B_SPLINE_SURFACE_WITH_KNOTS('',3,3,((#68645,#68646,#68647,#68648,#68649,
#68650,#68651,#68652,#68653,#68654,#68655,#68656,#68657,#68658,#68659,#68660,
#68661,#68662,#68663,#68664,#68665,#68666,#68667,#68668,#68669,#68670,#68671,
#68672,#68673,#68674,#68675,#68676,#68677,#68678,#68679,#68680,#68681,#68682,
#68683,#68684,#68685,#68686,#68687,#68688,#68689,#68690,#68691,#68692,#68693,
#68694,#68695,#68696,#68697,#68698,#68699,#68700,#68701,#68702,#68703,#68704,
#68705,#68706,#68707,#68708,#68709,#68710,#68711,#68712,#68713,#68714,#68715,
#68716,#68717,#68718,#68719,#68720,#68721,#68722,#68723,#68724,#68725,#68726,
#68727,#68728),(#68729,#68730,#68731,#68732,#68733,#68734,#68735,#68736,
#68737,#68738,#68739,#68740,#68741,#68742,#68743,#68744,#68745,#68746,#68747,
#68748,#68749,#68750,#68751,#68752,#68753,#68754,#68755,#68756,#68757,#68758,
#68759,#68760,#68761,#68762,#68763,#68764,#68765,#68766,#68767,#68768,#68769,
#68770,#68771,#68772,#68773,#68774,#68775,#68776,#68777,#68778,#68779,#68780,
#68781,#68782,#68783,#68784,#68785,#68786,#68787,#68788,#68789,#68790,#68791,
#68792,#68793,#68794,#68795,#68796,#68797,#68798,#68799,#68800,#68801,#68802,
#68803,#68804,#68805,#68806,#68807,#68808,#68809,#68810,#68811,#68812),
(#68813,#68814,#68815,#68816,#68817,#68818,#68819,#68820,#68821,#68822,
#68823,#68824,#68825,#68826,#68827,#68828,#68829,#68830,#68831,#68832,#68833,
#68834,#68835,#68836,#68837,#68838,#68839,#68840,#68841,#68842,#68843,#68844,
#68845,#68846,#68847,#68848,#68849,#68850,#68851,#68852,#68853,#68854,#68855,
#68856,#68857,#68858,#68859,#68860,#68861,#68862,#68863,#68864,#68865,#68866,
#68867,#68868,#68869,#68870,#68871,#68872,#68873,#68874,#68875,#68876,#68877,
#68878,#68879,#68880,#68881,#68882,#68883,#68884,#68885,#68886,#68887,#68888,
#68889,#68890,#68891,#68892,#68893,#68894,#68895,#68896),(#68897,#68898,
#68899,#68900,#68901,#68902,#68903,#68904,#68905,#68906,#68907,#68908,#68909,
#68910,#68911,#68912,#68913,#68914,#68915,#68916,#68917,#68918,#68919,#68920,
#68921,#68922,#68923,#68924,#68925,#68926,#68927,#68928,#68929,#68930,#68931,
#68932,#68933,#68934,#68935,#68936,#68937,#68938,#68939,#68940,#68941,#68942,
#68943,#68944,#68945,#68946,#68947,#68948,#68949,#68950,#68951,#68952,#68953,
#68954,#68955,#68956,#68957,#68958,#68959,#68960,#68961,#68962,#68963,#68964,
#68965,#68966,#68967,#68968,#68969,#68970,#68971,#68972,#68973,#68974,#68975,
#68976,#68977,#68978,#68979,#68980)),.UNSPECIFIED.,.F.,.F.,.F.,(4,4),(4,
1,1,1,1,1,1,1,1,1,1,1,1,1,1,1,1,1,1,1,1,1,1,1,1,1,1,1,1,1,1,1,1,1,1,1,1,
1,1,1,1,1,1,1,1,1,1,1,1,1,1,1,1,1,1,1,1,1,1,1,1,1,1,1,1,1,1,1,1,1,1,1,1,
1,1,1,1,1,1,1,1,4),(-0.000202954762976394,0.120064235496532),(0.85630617939849,
0.858856990877825,0.861344437291952,0.86383188370608,0.866319330120207,
0.868806776534335,0.871294222948462,0.872537946155526,0.87378166936259,
0.875025392569654,0.876269115776718,0.878480179255942,0.880691242735167,
0.882902306214391,0.886218901433228,0.889535496652065,0.891193794261483,
0.892852091870902,0.89451038948032,0.896168687089739,0.896997835894448,
0.897826984699157,0.899485282308575,0.900314431113284,0.901143579917994,
0.901558154320348,0.901972728722703,0.902801877527412,0.906118472746249,
0.906947621550958,0.907776770355667,0.909435067965086,0.91164613144431,
0.913857194923535,0.916068258402759,0.917173790142372,0.918279321881984,
0.920490385361208,0.922701448840433,0.924359746449851,0.92601804405927,
0.927676341668688,0.929334639278107,0.930163788082816,0.930992936887525,
0.931822085692234,0.932651234496943,0.933065808899298,0.933480383301653,
0.934309532106362,0.935138680911071,0.935553255313426,0.93596782971578,
0.939284424934617,0.942601020153454,0.945917615372291,0.949234210591127,
0.951445274070352,0.953656337549576,0.955867401028801,0.957525698638219,
0.959183996247638,0.960842293857056,0.962500591466475,0.964158889075893,
0.965817186685311,0.96747548429473,0.968304633099439,0.968719207501794,
0.969133781904148,0.972450377122985,0.974108674732403,0.975766972341822,
0.978254418755949,0.980741865170077,0.983229311584205,0.984473034791268,
0.985716757998332,0.98820420441246,0.990691650826587,0.993179097240715,
0.995869498417819),.UNSPECIFIED.);
#617=B_SPLINE_CURVE_WITH_KNOTS('',3,(#41522,#41523,#41524,#41525,#41526,
#41527,#41528,#41529,#41530,#41531,#41532,#41533,#41534,#41535,#41536,#41537,
#41538,#41539,#41540,#41541,#41542,#41543),.UNSPECIFIED.,.F.,.F.,(4,2,2,
2,2,2,2,2,2,2,4),(3.73107638342163E-6,0.0506459089674672,0.103371892378906,
0.203995846997698,0.297723322628345,0.347133425087129,0.435556350263891,
0.482653331242677,0.583240346238036,0.640653178327547,0.694267771013001),
 .UNSPECIFIED.);
#618=B_SPLINE_CURVE_WITH_KNOTS('',3,(#41545,#41546,#41547,#41548,#41549,
#41550,#41551,#41552,#41553,#41554,#41555,#41556,#41557,#41558,#41559,#41560,
#41561,#41562,#41563,#41564,#41565,#41566,#41567,#41568,#41569,#41570,#41571,
#41572,#41573,#41574,#41575,#41576,#41577,#41578,#41579,#41580,#41581,#41582,
#41583,#41584,#41585,#41586,#41587,#41588,#41589,#41590,#41591,#41592,#41593,
#41594,#41595,#41596,#41597,#41598,#41599,#41600,#41601,#41602,#41603,#41604,
#41605,#41606,#41607,#41608,#41609,#41610,#41611,#41612,#41613,#41614,#41615,
#41616,#41617,#41618,#41619,#41620,#41621,#41622,#41623,#41624,#41625,#41626,
#41627,#41628,#41629,#41630,#41631,#41632,#41633,#41634,#41635,#41636,#41637,
#41638,#41639,#41640,#41641,#41642,#41643,#41644,#41645,#41646,#41647,#41648,
#41649,#41650,#41651,#41652,#41653,#41654,#41655,#41656,#41657,#41658,#41659,
#41660,#41661,#41662,#41663,#41664,#41665,#41666,#41667,#41668,#41669,#41670,
#41671,#41672,#41673,#41674,#41675,#41676,#41677,#41678,#41679,#41680,#41681,
#41682,#41683,#41684,#41685,#41686,#41687,#41688,#41689,#41690,#41691,#41692,
#41693,#41694,#41695,#41696,#41697,#41698,#41699,#41700,#41701,#41702,#41703,
#41704,#41705,#41706,#41707,#41708,#41709,#41710,#41711,#41712,#41713,#41714,
#41715,#41716,#41717,#41718,#41719,#41720,#41721,#41722,#41723,#41724,#41725,
#41726,#41727,#41728,#41729,#41730,#41731,#41732,#41733,#41734,#41735,#41736,
#41737),.UNSPECIFIED.,.F.,.F.,(4,3,3,3,3,3,3,3,3,3,3,3,3,3,3,3,3,3,3,3,
3,3,3,3,3,3,3,3,3,3,3,3,3,3,3,3,3,3,3,3,3,3,3,3,3,3,3,3,3,3,3,3,3,3,3,3,
3,3,3,3,3,3,3,3,4),(0.00234954353479144,0.00310318921645473,0.0088582021338961,
0.00930481001264915,0.0216886296499449,0.0485537357742967,0.0600476559819482,
0.060077834493807,0.0708153993107394,0.0973229488478452,0.124174207582929,
0.150994548134737,0.168411939510706,0.173195847105295,0.173221725606229,
0.199629661690922,0.226438379404894,0.25331614970675,0.266220462053855,
0.286347834381452,0.286367093094366,0.312947470961036,0.339878442731592,
0.36419063552826,0.389390727847281,0.391018387762494,0.39951577415484,0.399520049495332,
0.426183119512092,0.453091259603804,0.46236150068436,0.489208228107559,
0.51267181785655,0.51268691960903,0.539532286181883,0.560782471473938,0.569211298980254,
0.569234438523911,0.595920151049213,0.621412765585973,0.622860168004852,
0.625813142893821,0.625848336448634,0.651175201287267,0.652699670111354,
0.659399028042767,0.686003429405952,0.712970949013868,0.738935139746066,
0.738982748431222,0.758164277735553,0.784631050256268,0.795443012593489,
0.795492931537947,0.819715584311038,0.823762057603835,0.823813147482631,
0.837908125570947,0.837958543617086,0.852030564169489,0.852083643327173,
0.85713132501906,0.880252976771596,0.883475761569799,0.894414923079292),
 .UNSPECIFIED.);
#619=B_SPLINE_CURVE_WITH_KNOTS('',3,(#41741,#41742,#41743,#41744,#41745,
#41746,#41747,#41748,#41749,#41750,#41751,#41752),.UNSPECIFIED.,.F.,.F.,
(4,2,2,2,2,4),(4.14401685134791,4.23919981484122,4.3234021788811,4.42503338177172,
4.48178100258938,4.53126296388924),.UNSPECIFIED.);
#620=B_SPLINE_CURVE_WITH_KNOTS('',3,(#41754,#41755,#41756,#41757,#41758,
#41759,#41760,#41761,#41762,#41763,#41764,#41765,#41766,#41767,#41768,#41769,
#41770,#41771,#41772,#41773,#41774,#41775,#41776,#41777,#41778,#41779,#41780,
#41781,#41782,#41783,#41784,#41785,#41786,#41787,#41788,#41789,#41790,#41791,
#41792,#41793,#41794,#41795,#41796,#41797,#41798,#41799,#41800,#41801,#41802,
#41803,#41804,#41805),.UNSPECIFIED.,.F.,.F.,(4,3,3,3,3,3,3,3,3,3,3,3,3,
3,3,3,3,4),(0.,0.0262870680174327,0.0526250957989455,0.0784797815042996,
0.10063173188014,0.101346503493714,0.123864269870963,0.146327018657836,
0.168872293830273,0.19141756900271,0.210943942314893,0.216050596552535,
0.240087946409699,0.253454166228182,0.27404349701453,0.294365188295977,
0.314525566744571,0.330523895440752),.UNSPECIFIED.);
#621=B_SPLINE_CURVE_WITH_KNOTS('',3,(#41808,#41809,#41810,#41811,#41812,
#41813,#41814,#41815,#41816,#41817,#41818,#41819,#41820,#41821,#41822,#41823,
#41824,#41825,#41826,#41827,#41828,#41829,#41830,#41831),.UNSPECIFIED.,
 .F.,.F.,(4,2,2,2,2,2,2,2,2,2,2,4),(2.73904782886837E-12,0.0817234061279085,
0.161552425644965,0.261638330253269,0.309328561956691,0.356314225569715,
0.402118903800116,0.477843813243927,0.569451511760358,0.604233221463172,
0.659917854360184,0.712631531767947),.UNSPECIFIED.);
#622=B_SPLINE_CURVE_WITH_KNOTS('',3,(#41836,#41837,#41838,#41839,#41840,
#41841,#41842,#41843,#41844,#41845,#41846,#41847,#41848,#41849,#41850,#41851,
#41852,#41853,#41854,#41855,#41856,#41857,#41858,#41859,#41860,#41861,#41862,
#41863,#41864,#41865,#41866,#41867,#41868,#41869,#41870,#41871,#41872,#41873,
#41874,#41875,#41876,#41877,#41878,#41879),.UNSPECIFIED.,.F.,.F.,(4,2,2,
2,2,2,2,2,2,2,2,2,2,2,2,2,2,2,2,2,2,4),(2.54700836416053,2.55527047039645,
2.6186560390472,2.6731150077874,2.76356237393918,2.86595286652909,2.96144125756534,
3.00742527171164,3.09922332533053,3.18621856024237,3.28775374837671,3.37402791853298,
3.47553035070879,3.51982920681099,3.56755802727897,3.66929833501538,3.76265070549564,
3.8643160955509,3.95044192085268,4.05174321628903,4.13710175052906,4.14401685134791),
 .UNSPECIFIED.);
#623=B_SPLINE_CURVE_WITH_KNOTS('',3,(#41881,#41882,#41883,#41884,#41885,
#41886,#41887,#41888,#41889,#41890,#41891,#41892,#41893,#41894,#41895,#41896,
#41897,#41898,#41899,#41900,#41901,#41902),.UNSPECIFIED.,.F.,.F.,(4,2,2,
2,2,2,2,2,2,2,4),(1.78915403369814E-6,0.0868924796927673,0.160732517221174,
0.248846661449348,0.346410911703831,0.431051162846719,0.524867255149695,
0.613111647621759,0.713356525426838,0.790010811238862,0.862101243151681),
 .UNSPECIFIED.);
#624=B_SPLINE_CURVE_WITH_KNOTS('',3,(#41903,#41904,#41905,#41906,#41907,
#41908,#41909,#41910,#41911,#41912,#41913,#41914,#41915,#41916,#41917,#41918,
#41919,#41920,#41921,#41922,#41923,#41924,#41925,#41926,#41927,#41928,#41929,
#41930,#41931,#41932,#41933,#41934,#41935,#41936,#41937,#41938,#41939,#41940,
#41941,#41942,#41943,#41944,#41945,#41946,#41947,#41948,#41949,#41950,#41951,
#41952,#41953,#41954,#41955,#41956,#41957,#41958,#41959,#41960,#41961,#41962,
#41963,#41964,#41965,#41966,#41967,#41968,#41969,#41970,#41971,#41972,#41973,
#41974,#41975,#41976,#41977,#41978,#41979,#41980,#41981,#41982,#41983,#41984,
#41985,#41986,#41987,#41988,#41989,#41990,#41991,#41992,#41993,#41994,#41995,
#41996,#41997,#41998,#41999,#42000,#42001,#42002,#42003,#42004,#42005,#42006,
#42007,#42008,#42009,#42010,#42011,#42012,#42013,#42014,#42015,#42016,#42017,
#42018,#42019,#42020,#42021,#42022,#42023,#42024,#42025,#42026,#42027,#42028,
#42029),.UNSPECIFIED.,.F.,.F.,(4,3,3,3,3,3,3,3,3,3,3,3,3,3,3,3,3,3,3,3,
3,3,3,3,3,3,3,3,3,3,3,3,3,3,3,3,3,3,3,3,3,3,4),(6.97767400438006E-5,0.0235124483256361,
0.0270464789573299,0.0540916358144278,0.0540924383659419,0.0808761116857087,
0.10182755879334,0.128477878765437,0.155397360247213,0.182107640682707,
0.203530646983436,0.207332017371417,0.207335173218032,0.233537240917649,
0.260215569308816,0.287100578155007,0.305135316889012,0.331037947464665,
0.332835591432724,0.358148063171977,0.360534126946588,0.360535865976435,
0.387324342918355,0.406659063564906,0.433301001733156,0.460207152642024,
0.486907643567796,0.508111183143103,0.513642026520772,0.513644119980954,
0.539917002725518,0.566646088148737,0.593538460524371,0.609500681295586,
0.636287771621458,0.661202837393452,0.663188937792746,0.66676046432175,
0.666767529697564,0.691789652308819,0.69357815457004,0.710837254295307,
0.727868008326198),.UNSPECIFIED.);
#625=B_SPLINE_CURVE_WITH_KNOTS('',3,(#42034,#42035,#42036,#42037,#42038,
#42039,#42040,#42041,#42042,#42043,#42044,#42045,#42046,#42047,#42048,#42049,
#42050,#42051,#42052,#42053,#42054,#42055,#42056,#42057,#42058,#42059,#42060,
#42061,#42062,#42063,#42064,#42065,#42066,#42067,#42068,#42069,#42070,#42071,
#42072,#42073,#42074,#42075,#42076,#42077,#42078,#42079,#42080,#42081,#42082,
#42083),.UNSPECIFIED.,.F.,.F.,(4,2,2,2,2,2,2,2,2,2,2,2,2,2,2,2,2,2,2,2,
2,2,2,2,4),(0.948102451772265,0.963248283802765,1.04166019732699,1.13852638559126,
1.24111112615258,1.28817418963009,1.38173677806716,1.48119583120305,1.52865407567559,
1.62580315113657,1.67715559130836,1.77123509905442,1.86940551833799,1.92006452837572,
1.96928463441235,2.07106552400663,2.11953556464442,2.1696635783818,2.2628314825113,
2.31268183523941,2.40975454513444,2.46028307555686,2.50010956658168,2.52690669878563,
2.54700836416053),.UNSPECIFIED.);
#626=B_SPLINE_CURVE_WITH_KNOTS('',3,(#42084,#42085,#42086,#42087,#42088,
#42089,#42090,#42091,#42092,#42093,#42094,#42095,#42096,#42097,#42098,#42099,
#42100,#42101,#42102,#42103,#42104,#42105,#42106,#42107,#42108,#42109,#42110,
#42111,#42112,#42113,#42114,#42115,#42116,#42117,#42118,#42119,#42120,#42121,
#42122,#42123,#42124,#42125,#42126,#42127,#42128,#42129),.UNSPECIFIED.,
 .F.,.F.,(4,2,2,2,2,2,2,2,2,2,2,2,2,2,2,2,2,2,2,2,2,2,4),(3.61415565987237E-6,
0.077382941848095,0.160320021301451,0.209315495312916,0.306998962340119,
0.403428249018374,0.453483402618285,0.502488421932669,0.552021971453635,
0.651021708478505,0.734535687626094,0.835245242957744,0.929270713532786,
0.97642189347609,1.0772912867649,1.17001200448534,1.22066776172236,1.26903355645575,
1.31675674395734,1.41727824130363,1.46576352901781,1.51581597882557,1.58755892759308),
 .UNSPECIFIED.);
#627=B_SPLINE_CURVE_WITH_KNOTS('',3,(#42135,#42136,#42137,#42138,#42139,
#42140,#42141,#42142,#42143,#42144,#42145,#42146,#42147,#42148,#42149,#42150,
#42151,#42152),.UNSPECIFIED.,.F.,.F.,(4,2,2,2,2,2,2,2,4),(1.58647040136232,
1.64954740781937,1.74368498223918,1.79306983672385,1.88170654786799,1.98253725725693,
2.07467976983039,2.1593136884966,2.23194989940745),.UNSPECIFIED.);
#628=B_SPLINE_CURVE_WITH_KNOTS('',3,(#42153,#42154,#42155,#42156,#42157,
#42158,#42159,#42160,#42161,#42162,#42163,#42164,#42165,#42166,#42167,#42168,
#42169,#42170,#42171,#42172,#42173,#42174,#42175,#42176,#42177,#42178),
 .UNSPECIFIED.,.F.,.F.,(4,2,2,2,2,2,2,2,2,2,2,2,4),(0.,0.0676700015567033,
0.122566337419964,0.205326521836919,0.282812301557027,0.378757335369595,
0.472380426030512,0.559981068984037,0.646990361523079,0.723350516868986,
0.799938201588545,0.867845104473521,0.948102451772265),.UNSPECIFIED.);
#629=B_SPLINE_CURVE_WITH_KNOTS('',3,(#42180,#42181,#42182,#42183,#42184,
#42185,#42186,#42187,#42188,#42189,#42190,#42191,#42192,#42193,#42194,#42195,
#42196,#42197,#42198,#42199,#42200,#42201,#42202,#42203,#42204,#42205,#42206,
#42207),.UNSPECIFIED.,.F.,.F.,(4,2,2,2,2,2,2,2,2,2,2,2,2,4),(1.58755892759308,
1.61118768308576,1.7120370068482,1.79401697393938,1.83561413499285,1.93632851510131,
2.01723367290632,2.05971469843759,2.16030698468104,2.24037081829283,2.33947585278893,
2.42806601707448,2.48424726450739,2.53786893574039),.UNSPECIFIED.);
#630=B_SPLINE_CURVE_WITH_KNOTS('',3,(#42208,#42209,#42210,#42211,#42212,
#42213,#42214,#42215,#42216,#42217,#42218,#42219,#42220,#42221,#42222,#42223,
#42224,#42225,#42226,#42227,#42228,#42229,#42230,#42231,#42232,#42233,#42234,
#42235,#42236,#42237,#42238,#42239,#42240,#42241,#42242,#42243,#42244,#42245,
#42246,#42247,#42248,#42249,#42250,#42251,#42252,#42253,#42254,#42255,#42256,
#42257,#42258,#42259,#42260,#42261,#42262,#42263,#42264,#42265,#42266,#42267,
#42268,#42269,#42270,#42271,#42272,#42273,#42274,#42275,#42276,#42277,#42278,
#42279,#42280,#42281,#42282,#42283,#42284,#42285,#42286,#42287,#42288,#42289,
#42290,#42291,#42292,#42293,#42294,#42295),.UNSPECIFIED.,.F.,.F.,(4,3,3,
3,3,3,3,3,3,3,3,3,3,3,3,3,3,3,3,3,3,3,3,3,3,3,3,3,3,4),(0.,0.0260937840727114,
0.0525749650683046,0.0790662183953249,0.10174715965396,0.128409551897913,
0.143179660817706,0.169333208229716,0.195892486876489,0.203377364754321,
0.229839532229633,0.256528353772948,0.282952141779042,0.304921331842682,
0.310762738631824,0.336812421877813,0.363315467390979,0.390012597263233,
0.406390796679477,0.433075871178777,0.459775676011333,0.478564893937639,
0.505168461021389,0.507799856305071,0.534148262403094,0.560816838480447,
0.587385623839857,0.604451917299051,0.60916481417943,0.63998402750676),
 .UNSPECIFIED.);
#631=B_SPLINE_CURVE_WITH_KNOTS('',3,(#42301,#42302,#42303,#42304),
 .UNSPECIFIED.,.F.,.F.,(4,4),(1.03705581745603,1.03710062472995),
 .UNSPECIFIED.);
#632=B_SPLINE_CURVE_WITH_KNOTS('',3,(#42305,#42306,#42307,#42308,#42309,
#42310,#42311,#42312,#42313,#42314,#42315,#42316,#42317,#42318,#42319,#42320,
#42321,#42322,#42323,#42324,#42325,#42326,#42327,#42328,#42329,#42330,#42331,
#42332,#42333,#42334,#42335,#42336,#42337,#42338,#42339,#42340,#42341,#42342,
#42343,#42344,#42345,#42346,#42347,#42348,#42349,#42350,#42351,#42352),
 .UNSPECIFIED.,.F.,.F.,(4,2,2,2,2,2,2,2,2,2,2,2,2,2,2,2,2,2,2,2,2,2,2,4),
(1.0000000652683E-6,0.0659798375703458,0.131960432135887,0.227947110507754,
0.278170740594184,0.32755046055882,0.377278851322222,0.426154139782107,
0.527372108276288,0.575321757958173,0.67648372491335,0.724474618070015,
0.825273934637277,0.87406352498187,0.975310913425844,1.06590783546145,1.11596419449799,
1.1622724896011,1.21029538172571,1.31150498364856,1.405531155535,1.50086798044765,
1.54850345928088,1.58647040136232),.UNSPECIFIED.);
#633=B_SPLINE_CURVE_WITH_KNOTS('',3,(#42353,#42354,#42355,#42356,#42357,
#42358,#42359,#42360,#42361,#42362,#42363,#42364,#42365,#42366,#42367,#42368,
#42369,#42370,#42371,#42372,#42373,#42374,#42375,#42376,#42377,#42378,#42379,
#42380,#42381,#42382,#42383,#42384,#42385,#42386,#42387,#42388,#42389,#42390,
#42391,#42392,#42393,#42394,#42395,#42396,#42397,#42398,#42399,#42400,#42401,
#42402),.UNSPECIFIED.,.F.,.F.,(4,2,2,2,2,2,2,2,2,2,2,2,2,2,2,2,2,2,2,2,
2,2,2,2,4),(0.000199761406301567,0.0690250162272561,0.120468154968914,0.221585345736489,
0.318571823185642,0.412447787590937,0.460525423192448,0.510348161937974,
0.559844210864398,0.660838829435275,0.709557966219876,0.757765007399357,
0.85247110551944,0.903280765958044,0.995810811626083,1.09264246022628,1.14040894397419,
1.24104431859928,1.29015750425647,1.35517589475524,1.398387594317,1.43868557502763,
1.48058004729817,1.57600852077177,1.59042890355212),.UNSPECIFIED.);
#634=B_SPLINE_CURVE_WITH_KNOTS('',3,(#42408,#42409,#42410,#42411,#42412,
#42413,#42414,#42415,#42416,#42417,#42418,#42419,#42420,#42421,#42422,#42423,
#42424,#42425),.UNSPECIFIED.,.F.,.F.,(4,2,2,2,2,2,2,2,4),(1.33398049474525E-6,
0.0691723805623115,0.134134919596717,0.179786156624329,0.276551377826846,
0.326554301751731,0.420325831437485,0.489305280783672,0.553050350028315),
 .UNSPECIFIED.);
#635=B_SPLINE_CURVE_WITH_KNOTS('',3,(#42426,#42427,#42428,#42429,#42430,
#42431,#42432,#42433,#42434,#42435,#42436,#42437,#42438,#42439,#42440,#42441,
#42442,#42443,#42444,#42445,#42446,#42447,#42448,#42449,#42450,#42451),
 .UNSPECIFIED.,.F.,.F.,(4,2,2,2,2,2,2,2,2,2,2,2,4),(3.15205015175211E-5,
0.0633644897124623,0.130089056650009,0.228142859899691,0.326403155931319,
0.422157763664604,0.518583456450466,0.619958904732367,0.719007867076939,
0.817973781907731,0.868478058477331,0.95165878657454,1.03705581745603),
 .UNSPECIFIED.);
#636=B_SPLINE_CURVE_WITH_KNOTS('',3,(#42452,#42453,#42454,#42455,#42456,
#42457,#42458,#42459,#42460,#42461,#42462,#42463,#42464,#42465,#42466,#42467,
#42468,#42469,#42470,#42471,#42472,#42473,#42474,#42475,#42476,#42477,#42478,
#42479,#42480,#42481,#42482,#42483,#42484,#42485,#42486,#42487,#42488,#42489,
#42490,#42491,#42492,#42493,#42494,#42495,#42496,#42497),.UNSPECIFIED.,
 .F.,.F.,(4,2,2,2,2,2,2,2,2,2,2,2,2,2,2,2,2,2,2,2,2,2,4),(1.59042890355212,
1.61509734716197,1.64572427898667,1.68535868251392,1.72156708258987,1.78007921656754,
1.84960897097247,1.93624638519471,2.02924170442665,2.12247140474378,2.22212513699261,
2.3077268420635,2.35571077411299,2.45666738417593,2.55076418648938,2.60085804292609,
2.69372336912999,2.74018787352896,2.8346144003695,2.92270245416146,3.02438495680549,
3.11184323544286,3.17817324820249),.UNSPECIFIED.);
#637=B_SPLINE_CURVE_WITH_KNOTS('',3,(#42503,#42504,#42505,#42506,#42507,
#42508,#42509,#42510,#42511,#42512,#42513,#42514),.UNSPECIFIED.,.F.,.F.,
(4,2,2,2,2,4),(1.58610784508116,1.65359225971699,1.70251946683584,1.79015455082039,
1.88930640561349,1.97403018723799),.UNSPECIFIED.);
#638=B_SPLINE_CURVE_WITH_KNOTS('',3,(#42515,#42516,#42517,#42518,#42519,
#42520,#42521,#42522,#42523,#42524,#42525,#42526,#42527,#42528,#42529,#42530,
#42531,#42532,#42533,#42534,#42535,#42536,#42537,#42538,#42539,#42540,#42541,
#42542,#42543,#42544,#42545,#42546,#42547,#42548,#42549,#42550,#42551,#42552,
#42553,#42554,#42555,#42556,#42557,#42558,#42559,#42560,#42561,#42562,#42563,
#42564,#42565,#42566,#42567,#42568,#42569,#42570,#42571,#42572,#42573,#42574,
#42575,#42576,#42577,#42578,#42579,#42580,#42581,#42582,#42583,#42584,#42585,
#42586,#42587,#42588,#42589,#42590,#42591,#42592,#42593,#42594,#42595,#42596,
#42597,#42598,#42599,#42600,#42601,#42602,#42603,#42604,#42605,#42606,#42607,
#42608,#42609,#42610,#42611,#42612,#42613,#42614,#42615,#42616,#42617,#42618,
#42619,#42620,#42621,#42622,#42623,#42624,#42625,#42626,#42627,#42628,#42629,
#42630,#42631,#42632,#42633,#42634,#42635,#42636,#42637,#42638,#42639,#42640,
#42641,#42642,#42643,#42644,#42645,#42646,#42647,#42648,#42649,#42650,#42651,
#42652,#42653,#42654,#42655,#42656,#42657,#42658,#42659,#42660,#42661,#42662,
#42663,#42664,#42665,#42666,#42667,#42668,#42669,#42670,#42671,#42672,#42673,
#42674,#42675,#42676,#42677,#42678,#42679,#42680,#42681,#42682,#42683,#42684,
#42685,#42686,#42687,#42688,#42689,#42690,#42691,#42692,#42693,#42694,#42695,
#42696,#42697,#42698,#42699,#42700,#42701,#42702,#42703,#42704,#42705,#42706,
#42707,#42708,#42709,#42710,#42711,#42712,#42713,#42714,#42715,#42716,#42717,
#42718,#42719,#42720,#42721,#42722,#42723,#42724,#42725,#42726,#42727,#42728,
#42729,#42730,#42731,#42732,#42733,#42734,#42735,#42736,#42737,#42738,#42739,
#42740,#42741,#42742,#42743),.UNSPECIFIED.,.F.,.F.,(4,3,3,3,3,3,3,3,3,3,
3,3,3,3,3,3,3,3,3,3,3,3,3,3,3,3,3,3,3,3,3,3,3,3,3,3,3,3,3,3,3,3,3,3,3,3,
3,3,3,3,3,3,3,3,3,3,3,3,3,3,3,3,3,3,3,3,3,3,3,3,3,3,3,3,3,3,4),(1.97046892380326E-7,
0.0165119087567328,0.0269521658292449,0.0514461508287838,0.053986697928493,
0.061957278941543,0.0619660940702222,0.0868551258564478,0.088772735096238,
0.10212602798035,0.129068676009789,0.156011324039229,0.156013890995603,
0.182913548427808,0.203854870580913,0.230701706835421,0.250045675689164,
0.250051837794113,0.27563745285687,0.277653721785625,0.305261767882086,
0.331953297927535,0.358937695991391,0.375451509787054,0.375458910130687,
0.400443220256602,0.402335123360528,0.406329654807662,0.432917759153746,
0.459832615589691,0.486691726360605,0.500788281582239,0.500791362256077,
0.507021309259397,0.533457855496874,0.560290345237192,0.587164758587564,
0.60737646809822,0.626070235128599,0.626079280624986,0.651201536368465,
0.652547853164669,0.680012430295542,0.707477007426416,0.734272256537736,
0.758887457771652,0.761271581217608,0.767098043492731,0.767106729118364,
0.791557876361479,0.793988196663842,0.807311994887596,0.833990067833167,
0.860961066123945,0.887784201963004,0.906820884562021,0.908051502841903,
0.908056675451242,0.934357362767099,0.961121352560656,0.988069529586017,
1.00602353353002,1.03072380463237,1.03297061250337,1.04901367065168,1.04902053837709,
1.07372752541493,1.07700485902145,1.10321909090914,1.10499604739123,1.1317485186321,
1.15875797074834,1.1836094806426,1.18562638883337,1.19002244111504,1.19003005836486,
1.20016986403664),.UNSPECIFIED.);
#639=B_SPLINE_CURVE_WITH_KNOTS('',3,(#42745,#42746,#42747,#42748,#42749,
#42750,#42751,#42752,#42753,#42754,#42755,#42756,#42757,#42758,#42759,#42760,
#42761,#42762),.UNSPECIFIED.,.F.,.F.,(4,2,2,2,2,2,2,2,4),(3.17817324820249,
3.21334005896499,3.30095732570528,3.40212874114706,3.48932390867776,3.59034661861351,
3.67575648182955,3.77639745946347,3.87258558614326),.UNSPECIFIED.);
#640=B_SPLINE_CURVE_WITH_KNOTS('',3,(#42763,#42764,#42765,#42766,#42767,
#42768,#42769,#42770,#42771,#42772,#42773,#42774,#42775,#42776,#42777,#42778,
#42779,#42780,#42781,#42782,#42783,#42784,#42785,#42786,#42787,#42788,#42789,
#42790,#42791,#42792,#42793,#42794,#42795,#42796,#42797,#42798,#42799,#42800,
#42801,#42802,#42803,#42804,#42805,#42806,#42807,#42808,#42809,#42810,#42811,
#42812,#42813,#42814,#42815,#42816,#42817,#42818,#42819,#42820,#42821,#42822,
#42823,#42824,#42825,#42826,#42827,#42828,#42829,#42830,#42831,#42832,#42833,
#42834,#42835,#42836,#42837,#42838,#42839,#42840,#42841,#42842,#42843,#42844,
#42845,#42846,#42847,#42848,#42849,#42850,#42851,#42852,#42853,#42854,#42855,
#42856,#42857,#42858,#42859,#42860,#42861,#42862,#42863,#42864,#42865,#42866,
#42867,#42868,#42869,#42870,#42871,#42872,#42873,#42874,#42875,#42876,#42877,
#42878,#42879,#42880,#42881,#42882,#42883,#42884,#42885,#42886,#42887,#42888,
#42889,#42890,#42891,#42892,#42893,#42894,#42895,#42896,#42897,#42898,#42899,
#42900,#42901,#42902,#42903,#42904,#42905,#42906,#42907,#42908,#42909,#42910,
#42911,#42912,#42913,#42914,#42915,#42916,#42917,#42918,#42919,#42920,#42921,
#42922,#42923,#42924,#42925,#42926,#42927,#42928),.UNSPECIFIED.,.F.,.F.,
(4,3,3,3,3,3,3,3,3,3,3,3,3,3,3,3,3,3,3,3,3,3,3,3,3,3,3,3,3,3,3,3,3,3,3,
3,3,3,3,3,3,3,3,3,3,3,3,3,3,3,3,3,3,3,3,4),(0.00195662276257164,0.0057265082120884,
0.00778343510459544,0.0262434362367702,0.0277363971949173,0.0324316244813748,
0.0591912596596283,0.0860114790298136,0.109672947671685,0.109673851626103,
0.12794618277961,0.154104266777492,0.180854266012755,0.193566709158549,
0.193570035685709,0.220316211357797,0.223705859480335,0.250575073070551,
0.275935977789185,0.277441778425786,0.277444286660766,0.302811945533245,
0.304181269015732,0.319745719238003,0.346298818737683,0.373152022009375,
0.399880935631714,0.416128760511614,0.440487000619039,0.443011467604648,
0.445160535678054,0.44516262425229,0.470169452132286,0.471533399549815,
0.49837210907613,0.512757329921647,0.539487448178301,0.566398841468605,
0.592995666409934,0.60958270433084,0.612904438499428,0.612904942401022,
0.639055399317768,0.665682621424802,0.692541721428282,0.706686554608931,
0.733464686518852,0.758577078163878,0.76027290818244,0.780655324452018,
0.7806575379144,0.804084831935261,0.830443692926505,0.857216066700044,0.884077928685615,
0.896610673280827),.UNSPECIFIED.);
#641=B_SPLINE_CURVE_WITH_KNOTS('',3,(#42933,#42934,#42935,#42936,#42937,
#42938,#42939,#42940,#42941,#42942,#42943,#42944,#42945,#42946,#42947,#42948,
#42949,#42950,#42951,#42952,#42953,#42954,#42955,#42956,#42957,#42958,#42959,
#42960,#42961,#42962,#42963,#42964,#42965,#42966,#42967,#42968,#42969,#42970,
#42971,#42972,#42973,#42974),.UNSPECIFIED.,.F.,.F.,(4,2,2,2,2,2,2,2,2,2,
2,2,2,2,2,2,2,2,2,2,4),(5.61108670082191E-6,0.0521038174851644,0.0935393401420401,
0.163487238226365,0.245209849008126,0.340133440268412,0.408755389589607,
0.509893079867885,0.608823499223934,0.699926438388842,0.797522199540615,
0.89858838991344,0.986966947055123,1.03605369324,1.12548372504641,1.22653559591547,
1.32179905784751,1.37055336956388,1.45918131120364,1.5599602720752,1.58610784508116),
 .UNSPECIFIED.);
#642=B_SPLINE_CURVE_WITH_KNOTS('',3,(#42976,#42977,#42978,#42979),
 .UNSPECIFIED.,.F.,.F.,(4,4),(0.896610673280827,0.896791920131866),
 .UNSPECIFIED.);
#643=B_SPLINE_CURVE_WITH_KNOTS('',3,(#42980,#42981,#42982,#42983,#42984,
#42985,#42986,#42987,#42988,#42989,#42990,#42991,#42992,#42993,#42994,#42995,
#42996,#42997,#42998,#42999,#43000,#43001,#43002,#43003,#43004,#43005,#43006,
#43007,#43008,#43009,#43010,#43011,#43012,#43013,#43014,#43015,#43016,#43017,
#43018,#43019),.UNSPECIFIED.,.F.,.F.,(4,2,2,2,2,2,2,2,2,2,2,2,2,2,2,2,2,
2,2,4),(5.2177231840437E-6,0.0530311686959936,0.114759217257224,0.211495904314178,
0.312968826970064,0.361760349371721,0.455764780613197,0.555669062486527,
0.605170600274074,0.70403338905179,0.804954817122082,0.906215196147122,
0.955080727331366,1.05100054971597,1.15212735488212,1.19901836385656,1.30009856105027,
1.39113241409266,1.49270447321307,1.58736511801968),.UNSPECIFIED.);
#644=B_SPLINE_CURVE_WITH_KNOTS('',3,(#43022,#43023,#43024,#43025,#43026,
#43027,#43028,#43029,#43030,#43031,#43032,#43033,#43034,#43035,#43036,#43037,
#43038,#43039,#43040,#43041,#43042,#43043,#43044,#43045),.UNSPECIFIED.,
 .F.,.F.,(4,2,2,2,2,2,2,2,2,2,2,4),(1.58736511801968,1.59210150155741,1.68173808769121,
1.72911766226968,1.82832409000194,1.92646536051439,2.01577372818829,2.06358998938427,
2.16172397625675,2.25737672526083,2.33277369713274,2.39803079505187),
 .UNSPECIFIED.);
#645=B_SPLINE_CURVE_WITH_KNOTS('',3,(#43047,#43048,#43049,#43050,#43051,
#43052,#43053,#43054,#43055,#43056,#43057,#43058,#43059,#43060,#43061,#43062,
#43063,#43064,#43065,#43066),.UNSPECIFIED.,.F.,.F.,(4,2,2,2,2,2,2,2,2,4),
(3.30476667653425E-5,0.0730119917909342,0.155321911197543,0.246835800980314,
0.348560854775418,0.439795908011992,0.541409392577865,0.6324553637244,0.681210482541812,
0.775512523779579),.UNSPECIFIED.);
#646=B_SPLINE_CURVE_WITH_KNOTS('',3,(#43070,#43071,#43072,#43073,#43074,
#43075,#43076,#43077,#43078,#43079),.UNSPECIFIED.,.F.,.F.,(4,2,2,2,4),(3.172018184782,
3.2383509868975,3.33901616963149,3.39429588367164,3.44364720042429),
 .UNSPECIFIED.);
#647=B_SPLINE_CURVE_WITH_KNOTS('',3,(#43080,#43081,#43082,#43083,#43084,
#43085,#43086,#43087,#43088,#43089,#43090,#43091,#43092,#43093,#43094,#43095,
#43096,#43097,#43098,#43099,#43100,#43101,#43102,#43103,#43104,#43105,#43106,
#43107,#43108,#43109,#43110,#43111,#43112,#43113,#43114,#43115),
 .UNSPECIFIED.,.F.,.F.,(4,2,2,2,2,2,2,2,2,2,2,2,2,2,2,2,2,4),(7.85099826035063E-5,
0.0835230548401281,0.176109879532006,0.268759385921064,0.370729149112131,
0.41970804661686,0.517513704143356,0.610332470955531,0.659293399050333,
0.706602751260405,0.807760001799314,0.856191841693314,0.95014160834287,
1.0514708942237,1.09993161210594,1.20132087842412,1.25267680689251,1.31839655317403),
 .UNSPECIFIED.);
#648=B_SPLINE_CURVE_WITH_KNOTS('',3,(#43120,#43121,#43122,#43123,#43124,
#43125,#43126,#43127,#43128,#43129,#43130,#43131,#43132,#43133,#43134,#43135,
#43136,#43137,#43138,#43139,#43140,#43141,#43142,#43143,#43144,#43145,#43146,
#43147,#43148,#43149,#43150,#43151,#43152,#43153,#43154,#43155,#43156,#43157,
#43158,#43159,#43160,#43161,#43162,#43163),.UNSPECIFIED.,.F.,.F.,(4,2,2,
2,2,2,2,2,2,2,2,2,2,2,2,2,2,2,2,2,2,4),(1.58714917405264,1.62487059328602,
1.67310993772542,1.72192229587615,1.81681073323228,1.86584217015149,1.96083596104287,
2.05613974965739,2.1040867325538,2.20532404072983,2.29897571506993,2.39974218606846,
2.48518687077461,2.5858894241594,2.66994998309819,2.77075629546814,2.86902915491451,
2.91827951445788,3.01205343509936,3.10410692331575,3.15229172786727,3.172018184782),
 .UNSPECIFIED.);
#649=B_SPLINE_CURVE_WITH_KNOTS('',3,(#43165,#43166,#43167,#43168,#43169,
#43170,#43171,#43172,#43173,#43174,#43175,#43176,#43177,#43178,#43179,#43180,
#43181,#43182,#43183,#43184,#43185,#43186,#43187,#43188,#43189,#43190,#43191,
#43192,#43193,#43194,#43195,#43196),.UNSPECIFIED.,.F.,.F.,(4,2,2,2,2,2,
2,2,2,2,2,2,2,2,2,4),(0.775512523779579,0.777139842577585,0.827904318957342,
0.876647272001025,0.977538689119265,1.07725466162777,1.12517655585581,1.22408411710603,
1.27204087343801,1.3204700519371,1.42213731037915,1.47124250018406,1.57003316977662,
1.61591228478928,1.68722356316175,1.75326419407806),.UNSPECIFIED.);
#650=B_SPLINE_CURVE_WITH_KNOTS('',3,(#43198,#43199,#43200,#43201,#43202,
#43203,#43204,#43205,#43206,#43207,#43208,#43209,#43210,#43211,#43212,#43213,
#43214,#43215,#43216,#43217,#43218,#43219,#43220,#43221,#43222,#43223,#43224,
#43225,#43226,#43227,#43228,#43229,#43230,#43231,#43232,#43233,#43234,#43235,
#43236,#43237,#43238,#43239,#43240,#43241,#43242,#43243,#43244,#43245,#43246,
#43247,#43248,#43249,#43250,#43251,#43252,#43253,#43254,#43255,#43256,#43257,
#43258,#43259,#43260,#43261,#43262,#43263,#43264,#43265,#43266,#43267,#43268,
#43269,#43270,#43271,#43272,#43273,#43274,#43275,#43276,#43277,#43278,#43279,
#43280,#43281,#43282,#43283,#43284,#43285,#43286,#43287,#43288,#43289,#43290,
#43291,#43292,#43293,#43294,#43295,#43296,#43297,#43298,#43299,#43300,#43301,
#43302,#43303),.UNSPECIFIED.,.F.,.F.,(4,3,3,3,3,3,3,3,3,3,3,3,3,3,3,3,3,
3,3,3,3,3,3,3,3,3,3,3,3,3,3,3,3,3,3,4),(0.,0.0223542576374909,0.0267832089461343,
0.0537106663391406,0.0806381237321469,0.0806454974621168,0.101827263080174,
0.128174021766349,0.1549636261091,0.181852320077753,0.203530354517993,0.228884303326543,
0.230456690199924,0.248570803195244,0.248582233437807,0.275068797818176,
0.301942959046185,0.305135333726472,0.331789806526895,0.358710123188655,
0.385428062240576,0.406659177973182,0.416447614847817,0.416448913630405,
0.442731090245464,0.46946613570733,0.496338911638681,0.508111106730458,
0.534947029113335,0.559945964594669,0.561774837982785,0.584338701001998,
0.584339726650227,0.608125666318232,0.609500547121593,0.611296099258107),
 .UNSPECIFIED.);
#651=B_SPLINE_CURVE_WITH_KNOTS('',3,(#43304,#43305,#43306,#43307),
 .UNSPECIFIED.,.F.,.F.,(4,4),(5.08580690585039E-5,0.000161519520353054),
 .UNSPECIFIED.);
#652=B_SPLINE_CURVE_WITH_KNOTS('',3,(#43313,#43314,#43315,#43316),
 .UNSPECIFIED.,.F.,.F.,(4,4),(1.06238567890844,1.06246996364553),
 .UNSPECIFIED.);
#653=B_SPLINE_CURVE_WITH_KNOTS('',3,(#43317,#43318,#43319,#43320,#43321,
#43322,#43323,#43324,#43325,#43326,#43327,#43328,#43329,#43330,#43331,#43332,
#43333,#43334,#43335,#43336,#43337,#43338,#43339,#43340,#43341,#43342,#43343,
#43344,#43345,#43346,#43347,#43348,#43349,#43350,#43351,#43352,#43353,#43354,
#43355,#43356,#43357,#43358,#43359,#43360,#43361,#43362,#43363,#43364),
 .UNSPECIFIED.,.F.,.F.,(4,2,2,2,2,2,2,2,2,2,2,2,2,2,2,2,2,2,2,2,2,2,2,4),
(1.00000016286752E-6,0.0862068928556652,0.185952757554959,0.253237461541151,
0.355299607682124,0.401863096771156,0.499562116678737,0.547297339803957,
0.597392338041793,0.646548704907709,0.747322930923275,0.795434512205605,
0.844803214979016,0.938204332302665,0.989388740266747,1.03857369442406,
1.08668491424657,1.18649323610714,1.23607437025058,1.33703207912544,1.43013146949498,
1.47866234274992,1.57414919062349,1.58714917405264),.UNSPECIFIED.);
#654=B_SPLINE_CURVE_WITH_KNOTS('',3,(#43365,#43366,#43367,#43368,#43369,
#43370,#43371,#43372,#43373,#43374,#43375,#43376,#43377,#43378,#43379,#43380,
#43381,#43382,#43383,#43384,#43385,#43386,#43387,#43388,#43389,#43390,#43391,
#43392,#43393,#43394,#43395,#43396,#43397,#43398,#43399,#43400,#43401,#43402,
#43403,#43404,#43405,#43406),.UNSPECIFIED.,.F.,.F.,(4,2,2,2,2,2,2,2,2,2,
2,2,2,2,2,2,2,2,2,2,4),(0.000161519520353054,0.0575337694029372,0.103369793689619,
0.181155008716227,0.278801444853426,0.378970141096557,0.450655431577042,
0.55217277736237,0.652186775252743,0.699348984508397,0.79445576961415,0.896119705397044,
0.993989743294838,1.09193882160934,1.19250903312403,1.27385529020416,1.31754056768087,
1.4189329957357,1.50211835110858,1.54743432722965,1.58876261697574),
 .UNSPECIFIED.);
#655=B_SPLINE_CURVE_WITH_KNOTS('',3,(#43412,#43413,#43414,#43415,#43416,
#43417,#43418,#43419,#43420,#43421,#43422,#43423,#43424,#43425,#43426,#43427),
 .UNSPECIFIED.,.F.,.F.,(4,2,2,2,2,2,2,4),(1.58640007399783,1.64139361802863,
1.73124878129425,1.77890017001795,1.87864360161113,1.97454422453998,2.04996787109459,
2.11556527080477),.UNSPECIFIED.);
#656=B_SPLINE_CURVE_WITH_KNOTS('',3,(#43428,#43429,#43430,#43431,#43432,
#43433,#43434,#43435,#43436,#43437,#43438,#43439,#43440,#43441,#43442,#43443,
#43444,#43445,#43446,#43447,#43448,#43449,#43450,#43451,#43452,#43453,#43454,
#43455),.UNSPECIFIED.,.F.,.F.,(4,2,2,2,2,2,2,2,2,2,2,2,2,4),(6.24427194408881E-5,
0.07322487298628,0.159468398207204,0.247468541542693,0.342187470127241,
0.39026831901386,0.481724140650963,0.531314422375744,0.632816993761995,
0.731666562356075,0.833221392964525,0.934705130830227,0.992889032154437,
1.06238567890844),.UNSPECIFIED.);
#657=B_SPLINE_CURVE_WITH_KNOTS('',3,(#43457,#43458,#43459,#43460),
 .UNSPECIFIED.,.F.,.F.,(4,4),(1.58876261697574,1.58885620615735),
 .UNSPECIFIED.);
#658=B_SPLINE_CURVE_WITH_KNOTS('',3,(#43462,#43463,#43464,#43465,#43466,
#43467,#43468,#43469,#43470,#43471,#43472,#43473,#43474,#43475,#43476,#43477,
#43478,#43479,#43480,#43481,#43482,#43483,#43484,#43485,#43486,#43487,#43488,
#43489,#43490,#43491),.UNSPECIFIED.,.F.,.F.,(4,2,2,2,2,2,2,2,2,2,2,2,2,
2,4),(1.00000006509386E-6,0.0682125041812062,0.143755754402067,0.235144527123705,
0.285235038132226,0.385699790431721,0.433437205858489,0.533041599863107,
0.633814101828482,0.723255246139578,0.823934860858259,0.918280079420942,
0.959774675011753,1.01516523885657,1.06608140280668),.UNSPECIFIED.);
#659=B_SPLINE_CURVE_WITH_KNOTS('',3,(#43492,#43493,#43494,#43495,#43496,
#43497,#43498,#43499,#43500,#43501,#43502,#43503,#43504,#43505,#43506,#43507,
#43508,#43509,#43510,#43511,#43512,#43513,#43514,#43515,#43516,#43517,#43518,
#43519,#43520,#43521,#43522,#43523,#43524,#43525,#43526,#43527,#43528,#43529,
#43530,#43531,#43532,#43533,#43534,#43535,#43536,#43537,#43538,#43539,#43540,
#43541,#43542,#43543,#43544,#43545,#43546,#43547,#43548,#43549,#43550,#43551,
#43552,#43553,#43554,#43555,#43556,#43557,#43558,#43559,#43560,#43561,#43562,
#43563,#43564,#43565,#43566,#43567,#43568,#43569,#43570,#43571,#43572,#43573,
#43574,#43575,#43576,#43577,#43578,#43579,#43580,#43581,#43582),
 .UNSPECIFIED.,.F.,.F.,(4,3,3,3,3,3,3,3,3,3,3,3,3,3,3,3,3,3,3,3,3,3,3,3,
3,3,3,3,3,3,4),(4.29564213299729E-5,0.0223677416501253,0.0260479680645344,
0.0525003704776632,0.0789988343680503,0.101747215251029,0.128400865748245,
0.141656975489527,0.141658872579743,0.167838207053778,0.194409625139364,
0.203377866560224,0.229878293290454,0.256578496059846,0.282984477837726,
0.304921755801306,0.309301818525669,0.309302371754537,0.33528185162595,
0.361716897293269,0.388345503430247,0.393231851464744,0.393232990413532,
0.406390647464245,0.432857974016374,0.459538001164057,0.477156228609294,
0.477156985334002,0.50380408957998,0.507799457538043,0.523223944008924),
 .UNSPECIFIED.);
#660=B_SPLINE_CURVE_WITH_KNOTS('',3,(#43588,#43589,#43590,#43591),
 .UNSPECIFIED.,.F.,.F.,(4,4),(1.1543754051628,1.15472425279361),
 .UNSPECIFIED.);
#661=B_SPLINE_CURVE_WITH_KNOTS('',3,(#43592,#43593,#43594,#43595,#43596,
#43597,#43598,#43599,#43600,#43601,#43602,#43603,#43604,#43605,#43606,#43607,
#43608,#43609,#43610,#43611,#43612,#43613,#43614,#43615,#43616,#43617,#43618,
#43619,#43620,#43621,#43622,#43623,#43624,#43625,#43626,#43627,#43628,#43629,
#43630,#43631,#43632,#43633),.UNSPECIFIED.,.F.,.F.,(4,2,2,2,2,2,2,2,2,2,
2,2,2,2,2,2,2,2,2,2,4),(1.00000007275659E-6,0.0559430608918217,0.118052148831411,
0.219093370540287,0.31153943656164,0.39946568280495,0.493720317281655,0.565610392093586,
0.666574137732805,0.764328770373596,0.863333475800359,0.911061255280105,
1.01027931209133,1.05782504393973,1.10453551958502,1.20560998841793,1.30342902587861,
1.35176877208222,1.44239422836734,1.54378429828248,1.58640007399783),
 .UNSPECIFIED.);
#662=B_SPLINE_CURVE_WITH_KNOTS('',3,(#43634,#43635,#43636,#43637,#43638,
#43639,#43640,#43641,#43642,#43643,#43644,#43645,#43646,#43647,#43648,#43649,
#43650,#43651,#43652,#43653,#43654,#43655,#43656,#43657,#43658,#43659,#43660,
#43661,#43662,#43663,#43664,#43665,#43666,#43667,#43668,#43669,#43670,#43671,
#43672,#43673,#43674,#43675,#43676,#43677),.UNSPECIFIED.,.F.,.F.,(4,2,2,
2,2,2,2,2,2,2,2,2,2,2,2,2,2,2,2,2,2,4),(1.69660442820801E-5,0.0621727637931074,
0.130603354249022,0.177156779445226,0.274547260879537,0.322784074818011,
0.424774095589815,0.522858893257094,0.614218395466428,0.710184977845561,
0.760102124203472,0.809561950944269,0.909508918270125,0.957396684954257,
1.05866387333694,1.15989818588819,1.20802386750222,1.30924683729453,1.41072994296973,
1.45924151970641,1.56039389518965,1.59029600936748),.UNSPECIFIED.);
#663=B_SPLINE_CURVE_WITH_KNOTS('',3,(#43681,#43682,#43683,#43684,#43685,
#43686,#43687,#43688,#43689,#43690,#43691,#43692,#43693,#43694),
 .UNSPECIFIED.,.F.,.F.,(4,2,2,2,2,2,4),(1.00000008239902E-6,0.0861469959055848,
0.16752892050755,0.218403038515653,0.313556177494288,0.377493724390283,
0.436724401093653),.UNSPECIFIED.);
#664=B_SPLINE_CURVE_WITH_KNOTS('',3,(#43695,#43696,#43697,#43698,#43699,
#43700,#43701,#43702,#43703,#43704,#43705,#43706,#43707,#43708,#43709,#43710,
#43711,#43712,#43713,#43714,#43715,#43716,#43717,#43718,#43719,#43720,#43721,
#43722,#43723,#43724),.UNSPECIFIED.,.F.,.F.,(4,2,2,2,2,2,2,2,2,2,2,2,2,
2,4),(9.80168944251376E-5,0.0680801262020133,0.14586143617603,0.240637522592241,
0.342636008430395,0.429957466029602,0.479549005869444,0.57745774353028,
0.679413618393056,0.780274067553753,0.82957824766732,0.922751478636959,
1.02443351086548,1.0866638759187,1.1543754051628),.UNSPECIFIED.);
#665=B_SPLINE_CURVE_WITH_KNOTS('',3,(#43726,#43727,#43728,#43729,#43730,
#43731,#43732,#43733,#43734,#43735,#43736,#43737,#43738,#43739,#43740,#43741,
#43742,#43743,#43744,#43745,#43746,#43747,#43748,#43749,#43750,#43751,#43752,
#43753,#43754,#43755,#43756,#43757,#43758,#43759,#43760,#43761,#43762,#43763,
#43764,#43765,#43766,#43767,#43768,#43769),.UNSPECIFIED.,.F.,.F.,(4,2,2,
2,2,2,2,2,2,2,2,2,2,2,2,2,2,2,2,2,2,4),(1.59029600936748,1.66099639496899,
1.70972552920993,1.75826113830702,1.8555767844832,1.90658130165602,1.99380312867189,
2.0415571279748,2.12874854987234,2.23031052191635,2.32543416384813,2.37432218963118,
2.46222816392711,2.56316053006413,2.65050249863099,2.75143612038196,2.83483132107615,
2.93564925455118,3.01983818334638,3.12056610545761,3.1647596713537,3.17771221179641),
 .UNSPECIFIED.);
#666=B_SPLINE_CURVE_WITH_KNOTS('',3,(#43776,#43777,#43778,#43779,#43780,
#43781,#43782,#43783,#43784,#43785),.UNSPECIFIED.,.F.,.F.,(4,2,2,2,4),(3.0201138090629,
3.05453144613298,3.14992585636195,3.22599329218501,3.2916937650692),
 .UNSPECIFIED.);
#667=B_SPLINE_CURVE_WITH_KNOTS('',3,(#43786,#43787,#43788,#43789,#43790,
#43791,#43792,#43793,#43794,#43795,#43796,#43797,#43798,#43799,#43800,#43801,
#43802,#43803,#43804,#43805,#43806,#43807,#43808,#43809,#43810,#43811,#43812,
#43813,#43814,#43815,#43816,#43817,#43818,#43819,#43820,#43821),
 .UNSPECIFIED.,.F.,.F.,(4,2,2,2,2,2,2,2,2,2,2,2,2,2,2,2,2,4),(1.0958252776401E-5,
0.092418778574395,0.192596706540116,0.293780595397689,0.378232209619974,
0.479502465400529,0.578999118141845,0.6577822457542,0.7066707546433,0.753368584600514,
0.854537225797866,0.903434258597658,1.00440369535868,1.05343457647593,1.10352028314666,
1.19797564688056,1.25878976507826,1.31553845584881),.UNSPECIFIED.);
#668=B_SPLINE_CURVE_WITH_KNOTS('',3,(#43823,#43824,#43825,#43826,#43827,
#43828,#43829,#43830,#43831,#43832,#43833,#43834,#43835,#43836,#43837,#43838,
#43839,#43840,#43841,#43842,#43843,#43844),.UNSPECIFIED.,.F.,.F.,(4,2,2,
2,2,2,2,2,2,2,4),(3.17771221179641,3.26518167660643,3.35089729791118,3.44993600095358,
3.49741136148196,3.57932065032728,3.68014994637309,3.76186490783962,3.80876819856172,
3.90286034910187,3.98725875054216),.UNSPECIFIED.);
#669=B_SPLINE_CURVE_WITH_KNOTS('',3,(#43845,#43846,#43847,#43848,#43849,
#43850,#43851,#43852,#43853,#43854,#43855,#43856,#43857,#43858,#43859,#43860,
#43861,#43862,#43863,#43864),.UNSPECIFIED.,.F.,.F.,(4,2,2,2,2,2,2,2,2,4),
(0.000416008717854399,0.0789160364521911,0.16820016970267,0.263721702794877,
0.364559327860852,0.41321857398184,0.511236725439311,0.601083545522871,
0.702713773320289,0.779618357029204),.UNSPECIFIED.);
#670=B_SPLINE_CURVE_WITH_KNOTS('',3,(#43869,#43870,#43871,#43872,#43873,
#43874,#43875,#43876,#43877,#43878,#43879,#43880,#43881,#43882,#43883,#43884,
#43885,#43886,#43887,#43888,#43889,#43890,#43891,#43892,#43893,#43894,#43895,
#43896,#43897,#43898,#43899,#43900,#43901,#43902,#43903,#43904,#43905,#43906,
#43907,#43908,#43909,#43910),.UNSPECIFIED.,.F.,.F.,(4,2,2,2,2,2,2,2,2,2,
2,2,2,2,2,2,2,2,2,2,4),(1.43368549808538,1.4979818748124,1.59722154075269,
1.64585489812321,1.74723097068974,1.79558854641402,1.89662306941936,1.94406137704963,
2.04514199145719,2.143137685293,2.19150536074381,2.28211255975149,2.38304812520079,
2.48116627820141,2.57177924368629,2.61913455000118,2.7202429392984,2.81788847408514,
2.90768888907198,2.95549757298729,3.0201138090629),.UNSPECIFIED.);
#671=B_SPLINE_CURVE_WITH_KNOTS('',3,(#43911,#43912,#43913,#43914,#43915,
#43916,#43917,#43918,#43919,#43920,#43921,#43922,#43923,#43924,#43925,#43926,
#43927,#43928,#43929,#43930,#43931,#43932,#43933,#43934,#43935,#43936,#43937,
#43938,#43939,#43940,#43941,#43942,#43943,#43944,#43945,#43946,#43947,#43948,
#43949,#43950),.UNSPECIFIED.,.F.,.F.,(4,2,2,2,2,2,2,2,2,2,2,2,2,2,2,2,2,
2,2,4),(0.779618357029204,0.802803112888372,0.883979095536384,0.982406118287473,
1.08387046468192,1.18507915430368,1.27523848509429,1.37664382134265,1.45559685079245,
1.49947953640491,1.60087007831783,1.6482837684803,1.74839371188088,1.84038573945747,
1.92318528656684,2.02304617346582,2.1129309070806,2.21416610470643,2.28802740994192,
2.370068662874),.UNSPECIFIED.);
#672=B_SPLINE_CURVE_WITH_KNOTS('',3,(#43956,#43957,#43958,#43959,#43960,
#43961),.UNSPECIFIED.,.F.,.F.,(4,2,4),(3.17236617648777,3.24318852578899,
3.32825735645484),.UNSPECIFIED.);
#673=B_SPLINE_CURVE_WITH_KNOTS('',3,(#43962,#43963,#43964,#43965,#43966,
#43967,#43968,#43969,#43970,#43971,#43972,#43973,#43974,#43975,#43976,#43977,
#43978,#43979,#43980,#43981,#43982,#43983,#43984,#43985,#43986,#43987,#43988,
#43989,#43990,#43991,#43992,#43993,#43994,#43995,#43996,#43997,#43998,#43999),
 .UNSPECIFIED.,.F.,.F.,(4,2,2,2,2,2,2,2,2,2,2,2,2,2,2,2,2,2,4),(4.69863450241475E-6,
0.0732561627926064,0.15152434590406,0.200526515945472,0.294383845688464,
0.389747970553781,0.486785957457453,0.536554022637231,0.585543930501015,
0.673421563000948,0.770749466128403,0.846941804556702,0.948162354569468,
1.04068442063129,1.13302357768077,1.22937273149936,1.30336321367283,1.40435174774173,
1.43368549808538),.UNSPECIFIED.);
#674=B_SPLINE_CURVE_WITH_KNOTS('',3,(#44001,#44002,#44003,#44004,#44005,
#44006,#44007,#44008,#44009,#44010,#44011,#44012,#44013,#44014,#44015,#44016,
#44017,#44018,#44019,#44020,#44021,#44022,#44023,#44024,#44025,#44026),
 .UNSPECIFIED.,.F.,.F.,(4,2,2,2,2,2,2,2,2,2,2,2,4),(2.78339753933959E-5,
0.081948818254421,0.171142740482219,0.263745465431853,0.314368120177807,
0.415241291507573,0.463391677990754,0.551622304139495,0.59977844847948,
0.694775022006912,0.742068116649189,0.841854494119041,0.9268893973431),
 .UNSPECIFIED.);
#675=B_SPLINE_CURVE_WITH_KNOTS('',3,(#44027,#44028,#44029,#44030,#44031,
#44032,#44033,#44034,#44035,#44036,#44037,#44038,#44039,#44040,#44041,#44042,
#44043,#44044,#44045,#44046,#44047,#44048,#44049,#44050,#44051,#44052,#44053,
#44054,#44055,#44056,#44057,#44058,#44059,#44060,#44061,#44062,#44063,#44064,
#44065,#44066,#44067,#44068,#44069,#44070,#44071,#44072,#44073,#44074,#44075,
#44076,#44077,#44078,#44079,#44080,#44081,#44082,#44083,#44084,#44085,#44086,
#44087,#44088,#44089,#44090,#44091,#44092,#44093,#44094,#44095,#44096,#44097,
#44098,#44099,#44100,#44101,#44102,#44103,#44104,#44105,#44106,#44107,#44108,
#44109,#44110,#44111,#44112,#44113,#44114,#44115,#44116,#44117,#44118,#44119,
#44120,#44121,#44122,#44123,#44124,#44125,#44126,#44127,#44128,#44129,#44130,
#44131,#44132,#44133,#44134,#44135,#44136,#44137,#44138,#44139,#44140,#44141,
#44142,#44143,#44144,#44145,#44146,#44147,#44148,#44149,#44150,#44151,#44152,
#44153,#44154,#44155,#44156),.UNSPECIFIED.,.F.,.F.,(4,3,3,3,3,3,3,3,3,3,
3,3,3,3,3,3,3,3,3,3,3,3,3,3,3,3,3,3,3,3,3,3,3,3,3,3,3,3,3,3,3,3,3,4),(5.40439274532324E-8,
0.0176084116492507,0.0269444774751041,0.0512050753871218,0.0539556220322877,
0.0630337718589102,0.0630394189146231,0.087122863216934,0.0898661186384374,
0.102147910187398,0.128657264222907,0.155580733384103,0.18254235728964,
0.203860958424688,0.227729591399546,0.230883610031478,0.251120014207219,
0.251131374633248,0.274693170456122,0.278168215719489,0.302781642299717,
0.305216417231759,0.331840197301536,0.358832442830213,0.385767896852117,
0.406270766662611,0.429577811886119,0.433319718368037,0.439138755580813,
0.439145684566976,0.46302409972116,0.465591224746269,0.490728914473221,
0.492579509125595,0.506987157359231,0.53377820352076,0.560836181114381,
0.587691673133311,0.607343110066019,0.627140086067375,0.627173899054037,
0.651460955435538,0.6536906004346,0.659723809344152),.UNSPECIFIED.);
#676=B_SPLINE_CURVE_WITH_KNOTS('',3,(#44161,#44162,#44163,#44164,#44165,
#44166,#44167,#44168,#44169,#44170,#44171,#44172,#44173,#44174,#44175,#44176,
#44177,#44178,#44179,#44180,#44181,#44182,#44183,#44184,#44185,#44186,#44187,
#44188,#44189,#44190,#44191,#44192,#44193,#44194,#44195,#44196,#44197,#44198,
#44199,#44200,#44201,#44202),.UNSPECIFIED.,.F.,.F.,(4,2,2,2,2,2,2,2,2,2,
2,2,2,2,2,2,2,2,2,2,4),(1.58754199438591,1.66428756220311,1.75505140709888,
1.85247262654257,1.94559879742955,1.99141264552402,2.09224806187651,2.17687381898934,
2.27760558432556,2.36115785782877,2.46273884078532,2.506970278523,2.6072783781268,
2.69242749120669,2.7910892863526,2.83848659087682,2.92081415544938,3.02162491455608,
3.10269311798798,3.15009710686931,3.17236617648777),.UNSPECIFIED.);
#677=B_SPLINE_CURVE_WITH_KNOTS('',3,(#44204,#44205,#44206,#44207,#44208,
#44209,#44210,#44211,#44212,#44213,#44214,#44215,#44216,#44217,#44218,#44219,
#44220,#44221,#44222,#44223,#44224,#44225,#44226,#44227,#44228,#44229,#44230,
#44231,#44232,#44233),.UNSPECIFIED.,.F.,.F.,(4,2,2,2,2,2,2,2,2,2,2,2,2,
2,4),(7.98383028724678E-6,0.0594068121132572,0.117173822001359,0.157563544309192,
0.25282538752385,0.353748066677795,0.452720576279622,0.547246751719325,
0.596227171842395,0.692274403534477,0.786468812754584,0.887236199880665,
0.984305583682174,1.04109120139304,1.09448507079122),.UNSPECIFIED.);
#678=B_SPLINE_CURVE_WITH_KNOTS('',3,(#44234,#44235,#44236,#44237,#44238,
#44239,#44240,#44241,#44242,#44243,#44244,#44245,#44246,#44247,#44248,#44249,
#44250,#44251,#44252,#44253,#44254,#44255,#44256,#44257,#44258,#44259,#44260,
#44261,#44262,#44263,#44264,#44265,#44266,#44267,#44268,#44269,#44270,#44271,
#44272,#44273,#44274,#44275,#44276,#44277,#44278,#44279,#44280,#44281,#44282,
#44283,#44284,#44285,#44286,#44287,#44288,#44289,#44290,#44291,#44292,#44293,
#44294,#44295,#44296,#44297,#44298,#44299,#44300,#44301,#44302,#44303,#44304,
#44305,#44306,#44307,#44308,#44309,#44310,#44311,#44312),.UNSPECIFIED.,
 .F.,.F.,(4,3,3,3,3,3,3,3,3,3,3,3,3,3,3,3,3,3,3,3,3,3,3,3,3,3,4),(4.58842016772256E-5,
0.0231862791791696,0.0267235302321618,0.0536803738369688,0.080637102547167,
0.0806372174417757,0.10182702398916,0.12820009816435,0.155010998250621,
0.181909348449436,0.203530246760958,0.22893505393977,0.230469238508873,
0.248568363744309,0.248569988525206,0.275074209658101,0.301949036381728,
0.305135524171737,0.331796956449855,0.358718535004781,0.385415027716635,
0.406659425239883,0.416445184312435,0.416446996309603,0.442599172427887,
0.469460613188687,0.494689467284077),.UNSPECIFIED.);
#679=B_SPLINE_CURVE_WITH_KNOTS('',3,(#44317,#44318,#44319,#44320,#44321,
#44322,#44323,#44324,#44325,#44326,#44327,#44328,#44329,#44330,#44331,#44332,
#44333,#44334,#44335,#44336,#44337,#44338,#44339,#44340,#44341,#44342,#44343,
#44344,#44345,#44346,#44347,#44348,#44349,#44350,#44351,#44352,#44353,#44354,
#44355,#44356,#44357,#44358,#44359,#44360,#44361,#44362),.UNSPECIFIED.,
 .F.,.F.,(4,2,2,2,2,2,2,2,2,2,2,2,2,2,2,2,2,2,2,2,2,2,4),(7.66834827221688E-5,
0.0534536371935326,0.110991983464426,0.203800972593915,0.30051808488584,
0.401775523626737,0.50287541759609,0.550982689569767,0.599782660106522,
0.694241313514436,0.745324528568043,0.839057782678784,0.93605559701574,
0.986137663701895,1.03517902588757,1.1362195664112,1.18508550988462,1.23535743991359,
1.28496964571626,1.38380065054698,1.47551163273244,1.57716784819653,1.58754199438591),
 .UNSPECIFIED.);
#680=B_SPLINE_CURVE_WITH_KNOTS('',3,(#44363,#44364,#44365,#44366,#44367,
#44368,#44369,#44370,#44371,#44372,#44373,#44374,#44375,#44376,#44377,#44378,
#44379,#44380,#44381,#44382,#44383,#44384,#44385,#44386,#44387,#44388,#44389,
#44390,#44391,#44392,#44393,#44394,#44395,#44396,#44397,#44398,#44399,#44400,
#44401,#44402),.UNSPECIFIED.,.F.,.F.,(4,2,2,2,2,2,2,2,2,2,2,2,2,2,2,2,2,
2,2,4),(6.4154566266032E-5,0.071031520425574,0.152747669641631,0.249042814711534,
0.35068929650393,0.399104833478405,0.496987801918373,0.590472086651412,
0.692109735972922,0.768401783904028,0.869620781995952,0.966429502947187,
1.0657318064452,1.11062560595854,1.19784021313316,1.29114674735375,1.38647354043681,
1.42966321924486,1.53134219242619,1.5898434740455),.UNSPECIFIED.);
#681=B_SPLINE_CURVE_WITH_KNOTS('',3,(#44405,#44406,#44407,#44408,#44409,
#44410,#44411,#44412,#44413,#44414,#44415,#44416,#44417,#44418,#44419,#44420,
#44421,#44422,#44423,#44424,#44425,#44426,#44427,#44428,#44429,#44430,#44431,
#44432,#44433,#44434,#44435,#44436),.UNSPECIFIED.,.F.,.F.,(4,2,2,2,2,2,
2,2,2,2,2,2,2,2,2,4),(1.5898434740455,1.6271433856272,1.71712100874479,
1.76388458955179,1.86488993045687,1.96329627655657,2.05442894894533,2.10180472376313,
2.2020473014041,2.30061824506391,2.39053591761843,2.43818655549719,2.5370859795822,
2.63367841104952,2.70812820243631,2.77288713491997),.UNSPECIFIED.);
#682=B_SPLINE_CURVE_WITH_KNOTS('',3,(#44438,#44439,#44440,#44441,#44442,
#44443,#44444,#44445,#44446,#44447,#44448,#44449,#44450,#44451),
 .UNSPECIFIED.,.F.,.F.,(4,2,2,2,2,2,4),(4.24690342800971E-5,0.0511137139916916,
0.106332852431889,0.202821163335648,0.298258915813529,0.34872538483187,
0.405519954193255),.UNSPECIFIED.);
#683=B_SPLINE_CURVE_WITH_KNOTS('',3,(#44455,#44456,#44457,#44458,#44459,
#44460,#44461,#44462,#44463,#44464,#44465,#44466,#44467,#44468),
 .UNSPECIFIED.,.F.,.F.,(4,2,2,2,2,2,4),(1.58698352057749,1.61948213694375,
1.66708283695248,1.76538888902147,1.86226817876712,1.93594907832504,1.99997761942734),
 .UNSPECIFIED.);
#684=B_SPLINE_CURVE_WITH_KNOTS('',3,(#44469,#44470,#44471,#44472,#44473,
#44474,#44475,#44476,#44477,#44478,#44479,#44480,#44481,#44482,#44483,#44484,
#44485,#44486,#44487,#44488,#44489,#44490,#44491,#44492,#44493,#44494,#44495,
#44496,#44497,#44498,#44499,#44500,#44501,#44502),.UNSPECIFIED.,.F.,.F.,
(4,2,2,2,2,2,2,2,2,2,2,2,2,2,2,2,4),(0.000131786380904477,0.102860341713039,
0.137101926847378,0.217735363923029,0.315916468892578,0.397129195041746,
0.493796267586976,0.592181782019098,0.694353461838846,0.742150853821977,
0.793256700217311,0.841719577877637,0.943713479381191,0.991689068265629,
1.03881655518178,1.10792105895507,1.18423727595816),.UNSPECIFIED.);
#685=B_SPLINE_CURVE_WITH_KNOTS('',3,(#44507,#44508,#44509,#44510,#44511,
#44512,#44513,#44514,#44515,#44516,#44517,#44518,#44519,#44520,#44521,#44522,
#44523,#44524,#44525,#44526,#44527,#44528,#44529,#44530,#44531,#44532,#44533,
#44534,#44535,#44536,#44537,#44538,#44539,#44540,#44541,#44542,#44543,#44544,
#44545,#44546),.UNSPECIFIED.,.F.,.F.,(4,2,2,2,2,2,2,2,2,2,2,2,2,2,2,2,2,
2,2,4),(0.000233386320108365,0.0639084378333196,0.115738834875602,0.195580708942554,
0.296872775675836,0.395308850829062,0.468647278901977,0.569260147218536,
0.659264789203345,0.706236945833907,0.80709174491497,0.907905842929024,
1.00009797247216,1.09497639692093,1.19505864006617,1.28468085990641,1.33202875244464,
1.43127168932415,1.5301694640538,1.58698352057749),.UNSPECIFIED.);
#686=B_SPLINE_CURVE_WITH_KNOTS('',3,(#44548,#44549,#44550,#44551),
 .UNSPECIFIED.,.F.,.F.,(4,4),(0.405519954193255,0.405690998123473),
 .UNSPECIFIED.);
#687=B_SPLINE_CURVE_WITH_KNOTS('',3,(#44552,#44553,#44554,#44555,#44556,
#44557,#44558,#44559,#44560,#44561,#44562,#44563,#44564,#44565,#44566,#44567,
#44568,#44569,#44570,#44571,#44572,#44573,#44574,#44575,#44576,#44577,#44578,
#44579,#44580,#44581,#44582,#44583,#44584,#44585,#44586,#44587,#44588,#44589,
#44590,#44591,#44592,#44593,#44594,#44595,#44596,#44597,#44598,#44599,#44600,
#44601,#44602,#44603,#44604,#44605),.UNSPECIFIED.,.F.,.F.,(4,2,2,2,2,2,
2,2,2,2,2,2,2,2,2,2,2,2,2,2,2,2,2,2,2,2,4),(0.000315760721890317,0.0671794601159759,
0.142466537729481,0.190297899820453,0.238768166053594,0.332946663979359,
0.430541047971958,0.526554088588678,0.557936308139163,0.569901596811977,
0.668190233380715,0.742459118264126,0.784100177232852,0.847618599139215,
0.949980342343833,1.04534048049391,1.08870174690026,1.13607572013548,1.17545912833599,
1.22708032066423,1.32273981517142,1.36325156389753,1.42070337211726,1.48376830446815,
1.52647813490246,1.5929584678999,1.59372842373243),.UNSPECIFIED.);
#688=B_SPLINE_CURVE_WITH_KNOTS('',3,(#44611,#44612,#44613,#44614,#44615,
#44616,#44617,#44618,#44619,#44620,#44621,#44622),.UNSPECIFIED.,.F.,.F.,
(4,2,2,2,2,4),(1.73689377313444E-6,0.0397074682898225,0.0816374594028487,
0.160434126623339,0.243474988518188,0.320867562725843),.UNSPECIFIED.);
#689=B_SPLINE_CURVE_WITH_KNOTS('',3,(#44624,#44625,#44626,#44627,#44628,
#44629,#44630,#44631,#44632,#44633,#44634,#44635,#44636,#44637,#44638,#44639,
#44640,#44641,#44642,#44643,#44644,#44645,#44646,#44647,#44648,#44649,#44650,
#44651,#44652,#44653,#44654,#44655,#44656,#44657,#44658,#44659,#44660,#44661,
#44662,#44663,#44664,#44665,#44666,#44667,#44668,#44669,#44670,#44671,#44672,
#44673,#44674,#44675,#44676,#44677,#44678,#44679,#44680,#44681,#44682,#44683,
#44684,#44685,#44686,#44687,#44688,#44689,#44690,#44691,#44692,#44693,#44694,
#44695,#44696,#44697,#44698,#44699,#44700,#44701,#44702,#44703,#44704,#44705,
#44706,#44707,#44708,#44709,#44710,#44711,#44712,#44713,#44714,#44715,#44716,
#44717,#44718,#44719,#44720,#44721,#44722,#44723,#44724,#44725,#44726,#44727,
#44728,#44729,#44730,#44731,#44732,#44733,#44734,#44735,#44736,#44737,#44738,
#44739,#44740,#44741,#44742,#44743,#44744,#44745,#44746,#44747,#44748,#44749,
#44750,#44751,#44752,#44753,#44754,#44755,#44756,#44757,#44758,#44759,#44760,
#44761,#44762,#44763,#44764,#44765,#44766,#44767,#44768,#44769,#44770,#44771,
#44772,#44773,#44774,#44775,#44776,#44777,#44778,#44779,#44780,#44781,#44782,
#44783,#44784,#44785,#44786,#44787,#44788,#44789,#44790,#44791,#44792,#44793,
#44794,#44795,#44796,#44797,#44798,#44799,#44800,#44801,#44802,#44803,#44804,
#44805,#44806,#44807,#44808,#44809,#44810,#44811,#44812,#44813,#44814,#44815,
#44816,#44817,#44818,#44819,#44820,#44821,#44822,#44823,#44824,#44825,#44826,
#44827,#44828,#44829,#44830,#44831,#44832,#44833,#44834,#44835,#44836,#44837,
#44838,#44839,#44840),.UNSPECIFIED.,.F.,.F.,(4,3,3,3,3,3,3,3,3,3,3,3,3,
3,3,3,3,3,3,3,3,3,3,3,3,3,3,3,3,3,3,3,3,3,3,3,3,3,3,3,3,3,3,3,3,3,3,3,3,
3,3,3,3,3,3,3,3,3,3,3,3,3,3,3,3,3,3,3,3,3,3,3,4),(5.31095027518764E-9,0.0191480404307811,
0.0268229569350739,0.0537675131188631,0.0804193339369082,0.0843763580558497,
0.0843766029239374,0.101824284415583,0.128087669003448,0.154826539242901,
0.181716882619413,0.203526770072898,0.229033516898158,0.2304418928167,0.25225492212391,
0.252260389184945,0.278990758257123,0.305132042464289,0.331749499982824,
0.358645858343833,0.385359014779447,0.406654209945588,0.42008278387528,
0.42009020951023,0.446361881136987,0.473090671353263,0.499996599516834,
0.508103946120237,0.534910171633633,0.561786915448796,0.586626585034112,
0.587962078272053,0.587964325643741,0.609493007642893,0.635865341378628,
0.662650747975075,0.689502249238686,0.710830175716059,0.735593555674911,
0.737737642485696,0.755707788969607,0.755715461128941,0.78036338986414,
0.782248582456849,0.809125623044456,0.812119352707047,0.838818701113506,
0.865764132225303,0.892456173463476,0.914207349002946,0.923466604850516,
0.923484364288651,0.948200823019635,0.949743733247729,0.976471741845332,
1.00339540898673,1.01588539484221,1.04269403687978,1.06814092402567,1.06958141316705,
1.09127739827948,1.09129934073672,1.11545127759809,1.11714505442693,1.14363806036283,
1.17047970433824,1.19722878067902,1.21807739682823,1.24123199345686,1.24517381391668,
1.25897306563341,1.25900354475818,1.27023098040024),.UNSPECIFIED.);
#690=B_SPLINE_CURVE_WITH_KNOTS('',3,(#44841,#44842,#44843,#44844),
 .UNSPECIFIED.,.F.,.F.,(4,4),(3.1560069292801E-5,0.000233386320108365),
 .UNSPECIFIED.);
#691=B_SPLINE_CURVE_WITH_KNOTS('',3,(#44846,#44847,#44848,#44849,#44850,
#44851,#44852,#44853,#44854,#44855,#44856,#44857,#44858,#44859,#44860,#44861,
#44862,#44863,#44864,#44865,#44866,#44867,#44868,#44869,#44870,#44871,#44872,
#44873,#44874,#44875,#44876,#44877,#44878,#44879,#44880,#44881,#44882,#44883,
#44884,#44885,#44886,#44887,#44888,#44889,#44890,#44891,#44892,#44893),
 .UNSPECIFIED.,.F.,.F.,(4,2,2,2,2,2,2,2,2,2,2,2,2,2,2,2,2,2,2,2,2,2,2,4),
(1.59372842373243,1.63638854674833,1.66111458565455,1.71028293204707,1.80937505144961,
1.91074393718392,1.95971059032954,2.05862989243709,2.10831236150241,2.15712578278928,
2.20499253693922,2.3068209642726,2.35606089004449,2.40548038645003,2.45275661630416,
2.55280385060893,2.59920187815348,2.68412836559863,2.76983887215137,2.87102125912343,
2.95553213085994,3.05760109679623,3.1222894965372,3.18599763231299),
 .UNSPECIFIED.);
#692=B_SPLINE_CURVE_WITH_KNOTS('',3,(#44894,#44895,#44896,#44897),
 .UNSPECIFIED.,.F.,.F.,(4,4),(1.00000009672838E-6,6.17888066936219E-5),
 .UNSPECIFIED.);
#693=B_SPLINE_CURVE_WITH_KNOTS('',3,(#44903,#44904,#44905,#44906,#44907,
#44908,#44909,#44910),.UNSPECIFIED.,.F.,.F.,(4,2,2,4),(1.58569301455726,
1.587634805142,1.6706642559489,1.74161014133595),.UNSPECIFIED.);
#694=B_SPLINE_CURVE_WITH_KNOTS('',3,(#44911,#44912,#44913,#44914,#44915,
#44916,#44917,#44918,#44919,#44920,#44921,#44922,#44923,#44924,#44925,#44926,
#44927,#44928,#44929,#44930,#44931,#44932,#44933,#44934,#44935,#44936,#44937,
#44938,#44939,#44940,#44941,#44942,#44943,#44944,#44945,#44946,#44947,#44948,
#44949,#44950,#44951,#44952,#44953,#44954,#44955,#44956,#44957,#44958,#44959,
#44960,#44961,#44962,#44963,#44964,#44965,#44966,#44967,#44968,#44969,#44970,
#44971,#44972,#44973,#44974,#44975,#44976,#44977,#44978,#44979,#44980,#44981,
#44982,#44983,#44984,#44985,#44986,#44987,#44988,#44989,#44990,#44991,#44992,
#44993,#44994,#44995,#44996,#44997,#44998,#44999,#45000,#45001,#45002,#45003,
#45004,#45005,#45006,#45007,#45008,#45009,#45010,#45011,#45012,#45013,#45014,
#45015,#45016,#45017,#45018,#45019,#45020,#45021,#45022,#45023,#45024,#45025,
#45026,#45027,#45028,#45029,#45030,#45031,#45032,#45033,#45034,#45035,#45036,
#45037,#45038,#45039,#45040,#45041,#45042,#45043,#45044,#45045,#45046,#45047,
#45048,#45049,#45050,#45051,#45052,#45053,#45054,#45055,#45056,#45057,#45058,
#45059,#45060,#45061,#45062,#45063,#45064,#45065,#45066,#45067,#45068,#45069,
#45070,#45071,#45072,#45073,#45074,#45075,#45076,#45077,#45078,#45079,#45080,
#45081,#45082,#45083,#45084,#45085,#45086,#45087,#45088,#45089,#45090,#45091,
#45092,#45093,#45094,#45095,#45096,#45097,#45098,#45099,#45100,#45101,#45102,
#45103,#45104,#45105,#45106,#45107,#45108,#45109,#45110,#45111,#45112,#45113,
#45114,#45115,#45116,#45117,#45118,#45119,#45120,#45121,#45122,#45123,#45124,
#45125,#45126,#45127,#45128,#45129,#45130,#45131,#45132,#45133,#45134,#45135,
#45136,#45137,#45138,#45139,#45140,#45141,#45142,#45143,#45144,#45145,#45146,
#45147,#45148,#45149,#45150,#45151,#45152,#45153,#45154,#45155,#45156,#45157,
#45158,#45159,#45160,#45161,#45162,#45163,#45164,#45165,#45166,#45167,#45168,
#45169,#45170,#45171,#45172,#45173,#45174,#45175,#45176,#45177,#45178,#45179,
#45180,#45181,#45182,#45183,#45184),.UNSPECIFIED.,.F.,.F.,(4,3,3,3,3,3,
3,3,3,3,3,3,3,3,3,3,3,3,3,3,3,3,3,3,3,3,3,3,3,3,3,3,3,3,3,3,3,3,3,3,3,3,
3,3,3,3,3,3,3,3,3,3,3,3,3,3,3,3,3,3,3,3,3,3,3,3,3,3,3,3,3,3,3,3,3,3,3,3,
3,3,3,3,3,3,3,3,3,3,3,3,3,4),(9.9865186199412E-8,0.0165170009540119,0.0269560963403509,
0.0516026360833156,0.0539939918893045,0.0619549903004816,0.0619569561518245,
0.0869496139842535,0.0887864088251827,0.102132027133151,0.129070531766969,
0.156009036400786,0.156009728784879,0.182902541024912,0.203851549956986,
0.230680355193655,0.250043336119814,0.250048492305348,0.275626936708897,
0.27764556096622,0.305247785812627,0.331937887925211,0.358922694967677,
0.375449181557498,0.37545383194231,0.400488263889334,0.402335048584807,
0.406320547266745,0.432920095075976,0.45984166967008,0.486692519308316,
0.500786019934413,0.500788193121711,0.507023039110945,0.53343108396808,
0.560251627646521,0.587156442098039,0.607377499256687,0.626067946696661,
0.626075385929146,0.652594867406431,0.679484622591304,0.696616153907565,
0.696623115086315,0.7074659160348,0.7339706204339,0.760896048377414,0.767095742268224,
0.767103284580723,0.794002576058669,0.807301789010731,0.833952495633197,
0.83754118627808,0.837547573059014,0.864398365331485,0.89120989339632,0.90682027159049,
0.908049260110694,0.908057170500754,0.934401369183197,0.961199033620948,
0.988154790632044,1.00602308450473,1.03060487918097,1.03298575801758,1.04901141337422,
1.04901899068072,1.07364088767949,1.07699866077235,1.10313522477293,1.10498590817048,
1.13172938424021,1.15873452930581,1.18360272650853,1.18560295888011,1.19002020304435,
1.19002635837203,1.20371732313993,1.23017716258453,1.25705058603626,1.2840098004507,
1.30214552504217,1.32624464129826,1.32907950882834,1.3309467369147,1.33095133640406,
1.35586247307618,1.35752131148749,1.38448911199129,1.40027033128569,1.42754750616507,
1.43259500515056),.UNSPECIFIED.);
#695=B_SPLINE_CURVE_WITH_KNOTS('',3,(#45186,#45187,#45188,#45189,#45190,
#45191,#45192,#45193,#45194,#45195,#45196,#45197,#45198,#45199,#45200,#45201,
#45202,#45203,#45204,#45205,#45206,#45207),.UNSPECIFIED.,.F.,.F.,(4,2,2,
2,2,2,2,2,2,2,4),(6.17888066936219E-5,0.0952321659214813,0.168572142996074,
0.269154246669155,0.361233599404335,0.462276827673878,0.552734576636099,
0.650535735082581,0.737701663102056,0.835191426558474,0.924653665098687),
 .UNSPECIFIED.);
#696=B_SPLINE_CURVE_WITH_KNOTS('',3,(#45208,#45209,#45210,#45211,#45212,
#45213,#45214,#45215,#45216,#45217,#45218,#45219,#45220,#45221,#45222,#45223,
#45224,#45225,#45226,#45227,#45228,#45229,#45230,#45231,#45232,#45233,#45234,
#45235,#45236,#45237,#45238,#45239,#45240,#45241,#45242,#45243,#45244,#45245,
#45246,#45247,#45248,#45249,#45250,#45251,#45252,#45253,#45254,#45255,#45256,
#45257,#45258,#45259,#45260,#45261,#45262,#45263,#45264,#45265,#45266,#45267,
#45268,#45269,#45270,#45271,#45272,#45273,#45274,#45275,#45276,#45277,#45278,
#45279,#45280,#45281,#45282,#45283,#45284,#45285,#45286,#45287,#45288,#45289,
#45290,#45291,#45292,#45293,#45294,#45295,#45296,#45297,#45298,#45299,#45300,
#45301,#45302,#45303,#45304,#45305,#45306,#45307,#45308,#45309,#45310,#45311,
#45312,#45313,#45314,#45315,#45316,#45317,#45318,#45319,#45320,#45321,#45322,
#45323,#45324,#45325,#45326,#45327,#45328,#45329,#45330,#45331,#45332,#45333,
#45334,#45335,#45336,#45337,#45338,#45339,#45340),.UNSPECIFIED.,.F.,.F.,
(4,3,3,3,3,3,3,3,3,3,3,3,3,3,3,3,3,3,3,3,3,3,3,3,3,3,3,3,3,3,3,3,3,3,3,
3,3,3,3,3,3,3,3,3,4),(1.66970259518317E-7,0.0195408023283141,0.0268240864561452,
0.0519109008684237,0.0519127124963912,0.0787226617260139,0.101671370691236,
0.107856553210952,0.107858116237918,0.132586573240225,0.135853998461347,
0.159529331929515,0.163849880684776,0.163855488459842,0.188513397271807,
0.190494891911395,0.203248940230886,0.229557891457817,0.256333149896959,
0.283269519729177,0.304748770645336,0.330172222241103,0.331703685429797,
0.356398100810531,0.35966945417196,0.383548279581913,0.386117015489908,
0.387635222914124,0.387651295959121,0.406179501373845,0.43224435118395,
0.458879218217511,0.485890019786178,0.507549821109392,0.534529392192245,
0.559845427216043,0.561539389676409,0.585730024157773,0.587972179090907,
0.608868993160356,0.61130729451897,0.611324084570082,0.635027594176061,
0.637557052005942,0.662236219249742),.UNSPECIFIED.);
#697=B_SPLINE_CURVE_WITH_KNOTS('',3,(#45345,#45346,#45347,#45348,#45349,
#45350,#45351,#45352,#45353,#45354,#45355,#45356,#45357,#45358,#45359,#45360,
#45361,#45362,#45363,#45364,#45365,#45366,#45367,#45368,#45369,#45370,#45371,
#45372,#45373,#45374,#45375,#45376,#45377,#45378,#45379,#45380,#45381,#45382,
#45383,#45384,#45385,#45386),.UNSPECIFIED.,.F.,.F.,(4,2,2,2,2,2,2,2,2,2,
2,2,2,2,2,2,2,2,2,2,4),(0.000200192691012083,0.0459634654450998,0.0897981263797104,
0.182563617677864,0.23043629516319,0.331499932350853,0.379339465965364,
0.480419798577262,0.572564637956923,0.622450255663974,0.723703481811166,
0.770906047985159,0.870735642587249,0.971506320484368,1.06104297895876,
1.16195264040926,1.25685403264272,1.30560365648842,1.39440414562203,1.49505415995523,
1.58569301455726),.UNSPECIFIED.);
#698=B_SPLINE_CURVE_WITH_KNOTS('',3,(#45387,#45388,#45389,#45390,#45391,
#45392,#45393,#45394,#45395,#45396,#45397,#45398,#45399,#45400,#45401,#45402,
#45403,#45404,#45405,#45406,#45407,#45408,#45409,#45410,#45411,#45412,#45413,
#45414,#45415,#45416,#45417,#45418,#45419,#45420,#45421,#45422,#45423,#45424,
#45425,#45426,#45427,#45428),.UNSPECIFIED.,.F.,.F.,(4,2,2,2,2,2,2,2,2,2,
2,2,2,2,2,2,2,2,2,2,4),(7.91614227771307E-5,0.0600035764138198,0.107716099660701,
0.18322851806419,0.284460041175081,0.377847341356911,0.465640487399806,
0.559597868052173,0.636518057225568,0.737491713471269,0.832117269395779,
0.925832800560101,0.975014451851033,1.07607976212091,1.1240775948849,1.22516313586639,
1.31513822178404,1.40585346672917,1.45293493568029,1.55386692466454,1.58754532392759),
 .UNSPECIFIED.);
#699=B_SPLINE_CURVE_WITH_KNOTS('',3,(#45434,#45435,#45436,#45437,#45438,
#45439),.UNSPECIFIED.,.F.,.F.,(4,2,4),(0.000101837034550224,0.0201470223705077,
0.0401954933212442),.UNSPECIFIED.);
#700=B_SPLINE_CURVE_WITH_KNOTS('',3,(#45441,#45442,#45443,#45444,#45445,
#45446,#45447,#45448,#45449,#45450,#45451,#45452,#45453,#45454,#45455,#45456,
#45457,#45458,#45459,#45460,#45461,#45462,#45463,#45464,#45465,#45466,#45467,
#45468,#45469,#45470,#45471,#45472,#45473,#45474,#45475,#45476,#45477,#45478,
#45479,#45480,#45481,#45482,#45483,#45484,#45485,#45486,#45487,#45488,#45489,
#45490,#45491,#45492,#45493,#45494,#45495,#45496,#45497,#45498,#45499,#45500,
#45501,#45502,#45503,#45504,#45505,#45506,#45507,#45508,#45509,#45510,#45511,
#45512,#45513,#45514,#45515,#45516,#45517,#45518,#45519,#45520,#45521,#45522,
#45523,#45524,#45525,#45526,#45527,#45528,#45529,#45530,#45531,#45532,#45533,
#45534,#45535,#45536,#45537,#45538,#45539,#45540,#45541,#45542,#45543,#45544,
#45545,#45546,#45547,#45548,#45549,#45550,#45551,#45552,#45553,#45554,#45555,
#45556,#45557,#45558,#45559,#45560,#45561,#45562,#45563,#45564,#45565,#45566,
#45567,#45568,#45569,#45570,#45571,#45572,#45573,#45574,#45575,#45576,#45577,
#45578,#45579,#45580,#45581,#45582,#45583,#45584,#45585,#45586,#45587,#45588,
#45589,#45590,#45591,#45592,#45593,#45594,#45595,#45596,#45597,#45598,#45599,
#45600,#45601,#45602,#45603,#45604,#45605,#45606,#45607,#45608,#45609,#45610,
#45611,#45612,#45613,#45614,#45615,#45616,#45617,#45618,#45619,#45620,#45621,
#45622,#45623,#45624,#45625,#45626,#45627,#45628,#45629,#45630,#45631,#45632,
#45633,#45634,#45635,#45636,#45637,#45638,#45639,#45640,#45641,#45642,#45643,
#45644,#45645,#45646,#45647,#45648,#45649,#45650,#45651,#45652,#45653,#45654,
#45655,#45656,#45657,#45658,#45659,#45660,#45661,#45662,#45663,#45664,#45665,
#45666,#45667,#45668,#45669,#45670,#45671,#45672,#45673,#45674,#45675,#45676,
#45677,#45678,#45679,#45680,#45681,#45682,#45683,#45684,#45685,#45686,#45687,
#45688,#45689,#45690,#45691,#45692,#45693,#45694,#45695,#45696,#45697,#45698,
#45699,#45700,#45701,#45702,#45703,#45704,#45705,#45706,#45707,#45708,#45709,
#45710,#45711,#45712,#45713,#45714,#45715,#45716,#45717,#45718,#45719,#45720,
#45721,#45722,#45723,#45724,#45725,#45726,#45727,#45728,#45729,#45730,#45731,
#45732,#45733,#45734,#45735,#45736,#45737,#45738,#45739,#45740,#45741,#45742,
#45743,#45744,#45745,#45746,#45747,#45748,#45749,#45750,#45751,#45752,#45753,
#45754,#45755,#45756,#45757,#45758,#45759,#45760,#45761,#45762,#45763,#45764,
#45765,#45766,#45767,#45768,#45769,#45770,#45771,#45772,#45773,#45774),
 .UNSPECIFIED.,.F.,.F.,(4,3,3,3,3,3,3,3,3,3,3,3,3,3,3,3,3,3,3,3,3,3,3,3,
3,3,3,3,3,3,3,3,3,3,3,3,3,3,3,3,3,3,3,3,3,3,3,3,3,3,3,3,3,3,3,3,3,3,3,3,
3,3,3,3,3,3,3,3,3,3,3,3,3,3,3,3,3,3,3,3,3,3,3,3,3,3,3,3,3,3,3,3,3,3,3,3,
3,3,3,3,3,3,3,3,3,3,3,3,3,3,3,4),(1.13292399530795E-7,0.0196928172933993,
0.0266956052075354,0.0503343617400793,0.0503391750759571,0.0643522297958899,
0.0643568684523188,0.0783591425935286,0.0783636026936431,0.101669107471721,
0.106302158127171,0.10630630451195,0.132795584592458,0.159597319790963,
0.162302887343916,0.162305864602742,0.189092019568487,0.203245868153258,
0.229777136283039,0.256613075626682,0.274235080436413,0.274235407135105,
0.301001096463727,0.304744104831594,0.331238225509686,0.358684698041346,
0.386131170573007,0.38613449810665,0.406172508592631,0.43259369534683,0.442014502970311,
0.442018453364401,0.470004342403802,0.49651923133194,0.497994181837294,
0.497999165742914,0.507541553513218,0.511940966359407,0.511946066546157,
0.525904535910578,0.525909869558653,0.549360849797592,0.551878270558614,
0.553893887146288,0.553898924376285,0.57841459029774,0.581377056379963,
0.604299021973496,0.608860225613638,0.609832456494235,0.633649156002123,
0.635717416259916,0.660670639785913,0.662198734481889,0.68917737665926,
0.711164765300409,0.738063711508917,0.765100247087221,0.790181412556859,
0.791720097711544,0.813130447497351,0.833487150899675,0.833496210994393,
0.856625714233385,0.859629993596308,0.88383669019327,0.887179645735812,
0.912669305169198,0.914729297875317,0.941517269106251,0.968556178625948,
0.995326318254519,1.01591627739398,1.03859646750578,1.04288287816545,1.05715560698756,
1.05717054613622,1.07968191134433,1.08347164461366,1.10689777465868,1.11035077795206,
1.11674748200187,1.14331205720645,1.17025616513136,1.19714941760193,1.21732834413762,
1.24062535644877,1.24433976862262,1.26683620881214,1.2711512358007,1.28081358130734,
1.28082854039954,1.30299671904022,1.30754584512882,1.31764387528724,1.34227944172055,
1.34399381708511,1.37082761041625,1.39786781667107,1.41761477840521,1.44291220243535,
1.44462869140057,1.46870092111847,1.47164935363387,1.49471334104812,1.49819054458882,
1.50442526885582,1.50443667340995,1.51726643247651,1.54198728460159,1.5439713432008,
1.55104955739032),.UNSPECIFIED.);
#701=B_SPLINE_CURVE_WITH_KNOTS('',3,(#45775,#45776,#45777,#45778),
 .UNSPECIFIED.,.F.,.F.,(4,4),(9.65841270823929E-5,0.000200192691012083),
 .UNSPECIFIED.);
#702=B_SPLINE_CURVE_WITH_KNOTS('',3,(#45780,#45781,#45782,#45783,#45784,
#45785,#45786,#45787,#45788,#45789,#45790,#45791,#45792,#45793,#45794,#45795,
#45796,#45797,#45798,#45799,#45800,#45801,#45802,#45803,#45804,#45805,#45806,
#45807),.UNSPECIFIED.,.F.,.F.,(4,2,2,2,2,2,2,2,2,2,2,2,2,4),(1.58754532392759,
1.65173348850276,1.69990823036454,1.79097132992545,1.89214817054913,1.99098341671071,
2.08088116422555,2.12847676160414,2.22733163510097,2.32484132890977,2.41387565781255,
2.46207264157115,2.55303228913833,2.63023061161303),.UNSPECIFIED.);
#703=B_SPLINE_CURVE_WITH_KNOTS('',3,(#45808,#45809,#45810,#45811,#45812,
#45813,#45814,#45815,#45816,#45817,#45818,#45819,#45820,#45821,#45822,#45823),
 .UNSPECIFIED.,.F.,.F.,(4,2,2,2,2,2,2,4),(0.000441888379867055,0.0712123258361295,
0.153637230093539,0.24663025572483,0.348304026319509,0.43875400981342,0.540436997579012,
0.543345573804166),.UNSPECIFIED.);
#704=B_SPLINE_CURVE_WITH_KNOTS('',3,(#45826,#45827,#45828,#45829,#45830,
#45831,#45832,#45833,#45834,#45835,#45836,#45837,#45838,#45839,#45840,#45841,
#45842,#45843,#45844,#45845,#45846,#45847,#45848,#45849,#45850,#45851,#45852,
#45853,#45854,#45855,#45856,#45857,#45858,#45859,#45860,#45861),
 .UNSPECIFIED.,.F.,.F.,(4,2,2,2,2,2,2,2,2,2,2,2,2,2,2,2,2,4),(0.543345573804166,
0.632883876225489,0.681859177676299,0.777577268298339,0.828233852261912,
0.877156775277406,0.978121049434662,1.0758107655072,1.12427682326688,1.22286953667497,
1.27082359754074,1.31918246207647,1.41998339373079,1.46885416546689,1.56843982737443,
1.61487450414648,1.68703359300301,1.75359080947889),.UNSPECIFIED.);
#705=B_SPLINE_CURVE_WITH_KNOTS('',3,(#45863,#45864,#45865,#45866,#45867,
#45868,#45869,#45870,#45871,#45872,#45873,#45874),.UNSPECIFIED.,.F.,.F.,
(4,2,2,2,2,4),(2.38764650524234E-5,0.0874762242858372,0.16161100104167,
0.263824592583728,0.351221429605352,0.377547520539708),.UNSPECIFIED.);
#706=B_SPLINE_CURVE_WITH_KNOTS('',3,(#45877,#45878,#45879,#45880,#45881,
#45882,#45883,#45884,#45885,#45886,#45887,#45888,#45889,#45890,#45891,#45892,
#45893,#45894,#45895,#45896,#45897,#45898,#45899,#45900,#45901,#45902,#45903,
#45904,#45905,#45906,#45907,#45908,#45909,#45910,#45911,#45912,#45913,#45914,
#45915,#45916),.UNSPECIFIED.,.F.,.F.,(4,2,2,2,2,2,2,2,2,2,2,2,2,2,2,2,2,
2,2,4),(2.87435079942613,2.90908627921352,2.99959019849851,3.09707993844391,
3.19714155267547,3.24484909228093,3.32636302699049,3.37071831260431,3.47159691287487,
3.56386995533199,3.65864007403778,3.75026808820601,3.84557562826543,3.9357192189986,
4.03247844544094,4.12174025181586,4.21882481577015,4.30566738965663,4.38862465799223,
4.45293375202886),.UNSPECIFIED.);
#707=B_SPLINE_CURVE_WITH_KNOTS('',3,(#45921,#45922,#45923,#45924,#45925,
#45926,#45927,#45928,#45929,#45930,#45931,#45932,#45933,#45934,#45935,#45936,
#45937,#45938,#45939,#45940,#45941,#45942,#45943,#45944,#45945,#45946,#45947,
#45948,#45949,#45950,#45951,#45952,#45953,#45954,#45955,#45956,#45957,#45958,
#45959,#45960,#45961,#45962),.UNSPECIFIED.,.F.,.F.,(4,2,2,2,2,2,2,2,2,2,
2,2,2,2,2,2,2,2,2,2,4),(1.29092315943205,1.38003890819178,1.47665828500728,
1.57754789064784,1.67848491879225,1.72634519454726,1.82718775987331,1.92805302106637,
1.97630062959479,2.07710589502321,2.17789125240703,2.22607075099038,2.32681039747117,
2.37675450699215,2.42514659011588,2.4721963487193,2.57324684507597,2.66851111481085,
2.76013041155395,2.8078211904013,2.87435079942613),.UNSPECIFIED.);
#708=B_SPLINE_CURVE_WITH_KNOTS('',3,(#45963,#45964,#45965,#45966,#45967,
#45968,#45969,#45970,#45971,#45972,#45973,#45974,#45975,#45976,#45977,#45978,
#45979,#45980,#45981,#45982,#45983,#45984,#45985,#45986,#45987,#45988,#45989,
#45990,#45991,#45992,#45993,#45994,#45995,#45996,#45997,#45998,#45999,#46000,
#46001,#46002),.UNSPECIFIED.,.F.,.F.,(4,2,2,2,2,2,2,2,2,2,2,2,2,2,2,2,2,
2,2,4),(0.377547520539708,0.452910059858426,0.497939063488615,0.581559294711028,
0.683061141383824,0.782198397513139,0.86638087248029,0.963221943764175,
1.03590139751064,1.1371715237912,1.23381855972917,1.32919735940209,1.42389091389379,
1.48878364666316,1.53500546453752,1.63207294506492,1.73242395947659,1.83142774699405,
1.92407009339033,1.9660107665537),.UNSPECIFIED.);
#709=B_SPLINE_CURVE_WITH_KNOTS('',3,(#46008,#46009,#46010,#46011,#46012,
#46013,#46014,#46015,#46016,#46017),.UNSPECIFIED.,.F.,.F.,(4,2,2,2,4),(1.58631321662086,
1.61402560378215,1.70207985040979,1.8000208134824,1.88377373488638),
 .UNSPECIFIED.);
#710=B_SPLINE_CURVE_WITH_KNOTS('',3,(#46018,#46019,#46020,#46021,#46022,
#46023,#46024,#46025,#46026,#46027,#46028,#46029,#46030,#46031,#46032,#46033,
#46034,#46035,#46036,#46037,#46038,#46039,#46040,#46041,#46042,#46043,#46044,
#46045,#46046,#46047,#46048,#46049,#46050,#46051,#46052,#46053,#46054,#46055,
#46056,#46057),.UNSPECIFIED.,.F.,.F.,(4,2,2,2,2,2,2,2,2,2,2,2,2,2,2,2,2,
2,2,4),(0.000337110448919753,0.0674382068481336,0.137790147250154,0.239065013113051,
0.325530449406533,0.422867756755189,0.512760640130854,0.605322501628678,
0.654807814067912,0.703885264670299,0.802873350225715,0.850409666676142,
0.899945799232159,0.949788722546396,1.04782193719607,1.09611534977182,1.14511541496357,
1.2384972774798,1.28809781873481,1.29092315943205),.UNSPECIFIED.);
#711=B_SPLINE_CURVE_WITH_KNOTS('',3,(#46059,#46060,#46061,#46062,#46063,
#46064,#46065,#46066,#46067,#46068,#46069,#46070,#46071,#46072,#46073,#46074,
#46075,#46076,#46077,#46078,#46079,#46080,#46081,#46082,#46083,#46084,#46085,
#46086,#46087,#46088,#46089,#46090,#46091,#46092),.UNSPECIFIED.,.F.,.F.,
(4,2,2,2,2,2,2,2,2,2,2,2,2,2,2,2,4),(1.9660107665537,2.02581281643668,2.12619938236871,
2.21649199339821,2.26384716561196,2.36159447778931,2.40948822197726,2.51058228712726,
2.60378230877955,2.69946776093669,2.74743080058653,2.8482918561081,2.94186174762132,
3.03568405796453,3.08339710005034,3.18073503357408,3.26409879879059),
 .UNSPECIFIED.);
#712=B_SPLINE_CURVE_WITH_KNOTS('',3,(#46093,#46094,#46095,#46096,#46097,
#46098,#46099,#46100,#46101,#46102),.UNSPECIFIED.,.F.,.F.,(4,2,2,2,4),(0.000401396573765282,
0.0767267724924665,0.171583258256695,0.259711836113359,0.289709300215736),
 .UNSPECIFIED.);
#713=B_SPLINE_CURVE_WITH_KNOTS('',3,(#46107,#46108,#46109,#46110,#46111,
#46112,#46113,#46114,#46115,#46116,#46117,#46118,#46119,#46120,#46121,#46122,
#46123,#46124,#46125,#46126,#46127,#46128,#46129,#46130,#46131,#46132,#46133,
#46134,#46135,#46136,#46137,#46138,#46139,#46140,#46141,#46142,#46143,#46144,
#46145,#46146,#46147,#46148),.UNSPECIFIED.,.F.,.F.,(4,2,2,2,2,2,2,2,2,2,
2,2,2,2,2,2,2,2,2,2,4),(6.19917750705267E-6,0.0779101723467662,0.163347403591141,
0.211369088637002,0.309559385368541,0.403161961538505,0.45435016612089,
0.546763115962883,0.596854200931595,0.6977571810982,0.744652526768696,0.844613323634994,
0.941898523491601,1.03126364841854,1.1324037693941,1.22675848757232,1.32139054199484,
1.36966233595816,1.47055391734561,1.56509118248676,1.58631321662086),
 .UNSPECIFIED.);
#714=B_SPLINE_CURVE_WITH_KNOTS('',3,(#46149,#46150,#46151,#46152,#46153,
#46154,#46155,#46156,#46157,#46158,#46159,#46160,#46161,#46162,#46163,#46164,
#46165,#46166,#46167,#46168,#46169,#46170,#46171,#46172,#46173,#46174,#46175,
#46176,#46177,#46178,#46179,#46180,#46181,#46182,#46183,#46184,#46185,#46186,
#46187,#46188,#46189,#46190),.UNSPECIFIED.,.F.,.F.,(4,2,2,2,2,2,2,2,2,2,
2,2,2,2,2,2,2,2,2,2,4),(0.289709300215736,0.354159359873933,0.450430540051697,
0.545790968368503,0.638492687552296,0.740854867193477,0.788324960692327,
0.879895408610432,0.976079549455883,1.07768471355924,1.17678702801279,1.22541491119139,
1.32694131959504,1.42604352921976,1.51879959847725,1.61507782511401,1.66515194848187,
1.71454858187282,1.8160243538418,1.86442895008864,1.88361728507473),
 .UNSPECIFIED.);
#715=B_SPLINE_CURVE_WITH_KNOTS('',3,(#46196,#46197,#46198,#46199,#46200,
#46201,#46202,#46203,#46204,#46205),.UNSPECIFIED.,.F.,.F.,(4,2,2,2,4),(1.19987423408312E-5,
0.0502654517634361,0.102318195477417,0.154980355752334,0.204643884264344),
 .UNSPECIFIED.);
#716=B_SPLINE_CURVE_WITH_KNOTS('',3,(#46206,#46207,#46208,#46209,#46210,
#46211,#46212,#46213,#46214,#46215,#46216,#46217,#46218,#46219,#46220,#46221,
#46222,#46223,#46224,#46225,#46226,#46227,#46228,#46229,#46230,#46231,#46232,
#46233,#46234,#46235,#46236,#46237,#46238,#46239,#46240,#46241,#46242,#46243,
#46244,#46245,#46246,#46247,#46248,#46249,#46250,#46251,#46252,#46253,#46254,
#46255,#46256,#46257,#46258,#46259,#46260,#46261,#46262,#46263,#46264,#46265,
#46266,#46267,#46268,#46269,#46270,#46271,#46272,#46273,#46274,#46275,#46276,
#46277,#46278,#46279,#46280,#46281,#46282,#46283,#46284,#46285,#46286,#46287,
#46288,#46289,#46290,#46291,#46292,#46293,#46294,#46295,#46296,#46297,#46298,
#46299,#46300,#46301,#46302,#46303,#46304,#46305,#46306,#46307,#46308,#46309,
#46310,#46311,#46312,#46313,#46314,#46315,#46316,#46317,#46318,#46319,#46320,
#46321,#46322,#46323,#46324,#46325,#46326,#46327,#46328,#46329,#46330,#46331,
#46332,#46333,#46334,#46335,#46336,#46337,#46338,#46339,#46340,#46341,#46342,
#46343,#46344,#46345,#46346,#46347,#46348,#46349,#46350,#46351,#46352,#46353,
#46354,#46355,#46356,#46357,#46358,#46359,#46360,#46361,#46362,#46363,#46364,
#46365,#46366,#46367,#46368,#46369,#46370,#46371,#46372,#46373,#46374,#46375,
#46376,#46377,#46378,#46379,#46380,#46381,#46382,#46383,#46384,#46385,#46386,
#46387,#46388,#46389,#46390,#46391,#46392,#46393,#46394,#46395,#46396,#46397,
#46398,#46399,#46400,#46401,#46402,#46403,#46404,#46405,#46406,#46407,#46408,
#46409,#46410,#46411,#46412,#46413,#46414,#46415,#46416,#46417,#46418,#46419,
#46420,#46421,#46422,#46423,#46424,#46425,#46426,#46427,#46428,#46429,#46430,
#46431,#46432,#46433,#46434,#46435,#46436,#46437,#46438,#46439,#46440,#46441,
#46442,#46443,#46444,#46445,#46446,#46447,#46448,#46449,#46450,#46451,#46452,
#46453,#46454,#46455,#46456,#46457,#46458,#46459,#46460,#46461,#46462,#46463,
#46464),.UNSPECIFIED.,.F.,.F.,(4,3,3,3,3,3,3,3,3,3,3,3,3,3,3,3,3,3,3,3,
3,3,3,3,3,3,3,3,3,3,3,3,3,3,3,3,3,3,3,3,3,3,3,3,3,3,3,3,3,3,3,3,3,3,3,3,
3,3,3,3,3,3,3,3,3,3,3,3,3,3,3,3,3,3,3,3,3,3,3,3,3,3,3,3,3,3,4),(1.33217227012311E-6,
0.0194681700743097,0.0267673112323403,0.0538008962348333,0.080584107915861,
0.101824443115546,0.126382254351437,0.128808154219708,0.140308379837731,
0.140331736201363,0.166497871296857,0.19194180857669,0.19335702062781,0.20352684729289,
0.23008128254457,0.257031409529791,0.28393764637694,0.305131966797111,0.329862153890025,
0.332137147300207,0.356221787991884,0.358969880802285,0.364186795008282,
0.364202261631717,0.388450168684,0.390849182797679,0.406654235569055,0.433023159921676,
0.459871705874179,0.486876245718093,0.508104082639558,0.533473857623085,
0.535121215478853,0.559667655210642,0.561941015242435,0.585613447401546,
0.587965212525989,0.587976323639518,0.609493077799452,0.63563971386527,
0.66232974601657,0.689346315814045,0.710830182576537,0.737822771061955,
0.762959610043142,0.764824563091553,0.788879951220074,0.791243080925086,
0.811643835672881,0.811657693323187,0.812119505296254,0.835513511256599,
0.837989836435306,0.862562815089907,0.864474914866434,0.891489423335006,
0.914208690295899,0.941141317294609,0.968210960766913,0.992952266363267,
0.994832587480743,1.0158936331595,1.03529802723853,1.03531295234316,1.05822446086301,
1.06140155475125,1.08529525625318,1.08927899950726,1.11434050369983,1.11715644426327,
1.14393065344995,1.17098540440778,1.19783521736686,1.21808204851952,1.24119892021897,
1.24512763049342,1.25897417085869,1.25898740261327,1.28275052598487,1.28544903653438,
1.31039702842331,1.31226081213009,1.31876428899761,1.34534096825719,1.3708141566497,
1.37082202499578,1.38667239091504),.UNSPECIFIED.);
#717=B_SPLINE_CURVE_WITH_KNOTS('',3,(#46465,#46466,#46467,#46468,#46469,
#46470,#46471,#46472,#46473,#46474,#46475,#46476,#46477,#46478,#46479,#46480,
#46481,#46482,#46483,#46484,#46485,#46486,#46487,#46488,#46489,#46490,#46491,
#46492,#46493,#46494,#46495,#46496,#46497,#46498,#46499,#46500,#46501,#46502,
#46503,#46504,#46505,#46506,#46507,#46508,#46509,#46510),.UNSPECIFIED.,
 .F.,.F.,(4,2,2,2,2,2,2,2,2,2,2,2,2,2,2,2,2,2,2,2,2,2,4),(1.88361728507473,
1.96613901790761,2.06744611316973,2.11575785090515,2.16536468174169,2.25859006675776,
2.30797163714038,2.35584195444279,2.45707357200554,2.50600802601238,2.55571013211468,
2.65209506654081,2.70006204432426,2.74877786583655,2.84768301560138,2.94883097916437,
2.99685457059701,3.09818140715212,3.19599431591786,3.27979391370675,3.36312376157902,
3.46429786859654,3.4738015741047),.UNSPECIFIED.);
#718=B_SPLINE_CURVE_WITH_KNOTS('',3,(#46513,#46514,#46515,#46516,#46517,
#46518,#46519,#46520,#46521,#46522,#46523,#46524,#46525,#46526,#46527,#46528,
#46529,#46530,#46531,#46532,#46533,#46534,#46535,#46536,#46537,#46538,#46539,
#46540),.UNSPECIFIED.,.F.,.F.,(4,2,2,2,2,2,2,2,2,2,2,2,2,4),(3.4738015741047,
3.55646460394477,3.65827175861552,3.74262585524875,3.84347823410159,3.92685548572533,
4.02844773414359,4.07274100135846,4.17305612403082,4.25792737984997,4.35287051687195,
4.40062979162429,4.4637145399754,4.51766419841934),.UNSPECIFIED.);
#719=B_SPLINE_CURVE_WITH_KNOTS('',3,(#46542,#46543,#46544,#46545,#46546,
#46547,#46548,#46549,#46550,#46551,#46552,#46553,#46554,#46555,#46556,#46557,
#46558,#46559,#46560,#46561,#46562,#46563,#46564,#46565,#46566,#46567,#46568,
#46569,#46570,#46571,#46572,#46573,#46574,#46575,#46576,#46577,#46578,#46579,
#46580,#46581,#46582,#46583,#46584,#46585,#46586,#46587,#46588,#46589,#46590,
#46591,#46592,#46593,#46594,#46595,#46596,#46597,#46598,#46599,#46600,#46601,
#46602,#46603,#46604,#46605,#46606,#46607,#46608,#46609,#46610,#46611,#46612,
#46613,#46614,#46615,#46616,#46617,#46618,#46619,#46620,#46621,#46622,#46623,
#46624,#46625,#46626,#46627,#46628,#46629,#46630,#46631,#46632,#46633,#46634,
#46635,#46636,#46637,#46638,#46639,#46640,#46641,#46642,#46643,#46644,#46645,
#46646,#46647),.UNSPECIFIED.,.F.,.F.,(4,3,3,3,3,3,3,3,3,3,3,3,3,3,3,3,3,
3,3,3,3,3,3,3,3,3,3,3,3,3,3,3,3,3,3,4),(0.,0.0265152916366039,0.0534408681373308,
0.0803732537892289,0.101671318199502,0.126768973351817,0.128669605927973,
0.153163172340859,0.155509697825392,0.16384911211717,0.163849430554983,
0.188424042846322,0.190512347195134,0.203249027869299,0.229570935958494,
0.256365848711328,0.283325187479159,0.304748913597632,0.330304499545278,
0.331728476013042,0.356523027277944,0.359681624709295,0.383638294470675,
0.386147280159222,0.387634773405548,0.387654846931905,0.406179509230895,
0.432211307600104,0.45880941260941,0.485718384707018,0.49948489014596,0.499498019517492,
0.507549805242806,0.527395571189254,0.52740934651372,0.545642469618713),
 .UNSPECIFIED.);
#720=B_SPLINE_CURVE_WITH_KNOTS('',3,(#46651,#46652,#46653,#46654),
 .UNSPECIFIED.,.F.,.F.,(4,4),(3.17692141158165,3.21705724092707),
 .UNSPECIFIED.);
#721=B_SPLINE_CURVE_WITH_KNOTS('',3,(#46655,#46656,#46657,#46658,#46659,
#46660,#46661,#46662,#46663,#46664,#46665,#46666,#46667,#46668,#46669,#46670,
#46671,#46672,#46673,#46674,#46675,#46676,#46677,#46678,#46679,#46680,#46681,
#46682,#46683,#46684,#46685,#46686,#46687,#46688,#46689,#46690,#46691,#46692,
#46693,#46694,#46695,#46696,#46697,#46698),.UNSPECIFIED.,.F.,.F.,(4,2,2,
2,2,2,2,2,2,2,2,2,2,2,2,2,2,2,2,2,2,4),(1.62006151030285E-6,0.0630919360385355,
0.141371266622184,0.240503139713508,0.287761650735986,0.384166379031894,
0.434674488379614,0.48430971532037,0.533052731490774,0.628943150682843,
0.678967965576476,0.773597067333852,0.823829482794688,0.919205173967643,
0.968856828764193,1.06534548410256,1.11441704174039,1.21144390918971,1.30591932981216,
1.40676744527164,1.47566588590981,1.54713662236737),.UNSPECIFIED.);
#722=B_SPLINE_CURVE_WITH_KNOTS('',3,(#46703,#46704,#46705,#46706,#46707,
#46708,#46709,#46710,#46711,#46712,#46713,#46714,#46715,#46716,#46717,#46718,
#46719,#46720,#46721,#46722,#46723,#46724,#46725,#46726,#46727,#46728,#46729,
#46730,#46731,#46732,#46733,#46734,#46735,#46736,#46737,#46738,#46739,#46740,
#46741,#46742,#46743,#46744,#46745,#46746),.UNSPECIFIED.,.F.,.F.,(4,2,2,
2,2,2,2,2,2,2,2,2,2,2,2,2,2,2,2,2,2,4),(1.59120053347567,1.60853341934407,
1.65661584810623,1.75505616994776,1.8462295408035,1.94706985801477,1.99655604703536,
2.04585088558141,2.09530509317676,2.19142149509141,2.29246978719122,2.38516127502823,
2.48243927585401,2.53024851712262,2.63125669011797,2.72417158686598,2.81887978492759,
2.86666299693515,2.96738709204182,3.05919840492306,3.14435325618814,3.17692141158165),
 .UNSPECIFIED.);
#723=B_SPLINE_CURVE_WITH_KNOTS('',3,(#46748,#46749,#46750,#46751,#46752,
#46753,#46754,#46755,#46756,#46757,#46758,#46759,#46760,#46761,#46762,#46763,
#46764,#46765,#46766,#46767,#46768,#46769,#46770,#46771,#46772,#46773,#46774,
#46775,#46776,#46777,#46778,#46779,#46780,#46781,#46782,#46783,#46784,#46785,
#46786,#46787,#46788,#46789),.UNSPECIFIED.,.F.,.F.,(4,2,2,2,2,2,2,2,2,2,
2,2,2,2,2,2,2,2,2,2,4),(0.000142530208232202,0.084807243665273,0.12049355472412,
0.219724371123383,0.292967991970656,0.39430418199766,0.490547781547131,
0.572968847782376,0.667961187809243,0.746000093988248,0.793791696819115,
0.875555352557861,0.973542726584909,1.07467540733736,1.12475371232168,1.21762151178067,
1.26566606434273,1.31580783326067,1.40843364165663,1.50260630133708,1.58743977472934),
 .UNSPECIFIED.);
#724=B_SPLINE_CURVE_WITH_KNOTS('',3,(#46790,#46791,#46792,#46793),
 .UNSPECIFIED.,.F.,.F.,(4,4),(1.00000007008057E-6,4.51866339753897E-5),
 .UNSPECIFIED.);
#725=B_SPLINE_CURVE_WITH_KNOTS('',3,(#46798,#46799,#46800,#46801,#46802,
#46803,#46804,#46805,#46806,#46807,#46808,#46809,#46810,#46811,#46812,#46813,
#46814,#46815,#46816,#46817,#46818,#46819,#46820,#46821,#46822,#46823,#46824,
#46825,#46826,#46827,#46828,#46829,#46830,#46831,#46832,#46833,#46834,#46835,
#46836,#46837),.UNSPECIFIED.,.F.,.F.,(4,2,2,2,2,2,2,2,2,2,2,2,2,2,2,2,2,
2,2,4),(0.000225597449676421,0.0742785979883565,0.172984943813638,0.21867109199009,
0.263583573029605,0.338100351692891,0.439755678406654,0.530561182861844,
0.630701087176066,0.680230522755222,0.766303621894736,0.867669669041908,
0.96729347126901,1.06300073179688,1.11181328265079,1.21259237443786,1.31385724331297,
1.41584938221636,1.51607755707357,1.59120053347567),.UNSPECIFIED.);
#726=B_SPLINE_CURVE_WITH_KNOTS('',3,(#46839,#46840,#46841,#46842,#46843,
#46844,#46845,#46846,#46847,#46848,#46849,#46850,#46851,#46852,#46853,#46854,
#46855,#46856,#46857,#46858,#46859,#46860,#46861,#46862,#46863,#46864,#46865,
#46866,#46867,#46868),.UNSPECIFIED.,.F.,.F.,(4,2,2,2,2,2,2,2,2,2,2,2,2,
2,4),(4.51866339753897E-5,0.0723418406247212,0.134392893639461,0.235357150136565,
0.327769542964459,0.37808460863748,0.478641278283578,0.579619814342238,
0.674620396174953,0.723420037361222,0.812330301317198,0.912981269215007,
1.00567215431713,1.08860054890301,1.15920864160196),.UNSPECIFIED.);
#727=B_SPLINE_CURVE_WITH_KNOTS('',3,(#46869,#46870,#46871,#46872,#46873,
#46874,#46875,#46876,#46877,#46878,#46879,#46880),.UNSPECIFIED.,.F.,.F.,
(4,2,2,2,2,4),(3.15245941783976E-5,0.0712582376283404,0.153901430321048,
0.246035781455943,0.347779076529136,0.426610112684851),.UNSPECIFIED.);
#728=B_SPLINE_CURVE_WITH_KNOTS('',3,(#46886,#46887,#46888,#46889,#46890,
#46891,#46892,#46893,#46894,#46895,#46896,#46897,#46898,#46899,#46900,#46901,
#46902,#46903,#46904,#46905,#46906,#46907,#46908,#46909,#46910,#46911,#46912,
#46913,#46914,#46915,#46916,#46917,#46918,#46919,#46920,#46921),
 .UNSPECIFIED.,.F.,.F.,(4,2,2,2,2,2,2,2,2,2,2,2,2,2,2,2,2,4),(1.58722454481072,
1.59524297044126,1.69317612751528,1.79281806368903,1.87978394745879,1.96899265118635,
2.06989725355135,2.16758224385157,2.25534165295551,2.34593089546819,2.44477013813802,
2.53454582142298,2.63253651296269,2.72236054424066,2.81965528443521,2.90701496351563,
3.00540629266297,3.09463589604302),.UNSPECIFIED.);
#729=B_SPLINE_CURVE_WITH_KNOTS('',3,(#46923,#46924,#46925,#46926,#46927,
#46928,#46929,#46930,#46931,#46932,#46933,#46934,#46935),.UNSPECIFIED.,
 .F.,.F.,(4,3,3,3,4),(0.0018605619201363,0.0062236786619737,0.0308774375217015,
0.0556573833848329,0.0777721094897591),.UNSPECIFIED.);
#730=B_SPLINE_CURVE_WITH_KNOTS('',3,(#46936,#46937,#46938,#46939),
 .UNSPECIFIED.,.F.,.F.,(4,4),(9.70452423452837E-6,0.000225597449676421),
 .UNSPECIFIED.);
#731=B_SPLINE_CURVE_WITH_KNOTS('',3,(#46941,#46942,#46943,#46944,#46945,
#46946,#46947,#46948,#46949,#46950,#46951,#46952,#46953,#46954,#46955,#46956,
#46957,#46958,#46959,#46960,#46961,#46962,#46963,#46964,#46965,#46966,#46967,
#46968,#46969,#46970,#46971,#46972,#46973,#46974,#46975,#46976,#46977,#46978,
#46979,#46980),.UNSPECIFIED.,.F.,.F.,(4,2,2,2,2,2,2,2,2,2,2,2,2,2,2,2,2,
2,2,4),(0.426610112684851,0.439472155416163,0.541098529643712,0.632374845173586,
0.681041387412177,0.777089284904803,0.827790203151545,0.876690951902663,
0.977656571294406,1.07524977633825,1.12372668491373,1.22223503711215,1.27018254242946,
1.31851261808215,1.41931586170264,1.46815778609337,1.56783530997388,1.6142737679206,
1.68646984809641,1.75330694074283),.UNSPECIFIED.);
#732=B_SPLINE_CURVE_WITH_KNOTS('',3,(#46981,#46982,#46983,#46984,#46985,
#46986,#46987,#46988,#46989,#46990),.UNSPECIFIED.,.F.,.F.,(4,2,2,2,4),(0.000434210888476285,
0.0630060612538896,0.136757874181064,0.232772050379,0.261585962310352),
 .UNSPECIFIED.);
#733=B_SPLINE_CURVE_WITH_KNOTS('',3,(#46996,#46997,#46998,#46999),
 .UNSPECIFIED.,.F.,.F.,(4,4),(1.41445606292759,1.4144793844605),
 .UNSPECIFIED.);
#734=B_SPLINE_CURVE_WITH_KNOTS('',3,(#47000,#47001,#47002,#47003,#47004,
#47005,#47006,#47007,#47008,#47009,#47010,#47011,#47012,#47013,#47014,#47015,
#47016,#47017,#47018,#47019,#47020,#47021,#47022,#47023,#47024,#47025,#47026,
#47027,#47028,#47029,#47030,#47031,#47032,#47033,#47034,#47035,#47036,#47037,
#47038,#47039,#47040,#47041),.UNSPECIFIED.,.F.,.F.,(4,2,2,2,2,2,2,2,2,2,
2,2,2,2,2,2,2,2,2,2,4),(1.00000013738019E-6,0.0796922243486748,0.164914931020009,
0.265180305781826,0.359335347902182,0.45669214052704,0.507219253269266,
0.555952281106953,0.65708827855891,0.751766673237182,0.801524920395762,
0.902500497171451,0.951104807532313,1.00077823719909,1.07925129178133,1.18069608155444,
1.25613712406717,1.3574635166215,1.44767761290287,1.54753048731727,1.58722454481072),
 .UNSPECIFIED.);
#735=B_SPLINE_CURVE_WITH_KNOTS('',3,(#47042,#47043,#47044,#47045,#47046,
#47047,#47048,#47049,#47050,#47051,#47052,#47053,#47054,#47055,#47056,#47057,
#47058,#47059,#47060,#47061,#47062,#47063,#47064,#47065,#47066,#47067,#47068,
#47069,#47070,#47071,#47072,#47073,#47074,#47075,#47076,#47077,#47078,#47079,
#47080,#47081,#47082,#47083),.UNSPECIFIED.,.F.,.F.,(4,2,2,2,2,2,2,2,2,2,
2,2,2,2,2,2,2,2,2,2,4),(0.261585962310352,0.330550507228154,0.422527548682331,
0.47237274394023,0.564999077065041,0.667050806886986,0.711465681558209,
0.800391700047598,0.902392081894043,1.00262065482135,1.08506201189223,1.18643635531154,
1.23566840489802,1.33738116675383,1.43802933084244,1.48690438160809,1.53618071386031,
1.63734686166833,1.68140483291318,1.78262408644938,1.85540224175298),
 .UNSPECIFIED.);
#736=B_SPLINE_CURVE_WITH_KNOTS('',3,(#47089,#47090,#47091,#47092,#47093,
#47094,#47095,#47096),.UNSPECIFIED.,.F.,.F.,(4,2,2,4),(1.58568783641564,
1.60107665321778,1.69047010281316,1.76702536599967),.UNSPECIFIED.);
#737=B_SPLINE_CURVE_WITH_KNOTS('',3,(#47097,#47098,#47099,#47100,#47101,
#47102,#47103,#47104,#47105,#47106,#47107,#47108,#47109,#47110,#47111,#47112,
#47113,#47114,#47115,#47116,#47117,#47118,#47119,#47120,#47121,#47122,#47123,
#47124,#47125,#47126,#47127,#47128,#47129,#47130,#47131,#47132,#47133,#47134,
#47135,#47136,#47137,#47138),.UNSPECIFIED.,.F.,.F.,(4,2,2,2,2,2,2,2,2,2,
2,2,2,2,2,2,2,2,2,2,4),(1.91775425791884E-5,0.0612944133050306,0.127958262779682,
0.228551343497341,0.277929273973939,0.369183603105148,0.465110204022711,
0.560983178942996,0.609100835872562,0.659754517209396,0.707271467351877,
0.80909755487051,0.896035614412291,0.996569978326781,1.04361179933817,1.09207570162642,
1.19392102568165,1.24233423984167,1.32720234730169,1.36928301115767,1.41445606292759),
 .UNSPECIFIED.);
#738=B_SPLINE_CURVE_WITH_KNOTS('',3,(#47140,#47141,#47142,#47143,#47144,
#47145,#47146,#47147,#47148,#47149,#47150,#47151,#47152,#47153,#47154,#47155,
#47156,#47157,#47158,#47159,#47160,#47161,#47162,#47163,#47164,#47165,#47166,
#47167,#47168,#47169,#47170,#47171,#47172,#47173,#47174,#47175,#47176,#47177),
 .UNSPECIFIED.,.F.,.F.,(4,2,2,2,2,2,2,2,2,2,2,2,2,2,2,2,2,2,4),(1.85540224175298,
1.8619285315257,1.96200419757285,2.01118534688469,2.10343957811208,2.20207178110793,
2.24977633671792,2.35130727897218,2.44561194476143,2.54209792847507,2.58987156038197,
2.69119674822331,2.78594737859994,2.83531674316662,2.9242056709114,3.02532340493309,
3.11793130320266,3.20245562576603,3.27462710206336),.UNSPECIFIED.);
#739=B_SPLINE_CURVE_WITH_KNOTS('',3,(#47178,#47179,#47180,#47181,#47182,
#47183),.UNSPECIFIED.,.F.,.F.,(4,2,4),(2.18613549776391E-5,0.086154780125611,
0.172243535902318),.UNSPECIFIED.);
#740=B_SPLINE_CURVE_WITH_KNOTS('',3,(#47186,#47187,#47188,#47189,#47190,
#47191,#47192,#47193,#47194,#47195,#47196,#47197,#47198,#47199,#47200,#47201,
#47202,#47203,#47204,#47205,#47206,#47207,#47208,#47209,#47210,#47211,#47212,
#47213,#47214,#47215,#47216,#47217,#47218,#47219,#47220,#47221,#47222,#47223),
 .UNSPECIFIED.,.F.,.F.,(4,2,2,2,2,2,2,2,2,2,2,2,2,2,2,2,2,2,4),(9.99999998785787E-7,
0.0872888446587809,0.181612821610965,0.277455319811984,0.372137063139133,
0.465554874798131,0.567846232837133,0.65372194201713,0.702757026771262,
0.798859431343223,0.900937352389522,0.989203218137305,1.08572229776357,
1.18152722648351,1.2828802925819,1.38294569604287,1.43164726657578,1.53286996181633,
1.5925198531225),.UNSPECIFIED.);
#741=B_SPLINE_CURVE_WITH_KNOTS('',3,(#47226,#47227,#47228,#47229,#47230,
#47231,#47232,#47233,#47234,#47235,#47236,#47237,#47238,#47239,#47240,#47241,
#47242,#47243,#47244,#47245,#47246,#47247,#47248,#47249,#47250,#47251,#47252,
#47253,#47254,#47255,#47256,#47257,#47258,#47259,#47260,#47261,#47262,#47263,
#47264,#47265,#47266,#47267,#47268,#47269),.UNSPECIFIED.,.F.,.F.,(4,2,2,
2,2,2,2,2,2,2,2,2,2,2,2,2,2,2,2,2,2,4),(3.63649524114627E-6,0.0506749674295985,
0.0987723951799838,0.199129291380623,0.247004760404853,0.345097478709695,
0.442075215447975,0.492724066396971,0.587904001990667,0.689009154908131,
0.735835483147296,0.836592304221807,0.883525845707275,0.930710618615424,
1.03064389394975,1.13038725002875,1.21973722341929,1.26726563753008,1.36559794931312,
1.46417011421529,1.55307633926682,1.58568783641564),.UNSPECIFIED.);
#742=B_SPLINE_CURVE_WITH_KNOTS('',3,(#47275,#47276,#47277,#47278),
 .UNSPECIFIED.,.F.,.F.,(4,4),(1.58766981265925,1.58767330633224),
 .UNSPECIFIED.);
#743=B_SPLINE_CURVE_WITH_KNOTS('',3,(#47280,#47281,#47282,#47283,#47284,
#47285,#47286),.UNSPECIFIED.,.F.,.F.,(4,3,4),(1.62164761664365E-5,0.0442981693467548,
0.0886134884474553),.UNSPECIFIED.);
#744=B_SPLINE_CURVE_WITH_KNOTS('',3,(#47287,#47288,#47289,#47290,#47291,
#47292,#47293,#47294,#47295,#47296,#47297,#47298,#47299,#47300,#47301,#47302,
#47303,#47304,#47305,#47306,#47307,#47308,#47309,#47310,#47311,#47312,#47313,
#47314,#47315,#47316,#47317,#47318,#47319,#47320,#47321,#47322,#47323,#47324,
#47325,#47326,#47327,#47328,#47329,#47330,#47331,#47332,#47333,#47334,#47335,
#47336,#47337,#47338,#47339,#47340,#47341,#47342,#47343,#47344,#47345,#47346,
#47347,#47348,#47349,#47350,#47351,#47352,#47353,#47354,#47355,#47356,#47357,
#47358,#47359,#47360,#47361,#47362,#47363,#47364,#47365,#47366,#47367,#47368,
#47369,#47370,#47371,#47372,#47373,#47374,#47375,#47376,#47377,#47378,#47379,
#47380,#47381,#47382,#47383,#47384,#47385,#47386,#47387,#47388,#47389,#47390,
#47391,#47392,#47393,#47394,#47395,#47396,#47397,#47398,#47399,#47400,#47401,
#47402,#47403,#47404,#47405,#47406,#47407,#47408,#47409,#47410,#47411,#47412,
#47413,#47414,#47415,#47416,#47417,#47418,#47419,#47420,#47421,#47422,#47423,
#47424,#47425,#47426,#47427,#47428,#47429,#47430,#47431,#47432,#47433,#47434,
#47435,#47436,#47437,#47438,#47439,#47440,#47441,#47442,#47443,#47444,#47445,
#47446,#47447,#47448,#47449,#47450,#47451,#47452,#47453,#47454,#47455,#47456,
#47457,#47458,#47459,#47460,#47461,#47462,#47463,#47464,#47465,#47466,#47467,
#47468,#47469,#47470,#47471,#47472,#47473,#47474,#47475,#47476,#47477,#47478,
#47479,#47480,#47481,#47482,#47483,#47484,#47485,#47486,#47487,#47488,#47489,
#47490,#47491,#47492,#47493,#47494,#47495,#47496,#47497,#47498,#47499,#47500,
#47501,#47502,#47503,#47504,#47505,#47506,#47507,#47508,#47509,#47510,#47511,
#47512,#47513,#47514,#47515,#47516,#47517,#47518,#47519,#47520,#47521,#47522,
#47523,#47524,#47525,#47526,#47527,#47528,#47529,#47530,#47531,#47532,#47533,
#47534,#47535,#47536,#47537,#47538,#47539,#47540,#47541,#47542,#47543,#47544,
#47545,#47546,#47547,#47548,#47549,#47550,#47551,#47552,#47553,#47554,#47555,
#47556,#47557,#47558,#47559,#47560,#47561,#47562,#47563,#47564,#47565,#47566,
#47567,#47568,#47569),.UNSPECIFIED.,.F.,.F.,(4,3,3,3,3,3,3,3,3,3,3,3,3,
3,3,3,3,3,3,3,3,3,3,3,3,3,3,3,3,3,3,3,3,3,3,3,3,3,3,3,3,3,3,3,3,3,3,3,3,
3,3,3,3,3,3,3,3,3,3,3,3,3,3,3,3,3,3,3,3,3,3,3,3,3,3,3,3,3,3,3,3,3,3,3,3,
3,3,3,3,3,3,3,3,3,4),(7.34837406725557E-8,0.019964867263137,0.0267693319277699,
0.0538018319699899,0.080579428135738,0.101824612826378,0.126388705926906,
0.128806294507739,0.140309322647435,0.140329659467777,0.165163912862995,
0.166493337341274,0.191905588690079,0.193354134040805,0.203526934231238,
0.230079241430717,0.257031002660155,0.28393706738352,0.305131955689965,
0.329790464210409,0.332136781123739,0.35614008309364,0.358965082758299,
0.364187796786279,0.364194448230442,0.388395041227389,0.390839887900307,
0.4066542974926,0.43300798160048,0.459851088836211,0.486886294610224,0.508104247050711,
0.535134837619628,0.560056375819446,0.562010330265102,0.586037386003401,
0.587966244395663,0.587967454966848,0.609493176432852,0.635682161969534,
0.662341510193711,0.689203081363828,0.699813410037673,0.699818853899349,
0.710830205766576,0.737539611782812,0.764413833638791,0.789460075551521,
0.790927600001401,0.811644907352174,0.811648797193604,0.812119671007486,
0.836086924852687,0.838125261897265,0.863339061094821,0.864709035325677,
0.891748760773525,0.914207077880491,0.941187256266604,0.968267314316379,
0.993011640482214,0.994880480564172,1.01590037275537,1.03529922270649,1.03531663017424,
1.05811313070032,1.06139837796637,1.0853081020415,1.08928336257022,1.11460462293563,
1.11716834717406,1.14394638546685,1.17098306230525,1.19773441829998,1.21808842694735,
1.24035953250997,1.2450783291986,1.2589753624395,1.25900871113918,1.2814308744521,
1.28528504821362,1.3084818360773,1.31218376228509,1.31876297219116,1.3453387934928,
1.37231702471802,1.39932418579149,1.41915612304848,1.44343126687223,1.44617731733548,
1.46954588616007,1.47307953308824,1.48265110768315,1.48265668956468,1.5030722252932),
 .UNSPECIFIED.);
#745=B_SPLINE_CURVE_WITH_KNOTS('',3,(#47570,#47571,#47572,#47573,#47574,
#47575,#47576,#47577,#47578,#47579,#47580,#47581,#47582,#47583,#47584,#47585,
#47586,#47587,#47588,#47589,#47590,#47591,#47592,#47593,#47594,#47595,#47596,
#47597,#47598,#47599,#47600,#47601,#47602,#47603,#47604,#47605,#47606,#47607,
#47608,#47609,#47610,#47611,#47612,#47613),.UNSPECIFIED.,.F.,.F.,(4,2,2,
2,2,2,2,2,2,2,2,2,2,2,2,2,2,2,2,2,2,4),(1.5925198531225,1.63115089761907,
1.68028338306566,1.7288487743576,1.82517709840843,1.87523647554672,1.97031689459656,
2.06752405104401,2.16861133619847,2.26968250121187,2.31826217170868,2.41824499459598,
2.51925552873196,2.56745564354346,2.66818108321483,2.71776519283693,2.7662031033493,
2.81370651120408,2.91461532539117,3.01101723620208,3.11201162580048,3.18046637425616),
 .UNSPECIFIED.);
#746=B_SPLINE_CURVE_WITH_KNOTS('',3,(#47618,#47619,#47620,#47621,#47622,
#47623,#47624,#47625,#47626,#47627,#47628,#47629,#47630,#47631,#47632,#47633,
#47634,#47635,#47636,#47637,#47638,#47639,#47640,#47641,#47642,#47643,#47644,
#47645,#47646,#47647,#47648,#47649,#47650,#47651,#47652,#47653,#47654,#47655,
#47656,#47657,#47658,#47659),.UNSPECIFIED.,.F.,.F.,(4,2,2,2,2,2,2,2,2,2,
2,2,2,2,2,2,2,2,2,2,4),(0.000332700259628768,0.0951610873337013,0.178264167133354,
0.273039667383402,0.371193805519262,0.467050098219079,0.547915762639124,
0.597950953485952,0.692817036535044,0.793845190917708,0.842969683744045,
0.892599286248275,0.988332887846854,1.03714150596388,1.13271901979353,1.18153079169454,
1.27832189716448,1.37232427040614,1.47310054254796,1.52908620914187,1.58766981265925),
 .UNSPECIFIED.);
#747=B_SPLINE_CURVE_WITH_KNOTS('',3,(#47661,#47662,#47663,#47664,#47665,
#47666,#47667,#47668,#47669,#47670,#47671,#47672,#47673,#47674,#47675,#47676,
#47677,#47678,#47679,#47680,#47681,#47682,#47683,#47684,#47685,#47686,#47687,
#47688),.UNSPECIFIED.,.F.,.F.,(4,2,2,2,2,2,2,2,2,2,2,2,2,4),(3.18046637425616,
3.19763502745909,3.29857986209492,3.39195214731422,3.48952696515865,3.58521097258035,
3.68156815331091,3.76906564255767,3.86983781821281,3.95777506098375,4.05877788923688,
4.14461580757828,4.24493867900757,4.33903702193303),.UNSPECIFIED.);
#748=B_SPLINE_CURVE_WITH_KNOTS('',3,(#47689,#47690,#47691,#47692,#47693,
#47694,#47695,#47696,#47697,#47698,#47699,#47700,#47701,#47702),
 .UNSPECIFIED.,.F.,.F.,(4,2,2,2,2,2,4),(7.39074714640052E-6,0.0560225944124789,
0.112993048660793,0.157595030319142,0.255703338428967,0.352232387034829,
0.428604909966747),.UNSPECIFIED.);
#749=B_SPLINE_CURVE_WITH_KNOTS('',3,(#47708,#47709,#47710,#47711,#47712,
#47713,#47714,#47715,#47716,#47717,#47718,#47719,#47720,#47721,#47722,#47723,
#47724,#47725,#47726,#47727,#47728,#47729,#47730,#47731,#47732,#47733,#47734,
#47735,#47736,#47737,#47738,#47739,#47740,#47741,#47742,#47743,#47744,#47745,
#47746,#47747),.UNSPECIFIED.,.F.,.F.,(4,2,2,2,2,2,2,2,2,2,2,2,2,2,2,2,2,
2,2,4),(1.58989822515966,1.59915917085918,1.69919078916423,1.74658988147312,
1.84785528875568,1.94360942344156,1.99292121519929,2.08243829086462,2.1835780720849,
2.27906545500479,2.3281489862221,2.41747307583334,2.51844181690281,2.61293340903648,
2.66193834680959,2.75064087305788,2.85136608761713,2.94359228351708,3.02794550059186,
3.09960259124824),.UNSPECIFIED.);
#750=B_SPLINE_CURVE_WITH_KNOTS('',3,(#47749,#47750,#47751,#47752,#47753,
#47754,#47755,#47756,#47757,#47758,#47759,#47760,#47761,#47762,#47763,#47764,
#47765,#47766,#47767,#47768,#47769,#47770,#47771,#47772,#47773,#47774,#47775,
#47776),.UNSPECIFIED.,.F.,.F.,(4,3,3,3,3,3,3,3,3,4),(0.00257022351332799,
0.00718554272612916,0.00853032056992718,0.0209145361963684,0.0449312967344481,
0.04781715587265,0.0642592511561034,0.0642736300230747,0.0700433819734726,
0.0784535026574735),.UNSPECIFIED.);
#751=B_SPLINE_CURVE_WITH_KNOTS('',3,(#47777,#47778,#47779,#47780),
 .UNSPECIFIED.,.F.,.F.,(4,4),(1.97025552236534E-5,0.000332700259628768),
 .UNSPECIFIED.);
#752=B_SPLINE_CURVE_WITH_KNOTS('',3,(#47781,#47782,#47783,#47784,#47785,
#47786,#47787,#47788,#47789,#47790,#47791,#47792,#47793,#47794,#47795,#47796,
#47797,#47798,#47799,#47800,#47801,#47802,#47803,#47804,#47805,#47806,#47807,
#47808,#47809,#47810,#47811,#47812,#47813,#47814,#47815,#47816,#47817,#47818,
#47819,#47820,#47821,#47822),.UNSPECIFIED.,.F.,.F.,(4,2,2,2,2,2,2,2,2,2,
2,2,2,2,2,2,2,2,2,2,4),(0.428604909966747,0.445529583287182,0.547065009487481,
0.624452539467869,0.725617321863814,0.819296188596134,0.914887254159531,
1.01199255838545,1.09096737493364,1.19247445741117,1.28625834692512,1.33639550374713,
1.43719821430216,1.50412082096437,1.55130356074699,1.64616163870914,1.74581251906439,
1.8369972558916,1.9185225652106,1.96301176268206,2.01706548363289),
 .UNSPECIFIED.);
#753=B_SPLINE_CURVE_WITH_KNOTS('',3,(#47827,#47828,#47829,#47830,#47831,
#47832,#47833,#47834,#47835,#47836,#47837,#47838,#47839,#47840,#47841,#47842,
#47843,#47844,#47845,#47846,#47847,#47848,#47849,#47850,#47851,#47852,#47853,
#47854,#47855,#47856,#47857,#47858,#47859,#47860,#47861,#47862,#47863,#47864,
#47865,#47866,#47867,#47868,#47869,#47870),.UNSPECIFIED.,.F.,.F.,(4,2,2,
2,2,2,2,2,2,2,2,2,2,2,2,2,2,2,2,2,2,4),(0.000341705276625282,0.0560928328092873,
0.102790668391616,0.184374451969009,0.286732434312196,0.331732934943196,
0.417676823545026,0.466062468242685,0.515746518663139,0.564570875086013,
0.643435069330897,0.744805452143349,0.841979042757459,0.925117184647647,
1.02054525775881,1.10245593081841,1.20364640868695,1.30106169525946,1.35051533162512,
1.45017308381718,1.55030069541036,1.58989822515966),.UNSPECIFIED.);
#754=B_SPLINE_CURVE_WITH_KNOTS('',3,(#47872,#47873,#47874,#47875,#47876,
#47877,#47878,#47879,#47880,#47881,#47882,#47883,#47884,#47885,#47886,#47887,
#47888,#47889,#47890,#47891,#47892,#47893,#47894,#47895,#47896,#47897,#47898,
#47899,#47900,#47901,#47902,#47903,#47904,#47905),.UNSPECIFIED.,.F.,.F.,
(4,2,2,2,2,2,2,2,2,2,2,2,2,2,2,2,4),(2.01706548363289,2.06402058510678,
2.11258685382852,2.21344856852205,2.31199447340875,2.36028586383664,2.45063151831325,
2.5514528244517,2.64909661933046,2.73923168408122,2.78684519594595,2.88733463019532,
2.98400799147551,3.0735739102523,3.12210765377232,3.21406068429801,3.29229578180851),
 .UNSPECIFIED.);
#755=B_SPLINE_CURVE_WITH_KNOTS('',3,(#47906,#47907,#47908,#47909,#47910,
#47911,#47912,#47913,#47914,#47915),.UNSPECIFIED.,.F.,.F.,(4,2,2,2,4),(0.000546235713184444,
0.0692821643427151,0.15084981789586,0.24746567567304,0.3106638555438),
 .UNSPECIFIED.);
#756=B_SPLINE_CURVE_WITH_KNOTS('',3,(#47921,#47922,#47923,#47924),
 .UNSPECIFIED.,.F.,.F.,(4,4),(1.58665344971703,1.58674871126382),
 .UNSPECIFIED.);
#757=B_SPLINE_CURVE_WITH_KNOTS('',3,(#47926,#47927,#47928,#47929,#47930,
#47931,#47932,#47933,#47934,#47935,#47936,#47937,#47938,#47939,#47940,#47941,
#47942,#47943,#47944,#47945,#47946,#47947,#47948,#47949,#47950,#47951,#47952,
#47953,#47954,#47955,#47956,#47957,#47958,#47959),.UNSPECIFIED.,.F.,.F.,
(4,2,2,2,2,2,2,2,2,2,2,2,2,2,2,2,4),(1.00000009372207E-6,0.0914529989276999,
0.191958650169849,0.276092173518159,0.376470995555748,0.459934127269538,
0.560923245043053,0.64585410666141,0.695543265710111,0.777019748534897,
0.822880712206414,0.923353130505685,1.0117585768333,1.11236877445855,1.19804423061871,
1.29811833254116,1.39109815874005),.UNSPECIFIED.);
#758=B_SPLINE_CURVE_WITH_KNOTS('',3,(#47961,#47962,#47963,#47964,#47965,
#47966,#47967,#47968,#47969,#47970,#47971,#47972,#47973,#47974,#47975,#47976,
#47977,#47978,#47979,#47980,#47981,#47982,#47983,#47984,#47985,#47986,#47987,
#47988,#47989,#47990,#47991),.UNSPECIFIED.,.F.,.F.,(4,3,3,3,3,3,3,3,3,3,
4),(0.00155980632875505,0.00467670428344775,0.0108997205793838,0.0233044349028981,
0.0483422336533325,0.0735317838257157,0.0983723994983146,0.118769142279212,
0.152602909073467,0.163507164534158,0.194306062421083),.UNSPECIFIED.);
#759=B_SPLINE_CURVE_WITH_KNOTS('',3,(#47992,#47993,#47994,#47995),
 .UNSPECIFIED.,.F.,.F.,(4,4),(0.00013539478902181,0.000341705276625282),
 .UNSPECIFIED.);
#760=B_SPLINE_CURVE_WITH_KNOTS('',3,(#47997,#47998,#47999,#48000,#48001,
#48002,#48003,#48004,#48005,#48006,#48007,#48008,#48009,#48010,#48011,#48012,
#48013,#48014,#48015,#48016,#48017,#48018,#48019,#48020,#48021,#48022,#48023,
#48024,#48025,#48026,#48027,#48028,#48029,#48030,#48031,#48032,#48033,#48034,
#48035,#48036,#48037,#48038),.UNSPECIFIED.,.F.,.F.,(4,2,2,2,2,2,2,2,2,2,
2,2,2,2,2,2,2,2,2,2,4),(0.3106638555438,0.345520813405148,0.438855187371024,
0.540468398856733,0.632954100967386,0.682167393955402,0.777701028875872,
0.828190357719904,0.877246102039471,0.978219152787592,1.07601538620938,
1.12452184255947,1.22317843275787,1.27114226129121,1.31952796216626,1.42033510923658,
1.4692222924981,1.56875812994508,1.61522154097716,1.68738346703665,1.75387240600549),
 .UNSPECIFIED.);
#761=B_SPLINE_CURVE_WITH_KNOTS('',3,(#48040,#48041,#48042,#48043,#48044,
#48045),.UNSPECIFIED.,.F.,.F.,(4,2,4),(1.70615880496912E-5,0.0719633053329676,
0.14405946356654),.UNSPECIFIED.);
#762=B_SPLINE_CURVE_WITH_KNOTS('',3,(#48046,#48047,#48048,#48049),
 .UNSPECIFIED.,.F.,.F.,(4,4),(4.2050335126144E-6,0.000109190503574576),
 .UNSPECIFIED.);
#763=B_SPLINE_CURVE_WITH_KNOTS('',3,(#48055,#48056,#48057,#48058),
 .UNSPECIFIED.,.F.,.F.,(4,4),(1.52690522644045,1.5269547118134),
 .UNSPECIFIED.);
#764=B_SPLINE_CURVE_WITH_KNOTS('',3,(#48059,#48060,#48061,#48062,#48063,
#48064,#48065,#48066,#48067,#48068,#48069,#48070,#48071,#48072,#48073,#48074,
#48075,#48076,#48077,#48078,#48079,#48080,#48081,#48082,#48083,#48084,#48085,
#48086,#48087,#48088,#48089,#48090,#48091,#48092,#48093,#48094,#48095,#48096,
#48097,#48098,#48099,#48100,#48101,#48102,#48103,#48104),.UNSPECIFIED.,
 .F.,.F.,(4,2,2,2,2,2,2,2,2,2,2,2,2,2,2,2,2,2,2,2,2,2,4),(8.20148954344905E-6,
0.0733429545867836,0.150301022577521,0.198847604410379,0.300002773164144,
0.399490303765739,0.448556694297784,0.496902763145731,0.592825595248763,
0.643551222672669,0.692340666989221,0.793378991921083,0.842199664407604,
0.892120800865433,0.986899677250673,1.08211067812445,1.12831172383911,1.22931229191877,
1.32305075053588,1.37144823302362,1.46280899557072,1.52902673345602,1.58665344971703),
 .UNSPECIFIED.);
#765=B_SPLINE_CURVE_WITH_KNOTS('',3,(#48105,#48106,#48107,#48108,#48109,
#48110,#48111,#48112,#48113,#48114,#48115,#48116,#48117,#48118,#48119,#48120,
#48121,#48122,#48123,#48124,#48125,#48126,#48127,#48128,#48129,#48130,#48131,
#48132,#48133,#48134,#48135,#48136,#48137,#48138,#48139,#48140,#48141,#48142,
#48143,#48144),.UNSPECIFIED.,.F.,.F.,(4,2,2,2,2,2,2,2,2,2,2,2,2,2,2,2,2,
2,2,4),(0.000109190503574576,0.0931915287847442,0.193793529234649,0.242818234568438,
0.340825947034013,0.430115799896213,0.531798734395658,0.632497388800296,
0.714755117226066,0.81324805833013,0.884777328630934,0.986517570464202,
1.03040325379661,1.10745127824861,1.20895044502336,1.30717346411687,1.39380073308839,
1.4943510402189,1.563518198958,1.59273035347225),.UNSPECIFIED.);
#766=B_SPLINE_CURVE_WITH_KNOTS('',3,(#48150,#48151,#48152,#48153,#48154,
#48155),.UNSPECIFIED.,.F.,.F.,(4,2,4),(3.17452747086746,3.17498472826448,
3.23986154436098),.UNSPECIFIED.);
#767=B_SPLINE_CURVE_WITH_KNOTS('',3,(#48156,#48157,#48158,#48159,#48160,
#48161,#48162,#48163,#48164,#48165,#48166,#48167,#48168,#48169,#48170,#48171,
#48172,#48173,#48174,#48175,#48176,#48177,#48178,#48179,#48180,#48181,#48182,
#48183,#48184,#48185,#48186,#48187,#48188,#48189,#48190,#48191,#48192,#48193,
#48194,#48195,#48196,#48197,#48198,#48199),.UNSPECIFIED.,.F.,.F.,(4,2,2,
2,2,2,2,2,2,2,2,2,2,2,2,2,2,2,2,2,2,4),(0.,0.0680186494305738,0.147676699355569,
0.235953182143958,0.285547214660472,0.376247643903819,0.470614224147492,
0.570259024729443,0.668194135923833,0.716238677096708,0.763441689184039,
0.860628057911294,0.910841062199871,0.956846564037905,1.05884988772573,
1.15320390167318,1.24910472962057,1.29541955762797,1.39740642862325,1.45930066606842,
1.49100971138413,1.52690522644045),.UNSPECIFIED.);
#768=B_SPLINE_CURVE_WITH_KNOTS('',3,(#48201,#48202,#48203,#48204,#48205,
#48206,#48207,#48208,#48209,#48210,#48211,#48212,#48213,#48214,#48215,#48216,
#48217,#48218,#48219,#48220,#48221,#48222,#48223,#48224,#48225,#48226,#48227,
#48228,#48229,#48230,#48231,#48232,#48233,#48234,#48235,#48236,#48237,#48238,
#48239,#48240),.UNSPECIFIED.,.F.,.F.,(4,2,2,2,2,2,2,2,2,2,2,2,2,2,2,2,2,
2,2,4),(1.59273035347225,1.66505000446301,1.74724033904894,1.79141405934091,
1.89276848186806,1.94106112316785,2.04236543169102,2.13992244944502,2.18875968529191,
2.27856804179947,2.37984834121376,2.47624614257626,2.52491305274713,2.61452913633043,
2.71554383228709,2.81108550047719,2.8596507303388,2.94828748249565,3.04448466377449,
3.12687551391254),.UNSPECIFIED.);
#769=B_SPLINE_CURVE_WITH_KNOTS('',3,(#48241,#48242,#48243,#48244),
 .UNSPECIFIED.,.F.,.F.,(4,4),(0.000550918055278865,0.0552481405980463),
 .UNSPECIFIED.);
#770=B_SPLINE_CURVE_WITH_KNOTS('',3,(#48249,#48250,#48251,#48252,#48253,
#48254,#48255,#48256,#48257,#48258,#48259,#48260,#48261,#48262,#48263,#48264,
#48265,#48266,#48267,#48268,#48269,#48270,#48271,#48272,#48273,#48274,#48275,
#48276,#48277,#48278,#48279,#48280,#48281,#48282,#48283,#48284,#48285,#48286,
#48287,#48288),.UNSPECIFIED.,.F.,.F.,(4,2,2,2,2,2,2,2,2,2,2,2,2,2,2,2,2,
2,2,4),(1.58954882556145,1.61994694155016,1.72111687689724,1.76953629068976,
1.86004171494891,1.96135645219197,2.05437746056574,2.10311900473412,2.19774598905527,
2.2986696589194,2.36402330234716,2.45765034270909,2.55918959039695,2.65837551289255,
2.74927194990235,2.83713438799803,2.90572543240668,3.00347539627398,3.10350357217783,
3.17452747086746),.UNSPECIFIED.);
#771=B_SPLINE_CURVE_WITH_KNOTS('',3,(#48289,#48290,#48291,#48292,#48293,
#48294,#48295,#48296,#48297,#48298,#48299,#48300,#48301,#48302,#48303,#48304,
#48305,#48306,#48307,#48308,#48309,#48310,#48311,#48312,#48313,#48314,#48315,
#48316,#48317,#48318,#48319,#48320,#48321,#48322,#48323,#48324,#48325,#48326,
#48327,#48328,#48329,#48330),.UNSPECIFIED.,.F.,.F.,(4,2,2,2,2,2,2,2,2,2,
2,2,2,2,2,2,2,2,2,2,4),(0.0552481405980463,0.0553431489108911,0.115543456159899,
0.210045383711121,0.306300846524538,0.398105513813643,0.487896698019488,
0.538071256306237,0.629719711437245,0.724376190949434,0.825197212458761,
0.924936205324376,0.973410366125791,1.07331868508949,1.17233739929906,1.22105376960377,
1.32230277165209,1.4202679363978,1.51436814529117,1.60994983209693,1.64703455004425),
 .UNSPECIFIED.);
#772=B_SPLINE_CURVE_WITH_KNOTS('',3,(#48336,#48337,#48338,#48339),
 .UNSPECIFIED.,.F.,.F.,(4,4),(0.0272291530888202,0.0273067833034242),
 .UNSPECIFIED.);
#773=B_SPLINE_CURVE_WITH_KNOTS('',3,(#48340,#48341,#48342,#48343,#48344,
#48345,#48346,#48347,#48348,#48349,#48350,#48351,#48352,#48353,#48354,#48355,
#48356,#48357,#48358,#48359,#48360,#48361,#48362,#48363,#48364,#48365,#48366,
#48367,#48368,#48369,#48370,#48371,#48372,#48373,#48374,#48375,#48376,#48377,
#48378,#48379,#48380,#48381,#48382,#48383),.UNSPECIFIED.,.F.,.F.,(4,2,2,
2,2,2,2,2,2,2,2,2,2,2,2,2,2,2,2,2,2,4),(1.00000018631629E-6,0.0905679837143679,
0.179742205585551,0.276160654514949,0.32512840106993,0.417516088904147,
0.466418315869915,0.566670317298738,0.654236472477998,0.75567445571018,
0.846198850084504,0.928573188796696,1.02712838427427,1.07634585028451,1.1748235354661,
1.22376269978151,1.31992682439122,1.37015346607007,1.4200367796879,1.52107771731938,
1.56988937965821,1.58954882556145),.UNSPECIFIED.);
#774=B_SPLINE_CURVE_WITH_KNOTS('',3,(#48384,#48385,#48386,#48387,#48388,
#48389,#48390,#48391,#48392,#48393,#48394,#48395,#48396,#48397,#48398,#48399,
#48400,#48401,#48402,#48403,#48404,#48405,#48406,#48407,#48408,#48409,#48410,
#48411,#48412,#48413,#48414,#48415,#48416,#48417,#48418,#48419,#48420,#48421,
#48422,#48423,#48424,#48425,#48426,#48427,#48428,#48429),.UNSPECIFIED.,
 .F.,.F.,(4,2,2,2,2,2,2,2,2,2,2,2,2,2,2,2,2,2,2,2,2,2,4),(1.64703455004425,
1.66024315979441,1.70914644311717,1.81028344660311,1.85831612652545,1.95937444897362,
2.06062861635938,2.10919013003134,2.15862064062204,2.25104129654871,2.30077954150846,
2.34822840849651,2.44910652315638,2.49603004296635,2.58332529821825,2.67779176069456,
2.72684247326199,2.81434388849864,2.91589263902365,3.01005996359688,3.09956324210311,
3.19323112914222,3.2335044050079),.UNSPECIFIED.);
#775=B_SPLINE_CURVE_WITH_KNOTS('',3,(#48436,#48437,#48438,#48439,#48440,
#48441,#48442,#48443,#48444,#48445,#48446,#48447,#48448,#48449,#48450,#48451,
#48452,#48453,#48454,#48455,#48456,#48457,#48458,#48459,#48460,#48461,#48462,
#48463,#48464,#48465,#48466,#48467,#48468,#48469,#48470,#48471,#48472,#48473,
#48474,#48475,#48476,#48477,#48478,#48479,#48480,#48481),.UNSPECIFIED.,
 .F.,.F.,(4,2,2,2,2,2,2,2,2,2,2,2,2,2,2,2,2,2,2,2,2,2,4),(-2.1855659803523,
-2.1060005592318,-2.01694296594534,-1.96901256052504,-1.86973206877917,
-1.77661798959221,-1.7274257082086,-1.67776494030543,-1.58450065227025,
-1.53434330399221,-1.43682863158872,-1.38746760106178,-1.28974491299529,
-1.23998499123436,-1.19135175996526,-1.14184453125496,-1.09301970067391,
-1.0431147266302,-0.994114591646302,-0.944106478309579,-0.895086657006542,
-0.844989929727302,-0.793898774335287),.UNSPECIFIED.);
#776=B_SPLINE_CURVE_WITH_KNOTS('',3,(#48483,#48484,#48485,#48486,#48487,
#48488,#48489,#48490,#48491,#48492,#48493,#48494,#48495,#48496,#48497,#48498,
#48499,#48500,#48501,#48502,#48503,#48504,#48505,#48506,#48507,#48508,#48509,
#48510,#48511,#48512,#48513,#48514,#48515,#48516,#48517,#48518,#48519,#48520,
#48521,#48522,#48523,#48524,#48525,#48526,#48527,#48528,#48529,#48530,#48531),
 .UNSPECIFIED.,.F.,.F.,(4,3,3,3,3,3,3,3,3,3,3,3,3,3,3,3,4),(0.00230840540264672,
0.00310329427917845,0.0166018506520161,0.0301004070248538,0.0544449092607173,
0.0571114353405323,0.0643911154884955,0.0644105816672325,0.0889679651173259,
0.0912098467045946,0.100490355331003,0.126749317454847,0.153598562219919,
0.158399345765457,0.15843447591468,0.185342050715828,0.194940455552248),
 .UNSPECIFIED.);
#777=B_SPLINE_CURVE_WITH_KNOTS('',3,(#48535,#48536,#48537,#48538,#48539,
#48540,#48541,#48542,#48543,#48544,#48545,#48546,#48547,#48548,#48549,#48550,
#48551,#48552,#48553,#48554,#48555,#48556),.UNSPECIFIED.,.F.,.F.,(4,2,2,
2,2,2,2,2,2,2,4),(0.000119906415017354,0.0675877728219243,0.149050275973358,
0.247839430914635,0.296210880517655,0.397796827580989,0.477892848335411,
0.573960419844177,0.621161322113836,0.702422731226525,0.795597339453887),
 .UNSPECIFIED.);
#778=B_SPLINE_CURVE_WITH_KNOTS('',3,(#48559,#48560,#48561,#48562,#48563,
#48564,#48565,#48566,#48567,#48568,#48569,#48570,#48571,#48572,#48573,#48574,
#48575,#48576,#48577,#48578,#48579,#48580),.UNSPECIFIED.,.F.,.F.,(4,2,2,
2,2,2,2,2,2,2,4),(-0.793898774335287,-0.746514719997815,-0.648277050769764,
-0.599653567815491,-0.499874425645475,-0.399738910701365,-0.305164360470678,
-0.207651154701469,-0.109238030629384,-0.0578922718396024,0.),
 .UNSPECIFIED.);
#779=B_SPLINE_CURVE_WITH_KNOTS('',3,(#48583,#48584,#48585,#48586,#48587,
#48588,#48589,#48590,#48591,#48592,#48593,#48594,#48595,#48596,#48597,#48598,
#48599,#48600,#48601,#48602,#48603,#48604,#48605,#48606,#48607,#48608,#48609,
#48610,#48611,#48612,#48613,#48614,#48615,#48616,#48617,#48618,#48619,#48620,
#48621,#48622,#48623,#48624),.UNSPECIFIED.,.F.,.F.,(4,2,2,2,2,2,2,2,2,2,
2,2,2,2,2,2,2,2,2,2,4),(4.04744268479612E-5,0.0723888050419246,0.150253876730198,
0.244248023045839,0.343763946381597,0.435081640514679,0.484290834942794,
0.584376734907669,0.681113147042144,0.72998400442407,0.779993622576139,
0.880540287813974,0.980078111135639,1.08102675755066,1.12973105890516,1.23061503227431,
1.27986097964202,1.37809314185868,1.42365730090318,1.49407955944685,1.55994181257962),
 .UNSPECIFIED.);
#780=B_SPLINE_CURVE_WITH_KNOTS('',3,(#48625,#48626,#48627,#48628,#48629,
#48630),.UNSPECIFIED.,.F.,.F.,(4,2,4),(2.4381224475444E-5,0.0136379782908506,
0.0272291530888202),.UNSPECIFIED.);
#781=B_SPLINE_CURVE_WITH_KNOTS('',3,(#48632,#48633,#48634,#48635,#48636,
#48637,#48638,#48639,#48640,#48641,#48642,#48643,#48644,#48645,#48646,#48647,
#48648,#48649,#48650,#48651,#48652,#48653,#48654,#48655,#48656,#48657,#48658,
#48659,#48660,#48661,#48662,#48663,#48664,#48665),.UNSPECIFIED.,.F.,.F.,
(4,2,2,2,2,2,2,2,2,2,2,2,2,2,2,2,4),(3.2335044050079,3.27389245423008,3.35865616251168,
3.45939263362858,3.54385578027792,3.64452294805333,3.72764425789838,3.82907930277935,
3.87317025517201,3.97294041952549,4.05858009238465,4.15598332557383,4.20351932199527,
4.2848801328365,4.38519455201069,4.44868477138579,4.50206007644754),
 .UNSPECIFIED.);
#782=B_SPLINE_CURVE_WITH_KNOTS('',3,(#48667,#48668,#48669,#48670),
 .UNSPECIFIED.,.F.,.F.,(4,4),(-5.68774429195932E-5,0.),.UNSPECIFIED.);
#783=B_SPLINE_CURVE_WITH_KNOTS('',3,(#48672,#48673,#48674,#48675,#48676,
#48677,#48678,#48679,#48680,#48681),.UNSPECIFIED.,.F.,.F.,(4,2,2,2,4),(0.000110635194286315,
0.0642159947776442,0.156548519658155,0.23536697325852,0.312794483273568),
 .UNSPECIFIED.);
#784=B_SPLINE_CURVE_WITH_KNOTS('',3,(#48682,#48683,#48684,#48685),
 .UNSPECIFIED.,.F.,.F.,(4,4),(1.00000011060521E-6,0.000119906415017354),
 .UNSPECIFIED.);
#785=B_SPLINE_CURVE_WITH_KNOTS('',3,(#48845,#48846,#48847,#48848,#48849,
#48850,#48851,#48852,#48853,#48854,#48855,#48856,#48857,#48858,#48859,#48860,
#48861,#48862,#48863,#48864,#48865,#48866,#48867,#48868,#48869,#48870,#48871,
#48872,#48873,#48874,#48875,#48876,#48877,#48878,#48879,#48880,#48881,#48882,
#48883,#48884,#48885,#48886,#48887,#48888,#48889,#48890,#48891,#48892,#48893,
#48894,#48895,#48896,#48897,#48898,#48899,#48900,#48901,#48902,#48903,#48904,
#48905,#48906,#48907,#48908,#48909,#48910,#48911,#48912,#48913,#48914,#48915,
#48916,#48917,#48918,#48919,#48920,#48921,#48922,#48923,#48924,#48925,#48926,
#48927,#48928,#48929,#48930,#48931,#48932,#48933,#48934,#48935,#48936,#48937,
#48938,#48939,#48940,#48941,#48942,#48943,#48944,#48945,#48946,#48947,#48948,
#48949,#48950,#48951,#48952,#48953,#48954,#48955,#48956,#48957,#48958,#48959,
#48960,#48961,#48962,#48963,#48964,#48965,#48966,#48967,#48968,#48969,#48970,
#48971,#48972,#48973,#48974,#48975,#48976,#48977,#48978,#48979,#48980,#48981,
#48982,#48983,#48984,#48985,#48986,#48987,#48988,#48989,#48990,#48991,#48992),
 .UNSPECIFIED.,.F.,.F.,(4,3,3,3,3,3,3,3,3,3,3,3,3,3,3,3,3,3,3,3,3,3,3,3,
3,3,3,3,3,3,3,3,3,3,3,3,3,3,3,3,3,3,3,3,3,3,3,3,3,4),(0.981527464250843,
0.982092490001789,0.982250570201131,0.982821922329735,0.983393387693289,
0.983942796582145,0.984165788573041,0.984222792790674,0.984769994125036,
0.985346304630392,0.985920888527997,0.986193875236633,0.986773936837428,
0.986804823810868,0.987331227961664,0.987856154503689,0.988163327839545,
0.988693044486107,0.989148450490744,0.989443859048694,0.989642599247085,
0.989889591278668,0.990013023081767,0.990074724548194,0.990136417005633,
0.990790401665348,0.991461921896627,0.992082894286521,0.992108550310556,
0.992714880848456,0.993325842358457,0.993927728447798,0.994080943138248,
0.994672953070892,0.994721929524347,0.995187789529314,0.995562865020324,
0.996032292855299,0.996503865055638,0.996971618828127,0.99703909746875,
0.997360964762174,0.997938692768488,0.998485881127698,0.998519885957476,
0.998680482381087,0.999045493804115,0.999413210914547,0.999780332009316,
1.),.UNSPECIFIED.);
#786=B_SPLINE_CURVE_WITH_KNOTS('',3,(#48993,#48994,#48995,#48996,#48997,
#48998,#48999,#49000,#49001,#49002,#49003,#49004,#49005,#49006,#49007,#49008,
#49009,#49010,#49011,#49012,#49013,#49014,#49015,#49016,#49017,#49018,#49019,
#49020,#49021,#49022,#49023,#49024,#49025,#49026,#49027,#49028,#49029,#49030,
#49031,#49032,#49033,#49034,#49035,#49036,#49037,#49038,#49039,#49040,#49041,
#49042,#49043,#49044,#49045,#49046,#49047,#49048,#49049,#49050,#49051,#49052,
#49053,#49054,#49055,#49056,#49057,#49058,#49059,#49060,#49061,#49062,#49063,
#49064,#49065,#49066,#49067,#49068,#49069,#49070,#49071,#49072,#49073,#49074,
#49075,#49076,#49077,#49078,#49079,#49080,#49081,#49082,#49083,#49084,#49085,
#49086,#49087,#49088,#49089,#49090,#49091,#49092,#49093,#49094,#49095,#49096,
#49097,#49098,#49099,#49100,#49101,#49102,#49103,#49104,#49105,#49106,#49107,
#49108,#49109,#49110,#49111,#49112,#49113,#49114,#49115,#49116,#49117,#49118,
#49119,#49120,#49121,#49122,#49123,#49124,#49125,#49126,#49127,#49128,#49129,
#49130,#49131,#49132,#49133,#49134,#49135,#49136,#49137,#49138,#49139,#49140,
#49141,#49142,#49143,#49144,#49145,#49146,#49147,#49148,#49149,#49150,#49151,
#49152,#49153,#49154,#49155,#49156,#49157,#49158,#49159,#49160,#49161,#49162,
#49163,#49164,#49165,#49166,#49167,#49168,#49169,#49170,#49171,#49172,#49173,
#49174,#49175,#49176,#49177,#49178,#49179,#49180,#49181,#49182,#49183,#49184,
#49185,#49186,#49187,#49188,#49189,#49190,#49191,#49192,#49193,#49194,#49195,
#49196,#49197,#49198,#49199,#49200,#49201,#49202,#49203,#49204,#49205,#49206,
#49207,#49208,#49209,#49210,#49211,#49212,#49213,#49214,#49215,#49216,#49217,
#49218,#49219,#49220,#49221,#49222,#49223,#49224,#49225,#49226,#49227,#49228,
#49229,#49230,#49231,#49232,#49233,#49234,#49235,#49236,#49237,#49238,#49239,
#49240,#49241,#49242,#49243,#49244,#49245,#49246,#49247,#49248,#49249,#49250,
#49251,#49252,#49253,#49254,#49255,#49256,#49257,#49258,#49259,#49260,#49261,
#49262,#49263,#49264,#49265,#49266,#49267,#49268,#49269,#49270,#49271,#49272,
#49273,#49274,#49275,#49276,#49277,#49278,#49279,#49280,#49281,#49282,#49283,
#49284,#49285,#49286,#49287,#49288,#49289,#49290,#49291,#49292,#49293,#49294,
#49295,#49296,#49297,#49298,#49299),.UNSPECIFIED.,.F.,.F.,(4,3,3,3,3,3,
3,3,3,3,3,3,3,3,3,3,3,3,3,3,3,3,3,3,3,3,3,3,3,3,3,3,3,3,3,3,3,3,3,3,3,3,
3,3,3,3,3,3,3,3,3,3,3,3,3,3,3,3,3,3,3,3,3,3,3,3,3,3,3,3,3,3,3,3,3,3,3,3,
3,3,3,3,3,3,3,3,3,3,3,3,3,3,3,3,3,3,3,3,3,3,3,3,4),(0.958582012693979,0.959057373153544,
0.959531895240945,0.959882163298524,0.960061197080218,0.960594634397,0.960883867419892,
0.961413301456373,0.961540412003173,0.961887365736604,0.962422945132031,
0.962888489257781,0.963423565588256,0.96388924157441,0.964441816459992,
0.964498841849082,0.964994923825078,0.96551746413172,0.966040004438362,
0.966547126147729,0.966895435246582,0.967423872663115,0.967457271694992,
0.968189830473271,0.968984752914132,0.969906680046786,0.970415701540902,
0.970600603406271,0.970785505271641,0.971155309002379,0.971587448549721,
0.971894916463857,0.972353492511569,0.972816476880084,0.972918959336232,
0.973374131386812,0.973985274440157,0.974113738848289,0.97456746908772,
0.974798134679613,0.974939154315201,0.975447610813723,0.975928659806014,
0.976323723048143,0.976623356656524,0.97720260783381,0.977433429455508,
0.977844575774526,0.978394852988506,0.978937302512818,0.979241928683297,
0.979436661700231,0.980111702826308,0.980442642818478,0.980783654976453,
0.981457437902959,0.981947209563255,0.982241057646065,0.98241526310154,
0.983131880691015,0.983452142949751,0.984204488767931,0.984365727673976,
0.98495683458611,0.985555059044411,0.986008035827076,0.986177825090869,
0.986358085398057,0.986461012609742,0.987286338640029,0.987965464622891,
0.988263610898574,0.988834391871281,0.989222790004238,0.989468539305708,
0.989863717687797,0.990058804384792,0.990138567180301,0.99059027119165,
0.990971780718536,0.991424690022283,0.991881017331188,0.99211085374424,
0.992704130080236,0.993282699864252,0.993804782958349,0.99397983369436,
0.99408314030818,0.994581798219916,0.995072076725526,0.995562355231135,
0.995988544787359,0.996408145874342,0.996820844800321,0.996993103554728,
0.99704157015409,0.997589077496104,0.998172708728611,0.998496173800892,
0.998520785077045,0.999156675232777,0.999733891928085,1.),.UNSPECIFIED.);
#787=B_SPLINE_CURVE_WITH_KNOTS('',3,(#49449,#49450,#49451,#49452,#49453,
#49454,#49455,#49456,#49457,#49458,#49459,#49460,#49461,#49462,#49463,#49464,
#49465,#49466,#49467,#49468,#49469,#49470,#49471,#49472,#49473,#49474,#49475,
#49476,#49477,#49478,#49479,#49480,#49481,#49482,#49483,#49484,#49485,#49486,
#49487,#49488,#49489,#49490,#49491,#49492,#49493,#49494,#49495,#49496,#49497,
#49498,#49499,#49500,#49501,#49502,#49503,#49504,#49505,#49506,#49507,#49508,
#49509,#49510,#49511,#49512,#49513,#49514,#49515,#49516,#49517,#49518,#49519,
#49520,#49521,#49522,#49523,#49524,#49525,#49526,#49527,#49528,#49529,#49530,
#49531,#49532,#49533,#49534,#49535,#49536,#49537,#49538,#49539,#49540,#49541,
#49542,#49543,#49544,#49545,#49546,#49547,#49548,#49549,#49550,#49551,#49552,
#49553,#49554,#49555,#49556,#49557,#49558,#49559,#49560,#49561,#49562,#49563,
#49564,#49565,#49566,#49567,#49568,#49569,#49570,#49571,#49572,#49573,#49574,
#49575,#49576,#49577,#49578,#49579,#49580,#49581,#49582,#49583,#49584,#49585,
#49586,#49587,#49588,#49589,#49590,#49591,#49592,#49593,#49594,#49595,#49596,
#49597,#49598,#49599,#49600,#49601,#49602,#49603,#49604,#49605,#49606,#49607,
#49608,#49609,#49610,#49611,#49612,#49613,#49614,#49615,#49616,#49617,#49618,
#49619,#49620,#49621,#49622,#49623,#49624,#49625,#49626,#49627,#49628,#49629,
#49630,#49631,#49632,#49633,#49634,#49635,#49636,#49637,#49638,#49639,#49640,
#49641,#49642,#49643,#49644,#49645,#49646,#49647,#49648,#49649,#49650,#49651,
#49652,#49653,#49654,#49655,#49656,#49657,#49658,#49659,#49660,#49661,#49662,
#49663,#49664,#49665,#49666,#49667,#49668,#49669,#49670,#49671,#49672,#49673,
#49674,#49675,#49676,#49677),.UNSPECIFIED.,.F.,.F.,(4,3,3,3,3,3,3,3,3,3,
3,3,3,3,3,3,3,3,3,3,3,3,3,3,3,3,3,3,3,3,3,3,3,3,3,3,3,3,3,3,3,3,3,3,3,3,
3,3,3,3,3,3,3,3,3,3,3,3,3,3,3,3,3,3,3,3,3,3,3,3,3,3,3,3,3,3,4),(0.,0.000359963247642554,
0.000730782414337265,0.00109740071145868,0.00147032031294004,0.0018432399144214,
0.00205249069972499,0.00246150015657244,0.00287147315877874,0.00327897649381078,
0.00368647982884281,0.00409556414483304,0.00466610669130213,0.00523323942328513,
0.00552971974326421,0.0059521096061035,0.00614735487448577,0.00656909827483017,
0.00698845597869335,0.00737295965768562,0.0079845207093368,0.00819395765445556,
0.00827915432352533,0.0083643463698637,0.00853472530094449,0.00887552345905345,
0.0094701356547484,0.00955776993844597,0.00983061287691415,0.0104636984438137,
0.0109235719412858,0.0115603343811466,0.0121819050867249,0.0122882660961427,
0.0122883630402977,0.0127442522716054,0.0132022542537409,0.013517092705757,
0.0136535057723781,0.0140302785058248,0.0141315060105641,0.0144387126629677,
0.0147285348775666,0.0147459193153712,0.0150194560827448,0.0156407003907238,
0.01626246681243,0.0163840835398903,0.0169918228636084,0.0172035725345998,
0.0174092876371001,0.0179973749126947,0.0184340180115974,0.0190184385959836,
0.0194590321259564,0.0196612257538283,0.0199723493251172,0.0204851674142444,
0.021014578815863,0.0215667288944599,0.0220834328614806,0.0221188789730568,
0.0225373035513935,0.023173079715083,0.0238191067694135,0.0244491815377821,
0.0245765321922854,0.0245864657268039,0.0251991054859768,0.0258053588018997,
0.0263050134535735,0.0266347536340908,0.0270341854115139,0.0275500268891959,
0.0280703359425124,0.0285935267829691,0.0286806425028429),.UNSPECIFIED.);
#788=B_SPLINE_CURVE_WITH_KNOTS('',3,(#49680,#49681,#49682,#49683,#49684,
#49685,#49686,#49687,#49688,#49689,#49690,#49691,#49692,#49693,#49694,#49695,
#49696,#49697,#49698,#49699,#49700,#49701,#49702,#49703,#49704,#49705),
 .UNSPECIFIED.,.F.,.F.,(4,1,1,1,1,1,1,1,1,1,1,1,1,1,1,1,1,1,1,1,1,1,1,4),
(0.,0.00168771915268776,0.00337543830537552,0.00675087661075104,0.0101263149161266,
0.0135017532215021,0.0157520454250858,0.0180023376286695,0.0202526298322531,
0.0219403489849409,0.0236280681376287,0.0253157872903164,0.0270035064430042,
0.0292537986465879,0.0315040908501715,0.0337543830537552,0.0360046752573389,
0.0382549674609226,0.0405052596645063,0.0427555518680899,0.0450058440716736,
0.0472561362752573,0.049506428478841,0.0516089027088776),.UNSPECIFIED.);
#789=B_SPLINE_CURVE_WITH_KNOTS('',3,(#49954,#49955,#49956,#49957,#49958,
#49959,#49960,#49961,#49962,#49963,#49964,#49965,#49966,#49967,#49968,#49969,
#49970,#49971,#49972,#49973,#49974,#49975,#49976,#49977,#49978,#49979,#49980,
#49981,#49982,#49983,#49984,#49985,#49986,#49987,#49988,#49989,#49990,#49991,
#49992,#49993,#49994,#49995,#49996,#49997,#49998,#49999,#50000,#50001,#50002,
#50003,#50004,#50005,#50006,#50007,#50008,#50009,#50010,#50011,#50012,#50013,
#50014,#50015,#50016,#50017,#50018,#50019,#50020,#50021,#50022,#50023,#50024,
#50025,#50026,#50027,#50028,#50029,#50030,#50031,#50032,#50033,#50034,#50035,
#50036,#50037,#50038,#50039,#50040,#50041,#50042,#50043,#50044,#50045,#50046,
#50047,#50048,#50049,#50050,#50051,#50052,#50053,#50054,#50055,#50056,#50057,
#50058,#50059,#50060,#50061,#50062,#50063,#50064,#50065,#50066,#50067,#50068,
#50069,#50070,#50071,#50072,#50073,#50074,#50075,#50076,#50077,#50078,#50079,
#50080,#50081,#50082,#50083,#50084,#50085,#50086,#50087,#50088,#50089,#50090,
#50091,#50092,#50093,#50094,#50095,#50096,#50097,#50098,#50099,#50100,#50101,
#50102,#50103,#50104,#50105,#50106,#50107,#50108,#50109,#50110,#50111,#50112,
#50113,#50114,#50115,#50116,#50117,#50118,#50119,#50120,#50121,#50122,#50123,
#50124,#50125,#50126,#50127,#50128,#50129,#50130,#50131,#50132,#50133,#50134,
#50135,#50136,#50137,#50138,#50139,#50140,#50141,#50142,#50143,#50144,#50145,
#50146,#50147,#50148,#50149,#50150,#50151,#50152,#50153,#50154,#50155,#50156,
#50157,#50158,#50159,#50160,#50161,#50162,#50163,#50164,#50165,#50166,#50167,
#50168,#50169,#50170,#50171,#50172,#50173,#50174,#50175,#50176,#50177,#50178,
#50179,#50180,#50181,#50182,#50183,#50184,#50185,#50186,#50187,#50188,#50189,
#50190,#50191,#50192,#50193,#50194,#50195,#50196,#50197,#50198,#50199,#50200,
#50201,#50202,#50203,#50204,#50205,#50206,#50207,#50208,#50209,#50210,#50211,
#50212,#50213,#50214,#50215,#50216,#50217,#50218,#50219,#50220,#50221,#50222,
#50223,#50224,#50225,#50226,#50227,#50228,#50229,#50230,#50231,#50232,#50233,
#50234,#50235,#50236,#50237,#50238,#50239,#50240,#50241,#50242,#50243,#50244,
#50245,#50246,#50247,#50248,#50249,#50250,#50251,#50252,#50253,#50254,#50255,
#50256,#50257,#50258,#50259,#50260,#50261,#50262,#50263,#50264,#50265,#50266,
#50267,#50268,#50269,#50270,#50271,#50272,#50273,#50274,#50275,#50276,#50277,
#50278,#50279,#50280,#50281,#50282,#50283,#50284,#50285,#50286,#50287,#50288,
#50289,#50290,#50291,#50292,#50293,#50294,#50295,#50296,#50297,#50298,#50299,
#50300,#50301,#50302,#50303,#50304,#50305,#50306,#50307,#50308,#50309,#50310,
#50311,#50312,#50313,#50314,#50315,#50316,#50317,#50318,#50319,#50320,#50321,
#50322,#50323,#50324,#50325,#50326,#50327,#50328,#50329,#50330,#50331,#50332,
#50333,#50334,#50335,#50336,#50337,#50338,#50339,#50340,#50341,#50342,#50343,
#50344,#50345,#50346,#50347,#50348,#50349,#50350,#50351,#50352,#50353,#50354,
#50355,#50356,#50357,#50358,#50359,#50360,#50361,#50362,#50363,#50364,#50365,
#50366,#50367,#50368,#50369,#50370,#50371,#50372,#50373,#50374,#50375,#50376,
#50377,#50378,#50379,#50380,#50381,#50382,#50383,#50384,#50385,#50386,#50387,
#50388,#50389,#50390,#50391,#50392,#50393,#50394,#50395,#50396,#50397,#50398,
#50399,#50400,#50401,#50402,#50403,#50404,#50405,#50406,#50407,#50408,#50409,
#50410,#50411,#50412,#50413,#50414,#50415,#50416,#50417,#50418,#50419,#50420,
#50421,#50422,#50423,#50424,#50425,#50426,#50427,#50428,#50429,#50430,#50431,
#50432,#50433,#50434,#50435,#50436,#50437,#50438,#50439,#50440,#50441,#50442,
#50443,#50444,#50445,#50446,#50447,#50448,#50449,#50450,#50451,#50452,#50453,
#50454,#50455,#50456,#50457,#50458,#50459,#50460,#50461,#50462,#50463,#50464,
#50465,#50466,#50467,#50468,#50469,#50470,#50471,#50472,#50473,#50474,#50475,
#50476,#50477,#50478,#50479,#50480,#50481,#50482,#50483,#50484,#50485,#50486,
#50487,#50488,#50489,#50490,#50491,#50492,#50493,#50494,#50495,#50496,#50497,
#50498,#50499,#50500,#50501,#50502,#50503,#50504,#50505,#50506,#50507,#50508,
#50509,#50510,#50511,#50512,#50513,#50514,#50515,#50516,#50517,#50518,#50519,
#50520,#50521,#50522,#50523,#50524),.UNSPECIFIED.,.F.,.F.,(4,3,3,3,3,3,
3,3,3,3,3,3,3,3,3,3,3,3,3,3,3,3,3,3,3,3,3,3,3,3,3,3,3,3,3,3,3,3,3,3,3,3,
3,3,3,3,3,3,3,3,3,3,3,3,3,3,3,3,3,3,3,3,3,3,3,3,3,3,3,3,3,3,3,3,3,3,3,3,
3,3,3,3,3,3,3,3,3,3,3,3,3,3,3,3,3,3,3,3,3,3,3,3,3,3,3,3,3,3,3,3,3,3,3,3,
3,3,3,3,3,3,3,3,3,3,3,3,3,3,3,3,3,3,3,3,3,3,3,3,3,3,3,3,3,3,3,3,3,3,3,3,
3,3,3,3,3,3,3,3,3,3,3,3,3,3,3,3,3,3,3,3,3,3,3,3,3,3,3,3,3,3,3,3,3,3,3,3,
3,3,3,3,4),(0.116743831555477,0.117271549516828,0.11780216534719,0.11788849433131,
0.118426160808469,0.118587303856748,0.11917275494541,0.119775021091971,
0.120086717938801,0.120430777434874,0.121054310593861,0.121685110717334,
0.122274251012999,0.12228523422923,0.123031324335223,0.123826254050568,
0.124117724591124,0.124484080881706,0.12508074012303,0.125679687701571,
0.125961198169249,0.126465937736982,0.126682936526009,0.127187310823517,
0.12769297006349,0.127804671747374,0.128380611942788,0.128882267748352,
0.129462222463457,0.1296481453255,0.130246401265819,0.130844664477249,0.131081032058959,
0.131491618903625,0.132216391580684,0.132961094929179,0.13328064537096,
0.133949583674458,0.134564074867167,0.134992464280823,0.135178566059875,
0.135480920211346,0.135944234328319,0.136407548445292,0.136969195600248,
0.137540892158841,0.137679203351775,0.13827235828395,0.138865513216126,
0.13940169277199,0.139877677745977,0.140415028110087,0.140948862946838,
0.141323477986959,0.141853960541869,0.142075928851122,0.142605303520816,
0.143140587343418,0.143664932145426,0.143781442757793,0.144272847527163,
0.144905224088376,0.145547409087995,0.145737719603048,0.146239407528626,
0.14679346636521,0.147203111292158,0.147754842038307,0.14793523366648,0.148082881106752,
0.148640997946119,0.149202345746228,0.149742549988632,0.149926354684877,
0.150134740024583,0.150666497234683,0.151218162748842,0.151731359132526,
0.151769828263002,0.152255334955058,0.152738824720568,0.153068393525934,
0.153546079527893,0.153613301841127,0.154134366158647,0.154663823869616,
0.15518067074369,0.155456775419252,0.155933374262726,0.156001424139149,
0.156474008906968,0.156949475429383,0.157300248997378,0.157822080516296,
0.158342074467166,0.158850602623591,0.158934402298568,0.159143722575503,
0.159618178955598,0.160094893609646,0.160566033713449,0.160987196153628,
0.161534655156901,0.16186632610495,0.162409222101943,0.162597882746008,
0.162830669731753,0.163329952357396,0.164061883361872,0.164674143309878,
0.164794026868702,0.165224924373528,0.165639434318916,0.16605195816296,
0.16646105129726,0.166517616888004,0.166948623268704,0.167376252184625,
0.167726925135452,0.168152505538122,0.168361090466129,0.168918885736223,
0.169493042266387,0.170052921258187,0.170204564044254,0.170661873459268,
0.17111916645363,0.171583602038004,0.172048037622379,0.172128378269063,
0.172672616208526,0.172861957993751,0.173407038755241,0.1735948610192,0.173891511200504,
0.174445121479788,0.17499691825412,0.175548715028451,0.17573498477863,0.176037821849044,
0.176526392526301,0.177132526087169,0.177503099434671,0.178104359208324,
0.178192949549463,0.178698491217907,0.179210480324561,0.179457562571755,
0.179967365167328,0.180470635330094,0.180650914320297,0.181182328720393,
0.181656663721916,0.182185008959917,0.182710296611938,0.18310887909113,
0.183628901543184,0.183855228361026,0.184378510206937,0.184904700846289,
0.185423217261101,0.185566843861964,0.18605279219044,0.186521820203989,
0.186795826247381,0.187361663261442,0.187921947018491,0.188024808632798,
0.18825153231159,0.188963922315969,0.189709904046076,0.190450508127851,
0.190482773403631,0.19109726459634,0.191711755789048,0.19220148550707,0.192651271329696,
0.192940738174465,0.193247983770819,0.193555229367173,0.194102040676105,
0.194169720559882,0.194528383952344,0.19478421175259,0.194852339466579,
0.195183787620667,0.195398702945298,0.19585180183904,0.19630739318511,0.196762420619596,
0.197048670931309),.UNSPECIFIED.);
#790=B_SPLINE_CURVE_WITH_KNOTS('',3,(#50525,#50526,#50527,#50528,#50529,
#50530,#50531,#50532,#50533,#50534,#50535,#50536,#50537,#50538,#50539,#50540,
#50541,#50542,#50543,#50544,#50545,#50546,#50547,#50548,#50549,#50550,#50551,
#50552,#50553,#50554,#50555,#50556,#50557,#50558,#50559,#50560,#50561,#50562,
#50563,#50564,#50565,#50566,#50567),.UNSPECIFIED.,.F.,.F.,(4,1,1,1,1,1,
1,1,1,1,1,1,1,1,1,1,1,1,1,1,1,1,1,1,1,1,1,1,1,1,1,1,1,1,1,1,1,1,1,1,4),
(0.139688666527305,0.141888509865,0.144088353202694,0.146288196540389,0.148488039878084,
0.150687883215779,0.152887726553474,0.155087569891169,0.157287413228864,
0.160220537679124,0.163153662129384,0.164620224354514,0.166086786579644,
0.167553348804774,0.169019911029903,0.171953035480163,0.174886159930423,
0.177086003268118,0.179285846605813,0.181485689943508,0.183685533281203,
0.184235494115627,0.18478545495005,0.185885376618898,0.188085219956593,
0.190285063294288,0.192484906631983,0.194684749969677,0.196884593307372,
0.199084436645067,0.200184358313915,0.200734319148339,0.201284279982762,
0.203484123320457,0.205683966658152,0.207883809995847,0.210083653333542,
0.213016777783802,0.215949902234062,0.218883026684322,0.219978350651175),
 .UNSPECIFIED.);
#791=B_SPLINE_CURVE_WITH_KNOTS('',3,(#50844,#50845,#50846,#50847,#50848,
#50849,#50850,#50851,#50852,#50853,#50854,#50855,#50856,#50857,#50858,#50859,
#50860,#50861,#50862,#50863,#50864,#50865,#50866,#50867,#50868,#50869,#50870,
#50871,#50872,#50873,#50874,#50875,#50876,#50877,#50878,#50879,#50880,#50881,
#50882,#50883,#50884,#50885,#50886,#50887,#50888,#50889,#50890,#50891,#50892,
#50893,#50894,#50895,#50896,#50897,#50898,#50899,#50900,#50901,#50902,#50903,
#50904,#50905,#50906,#50907,#50908,#50909,#50910,#50911,#50912,#50913,#50914,
#50915,#50916,#50917,#50918,#50919,#50920,#50921,#50922,#50923,#50924,#50925,
#50926,#50927,#50928,#50929,#50930,#50931,#50932,#50933,#50934,#50935,#50936,
#50937,#50938,#50939,#50940,#50941,#50942,#50943,#50944,#50945,#50946,#50947,
#50948,#50949,#50950,#50951,#50952,#50953,#50954,#50955,#50956,#50957,#50958,
#50959,#50960,#50961,#50962,#50963,#50964,#50965,#50966,#50967,#50968,#50969,
#50970,#50971,#50972,#50973,#50974,#50975,#50976,#50977,#50978,#50979,#50980,
#50981,#50982,#50983,#50984,#50985,#50986,#50987,#50988,#50989,#50990,#50991,
#50992,#50993,#50994,#50995,#50996,#50997,#50998,#50999,#51000,#51001,#51002,
#51003,#51004,#51005,#51006,#51007,#51008,#51009,#51010,#51011,#51012,#51013,
#51014,#51015,#51016,#51017,#51018,#51019,#51020,#51021,#51022,#51023,#51024,
#51025,#51026,#51027,#51028,#51029,#51030,#51031,#51032,#51033,#51034,#51035,
#51036,#51037,#51038,#51039,#51040,#51041,#51042,#51043,#51044,#51045,#51046,
#51047,#51048,#51049,#51050,#51051,#51052,#51053,#51054,#51055,#51056,#51057,
#51058,#51059,#51060,#51061,#51062,#51063,#51064,#51065,#51066,#51067,#51068,
#51069,#51070,#51071,#51072,#51073,#51074,#51075,#51076,#51077,#51078,#51079,
#51080,#51081,#51082,#51083,#51084,#51085,#51086,#51087,#51088,#51089,#51090,
#51091,#51092,#51093,#51094,#51095,#51096,#51097,#51098,#51099,#51100,#51101,
#51102,#51103,#51104,#51105,#51106,#51107,#51108,#51109,#51110,#51111,#51112,
#51113,#51114,#51115,#51116,#51117,#51118,#51119,#51120,#51121,#51122,#51123,
#51124,#51125,#51126,#51127,#51128,#51129,#51130,#51131,#51132,#51133,#51134,
#51135,#51136,#51137,#51138,#51139,#51140,#51141,#51142,#51143,#51144,#51145,
#51146,#51147,#51148,#51149,#51150,#51151,#51152,#51153,#51154,#51155,#51156,
#51157,#51158,#51159,#51160,#51161,#51162,#51163,#51164,#51165,#51166,#51167,
#51168,#51169,#51170,#51171,#51172,#51173,#51174,#51175,#51176,#51177,#51178,
#51179,#51180,#51181,#51182,#51183,#51184,#51185,#51186,#51187,#51188,#51189,
#51190,#51191,#51192,#51193,#51194,#51195,#51196,#51197,#51198,#51199,#51200,
#51201,#51202,#51203,#51204,#51205,#51206,#51207,#51208,#51209,#51210,#51211,
#51212,#51213,#51214,#51215,#51216,#51217,#51218,#51219,#51220,#51221,#51222,
#51223,#51224,#51225,#51226,#51227,#51228,#51229,#51230,#51231,#51232,#51233,
#51234,#51235,#51236,#51237,#51238,#51239),.UNSPECIFIED.,.F.,.F.,(4,2,2,
2,2,2,2,2,2,2,2,2,2,2,2,2,2,2,2,2,2,2,2,2,2,2,2,2,2,2,2,2,2,2,2,2,2,2,2,
2,2,2,2,2,2,2,2,2,2,2,2,2,2,2,2,2,2,2,2,2,2,2,2,2,2,2,2,2,2,2,2,2,2,2,2,
2,2,2,2,2,2,2,2,2,2,2,2,2,2,2,2,2,2,2,2,2,2,2,2,2,2,2,2,2,2,2,2,2,2,2,2,
2,2,2,2,2,2,2,2,2,2,2,2,2,2,2,2,2,2,2,2,2,2,2,2,2,2,2,2,2,2,2,2,2,2,2,2,
2,2,2,2,2,2,2,2,2,2,2,2,2,2,2,2,2,2,2,2,2,2,2,2,2,2,2,2,2,2,2,2,2,2,2,2,
2,2,2,2,2,2,2,2,2,2,2,2,2,2,4),(0.285111806346874,0.285640371084623,0.286169688619292,
0.286253528781122,0.28679049202008,0.286954925748233,0.287624941988217,
0.288322782411678,0.288452680346209,0.288798399656758,0.289447319071883,
0.29011084240271,0.290641873565284,0.290652246933881,0.291414851470538,
0.291751755837375,0.292485347473809,0.292851528592237,0.293505663327753,
0.293951003885431,0.294281878521236,0.294411806864067,0.294947623823447,
0.295050766229014,0.295600713975397,0.296013174785185,0.296163107931787,
0.296266722938215,0.296813898716011,0.297250557214549,0.29781023827113,
0.298006955465365,0.29814817767842,0.298824649511877,0.299450041448425,
0.29985924310791,0.300456377556101,0.301066857549586,0.301648532377361,
0.302261918074419,0.302317208319277,0.302848546895361,0.303388381324519,
0.303846251520219,0.304388329451953,0.304775173530644,0.305337847954477,
0.305912156270017,0.306046151016494,0.306639644879253,0.307233138742011,
0.307749298247224,0.308245332269785,0.308763863101548,0.309076612650536,
0.30987698412567,0.310443547903747,0.310920086559061,0.311781227445867,
0.312588144003948,0.312642368332673,0.312763560467587,0.313303200481775,
0.31386237748905,0.314427200435492,0.314607034376112,0.315046976447381,
0.315483786381483,0.315573150254336,0.316013598145793,0.316450508284637,
0.316964560632992,0.317475657386103,0.317962930768564,0.318293982193163,
0.318501368989331,0.318904406997231,0.319215719147425,0.319637107883235,
0.320063230859427,0.320137456101688,0.320614464130452,0.320828758817385,
0.32105919305595,0.32143188567371,0.32161347578906,0.321750495771647,0.321980930010213,
0.322465194307811,0.322962701555398,0.323455598846691,0.323922283517711,
0.32428527239587,0.324363062752028,0.324816416375222,0.325266314686911,
0.325667877827264,0.326212295021501,0.326765838711299,0.327296277392487,
0.327864683041269,0.328403985140896,0.328433088690051,0.328909994031669,
0.329354825644314,0.329964329620402,0.330231406193989,0.330843324987258,
0.331198299552839,0.331699223621591,0.332242822753204,0.332432288182419,
0.332798816968857,0.333041773461365,0.333165629225368,0.333595533761498,
0.334009505508754,0.334421685174999,0.334830881689862,0.33488524736989,
0.335330563646124,0.335773794074081,0.336100769244151,0.336540569023547,
0.336728721278415,0.337189589755546,0.337567352148602,0.337650458232678,
0.338132913214294,0.33857219518694,0.338994920565243,0.339033472503465,
0.339453103438159,0.339493932141203,0.33981815411855,0.340142638771275,
0.340415669095466,0.340838079174422,0.341260533567594,0.341682693714999,
0.341963208106005,0.342259143003991,0.342947012186205,0.343638635766066,
0.343918284848948,0.344362602634211,0.345116924982843,0.345871247331475,
0.346274226969221,0.347049537036131,0.347586983698222,0.347824847103041,
0.348374001532803,0.348648513521792,0.348923042595576,0.349472333873503,
0.349623750066329,0.349773890326151,0.350021898056725,0.35065911454714,
0.35112045281866,0.351343653761936,0.351484905463245,0.351852249073299,
0.352115036902343,0.352219592683353,0.35239824950088,0.352705495152301,
0.353172017206261,0.353638044531663,0.353934477757984,0.354419567683639,
0.355097222338029,0.355783241653761,0.356392442969351,0.356619162091783,
0.357060054857063,0.357504178211808,0.357621425575035,0.357996578083137,
0.358235916877876,0.358653902590294,0.358818025956889,0.358850408180718,
0.359578759831332,0.360297492507432,0.360975177719308,0.361016225183532,
0.361308373392085,0.361859361467179,0.362420715176227,0.362979009728679,
0.363215660397334,0.363766338603452,0.364237719657693,0.364712606478098,
0.365187957031571,0.365413919238787),.UNSPECIFIED.);
#792=B_SPLINE_CURVE_WITH_KNOTS('',3,(#51240,#51241,#51242,#51243,#51244,
#51245,#51246,#51247,#51248,#51249,#51250,#51251,#51252,#51253,#51254,#51255,
#51256,#51257,#51258,#51259,#51260,#51261,#51262,#51263,#51264,#51265,#51266,
#51267,#51268,#51269,#51270,#51271,#51272,#51273,#51274,#51275,#51276,#51277,
#51278,#51279,#51280,#51281,#51282,#51283,#51284,#51285,#51286,#51287,#51288,
#51289,#51290,#51291,#51292,#51293,#51294,#51295,#51296,#51297,#51298,#51299,
#51300,#51301,#51302,#51303,#51304,#51305,#51306,#51307,#51308,#51309,#51310,
#51311,#51312,#51313,#51314,#51315,#51316,#51317,#51318,#51319,#51320,#51321,
#51322,#51323,#51324,#51325,#51326,#51327,#51328,#51329,#51330,#51331,#51332,
#51333,#51334,#51335,#51336,#51337,#51338,#51339,#51340,#51341,#51342,#51343,
#51344,#51345,#51346,#51347,#51348,#51349,#51350,#51351,#51352,#51353,#51354,
#51355,#51356,#51357,#51358,#51359,#51360,#51361,#51362,#51363,#51364,#51365,
#51366,#51367,#51368,#51369,#51370,#51371,#51372,#51373,#51374,#51375,#51376,
#51377,#51378,#51379,#51380,#51381,#51382,#51383,#51384,#51385,#51386,#51387,
#51388,#51389,#51390,#51391,#51392,#51393,#51394,#51395,#51396,#51397,#51398,
#51399,#51400,#51401,#51402,#51403,#51404,#51405,#51406,#51407,#51408,#51409,
#51410,#51411,#51412,#51413,#51414,#51415,#51416,#51417,#51418,#51419,#51420,
#51421,#51422,#51423,#51424,#51425,#51426,#51427,#51428,#51429,#51430,#51431,
#51432,#51433,#51434,#51435,#51436,#51437,#51438,#51439,#51440,#51441,#51442,
#51443,#51444,#51445,#51446,#51447,#51448,#51449,#51450,#51451,#51452,#51453,
#51454,#51455,#51456,#51457,#51458,#51459,#51460,#51461,#51462,#51463,#51464,
#51465,#51466,#51467,#51468,#51469,#51470,#51471,#51472,#51473,#51474,#51475,
#51476,#51477,#51478,#51479,#51480,#51481,#51482,#51483,#51484,#51485,#51486,
#51487,#51488,#51489,#51490,#51491,#51492,#51493,#51494,#51495,#51496,#51497,
#51498,#51499,#51500,#51501,#51502,#51503,#51504,#51505,#51506,#51507,#51508,
#51509,#51510,#51511,#51512,#51513,#51514,#51515,#51516,#51517,#51518,#51519,
#51520,#51521,#51522,#51523,#51524,#51525,#51526,#51527,#51528,#51529,#51530,
#51531,#51532,#51533,#51534,#51535,#51536,#51537,#51538,#51539,#51540,#51541,
#51542,#51543,#51544,#51545,#51546,#51547,#51548,#51549,#51550,#51551,#51552,
#51553,#51554,#51555,#51556,#51557,#51558,#51559,#51560,#51561,#51562,#51563,
#51564,#51565,#51566,#51567,#51568,#51569,#51570,#51571,#51572,#51573,#51574,
#51575,#51576,#51577,#51578,#51579,#51580,#51581,#51582,#51583,#51584,#51585,
#51586,#51587,#51588,#51589,#51590,#51591,#51592,#51593,#51594,#51595,#51596,
#51597,#51598,#51599,#51600,#51601,#51602,#51603,#51604,#51605,#51606,#51607,
#51608,#51609,#51610,#51611,#51612,#51613,#51614,#51615,#51616,#51617,#51618,
#51619,#51620,#51621,#51622,#51623,#51624,#51625,#51626,#51627,#51628,#51629,
#51630,#51631,#51632,#51633,#51634,#51635,#51636,#51637,#51638,#51639,#51640,
#51641,#51642,#51643,#51644,#51645,#51646,#51647,#51648,#51649,#51650,#51651,
#51652,#51653,#51654,#51655,#51656,#51657,#51658,#51659,#51660,#51661,#51662,
#51663,#51664,#51665,#51666,#51667,#51668,#51669,#51670,#51671,#51672,#51673,
#51674,#51675,#51676,#51677,#51678,#51679,#51680,#51681,#51682,#51683,#51684,
#51685,#51686,#51687,#51688,#51689,#51690,#51691,#51692,#51693,#51694,#51695,
#51696,#51697,#51698,#51699,#51700,#51701,#51702,#51703,#51704,#51705,#51706,
#51707,#51708,#51709,#51710,#51711,#51712,#51713,#51714,#51715,#51716,#51717,
#51718,#51719,#51720,#51721,#51722,#51723,#51724,#51725,#51726,#51727,#51728,
#51729,#51730,#51731,#51732,#51733,#51734,#51735,#51736,#51737,#51738,#51739,
#51740,#51741,#51742,#51743,#51744,#51745,#51746,#51747,#51748,#51749,#51750,
#51751,#51752,#51753,#51754,#51755,#51756,#51757,#51758,#51759,#51760,#51761,
#51762,#51763,#51764,#51765,#51766,#51767,#51768,#51769,#51770,#51771,#51772,
#51773,#51774,#51775,#51776,#51777,#51778,#51779,#51780,#51781,#51782,#51783,
#51784,#51785,#51786,#51787,#51788,#51789,#51790,#51791,#51792,#51793,#51794,
#51795,#51796,#51797,#51798,#51799,#51800,#51801,#51802,#51803,#51804,#51805,
#51806,#51807,#51808,#51809,#51810,#51811,#51812,#51813,#51814,#51815,#51816,
#51817,#51818,#51819,#51820,#51821,#51822,#51823,#51824,#51825,#51826,#51827,
#51828,#51829,#51830,#51831,#51832,#51833,#51834,#51835,#51836,#51837,#51838,
#51839,#51840,#51841,#51842,#51843,#51844,#51845,#51846,#51847,#51848,#51849,
#51850,#51851,#51852,#51853,#51854,#51855,#51856,#51857,#51858,#51859,#51860,
#51861,#51862,#51863,#51864,#51865,#51866,#51867,#51868,#51869,#51870,#51871,
#51872,#51873,#51874,#51875,#51876,#51877,#51878,#51879,#51880,#51881,#51882,
#51883,#51884,#51885,#51886,#51887,#51888,#51889,#51890,#51891,#51892,#51893,
#51894,#51895,#51896,#51897,#51898,#51899,#51900,#51901,#51902,#51903,#51904,
#51905,#51906,#51907,#51908,#51909,#51910,#51911,#51912,#51913,#51914,#51915,
#51916,#51917,#51918,#51919,#51920,#51921,#51922,#51923,#51924,#51925,#51926,
#51927,#51928,#51929,#51930,#51931,#51932,#51933,#51934,#51935,#51936,#51937,
#51938,#51939,#51940,#51941,#51942,#51943,#51944,#51945,#51946,#51947,#51948,
#51949,#51950,#51951,#51952,#51953,#51954,#51955,#51956,#51957,#51958,#51959,
#51960,#51961,#51962,#51963,#51964,#51965,#51966,#51967,#51968,#51969,#51970,
#51971,#51972,#51973,#51974,#51975,#51976,#51977,#51978,#51979,#51980,#51981,
#51982,#51983,#51984,#51985,#51986,#51987,#51988,#51989,#51990,#51991,#51992,
#51993,#51994,#51995,#51996,#51997,#51998,#51999,#52000,#52001,#52002,#52003,
#52004,#52005,#52006,#52007,#52008,#52009,#52010,#52011,#52012,#52013,#52014,
#52015,#52016,#52017,#52018,#52019,#52020,#52021,#52022,#52023,#52024,#52025,
#52026,#52027,#52028,#52029,#52030,#52031,#52032,#52033,#52034,#52035,#52036,
#52037,#52038,#52039,#52040,#52041,#52042,#52043,#52044,#52045,#52046,#52047,
#52048,#52049,#52050,#52051,#52052,#52053,#52054,#52055,#52056,#52057,#52058,
#52059,#52060,#52061,#52062,#52063,#52064,#52065,#52066,#52067,#52068,#52069,
#52070,#52071,#52072,#52073,#52074,#52075,#52076,#52077,#52078,#52079,#52080,
#52081,#52082,#52083,#52084,#52085,#52086,#52087,#52088,#52089,#52090,#52091,
#52092,#52093,#52094,#52095,#52096,#52097,#52098,#52099,#52100,#52101,#52102,
#52103,#52104,#52105,#52106,#52107,#52108,#52109,#52110,#52111,#52112,#52113),
 .UNSPECIFIED.,.F.,.F.,(4,3,3,3,3,3,3,3,3,3,3,3,3,3,3,3,3,3,3,3,3,3,3,3,
3,3,3,3,3,3,3,3,3,3,3,3,3,3,3,3,3,3,3,3,3,3,3,3,3,3,3,3,3,3,3,3,3,3,3,3,
3,3,3,3,3,3,3,3,3,3,3,3,3,3,3,3,3,3,3,3,3,3,3,3,3,3,3,3,3,3,3,3,3,3,3,3,
3,3,3,3,3,3,3,3,3,3,3,3,3,3,3,3,3,3,3,3,3,3,3,3,3,3,3,3,3,3,3,3,3,3,3,3,
3,3,3,3,3,3,3,3,3,3,3,3,3,3,3,3,3,3,3,3,3,3,3,3,3,3,3,3,3,3,3,3,3,3,3,3,
3,3,3,3,3,3,3,3,3,3,3,3,3,3,3,3,3,3,3,3,3,3,3,3,3,3,3,3,3,3,3,3,3,3,3,3,
3,3,3,3,3,3,3,3,3,3,3,3,3,3,3,3,3,3,3,3,3,3,3,3,3,3,3,3,3,3,3,3,3,3,3,3,
3,3,3,3,3,3,3,3,3,3,3,3,3,3,3,3,3,3,3,3,3,3,3,3,3,3,3,3,3,3,3,3,3,3,3,3,
3,3,3,3,3,3,3,3,3,3,3,3,3,3,3,4),(0.30805700545397,0.30842631823362,0.30867821759715,
0.30907401465744,0.309475521913904,0.30969878573946,0.310084850075262,0.310256126873765,
0.310256131102317,0.31059915974391,0.310835644928473,0.310917103883896,
0.311361464873264,0.311498503382682,0.312073982405682,0.312281423858008,
0.31242181744669,0.312456103104523,0.312780347773963,0.313361229956204,
0.314014862562268,0.314383874965016,0.314631411651958,0.314656073911279,
0.31481593937699,0.315325948261099,0.315752028210539,0.316185345841358,
0.316667243001024,0.316855974913424,0.317049160857981,0.317498738314017,
0.317815960493163,0.318192323873742,0.318421262314861,0.318738484211031,
0.318941104723126,0.3190557061072,0.319220033386332,0.319606200915324,0.319815849720664,
0.320142002166964,0.320563452996499,0.320744645139698,0.320833011079153,
0.321063450110493,0.321255347685694,0.321255392999736,0.321524402339523,
0.321754578820996,0.321984584513574,0.322349421139369,0.322513789514616,
0.322870191717163,0.32304938384856,0.323393413079713,0.323455191002369,
0.323455232867165,0.323799503315996,0.324143773764826,0.324286339644825,
0.324763826258503,0.324970686981935,0.325460304805887,0.325655034319044,
0.325655055286748,0.325668256652078,0.326023574000325,0.326252717295575,
0.326698188297976,0.326845081523442,0.3272876544818,0.327610450600534,0.327610528635596,
0.328209641918397,0.328431862720052,0.328780692444404,0.329130126327003,
0.329354547318243,0.329565866882023,0.32956593140403,0.330100378669315,
0.330685215141153,0.331103249152332,0.331375304475226,0.331521283163512,
0.331521356570397,0.331871387584888,0.332086250581248,0.332381287496353,
0.332673958597452,0.333042290801308,0.333395745129851,0.333632492368121,
0.333978279196955,0.334210361582656,0.334454407585746,0.334454426442488,
0.334754111974627,0.334886072344529,0.335403290978656,0.335930000811901,
0.336450809179484,0.336724089775649,0.337030157298995,0.337184706716219,
0.337387532007979,0.337646409194722,0.338015497358372,0.33819427196612,
0.338567449746788,0.339058128376821,0.339122122235974,0.339487702719904,
0.339795946924541,0.340023804866389,0.340320635989051,0.340320656430213,
0.340617966980718,0.340986830911199,0.341447995770135,0.341580162111079,
0.342037187299761,0.342176675861317,0.342255410107777,0.342694862902167,
0.342851202420166,0.34321968720601,0.343253725017748,0.343388466069785,
0.343437040198125,0.343620358480361,0.343987004308469,0.344353653400577,
0.344720289869125,0.34502217580816,0.345511481737521,0.345903021475991,
0.346186825413991,0.346290019253806,0.346684134854412,0.346771735966535,
0.347256414984072,0.347376120546762,0.347684959692493,0.347792901755893,
0.348182416648847,0.348397335910164,0.348801260494588,0.348983690663044,
0.349120029696914,0.349120110024139,0.349511878656296,0.349638586328738,
0.350171678805315,0.350713863430756,0.351247950412733,0.351478110296708,
0.35186663869738,0.352012882520311,0.352053119511091,0.352146286790599,
0.352427332072899,0.3527083773552,0.353202448566926,0.353337453014862,0.353896724536809,
0.353936185320789,0.354252997435823,0.354253088674553,0.354839320655598,
0.354983812875947,0.355725074809772,0.356359295716468,0.356394072507208,
0.356452840752499,0.356452895274245,0.356916177408798,0.357066671348408,
0.357622935711093,0.358047275428847,0.358237001903881,0.358624756547822,
0.358652684069174,0.358652749921928,0.358851700177434,0.359385433389968,
0.359513252456057,0.360182889920953,0.360680968940598,0.360852527385849,
0.360852705659415,0.361309720004682,0.361811647734616,0.361875865205525,
0.362464117954024,0.362872432638893,0.363015400675881,0.363052370702524,
0.363052465480579,0.363597343389616,0.363766420397923,0.364305316667945,
0.364783190914614,0.36484286397938,0.365215551503501,0.3652522140192,0.365252324151075,
0.365670733157252,0.365749468314731,0.366223171767458,0.366714758604002,
0.367141779079656,0.367206704044414,0.367452050719647,0.367452057335875,
0.367867540123123,0.367973089388087,0.368493675853447,0.368678577352071,
0.369194715739538,0.36957912160619,0.36965190065255,0.370143634964898,0.370264773959565,
0.370317917286151,0.370877630019394,0.370932260622303,0.371543209374464,
0.371851736655365,0.371851743969226,0.371956775378399,0.372563771377561,
0.372624713224631,0.373288916771482,0.373595811316661,0.374051574336618,
0.374051587285901,0.374489729711754,0.374611777628573,0.375177352642783,
0.375441071936421,0.376002562899652,0.37625141481233,0.376251430602576,
0.376615047791481,0.376801375987611,0.376801391431745,0.37714273544159,
0.377287061331257,0.377351338795321,0.377351352260914,0.377691341885409,
0.378031167005512,0.378370314928258,0.378451273919252,0.378451289411068,
0.378889799191242,0.379021732686115,0.379408904421259,0.379813728063135,
0.3802739252859,0.38082118757719,0.380973407178383,0.381322088637239,0.38138439299867,
0.381384398341485,0.381744123785997,0.381875836108492,0.382379199283566,
0.382734926594743,0.38297774345126,0.383319049897772,0.383714884070583,
0.383818286330745,0.384157088697015,0.384317522763719,0.38431753840627,
0.384663023268301,0.385080001174113,0.385156982202099,0.385645601046297,
0.386123472022762,0.386503161337802,0.386882830473844,0.386998692941381,
0.387250647185953,0.387250674077535,0.387583139088101,0.387916429900176,
0.388249309169795,0.388346186021293),.UNSPECIFIED.);
#793=B_SPLINE_CURVE_WITH_KNOTS('',3,(#52366,#52367,#52368,#52369,#52370,
#52371,#52372,#52373,#52374,#52375,#52376,#52377,#52378,#52379,#52380,#52381,
#52382,#52383,#52384,#52385,#52386,#52387,#52388,#52389,#52390,#52391,#52392,
#52393,#52394,#52395,#52396,#52397,#52398,#52399,#52400,#52401,#52402,#52403,
#52404,#52405,#52406,#52407,#52408,#52409,#52410,#52411,#52412,#52413,#52414,
#52415,#52416,#52417,#52418,#52419,#52420,#52421,#52422,#52423,#52424,#52425,
#52426,#52427,#52428,#52429,#52430,#52431,#52432,#52433,#52434,#52435,#52436,
#52437,#52438,#52439,#52440,#52441,#52442,#52443,#52444,#52445,#52446,#52447,
#52448,#52449,#52450,#52451,#52452,#52453,#52454,#52455,#52456,#52457,#52458,
#52459,#52460,#52461,#52462,#52463,#52464,#52465,#52466,#52467,#52468,#52469,
#52470,#52471,#52472,#52473,#52474,#52475,#52476,#52477,#52478,#52479,#52480,
#52481,#52482,#52483,#52484,#52485,#52486,#52487,#52488,#52489,#52490,#52491,
#52492,#52493,#52494,#52495,#52496,#52497,#52498,#52499,#52500,#52501,#52502,
#52503,#52504,#52505,#52506,#52507,#52508,#52509,#52510,#52511,#52512,#52513,
#52514,#52515,#52516,#52517,#52518,#52519,#52520,#52521,#52522,#52523,#52524,
#52525,#52526,#52527,#52528,#52529,#52530,#52531,#52532,#52533,#52534,#52535,
#52536,#52537,#52538,#52539,#52540,#52541,#52542,#52543,#52544,#52545,#52546,
#52547,#52548,#52549,#52550,#52551,#52552,#52553,#52554,#52555,#52556,#52557,
#52558,#52559,#52560,#52561,#52562,#52563,#52564,#52565,#52566,#52567,#52568,
#52569,#52570,#52571,#52572,#52573,#52574,#52575,#52576,#52577,#52578,#52579,
#52580,#52581,#52582,#52583,#52584,#52585,#52586,#52587,#52588,#52589,#52590,
#52591,#52592,#52593,#52594,#52595,#52596,#52597,#52598,#52599,#52600,#52601,
#52602,#52603,#52604,#52605,#52606,#52607,#52608,#52609,#52610,#52611,#52612,
#52613,#52614,#52615,#52616,#52617,#52618,#52619,#52620,#52621,#52622,#52623,
#52624,#52625,#52626,#52627,#52628,#52629,#52630,#52631,#52632,#52633,#52634,
#52635,#52636,#52637,#52638,#52639,#52640,#52641,#52642,#52643,#52644,#52645,
#52646,#52647,#52648,#52649,#52650,#52651,#52652,#52653,#52654,#52655,#52656,
#52657,#52658,#52659,#52660,#52661,#52662,#52663,#52664,#52665,#52666,#52667,
#52668,#52669,#52670,#52671,#52672,#52673,#52674,#52675,#52676,#52677,#52678,
#52679,#52680,#52681,#52682,#52683,#52684,#52685,#52686,#52687,#52688,#52689,
#52690,#52691,#52692,#52693,#52694,#52695,#52696,#52697,#52698,#52699,#52700,
#52701,#52702,#52703,#52704,#52705,#52706,#52707,#52708,#52709,#52710,#52711,
#52712,#52713,#52714,#52715,#52716,#52717,#52718,#52719,#52720,#52721,#52722,
#52723,#52724,#52725,#52726,#52727,#52728,#52729,#52730,#52731,#52732,#52733,
#52734,#52735,#52736,#52737,#52738,#52739,#52740,#52741,#52742,#52743,#52744,
#52745,#52746,#52747,#52748,#52749,#52750,#52751,#52752,#52753,#52754,#52755,
#52756,#52757,#52758,#52759,#52760,#52761,#52762,#52763,#52764,#52765,#52766,
#52767,#52768,#52769,#52770,#52771,#52772,#52773,#52774,#52775,#52776,#52777,
#52778,#52779,#52780,#52781,#52782,#52783,#52784,#52785,#52786,#52787,#52788,
#52789,#52790,#52791,#52792,#52793,#52794,#52795,#52796,#52797,#52798,#52799,
#52800,#52801,#52802,#52803,#52804,#52805,#52806,#52807,#52808,#52809,#52810,
#52811,#52812,#52813,#52814,#52815,#52816,#52817,#52818,#52819,#52820,#52821,
#52822,#52823,#52824,#52825,#52826,#52827,#52828,#52829,#52830,#52831,#52832,
#52833,#52834,#52835,#52836,#52837,#52838,#52839,#52840,#52841,#52842,#52843,
#52844,#52845,#52846,#52847,#52848,#52849,#52850,#52851,#52852,#52853,#52854,
#52855,#52856,#52857,#52858,#52859,#52860,#52861,#52862,#52863,#52864,#52865,
#52866,#52867,#52868,#52869,#52870,#52871,#52872,#52873,#52874,#52875,#52876,
#52877,#52878,#52879,#52880,#52881,#52882,#52883,#52884,#52885,#52886,#52887,
#52888,#52889,#52890,#52891,#52892,#52893,#52894,#52895,#52896,#52897,#52898,
#52899,#52900,#52901,#52902,#52903,#52904,#52905,#52906,#52907,#52908,#52909,
#52910,#52911,#52912,#52913,#52914,#52915,#52916,#52917,#52918,#52919,#52920,
#52921,#52922,#52923,#52924,#52925,#52926,#52927,#52928,#52929,#52930,#52931,
#52932,#52933,#52934,#52935,#52936,#52937,#52938,#52939,#52940,#52941,#52942,
#52943,#52944,#52945,#52946,#52947,#52948,#52949,#52950,#52951,#52952,#52953,
#52954,#52955,#52956,#52957,#52958,#52959,#52960,#52961,#52962,#52963,#52964,
#52965,#52966,#52967,#52968,#52969,#52970,#52971,#52972,#52973,#52974,#52975,
#52976,#52977,#52978,#52979,#52980,#52981,#52982,#52983,#52984,#52985,#52986,
#52987,#52988,#52989,#52990,#52991,#52992,#52993,#52994,#52995,#52996,#52997,
#52998,#52999,#53000,#53001,#53002,#53003,#53004,#53005,#53006,#53007,#53008,
#53009,#53010,#53011,#53012,#53013,#53014,#53015,#53016,#53017,#53018,#53019,
#53020,#53021,#53022,#53023,#53024,#53025,#53026,#53027,#53028,#53029,#53030,
#53031,#53032,#53033,#53034,#53035,#53036,#53037,#53038,#53039,#53040,#53041,
#53042,#53043,#53044,#53045,#53046,#53047,#53048,#53049,#53050,#53051,#53052,
#53053,#53054,#53055,#53056,#53057,#53058,#53059,#53060,#53061,#53062,#53063,
#53064,#53065,#53066,#53067,#53068,#53069,#53070,#53071,#53072,#53073,#53074,
#53075,#53076,#53077,#53078,#53079,#53080,#53081,#53082,#53083,#53084,#53085,
#53086,#53087,#53088,#53089,#53090,#53091,#53092,#53093,#53094,#53095,#53096,
#53097,#53098,#53099,#53100,#53101,#53102,#53103,#53104,#53105,#53106,#53107,
#53108,#53109,#53110,#53111,#53112,#53113,#53114,#53115,#53116,#53117,#53118,
#53119,#53120,#53121,#53122,#53123,#53124,#53125,#53126,#53127,#53128,#53129,
#53130,#53131,#53132,#53133,#53134,#53135,#53136,#53137,#53138,#53139,#53140,
#53141,#53142,#53143,#53144,#53145,#53146,#53147,#53148,#53149,#53150,#53151,
#53152,#53153,#53154,#53155,#53156,#53157,#53158,#53159,#53160,#53161,#53162,
#53163,#53164,#53165,#53166,#53167,#53168,#53169,#53170,#53171,#53172,#53173,
#53174,#53175,#53176,#53177,#53178,#53179,#53180,#53181,#53182,#53183,#53184,
#53185,#53186,#53187,#53188,#53189,#53190,#53191,#53192,#53193,#53194,#53195,
#53196,#53197,#53198,#53199,#53200,#53201,#53202,#53203,#53204,#53205,#53206,
#53207,#53208,#53209,#53210,#53211,#53212,#53213,#53214,#53215,#53216,#53217,
#53218,#53219,#53220,#53221,#53222,#53223,#53224,#53225,#53226,#53227,#53228,
#53229,#53230,#53231,#53232,#53233,#53234,#53235,#53236,#53237,#53238,#53239,
#53240,#53241,#53242,#53243,#53244,#53245,#53246,#53247,#53248,#53249,#53250,
#53251,#53252,#53253,#53254,#53255,#53256,#53257,#53258,#53259,#53260,#53261,
#53262,#53263,#53264,#53265,#53266,#53267,#53268,#53269,#53270,#53271,#53272,
#53273,#53274,#53275,#53276,#53277,#53278,#53279,#53280,#53281,#53282,#53283,
#53284,#53285,#53286,#53287,#53288,#53289,#53290,#53291,#53292,#53293,#53294,
#53295,#53296,#53297,#53298,#53299,#53300,#53301,#53302,#53303,#53304,#53305,
#53306,#53307,#53308,#53309,#53310,#53311,#53312,#53313,#53314,#53315,#53316,
#53317,#53318,#53319,#53320,#53321,#53322,#53323,#53324,#53325,#53326),
 .UNSPECIFIED.,.F.,.F.,(4,3,3,3,3,3,3,3,3,3,3,3,3,3,3,3,3,3,3,3,3,3,3,3,
3,3,3,3,3,3,3,3,3,3,3,3,3,3,3,3,3,3,3,3,3,3,3,3,3,3,3,3,3,3,3,3,3,3,3,3,
3,3,3,3,3,3,3,3,3,3,3,3,3,3,3,3,3,3,3,3,3,3,3,3,3,3,3,3,3,3,3,3,3,3,3,3,
3,3,3,3,3,3,3,3,3,3,3,3,3,3,3,3,3,3,3,3,3,3,3,3,3,3,3,3,3,3,3,3,3,3,3,3,
3,3,3,3,3,3,3,3,3,3,3,3,3,3,3,3,3,3,3,3,3,3,3,3,3,3,3,3,3,3,3,3,3,3,3,3,
3,3,3,3,3,3,3,3,3,3,3,3,3,3,3,3,3,3,3,3,3,3,3,3,3,3,3,3,3,3,3,3,3,3,3,3,
3,3,3,3,3,3,3,3,3,3,3,3,3,3,3,3,3,3,3,3,3,3,3,3,3,3,3,3,3,3,3,3,3,3,3,3,
3,3,3,3,3,3,3,3,3,3,3,3,3,3,3,3,3,3,3,3,3,3,3,3,3,3,3,3,3,3,3,3,3,3,3,3,
3,3,3,3,3,3,3,3,3,3,3,3,3,3,3,3,3,3,3,3,3,3,3,3,3,3,3,3,3,3,3,3,3,3,3,3,
3,3,3,3,3,3,3,3,4),(0.45348023372167,0.453790469791108,0.453924734856489,
0.454245381133265,0.454368139113723,0.454621936522178,0.454919149780836,
0.455072257562434,0.45532256751791,0.45532260007357,0.455622708409302,0.455797353300424,
0.456277816308681,0.456622306513274,0.456746369309662,0.457104413997482,
0.457166041104501,0.457166189575094,0.457446635158765,0.457554086603849,
0.457905084192223,0.458018742216773,0.458270496828743,0.458488382055047,
0.458844074732817,0.458952016875946,0.459008977890699,0.459009514691093,
0.459398406076876,0.459620969601057,0.459903843026781,0.460186894759034,
0.460283544912754,0.460486819924068,0.460773324540919,0.460852988277684,
0.460853120225679,0.461266936093801,0.461346485692105,0.46170263458956,
0.461854442266315,0.462238635524003,0.462366824300372,0.462696461864275,
0.462696604245544,0.462988521681667,0.463133914236636,0.463417597442529,
0.463755365498805,0.463850537419796,0.464173842317907,0.46428814986503,
0.464539935450866,0.464540327636473,0.464901176448483,0.465262025260493,
0.465613771301447,0.465946005612296,0.466278618910396,0.466344666797197,
0.466383298363033,0.466383409037458,0.466774064832716,0.466944209080824,
0.467337869911513,0.467501868151571,0.467811578920541,0.468226528326458,
0.468226882624049,0.468655674825323,0.468895378482076,0.469561741320397,
0.469934771302287,0.470012543462751,0.470500435874145,0.470684163544798,
0.470684847406171,0.471074772144608,0.47133474243947,0.471768693167588,
0.472214358331939,0.472764783968333,0.473142136752783,0.473240103260704,
0.473627511153589,0.473685335200338,0.474077597308726,0.474239098296372,
0.47441546230957,0.474750579062031,0.47497023105009,0.475331404887055,0.475521202319557,
0.47560036886865,0.475600776970414,0.475974272746165,0.476153675504332,
0.476473395039719,0.476615557370942,0.476999620058135,0.477169933569646,
0.477604839358826,0.47772129540641,0.478058380682379,0.478058741752536,
0.478554525741549,0.478603057217752,0.47881504225536,0.479259883139497,
0.479358511396559,0.479799823928292,0.479937608965608,0.480339809101745,
0.480476191729039,0.480516706534658,0.480516914981747,0.480858990635641,
0.481011723036403,0.481531322336638,0.481680088986041,0.482211231263052,
0.482360252095033,0.482826342205504,0.48297467131678,0.482974972844709,
0.483208180585816,0.483758094960384,0.483888449525093,0.484433466733313,
0.484572381520078,0.484818144903371,0.484818299872858,0.485221553888479,
0.485405226580635,0.485864202115283,0.486033422535298,0.486453511711716,
0.486661518258747,0.486661618489962,0.48706078821189,0.487188699971035,
0.487604313151055,0.488050168328899,0.488132704130397,0.488504828204312,
0.488505092076554,0.488980465449272,0.489112591207691,0.489646229297193,
0.489715244453029,0.489804221670911,0.490268682788055,0.490348340750487,
0.490348565663145,0.490859220333916,0.491027563260648,0.491271745610459,
0.491455071126767,0.491638390913829,0.492005057114982,0.492191896303053,
0.492192039249736,0.492738480426435,0.49336841108412,0.493427599001982,
0.493960279715027,0.494035385631583,0.494035512836328,0.49420528989616,
0.494900188530942,0.495605736321105,0.495670996327693,0.495878986422919,
0.495879043022329,0.496403845981915,0.497004333193076,0.497136418879869,
0.497319550607677,0.497502688303911,0.497722513479523,0.497869017202689,
0.498183421184899,0.498238753332429,0.498601686955044,0.498644196802806,
0.498644307940159,0.499105065199454,0.499565756669991,0.499565933596102,
0.500043574105038,0.500520944462694,0.500989782434813,0.501409407182693,
0.501409460797714,0.501533833466022,0.501974247889604,0.502010259570668,
0.502485617123122,0.502955772406981,0.503252748847819,0.503252880769284,
0.503640708900326,0.503726654127854,0.504196924619551,0.504464444297072,
0.50493723358145,0.505096354355876,0.505096372603651,0.505583039999626,
0.506074503568958,0.506553654026795,0.506939827942467,0.507327666055506,
0.507397317486871,0.507400696339115,0.507400745932985,0.507807282713654,
0.50821458149422,0.508621067184384,0.508783203899882,0.508783301529058,
0.509176966489728,0.509218498324237,0.509653960252979,0.510088821396247,
0.510329322034527,0.510626775115649,0.511348787261653,0.512110048863779,
0.512283442870139,0.512470237026294,0.512470248702241,0.512946059522407,
0.513041330770913,0.513639081561961,0.514134415348567,0.514204547981925,
0.51423683235301,0.514671061881375,0.514803582855506,0.514928213484362,
0.514928218967118,0.515334525052906,0.515454273862953,0.515988239961532,
0.516193434372497,0.516724661608416,0.517119848376792,0.517250490128293,
0.517386178266484,0.517386203705458,0.517793168800916,0.517910498018892,
0.518326825457484,0.518393745780107,0.518856558800808,0.518915054636807,
0.519324323912781,0.519433138548259,0.519795436072675,0.519844143048606,
0.519844149609364,0.520250525584912,0.520360005731246,0.520592238370696,
0.521050486855063,0.521111593796236,0.521543438514737,0.521632517341446,
0.522032817715619,0.522146085214015,0.522302107830728,0.522302123690607,
0.522667271225169,0.522791471835816,0.523271974962783,0.523374754316014,
0.52391494096234,0.523965718788713,0.524427475731704,0.524552209759413,
0.524760040597086,0.52476007261285,0.524988288844166,0.525632082109919,
0.526276088239782,0.526848232541706,0.526886097506026,0.527185208253064,
0.527218037394971,0.527218055331716,0.52769028709017,0.527882394720423,
0.528427395915005,0.528568702738237,0.529128361973499,0.529247631186266,
0.52938358734141,0.529642816166946,0.529675973102647,0.529676002177093,
0.530155413416485,0.530290493372624,0.53029054627694,0.530740029860379,
0.530904984568154,0.530905035074824,0.531241074620977,0.531519451599375,
0.531519475763684,0.531582823133813,0.531896566102861,0.531959892648512,
0.532133966959215,0.532134064211177,0.532511118973597,0.532687508961153,
0.533124008239765,0.533251893760347,0.533664164121437,0.533781533154975),
 .UNSPECIFIED.);
#794=B_SPLINE_CURVE_WITH_KNOTS('',3,(#53327,#53328,#53329,#53330,#53331,
#53332,#53333,#53334,#53335,#53336,#53337,#53338,#53339,#53340,#53341,#53342,
#53343,#53344,#53345,#53346,#53347,#53348,#53349,#53350,#53351,#53352,#53353,
#53354,#53355,#53356,#53357,#53358,#53359,#53360,#53361,#53362,#53363,#53364,
#53365,#53366,#53367),.UNSPECIFIED.,.F.,.F.,(4,1,1,1,1,1,1,1,1,1,1,1,1,
1,1,1,1,1,1,1,1,1,1,1,1,1,1,1,1,1,1,1,1,1,1,1,1,1,4),(0.476423916058673,
0.478623759221241,0.480823602383808,0.483023445546375,0.485223288708942,
0.487423131871509,0.489622975034076,0.491822818196643,0.49402266135921,
0.495978077503714,0.497933493648219,0.499888909792723,0.502822034009479,
0.505755158226235,0.508688282442991,0.511621406659747,0.514554530876503,
0.51748765509326,0.518220936147449,0.518954217201638,0.519687498255827,
0.520420779310016,0.522620622472583,0.52482046563515,0.527020308797717,
0.529220151960284,0.531419995122852,0.533619838285419,0.535819681447986,
0.538019524610553,0.54021936777312,0.542419210935687,0.544619054098254,
0.546818897260821,0.549018740423388,0.551218583585956,0.554151707802712,
0.55561826991109,0.556713614780248),.UNSPECIFIED.);
#795=B_SPLINE_CURVE_WITH_KNOTS('',3,(#53596,#53597,#53598,#53599,#53600,
#53601,#53602,#53603,#53604,#53605,#53606,#53607,#53608,#53609,#53610,#53611,
#53612,#53613,#53614,#53615,#53616,#53617,#53618,#53619,#53620,#53621,#53622,
#53623,#53624,#53625,#53626,#53627,#53628,#53629,#53630,#53631,#53632,#53633,
#53634,#53635,#53636,#53637,#53638,#53639,#53640,#53641,#53642,#53643,#53644,
#53645,#53646,#53647,#53648,#53649,#53650,#53651,#53652,#53653,#53654,#53655,
#53656,#53657,#53658,#53659,#53660,#53661,#53662,#53663,#53664,#53665,#53666,
#53667,#53668,#53669,#53670,#53671,#53672,#53673,#53674,#53675,#53676,#53677,
#53678,#53679,#53680,#53681,#53682,#53683,#53684,#53685,#53686,#53687,#53688,
#53689,#53690,#53691,#53692,#53693,#53694,#53695,#53696,#53697,#53698,#53699,
#53700,#53701,#53702,#53703,#53704,#53705,#53706,#53707,#53708,#53709,#53710,
#53711,#53712,#53713,#53714,#53715,#53716,#53717,#53718,#53719,#53720,#53721,
#53722,#53723,#53724,#53725,#53726,#53727,#53728,#53729,#53730,#53731,#53732,
#53733,#53734,#53735,#53736,#53737,#53738,#53739,#53740,#53741,#53742,#53743,
#53744,#53745,#53746,#53747,#53748,#53749,#53750,#53751,#53752,#53753,#53754,
#53755,#53756,#53757,#53758,#53759,#53760,#53761,#53762,#53763,#53764,#53765,
#53766,#53767,#53768,#53769,#53770,#53771,#53772,#53773,#53774,#53775,#53776,
#53777,#53778,#53779,#53780,#53781,#53782,#53783,#53784,#53785,#53786,#53787,
#53788,#53789,#53790,#53791,#53792,#53793,#53794,#53795,#53796,#53797,#53798,
#53799,#53800,#53801,#53802,#53803,#53804,#53805,#53806,#53807,#53808,#53809,
#53810,#53811,#53812,#53813,#53814,#53815,#53816,#53817,#53818,#53819,#53820,
#53821,#53822,#53823,#53824,#53825,#53826,#53827,#53828,#53829,#53830,#53831,
#53832,#53833,#53834,#53835,#53836,#53837,#53838,#53839,#53840,#53841,#53842,
#53843,#53844,#53845,#53846,#53847,#53848,#53849,#53850,#53851,#53852,#53853,
#53854,#53855,#53856,#53857,#53858,#53859,#53860,#53861,#53862,#53863,#53864,
#53865,#53866,#53867,#53868,#53869,#53870,#53871,#53872,#53873,#53874,#53875,
#53876,#53877,#53878,#53879,#53880,#53881,#53882,#53883,#53884,#53885,#53886,
#53887,#53888,#53889,#53890,#53891,#53892,#53893,#53894,#53895,#53896,#53897,
#53898,#53899,#53900,#53901,#53902,#53903,#53904,#53905,#53906,#53907,#53908,
#53909,#53910,#53911,#53912,#53913,#53914,#53915,#53916,#53917,#53918,#53919,
#53920,#53921,#53922,#53923,#53924,#53925,#53926,#53927,#53928,#53929,#53930,
#53931,#53932,#53933,#53934,#53935,#53936,#53937,#53938,#53939,#53940,#53941,
#53942,#53943,#53944,#53945,#53946,#53947,#53948,#53949,#53950,#53951,#53952,
#53953,#53954,#53955,#53956,#53957,#53958,#53959,#53960,#53961,#53962,#53963,
#53964,#53965,#53966,#53967,#53968,#53969,#53970,#53971,#53972,#53973,#53974,
#53975,#53976,#53977,#53978,#53979,#53980,#53981,#53982,#53983,#53984,#53985,
#53986,#53987,#53988,#53989,#53990,#53991,#53992,#53993,#53994,#53995,#53996,
#53997,#53998,#53999,#54000,#54001,#54002,#54003,#54004,#54005,#54006,#54007,
#54008,#54009,#54010,#54011,#54012,#54013,#54014,#54015,#54016,#54017,#54018,
#54019,#54020,#54021,#54022,#54023,#54024,#54025,#54026,#54027,#54028,#54029,
#54030,#54031,#54032,#54033,#54034,#54035,#54036,#54037,#54038,#54039,#54040,
#54041,#54042,#54043,#54044,#54045,#54046,#54047,#54048,#54049,#54050,#54051,
#54052,#54053,#54054,#54055,#54056,#54057,#54058,#54059,#54060,#54061,#54062,
#54063,#54064,#54065,#54066,#54067,#54068,#54069,#54070,#54071,#54072,#54073,
#54074,#54075,#54076,#54077,#54078,#54079,#54080,#54081,#54082,#54083,#54084,
#54085,#54086,#54087,#54088,#54089,#54090,#54091,#54092,#54093,#54094,#54095,
#54096,#54097,#54098,#54099,#54100,#54101,#54102,#54103,#54104,#54105,#54106,
#54107,#54108,#54109,#54110,#54111,#54112,#54113,#54114,#54115,#54116,#54117,
#54118,#54119,#54120,#54121,#54122,#54123,#54124,#54125,#54126,#54127,#54128,
#54129,#54130,#54131,#54132,#54133,#54134,#54135,#54136,#54137,#54138,#54139,
#54140,#54141,#54142,#54143,#54144,#54145,#54146,#54147,#54148,#54149,#54150,
#54151,#54152,#54153,#54154,#54155,#54156,#54157,#54158,#54159,#54160,#54161,
#54162,#54163,#54164,#54165,#54166,#54167,#54168,#54169,#54170,#54171,#54172,
#54173,#54174,#54175,#54176,#54177,#54178,#54179,#54180,#54181,#54182,#54183,
#54184,#54185,#54186,#54187,#54188,#54189,#54190,#54191,#54192,#54193,#54194,
#54195,#54196,#54197,#54198,#54199,#54200,#54201,#54202,#54203,#54204,#54205,
#54206,#54207,#54208,#54209,#54210,#54211,#54212,#54213,#54214,#54215,#54216,
#54217,#54218,#54219,#54220,#54221,#54222,#54223,#54224,#54225,#54226,#54227,
#54228,#54229,#54230,#54231,#54232,#54233,#54234,#54235,#54236,#54237,#54238,
#54239,#54240,#54241,#54242,#54243,#54244,#54245,#54246,#54247,#54248,#54249,
#54250,#54251,#54252,#54253,#54254,#54255,#54256,#54257,#54258,#54259,#54260,
#54261,#54262,#54263,#54264,#54265,#54266,#54267,#54268,#54269,#54270,#54271,
#54272,#54273,#54274,#54275,#54276,#54277,#54278,#54279,#54280,#54281,#54282,
#54283,#54284,#54285,#54286,#54287,#54288,#54289,#54290,#54291,#54292,#54293,
#54294,#54295,#54296,#54297,#54298,#54299,#54300,#54301,#54302,#54303,#54304,
#54305,#54306,#54307,#54308,#54309,#54310,#54311,#54312,#54313,#54314,#54315,
#54316,#54317,#54318,#54319,#54320,#54321,#54322,#54323,#54324,#54325,#54326,
#54327,#54328,#54329,#54330,#54331,#54332,#54333,#54334,#54335,#54336,#54337,
#54338,#54339,#54340,#54341,#54342,#54343,#54344,#54345,#54346,#54347,#54348,
#54349,#54350,#54351,#54352,#54353,#54354,#54355,#54356,#54357,#54358,#54359,
#54360,#54361,#54362,#54363,#54364,#54365,#54366,#54367,#54368,#54369,#54370,
#54371,#54372,#54373,#54374,#54375,#54376,#54377,#54378,#54379,#54380,#54381,
#54382,#54383,#54384,#54385,#54386,#54387,#54388,#54389,#54390,#54391,#54392,
#54393,#54394,#54395,#54396,#54397,#54398,#54399,#54400,#54401,#54402,#54403,
#54404,#54405,#54406,#54407,#54408,#54409,#54410,#54411,#54412,#54413,#54414,
#54415,#54416,#54417,#54418,#54419,#54420,#54421,#54422,#54423,#54424,#54425,
#54426,#54427,#54428,#54429,#54430,#54431,#54432,#54433,#54434,#54435,#54436,
#54437,#54438,#54439,#54440,#54441,#54442,#54443,#54444,#54445,#54446,#54447,
#54448,#54449,#54450,#54451,#54452,#54453,#54454,#54455,#54456,#54457,#54458,
#54459,#54460,#54461,#54462,#54463,#54464,#54465,#54466,#54467,#54468,#54469,
#54470,#54471,#54472,#54473,#54474,#54475,#54476,#54477,#54478,#54479,#54480,
#54481,#54482,#54483,#54484,#54485,#54486,#54487,#54488,#54489,#54490,#54491,
#54492,#54493,#54494,#54495,#54496,#54497,#54498,#54499,#54500,#54501,#54502,
#54503,#54504,#54505,#54506,#54507,#54508,#54509,#54510,#54511,#54512,#54513,
#54514,#54515,#54516,#54517,#54518,#54519,#54520),.UNSPECIFIED.,.F.,.F.,
(4,3,3,3,3,3,3,3,3,3,3,3,3,3,3,3,3,3,3,3,3,3,3,3,3,3,3,3,3,3,3,3,3,3,3,
3,3,3,3,3,3,3,3,3,3,3,3,3,3,3,3,3,3,3,3,3,3,3,3,3,3,3,3,3,3,3,3,3,3,3,3,
3,3,3,3,3,3,3,3,3,3,3,3,3,3,3,3,3,3,3,3,3,3,3,3,3,3,3,3,3,3,3,3,3,3,3,3,
3,3,3,3,3,3,3,3,3,3,3,3,3,3,3,3,3,3,3,3,3,3,3,3,3,3,3,3,3,3,3,3,3,3,3,3,
3,3,3,3,3,3,3,3,3,3,3,3,3,3,3,3,3,3,3,3,3,3,3,3,3,3,3,3,3,3,3,3,3,3,3,3,
3,3,3,3,3,3,3,3,3,3,3,3,3,3,3,3,3,3,3,3,3,3,3,3,3,3,3,3,3,3,3,3,3,3,3,3,
3,3,3,3,3,3,3,3,3,3,3,3,3,3,3,3,3,3,3,3,3,3,3,3,3,3,3,3,3,3,3,3,3,3,3,3,
3,3,3,3,3,3,3,3,3,3,3,3,3,3,3,3,3,3,3,3,3,3,3,3,3,3,3,3,3,3,3,3,3,3,3,3,
3,3,3,3,3,3,3,3,3,3,3,3,3,3,3,3,3,3,3,3,3,4),(0.621846856583102,0.621892368004092,
0.622217754402355,0.622512398940775,0.622842115954442,0.622991576945145,
0.623260935267364,0.62352959867094,0.623614317432359,0.623690005388955,
0.623690199736931,0.624239382984407,0.624823524763165,0.625380980181381,
0.625533666494912,0.625533673395834,0.62581659080554,0.625922630075138,
0.62632966176229,0.626661915347805,0.627058444237377,0.627377147054738,
0.627377166815579,0.627388799295699,0.627853878881753,0.628137038123222,
0.628947485830711,0.629220598439111,0.629220620713642,0.629519077136893,
0.629586450804523,0.629979828156307,0.630244781179595,0.630673671783401,
0.630874607656459,0.631063927555557,0.631064094372546,0.631404070692801,
0.631577505275728,0.631785531280198,0.632111327850892,0.632298280612031,
0.632616998065837,0.632720056214535,0.632879518135696,0.6329072533034,0.63297441474824,
0.633398286175892,0.633523264465984,0.633810420114705,0.633985383022046,
0.63435647066126,0.634535019501422,0.634750641816437,0.635171345412579,
0.635612887009179,0.636118305501101,0.636353650182501,0.63652852424096,
0.636594267207711,0.636656907174331,0.636947027746356,0.637161234610997,
0.637490113291513,0.637652203413422,0.637992574863838,0.638162278120342,
0.638523409865301,0.63867876879381,0.639029560275845,0.639051974756686,
0.639052480227795,0.639411066819603,0.639513905773405,0.639772948973219,
0.639979341092053,0.640326035026194,0.640437249538887,0.640580189492334,
0.640893742032511,0.641045334456777,0.641350157683134,0.641510445106334,
0.641510520468996,0.641855447338863,0.642145741044356,0.642504786958309,
0.642781036982378,0.643143260455569,0.643429755604233,0.643787947840224,
0.643968337255306,0.643968409984872,0.644311970313094,0.644519894040162,
0.64487515938326,0.644979314629088,0.645364126006925,0.645532913269996,
0.645898207943654,0.646077762835349,0.646426104551011,0.646426374863411,
0.646903296177914,0.646968824192859,0.647178376789036,0.647616325850096,
0.647718937150597,0.648155393765759,0.648266193553022,0.648668146628746,
0.64880222161661,0.648884320276792,0.648884339741949,0.649226800377354,
0.64937595891545,0.64989765197277,0.650030480626183,0.650564348293318,0.650690367012657,
0.651160839486392,0.651342199845661,0.651342304620487,0.651574257682463,
0.652178608548435,0.652307398772069,0.652804778862935,0.653185506970598,
0.653433745519239,0.653733088132842,0.653976851830688,0.654311059815641,
0.654683356014655,0.65495462603492,0.655028760084688,0.655125927070742,
0.655552992353464,0.655591184342934,0.655921086710341,0.65597513120871,
0.656435130214724,0.656535762886226,0.656974326652741,0.657099447125672,
0.657333334797077,0.657333594011925,0.657849778299409,0.65788352032917,
0.658174361190189,0.658716199256103,0.658716231150652,0.659235096782956,
0.659367077841226,0.659639218198966,0.660216832023549,0.660282720594914,
0.660372165593032,0.660535409556554,0.66055973216036,0.6606773284617,0.661105887847589,
0.661827729130058,0.661967148644685,0.66240314657391,0.662403243536604,
0.662570692333655,0.663031924300911,0.663324880441152,0.663324883403362,
0.663780122147482,0.664035884325968,0.664768810217626,0.665452699119168,
0.665501736109285,0.665977218153675,0.666089925560195,0.666090093891718,
0.666405252042465,0.666715525057786,0.666969145781492,0.667392274044864,
0.667451356666056,0.667933323118611,0.667933567550621,0.668399012595211,
0.668850026105056,0.66931353365729,0.669753436268086,0.669777041209525,
0.669777063757701,0.66990175999802,0.670336541074922,0.670363468260186,
0.670823820213632,0.671279676695711,0.671620351658753,0.671620514868429,
0.672012982164485,0.672096242248359,0.672568466796311,0.672832807138605,
0.673307273781809,0.673463988527333,0.673463993254202,0.673949266280578,
0.674436321409013,0.674846535338015,0.674846593771511,0.67516463195361,
0.675307462186237,0.675307473834191,0.675765484218751,0.676238176537912,
0.676713164461141,0.677072734813525,0.677150860525229,0.677150935845141,
0.677541464645956,0.677593947489397,0.678037275633189,0.678479948931442,
0.678696094435218,0.678994409504044,0.678994424995288,0.679636251815923,
0.680304809352545,0.680650824154123,0.680837873863623,0.680837883162948,
0.681313451598143,0.681396506836904,0.681963063308275,0.682464379490378,
0.682518500564243,0.682604390363344,0.68303635841607,0.68316020954716,0.683295848041487,
0.683295854986793,0.683697951637246,0.683821949446226,0.684356147216294,
0.684561096692745,0.685028766729934,0.685092464044742,0.685475155241169,
0.685618632271069,0.685753812920025,0.685753835579768,0.686138943891943,
0.686281011537786,0.686761323597106,0.687245578329172,0.687285493897112,
0.687751354770776,0.687806434760149,0.688169131423624,0.688211777798563,
0.688571197333438,0.688730739103929,0.689113056311331,0.689481928590921,
0.68992985984292,0.690005858927733,0.690403744007667,0.690522537141612,
0.690669742677102,0.690669765081458,0.691010156824626,0.691158411304279,
0.691656278311949,0.691725835072625,0.692243766277744,0.692300043756321,
0.69275115179365,0.692864587804725,0.69312770755564,0.693355096033911,0.694008810835572,
0.694146584170164,0.694831159081235,0.694926491298771,0.695496197861561,
0.695553192932812,0.695585672434178,0.695585728026548,0.696093025979352,
0.696164280447754,0.696749200143603,0.697319347282953,0.697751415553726,
0.698043637312717,0.698043809025599,0.698443081416774,0.698575319251526,
0.699021391544107,0.699114416684524,0.699596756504331,0.69965572425361,
0.699952328223295,0.70026812359144,0.700501602191255,0.700501819333784,
0.700977661104677,0.701462623953163,0.701730584630524,0.701730673094993,
0.702107832683567,0.702150215830222),.UNSPECIFIED.);
#796=B_SPLINE_CURVE_WITH_KNOTS('',3,(#54521,#54522,#54523,#54524,#54525,
#54526,#54527,#54528,#54529,#54530,#54531,#54532,#54533,#54534,#54535,#54536,
#54537,#54538,#54539,#54540,#54541,#54542,#54543,#54544,#54545,#54546,#54547,
#54548,#54549,#54550,#54551,#54552,#54553,#54554,#54555,#54556,#54557,#54558,
#54559,#54560,#54561,#54562,#54563,#54564,#54565,#54566,#54567,#54568,#54569,
#54570,#54571,#54572,#54573,#54574,#54575,#54576,#54577,#54578,#54579,#54580,
#54581,#54582,#54583,#54584,#54585,#54586,#54587,#54588,#54589,#54590,#54591,
#54592,#54593,#54594,#54595,#54596,#54597,#54598,#54599,#54600,#54601,#54602,
#54603,#54604,#54605,#54606,#54607,#54608,#54609,#54610,#54611,#54612,#54613,
#54614,#54615,#54616,#54617,#54618,#54619,#54620,#54621,#54622,#54623,#54624,
#54625,#54626,#54627,#54628,#54629,#54630,#54631,#54632,#54633,#54634,#54635,
#54636,#54637,#54638,#54639,#54640,#54641,#54642,#54643,#54644,#54645,#54646,
#54647,#54648,#54649,#54650,#54651,#54652,#54653,#54654,#54655,#54656,#54657,
#54658,#54659,#54660,#54661,#54662,#54663,#54664,#54665,#54666,#54667,#54668,
#54669,#54670,#54671,#54672,#54673,#54674,#54675,#54676,#54677,#54678,#54679,
#54680,#54681,#54682,#54683,#54684,#54685,#54686,#54687,#54688,#54689,#54690,
#54691,#54692,#54693,#54694,#54695,#54696,#54697,#54698,#54699,#54700,#54701,
#54702,#54703,#54704,#54705,#54706,#54707,#54708,#54709,#54710,#54711,#54712,
#54713,#54714,#54715,#54716,#54717,#54718,#54719,#54720,#54721,#54722,#54723,
#54724,#54725,#54726,#54727,#54728,#54729,#54730,#54731,#54732,#54733,#54734,
#54735,#54736,#54737,#54738,#54739,#54740,#54741,#54742,#54743,#54744,#54745,
#54746,#54747,#54748,#54749,#54750,#54751,#54752,#54753,#54754,#54755,#54756,
#54757,#54758,#54759,#54760,#54761,#54762,#54763,#54764,#54765,#54766,#54767,
#54768,#54769,#54770,#54771,#54772,#54773,#54774,#54775,#54776,#54777,#54778,
#54779,#54780,#54781,#54782,#54783,#54784,#54785,#54786,#54787,#54788,#54789,
#54790,#54791,#54792,#54793,#54794,#54795,#54796,#54797,#54798,#54799,#54800,
#54801,#54802,#54803,#54804,#54805,#54806,#54807,#54808,#54809,#54810,#54811,
#54812,#54813,#54814,#54815,#54816,#54817,#54818,#54819,#54820,#54821,#54822,
#54823,#54824,#54825,#54826,#54827,#54828,#54829,#54830,#54831,#54832,#54833,
#54834,#54835,#54836,#54837,#54838,#54839,#54840,#54841,#54842,#54843,#54844,
#54845,#54846,#54847,#54848,#54849,#54850,#54851,#54852,#54853,#54854,#54855,
#54856,#54857,#54858,#54859,#54860,#54861,#54862,#54863,#54864,#54865,#54866,
#54867,#54868,#54869,#54870,#54871,#54872,#54873,#54874,#54875,#54876,#54877,
#54878,#54879,#54880,#54881,#54882,#54883,#54884,#54885,#54886,#54887,#54888,
#54889,#54890,#54891,#54892,#54893,#54894,#54895,#54896,#54897,#54898,#54899,
#54900,#54901,#54902,#54903,#54904,#54905,#54906,#54907,#54908,#54909,#54910,
#54911,#54912,#54913,#54914,#54915,#54916,#54917,#54918,#54919,#54920,#54921,
#54922,#54923,#54924,#54925,#54926,#54927,#54928,#54929,#54930,#54931,#54932,
#54933,#54934,#54935,#54936,#54937,#54938,#54939,#54940,#54941,#54942,#54943,
#54944,#54945,#54946,#54947,#54948,#54949,#54950,#54951,#54952,#54953,#54954,
#54955,#54956,#54957,#54958,#54959,#54960,#54961,#54962,#54963,#54964,#54965,
#54966,#54967,#54968,#54969,#54970,#54971,#54972,#54973,#54974,#54975,#54976,
#54977,#54978,#54979,#54980,#54981,#54982,#54983,#54984,#54985,#54986,#54987,
#54988,#54989,#54990,#54991,#54992,#54993,#54994,#54995,#54996,#54997,#54998,
#54999,#55000,#55001,#55002,#55003,#55004,#55005,#55006,#55007,#55008,#55009,
#55010,#55011,#55012,#55013,#55014,#55015,#55016,#55017,#55018,#55019,#55020,
#55021,#55022,#55023,#55024,#55025,#55026,#55027,#55028,#55029,#55030,#55031,
#55032,#55033,#55034,#55035,#55036,#55037,#55038,#55039,#55040,#55041,#55042,
#55043,#55044,#55045,#55046,#55047,#55048,#55049,#55050,#55051,#55052,#55053,
#55054,#55055,#55056,#55057,#55058,#55059,#55060,#55061,#55062,#55063,#55064,
#55065,#55066,#55067,#55068,#55069,#55070,#55071,#55072,#55073,#55074,#55075,
#55076,#55077,#55078,#55079,#55080,#55081,#55082,#55083,#55084,#55085,#55086,
#55087,#55088,#55089,#55090,#55091,#55092,#55093,#55094,#55095,#55096,#55097,
#55098,#55099,#55100,#55101,#55102,#55103,#55104,#55105,#55106,#55107,#55108,
#55109,#55110,#55111,#55112,#55113,#55114,#55115,#55116,#55117,#55118,#55119,
#55120,#55121,#55122,#55123,#55124,#55125,#55126,#55127,#55128,#55129,#55130,
#55131,#55132,#55133,#55134,#55135,#55136,#55137,#55138,#55139,#55140,#55141,
#55142,#55143,#55144,#55145,#55146,#55147,#55148,#55149,#55150,#55151,#55152,
#55153,#55154,#55155,#55156,#55157,#55158,#55159,#55160,#55161,#55162,#55163,
#55164,#55165,#55166,#55167,#55168,#55169,#55170,#55171,#55172,#55173,#55174,
#55175,#55176,#55177,#55178,#55179,#55180,#55181,#55182,#55183,#55184,#55185,
#55186,#55187,#55188,#55189,#55190,#55191,#55192,#55193,#55194,#55195,#55196,
#55197,#55198,#55199,#55200,#55201,#55202,#55203,#55204,#55205,#55206,#55207,
#55208,#55209,#55210,#55211,#55212,#55213,#55214,#55215,#55216,#55217,#55218,
#55219,#55220,#55221,#55222,#55223,#55224,#55225,#55226,#55227,#55228,#55229,
#55230,#55231,#55232,#55233,#55234,#55235,#55236,#55237,#55238,#55239,#55240,
#55241,#55242,#55243,#55244,#55245,#55246,#55247,#55248,#55249,#55250,#55251,
#55252,#55253,#55254,#55255,#55256,#55257,#55258,#55259,#55260,#55261,#55262,
#55263,#55264,#55265,#55266,#55267,#55268,#55269,#55270,#55271,#55272,#55273,
#55274,#55275,#55276,#55277,#55278,#55279,#55280,#55281,#55282,#55283,#55284,
#55285,#55286,#55287,#55288,#55289,#55290,#55291,#55292,#55293,#55294,#55295,
#55296,#55297,#55298,#55299,#55300,#55301,#55302,#55303,#55304,#55305,#55306,
#55307,#55308,#55309,#55310,#55311,#55312,#55313,#55314,#55315,#55316,#55317,
#55318,#55319,#55320,#55321,#55322,#55323,#55324,#55325,#55326,#55327,#55328,
#55329,#55330,#55331,#55332,#55333,#55334,#55335,#55336,#55337,#55338,#55339,
#55340,#55341,#55342,#55343,#55344,#55345,#55346,#55347,#55348,#55349,#55350,
#55351,#55352,#55353,#55354,#55355,#55356,#55357,#55358,#55359,#55360,#55361,
#55362,#55363,#55364,#55365,#55366,#55367,#55368,#55369,#55370,#55371,#55372,
#55373,#55374,#55375,#55376,#55377,#55378,#55379,#55380,#55381,#55382,#55383,
#55384,#55385,#55386,#55387,#55388,#55389,#55390,#55391,#55392,#55393,#55394,
#55395,#55396,#55397,#55398,#55399,#55400,#55401,#55402,#55403,#55404,#55405,
#55406,#55407,#55408,#55409,#55410,#55411,#55412,#55413,#55414,#55415,#55416,
#55417,#55418),.UNSPECIFIED.,.F.,.F.,(4,3,3,3,3,3,3,3,3,3,3,3,3,3,3,3,3,
3,3,3,3,3,3,3,3,3,3,3,3,3,3,3,3,3,3,3,3,3,3,3,3,3,3,3,3,3,3,3,3,3,3,3,3,
3,3,3,3,3,3,3,3,3,3,3,3,3,3,3,3,3,3,3,3,3,3,3,3,3,3,3,3,3,3,3,3,3,3,3,3,
3,3,3,3,3,3,3,3,3,3,3,3,3,3,3,3,3,3,3,3,3,3,3,3,3,3,3,3,3,3,3,3,3,3,3,3,
3,3,3,3,3,3,3,3,3,3,3,3,3,3,3,3,3,3,3,3,3,3,3,3,3,3,3,3,3,3,3,3,3,3,3,3,
3,3,3,3,3,3,3,3,3,3,3,3,3,3,3,3,3,3,3,3,3,3,3,3,3,3,3,3,3,3,3,3,3,3,3,3,
3,3,3,3,3,3,3,3,3,3,3,3,3,3,3,3,3,3,3,3,3,3,3,3,3,3,3,3,3,3,3,3,3,3,3,3,
3,3,3,3,3,3,3,3,3,3,3,3,3,3,3,3,3,3,3,3,3,3,3,3,3,3,3,3,3,3,3,3,3,3,3,3,
3,3,3,3,3,3,3,3,3,3,3,3,3,3,3,3,3,3,3,3,3,3,3,3,3,3,3,3,3,3,4),(0.644791544335362,
0.645153526214939,0.645310959618977,0.645676474496103,0.645833977154658,
0.646251301875498,0.646353924248001,0.646424939099399,0.646751072183065,
0.646950625627699,0.64699138736001,0.646991525407673,0.64741101203503,0.647643683290812,
0.648195346727212,0.648314485471916,0.648760289982565,0.64888432497532,
0.649191230384658,0.64919137322513,0.649743701241436,0.650140118372147,
0.650719692365367,0.651214822882452,0.651343080325357,0.651391073409306,
0.651391118944592,0.651951507715739,0.652100355662719,0.652712754250196,
0.652802674436081,0.653186195416618,0.65350741365838,0.653590916433954,
0.653590949962743,0.653951215231746,0.654105156926794,0.654482857907031,
0.654630094944148,0.655028794384741,0.655315168920487,0.655559771981192,
0.655790759458603,0.655790903513987,0.656185724410983,0.65638239282991,
0.656821086322865,0.65697575108274,0.657332254560426,0.657734962677141,
0.657924154301468,0.657990683752338,0.658460186042501,0.658709155264617,
0.658929817760636,0.6593803011134,0.659694947721945,0.660021259979664,0.66019060041926,
0.660511836060965,0.660952534313357,0.661343081661848,0.661695233509873,
0.66204282942369,0.662216627380598,0.662328533219871,0.662390425337507,
0.66240491166612,0.662761745796994,0.662955596401597,0.663264831817701,
0.663328505469564,0.663704741137132,0.663892542138641,0.664235780750512,
0.664467522099156,0.664785121524789,0.665033275081114,0.665323412565411,
0.665323504224367,0.665592315581149,0.665778427922754,0.666074241307012,
0.666091977245835,0.666470976691864,0.666543952896891,0.666789974581843,
0.666789995247387,0.667330927477148,0.667393714335977,0.667933178703534,
0.668256536598275,0.668256544848671,0.668605057755227,0.66877470553658,
0.669134150256417,0.66930821010701,0.669677339906848,0.669774720705461,
0.670125227874921,0.670310269821686,0.670651527670531,0.670830859015959,
0.67118966063114,0.671189662891252,0.671538735284599,0.671618030118071,
0.67208399631781,0.672135733711233,0.672661552360578,0.673044160487637,
0.673179325034197,0.673525613633103,0.673848078572894,0.674076140309273,
0.674122729337065,0.67420257814757,0.674559244662587,0.67486862550672,0.675257295657817,
0.675637894901448,0.675983426972843,0.676427553621864,0.676741731944786,
0.676911294803007,0.677025830947751,0.677055910267708,0.677151777331771,
0.677655659551064,0.677713913776227,0.67816429033793,0.678292630192222,
0.678763137657689,0.678874664674428,0.678993708944106,0.679352446613448,
0.679572038930489,0.67989743364412,0.679989025127146,0.679989032729732,
0.680417499639778,0.680529121847719,0.680837199560911,0.681190702812042,
0.681376485586431,0.681832054604986,0.681918146094485,0.682188840285563,
0.68218887575438,0.682592647713095,0.682741217853742,0.683080469862056,
0.683293559953105,0.68363245094592,0.683841139366067,0.684230019465082,
0.684388688142652,0.684388718779029,0.68477543417128,0.684901445944761,
0.685237165836678,0.685419525169911,0.685752152648389,0.686135017102178,
0.686270873035483,0.686588561803677,0.686588563961573,0.68701213394025,
0.687208852037015,0.687645656957109,0.687832869652567,0.688210448282073,
0.688603622060726,0.688788404828325,0.688788445304447,0.689234599453257,
0.689460878957657,0.690014332354325,0.690145416254356,0.690621741553209,
0.690667884777815,0.690988247852973,0.690988419520626,0.691578457316744,
0.691668549527717,0.692360626115915,0.69293700643562,0.693026399397215,
0.693126468529246,0.693188090877621,0.693188210019722,0.693927397679595,
0.693979095312235,0.694775852319244,0.695387933902269,0.695388047386415,
0.695584235585489,0.696108116218357,0.696229480688965,0.696870106729419,
0.697364125699618,0.697498050280852,0.697587776926917,0.697587885484661,
0.698042602111492,0.698519485036437,0.698556272656978,0.699069574081016,
0.699500643103421,0.699574567853642,0.699787589992094,0.699787619951565,
0.700415085712946,0.700499821760193,0.701126162407082,0.701603988320641,
0.701728364262427,0.701987439035147,0.701987462976214,0.702537414953183,
0.7028430229729,0.703057651041027,0.703388907902351,0.703603444135822,0.70418727088409,
0.704361221807698,0.704789009876726,0.705188575134246,0.705488249077386,
0.705913030342945,0.706150150624875,0.706292385171816,0.706382421329585,
0.706387270906805,0.706710299363978,0.706972180134217,0.707375869617682,
0.707647452157423,0.707957694005688,0.70829012570918,0.708586938068078,
0.708659205690346,0.708990910364272,0.709365643469127,0.709644137700458,
0.709921252561858,0.710299578784898,0.710332334411613,0.710688552901087,
0.710786835074806,0.710787432953519,0.711123697531024,0.711299298463576,
0.711656326506015,0.711714602623934,0.71202822819272,0.712174659651686,
0.712694888330029,0.712986678099454,0.712986879391121,0.713441669408398,
0.71366310711077,0.714017902447798,0.714694833321608,0.715092726948194,
0.715186521124103,0.715186555121356,0.715694340947741,0.71586053451435,
0.716367122125722,0.716876743137236,0.717285120793596,0.717386364148751,
0.71738638419871,0.71770367156283,0.718370718748376,0.718997757402535,0.719548123644611,
0.719586207173399,0.719586275934013,0.71998749286588,0.720388799951697,
0.720788181016139,0.721052769189831,0.721052822585763,0.721391810704347,
0.721928057393333,0.722030765857978,0.722621495484741,0.72268180044997,
0.723118129548938,0.7232370927966,0.723599034779558,0.723879022187679,0.723985893222695,
0.723985955035569,0.724315949004016,0.724646856840013,0.724978232920593,
0.725079475029497),.UNSPECIFIED.);
#797=B_SPLINE_CURVE_WITH_KNOTS('',3,(#55651,#55652,#55653,#55654,#55655,
#55656,#55657,#55658,#55659,#55660,#55661,#55662,#55663,#55664,#55665,#55666,
#55667,#55668,#55669,#55670,#55671,#55672,#55673,#55674,#55675,#55676,#55677,
#55678,#55679,#55680,#55681,#55682,#55683,#55684,#55685,#55686,#55687,#55688,
#55689,#55690,#55691,#55692,#55693,#55694,#55695,#55696,#55697,#55698,#55699,
#55700,#55701,#55702,#55703,#55704,#55705,#55706,#55707,#55708,#55709,#55710,
#55711,#55712,#55713,#55714,#55715,#55716,#55717,#55718,#55719,#55720,#55721,
#55722,#55723,#55724,#55725,#55726,#55727,#55728,#55729,#55730,#55731,#55732,
#55733,#55734,#55735,#55736,#55737,#55738,#55739,#55740,#55741,#55742,#55743,
#55744,#55745,#55746,#55747,#55748,#55749,#55750,#55751,#55752,#55753,#55754,
#55755,#55756,#55757,#55758,#55759,#55760,#55761,#55762,#55763,#55764,#55765,
#55766,#55767,#55768,#55769,#55770,#55771,#55772,#55773,#55774,#55775,#55776,
#55777,#55778,#55779,#55780,#55781,#55782,#55783,#55784,#55785,#55786,#55787,
#55788,#55789,#55790,#55791,#55792,#55793,#55794,#55795,#55796,#55797,#55798,
#55799,#55800,#55801,#55802,#55803,#55804,#55805,#55806,#55807,#55808,#55809,
#55810,#55811,#55812,#55813,#55814,#55815,#55816,#55817,#55818,#55819,#55820,
#55821,#55822,#55823,#55824,#55825,#55826,#55827,#55828,#55829,#55830,#55831,
#55832,#55833,#55834,#55835,#55836,#55837,#55838,#55839,#55840,#55841,#55842,
#55843,#55844,#55845,#55846,#55847,#55848,#55849,#55850,#55851,#55852,#55853,
#55854,#55855,#55856,#55857,#55858,#55859,#55860,#55861,#55862,#55863,#55864,
#55865,#55866,#55867,#55868,#55869,#55870,#55871,#55872,#55873,#55874,#55875,
#55876,#55877,#55878,#55879,#55880,#55881,#55882,#55883,#55884,#55885,#55886,
#55887,#55888,#55889,#55890,#55891,#55892,#55893,#55894,#55895,#55896,#55897,
#55898,#55899,#55900,#55901,#55902,#55903,#55904,#55905,#55906,#55907,#55908,
#55909,#55910,#55911,#55912,#55913,#55914,#55915,#55916,#55917,#55918,#55919,
#55920,#55921,#55922,#55923,#55924,#55925,#55926,#55927,#55928,#55929,#55930,
#55931,#55932,#55933,#55934,#55935,#55936,#55937,#55938,#55939,#55940,#55941,
#55942,#55943,#55944,#55945,#55946,#55947,#55948,#55949,#55950,#55951,#55952,
#55953,#55954,#55955,#55956,#55957,#55958,#55959,#55960,#55961,#55962,#55963,
#55964,#55965,#55966,#55967,#55968,#55969,#55970,#55971,#55972,#55973,#55974,
#55975,#55976,#55977,#55978,#55979,#55980,#55981,#55982,#55983,#55984,#55985,
#55986,#55987,#55988,#55989,#55990,#55991,#55992,#55993,#55994,#55995,#55996,
#55997,#55998,#55999,#56000,#56001,#56002,#56003,#56004,#56005,#56006,#56007,
#56008,#56009,#56010,#56011,#56012,#56013,#56014,#56015,#56016,#56017,#56018,
#56019,#56020,#56021,#56022,#56023,#56024,#56025,#56026,#56027,#56028,#56029,
#56030,#56031,#56032,#56033,#56034,#56035,#56036,#56037,#56038,#56039,#56040,
#56041,#56042,#56043,#56044,#56045,#56046,#56047,#56048,#56049,#56050,#56051,
#56052,#56053,#56054,#56055,#56056,#56057,#56058,#56059,#56060,#56061,#56062,
#56063,#56064,#56065,#56066,#56067,#56068,#56069,#56070,#56071,#56072,#56073,
#56074,#56075,#56076,#56077,#56078,#56079,#56080,#56081,#56082,#56083,#56084,
#56085,#56086,#56087,#56088,#56089,#56090,#56091,#56092,#56093,#56094,#56095,
#56096,#56097,#56098,#56099,#56100,#56101,#56102,#56103,#56104,#56105,#56106,
#56107,#56108,#56109,#56110,#56111,#56112,#56113,#56114,#56115,#56116,#56117,
#56118,#56119,#56120,#56121,#56122,#56123,#56124,#56125,#56126,#56127,#56128,
#56129,#56130,#56131,#56132,#56133,#56134,#56135,#56136,#56137,#56138,#56139,
#56140,#56141,#56142,#56143,#56144,#56145,#56146,#56147,#56148,#56149,#56150,
#56151,#56152,#56153,#56154,#56155,#56156,#56157,#56158,#56159,#56160,#56161,
#56162,#56163,#56164,#56165,#56166,#56167,#56168,#56169,#56170,#56171,#56172,
#56173,#56174,#56175,#56176,#56177,#56178,#56179,#56180,#56181,#56182,#56183,
#56184,#56185,#56186,#56187,#56188,#56189,#56190,#56191,#56192,#56193,#56194,
#56195,#56196,#56197,#56198,#56199,#56200,#56201,#56202,#56203,#56204,#56205,
#56206,#56207,#56208,#56209,#56210,#56211,#56212,#56213,#56214,#56215,#56216,
#56217,#56218,#56219,#56220,#56221,#56222,#56223,#56224,#56225,#56226,#56227,
#56228,#56229,#56230,#56231,#56232,#56233),.UNSPECIFIED.,.F.,.F.,(4,3,3,
3,3,3,3,3,3,3,3,3,3,3,3,3,3,3,3,3,3,3,3,3,3,3,3,3,3,3,3,3,3,3,3,3,3,3,3,
3,3,3,3,3,3,3,3,3,3,3,3,3,3,3,3,3,3,3,3,3,3,3,3,3,3,3,3,3,3,3,3,3,3,3,3,
3,3,3,3,3,3,3,3,3,3,3,3,3,3,3,3,3,3,3,3,3,3,3,3,3,3,3,3,3,3,3,3,3,3,3,3,
3,3,3,3,3,3,3,3,3,3,3,3,3,3,3,3,3,3,3,3,3,3,3,3,3,3,3,3,3,3,3,3,3,3,3,3,
3,3,3,3,3,3,3,3,3,3,3,3,3,3,3,3,3,3,3,3,3,3,3,3,3,3,3,3,3,3,3,3,3,3,3,3,
3,3,3,3,3,3,3,3,3,3,3,4),(0.915748838693565,0.916067586719041,0.916618732140758,
0.917169877562474,0.917721481216459,0.918241275309113,0.918273084870444,
0.918757739489292,0.919246857269427,0.919746927616459,0.920247700587533,
0.920483825124084,0.920990364456346,0.921484789544461,0.9217667121008,0.922249664809996,
0.922698785915839,0.92318275926108,0.923671046736705,0.924149740011753,
0.924356372081894,0.924775684712307,0.925307267240614,0.925860796180226,
0.926019879675272,0.926576660565611,0.927130916852163,0.927678914489343,
0.927784657323815,0.928394696744112,0.929031497175013,0.929338792057307,
0.92979063906482,0.930168046555878,0.930997525017763,0.931796620805825,
0.931827442761244,0.932381920865375,0.932656371732784,0.933070393415616,
0.933484504567997,0.93380260254683,0.934313586850845,0.934917026397449,
0.935142074968692,0.935307088852584,0.93555558405891,0.935968790006292,
0.936418900111347,0.936811575158338,0.937527538981205,0.93827342969671,
0.938995279415561,0.939284250243221,0.939820547769846,0.940071295487471,
0.940322043205097,0.940823538640348,0.940948912499161,0.941074286357974,
0.9413250340756,0.941575781793225,0.941701155652038,0.941826529510851,0.942249264940764,
0.942495190091186,0.942603578551054,0.943095900896275,0.943580323596278,
0.943832511251856,0.944166841542024,0.944501171832191,0.944938638928722,
0.945169832412526,0.945538045761981,0.945838492992861,0.945921380498607,
0.946297882566809,0.946507153573196,0.946950286941434,0.94739738083765,
0.947844474733866,0.948324751514134,0.948804857448725,0.949234065154626,
0.949712200936782,0.949850456474872,0.950647440566719,0.951441288481875,
0.951856438215877,0.952410060135101,0.952962335487208,0.953508063872448,
0.953650084172403,0.953862419956882,0.954510225961816,0.955186614305362,
0.955863002648908,0.955868401697887,0.956564283223973,0.957261946421114,
0.957522607015327,0.957874383438892,0.958471899894767,0.959072403401592,
0.959183774960762,0.959781949211659,0.959880365179897,0.960281925199207,
0.960682630542461,0.960845791924747,0.9608833560504,0.961311031019981,0.961737255803494,
0.961886346920902,0.962308282220108,0.962507322521059,0.962889337791405,
0.963271501480925,0.963651777930102,0.963892328661908,0.96416714743821,
0.964728584203379,0.965299528905214,0.965822212371328,0.966383697312681,
0.966901301273415,0.967445154901957,0.967481492533015,0.968027964557667,
0.968308874491794,0.968722367006821,0.969136310989922,0.969677231781982,
0.969910273884923,0.970342754897255,0.970786543600009,0.971235578300656,
0.971682710908604,0.972126784752767,0.972454518470128,0.972919246496431,
0.973450678525925,0.974001282847571,0.974116846453059,0.974667737072339,
0.975220565268069,0.975773393463799,0.975928219107938,0.976507314070495,
0.977104755059656,0.977432705413692,0.977935838204517,0.978257070471356,
0.978765012877377,0.978937191719446,0.97959434532721,0.980205160388321,
0.9804416780252,0.980740989458624,0.98143807725267,0.981946164330954,0.982434467230622,
0.982922769293201,0.98322518755684,0.983450650636708,0.983992206813968,
0.984468374379881,0.984955136942461,0.98547473936798,0.985712352984715,
0.986234938879445,0.986459623248215,0.986990260954347,0.987532112492594,
0.987964109553969,0.988202177576321,0.9886837301815,0.989175358682956,0.989468595859723,
0.989973288090569,0.990473310403973,0.990693251075575,0.990973082165477,
0.991469851085119,0.991986421692916,0.992500190747837,0.992994577671546,
0.993177675872154,0.993680925517914,0.993982054776985,0.994478920023504,
0.99498840685027,0.99550066833255,0.995667097027233),.UNSPECIFIED.);
#798=B_SPLINE_CURVE_WITH_KNOTS('',3,(#56595,#56596,#56597,#56598,#56599,
#56600,#56601,#56602,#56603,#56604,#56605,#56606,#56607,#56608,#56609,#56610,
#56611,#56612,#56613,#56614,#56615,#56616,#56617,#56618,#56619,#56620,#56621,
#56622,#56623,#56624,#56625,#56626,#56627,#56628,#56629,#56630,#56631,#56632,
#56633,#56634,#56635,#56636,#56637,#56638,#56639,#56640,#56641,#56642,#56643,
#56644,#56645,#56646,#56647,#56648,#56649,#56650,#56651,#56652,#56653,#56654,
#56655,#56656,#56657,#56658,#56659,#56660,#56661,#56662,#56663,#56664,#56665,
#56666,#56667,#56668,#56669,#56670,#56671,#56672,#56673,#56674,#56675,#56676,
#56677,#56678,#56679,#56680,#56681,#56682,#56683,#56684,#56685,#56686,#56687,
#56688,#56689,#56690,#56691,#56692,#56693,#56694,#56695,#56696,#56697,#56698,
#56699,#56700,#56701,#56702,#56703,#56704,#56705,#56706,#56707,#56708,#56709,
#56710,#56711,#56712,#56713,#56714,#56715,#56716,#56717,#56718,#56719,#56720,
#56721,#56722,#56723,#56724,#56725,#56726,#56727,#56728,#56729,#56730,#56731,
#56732,#56733,#56734,#56735,#56736,#56737,#56738,#56739,#56740,#56741,#56742,
#56743,#56744,#56745,#56746,#56747,#56748,#56749,#56750,#56751,#56752,#56753,
#56754,#56755,#56756,#56757,#56758,#56759,#56760,#56761,#56762,#56763,#56764,
#56765,#56766,#56767,#56768,#56769,#56770,#56771,#56772,#56773,#56774,#56775,
#56776,#56777,#56778,#56779,#56780,#56781,#56782,#56783,#56784,#56785,#56786,
#56787,#56788,#56789,#56790,#56791,#56792,#56793,#56794,#56795,#56796,#56797,
#56798,#56799,#56800,#56801,#56802,#56803,#56804,#56805,#56806,#56807,#56808,
#56809,#56810,#56811,#56812,#56813,#56814,#56815,#56816,#56817,#56818,#56819,
#56820,#56821,#56822,#56823,#56824,#56825,#56826,#56827,#56828,#56829,#56830,
#56831,#56832,#56833,#56834,#56835,#56836,#56837,#56838,#56839,#56840,#56841,
#56842,#56843,#56844,#56845,#56846,#56847,#56848,#56849,#56850,#56851,#56852,
#56853,#56854,#56855,#56856,#56857,#56858,#56859,#56860,#56861,#56862,#56863,
#56864,#56865,#56866,#56867,#56868,#56869,#56870,#56871,#56872,#56873,#56874,
#56875,#56876,#56877,#56878,#56879,#56880,#56881,#56882,#56883,#56884,#56885,
#56886,#56887,#56888,#56889,#56890,#56891,#56892,#56893,#56894,#56895,#56896,
#56897,#56898,#56899,#56900,#56901,#56902,#56903,#56904,#56905,#56906,#56907,
#56908,#56909,#56910,#56911,#56912,#56913,#56914,#56915,#56916,#56917,#56918,
#56919,#56920,#56921,#56922,#56923,#56924,#56925,#56926,#56927,#56928,#56929,
#56930,#56931,#56932,#56933,#56934,#56935,#56936,#56937,#56938,#56939,#56940,
#56941,#56942,#56943,#56944,#56945,#56946,#56947,#56948,#56949,#56950,#56951,
#56952,#56953,#56954,#56955,#56956,#56957,#56958,#56959,#56960,#56961,#56962,
#56963,#56964,#56965,#56966,#56967,#56968,#56969,#56970,#56971,#56972,#56973,
#56974,#56975,#56976,#56977,#56978,#56979,#56980,#56981,#56982,#56983,#56984,
#56985,#56986,#56987,#56988,#56989,#56990,#56991,#56992,#56993,#56994,#56995,
#56996,#56997,#56998,#56999,#57000,#57001,#57002,#57003,#57004,#57005,#57006,
#57007,#57008,#57009,#57010,#57011,#57012,#57013,#57014,#57015,#57016,#57017,
#57018,#57019,#57020,#57021,#57022,#57023,#57024,#57025,#57026,#57027,#57028,
#57029,#57030,#57031,#57032,#57033,#57034,#57035,#57036,#57037,#57038,#57039,
#57040,#57041,#57042,#57043,#57044,#57045,#57046,#57047,#57048,#57049,#57050,
#57051,#57052,#57053,#57054,#57055,#57056,#57057,#57058,#57059,#57060,#57061,
#57062,#57063,#57064,#57065,#57066,#57067,#57068,#57069,#57070,#57071,#57072,
#57073,#57074,#57075,#57076,#57077,#57078,#57079,#57080,#57081,#57082,#57083,
#57084,#57085,#57086,#57087,#57088,#57089,#57090,#57091,#57092,#57093,#57094,
#57095,#57096,#57097,#57098,#57099,#57100,#57101,#57102,#57103,#57104,#57105,
#57106,#57107,#57108,#57109,#57110,#57111,#57112,#57113,#57114,#57115,#57116,
#57117,#57118,#57119,#57120,#57121,#57122,#57123,#57124,#57125,#57126,#57127,
#57128,#57129,#57130,#57131,#57132,#57133,#57134,#57135,#57136,#57137,#57138,
#57139,#57140,#57141,#57142,#57143,#57144),.UNSPECIFIED.,.F.,.F.,(4,3,3,
3,3,3,3,3,3,3,3,3,3,3,3,3,3,3,3,3,3,3,3,3,3,3,3,3,3,3,3,3,3,3,3,3,3,3,3,
3,3,3,3,3,3,3,3,3,3,3,3,3,3,3,3,3,3,3,3,3,3,3,3,3,3,3,3,3,3,3,3,3,3,3,3,
3,3,3,3,3,3,3,3,3,3,3,3,3,3,3,3,3,3,3,3,3,3,3,3,3,3,3,3,3,3,3,3,3,3,3,3,
3,3,3,3,3,3,3,3,3,3,3,3,3,3,3,3,3,3,3,3,3,3,3,3,3,3,3,3,3,3,3,3,3,3,3,3,
3,3,3,3,3,3,3,3,3,3,3,3,3,3,3,3,3,3,3,3,3,3,3,3,3,3,3,3,3,3,3,3,3,3,3,3,
4),(0.0739106570180644,0.0742505665322785,0.0749231593883048,0.0755866481880669,
0.0759087958897528,0.076109515853017,0.0766704676188221,0.0772427974835055,
0.0775672823813314,0.0781410133149838,0.0783083908329088,0.0789200737186309,
0.0792265158692337,0.0798668908410172,0.0804745670761699,0.0805072658128007,
0.0808859595499181,0.0814877117812548,0.0820930282493823,0.0825447199390884,
0.0827061407926925,0.0833087258292241,0.0839238796533188,0.0842038066950157,
0.0848203409180411,0.0849050157725843,0.0854899487551179,0.0858631843941102,
0.0864523004693559,0.087032068073914,0.0871038907524762,0.0875229639776386,
0.0882679936403748,0.0890439628033391,0.0891822488886336,0.089302765732368,
0.0898310045056427,0.0903636653995039,0.0908393319980337,0.0913718057085553,
0.0915016407122598,0.0920835465321469,0.0924996977112301,0.0930930176814939,
0.0936813910903183,0.0941575341655823,0.0944334740187823,0.0951651912138979,
0.0958167134838409,0.0958993906720435,0.0966323489986741,0.0973181599504825,
0.0973653073253047,0.0974755459779731,0.0980219245564783,0.0985838235379587,
0.0991325409926556,0.0997148408122413,0.100258221552417,0.100297140631827,
0.100792995183773,0.101308629054549,0.101830716554359,0.102345774153224,
0.102450652527534,0.102965706889615,0.10322897393835,0.103738172914004,
0.104113788359032,0.104627808420626,0.105146290123506,0.10565440664557,
0.105770524262713,0.106160807244872,0.106705901621213,0.107271149233365,
0.107430308244803,0.107997658854337,0.108559372191222,0.109092640551394,
0.109640205515494,0.110205338349633,0.110773045133129,0.111291515531286,
0.111806384546412,0.111850938235435,0.112365499248319,0.112877106880496,
0.113381077069814,0.113490390511178,0.114064065326149,0.114681693127011,
0.114893126254671,0.115510243216294,0.11568926549107,0.115722281841006,
0.116393734861723,0.117070158047736,0.117380439167713,0.117888140470962,
0.118499435575117,0.119039707104872,0.119649338716235,0.120087015450854,
0.12069921012744,0.121330234043752,0.121955732108456,0.122285890430745,
0.122358373459964,0.12300483067754,0.12365625651878,0.124017367865778,0.124484765410637,
0.125098996875331,0.125677401720794,0.12628924989947,0.126683640390529,
0.127260089345903,0.127337209863532,0.127914998541037,0.128442609316833,
0.128882515370421,0.12936438870894,0.12954913842743,0.130034891721818,0.130520457661336,
0.131003051321121,0.131081390350313,0.131618115585724,0.131761670629781,
0.132314371274939,0.132867071920098,0.133280265330205,0.13375140920545,
0.133973203597052,0.134449087317234,0.134925679495375,0.135400668751173,
0.135479140310096,0.135969345652594,0.136459550995091,0.136945358596306,
0.137428217493013,0.137678015289988,0.138189487685163,0.138701835983074,
0.13894804272558,0.139460242574507,0.13987689026988,0.140333710283354,0.140792571382241,
0.141247205717867,0.141435605416639,0.141894660642086,0.142075765249772,
0.142544562020476,0.143016314713469,0.14349170384893,0.143924407321535,
0.144274640229664,0.144869070757695,0.145455531262855,0.145740556882925,
0.146224374908676,0.146412980072117,0.146898415400794,0.147206473536186,
0.147638362202818,0.147939431862817,0.148393236367263,0.14884865756534,
0.148901346511435,0.14936212130732,0.149819542963643,0.150138306842709,
0.150607829238979,0.151087910716682,0.151392024260246,0.151867636287259,
0.15234404539651,0.15280700372131,0.153070140149231,0.153474908875717,0.153879677602202),
 .UNSPECIFIED.);
#799=B_SPLINE_CURVE_WITH_KNOTS('',3,(#57421,#57422,#57423,#57424,#57425,
#57426,#57427,#57428,#57429,#57430,#57431,#57432,#57433,#57434,#57435,#57436,
#57437,#57438,#57439,#57440,#57441,#57442,#57443,#57444,#57445,#57446,#57447,
#57448,#57449,#57450,#57451,#57452,#57453,#57454,#57455,#57456,#57457,#57458,
#57459,#57460,#57461,#57462,#57463,#57464,#57465,#57466,#57467,#57468,#57469,
#57470,#57471,#57472,#57473,#57474,#57475,#57476,#57477,#57478,#57479,#57480,
#57481,#57482,#57483,#57484,#57485,#57486,#57487,#57488,#57489,#57490,#57491,
#57492,#57493,#57494,#57495,#57496,#57497,#57498,#57499,#57500,#57501,#57502,
#57503,#57504,#57505,#57506,#57507,#57508,#57509,#57510,#57511,#57512,#57513,
#57514,#57515,#57516,#57517,#57518,#57519,#57520,#57521,#57522,#57523,#57524,
#57525,#57526,#57527,#57528,#57529,#57530,#57531,#57532,#57533,#57534,#57535,
#57536,#57537,#57538,#57539,#57540,#57541,#57542,#57543,#57544,#57545,#57546,
#57547,#57548,#57549,#57550,#57551,#57552,#57553,#57554,#57555,#57556,#57557,
#57558,#57559,#57560,#57561,#57562,#57563,#57564,#57565,#57566,#57567,#57568,
#57569,#57570,#57571,#57572,#57573,#57574,#57575,#57576,#57577,#57578,#57579,
#57580,#57581,#57582,#57583,#57584,#57585,#57586,#57587,#57588,#57589,#57590,
#57591,#57592,#57593,#57594,#57595,#57596,#57597,#57598,#57599,#57600,#57601,
#57602,#57603,#57604,#57605,#57606,#57607,#57608,#57609,#57610,#57611,#57612,
#57613,#57614,#57615,#57616,#57617,#57618,#57619,#57620,#57621,#57622,#57623,
#57624,#57625,#57626,#57627,#57628,#57629,#57630,#57631,#57632,#57633,#57634,
#57635,#57636,#57637,#57638,#57639,#57640,#57641,#57642,#57643,#57644,#57645,
#57646,#57647,#57648,#57649,#57650,#57651,#57652,#57653,#57654,#57655,#57656,
#57657,#57658,#57659,#57660,#57661,#57662,#57663,#57664,#57665,#57666,#57667,
#57668,#57669,#57670,#57671,#57672,#57673,#57674,#57675,#57676,#57677,#57678,
#57679,#57680,#57681,#57682,#57683,#57684,#57685,#57686,#57687,#57688,#57689,
#57690,#57691,#57692,#57693,#57694,#57695,#57696,#57697,#57698,#57699,#57700,
#57701,#57702,#57703,#57704,#57705,#57706,#57707,#57708,#57709,#57710,#57711,
#57712,#57713,#57714,#57715,#57716,#57717,#57718,#57719,#57720,#57721,#57722,
#57723,#57724,#57725,#57726,#57727,#57728,#57729,#57730,#57731,#57732,#57733,
#57734,#57735,#57736,#57737,#57738,#57739,#57740,#57741,#57742,#57743,#57744,
#57745,#57746,#57747,#57748,#57749,#57750,#57751,#57752,#57753,#57754,#57755,
#57756,#57757,#57758,#57759,#57760,#57761,#57762,#57763,#57764,#57765,#57766,
#57767,#57768,#57769,#57770,#57771,#57772,#57773,#57774,#57775,#57776,#57777,
#57778,#57779,#57780,#57781,#57782,#57783,#57784,#57785,#57786,#57787,#57788,
#57789,#57790,#57791,#57792,#57793,#57794,#57795,#57796,#57797,#57798,#57799,
#57800,#57801,#57802,#57803,#57804,#57805,#57806,#57807,#57808,#57809,#57810,
#57811,#57812,#57813,#57814,#57815,#57816,#57817,#57818,#57819,#57820,#57821,
#57822,#57823,#57824,#57825,#57826,#57827,#57828,#57829,#57830,#57831,#57832,
#57833,#57834,#57835,#57836,#57837,#57838,#57839,#57840,#57841,#57842,#57843,
#57844,#57845,#57846,#57847,#57848,#57849,#57850,#57851,#57852,#57853,#57854,
#57855,#57856,#57857,#57858,#57859,#57860,#57861,#57862,#57863,#57864,#57865,
#57866,#57867,#57868,#57869,#57870,#57871,#57872,#57873,#57874,#57875,#57876,
#57877,#57878,#57879,#57880,#57881,#57882,#57883,#57884,#57885,#57886,#57887,
#57888,#57889,#57890,#57891,#57892,#57893,#57894,#57895,#57896,#57897,#57898,
#57899,#57900,#57901,#57902,#57903,#57904,#57905,#57906,#57907,#57908,#57909,
#57910,#57911,#57912,#57913,#57914,#57915,#57916,#57917,#57918,#57919,#57920,
#57921,#57922,#57923,#57924,#57925,#57926,#57927,#57928,#57929,#57930,#57931,
#57932,#57933,#57934,#57935,#57936,#57937,#57938,#57939,#57940,#57941,#57942,
#57943,#57944,#57945,#57946,#57947,#57948,#57949,#57950,#57951,#57952,#57953,
#57954,#57955,#57956,#57957,#57958,#57959,#57960,#57961,#57962,#57963,#57964,
#57965,#57966,#57967,#57968,#57969,#57970,#57971,#57972,#57973,#57974,#57975,
#57976),.UNSPECIFIED.,.F.,.F.,(4,3,3,3,3,3,3,3,3,3,3,3,3,3,3,3,3,3,3,3,
3,3,3,3,3,3,3,3,3,3,3,3,3,3,3,3,3,3,3,3,3,3,3,3,3,3,3,3,3,3,3,3,3,3,3,3,
3,3,3,3,3,3,3,3,3,3,3,3,3,3,3,3,3,3,3,3,3,3,3,3,3,3,3,3,3,3,3,3,3,3,3,3,
3,3,3,3,3,3,3,3,3,3,3,3,3,3,3,3,3,3,3,3,3,3,3,3,3,3,3,3,3,3,3,3,3,3,3,3,
3,3,3,3,3,3,3,3,3,3,3,3,3,3,3,3,3,3,3,3,3,3,3,3,3,3,3,3,3,3,3,3,3,3,3,3,
3,3,3,3,3,3,3,3,3,3,3,3,3,3,3,3,3,3,3,3,3,4),(0.242278780929826,0.242618092734303,
0.24333413469777,0.244041377852319,0.244276211430585,0.244477134072873,
0.245048716885547,0.245630318148922,0.245934257263667,0.24651646348893,
0.246676009090878,0.247275528750946,0.247593525392491,0.248197421968456,
0.248793107754317,0.248874884108883,0.249253083014459,0.249841372675952,
0.250430946208237,0.25091227673342,0.251073759126888,0.251694184001655,
0.252331325282905,0.252572255228947,0.253211703330374,0.253272634144893,
0.253915385740023,0.254232115752439,0.254875938471737,0.255471509162898,
0.255892371854385,0.256671581711036,0.257488034344503,0.257670384180903,
0.258104037545759,0.258647290627824,0.25919235253277,0.259720571055585,
0.259869259198908,0.260315674536895,0.260920072763573,0.261541478450576,
0.26215654026975,0.262525647993766,0.262801092556248,0.263395374712079,
0.263631320840352,0.264232047831297,0.264267009234918,0.264736085275376,
0.264999967574253,0.265520860472095,0.265732925913588,0.266363313930647,
0.26694788496221,0.267198842592258,0.26796439105204,0.268664759270928,0.269159798730286,
0.269838257667216,0.270130675949598,0.27065940760475,0.270818435077856,
0.271334239762136,0.271596592628268,0.272121943008842,0.272478740635087,
0.273006150744408,0.273535551497999,0.274049971110777,0.274528425985608,
0.27496557447442,0.275526621230416,0.275794006797749,0.276377267361676,
0.276945889259611,0.277450741186514,0.277460259342948,0.278071205706145,
0.278688949701149,0.279110613584496,0.279659134360953,0.28030602981158,
0.280770741699047,0.281406076164999,0.281858009378958,0.28243267024347,
0.283055968940653,0.283681117572295,0.284056884396963,0.28409226323821,
0.284782864424869,0.285484490530849,0.28575124579018,0.286255759414968,
0.286581040013058,0.287155883361734,0.287409792675525,0.287982238169878,
0.288238782002927,0.288454634432973,0.288986046819895,0.289068666071738,
0.289603870252683,0.290139223277884,0.290653509450978,0.291141623420863,
0.29161324931921,0.29175294695998,0.292315024123177,0.292385994793472,0.292852384468983,
0.293313484425323,0.293775351727085,0.293951821977985,0.294044613232258,
0.294457492982334,0.294869659538409,0.295051259486988,0.295531943183432,
0.295703522559497,0.296188974291973,0.296673748337722,0.297155815944093,
0.297250134504992,0.297731578182707,0.297915726534434,0.29839946085133,
0.298883836628845,0.299363939507877,0.299449009522997,0.299984447864382,
0.300127479234637,0.300680364295311,0.301219414013074,0.301647884541002,
0.302211754014893,0.302338298452502,0.302904677623029,0.302959531988322,
0.303518684943125,0.303581301750564,0.303846759559007,0.304359108159607,
0.304825946455333,0.305342469693399,0.305858608951964,0.306045634577012,
0.306534541228051,0.307021795839783,0.307314705683034,0.307799676321633,
0.308244509595017,0.308560286619933,0.309078981781974,0.309598360370356,
0.309804512206349,0.310325829198734,0.310443384613022,0.310937225600257,
0.311434800905744,0.311930980948835,0.31229262793642,0.312642259631027,
0.313177966841344,0.313722311584695,0.314253098011966,0.31477866501222,
0.315309133748266,0.315574092988367,0.316040840884101,0.31651564394236,
0.316987351420504,0.317269581931868,0.317742925877595,0.318206935144652,
0.318505926345707,0.31896678814637,0.319438255897193,0.319761756688362,
0.320227810551655,0.320695470738025,0.321150972778566,0.321437759703047,
0.321843502411458,0.322249245119868),.UNSPECIFIED.);
#800=B_SPLINE_CURVE_WITH_KNOTS('',3,(#58233,#58234,#58235,#58236,#58237,
#58238,#58239,#58240,#58241,#58242,#58243,#58244,#58245,#58246,#58247,#58248,
#58249,#58250,#58251,#58252,#58253,#58254,#58255,#58256,#58257,#58258,#58259,
#58260,#58261,#58262,#58263,#58264,#58265,#58266,#58267,#58268,#58269),
 .UNSPECIFIED.,.F.,.F.,(4,1,1,1,1,1,1,1,1,1,1,1,1,1,1,1,1,1,1,1,1,1,1,1,
1,1,1,1,1,1,1,1,1,1,4),(0.410646223392491,0.412844762664804,0.415043637537941,
0.417242512411078,0.419441387284215,0.421640262157351,0.423839137030488,
0.426038011903625,0.428236886776761,0.43019144221955,0.431168719940944,
0.434100553105126,0.437032386269308,0.439964219433491,0.442896052597673,
0.445827885761855,0.448759718926038,0.45169155209022,0.454623385254402,
0.457555218418585,0.460487051582767,0.463418884746949,0.465617759620086,
0.467816634493223,0.470015509366359,0.472214384239496,0.474413259112633,
0.47661213398577,0.478811008858906,0.481009883732043,0.48320875860518,0.485407633478317,
0.487606508351453,0.48980538322459,0.490612244996583),.UNSPECIFIED.);
#801=B_SPLINE_CURVE_WITH_KNOTS('',3,(#58522,#58523,#58524,#58525,#58526,
#58527,#58528,#58529,#58530,#58531,#58532,#58533,#58534,#58535,#58536,#58537,
#58538,#58539,#58540,#58541,#58542,#58543,#58544,#58545,#58546,#58547,#58548,
#58549,#58550,#58551,#58552,#58553,#58554,#58555,#58556,#58557,#58558,#58559,
#58560,#58561,#58562),.UNSPECIFIED.,.F.,.F.,(4,1,1,1,1,1,1,1,1,1,1,1,1,
1,1,1,1,1,1,1,1,1,1,1,1,1,1,1,1,1,1,1,1,1,1,1,1,1,4),(0.579016667860491,
0.581212386019991,0.583411260963338,0.585610135906685,0.587809010850032,
0.590007885793379,0.592206760736727,0.594405635680074,0.596604510623421,
0.599536343881217,0.602468177139013,0.605400010396809,0.605949729132646,
0.607598885340156,0.609797760283503,0.61199663522685,0.614195510170197,
0.616394385113544,0.618593260056891,0.620792135000238,0.621891572471912,
0.622991009943585,0.625922843201381,0.627388759830279,0.629587634773626,
0.631786509716973,0.633985384660321,0.636184259603668,0.637650176232566,
0.640582009490362,0.642780884433709,0.644979759377056,0.647178634320403,
0.64937750926375,0.651576384207097,0.653775259150444,0.655974134093791,
0.658173009037138,0.658979631102386),.UNSPECIFIED.);
#802=B_SPLINE_CURVE_WITH_KNOTS('',3,(#58791,#58792,#58793,#58794,#58795,
#58796,#58797,#58798,#58799,#58800,#58801,#58802,#58803,#58804,#58805,#58806,
#58807,#58808,#58809,#58810,#58811,#58812,#58813,#58814,#58815,#58816,#58817,
#58818,#58819,#58820,#58821,#58822,#58823,#58824,#58825,#58826,#58827,#58828,
#58829,#58830,#58831,#58832,#58833,#58834,#58835,#58836,#58837,#58838,#58839,
#58840,#58841,#58842,#58843,#58844,#58845,#58846,#58847,#58848,#58849,#58850,
#58851,#58852,#58853,#58854,#58855,#58856,#58857,#58858,#58859,#58860,#58861,
#58862,#58863,#58864,#58865,#58866,#58867,#58868,#58869,#58870,#58871,#58872,
#58873,#58874,#58875,#58876,#58877,#58878,#58879,#58880,#58881,#58882,#58883,
#58884,#58885,#58886,#58887,#58888,#58889,#58890,#58891,#58892,#58893,#58894,
#58895,#58896,#58897,#58898,#58899,#58900,#58901,#58902,#58903,#58904,#58905,
#58906,#58907,#58908,#58909,#58910,#58911,#58912,#58913,#58914,#58915,#58916,
#58917,#58918,#58919,#58920,#58921,#58922,#58923,#58924,#58925,#58926,#58927,
#58928,#58929,#58930,#58931,#58932,#58933,#58934,#58935,#58936,#58937,#58938,
#58939,#58940,#58941,#58942,#58943,#58944,#58945,#58946,#58947,#58948,#58949,
#58950,#58951,#58952,#58953,#58954,#58955,#58956,#58957,#58958,#58959,#58960,
#58961,#58962,#58963,#58964,#58965,#58966,#58967,#58968,#58969,#58970,#58971,
#58972,#58973,#58974,#58975,#58976,#58977,#58978,#58979,#58980,#58981,#58982,
#58983,#58984,#58985,#58986,#58987,#58988,#58989,#58990,#58991,#58992,#58993,
#58994,#58995,#58996,#58997,#58998,#58999,#59000,#59001,#59002,#59003,#59004,
#59005,#59006,#59007,#59008,#59009,#59010,#59011,#59012,#59013,#59014,#59015,
#59016,#59017,#59018,#59019,#59020,#59021,#59022,#59023,#59024,#59025,#59026,
#59027,#59028,#59029,#59030,#59031,#59032,#59033,#59034,#59035,#59036,#59037,
#59038,#59039,#59040,#59041,#59042,#59043,#59044,#59045,#59046,#59047,#59048,
#59049,#59050,#59051,#59052,#59053,#59054,#59055,#59056,#59057,#59058,#59059,
#59060,#59061,#59062,#59063,#59064,#59065,#59066,#59067,#59068,#59069,#59070,
#59071,#59072,#59073,#59074,#59075,#59076,#59077,#59078,#59079,#59080,#59081,
#59082,#59083,#59084,#59085,#59086,#59087,#59088,#59089,#59090,#59091,#59092,
#59093,#59094,#59095,#59096,#59097,#59098,#59099,#59100,#59101,#59102,#59103,
#59104,#59105,#59106,#59107,#59108,#59109,#59110,#59111,#59112,#59113,#59114,
#59115,#59116,#59117,#59118,#59119,#59120,#59121,#59122,#59123,#59124,#59125,
#59126,#59127,#59128,#59129,#59130,#59131,#59132,#59133,#59134,#59135,#59136,
#59137,#59138,#59139,#59140,#59141,#59142,#59143,#59144,#59145,#59146,#59147,
#59148,#59149,#59150,#59151,#59152,#59153,#59154,#59155,#59156,#59157,#59158,
#59159,#59160,#59161,#59162,#59163,#59164,#59165,#59166,#59167,#59168,#59169,
#59170,#59171,#59172,#59173,#59174,#59175,#59176,#59177,#59178,#59179,#59180,
#59181,#59182,#59183,#59184,#59185,#59186,#59187,#59188,#59189,#59190,#59191,
#59192,#59193,#59194,#59195,#59196,#59197,#59198,#59199,#59200,#59201,#59202,
#59203,#59204,#59205,#59206,#59207,#59208,#59209,#59210,#59211,#59212,#59213,
#59214,#59215,#59216,#59217,#59218,#59219,#59220,#59221,#59222,#59223,#59224,
#59225,#59226,#59227,#59228,#59229,#59230,#59231,#59232,#59233,#59234,#59235,
#59236,#59237,#59238,#59239,#59240,#59241,#59242,#59243,#59244,#59245,#59246,
#59247,#59248,#59249,#59250,#59251,#59252,#59253,#59254,#59255,#59256,#59257,
#59258,#59259,#59260,#59261,#59262,#59263,#59264,#59265,#59266,#59267,#59268,
#59269,#59270,#59271,#59272,#59273,#59274,#59275,#59276,#59277,#59278,#59279,
#59280,#59281,#59282,#59283,#59284,#59285,#59286,#59287,#59288,#59289,#59290,
#59291,#59292,#59293,#59294,#59295,#59296,#59297,#59298,#59299,#59300,#59301,
#59302,#59303,#59304,#59305,#59306,#59307,#59308,#59309,#59310,#59311,#59312,
#59313,#59314,#59315,#59316,#59317,#59318,#59319,#59320,#59321,#59322,#59323,
#59324,#59325,#59326,#59327,#59328,#59329,#59330,#59331,#59332,#59333,#59334,
#59335,#59336,#59337,#59338,#59339,#59340,#59341,#59342,#59343,#59344,#59345,
#59346,#59347,#59348,#59349,#59350,#59351,#59352,#59353,#59354,#59355,#59356,
#59357,#59358,#59359,#59360,#59361,#59362,#59363,#59364,#59365,#59366,#59367,
#59368,#59369,#59370,#59371,#59372,#59373,#59374,#59375,#59376,#59377,#59378,
#59379,#59380,#59381,#59382,#59383,#59384,#59385,#59386,#59387,#59388,#59389,
#59390,#59391,#59392,#59393,#59394,#59395,#59396,#59397,#59398,#59399,#59400,
#59401,#59402,#59403,#59404,#59405,#59406,#59407,#59408,#59409,#59410,#59411,
#59412,#59413,#59414,#59415,#59416,#59417,#59418,#59419,#59420,#59421,#59422,
#59423,#59424,#59425,#59426,#59427,#59428,#59429,#59430,#59431,#59432,#59433,
#59434,#59435,#59436,#59437,#59438,#59439,#59440,#59441,#59442,#59443,#59444,
#59445,#59446,#59447,#59448,#59449,#59450,#59451,#59452,#59453,#59454,#59455,
#59456,#59457,#59458,#59459,#59460,#59461,#59462,#59463,#59464,#59465,#59466,
#59467,#59468,#59469,#59470,#59471,#59472,#59473,#59474,#59475,#59476,#59477,
#59478,#59479,#59480,#59481,#59482,#59483,#59484,#59485,#59486,#59487,#59488,
#59489,#59490,#59491,#59492,#59493,#59494,#59495,#59496,#59497,#59498,#59499,
#59500,#59501,#59502,#59503,#59504,#59505,#59506,#59507,#59508,#59509,#59510,
#59511,#59512,#59513,#59514,#59515,#59516,#59517,#59518,#59519,#59520,#59521,
#59522,#59523,#59524,#59525,#59526,#59527,#59528,#59529,#59530,#59531,#59532,
#59533,#59534,#59535,#59536,#59537,#59538,#59539,#59540,#59541,#59542,#59543,
#59544,#59545,#59546,#59547,#59548,#59549,#59550,#59551,#59552,#59553,#59554,
#59555,#59556,#59557,#59558,#59559,#59560,#59561,#59562,#59563,#59564,#59565,
#59566,#59567,#59568,#59569,#59570,#59571,#59572,#59573,#59574,#59575,#59576,
#59577,#59578,#59579,#59580,#59581,#59582,#59583,#59584,#59585,#59586,#59587,
#59588,#59589,#59590,#59591,#59592,#59593,#59594,#59595,#59596,#59597,#59598,
#59599,#59600,#59601,#59602,#59603,#59604,#59605,#59606,#59607,#59608,#59609,
#59610,#59611,#59612,#59613,#59614,#59615,#59616,#59617,#59618,#59619,#59620,
#59621,#59622,#59623,#59624,#59625,#59626,#59627,#59628,#59629,#59630,#59631,
#59632,#59633,#59634,#59635,#59636,#59637,#59638,#59639,#59640,#59641,#59642,
#59643,#59644,#59645,#59646,#59647,#59648,#59649,#59650,#59651,#59652,#59653,
#59654,#59655,#59656,#59657,#59658,#59659,#59660,#59661,#59662,#59663,#59664,
#59665,#59666,#59667,#59668,#59669,#59670,#59671,#59672,#59673,#59674,#59675,
#59676,#59677,#59678,#59679,#59680,#59681,#59682,#59683,#59684,#59685,#59686,
#59687,#59688,#59689,#59690,#59691,#59692,#59693,#59694,#59695,#59696,#59697,
#59698,#59699,#59700,#59701,#59702,#59703,#59704,#59705,#59706,#59707,#59708,
#59709),.UNSPECIFIED.,.F.,.F.,(4,3,3,3,3,3,3,3,3,3,3,3,3,3,3,3,3,3,3,3,
3,3,3,3,3,3,3,3,3,3,3,3,3,3,3,3,3,3,3,3,3,3,3,3,3,3,3,3,3,3,3,3,3,3,3,3,
3,3,3,3,3,3,3,3,3,3,3,3,3,3,3,3,3,3,3,3,3,3,3,3,3,3,3,3,3,3,3,3,3,3,3,3,
3,3,3,3,3,3,3,3,3,3,3,3,3,3,3,3,3,3,3,3,3,3,3,3,3,3,3,3,3,3,3,3,3,3,3,3,
3,3,3,3,3,3,3,3,3,3,3,3,3,3,3,3,3,3,3,3,3,3,3,3,3,3,3,3,3,3,3,3,3,3,3,3,
3,3,3,3,3,3,3,3,3,3,3,3,3,3,3,3,3,3,3,3,3,3,3,3,3,3,3,3,3,3,3,3,3,3,3,3,
3,3,3,3,3,3,3,3,3,3,3,3,3,3,3,3,3,3,3,3,3,3,3,3,3,3,3,3,3,3,3,3,3,3,3,3,
3,3,3,3,3,3,3,3,3,3,3,3,3,3,3,3,3,3,3,3,3,3,3,3,3,3,3,3,3,3,3,3,3,3,3,3,
3,3,3,3,3,3,3,3,3,3,3,3,3,3,3,3,3,3,3,3,3,3,3,3,3,3,3,3,3,3,3,3,3,3,4),
(0.747382054616714,0.747723038678491,0.748202269571123,0.74844883371857,
0.749008302929647,0.74916671941293,0.749528589991814,0.749579915917099,
0.749580010757179,0.749880419804752,0.749935683138351,0.750396885757279,
0.750520960225312,0.75097500210156,0.751115880591238,0.751531129716683,
0.751697873792483,0.751778842328894,0.751778885415099,0.752087027424461,
0.752147527493318,0.752710384626379,0.753252218158787,0.753689424921576,
0.753804640846901,0.753977760073019,0.753977856839936,0.75408108747541,
0.754272811119852,0.754357333043548,0.754699169061808,0.754867244488106,
0.755166403756855,0.755388891802379,0.755692376950258,0.755909909618255,
0.756176186880368,0.756261221312009,0.756625573646643,0.756670821449427,
0.757100721728996,0.757171848282764,0.757450691416385,0.757672875116101,
0.757944696329765,0.758168389129736,0.758375313153121,0.758467352615369,
0.758844930392626,0.75910288258438,0.75938033151878,0.759819370162283,0.76010368649377,
0.760574112800631,0.76099205141762,0.761293258545597,0.76140999003461,0.761739345794588,
0.761825011746506,0.762318635961665,0.762654832237045,0.762773128011837,
0.762773258704699,0.763163612286573,0.763304930448033,0.763483618470429,
0.764019382630583,0.764311891898089,0.764764186400357,0.764840655750405,
0.764972023353423,0.764972133362619,0.765142182321038,0.765487971287168,
0.765709927374939,0.765971621054858,0.766552642238766,0.766799771284327,
0.767193837514219,0.767372463085503,0.767628716700242,0.767903900615377,
0.767903966239845,0.768353405009465,0.768650907782731,0.769033201735314,
0.769287361593117,0.769369882678459,0.769369920962504,0.769785302193162,
0.770039179151212,0.770462476011809,0.770785965982225,0.770835773634281,
0.770835799117072,0.770945912131936,0.771342306762054,0.771486999743917,
0.771901330964326,0.772044984188627,0.772475802820194,0.772602228832398,
0.772942395894644,0.773184930413349,0.773514816942057,0.773725206909473,
0.773767558086762,0.773767631994299,0.774186188963178,0.774262105726299,
0.77477864263865,0.775301458601153,0.775816670237033,0.775919541898361,
0.776309266557836,0.776546231145194,0.776698991217311,0.776775534823269,
0.777138450090972,0.777205482842393,0.77753215344153,0.777582747727868,
0.777957135771029,0.778093502396538,0.778608378739238,0.779030365986988,
0.779112889064764,0.779239979157345,0.779609566486991,0.779631140889186,
0.779631297748752,0.779956665100638,0.780169911509665,0.780531191103311,
0.780728103769669,0.780900663678196,0.781299942217719,0.781460567508864,
0.78185932742848,0.78201572572199,0.782391400280891,0.782563050622278,0.782563130625979,
0.782964008759921,0.783111640805055,0.78361561358035,0.783704798968149,
0.784208259868694,0.784305593985655,0.784761888807492,0.784762005283899,
0.785123582173051,0.785322296162653,0.78577830524352,0.785866123240921,
0.786338607216922,0.78641350159137,0.786825803734849,0.786960813347516,
0.786960879941819,0.787327998131616,0.787535326014198,0.788083399091502,
0.788138035729741,0.788681878089593,0.788742765766024,0.789159710924315,
0.789159754599739,0.789193388003017,0.789715694225066,0.789807334753473,
0.790429064212927,0.790851068948597,0.791262045509168,0.791358565392232,
0.791358629257659,0.791800808504292,0.791982707831161,0.79250987342608,
0.793019764643509,0.793133205933914,0.793557503915579,0.793557507375853,
0.794020865954325,0.794168625464213,0.794773937904032,0.794836761703345,
0.795403737480731,0.795500193464019,0.795756378573499,0.795756386599024,
0.795826979655061,0.796462092472985,0.797100232755515,0.79748544524889,
0.797914918373215,0.797955253231419,0.797955261888282,0.798421202840041,
0.79847889762451,0.798730652250557,0.79925557914175,0.799778777006595,0.800154127889339,
0.800154139653922,0.800752363184986,0.800804399518246,0.801407801642156,
0.801930308659008,0.802005444173409,0.802353002547259,0.802353022430264,
0.80246383986443,0.803061505625562,0.80366471129822,0.804123378741273,0.804538721293759,
0.804551877205179,0.804551905522224,0.805023654326599,0.805134139385097,
0.805694313921552,0.80572529726815,0.805783946796156,0.806371824062616,
0.806750751863099,0.806750779738102,0.807286825348273,0.807341143428747,
0.807444172866529,0.808032395395678,0.808066108539222,0.808646875573981,
0.808688305252117,0.808949626521019,0.808949630238794,0.809382225807286,
0.809519805753925,0.809932883978935,0.810452376293869,0.810505441540481,
0.81098571268166,0.811070464319094,0.811148395102808,0.811148501178939,
0.811176420276288,0.81160573932313,0.811739281771248,0.812301869196572,
0.812419820582741,0.81298439977347,0.813347341007746,0.813347375836859,
0.813716239417427,0.813813496249108,0.814284176332224,0.814666964667789,
0.814905184228181,0.815373273192269,0.815545897535462,0.815546250494779,
0.815978763041164,0.816250742584155,0.816924770873125,0.81696629174527,
0.817391265768666,0.817702097809648,0.817744729731671,0.817745125152699,
0.818193730523411,0.81825983321799,0.818633503933522,0.819145183541033,
0.819643237645425,0.819876160343907,0.819943925946354,0.819943999810619,
0.820417494266013,0.820767236993593,0.821122107885917,0.821700672166623,
0.82192438241048,0.822142874468539,0.822142942441421,0.822366378794246,
0.822812878269025,0.822988386454827,0.823375661000645,0.82343626103651,
0.823608790907153,0.823608958191491,0.823963851307888,0.824171091480278,
0.824582975191355,0.824746096576986,0.824858532840308,0.825273656933478,
0.825433414257374,0.825841003525415,0.825997545689005,0.826332597592095,
0.826540623784379,0.82654076757806,0.826870780522054,0.826944975091906,
0.827278644560235,0.82734781356787),.UNSPECIFIED.);
#803=B_SPLINE_CURVE_WITH_KNOTS('',3,(#59710,#59711,#59712,#59713,#59714,
#59715,#59716,#59717,#59718,#59719,#59720,#59721,#59722,#59723,#59724,#59725,
#59726,#59727,#59728,#59729,#59730,#59731,#59732,#59733,#59734,#59735,#59736,
#59737,#59738,#59739,#59740,#59741,#59742,#59743,#59744,#59745,#59746,#59747,
#59748,#59749,#59750,#59751,#59752,#59753,#59754,#59755,#59756,#59757,#59758,
#59759,#59760,#59761,#59762,#59763,#59764,#59765,#59766,#59767,#59768,#59769,
#59770,#59771,#59772,#59773,#59774,#59775,#59776,#59777,#59778,#59779,#59780,
#59781,#59782,#59783,#59784,#59785,#59786,#59787,#59788,#59789,#59790,#59791,
#59792,#59793,#59794,#59795,#59796,#59797,#59798,#59799,#59800,#59801,#59802,
#59803,#59804,#59805,#59806,#59807,#59808,#59809,#59810,#59811,#59812,#59813,
#59814,#59815,#59816,#59817,#59818,#59819,#59820,#59821,#59822,#59823,#59824,
#59825,#59826,#59827,#59828,#59829,#59830,#59831,#59832,#59833,#59834,#59835,
#59836,#59837,#59838,#59839,#59840,#59841,#59842,#59843,#59844,#59845,#59846,
#59847,#59848,#59849,#59850,#59851,#59852,#59853,#59854,#59855,#59856,#59857,
#59858,#59859,#59860,#59861,#59862,#59863,#59864,#59865,#59866,#59867,#59868,
#59869,#59870,#59871,#59872,#59873,#59874,#59875,#59876,#59877,#59878,#59879,
#59880,#59881,#59882,#59883,#59884,#59885,#59886,#59887,#59888,#59889,#59890,
#59891,#59892,#59893,#59894,#59895,#59896,#59897,#59898,#59899,#59900,#59901,
#59902,#59903,#59904,#59905,#59906,#59907,#59908,#59909,#59910,#59911,#59912,
#59913,#59914,#59915,#59916,#59917,#59918,#59919,#59920,#59921,#59922,#59923,
#59924,#59925,#59926,#59927,#59928,#59929,#59930,#59931,#59932,#59933,#59934,
#59935,#59936,#59937,#59938,#59939,#59940,#59941,#59942,#59943,#59944,#59945,
#59946,#59947,#59948,#59949,#59950,#59951,#59952,#59953,#59954,#59955,#59956,
#59957,#59958,#59959,#59960,#59961,#59962,#59963,#59964,#59965,#59966,#59967,
#59968,#59969,#59970,#59971,#59972,#59973,#59974,#59975,#59976,#59977,#59978,
#59979,#59980,#59981,#59982,#59983,#59984,#59985,#59986,#59987,#59988,#59989,
#59990,#59991,#59992,#59993,#59994,#59995,#59996,#59997,#59998,#59999,#60000,
#60001,#60002,#60003,#60004,#60005,#60006,#60007,#60008,#60009,#60010,#60011,
#60012,#60013,#60014,#60015,#60016,#60017,#60018,#60019,#60020,#60021,#60022,
#60023,#60024,#60025,#60026,#60027,#60028,#60029,#60030,#60031,#60032,#60033,
#60034,#60035,#60036,#60037,#60038,#60039,#60040,#60041,#60042,#60043,#60044,
#60045,#60046,#60047,#60048,#60049,#60050,#60051,#60052,#60053,#60054,#60055,
#60056,#60057,#60058,#60059,#60060,#60061,#60062,#60063,#60064,#60065,#60066,
#60067,#60068,#60069,#60070,#60071,#60072,#60073,#60074,#60075,#60076,#60077,
#60078,#60079,#60080,#60081,#60082,#60083,#60084,#60085,#60086,#60087,#60088,
#60089,#60090,#60091,#60092,#60093,#60094,#60095,#60096,#60097,#60098,#60099,
#60100,#60101,#60102,#60103,#60104,#60105,#60106,#60107,#60108,#60109,#60110,
#60111,#60112,#60113,#60114,#60115,#60116,#60117,#60118,#60119,#60120,#60121,
#60122,#60123,#60124,#60125,#60126,#60127,#60128,#60129,#60130,#60131,#60132,
#60133,#60134,#60135,#60136,#60137,#60138,#60139,#60140,#60141,#60142,#60143,
#60144,#60145,#60146,#60147,#60148,#60149,#60150,#60151,#60152,#60153,#60154,
#60155,#60156,#60157,#60158,#60159,#60160,#60161,#60162,#60163,#60164,#60165,
#60166,#60167,#60168,#60169,#60170,#60171,#60172,#60173,#60174,#60175,#60176,
#60177,#60178,#60179,#60180,#60181,#60182,#60183,#60184,#60185,#60186,#60187,
#60188,#60189,#60190,#60191,#60192,#60193,#60194,#60195,#60196,#60197,#60198,
#60199,#60200,#60201,#60202,#60203,#60204,#60205,#60206,#60207,#60208,#60209,
#60210,#60211,#60212,#60213,#60214,#60215,#60216,#60217,#60218,#60219,#60220,
#60221,#60222,#60223,#60224,#60225,#60226,#60227,#60228,#60229,#60230,#60231,
#60232,#60233,#60234,#60235,#60236,#60237,#60238,#60239,#60240,#60241,#60242,
#60243,#60244,#60245,#60246,#60247,#60248,#60249,#60250,#60251,#60252,#60253,
#60254,#60255,#60256,#60257,#60258,#60259,#60260,#60261,#60262,#60263,#60264,
#60265,#60266,#60267,#60268,#60269,#60270,#60271,#60272,#60273,#60274,#60275,
#60276,#60277,#60278,#60279,#60280,#60281,#60282,#60283,#60284,#60285,#60286,
#60287,#60288,#60289,#60290,#60291,#60292,#60293,#60294,#60295,#60296,#60297,
#60298,#60299,#60300,#60301,#60302,#60303,#60304,#60305,#60306,#60307,#60308,
#60309,#60310,#60311,#60312,#60313,#60314,#60315,#60316,#60317,#60318,#60319,
#60320,#60321,#60322,#60323,#60324,#60325,#60326,#60327,#60328,#60329,#60330,
#60331,#60332,#60333,#60334,#60335,#60336,#60337,#60338,#60339,#60340,#60341,
#60342,#60343,#60344,#60345,#60346,#60347,#60348,#60349,#60350,#60351,#60352,
#60353,#60354,#60355,#60356,#60357,#60358,#60359,#60360,#60361,#60362,#60363,
#60364,#60365,#60366,#60367,#60368,#60369,#60370,#60371,#60372,#60373,#60374,
#60375,#60376,#60377,#60378,#60379,#60380,#60381,#60382,#60383,#60384,#60385,
#60386,#60387,#60388,#60389,#60390,#60391,#60392,#60393,#60394,#60395,#60396,
#60397,#60398,#60399,#60400,#60401,#60402,#60403,#60404,#60405,#60406,#60407,
#60408,#60409,#60410,#60411,#60412,#60413,#60414,#60415,#60416,#60417,#60418,
#60419,#60420,#60421,#60422,#60423,#60424,#60425,#60426,#60427,#60428,#60429,
#60430,#60431,#60432,#60433,#60434,#60435,#60436,#60437,#60438,#60439,#60440,
#60441,#60442,#60443,#60444,#60445,#60446,#60447,#60448,#60449,#60450,#60451,
#60452,#60453,#60454,#60455,#60456,#60457,#60458,#60459,#60460,#60461,#60462,
#60463,#60464,#60465,#60466,#60467,#60468,#60469,#60470,#60471,#60472,#60473,
#60474,#60475,#60476,#60477,#60478,#60479,#60480,#60481,#60482,#60483,#60484,
#60485,#60486,#60487,#60488,#60489,#60490,#60491,#60492,#60493,#60494,#60495,
#60496,#60497,#60498,#60499,#60500,#60501,#60502,#60503,#60504,#60505,#60506,
#60507,#60508,#60509,#60510,#60511,#60512,#60513,#60514,#60515,#60516,#60517,
#60518,#60519,#60520,#60521,#60522,#60523,#60524,#60525,#60526,#60527,#60528,
#60529,#60530,#60531,#60532,#60533,#60534,#60535,#60536,#60537,#60538,#60539,
#60540,#60541,#60542,#60543,#60544,#60545,#60546,#60547,#60548,#60549,#60550,
#60551,#60552,#60553,#60554,#60555,#60556,#60557,#60558,#60559,#60560,#60561,
#60562,#60563,#60564,#60565,#60566,#60567,#60568,#60569,#60570,#60571,#60572,
#60573,#60574,#60575,#60576,#60577,#60578,#60579,#60580,#60581,#60582,#60583,
#60584,#60585,#60586,#60587,#60588,#60589,#60590,#60591,#60592,#60593,#60594,
#60595,#60596,#60597,#60598,#60599,#60600,#60601,#60602,#60603,#60604,#60605,
#60606,#60607,#60608,#60609,#60610,#60611,#60612,#60613,#60614,#60615,#60616,
#60617,#60618,#60619),.UNSPECIFIED.,.F.,.F.,(4,3,3,3,3,3,3,3,3,3,3,3,3,
3,3,3,3,3,3,3,3,3,3,3,3,3,3,3,3,3,3,3,3,3,3,3,3,3,3,3,3,3,3,3,3,3,3,3,3,
3,3,3,3,3,3,3,3,3,3,3,3,3,3,3,3,3,3,3,3,3,3,3,3,3,3,3,3,3,3,3,3,3,3,3,3,
3,3,3,3,3,3,3,3,3,3,3,3,3,3,3,3,3,3,3,3,3,3,3,3,3,3,3,3,3,3,3,3,3,3,3,3,
3,3,3,3,3,3,3,3,3,3,3,3,3,3,3,3,3,3,3,3,3,3,3,3,3,3,3,3,3,3,3,3,3,3,3,3,
3,3,3,3,3,3,3,3,3,3,3,3,3,3,3,3,3,3,3,3,3,3,3,3,3,3,3,3,3,3,3,3,3,3,3,3,
3,3,3,3,3,3,3,3,3,3,3,3,3,3,3,3,3,3,3,3,3,3,3,3,3,3,3,3,3,3,3,3,3,3,3,3,
3,3,3,3,3,3,3,3,3,3,3,3,3,3,3,3,3,3,3,3,3,3,3,3,3,3,3,3,3,3,3,3,3,3,3,3,
3,3,3,3,3,3,3,3,3,3,3,3,3,3,3,3,3,3,3,3,3,3,3,3,3,3,3,3,3,3,3,3,3,3,3,3,
3,3,4),(0.790214816153757,0.790569912932159,0.790786698957973,0.791139692395635,
0.791358581762188,0.791675459555256,0.791914515211802,0.792057822178675,
0.792057831484434,0.792493279308416,0.792711744571504,0.79311285344863,
0.793385243105577,0.793557244181597,0.793854927123416,0.793901305088964,
0.79390138484995,0.794490247500423,0.794524685966545,0.795060349260568,
0.795150689706796,0.795641447294025,0.795744778693493,0.795744902796468,
0.795756264150162,0.796253752507393,0.796565617446721,0.797070681716938,
0.797443362301572,0.797588252298022,0.79758829497373,0.79788503399331,0.797955223872942,
0.798366962195766,0.798548980017166,0.798940476557062,0.799145711584124,
0.799431658291204,0.799431725902551,0.799770230437916,0.800108734973281,
0.800153888614457,0.800353462704815,0.800353573020671,0.800700609162085,
0.801047645303499,0.801275072152928,0.801275199507079,0.801678092781813,
0.80186073652046,0.802207367685839,0.802352732650851,0.802679702991785,
0.802942094934437,0.803118617066971,0.803118673111608,0.803618695631444,
0.803723128122228,0.804120769610145,0.804328625876611,0.80455071990004,
0.804847805473215,0.804962076432187,0.804962146716138,0.805392011572228,
0.805581733389879,0.805988419180543,0.806211517645016,0.806626052872013,
0.806748520090158,0.80706517708908,0.807381834088002,0.807420098105313,
0.807420111522176,0.807774893845597,0.807948018092396,0.808318558284417,
0.808483891046771,0.808864968822568,0.808946153705399,0.809247906925796,
0.809484508039827,0.809774604717984,0.809877765126567,0.809878076328215,
0.810266399909876,0.810438745953138,0.81074548755304,0.811012264872445,
0.811146230491986,0.811486022599776,0.81174113581312,0.812102974217444,
0.812335704768818,0.812336041134254,0.812757787169612,0.812857948877311,
0.813194767928685,0.813345555347721,0.813669091587204,0.813869928052145,
0.814179233637975,0.814325893075373,0.814823251814232,0.815033743755928,
0.815409658391976,0.815545654013101,0.816022780873877,0.816022988343312,
0.816535817934084,0.81691305656922,0.817477046607752,0.81783420511667,0.817866343878736,
0.818061061817964,0.818890304486143,0.818992814305639,0.819544058180871,
0.819709890213367,0.81970993555237,0.819946773129324,0.820391044797367,
0.820631575017876,0.820631672354634,0.821265185675308,0.821553281414016,
0.821553409156899,0.82195500201065,0.822144691572379,0.822475145959163,
0.822475375562885,0.822958579423763,0.823396882761428,0.823397330385553,
0.823611558691224,0.824050027286603,0.824127670438347,0.824541261726617,
0.824649041718287,0.825040793236437,0.82516444291762,0.825240146990458,
0.825240356365957,0.825643669093472,0.825750536801151,0.826218237406702,
0.826260652935695,0.826538839416065,0.826978888682608,0.827049298085276,
0.827083829970486,0.827084172483868,0.827584387071297,0.82809359697854,
0.828312812373505,0.828312815339727,0.828739235283743,0.829278570140441,
0.829374073879451,0.83002507227085,0.830539632263667,0.830671852698409,
0.830770767118543,0.830770777179544,0.830936805196092,0.831604426167356,
0.832267657031647,0.832614250784073,0.832614297691869,0.833134202083226,
0.833659647271449,0.833687434251001,0.834131164567614,0.834233805815265,
0.834457531345718,0.834571947612787,0.834929967250832,0.835272505355427,
0.83555815407035,0.83587651695162,0.836300990365938,0.836417647858886,0.836814204529502,
0.837212975469315,0.837529335421427,0.837841610906211,0.838103107461859,
0.838144473241817,0.838634835439669,0.839248721546978,0.839373472293171,
0.839703219006991,0.839737659885107,0.840270122220773,0.840378982536802,
0.841020766527459,0.841530821308701,0.841650107719815,0.84183154700295,
0.841831618806718,0.841937257470971,0.842504843189513,0.842753326810742,
0.842753355608982,0.843249236999302,0.843517750503382,0.843675117075162,
0.844012011750895,0.844327955724285,0.844677187878075,0.845140805062117,
0.8452153479961,0.845518485467049,0.845518566015776,0.845885120201988,0.846287553509617,
0.846440258754865,0.846758168216791,0.847065903222691,0.847362035674858,
0.847362039620305,0.847779647091993,0.848207802813831,0.848634701462988,
0.849055960793595,0.849205430527273,0.849351336210306,0.849675297785354,
0.849999259360402,0.850443911663908,0.850825142152362,0.850893126352701,
0.851048970462266,0.851048986829363,0.851448702552374,0.851852092648127,
0.852255655565265,0.852655855305455,0.852892365677593,0.853001820079873,
0.853440069578575,0.853759624066998,0.854289093810722,0.854649662780378,
0.854735833886438,0.855090996185286,0.855449762088454,0.855809942981132,
0.856211176172309,0.856488002469863,0.856579317156367,0.856740923477002,
0.857097483084965,0.857448573969311,0.857808311033977,0.85823331905572,
0.858925246424692,0.859037302113415,0.859400435455285,0.85965177878236,
0.859651863650498,0.860188619633516,0.860266343442275,0.860266354852008,
0.860880846053518,0.861453580045515,0.861495306845753,0.861495337255027,
0.861720726503584,0.862176216652237,0.862304564574268,0.862724319658047,
0.86272439754642,0.863110086730732,0.863338810859556,0.863338850477214,
0.863795598860009,0.86392008869005,0.863953302061066,0.86395332216636,0.864523981256641,
0.864759302376409,0.865531958560339,0.866119118894912,0.866411266867105,
0.866411347434597,0.866816667763681,0.866925804754119,0.867318486347646,
0.867447810671785,0.867963858198031,0.868277772104125,0.868317527056099,
0.86861873835963,0.868835480088362,0.868869231673143,0.868869394883433,
0.869238287384484,0.869362882010857,0.869673090830737,0.869862242626579,
0.870305722055053,0.870366513820095,0.870517391042945),.UNSPECIFIED.);
#804=B_SPLINE_CURVE_WITH_KNOTS('',3,(#60952,#60953,#60954,#60955,#60956,
#60957,#60958,#60959,#60960,#60961,#60962,#60963,#60964,#60965,#60966,#60967,
#60968,#60969,#60970,#60971,#60972,#60973,#60974,#60975,#60976,#60977,#60978,
#60979,#60980,#60981,#60982,#60983,#60984,#60985,#60986,#60987,#60988,#60989,
#60990,#60991,#60992,#60993,#60994,#60995,#60996,#60997,#60998,#60999,#61000,
#61001,#61002,#61003,#61004,#61005,#61006,#61007,#61008,#61009,#61010,#61011,
#61012,#61013,#61014,#61015,#61016,#61017,#61018,#61019,#61020,#61021,#61022,
#61023,#61024,#61025,#61026,#61027,#61028,#61029,#61030,#61031,#61032,#61033,
#61034,#61035,#61036,#61037,#61038,#61039,#61040,#61041,#61042,#61043,#61044,
#61045,#61046,#61047,#61048,#61049,#61050,#61051,#61052,#61053,#61054,#61055,
#61056,#61057,#61058,#61059,#61060,#61061,#61062,#61063,#61064,#61065,#61066,
#61067,#61068,#61069,#61070,#61071,#61072,#61073,#61074,#61075,#61076,#61077,
#61078,#61079,#61080,#61081,#61082,#61083,#61084,#61085,#61086,#61087,#61088,
#61089,#61090,#61091,#61092,#61093,#61094,#61095,#61096,#61097,#61098,#61099,
#61100,#61101,#61102,#61103,#61104,#61105,#61106,#61107,#61108,#61109,#61110,
#61111,#61112,#61113,#61114,#61115,#61116,#61117,#61118,#61119,#61120,#61121,
#61122,#61123,#61124,#61125,#61126,#61127,#61128,#61129,#61130,#61131,#61132,
#61133,#61134,#61135,#61136,#61137,#61138,#61139,#61140,#61141,#61142,#61143,
#61144,#61145,#61146,#61147,#61148,#61149,#61150,#61151,#61152,#61153,#61154,
#61155,#61156,#61157,#61158,#61159,#61160,#61161,#61162,#61163,#61164,#61165,
#61166,#61167,#61168,#61169,#61170,#61171,#61172,#61173,#61174,#61175,#61176,
#61177,#61178,#61179,#61180,#61181,#61182,#61183,#61184,#61185,#61186,#61187,
#61188,#61189,#61190,#61191,#61192,#61193,#61194,#61195,#61196,#61197,#61198,
#61199,#61200,#61201,#61202,#61203,#61204,#61205,#61206,#61207,#61208,#61209,
#61210,#61211,#61212,#61213,#61214,#61215,#61216,#61217,#61218,#61219,#61220,
#61221,#61222,#61223,#61224,#61225,#61226,#61227,#61228,#61229,#61230,#61231,
#61232,#61233,#61234,#61235,#61236,#61237,#61238,#61239,#61240,#61241,#61242,
#61243,#61244,#61245,#61246,#61247,#61248,#61249,#61250,#61251,#61252,#61253,
#61254,#61255,#61256,#61257,#61258,#61259,#61260,#61261,#61262,#61263,#61264,
#61265,#61266,#61267,#61268,#61269,#61270,#61271,#61272,#61273,#61274,#61275,
#61276,#61277,#61278,#61279,#61280,#61281,#61282,#61283,#61284,#61285,#61286,
#61287,#61288,#61289,#61290,#61291,#61292,#61293,#61294,#61295,#61296,#61297,
#61298,#61299,#61300,#61301,#61302,#61303,#61304,#61305,#61306,#61307,#61308,
#61309,#61310,#61311,#61312,#61313,#61314,#61315,#61316,#61317,#61318,#61319,
#61320,#61321,#61322,#61323,#61324,#61325,#61326,#61327,#61328,#61329,#61330,
#61331,#61332,#61333,#61334,#61335,#61336,#61337,#61338,#61339,#61340,#61341,
#61342,#61343,#61344,#61345,#61346,#61347,#61348,#61349,#61350,#61351,#61352,
#61353,#61354,#61355,#61356,#61357,#61358,#61359,#61360,#61361,#61362,#61363,
#61364,#61365,#61366,#61367,#61368,#61369,#61370,#61371,#61372,#61373,#61374,
#61375,#61376,#61377,#61378,#61379,#61380,#61381,#61382,#61383,#61384,#61385,
#61386,#61387,#61388,#61389,#61390,#61391,#61392,#61393,#61394,#61395,#61396,
#61397,#61398,#61399,#61400,#61401,#61402,#61403,#61404,#61405,#61406,#61407,
#61408,#61409,#61410,#61411,#61412,#61413,#61414,#61415,#61416,#61417,#61418,
#61419,#61420,#61421,#61422,#61423,#61424,#61425,#61426,#61427,#61428,#61429,
#61430,#61431,#61432,#61433,#61434,#61435,#61436,#61437,#61438,#61439,#61440,
#61441,#61442,#61443,#61444,#61445,#61446,#61447,#61448,#61449,#61450,#61451,
#61452,#61453,#61454,#61455,#61456,#61457,#61458,#61459,#61460,#61461,#61462,
#61463,#61464,#61465,#61466,#61467,#61468,#61469,#61470,#61471,#61472,#61473,
#61474,#61475,#61476,#61477,#61478,#61479,#61480,#61481,#61482,#61483,#61484,
#61485,#61486,#61487,#61488,#61489,#61490,#61491,#61492,#61493,#61494,#61495,
#61496,#61497,#61498,#61499,#61500,#61501,#61502,#61503,#61504,#61505,#61506,
#61507,#61508,#61509,#61510,#61511,#61512,#61513,#61514,#61515,#61516,#61517,
#61518,#61519,#61520,#61521,#61522,#61523,#61524,#61525,#61526,#61527,#61528,
#61529,#61530,#61531,#61532,#61533,#61534,#61535,#61536,#61537,#61538,#61539,
#61540,#61541,#61542,#61543,#61544,#61545,#61546,#61547,#61548,#61549,#61550,
#61551,#61552,#61553,#61554,#61555,#61556,#61557,#61558,#61559,#61560,#61561,
#61562,#61563,#61564,#61565,#61566,#61567,#61568,#61569,#61570,#61571,#61572,
#61573,#61574,#61575,#61576,#61577,#61578,#61579,#61580,#61581,#61582,#61583,
#61584,#61585,#61586,#61587,#61588,#61589,#61590,#61591,#61592,#61593,#61594,
#61595,#61596,#61597,#61598,#61599,#61600,#61601,#61602,#61603,#61604,#61605,
#61606,#61607,#61608,#61609,#61610,#61611,#61612,#61613,#61614,#61615,#61616,
#61617,#61618,#61619,#61620,#61621,#61622,#61623,#61624,#61625,#61626,#61627,
#61628,#61629,#61630,#61631,#61632,#61633,#61634,#61635,#61636,#61637,#61638,
#61639,#61640,#61641,#61642,#61643,#61644,#61645,#61646,#61647,#61648,#61649,
#61650,#61651,#61652,#61653,#61654,#61655,#61656,#61657,#61658,#61659,#61660,
#61661,#61662,#61663,#61664,#61665,#61666,#61667,#61668,#61669,#61670,#61671,
#61672,#61673,#61674,#61675,#61676,#61677,#61678,#61679,#61680,#61681,#61682,
#61683,#61684,#61685,#61686,#61687,#61688,#61689,#61690,#61691,#61692,#61693,
#61694,#61695,#61696,#61697,#61698,#61699,#61700,#61701,#61702,#61703,#61704,
#61705,#61706,#61707,#61708,#61709,#61710,#61711,#61712,#61713,#61714,#61715,
#61716,#61717,#61718,#61719,#61720,#61721,#61722,#61723,#61724,#61725,#61726,
#61727,#61728,#61729,#61730,#61731,#61732,#61733,#61734,#61735,#61736,#61737,
#61738,#61739,#61740,#61741,#61742,#61743,#61744,#61745,#61746,#61747,#61748,
#61749,#61750,#61751,#61752,#61753,#61754,#61755,#61756,#61757,#61758,#61759,
#61760,#61761,#61762,#61763,#61764,#61765,#61766,#61767,#61768,#61769,#61770,
#61771,#61772,#61773,#61774,#61775,#61776,#61777,#61778,#61779,#61780,#61781,
#61782,#61783,#61784,#61785,#61786,#61787,#61788,#61789,#61790,#61791,#61792,
#61793,#61794,#61795,#61796,#61797,#61798,#61799,#61800,#61801,#61802,#61803,
#61804,#61805,#61806,#61807,#61808,#61809,#61810,#61811,#61812,#61813,#61814,
#61815,#61816,#61817,#61818,#61819,#61820,#61821,#61822,#61823,#61824,#61825,
#61826,#61827,#61828,#61829,#61830,#61831,#61832,#61833,#61834,#61835,#61836,
#61837,#61838,#61839,#61840,#61841,#61842,#61843,#61844,#61845,#61846,#61847,
#61848,#61849),.UNSPECIFIED.,.F.,.F.,(4,3,3,3,3,3,3,3,3,3,3,3,3,3,3,3,3,
3,3,3,3,3,3,3,3,3,3,3,3,3,3,3,3,3,3,3,3,3,3,3,3,3,3,3,3,3,3,3,3,3,3,3,3,
3,3,3,3,3,3,3,3,3,3,3,3,3,3,3,3,3,3,3,3,3,3,3,3,3,3,3,3,3,3,3,3,3,3,3,3,
3,3,3,3,3,3,3,3,3,3,3,3,3,3,3,3,3,3,3,3,3,3,3,3,3,3,3,3,3,3,3,3,3,3,3,3,
3,3,3,3,3,3,3,3,3,3,3,3,3,3,3,3,3,3,3,3,3,3,3,3,3,3,3,3,3,3,3,3,3,3,3,3,
3,3,3,3,3,3,3,3,3,3,3,3,3,3,3,3,3,3,3,3,3,3,3,3,3,3,3,3,3,3,3,3,3,3,3,3,
3,3,3,3,3,3,3,3,3,3,3,3,3,3,3,3,3,3,3,3,3,3,3,3,3,3,3,3,3,3,3,3,3,3,3,3,
3,3,3,3,3,3,3,3,3,3,3,3,3,3,3,3,3,3,3,3,3,3,3,3,3,3,3,3,3,3,3,3,3,3,3,3,
3,3,3,3,3,3,3,3,3,3,3,3,3,3,3,3,3,3,3,3,3,3,3,3,3,3,3,3,3,3,4),(0.0145921063417177,
0.01494498896954,0.0151414343792162,0.0155991031283622,0.0157494739476449,
0.0161489199803882,0.0163480559569645,0.0167526091727277,0.0169360751976015,
0.0170193973464053,0.0170194368213593,0.017368557965186,0.017521980587612,
0.0179163174749734,0.0179994507332042,0.0184148530732642,0.0185039806404691,
0.018857211607717,0.0190058494900324,0.0193876186564051,0.0195077183395957,
0.0195079706482738,0.0198311533711606,0.0200317596461261,0.0202503103719008,
0.020712687016784,0.020773069117367,0.0212500144542332,0.0213012015559477,
0.0216870599385147,0.0218178729007355,0.0219407406253231,0.0219963072985394,
0.0223875675982871,0.0225295413822536,0.0229607422921723,0.0230774597141039,
0.0235737137924015,0.0236252067105452,0.0240275589477095,0.0241724863409542,
0.0243476689468201,0.0244638276318662,0.0244848324667108,0.0248526753933804,
0.0250787991879157,0.0253146788360168,0.0258102135546507,0.0259168701165055,
0.0264598074834853,0.0267780626666368,0.0269730901210823,0.0272126543850709,
0.027774826839563,0.0283800367456755,0.0288868553501964,0.0291740997766178,
0.0293794134355193,0.0294613442030393,0.0298883423612777,0.0300672827309982,
0.0304989744969724,0.0306856802261637,0.0311692758229822,0.0312898616254177,
0.0315033199524961,0.0318474081826925,0.0319493233055476,0.0319495774493657,
0.0323241990368826,0.0325826602113226,0.0329349866443945,0.0332374621276672,
0.0336396831011873,0.0337542991621983,0.0340711733376522,0.0343871557854915,
0.0344375457644208,0.034437644298738,0.0348067288873789,0.035008487163829,
0.0353899966968821,0.0355880146777214,0.0359760061919466,0.036003201468871,
0.0363168331776758,0.0365865863245377,0.0366492531037856,0.0366494851815739,
0.0370321297719284,0.0372744054545636,0.0376680801317804,0.0379060310150702,
0.0382521170686287,0.0385643313210177,0.0388612363976579,0.0388613260644098,
0.0392468618100091,0.0394856493157112,0.0398823752779798,0.0401166952531944,
0.0405017407618004,0.0407874538545231,0.0410731669472457,0.041073373049391,
0.0415528364149162,0.0417234699352747,0.0422278153850288,0.0424833601809103,
0.0426585635414544,0.0427321608347829,0.0431787156631357,0.0435358814900289,
0.0439636463244554,0.0442190052732109,0.0443755165973623,0.0443914111588819,
0.0448061473436753,0.0450377385277743,0.0455100533378483,0.0457802046179519,
0.0459562287504106,0.0460503558980555,0.0464650013081703,0.0467517837969972,
0.0472406262110292,0.0475255561546537,0.0477089375385147,0.0482916049754539,
0.0483397610150859,0.0488078257374213,0.0489558236703124,0.0493674487514282,
0.0493675702578804,0.0495086767683798,0.0499464719641969,0.0503781450874696,
0.0508096397703441,0.0510264509200073,0.0510265016895091,0.0513688483338306,
0.0515522143160684,0.0517586266481565,0.0521261839347652,0.0522851145121985,
0.0526853315821342,0.0526854794191335,0.0531575822864484,0.0535147719131977,
0.0535147886692577,0.0539144371248942,0.0540086974632535,0.0543440632094634,
0.0543442122442611,0.0548980825124975,0.0552140451327165,0.0556956457278704,
0.0559524544057642,0.056002955937668,0.0561453754914953,0.0566384143871544,
0.0569984287008584,0.0573827363405339,0.0576444702300798,0.0576617948411024,
0.0578814588978127,0.058478447965699,0.0590684263941783,0.0592803287184296,
0.0593207428682015,0.0594278417913414,0.0598862183712118,0.059918983327099,
0.0603547928964372,0.0603900975280435,0.0605647804224837,0.0605650147272371,
0.0607571971489412,0.0609796303876242,0.0609797348927689,0.0613071045479967,
0.0613955167415226,0.0617853574226454,0.0618109415534416,0.0622251185198664,
0.0624322070030788,0.0625690933163434,0.0626392954862912,0.063034094394662,
0.0634288933030329,0.0637944392139662,0.063820776649469,0.0641301759876878,
0.0642973774473228,0.0642974962170227,0.064773979836535,0.0652629661483903,
0.0657532222072641,0.0658198274911648,0.0659563768791496,0.065956444076727,
0.0664746556612816,0.066998085538047,0.0675072939241088,0.0676152575412766,
0.0676153404644975,0.0680300808427615,0.0684448133482964,0.0689677513501084,
0.0692742443628509,0.0702037589037057,0.0708130175714309,0.0709331218184356,
0.0716612249019194,0.0723947655040235,0.0725750783176391,0.0725918995276573,
0.0725919649161931,0.0733628468827993,0.0741415931240865,0.0742507801897843,
0.074250855677326,0.0742633055451511,0.0748300972933925,0.0753995067141672,
0.0759096608519112,0.0759097695124051,0.0764048701624809,0.0765139566729015,
0.0770037536150007,0.0774264581899242,0.0774949581656026,0.0775685415140381,
0.0775685818723875,0.0780510140055978,0.0781653632510877,0.078681519696992,
0.0787272828532932,0.0787621849881373,0.0792274221761651,0.0792275499018148,
0.0797384782875757,0.0798711594614943,0.0804702982385853,0.080886302838292,
0.0808865897272711,0.0810111587464966,0.0814218995478847,0.0814565399643726,
0.0819050207731814,0.0823193328874672,0.082353789129362,0.0825450841594454,
0.0825451835004189,0.0829466330378264,0.0830276770380248,0.0835106162604698,
0.0839506252503161,0.0839828547202685,0.0842040641625458,0.084204455951171,
0.0843824864714303,0.0848283015634868,0.085081553804432,0.0854720404128058,
0.0857565544251839,0.0858626689985701,0.0858629448246728,0.0862409044962003,
0.0866229519670493,0.0870038229220728,0.0873761996372048,0.0875218254867997,
0.08752211742225,0.0877596849540256,0.0881665392263277,0.0882177692466477,
0.0886992376977871,0.089049265273922,0.0891534495533465,0.0891802236073339,
0.0891807061489266,0.0895954263144584,0.0900046203066122,0.0904221035588329,
0.0908395696551521,0.0908395868110536,0.0911367582134736,0.0917997669311156,
0.0918912333247692,0.0922890067306582,0.0924984225576922,0.0924984674731805,
0.0928255904719477,0.0933612307645322,0.0939025070602852,0.0941572866208839,
0.0941573481353074,0.0944913654294245,0.0945119390290117),.UNSPECIFIED.);
#805=B_SPLINE_CURVE_WITH_KNOTS('',3,(#62206,#62207,#62208,#62209,#62210,
#62211,#62212,#62213,#62214,#62215,#62216,#62217,#62218,#62219,#62220,#62221,
#62222,#62223,#62224,#62225,#62226,#62227,#62228,#62229,#62230,#62231,#62232,
#62233,#62234,#62235,#62236,#62237,#62238,#62239,#62240,#62241,#62242,#62243,
#62244,#62245,#62246,#62247,#62248,#62249,#62250,#62251,#62252,#62253,#62254,
#62255,#62256,#62257,#62258,#62259,#62260,#62261,#62262,#62263,#62264,#62265,
#62266,#62267,#62268,#62269,#62270,#62271,#62272,#62273,#62274,#62275,#62276,
#62277,#62278,#62279,#62280,#62281,#62282,#62283,#62284,#62285,#62286,#62287,
#62288,#62289,#62290,#62291,#62292,#62293,#62294,#62295,#62296,#62297,#62298,
#62299,#62300,#62301,#62302,#62303,#62304,#62305,#62306,#62307,#62308,#62309,
#62310,#62311,#62312,#62313,#62314,#62315,#62316,#62317,#62318,#62319,#62320,
#62321,#62322,#62323,#62324,#62325,#62326,#62327,#62328,#62329,#62330,#62331,
#62332,#62333,#62334,#62335,#62336,#62337,#62338,#62339,#62340,#62341,#62342,
#62343,#62344,#62345,#62346,#62347,#62348,#62349,#62350,#62351,#62352,#62353,
#62354,#62355,#62356,#62357,#62358,#62359,#62360,#62361,#62362,#62363,#62364,
#62365,#62366,#62367,#62368,#62369,#62370,#62371,#62372,#62373,#62374,#62375,
#62376,#62377,#62378,#62379,#62380,#62381,#62382,#62383,#62384,#62385,#62386,
#62387,#62388,#62389,#62390,#62391,#62392,#62393,#62394,#62395,#62396,#62397,
#62398,#62399,#62400,#62401,#62402,#62403,#62404,#62405,#62406,#62407,#62408,
#62409,#62410,#62411,#62412,#62413,#62414,#62415,#62416,#62417,#62418,#62419,
#62420,#62421,#62422,#62423,#62424,#62425,#62426,#62427,#62428,#62429,#62430,
#62431,#62432,#62433,#62434,#62435,#62436,#62437,#62438,#62439,#62440,#62441,
#62442,#62443,#62444,#62445,#62446,#62447,#62448,#62449,#62450,#62451,#62452,
#62453,#62454,#62455,#62456,#62457,#62458,#62459,#62460,#62461,#62462,#62463,
#62464,#62465,#62466,#62467,#62468,#62469,#62470,#62471,#62472,#62473,#62474,
#62475,#62476,#62477,#62478,#62479,#62480,#62481,#62482,#62483,#62484,#62485,
#62486,#62487,#62488,#62489,#62490,#62491,#62492,#62493,#62494,#62495,#62496,
#62497,#62498,#62499,#62500,#62501,#62502,#62503,#62504,#62505,#62506,#62507,
#62508,#62509,#62510,#62511,#62512,#62513,#62514,#62515,#62516,#62517,#62518,
#62519,#62520,#62521,#62522,#62523,#62524,#62525,#62526,#62527,#62528,#62529,
#62530,#62531,#62532,#62533,#62534,#62535,#62536,#62537,#62538,#62539,#62540,
#62541,#62542,#62543,#62544,#62545,#62546,#62547,#62548,#62549,#62550,#62551,
#62552,#62553,#62554,#62555,#62556,#62557,#62558,#62559,#62560,#62561,#62562,
#62563,#62564,#62565,#62566,#62567,#62568,#62569,#62570,#62571,#62572,#62573,
#62574,#62575,#62576,#62577,#62578,#62579,#62580,#62581,#62582,#62583,#62584,
#62585,#62586,#62587,#62588,#62589,#62590,#62591,#62592,#62593,#62594,#62595,
#62596,#62597,#62598,#62599,#62600,#62601,#62602,#62603,#62604,#62605,#62606,
#62607,#62608,#62609,#62610,#62611,#62612,#62613,#62614,#62615,#62616,#62617,
#62618,#62619,#62620,#62621,#62622,#62623,#62624,#62625,#62626,#62627,#62628,
#62629,#62630,#62631,#62632,#62633,#62634,#62635,#62636,#62637,#62638,#62639,
#62640,#62641,#62642,#62643,#62644,#62645,#62646,#62647,#62648,#62649,#62650,
#62651,#62652,#62653,#62654,#62655,#62656,#62657,#62658,#62659,#62660,#62661,
#62662,#62663,#62664,#62665,#62666,#62667,#62668,#62669,#62670,#62671,#62672,
#62673,#62674,#62675,#62676,#62677,#62678,#62679,#62680,#62681,#62682,#62683,
#62684,#62685,#62686,#62687,#62688,#62689,#62690,#62691,#62692,#62693,#62694,
#62695,#62696,#62697,#62698,#62699,#62700,#62701,#62702,#62703,#62704,#62705,
#62706,#62707,#62708,#62709,#62710,#62711,#62712,#62713,#62714,#62715,#62716,
#62717,#62718,#62719,#62720,#62721,#62722,#62723,#62724,#62725,#62726,#62727,
#62728,#62729,#62730,#62731,#62732,#62733,#62734,#62735,#62736,#62737,#62738,
#62739,#62740,#62741,#62742,#62743,#62744,#62745,#62746,#62747,#62748,#62749,
#62750,#62751,#62752,#62753,#62754,#62755,#62756,#62757,#62758,#62759,#62760,
#62761,#62762,#62763,#62764,#62765,#62766,#62767,#62768,#62769,#62770,#62771,
#62772,#62773,#62774,#62775,#62776,#62777,#62778,#62779,#62780,#62781,#62782,
#62783,#62784,#62785,#62786,#62787,#62788,#62789,#62790,#62791,#62792,#62793,
#62794,#62795,#62796,#62797,#62798,#62799,#62800,#62801,#62802,#62803,#62804,
#62805,#62806,#62807,#62808,#62809,#62810,#62811,#62812,#62813,#62814,#62815,
#62816,#62817,#62818,#62819,#62820,#62821,#62822,#62823,#62824,#62825,#62826,
#62827,#62828,#62829,#62830,#62831,#62832,#62833,#62834,#62835,#62836,#62837,
#62838,#62839,#62840,#62841,#62842,#62843,#62844,#62845,#62846,#62847,#62848,
#62849,#62850,#62851,#62852,#62853,#62854,#62855,#62856,#62857,#62858,#62859,
#62860,#62861,#62862,#62863,#62864,#62865,#62866,#62867,#62868,#62869,#62870,
#62871,#62872,#62873,#62874,#62875,#62876,#62877,#62878,#62879,#62880,#62881,
#62882,#62883,#62884,#62885,#62886,#62887,#62888,#62889,#62890,#62891,#62892,
#62893,#62894,#62895,#62896,#62897,#62898,#62899,#62900,#62901,#62902,#62903,
#62904,#62905,#62906,#62907,#62908,#62909,#62910,#62911,#62912,#62913,#62914,
#62915,#62916,#62917,#62918,#62919,#62920,#62921,#62922,#62923,#62924,#62925,
#62926,#62927,#62928,#62929,#62930,#62931,#62932,#62933,#62934,#62935,#62936,
#62937,#62938,#62939,#62940,#62941,#62942,#62943,#62944,#62945,#62946,#62947,
#62948,#62949,#62950,#62951,#62952,#62953,#62954,#62955,#62956,#62957,#62958,
#62959,#62960,#62961,#62962,#62963,#62964,#62965,#62966,#62967,#62968,#62969,
#62970,#62971,#62972,#62973,#62974,#62975,#62976,#62977,#62978,#62979,#62980,
#62981,#62982,#62983,#62984,#62985,#62986,#62987,#62988,#62989,#62990,#62991,
#62992,#62993,#62994,#62995,#62996,#62997,#62998,#62999,#63000,#63001,#63002,
#63003,#63004,#63005,#63006,#63007,#63008,#63009,#63010,#63011,#63012,#63013,
#63014,#63015,#63016,#63017,#63018,#63019,#63020,#63021,#63022,#63023,#63024,
#63025,#63026,#63027,#63028,#63029,#63030,#63031,#63032,#63033,#63034,#63035,
#63036,#63037,#63038,#63039,#63040,#63041,#63042,#63043,#63044,#63045,#63046,
#63047,#63048,#63049,#63050,#63051,#63052,#63053,#63054,#63055,#63056,#63057,
#63058,#63059,#63060,#63061,#63062,#63063,#63064,#63065,#63066,#63067,#63068,
#63069,#63070,#63071,#63072,#63073,#63074,#63075,#63076,#63077,#63078,#63079,
#63080,#63081,#63082,#63083,#63084,#63085,#63086,#63087,#63088,#63089,#63090,
#63091,#63092,#63093,#63094,#63095,#63096,#63097,#63098,#63099,#63100,#63101,
#63102,#63103,#63104,#63105,#63106,#63107,#63108,#63109,#63110,#63111,#63112,
#63113,#63114,#63115,#63116,#63117,#63118,#63119,#63120,#63121,#63122,#63123,
#63124,#63125,#63126,#63127,#63128,#63129,#63130,#63131,#63132,#63133,#63134,
#63135,#63136,#63137,#63138,#63139,#63140,#63141,#63142),.UNSPECIFIED.,
 .F.,.F.,(4,3,3,3,3,3,3,3,3,3,3,3,3,3,3,3,3,3,3,3,3,3,3,3,3,3,3,3,3,3,3,
3,3,3,3,3,3,3,3,3,3,3,3,3,3,3,3,3,3,3,3,3,3,3,3,3,3,3,3,3,3,3,3,3,3,3,3,
3,3,3,3,3,3,3,3,3,3,3,3,3,3,3,3,3,3,3,3,3,3,3,3,3,3,3,3,3,3,3,3,3,3,3,3,
3,3,3,3,3,3,3,3,3,3,3,3,3,3,3,3,3,3,3,3,3,3,3,3,3,3,3,3,3,3,3,3,3,3,3,3,
3,3,3,3,3,3,3,3,3,3,3,3,3,3,3,3,3,3,3,3,3,3,3,3,3,3,3,3,3,3,3,3,3,3,3,3,
3,3,3,3,3,3,3,3,3,3,3,3,3,3,3,3,3,3,3,3,3,3,3,3,3,3,3,3,3,3,3,3,3,3,3,3,
3,3,3,3,3,3,3,3,3,3,3,3,3,3,3,3,3,3,3,3,3,3,3,3,3,3,3,3,3,3,3,3,3,3,3,3,
3,3,3,3,3,3,3,3,3,3,3,3,3,3,3,3,3,3,3,3,3,3,3,3,3,3,3,3,3,3,3,3,3,3,3,3,
3,3,3,3,3,3,3,3,3,3,3,3,3,3,3,3,3,3,3,3,3,3,3,3,3,3,3,3,3,4),(0.182899145085017,
0.183263528687836,0.183473753205273,0.183684503249907,0.184233646645112,
0.18469728350229,0.184783016732281,0.185176818032187,0.185344322912941,
0.18538724782252,0.185387336016129,0.185747562346674,0.185883607088664,
0.186365622168009,0.186468694243726,0.186938533254263,0.187062418288696,
0.187554538554016,0.187640861312347,0.187803828183196,0.187875873458272,
0.188083107361859,0.188716731739939,0.189363513501688,0.189992344245774,
0.190283169440411,0.190363966683647,0.190364102474105,0.190819712278314,
0.191116111418507,0.191656164316416,0.191907597584301,0.192420613141666,
0.192484027826661,0.192793156576219,0.192852282017407,0.192852555815474,
0.193408651590982,0.193926082297544,0.194096439684286,0.194096625798643,
0.194422182597619,0.194581200875238,0.19468462481958,0.194991998383055,
0.195173242549772,0.195336831695984,0.195340844506715,0.195845155854362,
0.195982133749486,0.196359273198225,0.196434056879778,0.19658477886086,
0.196610731556704,0.19688598001007,0.197196240942322,0.197322767162915,
0.197762903007137,0.197828912684925,0.197829208096378,0.198203938783702,
0.19850964682361,0.198867073655538,0.19908576582645,0.199462431600692,0.199774653157635,
0.200140083916306,0.200185540730199,0.200317212902433,0.200317228018684,
0.200701854027722,0.200735557379781,0.201090409704972,0.201285041487425,
0.201561246657516,0.201561385685564,0.201997298267757,0.202087477562286,
0.202549150829979,0.202627626661227,0.202805543352443,0.202805554004613,
0.203136026419175,0.203308333327251,0.203484783426379,0.203844371890436,
0.203989257925437,0.204334977082562,0.204464326246553,0.204464420241616,
0.204833978453808,0.205097849331174,0.205473202780681,0.205683116128945,
0.206004866844681,0.206122912740792,0.206123297130789,0.206787047742686,
0.207389397027825,0.207468693245331,0.207781893952244,0.207782174019962,
0.207881695599617,0.208357870522842,0.20855089979797,0.209050016756459,
0.209230270269441,0.20944082211402,0.209441050909135,0.209756996578365,
0.209904380159533,0.210081414225744,0.210392327296829,0.210544641877459,
0.210838269106101,0.211013217833463,0.211100582903117,0.211565146641376,
0.2120098364277,0.212203496194613,0.212600241665112,0.212714780986435,0.212758685799301,
0.21275880468748,0.213015575233525,0.213387538030512,0.213581822153208,
0.213915939562133,0.21414409078994,0.214417681576653,0.214417912539699,
0.214725395351362,0.214873542956843,0.215246819780476,0.21524712002124,
0.215597339087354,0.215849135163016,0.21586842898292,0.215947558153467,
0.216075777605415,0.216076558465826,0.216467629524831,0.216632026988447,
0.217027887015844,0.217239456887018,0.217588561536885,0.217735435354999,
0.217735621855321,0.218071372391186,0.218236078391015,0.218586937030159,
0.218739189032184,0.218880083140786,0.219198193148187,0.219394098580177,
0.219394312244172,0.219908073787879,0.220430925972927,0.220946014987092,
0.221052933340913,0.221053189133344,0.221378486882475,0.221494608624949,
0.221811069574464,0.222146916265991,0.22226156779849,0.222585586794641,
0.222712066022517,0.223088482336287,0.223224545610072,0.223740289263314,
0.22423957732554,0.224370930705853,0.22437094291169,0.224689150297459,0.224746152019814,
0.225147743921987,0.225234858801252,0.225669314512927,0.225727231999456,
0.225920161194922,0.22603035389434,0.226742531591767,0.227135737726978,
0.227136062561739,0.227436404308476,0.227682241087317,0.228136327237122,
0.228279114908813,0.2287243324094,0.228876111457403,0.229149039882898,0.229347573579209,
0.22934769422317,0.229729127128221,0.229900532542266,0.229900575950594,
0.230319862058617,0.230453472410766,0.230453491505324,0.230616055486533,
0.230977299704976,0.23133732057681,0.231474494916104,0.231559769410146,
0.231944659340071,0.23205681445195,0.232418497812745,0.232547396014727,
0.233048212764105,0.233476881337157,0.233549029513483,0.233771167700448,
0.233771245283669,0.234237080556968,0.234725330117285,0.235213122506284,
0.235685032912032,0.2359830811359,0.235983129298908,0.236368180533942,0.236412945639474,
0.236485191592944,0.236907418779729,0.237336469114539,0.237641958025073,
0.237642030808215,0.238086117418035,0.238532563475558,0.238977264207995,
0.239300834914246,0.239300875336245,0.239415854171785,0.2399662531224,0.23999991490173,
0.24058693707282,0.240959711803418,0.240959742766705,0.241372003695055,
0.241874921163338,0.24237737025309,0.242618588692591,0.242618621288792,
0.243197964750271,0.24326742749683,0.243327117996986,0.243934756051637,
0.243969138825144,0.244277465581764,0.244277486659965,0.244304836536952,
0.24491620539582,0.245282427391075,0.245830524511867,0.245892515830428,
0.245936342470937,0.245936366376164,0.246382230731561,0.24721347027279,
0.247481706076934,0.24759521936011,0.247595273647355,0.248195322597542,
0.248795817345073,0.249254096249282,0.249254158720183,0.24968115631505,
0.250332658316406,0.250752796550357,0.250912973138455,0.250912991795234,
0.251372312400339,0.251411676272452,0.25187978233059,0.252375953614537,
0.252571840869658,0.252571850027628,0.253030524043992,0.253127602265603,
0.253688741088463,0.254079559629245,0.254230726916801,0.254230771577903,
0.254711318370289,0.25519441871275,0.255677046663041,0.255889552746644,
0.255889603805974,0.256279511385039,0.25677729203742,0.256834645518382,
0.257392271578631,0.2578412944297,0.257949164758202,0.258101395718981,0.258101439658204,
0.258479809094404,0.258980782226928,0.259040142400447,0.259604452734636,
0.260055790373525,0.260166297783907,0.260313243681732,0.260313275510435,
0.260679509571009,0.26120622208671,0.261290799359835,0.26190795536125,0.262358765504495,
0.262525048300564,0.262525111362665,0.262853849358093,0.262879005814513),
 .UNSPECIFIED.);
#806=B_SPLINE_CURVE_WITH_KNOTS('',3,(#63479,#63480,#63481,#63482,#63483,
#63484,#63485,#63486,#63487,#63488,#63489,#63490,#63491,#63492,#63493,#63494,
#63495,#63496,#63497,#63498,#63499,#63500,#63501,#63502,#63503,#63504,#63505,
#63506,#63507,#63508,#63509,#63510,#63511,#63512,#63513,#63514,#63515,#63516,
#63517,#63518,#63519,#63520,#63521,#63522,#63523,#63524,#63525,#63526,#63527,
#63528,#63529,#63530,#63531,#63532,#63533,#63534,#63535,#63536,#63537,#63538,
#63539,#63540,#63541,#63542,#63543,#63544,#63545,#63546,#63547,#63548,#63549,
#63550,#63551,#63552,#63553,#63554,#63555,#63556,#63557,#63558,#63559,#63560,
#63561,#63562,#63563,#63564,#63565,#63566,#63567,#63568,#63569,#63570,#63571,
#63572,#63573,#63574,#63575,#63576,#63577,#63578,#63579,#63580,#63581,#63582,
#63583,#63584,#63585,#63586,#63587,#63588,#63589,#63590,#63591,#63592,#63593,
#63594,#63595,#63596,#63597,#63598,#63599,#63600,#63601,#63602,#63603,#63604,
#63605,#63606,#63607,#63608,#63609,#63610,#63611,#63612,#63613,#63614,#63615,
#63616,#63617,#63618,#63619,#63620,#63621,#63622,#63623,#63624,#63625,#63626,
#63627,#63628,#63629,#63630,#63631,#63632,#63633,#63634,#63635,#63636,#63637,
#63638,#63639,#63640,#63641,#63642,#63643,#63644,#63645,#63646,#63647,#63648,
#63649,#63650,#63651,#63652,#63653,#63654,#63655,#63656,#63657,#63658,#63659,
#63660,#63661,#63662,#63663,#63664,#63665,#63666,#63667,#63668,#63669,#63670,
#63671,#63672,#63673,#63674,#63675,#63676,#63677,#63678,#63679,#63680,#63681,
#63682,#63683,#63684,#63685,#63686,#63687,#63688,#63689,#63690,#63691,#63692,
#63693,#63694,#63695,#63696,#63697,#63698,#63699,#63700,#63701,#63702,#63703,
#63704,#63705,#63706,#63707,#63708,#63709,#63710,#63711,#63712,#63713,#63714,
#63715,#63716,#63717,#63718,#63719,#63720,#63721,#63722,#63723,#63724,#63725,
#63726,#63727,#63728,#63729,#63730,#63731,#63732,#63733,#63734,#63735,#63736,
#63737,#63738,#63739,#63740,#63741,#63742,#63743,#63744,#63745,#63746,#63747,
#63748,#63749,#63750,#63751,#63752,#63753,#63754,#63755,#63756,#63757,#63758,
#63759,#63760,#63761,#63762,#63763,#63764,#63765,#63766,#63767,#63768,#63769,
#63770,#63771,#63772,#63773,#63774,#63775,#63776,#63777,#63778,#63779,#63780,
#63781,#63782,#63783,#63784,#63785,#63786,#63787,#63788,#63789,#63790,#63791,
#63792,#63793,#63794,#63795,#63796,#63797,#63798,#63799,#63800,#63801,#63802,
#63803,#63804,#63805,#63806,#63807,#63808,#63809,#63810,#63811,#63812,#63813,
#63814,#63815,#63816,#63817,#63818,#63819,#63820,#63821,#63822,#63823,#63824,
#63825,#63826,#63827,#63828,#63829,#63830,#63831,#63832,#63833,#63834,#63835,
#63836,#63837,#63838,#63839,#63840,#63841,#63842,#63843,#63844,#63845,#63846,
#63847,#63848,#63849,#63850,#63851,#63852,#63853,#63854,#63855,#63856,#63857,
#63858,#63859,#63860,#63861,#63862,#63863,#63864,#63865,#63866,#63867,#63868,
#63869,#63870,#63871,#63872,#63873,#63874,#63875,#63876,#63877,#63878,#63879,
#63880,#63881,#63882,#63883,#63884,#63885,#63886,#63887,#63888,#63889,#63890,
#63891,#63892,#63893,#63894,#63895,#63896,#63897,#63898,#63899,#63900,#63901,
#63902,#63903,#63904,#63905,#63906,#63907,#63908,#63909,#63910,#63911,#63912,
#63913,#63914,#63915,#63916,#63917,#63918,#63919,#63920,#63921,#63922,#63923,
#63924,#63925,#63926,#63927,#63928,#63929,#63930,#63931,#63932,#63933,#63934,
#63935,#63936,#63937,#63938,#63939,#63940,#63941,#63942,#63943,#63944,#63945,
#63946,#63947,#63948,#63949,#63950,#63951,#63952,#63953,#63954,#63955,#63956,
#63957,#63958,#63959,#63960,#63961,#63962,#63963,#63964,#63965,#63966,#63967,
#63968,#63969,#63970,#63971,#63972,#63973,#63974,#63975,#63976,#63977,#63978,
#63979,#63980,#63981,#63982,#63983,#63984,#63985,#63986,#63987,#63988,#63989,
#63990,#63991,#63992,#63993,#63994,#63995,#63996,#63997,#63998,#63999,#64000,
#64001,#64002,#64003,#64004,#64005,#64006,#64007,#64008,#64009,#64010,#64011,
#64012,#64013,#64014,#64015,#64016,#64017,#64018,#64019,#64020,#64021,#64022,
#64023,#64024,#64025,#64026,#64027,#64028,#64029,#64030,#64031,#64032,#64033,
#64034,#64035,#64036,#64037,#64038,#64039,#64040,#64041,#64042,#64043,#64044,
#64045,#64046,#64047,#64048,#64049,#64050,#64051,#64052,#64053,#64054,#64055),
 .UNSPECIFIED.,.F.,.F.,(4,3,3,3,3,3,3,3,3,3,3,3,3,3,3,3,3,3,3,3,3,3,3,3,
3,3,3,3,3,3,3,3,3,3,3,3,3,3,3,3,3,3,3,3,3,3,3,3,3,3,3,3,3,3,3,3,3,3,3,3,
3,3,3,3,3,3,3,3,3,3,3,3,3,3,3,3,3,3,3,3,3,3,3,3,3,3,3,3,3,3,3,3,3,3,3,3,
3,3,3,3,3,3,3,3,3,3,3,3,3,3,3,3,3,3,3,3,3,3,3,3,3,3,3,3,3,3,3,3,3,3,3,3,
3,3,3,3,3,3,3,3,3,3,3,3,3,3,3,3,3,3,3,3,3,3,3,3,3,3,3,3,3,3,3,3,3,3,3,3,
3,3,3,3,3,3,3,3,3,3,3,3,3,3,3,3,3,3,3,3,3,3,3,3,4),(0.351267156365414,0.351750391359728,
0.352053768574433,0.352534925272286,0.353021590178722,0.35349882735455,
0.353754974599999,0.35425310170779,0.354784707541866,0.355327216319465,
0.355864800511277,0.356243289735703,0.35645105803837,0.357343280142757,
0.358206061509809,0.358651247070275,0.358731604871407,0.359324925451463,
0.359931723984194,0.360527984817262,0.360850748009482,0.361219920007111,
0.361806003340944,0.362428787462243,0.363051571583543,0.363659465672652,
0.363708235142815,0.364198446345135,0.364681457285473,0.364952392710666,
0.365253537864432,0.365725044071475,0.366196550278518,0.366758624783651,
0.367333348044981,0.367454340554546,0.36803001293294,0.368601585530452,
0.368684865414222,0.36924531748377,0.369654410669678,0.369929022982074,
0.370461401312978,0.371012766981758,0.371173180549926,0.371682892872077,
0.37185357714997,0.372365561697048,0.372832057307062,0.373475163656902,
0.37405258729195,0.374490934064198,0.375138184729189,0.3757916587624,0.376149810821334,
0.376251494518407,0.376800852830691,0.377350204648083,0.37780868757847,
0.378293420562503,0.378449369799278,0.378958467067442,0.379467564335606,
0.380028116995775,0.380577279044258,0.381126441092742,0.381382977762748,
0.381946259261549,0.382501112798003,0.382785317849878,0.383390635373774,
0.383975894741936,0.384315038402458,0.384444194607014,0.385016831019777,
0.385273632985582,0.385736697642693,0.38610307136415,0.386594706101067,
0.387084931607747,0.387249534242943,0.387734703639615,0.387761948121286,
0.388282278030875,0.388811554714553,0.389330608847941,0.389420824878422,
0.389861750321648,0.390181517755373,0.390630609695465,0.391079701635558,
0.391568863820643,0.392061173207715,0.392538953584999,0.392738578392693,
0.39311567715121,0.393567869297984,0.394020621172992,0.394397455149829,
0.394848055603842,0.395296854174968,0.395737074251576,0.396048735953485,
0.396056331906965,0.396496321886107,0.396935932582208,0.397371685468723,
0.397715208664101,0.398101041883674,0.398483464171324,0.398821126502192,
0.398982064711357,0.39933496660133,0.399686788844184,0.399927044340283,
0.400380681565484,0.400836075142965,0.401289973659049,0.401737212312914,
0.401916265365166,0.402138880016464,0.402645572315188,0.403166490416785,
0.403682641320516,0.404187093648233,0.404350715692645,0.404850487385546,
0.405362632432205,0.405877181689164,0.406009592449781,0.406315536957987,
0.407119550268592,0.407668469206917,0.407781616513089,0.40828507633214,
0.408806211148097,0.409327345964053,0.40973700362179,0.409981450776902,
0.410225887810325,0.410772422439078,0.410986222721189,0.411540821737823,
0.41169281377135,0.412247864394274,0.412645099478325,0.413172611534843,
0.413648463917508,0.41417165474335,0.414303976235461,0.414797132526775,
0.415133414614029,0.41552667033309,0.415849135458713,0.415962852992597,
0.416378061007014,0.416792291371165,0.417484374377118,0.417621729749733,
0.418049547352951,0.418497188898418,0.4189463751368,0.419280606506868,0.419776608752345,
0.420248109372826,0.420741112431842,0.420939483264004,0.421367394376181,
0.421797032915755,0.422227524743399,0.422447519620171,0.42259836002114,
0.42309112946944,0.423585109863308,0.424076779760356,0.424257236778276,
0.424647136307702,0.425151048627296,0.425657100548399,0.426163649110633,
0.426469072454458,0.426846990838846,0.42737415954416,0.427904473124376,
0.428435378236698,0.428680908130639,0.429046510090048,0.429582357542127,
0.430121732722553,0.430661132028704,0.43089274380682,0.431217811560911,
0.431246327079438),.UNSPECIFIED.);
#807=B_SPLINE_CURVE_WITH_KNOTS('',3,(#64400,#64401,#64402,#64403,#64404,
#64405,#64406,#64407,#64408,#64409,#64410,#64411,#64412,#64413,#64414,#64415,
#64416,#64417,#64418,#64419,#64420,#64421,#64422,#64423,#64424,#64425,#64426,
#64427,#64428,#64429,#64430,#64431,#64432,#64433,#64434,#64435,#64436,#64437,
#64438,#64439,#64440,#64441,#64442,#64443,#64444,#64445,#64446,#64447,#64448,
#64449,#64450,#64451,#64452,#64453,#64454,#64455,#64456,#64457,#64458,#64459,
#64460,#64461,#64462,#64463,#64464,#64465,#64466,#64467,#64468,#64469,#64470,
#64471,#64472,#64473,#64474,#64475,#64476,#64477,#64478,#64479,#64480,#64481,
#64482,#64483,#64484,#64485,#64486,#64487,#64488,#64489,#64490,#64491,#64492,
#64493,#64494,#64495,#64496,#64497,#64498,#64499,#64500,#64501,#64502,#64503,
#64504,#64505,#64506,#64507,#64508,#64509,#64510,#64511,#64512,#64513,#64514,
#64515,#64516,#64517,#64518,#64519,#64520,#64521,#64522,#64523,#64524,#64525,
#64526,#64527,#64528,#64529,#64530,#64531,#64532,#64533,#64534,#64535,#64536,
#64537,#64538,#64539,#64540,#64541,#64542,#64543,#64544,#64545,#64546,#64547,
#64548,#64549,#64550,#64551,#64552,#64553,#64554,#64555,#64556,#64557,#64558,
#64559,#64560,#64561,#64562,#64563,#64564,#64565,#64566,#64567,#64568,#64569,
#64570,#64571,#64572,#64573,#64574,#64575,#64576,#64577,#64578,#64579,#64580,
#64581,#64582,#64583,#64584,#64585,#64586,#64587,#64588,#64589,#64590,#64591,
#64592,#64593,#64594,#64595,#64596,#64597,#64598,#64599,#64600,#64601,#64602,
#64603,#64604,#64605,#64606,#64607,#64608,#64609,#64610,#64611,#64612,#64613,
#64614,#64615,#64616,#64617,#64618,#64619,#64620,#64621,#64622,#64623,#64624,
#64625,#64626,#64627,#64628,#64629,#64630,#64631,#64632,#64633,#64634,#64635,
#64636,#64637,#64638,#64639,#64640,#64641,#64642,#64643,#64644,#64645,#64646,
#64647,#64648,#64649,#64650,#64651,#64652,#64653,#64654,#64655,#64656,#64657,
#64658,#64659,#64660,#64661,#64662,#64663,#64664,#64665,#64666,#64667,#64668,
#64669,#64670,#64671,#64672,#64673,#64674,#64675,#64676,#64677,#64678,#64679,
#64680,#64681,#64682,#64683,#64684,#64685,#64686,#64687,#64688,#64689,#64690,
#64691,#64692,#64693,#64694,#64695,#64696,#64697,#64698,#64699,#64700,#64701,
#64702,#64703,#64704,#64705,#64706,#64707,#64708,#64709,#64710,#64711,#64712,
#64713,#64714,#64715,#64716,#64717,#64718,#64719,#64720,#64721,#64722,#64723,
#64724,#64725,#64726,#64727,#64728,#64729,#64730,#64731,#64732,#64733,#64734,
#64735,#64736,#64737,#64738,#64739,#64740,#64741,#64742,#64743,#64744,#64745,
#64746,#64747,#64748,#64749,#64750,#64751,#64752,#64753,#64754,#64755,#64756,
#64757,#64758,#64759,#64760,#64761,#64762,#64763,#64764,#64765,#64766,#64767,
#64768,#64769,#64770,#64771,#64772,#64773,#64774,#64775,#64776,#64777,#64778,
#64779,#64780,#64781,#64782,#64783,#64784,#64785,#64786,#64787,#64788,#64789,
#64790,#64791,#64792,#64793,#64794,#64795,#64796,#64797,#64798,#64799,#64800,
#64801,#64802,#64803,#64804,#64805,#64806,#64807,#64808,#64809,#64810,#64811,
#64812,#64813,#64814,#64815,#64816,#64817,#64818,#64819,#64820,#64821,#64822,
#64823,#64824,#64825,#64826,#64827,#64828,#64829,#64830,#64831,#64832,#64833,
#64834,#64835,#64836,#64837,#64838,#64839,#64840,#64841,#64842,#64843,#64844,
#64845,#64846,#64847,#64848,#64849,#64850,#64851,#64852,#64853,#64854,#64855,
#64856,#64857,#64858,#64859,#64860,#64861,#64862,#64863,#64864,#64865,#64866,
#64867,#64868,#64869,#64870,#64871,#64872,#64873,#64874,#64875,#64876,#64877,
#64878,#64879,#64880,#64881,#64882,#64883,#64884,#64885,#64886,#64887,#64888,
#64889,#64890,#64891,#64892,#64893,#64894,#64895,#64896,#64897,#64898,#64899,
#64900,#64901,#64902,#64903,#64904,#64905,#64906,#64907,#64908,#64909,#64910,
#64911,#64912,#64913,#64914,#64915,#64916,#64917,#64918,#64919,#64920,#64921,
#64922,#64923,#64924,#64925,#64926,#64927,#64928,#64929,#64930,#64931,#64932,
#64933,#64934,#64935,#64936,#64937,#64938,#64939,#64940,#64941,#64942,#64943,
#64944,#64945,#64946,#64947,#64948,#64949,#64950,#64951,#64952,#64953,#64954,
#64955,#64956,#64957,#64958,#64959,#64960,#64961,#64962,#64963,#64964,#64965,
#64966,#64967,#64968,#64969,#64970,#64971,#64972,#64973,#64974,#64975,#64976,
#64977,#64978,#64979,#64980,#64981,#64982,#64983,#64984,#64985,#64986,#64987,
#64988,#64989,#64990,#64991,#64992,#64993,#64994,#64995,#64996,#64997,#64998,
#64999,#65000,#65001,#65002,#65003,#65004,#65005,#65006,#65007,#65008,#65009,
#65010,#65011,#65012,#65013,#65014,#65015,#65016,#65017,#65018,#65019,#65020,
#65021,#65022,#65023,#65024,#65025,#65026,#65027,#65028,#65029,#65030,#65031,
#65032,#65033,#65034,#65035,#65036,#65037,#65038,#65039,#65040,#65041,#65042,
#65043,#65044,#65045,#65046,#65047,#65048,#65049,#65050,#65051,#65052,#65053,
#65054,#65055,#65056,#65057,#65058,#65059,#65060,#65061,#65062,#65063,#65064,
#65065,#65066,#65067,#65068,#65069,#65070,#65071,#65072,#65073,#65074,#65075,
#65076,#65077,#65078,#65079,#65080,#65081,#65082,#65083,#65084,#65085,#65086,
#65087,#65088,#65089,#65090,#65091,#65092,#65093,#65094,#65095,#65096,#65097,
#65098,#65099,#65100,#65101,#65102,#65103,#65104,#65105,#65106,#65107,#65108,
#65109,#65110,#65111,#65112,#65113,#65114,#65115,#65116,#65117,#65118,#65119,
#65120,#65121,#65122,#65123,#65124,#65125,#65126,#65127,#65128,#65129,#65130,
#65131,#65132,#65133,#65134,#65135,#65136,#65137,#65138,#65139,#65140,#65141,
#65142,#65143,#65144,#65145,#65146,#65147,#65148,#65149,#65150,#65151,#65152,
#65153,#65154,#65155,#65156,#65157,#65158,#65159,#65160,#65161,#65162,#65163,
#65164,#65165,#65166,#65167,#65168,#65169,#65170,#65171,#65172,#65173,#65174,
#65175,#65176,#65177,#65178,#65179,#65180,#65181,#65182,#65183,#65184,#65185,
#65186,#65187,#65188,#65189,#65190,#65191,#65192,#65193,#65194,#65195,#65196,
#65197,#65198,#65199,#65200,#65201,#65202,#65203,#65204,#65205,#65206,#65207,
#65208,#65209,#65210,#65211,#65212,#65213,#65214,#65215,#65216,#65217,#65218,
#65219,#65220,#65221,#65222,#65223,#65224,#65225,#65226,#65227,#65228,#65229,
#65230,#65231,#65232,#65233,#65234,#65235,#65236,#65237,#65238,#65239,#65240,
#65241,#65242,#65243,#65244,#65245,#65246,#65247,#65248,#65249,#65250,#65251,
#65252,#65253,#65254,#65255,#65256,#65257,#65258,#65259,#65260,#65261,#65262,
#65263,#65264,#65265,#65266,#65267,#65268,#65269,#65270,#65271,#65272,#65273,
#65274,#65275,#65276,#65277,#65278,#65279,#65280,#65281,#65282,#65283,#65284,
#65285,#65286,#65287,#65288,#65289,#65290,#65291,#65292,#65293,#65294,#65295,
#65296,#65297,#65298,#65299,#65300,#65301,#65302,#65303,#65304,#65305,#65306,
#65307,#65308,#65309,#65310,#65311,#65312,#65313,#65314,#65315,#65316,#65317,
#65318,#65319,#65320,#65321,#65322,#65323,#65324,#65325,#65326,#65327,#65328,
#65329,#65330,#65331,#65332,#65333,#65334,#65335,#65336,#65337,#65338,#65339,
#65340,#65341,#65342,#65343,#65344,#65345,#65346,#65347,#65348,#65349,#65350,
#65351,#65352,#65353,#65354,#65355,#65356,#65357,#65358,#65359,#65360,#65361,
#65362,#65363,#65364,#65365,#65366,#65367,#65368,#65369),.UNSPECIFIED.,
 .F.,.F.,(4,3,3,3,3,3,3,3,3,3,3,3,3,3,3,3,3,3,3,3,3,3,3,3,3,3,3,3,3,3,3,
3,3,3,3,3,3,3,3,3,3,3,3,3,3,3,3,3,3,3,3,3,3,3,3,3,3,3,3,3,3,3,3,3,3,3,3,
3,3,3,3,3,3,3,3,3,3,3,3,3,3,3,3,3,3,3,3,3,3,3,3,3,3,3,3,3,3,3,3,3,3,3,3,
3,3,3,3,3,3,3,3,3,3,3,3,3,3,3,3,3,3,3,3,3,3,3,3,3,3,3,3,3,3,3,3,3,3,3,3,
3,3,3,3,3,3,3,3,3,3,3,3,3,3,3,3,3,3,3,3,3,3,3,3,3,3,3,3,3,3,3,3,3,3,3,3,
3,3,3,3,3,3,3,3,3,3,3,3,3,3,3,3,3,3,3,3,3,3,3,3,3,3,3,3,3,3,3,3,3,3,3,3,
3,3,3,3,3,3,3,3,3,3,3,3,3,3,3,3,3,3,3,3,3,3,3,3,3,3,3,3,3,3,3,3,3,3,3,3,
3,3,3,3,3,3,3,3,3,3,3,3,3,3,3,3,3,3,3,3,3,3,3,3,3,3,3,3,3,3,3,3,3,3,3,3,
3,3,3,3,3,3,3,3,3,3,3,3,3,3,3,3,3,3,3,3,3,3,3,3,3,3,3,3,3,3,3,3,3,3,3,3,
3,3,3,3,4),(0.519634288272965,0.519685328699529,0.520064748915136,0.520317377395171,
0.52041882622757,0.520862629228728,0.521055598791493,0.521608503818973,
0.521683880116917,0.521949407569178,0.522103609227474,0.522122900721666,
0.522194625439873,0.522546034517934,0.522620445475116,0.523096346355821,
0.523177630920305,0.523660881144983,0.52374147215814,0.524221681230113,
0.524281202764036,0.524482495257025,0.524611230176765,0.524716416437288,
0.524820933369932,0.52536566976277,0.525453436385481,0.526106323961512,
0.526754869685056,0.527020889720284,0.527099233743331,0.527099277203579,
0.527582135112661,0.527757221295722,0.528314043234494,0.528430114927927,
0.528993375460614,0.529086167710458,0.529219959775975,0.529543895701582,
0.52958754890012,0.529587630937454,0.529977456891594,0.530156916054297,
0.530588309840476,0.530738497933387,0.531180168104028,0.531312507498718,
0.531418964631181,0.531746460164742,0.532002956712191,0.532075864056908,
0.532076060866791,0.532440903797139,0.53262808670734,0.533011517229871,
0.533190418858229,0.533577201788498,0.533618895324374,0.533955285664405,
0.534183375759633,0.534491968780854,0.534564179213697,0.534564531741459,
0.534874225454161,0.5350741437442,0.53541539953875,0.535592193256161,0.535819310443381,
0.536169477904769,0.536339628003893,0.536678131841218,0.536853677988387,
0.537052494370486,0.537052895108299,0.537405347814862,0.537608154053057,
0.537931950012464,0.538021099168023,0.538405583141743,0.538578329449285,
0.53895141665959,0.539138229913681,0.539496520171077,0.539540809527275,
0.539540988570634,0.539861663840644,0.540059301442978,0.540221061997415,
0.540602465762505,0.540736575089981,0.541102630644287,0.541180856588068,
0.541199557458666,0.541307545250463,0.541691361588774,0.541967913239337,
0.542356014405844,0.542419354920138,0.5427453555008,0.542858064226597,0.542945322977705,
0.543503914014392,0.543607680490904,0.54412414824012,0.54425799078739,0.544516855983004,
0.544517439840852,0.54461756988546,0.545052109445124,0.545442006868756,
0.545880174090394,0.546176087079588,0.546176316612045,0.546499735836316,
0.54667364546119,0.546815758868419,0.547186662019704,0.547325476125828,
0.547680850612868,0.547835182761928,0.547835193383237,0.548247442724799,
0.548422790618243,0.548664587179423,0.548664631768834,0.549013350718906,
0.549341372305563,0.54949407015443,0.549494225068885,0.550019243808671,
0.550479626932218,0.550539415922156,0.550964046420334,0.551033927493458,
0.551152905048832,0.551152946925622,0.551217046456726,0.551638420351807,
0.551907137251258,0.551982385311219,0.55198292810655,0.55239795763465,0.552605363661335,
0.552811823696815,0.552812789177049,0.553103236083438,0.553346610897895,
0.553617111751246,0.553887612604596,0.554148146967989,0.554540173762878,
0.554684868911349,0.555070009559826,0.555208905676705,0.555584558639431,
0.55561318736948,0.555918776435394,0.5561295772392,0.556129951812526,0.556417857233963,
0.556614544343955,0.556951756087017,0.557110879990134,0.557460926408367,
0.557611236045966,0.557815627826188,0.558170539705477,0.558316410385829,
0.55866373208175,0.558812915816199,0.559195892885701,0.559290662375238,
0.559395069100249,0.559447922497438,0.559783274014755,0.560018781254633,
0.560509613861431,0.560562494403706,0.561068870852784,0.561106207552778,
0.5611064241511,0.561570163349529,0.561613622761172,0.562110304428833,0.562218088325341,
0.562720821705787,0.56276508432397,0.562765506512604,0.563096386740074,
0.56335672413056,0.563751060238607,0.563955559845074,0.564343253512623,
0.564423125352024,0.564807306948141,0.565012225582776,0.565338252441909,
0.565595137789165,0.565937492527023,0.566082837866355,0.566083305223524,
0.566290558602028,0.566497870458405,0.56662436047434,0.566912276251951,
0.566912553185446,0.567351614620598,0.567741714637548,0.56774196785478,
0.568233190525925,0.568262889249545,0.568571153023144,0.568571203661145,
0.56882537837842,0.569239105243424,0.569287877949591,0.569400580543106,
0.569553117821054,0.570186121177483,0.57068515625277,0.571021295028928,
0.571059323946559,0.571219571436256,0.571778523153722,0.572328620057531,
0.57271816815427,0.572718344951125,0.57313602810784,0.573185294676041,0.573217271654526,
0.573684047634441,0.574096811422129,0.574151787876143,0.574377198662668,
0.574377221722318,0.574851542486652,0.575326375323,0.575795357182198,0.57603603375322,
0.57603609849351,0.576146419885079,0.57656190279015,0.576978136439357,0.577392543078506,
0.577694975264703,0.577695006938886,0.578087616610859,0.578188843009782,
0.578683381655279,0.579079581222031,0.579353816732127,0.579353852035895,
0.579747707031495,0.580148705440453,0.580549216095425,0.580946733847149,
0.581012698465323,0.581012728807088,0.581450019985727,0.581513943575523,
0.581989771834821,0.582015158343958,0.582489114392038,0.582671590517892,
0.58267160557828,0.583084254741761,0.583115660889144,0.583546735106938,
0.58366588366946,0.584114024632597,0.584216076115485,0.584330458037086,
0.584330482349473,0.584995793416719,0.585316469886586,0.585799041310968,
0.585989349773787,0.585989359120665,0.586417179063202,0.586879871687596,
0.587342969056041,0.58764821966101,0.587648235891858,0.588117971918786,
0.588144008688664,0.588617152903228,0.589110011816295,0.58930711266305,
0.589769585860652,0.589872824892581,0.59044241083114,0.590817402878396,
0.590965989434243,0.590966142307199,0.591531270699443,0.591606910100047,
0.592259975940435,0.592624866205435,0.592625013025626,0.593015942520109,
0.593574386378729,0.593823107660491,0.594309857022409,0.594626170563338,
0.594836701900359,0.594836877607622,0.595213571428038,0.595722866777785,
0.595849042762403,0.596440903702074,0.596475072270493,0.596892830512108,
0.597048490362349,0.597048537595282,0.597412222783684,0.597953152400304,
0.598042720995882,0.598682854065377,0.59914438845755,0.599260172474802,
0.599260373290205,0.599543077637962,0.599608753599983),.UNSPECIFIED.);
#808=B_SPLINE_CURVE_WITH_KNOTS('',3,(#65734,#65735,#65736,#65737,#65738,
#65739,#65740,#65741,#65742,#65743,#65744,#65745,#65746,#65747,#65748,#65749,
#65750,#65751,#65752,#65753,#65754,#65755,#65756,#65757,#65758,#65759,#65760,
#65761,#65762,#65763,#65764,#65765,#65766,#65767,#65768,#65769,#65770,#65771,
#65772,#65773,#65774,#65775,#65776,#65777,#65778,#65779,#65780,#65781,#65782,
#65783,#65784,#65785,#65786),.UNSPECIFIED.,.F.,.F.,(4,1,1,1,1,1,1,1,1,1,
1,1,1,1,1,1,1,1,1,1,1,1,1,1,1,1,1,1,1,1,1,1,1,1,1,1,1,1,1,1,1,1,1,1,1,1,
1,1,1,1,4),(0.688002641823372,0.690490227769403,0.692978542756553,0.695466857743702,
0.697955172730851,0.700443487718,0.702931802705149,0.705420117692299,0.707908432679448,
0.710120268223581,0.712332103767713,0.714543939311846,0.716202815969945,
0.717861692628045,0.719520569286144,0.721179445944244,0.722838322602343,
0.724497199260443,0.726156075918542,0.727814952576642,0.729473829234741,
0.731132705892841,0.73279158255094,0.73445045920904,0.736109335867139,0.737768212525239,
0.739427089183338,0.741085965841438,0.742191883613504,0.74329780138557,
0.745509636929703,0.747721472473835,0.749933308017968,0.752145143562101,
0.753251061334167,0.7538040202202,0.754080499663217,0.754356979106233,0.757674732422432,
0.759333609080532,0.760992485738631,0.761407204903156,0.761821924067681,
0.762651362396731,0.763480800725781,0.76431023905483,0.76513967738388,0.76596911571293,
0.766798554041979,0.767627992371029,0.767981201714498),.UNSPECIFIED.);
#809=B_SPLINE_CURVE_WITH_KNOTS('',3,(#67268,#67269,#67270,#67271,#67272,
#67273,#67274,#67275,#67276,#67277,#67278,#67279,#67280,#67281,#67282,#67283,
#67284,#67285,#67286,#67287,#67288,#67289,#67290,#67291,#67292,#67293,#67294,
#67295,#67296,#67297,#67298,#67299,#67300,#67301,#67302,#67303,#67304,#67305,
#67306,#67307,#67308,#67309,#67310,#67311,#67312,#67313,#67314,#67315,#67316,
#67317,#67318,#67319,#67320,#67321,#67322,#67323,#67324,#67325),
 .UNSPECIFIED.,.F.,.F.,(4,1,1,1,1,1,1,1,1,1,1,1,1,1,1,1,1,1,1,1,1,1,1,1,
1,1,1,1,1,1,1,1,1,1,1,1,1,1,1,1,1,1,1,1,1,1,1,1,1,1,1,1,1,1,1,4),(0.813159529437338,
0.815359014876381,0.817558857709555,0.819758700542729,0.821958543375904,
0.824158386209078,0.826358229042252,0.828558071875427,0.830757914708601,
0.832224476597384,0.833691038486167,0.83515760037495,0.835890881319341,
0.836624162263733,0.837357443208124,0.839557286041298,0.841757128874473,
0.843956971707647,0.846156814540821,0.848356657373996,0.85055650020717,
0.852756343040344,0.853856264456931,0.854956185873519,0.857156028706693,
0.857889309651084,0.858622590595476,0.859355871539867,0.860089152484259,
0.86082243342865,0.861555714373042,0.862655635789629,0.863755557206216,
0.864855478622803,0.86595540003939,0.868155242872565,0.870355085705739,
0.871821647594522,0.874754771372088,0.875854692788675,0.876954614205262,
0.879154457038436,0.880254378455023,0.880804339163317,0.881079319517464,
0.881354299871611,0.883554142704785,0.885753985537959,0.887953828371133,
0.890153671204308,0.892353514037482,0.89253683427358,0.892628494391629,
0.892720154509678,0.893086794981873,0.893448166194802),.UNSPECIFIED.);
#810=B_SPLINE_CURVE_WITH_KNOTS('',3,(#67678,#67679,#67680,#67681,#67682,
#67683,#67684,#67685,#67686,#67687,#67688,#67689,#67690,#67691,#67692,#67693,
#67694,#67695,#67696,#67697,#67698,#67699,#67700,#67701,#67702,#67703,#67704,
#67705,#67706,#67707,#67708,#67709,#67710,#67711,#67712,#67713,#67714,#67715,
#67716,#67717,#67718,#67719,#67720,#67721,#67722,#67723,#67724,#67725,#67726,
#67727,#67728,#67729,#67730,#67731,#67732,#67733,#67734,#67735,#67736,#67737,
#67738,#67739,#67740,#67741,#67742,#67743,#67744,#67745,#67746,#67747,#67748,
#67749,#67750,#67751,#67752,#67753,#67754,#67755,#67756,#67757,#67758,#67759,
#67760,#67761,#67762,#67763,#67764,#67765,#67766,#67767,#67768,#67769,#67770,
#67771,#67772,#67773,#67774,#67775,#67776,#67777,#67778,#67779,#67780,#67781,
#67782,#67783,#67784,#67785,#67786,#67787,#67788,#67789,#67790,#67791,#67792,
#67793,#67794,#67795,#67796,#67797,#67798,#67799,#67800,#67801,#67802,#67803,
#67804,#67805,#67806,#67807,#67808,#67809,#67810,#67811,#67812,#67813,#67814,
#67815,#67816,#67817,#67818,#67819,#67820,#67821,#67822,#67823,#67824,#67825,
#67826,#67827,#67828,#67829,#67830,#67831,#67832,#67833,#67834,#67835,#67836,
#67837,#67838,#67839,#67840,#67841,#67842,#67843,#67844,#67845,#67846,#67847,
#67848,#67849,#67850,#67851,#67852,#67853,#67854,#67855,#67856,#67857,#67858,
#67859,#67860,#67861,#67862,#67863,#67864,#67865,#67866,#67867,#67868,#67869,
#67870,#67871,#67872,#67873,#67874,#67875,#67876,#67877,#67878,#67879,#67880,
#67881,#67882,#67883,#67884,#67885,#67886,#67887,#67888,#67889,#67890,#67891,
#67892,#67893,#67894,#67895,#67896,#67897,#67898,#67899,#67900,#67901,#67902,
#67903,#67904,#67905,#67906,#67907,#67908,#67909,#67910,#67911,#67912,#67913,
#67914,#67915,#67916,#67917,#67918,#67919,#67920,#67921,#67922,#67923,#67924,
#67925,#67926,#67927,#67928,#67929,#67930,#67931,#67932,#67933,#67934,#67935,
#67936,#67937,#67938,#67939,#67940,#67941,#67942,#67943,#67944,#67945,#67946,
#67947,#67948,#67949,#67950,#67951,#67952,#67953,#67954,#67955,#67956,#67957,
#67958,#67959,#67960,#67961,#67962,#67963,#67964,#67965,#67966,#67967,#67968,
#67969,#67970,#67971,#67972,#67973,#67974,#67975,#67976,#67977,#67978,#67979,
#67980,#67981,#67982,#67983,#67984,#67985,#67986,#67987,#67988,#67989,#67990,
#67991,#67992,#67993,#67994,#67995,#67996,#67997,#67998,#67999,#68000,#68001,
#68002,#68003,#68004,#68005,#68006,#68007,#68008,#68009,#68010,#68011,#68012,
#68013,#68014,#68015,#68016,#68017,#68018,#68019,#68020,#68021,#68022,#68023,
#68024,#68025,#68026,#68027,#68028,#68029,#68030,#68031,#68032,#68033,#68034,
#68035,#68036,#68037,#68038,#68039,#68040,#68041,#68042,#68043,#68044,#68045,
#68046,#68047,#68048,#68049,#68050,#68051,#68052,#68053,#68054,#68055,#68056,
#68057,#68058,#68059,#68060,#68061,#68062,#68063,#68064,#68065,#68066,#68067,
#68068,#68069,#68070,#68071,#68072,#68073,#68074,#68075,#68076,#68077,#68078,
#68079,#68080,#68081,#68082,#68083,#68084,#68085,#68086,#68087,#68088,#68089,
#68090,#68091,#68092,#68093,#68094,#68095,#68096,#68097,#68098,#68099,#68100,
#68101,#68102,#68103,#68104,#68105,#68106,#68107,#68108,#68109,#68110,#68111,
#68112,#68113,#68114,#68115,#68116,#68117,#68118,#68119,#68120,#68121,#68122,
#68123,#68124,#68125,#68126,#68127,#68128,#68129,#68130,#68131,#68132,#68133,
#68134,#68135,#68136,#68137,#68138,#68139,#68140,#68141,#68142,#68143,#68144,
#68145,#68146,#68147,#68148,#68149,#68150,#68151,#68152,#68153,#68154,#68155,
#68156,#68157,#68158,#68159,#68160,#68161,#68162,#68163,#68164,#68165,#68166,
#68167,#68168,#68169,#68170,#68171,#68172,#68173,#68174,#68175,#68176,#68177,
#68178,#68179,#68180,#68181,#68182,#68183,#68184,#68185,#68186,#68187,#68188,
#68189,#68190,#68191,#68192,#68193,#68194,#68195,#68196,#68197,#68198,#68199,
#68200,#68201,#68202,#68203,#68204,#68205,#68206,#68207,#68208,#68209,#68210,
#68211,#68212,#68213,#68214,#68215,#68216,#68217,#68218,#68219,#68220,#68221,
#68222,#68223,#68224,#68225,#68226,#68227,#68228,#68229,#68230,#68231,#68232,
#68233,#68234,#68235,#68236,#68237,#68238,#68239,#68240,#68241,#68242,#68243,
#68244,#68245,#68246,#68247,#68248,#68249,#68250,#68251,#68252,#68253,#68254,
#68255,#68256,#68257,#68258,#68259,#68260,#68261,#68262,#68263,#68264,#68265,
#68266,#68267,#68268,#68269,#68270,#68271,#68272,#68273,#68274,#68275,#68276,
#68277,#68278,#68279,#68280,#68281,#68282,#68283,#68284,#68285,#68286,#68287,
#68288,#68289,#68290,#68291,#68292,#68293,#68294,#68295,#68296,#68297,#68298,
#68299,#68300,#68301,#68302,#68303,#68304,#68305,#68306,#68307,#68308,#68309,
#68310,#68311,#68312,#68313,#68314,#68315,#68316,#68317,#68318,#68319,#68320,
#68321,#68322,#68323,#68324,#68325,#68326,#68327,#68328,#68329,#68330,#68331,
#68332,#68333,#68334,#68335,#68336,#68337,#68338,#68339,#68340,#68341,#68342,
#68343,#68344,#68345,#68346,#68347,#68348,#68349,#68350,#68351,#68352,#68353,
#68354,#68355,#68356,#68357,#68358,#68359,#68360,#68361,#68362,#68363,#68364,
#68365,#68366,#68367,#68368,#68369,#68370,#68371,#68372,#68373,#68374,#68375,
#68376,#68377,#68378,#68379,#68380,#68381,#68382,#68383,#68384,#68385,#68386,
#68387,#68388,#68389,#68390,#68391,#68392,#68393,#68394,#68395,#68396,#68397,
#68398,#68399,#68400,#68401,#68402,#68403,#68404,#68405,#68406,#68407,#68408,
#68409,#68410,#68411,#68412,#68413,#68414,#68415,#68416,#68417,#68418,#68419,
#68420,#68421,#68422,#68423,#68424,#68425,#68426,#68427,#68428,#68429,#68430,
#68431,#68432,#68433,#68434,#68435,#68436,#68437,#68438,#68439,#68440,#68441,
#68442,#68443,#68444,#68445,#68446,#68447,#68448,#68449,#68450,#68451,#68452,
#68453,#68454,#68455,#68456,#68457,#68458,#68459,#68460,#68461,#68462,#68463,
#68464,#68465,#68466,#68467,#68468,#68469,#68470,#68471,#68472,#68473,#68474,
#68475,#68476,#68477,#68478,#68479,#68480,#68481,#68482,#68483,#68484,#68485,
#68486,#68487,#68488,#68489,#68490,#68491,#68492,#68493,#68494,#68495,#68496,
#68497,#68498,#68499,#68500,#68501,#68502,#68503,#68504,#68505,#68506,#68507,
#68508,#68509,#68510,#68511,#68512,#68513,#68514,#68515,#68516,#68517,#68518,
#68519,#68520,#68521,#68522,#68523,#68524,#68525,#68526,#68527,#68528,#68529,
#68530,#68531,#68532,#68533,#68534,#68535,#68536,#68537,#68538,#68539,#68540,
#68541,#68542,#68543,#68544,#68545,#68546,#68547,#68548,#68549,#68550,#68551,
#68552,#68553,#68554,#68555,#68556,#68557,#68558,#68559,#68560,#68561,#68562,
#68563,#68564,#68565,#68566,#68567,#68568,#68569,#68570,#68571,#68572,#68573,
#68574,#68575,#68576,#68577,#68578,#68579,#68580,#68581,#68582,#68583,#68584,
#68585,#68586,#68587,#68588,#68589,#68590,#68591,#68592,#68593,#68594,#68595,
#68596,#68597,#68598,#68599,#68600,#68601,#68602,#68603,#68604,#68605,#68606,
#68607,#68608,#68609,#68610,#68611,#68612,#68613,#68614,#68615,#68616,#68617,
#68618,#68619,#68620,#68621,#68622,#68623,#68624,#68625,#68626,#68627,#68628,
#68629,#68630,#68631,#68632,#68633,#68634,#68635,#68636,#68637,#68638,#68639,
#68640,#68641,#68642,#68643,#68644),.UNSPECIFIED.,.F.,.F.,(4,3,3,3,3,3,
3,3,3,3,3,3,3,3,3,3,3,3,3,3,3,3,3,3,3,3,3,3,3,3,3,3,3,3,3,3,3,3,3,3,3,3,
3,3,3,3,3,3,3,3,3,3,3,3,3,3,3,3,3,3,3,3,3,3,3,3,3,3,3,3,3,3,3,3,3,3,3,3,
3,3,3,3,3,3,3,3,3,3,3,3,3,3,3,3,3,3,3,3,3,3,3,3,3,3,3,3,3,3,3,3,3,3,3,3,
3,3,3,3,3,3,3,3,3,3,3,3,3,3,3,3,3,3,3,3,3,3,3,3,3,3,3,3,3,3,3,3,3,3,3,3,
3,3,3,3,3,3,3,3,3,3,3,3,3,3,3,3,3,3,3,3,3,3,3,3,3,3,3,3,3,3,3,3,3,3,3,3,
3,3,3,3,3,3,3,3,3,3,3,3,3,3,3,3,3,3,3,3,3,3,3,3,3,3,3,3,3,3,3,3,3,3,3,3,
3,3,3,3,3,3,3,3,3,3,3,3,3,3,3,3,3,3,3,3,3,3,3,3,3,3,3,3,3,3,3,3,3,3,3,3,
3,3,3,3,3,3,3,3,3,3,3,3,3,3,3,3,3,3,3,3,3,3,3,3,3,3,3,3,3,3,3,3,3,3,3,3,
3,3,3,3,3,3,3,3,3,3,3,3,3,3,3,3,3,3,3,3,3,3,3,3,3,3,3,3,4),(0.856370509464718,
0.856739710126176,0.856941604650561,0.857157463028789,0.857728097172609,
0.857889710219808,0.858455007199432,0.858622556190436,0.858856880166661,
0.858856990877825,0.859220635558683,0.859356155617663,0.859900245426217,
0.86008841202652,0.86059414452884,0.860635206101866,0.860820640290637,0.861206260844417,
0.861344429784462,0.861344437291952,0.861554210482135,0.862000485740877,
0.862124540013047,0.862595676556938,0.862653396798758,0.863116747727199,
0.863224409502402,0.863651619529005,0.863752914872577,0.86383188370608,
0.863832010953973,0.864231153625413,0.864379515660299,0.864812069623318,
0.864852826667762,0.865403258519047,0.865808793566429,0.865952319957288,
0.866319330120207,0.866319743320668,0.866688117823291,0.866898517600103,
0.86730618182318,0.867526014023919,0.867925662148695,0.868121848041472,
0.868153510447734,0.868543579726341,0.868757896298623,0.868806776534335,
0.8688072293163,0.869207754885257,0.869618033069385,0.869669922765494,0.870017419969291,
0.870355051628635,0.870732516059687,0.871089200032129,0.87125701384248,
0.871294268262353,0.871360824031647,0.871683079267071,0.871823348435623,
0.872156731118901,0.872283865069682,0.872537946155526,0.87253825597237,
0.873069937605435,0.873548261234971,0.873763600880015,0.87378166936259,
0.873781779373382,0.87408481375249,0.874210878426716,0.874545716993315,
0.874633113921817,0.874753735812206,0.875024584111161,0.875025392569654,
0.875384898969503,0.875447491540601,0.875827691453192,0.875853867950656,
0.876268869897062,0.876269115776718,0.876585265584936,0.876774748855083,
0.876953119288411,0.877343592214753,0.877458393130804,0.877831111513812,
0.877969286193373,0.87840678928135,0.878480179255942,0.878480344993447,
0.87879194090105,0.87910295087439,0.87915231397627,0.879584531980476,0.879802996579847,
0.880111835486817,0.880252435165722,0.880691242735167,0.880691684404755,
0.881074207456304,0.881332551760943,0.881692354816355,0.88201939931933,
0.88246085276686,0.882712790984588,0.882902306214391,0.882903292719097,
0.883209674962912,0.883397627564955,0.883556714133813,0.884042481261811,
0.884544402441087,0.88504328705427,0.885523235920033,0.885724698943558,
0.885752508450121,0.88612212093931,0.886218901433228,0.886219625571857,
0.886537647333598,0.886707761785872,0.886974326236772,0.887211981951545,
0.887551235931704,0.887729114878847,0.8879560400736,0.888300204156477,0.888473221575917,
0.88878646732094,0.889004359113991,0.88928438686396,0.889504870756455,0.889536078306289,
0.889900762160951,0.890116587626518,0.890603106978639,0.891062191854129,
0.891193794261483,0.891194106502742,0.891732405714557,0.891943414975812,
0.89235407755958,0.892537660293242,0.892629451947967,0.892721242487384,
0.892852091870902,0.892852276487536,0.893088279783021,0.893510409052143,
0.893658802645668,0.893821329466465,0.894211435057065,0.894393765759537,
0.89451038948032,0.894510493238327,0.894901352996297,0.895287599092038,
0.895702170859857,0.896103458643209,0.896168687089739,0.896168712319676,
0.896567659105487,0.896754419127474,0.896997800787915,0.896997835894448,
0.897496487037925,0.89772245833648,0.897826936126778,0.897992419076711,
0.898220722714388,0.898769754683305,0.898953707057181,0.899136939501272,
0.899320178893095,0.89948519444784,0.899686677582514,0.90005314101267,0.900314329369707,
0.900419642490131,0.900898645228698,0.901143479480045,0.901152743988307,
0.901492719454058,0.901558081566027,0.901724949122927,0.901972666219304,
0.901972728722703,0.902351164518496,0.902618371808164,0.902801875181428,
0.902801877527412,0.903171552794411,0.903540854898999,0.903952120779196,
0.904084917817704,0.904590636256751,0.904832418839058,0.905379797910794,
0.905550697078066,0.905900919943512,0.906118472746249,0.9061185171396,0.906468240531146,
0.906816938564654,0.906947604592874,0.906947621550958,0.907017340702522,
0.907399284623962,0.907776770355667,0.907776802867114,0.908241313754553,
0.90828552324162,0.908484350706353,0.908990207617589,0.909435067965086,
0.909435144078441,0.90985913862168,0.909951279775271,0.910614001596101,
0.911269042084864,0.911417756555064,0.91164613144431,0.911646157495504,
0.912099113248859,0.912191784393921,0.912742716916304,0.912884559760023,
0.9134021509074,0.913433410843006,0.913819002254019,0.913857194923535,0.913857288302221,
0.914285977812487,0.914418745168495,0.914842047306868,0.915401504308667,
0.915841264194839,0.91595605892196,0.916068258402759,0.91606831730272,0.916453159009049,
0.916798645433519,0.917173790142372,0.917173828804338,0.917622268037278,
0.917776470821123,0.918223528974704,0.918279321881984,0.91827938061333,
0.918754802595467,0.919295871548816,0.919404876537645,0.919964840577214,
0.920059693976517,0.920490385361208,0.920490495469795,0.920953807375547,
0.921500637114346,0.921647287968573,0.922154668126846,0.922333425482766,
0.922701448840433,0.922701525067417,0.923152318153573,0.923698348353999,
0.924166610876225,0.92424665199397,0.924359746449851,0.924359806127616,
0.924837979949728,0.924908244107517,0.925350209741723,0.925896246655443,
0.92601804405927,0.926018077499045,0.926511614483731,0.926685236328919,
0.927275246146838,0.927365910698766,0.92754902089914,0.927676341668688,
0.927676408620273,0.928236970237227,0.928804914273471,0.929334624595944,
0.929334639278107,0.929748496617437,0.930163740203712,0.930163788082816,
0.93058891693644,0.930992811539352,0.930992936887525,0.93140751128988,0.931822021399953,
0.931822085692234,0.931948840165757,0.932345748446948,0.932651066673402,
0.932651234496943,0.933065609618207,0.933065808899298,0.933480208305583,
0.933480383301653,0.933883400287811,0.934150258990416,0.934309417204156,
0.934309532106362,0.934724106508717,0.935138461211252,0.935138680911071,
0.935476768984967,0.935553064830452,0.935553255313426,0.935848405917604,
0.935967680546784,0.93596782971578,0.936254160901786,0.936350378361133),
 .UNSPECIFIED.);
#1716=SHAPE_REPRESENTATION_RELATIONSHIP('SRR','None',#135340,#1729);
#1729=ADVANCED_BREP_SHAPE_REPRESENTATION('',(#1755),#135272);
#1742=STYLED_ITEM('',(#135414),#1755);
#1755=MANIFOLD_SOLID_BREP('Body1',#32078);
#1786=CYLINDRICAL_SURFACE('',#32404,2.5);
#1787=CYLINDRICAL_SURFACE('',#32406,2.5);
#1788=CYLINDRICAL_SURFACE('',#32407,2.5);
#1789=CYLINDRICAL_SURFACE('',#32408,2.5);
#1790=CYLINDRICAL_SURFACE('',#32409,2.5);
#1791=CYLINDRICAL_SURFACE('',#32410,2.5);
#1792=CYLINDRICAL_SURFACE('',#32411,2.5);
#1793=CYLINDRICAL_SURFACE('',#32412,2.5);
#1794=CYLINDRICAL_SURFACE('',#32413,2.5);
#1795=CYLINDRICAL_SURFACE('',#32414,2.5);
#1796=CYLINDRICAL_SURFACE('',#32415,2.5);
#1797=CYLINDRICAL_SURFACE('',#32416,2.5);
#1798=CYLINDRICAL_SURFACE('',#32417,2.5);
#1799=CYLINDRICAL_SURFACE('',#32418,2.5);
#1800=CYLINDRICAL_SURFACE('',#32419,2.5);
#1801=CYLINDRICAL_SURFACE('',#32420,2.5);
#1802=CYLINDRICAL_SURFACE('',#32421,2.5);
#1803=CYLINDRICAL_SURFACE('',#32422,2.5);
#1804=CYLINDRICAL_SURFACE('',#32423,2.5);
#1805=CYLINDRICAL_SURFACE('',#32424,2.5);
#1806=CYLINDRICAL_SURFACE('',#32425,2.5);
#1807=CYLINDRICAL_SURFACE('',#32426,2.5);
#1808=CYLINDRICAL_SURFACE('',#32427,2.5);
#1809=CYLINDRICAL_SURFACE('',#32428,2.5);
#1810=CYLINDRICAL_SURFACE('',#32429,2.5);
#1811=CYLINDRICAL_SURFACE('',#32430,2.5);
#1812=CYLINDRICAL_SURFACE('',#32431,2.5);
#1813=CYLINDRICAL_SURFACE('',#32432,2.5);
#1814=CYLINDRICAL_SURFACE('',#32433,2.5);
#1815=CYLINDRICAL_SURFACE('',#32434,2.5);
#1816=CYLINDRICAL_SURFACE('',#32435,2.5);
#1817=CYLINDRICAL_SURFACE('',#32436,2.5);
#1818=CYLINDRICAL_SURFACE('',#32437,2.5);
#1819=CYLINDRICAL_SURFACE('',#32438,2.5);
#1820=CYLINDRICAL_SURFACE('',#32439,2.5);
#1821=CYLINDRICAL_SURFACE('',#32440,2.5);
#1822=CYLINDRICAL_SURFACE('',#32441,2.5);
#1823=CYLINDRICAL_SURFACE('',#32442,2.5);
#1824=CYLINDRICAL_SURFACE('',#32443,2.5);
#1825=CYLINDRICAL_SURFACE('',#32444,2.5);
#1826=CYLINDRICAL_SURFACE('',#32445,2.5);
#1827=CYLINDRICAL_SURFACE('',#32446,2.5);
#1828=CYLINDRICAL_SURFACE('',#32447,2.5);
#1829=CYLINDRICAL_SURFACE('',#32448,2.5);
#1830=CYLINDRICAL_SURFACE('',#32449,2.5);
#1831=CYLINDRICAL_SURFACE('',#32450,2.5);
#1832=CYLINDRICAL_SURFACE('',#32451,2.5);
#1833=CYLINDRICAL_SURFACE('',#32453,2.5);
#1834=CYLINDRICAL_SURFACE('',#32465,2.);
#1835=CYLINDRICAL_SURFACE('',#32472,2.);
#2034=FACE_BOUND('',#5298,.T.);
#2035=FACE_BOUND('',#5300,.T.);
#2036=FACE_BOUND('',#5303,.T.);
#2272=PLANE('',#32454);
#2273=PLANE('',#32456);
#2274=PLANE('',#32458);
#2275=PLANE('',#32459);
#2276=PLANE('',#32460);
#2277=PLANE('',#32461);
#2278=PLANE('',#32467);
#2279=PLANE('',#32470);
#2280=PLANE('',#32476);
#3443=FACE_OUTER_BOUND('',#5215,.T.);
#3444=FACE_OUTER_BOUND('',#5216,.T.);
#3445=FACE_OUTER_BOUND('',#5217,.T.);
#3446=FACE_OUTER_BOUND('',#5218,.T.);
#3447=FACE_OUTER_BOUND('',#5219,.T.);
#3448=FACE_OUTER_BOUND('',#5220,.T.);
#3449=FACE_OUTER_BOUND('',#5221,.T.);
#3450=FACE_OUTER_BOUND('',#5222,.T.);
#3451=FACE_OUTER_BOUND('',#5223,.T.);
#3452=FACE_OUTER_BOUND('',#5224,.T.);
#3453=FACE_OUTER_BOUND('',#5225,.T.);
#3454=FACE_OUTER_BOUND('',#5226,.T.);
#3455=FACE_OUTER_BOUND('',#5227,.T.);
#3456=FACE_OUTER_BOUND('',#5228,.T.);
#3457=FACE_OUTER_BOUND('',#5229,.T.);
#3458=FACE_OUTER_BOUND('',#5230,.T.);
#3459=FACE_OUTER_BOUND('',#5231,.T.);
#3460=FACE_OUTER_BOUND('',#5232,.T.);
#3461=FACE_OUTER_BOUND('',#5233,.T.);
#3462=FACE_OUTER_BOUND('',#5234,.T.);
#3463=FACE_OUTER_BOUND('',#5235,.T.);
#3464=FACE_OUTER_BOUND('',#5236,.T.);
#3465=FACE_OUTER_BOUND('',#5237,.T.);
#3466=FACE_OUTER_BOUND('',#5238,.T.);
#3467=FACE_OUTER_BOUND('',#5239,.T.);
#3468=FACE_OUTER_BOUND('',#5240,.T.);
#3469=FACE_OUTER_BOUND('',#5241,.T.);
#3470=FACE_OUTER_BOUND('',#5242,.T.);
#3471=FACE_OUTER_BOUND('',#5243,.T.);
#3472=FACE_OUTER_BOUND('',#5244,.T.);
#3473=FACE_OUTER_BOUND('',#5245,.T.);
#3474=FACE_OUTER_BOUND('',#5246,.T.);
#3475=FACE_OUTER_BOUND('',#5247,.T.);
#3476=FACE_OUTER_BOUND('',#5248,.T.);
#3477=FACE_OUTER_BOUND('',#5249,.T.);
#3478=FACE_OUTER_BOUND('',#5250,.T.);
#3479=FACE_OUTER_BOUND('',#5251,.T.);
#3480=FACE_OUTER_BOUND('',#5252,.T.);
#3481=FACE_OUTER_BOUND('',#5253,.T.);
#3482=FACE_OUTER_BOUND('',#5254,.T.);
#3483=FACE_OUTER_BOUND('',#5255,.T.);
#3484=FACE_OUTER_BOUND('',#5256,.T.);
#3485=FACE_OUTER_BOUND('',#5257,.T.);
#3486=FACE_OUTER_BOUND('',#5258,.T.);
#3487=FACE_OUTER_BOUND('',#5259,.T.);
#3488=FACE_OUTER_BOUND('',#5260,.T.);
#3489=FACE_OUTER_BOUND('',#5261,.T.);
#3490=FACE_OUTER_BOUND('',#5262,.T.);
#3491=FACE_OUTER_BOUND('',#5263,.T.);
#3492=FACE_OUTER_BOUND('',#5264,.T.);
#3493=FACE_OUTER_BOUND('',#5265,.T.);
#3494=FACE_OUTER_BOUND('',#5266,.T.);
#3495=FACE_OUTER_BOUND('',#5267,.T.);
#3496=FACE_OUTER_BOUND('',#5268,.T.);
#3497=FACE_OUTER_BOUND('',#5269,.T.);
#3498=FACE_OUTER_BOUND('',#5270,.T.);
#3499=FACE_OUTER_BOUND('',#5271,.T.);
#3500=FACE_OUTER_BOUND('',#5272,.T.);
#3501=FACE_OUTER_BOUND('',#5273,.T.);
#3502=FACE_OUTER_BOUND('',#5274,.T.);
#3503=FACE_OUTER_BOUND('',#5275,.T.);
#3504=FACE_OUTER_BOUND('',#5276,.T.);
#3505=FACE_OUTER_BOUND('',#5277,.T.);
#3506=FACE_OUTER_BOUND('',#5278,.T.);
#3507=FACE_OUTER_BOUND('',#5279,.T.);
#3508=FACE_OUTER_BOUND('',#5280,.T.);
#3509=FACE_OUTER_BOUND('',#5281,.T.);
#3510=FACE_OUTER_BOUND('',#5282,.T.);
#3511=FACE_OUTER_BOUND('',#5283,.T.);
#3512=FACE_OUTER_BOUND('',#5284,.T.);
#3513=FACE_OUTER_BOUND('',#5285,.T.);
#3514=FACE_OUTER_BOUND('',#5286,.T.);
#3515=FACE_OUTER_BOUND('',#5287,.T.);
#3516=FACE_OUTER_BOUND('',#5288,.T.);
#3517=FACE_OUTER_BOUND('',#5289,.T.);
#3518=FACE_OUTER_BOUND('',#5290,.T.);
#3519=FACE_OUTER_BOUND('',#5291,.T.);
#3520=FACE_OUTER_BOUND('',#5292,.T.);
#3521=FACE_OUTER_BOUND('',#5293,.T.);
#3522=FACE_OUTER_BOUND('',#5294,.T.);
#3523=FACE_OUTER_BOUND('',#5295,.T.);
#3524=FACE_OUTER_BOUND('',#5296,.T.);
#3525=FACE_OUTER_BOUND('',#5297,.T.);
#3526=FACE_OUTER_BOUND('',#5299,.T.);
#3527=FACE_OUTER_BOUND('',#5301,.T.);
#3528=FACE_OUTER_BOUND('',#5302,.T.);
#3529=FACE_OUTER_BOUND('',#5304,.T.);
#3530=FACE_OUTER_BOUND('',#5305,.T.);
#3531=FACE_OUTER_BOUND('',#5306,.T.);
#5215=EDGE_LOOP('',(#21422,#21423,#21424,#21425,#21426,#21427,#21428,#21429,
#21430,#21431));
#5216=EDGE_LOOP('',(#21432,#21433,#21434,#21435,#21436));
#5217=EDGE_LOOP('',(#21437,#21438,#21439,#21440));
#5218=EDGE_LOOP('',(#21441,#21442,#21443,#21444,#21445,#21446));
#5219=EDGE_LOOP('',(#21447,#21448,#21449,#21450,#21451));
#5220=EDGE_LOOP('',(#21452,#21453,#21454,#21455,#21456));
#5221=EDGE_LOOP('',(#21457,#21458,#21459,#21460,#21461,#21462));
#5222=EDGE_LOOP('',(#21463,#21464,#21465,#21466,#21467));
#5223=EDGE_LOOP('',(#21468,#21469,#21470,#21471,#21472,#21473));
#5224=EDGE_LOOP('',(#21474,#21475,#21476,#21477,#21478,#21479));
#5225=EDGE_LOOP('',(#21480,#21481,#21482,#21483,#21484));
#5226=EDGE_LOOP('',(#21485,#21486,#21487,#21488,#21489,#21490,#21491));
#5227=EDGE_LOOP('',(#21492,#21493,#21494,#21495,#21496));
#5228=EDGE_LOOP('',(#21497,#21498,#21499,#21500,#21501));
#5229=EDGE_LOOP('',(#21502,#21503,#21504,#21505,#21506,#21507));
#5230=EDGE_LOOP('',(#21508,#21509,#21510,#21511));
#5231=EDGE_LOOP('',(#21512,#21513,#21514,#21515,#21516,#21517));
#5232=EDGE_LOOP('',(#21518,#21519,#21520,#21521,#21522));
#5233=EDGE_LOOP('',(#21523,#21524,#21525,#21526));
#5234=EDGE_LOOP('',(#21527,#21528,#21529,#21530,#21531,#21532));
#5235=EDGE_LOOP('',(#21533,#21534,#21535,#21536,#21537));
#5236=EDGE_LOOP('',(#21538,#21539,#21540,#21541,#21542,#21543,#21544));
#5237=EDGE_LOOP('',(#21545,#21546,#21547,#21548,#21549,#21550));
#5238=EDGE_LOOP('',(#21551,#21552,#21553,#21554));
#5239=EDGE_LOOP('',(#21555,#21556,#21557,#21558,#21559,#21560,#21561));
#5240=EDGE_LOOP('',(#21562,#21563,#21564,#21565,#21566));
#5241=EDGE_LOOP('',(#21567,#21568,#21569,#21570));
#5242=EDGE_LOOP('',(#21571,#21572,#21573,#21574,#21575,#21576));
#5243=EDGE_LOOP('',(#21577,#21578,#21579,#21580));
#5244=EDGE_LOOP('',(#21581,#21582,#21583,#21584,#21585));
#5245=EDGE_LOOP('',(#21586,#21587,#21588,#21589,#21590,#21591));
#5246=EDGE_LOOP('',(#21592,#21593,#21594,#21595,#21596));
#5247=EDGE_LOOP('',(#21597,#21598,#21599,#21600,#21601));
#5248=EDGE_LOOP('',(#21602,#21603,#21604,#21605,#21606,#21607,#21608));
#5249=EDGE_LOOP('',(#21609,#21610,#21611,#21612,#21613));
#5250=EDGE_LOOP('',(#21614,#21615,#21616,#21617,#21618,#21619));
#5251=EDGE_LOOP('',(#21620,#21621,#21622,#21623));
#5252=EDGE_LOOP('',(#21624,#21625,#21626,#21627,#21628,#21629));
#5253=EDGE_LOOP('',(#21630,#21631,#21632,#21633,#21634));
#5254=EDGE_LOOP('',(#21635,#21636,#21637,#21638,#21639,#21640));
#5255=EDGE_LOOP('',(#21641,#21642,#21643,#21644,#21645));
#5256=EDGE_LOOP('',(#21646,#21647,#21648,#21649,#21650,#21651,#21652,#21653,
#21654));
#5257=EDGE_LOOP('',(#21655,#21656,#21657,#21658,#21659));
#5258=EDGE_LOOP('',(#21660,#21661,#21662,#21663,#21664,#21665));
#5259=EDGE_LOOP('',(#21666,#21667,#21668,#21669));
#5260=EDGE_LOOP('',(#21670,#21671,#21672,#21673,#21674));
#5261=EDGE_LOOP('',(#21675,#21676,#21677,#21678,#21679,#21680,#21681,#21682,
#21683));
#5262=EDGE_LOOP('',(#21684,#21685,#21686,#21687,#21688,#21689,#21690,#21691));
#5263=EDGE_LOOP('',(#21692,#21693));
#5264=EDGE_LOOP('',(#21694,#21695));
#5265=EDGE_LOOP('',(#21696,#21697,#21698,#21699));
#5266=EDGE_LOOP('',(#21700,#21701,#21702,#21703));
#5267=EDGE_LOOP('',(#21704,#21705,#21706,#21707,#21708));
#5268=EDGE_LOOP('',(#21709,#21710,#21711,#21712,#21713));
#5269=EDGE_LOOP('',(#21714,#21715,#21716,#21717,#21718,#21719,#21720,#21721,
#21722));
#5270=EDGE_LOOP('',(#21723,#21724,#21725,#21726,#21727,#21728));
#5271=EDGE_LOOP('',(#21729,#21730,#21731,#21732,#21733,#21734));
#5272=EDGE_LOOP('',(#21735,#21736,#21737,#21738,#21739,#21740));
#5273=EDGE_LOOP('',(#21741,#21742,#21743,#21744,#21745,#21746,#21747));
#5274=EDGE_LOOP('',(#21748,#21749,#21750,#21751));
#5275=EDGE_LOOP('',(#21752,#21753,#21754,#21755,#21756,#21757,#21758,#21759,
#21760,#21761));
#5276=EDGE_LOOP('',(#21762,#21763,#21764,#21765,#21766,#21767,#21768,#21769,
#21770,#21771));
#5277=EDGE_LOOP('',(#21772,#21773,#21774,#21775,#21776,#21777,#21778,#21779,
#21780));
#5278=EDGE_LOOP('',(#21781,#21782,#21783,#21784,#21785,#21786,#21787,#21788));
#5279=EDGE_LOOP('',(#21789,#21790,#21791,#21792,#21793,#21794,#21795,#21796,
#21797,#21798));
#5280=EDGE_LOOP('',(#21799,#21800,#21801,#21802,#21803,#21804,#21805,#21806,
#21807,#21808,#21809));
#5281=EDGE_LOOP('',(#21810,#21811,#21812,#21813,#21814,#21815,#21816,#21817,
#21818,#21819));
#5282=EDGE_LOOP('',(#21820,#21821,#21822,#21823,#21824,#21825,#21826,#21827,
#21828,#21829));
#5283=EDGE_LOOP('',(#21830,#21831,#21832,#21833,#21834,#21835,#21836,#21837,
#21838,#21839,#21840,#21841));
#5284=EDGE_LOOP('',(#21842,#21843,#21844,#21845,#21846,#21847,#21848,#21849,
#21850,#21851,#21852));
#5285=EDGE_LOOP('',(#21853,#21854,#21855,#21856));
#5286=EDGE_LOOP('',(#21857,#21858,#21859,#21860,#21861,#21862,#21863,#21864,
#21865,#21866,#21867,#21868));
#5287=EDGE_LOOP('',(#21869,#21870,#21871,#21872,#21873,#21874,#21875,#21876));
#5288=EDGE_LOOP('',(#21877,#21878,#21879,#21880,#21881,#21882,#21883,#21884,
#21885));
#5289=EDGE_LOOP('',(#21886,#21887,#21888,#21889,#21890,#21891,#21892,#21893,
#21894));
#5290=EDGE_LOOP('',(#21895,#21896,#21897,#21898,#21899,#21900,#21901,#21902,
#21903));
#5291=EDGE_LOOP('',(#21904,#21905,#21906,#21907,#21908,#21909));
#5292=EDGE_LOOP('',(#21910,#21911,#21912,#21913,#21914,#21915,#21916,#21917,
#21918,#21919));
#5293=EDGE_LOOP('',(#21920,#21921,#21922,#21923,#21924,#21925,#21926,#21927,
#21928,#21929));
#5294=EDGE_LOOP('',(#21930,#21931,#21932,#21933));
#5295=EDGE_LOOP('',(#21934));
#5296=EDGE_LOOP('',(#21935,#21936,#21937,#21938));
#5297=EDGE_LOOP('',(#21939,#21940,#21941,#21942));
#5298=EDGE_LOOP('',(#21943,#21944,#21945,#21946));
#5299=EDGE_LOOP('',(#21947));
#5300=EDGE_LOOP('',(#21948));
#5301=EDGE_LOOP('',(#21949,#21950,#21951,#21952));
#5302=EDGE_LOOP('',(#21953));
#5303=EDGE_LOOP('',(#21954));
#5304=EDGE_LOOP('',(#21955,#21956,#21957,#21958));
#5305=EDGE_LOOP('',(#21959,#21960,#21961,#21962));
#5306=EDGE_LOOP('',(#21963));
#7223=LINE('',#41519,#10060);
#7224=LINE('',#41739,#10061);
#7225=LINE('',#41807,#10062);
#7226=LINE('',#41835,#10063);
#7227=LINE('',#42033,#10064);
#7228=LINE('',#42133,#10065);
#7229=LINE('',#42299,#10066);
#7230=LINE('',#42406,#10067);
#7231=LINE('',#42501,#10068);
#7232=LINE('',#42932,#10069);
#7233=LINE('',#43068,#10070);
#7234=LINE('',#43119,#10071);
#7235=LINE('',#43311,#10072);
#7236=LINE('',#43410,#10073);
#7237=LINE('',#43586,#10074);
#7238=LINE('',#43770,#10075);
#7239=LINE('',#43774,#10076);
#7240=LINE('',#43868,#10077);
#7241=LINE('',#43954,#10078);
#7242=LINE('',#44160,#10079);
#7243=LINE('',#44316,#10080);
#7244=LINE('',#44453,#10081);
#7245=LINE('',#44506,#10082);
#7246=LINE('',#44609,#10083);
#7247=LINE('',#44901,#10084);
#7248=LINE('',#45344,#10085);
#7249=LINE('',#45432,#10086);
#7250=LINE('',#45876,#10087);
#7251=LINE('',#45920,#10088);
#7252=LINE('',#46006,#10089);
#7253=LINE('',#46106,#10090);
#7254=LINE('',#46194,#10091);
#7255=LINE('',#46649,#10092);
#7256=LINE('',#46702,#10093);
#7257=LINE('',#46797,#10094);
#7258=LINE('',#46884,#10095);
#7259=LINE('',#46994,#10096);
#7260=LINE('',#47087,#10097);
#7261=LINE('',#47225,#10098);
#7262=LINE('',#47273,#10099);
#7263=LINE('',#47617,#10100);
#7264=LINE('',#47706,#10101);
#7265=LINE('',#47826,#10102);
#7266=LINE('',#47919,#10103);
#7267=LINE('',#48053,#10104);
#7268=LINE('',#48148,#10105);
#7269=LINE('',#48248,#10106);
#7270=LINE('',#48334,#10107);
#7271=LINE('',#48434,#10108);
#7272=LINE('',#48533,#10109);
#7273=LINE('',#48558,#10110);
#7274=LINE('',#48690,#10111);
#7275=LINE('',#48695,#10112);
#7276=LINE('',#48697,#10113);
#7277=LINE('',#48698,#10114);
#7278=LINE('',#48701,#10115);
#7279=LINE('',#48703,#10116);
#7280=LINE('',#48704,#10117);
#7281=LINE('',#49679,#10118);
#7282=LINE('',#56338,#10119);
#7283=LINE('',#66015,#10120);
#7284=LINE('',#68988,#10121);
#7285=LINE('',#68992,#10122);
#7286=LINE('',#68996,#10123);
#7287=LINE('',#69004,#10124);
#7288=LINE('',#69007,#10125);
#10060=VECTOR('',#34723,2.5);
#10061=VECTOR('',#34726,2.5);
#10062=VECTOR('',#34727,10.);
#10063=VECTOR('',#34730,2.5);
#10064=VECTOR('',#34733,2.5);
#10065=VECTOR('',#34736,2.5);
#10066=VECTOR('',#34739,2.5);
#10067=VECTOR('',#34742,2.5);
#10068=VECTOR('',#34745,2.5);
#10069=VECTOR('',#34748,2.5);
#10070=VECTOR('',#34751,2.5);
#10071=VECTOR('',#34754,2.5);
#10072=VECTOR('',#34757,2.5);
#10073=VECTOR('',#34760,2.5);
#10074=VECTOR('',#34763,2.5);
#10075=VECTOR('',#34766,2.5);
#10076=VECTOR('',#34769,2.5);
#10077=VECTOR('',#34772,2.5);
#10078=VECTOR('',#34775,2.5);
#10079=VECTOR('',#34778,2.5);
#10080=VECTOR('',#34781,2.5);
#10081=VECTOR('',#34784,2.5);
#10082=VECTOR('',#34787,2.5);
#10083=VECTOR('',#34790,2.5);
#10084=VECTOR('',#34793,2.5);
#10085=VECTOR('',#34796,2.5);
#10086=VECTOR('',#34799,2.5);
#10087=VECTOR('',#34802,2.5);
#10088=VECTOR('',#34805,2.5);
#10089=VECTOR('',#34808,2.5);
#10090=VECTOR('',#34811,2.5);
#10091=VECTOR('',#34814,2.5);
#10092=VECTOR('',#34817,2.5);
#10093=VECTOR('',#34820,2.5);
#10094=VECTOR('',#34823,2.5);
#10095=VECTOR('',#34826,2.5);
#10096=VECTOR('',#34829,2.5);
#10097=VECTOR('',#34832,2.5);
#10098=VECTOR('',#34835,2.5);
#10099=VECTOR('',#34838,2.5);
#10100=VECTOR('',#34841,2.5);
#10101=VECTOR('',#34844,2.5);
#10102=VECTOR('',#34847,2.5);
#10103=VECTOR('',#34850,2.5);
#10104=VECTOR('',#34853,2.5);
#10105=VECTOR('',#34856,2.5);
#10106=VECTOR('',#34859,2.5);
#10107=VECTOR('',#34862,2.5);
#10108=VECTOR('',#34867,2.5);
#10109=VECTOR('',#34868,2.5);
#10110=VECTOR('',#34869,10.);
#10111=VECTOR('',#34876,10.);
#10112=VECTOR('',#34881,10.);
#10113=VECTOR('',#34884,10.);
#10114=VECTOR('',#34885,10.);
#10115=VECTOR('',#34888,10.);
#10116=VECTOR('',#34889,10.);
#10117=VECTOR('',#34890,10.);
#10118=VECTOR('',#34891,10.);
#10119=VECTOR('',#34892,10.);
#10120=VECTOR('',#34893,10.);
#10121=VECTOR('',#34904,1.85);
#10122=VECTOR('',#34909,2.);
#10123=VECTOR('',#34914,2.35);
#10124=VECTOR('',#34925,2.);
#10125=VECTOR('',#34928,1.85);
#12814=CIRCLE('',#32405,2.5);
#12815=CIRCLE('',#32452,2.5);
#12816=CIRCLE('',#32455,2.);
#12817=CIRCLE('',#32457,2.);
#12818=CIRCLE('',#32462,1.7);
#12819=CIRCLE('',#32464,2.);
#12820=CIRCLE('',#32466,2.);
#12821=CIRCLE('',#32469,2.2);
#12822=CIRCLE('',#32471,2.);
#12823=CIRCLE('',#32473,2.);
#12824=CIRCLE('',#32475,1.7);
#13390=VERTEX_POINT('',#41517);
#13391=VERTEX_POINT('',#41518);
#13392=VERTEX_POINT('',#41521);
#13393=VERTEX_POINT('',#41544);
#13394=VERTEX_POINT('',#41738);
#13395=VERTEX_POINT('',#41740);
#13396=VERTEX_POINT('',#41753);
#13397=VERTEX_POINT('',#41806);
#13398=VERTEX_POINT('',#41833);
#13399=VERTEX_POINT('',#41834);
#13400=VERTEX_POINT('',#41880);
#13401=VERTEX_POINT('',#42031);
#13402=VERTEX_POINT('',#42032);
#13403=VERTEX_POINT('',#42131);
#13404=VERTEX_POINT('',#42132);
#13405=VERTEX_POINT('',#42134);
#13406=VERTEX_POINT('',#42179);
#13407=VERTEX_POINT('',#42297);
#13408=VERTEX_POINT('',#42298);
#13409=VERTEX_POINT('',#42300);
#13410=VERTEX_POINT('',#42404);
#13411=VERTEX_POINT('',#42405);
#13412=VERTEX_POINT('',#42407);
#13413=VERTEX_POINT('',#42499);
#13414=VERTEX_POINT('',#42500);
#13415=VERTEX_POINT('',#42502);
#13416=VERTEX_POINT('',#42744);
#13417=VERTEX_POINT('',#42930);
#13418=VERTEX_POINT('',#42931);
#13419=VERTEX_POINT('',#42975);
#13420=VERTEX_POINT('',#43021);
#13421=VERTEX_POINT('',#43046);
#13422=VERTEX_POINT('',#43067);
#13423=VERTEX_POINT('',#43069);
#13424=VERTEX_POINT('',#43117);
#13425=VERTEX_POINT('',#43118);
#13426=VERTEX_POINT('',#43164);
#13427=VERTEX_POINT('',#43197);
#13428=VERTEX_POINT('',#43309);
#13429=VERTEX_POINT('',#43310);
#13430=VERTEX_POINT('',#43312);
#13431=VERTEX_POINT('',#43408);
#13432=VERTEX_POINT('',#43409);
#13433=VERTEX_POINT('',#43411);
#13434=VERTEX_POINT('',#43456);
#13435=VERTEX_POINT('',#43461);
#13436=VERTEX_POINT('',#43584);
#13437=VERTEX_POINT('',#43585);
#13438=VERTEX_POINT('',#43587);
#13439=VERTEX_POINT('',#43679);
#13440=VERTEX_POINT('',#43680);
#13441=VERTEX_POINT('',#43725);
#13442=VERTEX_POINT('',#43772);
#13443=VERTEX_POINT('',#43773);
#13444=VERTEX_POINT('',#43775);
#13445=VERTEX_POINT('',#43822);
#13446=VERTEX_POINT('',#43866);
#13447=VERTEX_POINT('',#43867);
#13448=VERTEX_POINT('',#43952);
#13449=VERTEX_POINT('',#43953);
#13450=VERTEX_POINT('',#43955);
#13451=VERTEX_POINT('',#44000);
#13452=VERTEX_POINT('',#44158);
#13453=VERTEX_POINT('',#44159);
#13454=VERTEX_POINT('',#44203);
#13455=VERTEX_POINT('',#44314);
#13456=VERTEX_POINT('',#44315);
#13457=VERTEX_POINT('',#44404);
#13458=VERTEX_POINT('',#44437);
#13459=VERTEX_POINT('',#44452);
#13460=VERTEX_POINT('',#44454);
#13461=VERTEX_POINT('',#44504);
#13462=VERTEX_POINT('',#44505);
#13463=VERTEX_POINT('',#44547);
#13464=VERTEX_POINT('',#44607);
#13465=VERTEX_POINT('',#44608);
#13466=VERTEX_POINT('',#44610);
#13467=VERTEX_POINT('',#44623);
#13468=VERTEX_POINT('',#44845);
#13469=VERTEX_POINT('',#44899);
#13470=VERTEX_POINT('',#44900);
#13471=VERTEX_POINT('',#44902);
#13472=VERTEX_POINT('',#45185);
#13473=VERTEX_POINT('',#45342);
#13474=VERTEX_POINT('',#45343);
#13475=VERTEX_POINT('',#45430);
#13476=VERTEX_POINT('',#45431);
#13477=VERTEX_POINT('',#45433);
#13478=VERTEX_POINT('',#45440);
#13479=VERTEX_POINT('',#45779);
#13480=VERTEX_POINT('',#45825);
#13481=VERTEX_POINT('',#45862);
#13482=VERTEX_POINT('',#45875);
#13483=VERTEX_POINT('',#45918);
#13484=VERTEX_POINT('',#45919);
#13485=VERTEX_POINT('',#46004);
#13486=VERTEX_POINT('',#46005);
#13487=VERTEX_POINT('',#46007);
#13488=VERTEX_POINT('',#46058);
#13489=VERTEX_POINT('',#46104);
#13490=VERTEX_POINT('',#46105);
#13491=VERTEX_POINT('',#46192);
#13492=VERTEX_POINT('',#46193);
#13493=VERTEX_POINT('',#46195);
#13494=VERTEX_POINT('',#46512);
#13495=VERTEX_POINT('',#46541);
#13496=VERTEX_POINT('',#46648);
#13497=VERTEX_POINT('',#46650);
#13498=VERTEX_POINT('',#46700);
#13499=VERTEX_POINT('',#46701);
#13500=VERTEX_POINT('',#46747);
#13501=VERTEX_POINT('',#46795);
#13502=VERTEX_POINT('',#46796);
#13503=VERTEX_POINT('',#46838);
#13504=VERTEX_POINT('',#46882);
#13505=VERTEX_POINT('',#46883);
#13506=VERTEX_POINT('',#46885);
#13507=VERTEX_POINT('',#46922);
#13508=VERTEX_POINT('',#46940);
#13509=VERTEX_POINT('',#46992);
#13510=VERTEX_POINT('',#46993);
#13511=VERTEX_POINT('',#46995);
#13512=VERTEX_POINT('',#47085);
#13513=VERTEX_POINT('',#47086);
#13514=VERTEX_POINT('',#47088);
#13515=VERTEX_POINT('',#47139);
#13516=VERTEX_POINT('',#47185);
#13517=VERTEX_POINT('',#47224);
#13518=VERTEX_POINT('',#47271);
#13519=VERTEX_POINT('',#47272);
#13520=VERTEX_POINT('',#47274);
#13521=VERTEX_POINT('',#47279);
#13522=VERTEX_POINT('',#47615);
#13523=VERTEX_POINT('',#47616);
#13524=VERTEX_POINT('',#47660);
#13525=VERTEX_POINT('',#47704);
#13526=VERTEX_POINT('',#47705);
#13527=VERTEX_POINT('',#47707);
#13528=VERTEX_POINT('',#47748);
#13529=VERTEX_POINT('',#47824);
#13530=VERTEX_POINT('',#47825);
#13531=VERTEX_POINT('',#47871);
#13532=VERTEX_POINT('',#47917);
#13533=VERTEX_POINT('',#47918);
#13534=VERTEX_POINT('',#47920);
#13535=VERTEX_POINT('',#47925);
#13536=VERTEX_POINT('',#47960);
#13537=VERTEX_POINT('',#47996);
#13538=VERTEX_POINT('',#48039);
#13539=VERTEX_POINT('',#48051);
#13540=VERTEX_POINT('',#48052);
#13541=VERTEX_POINT('',#48054);
#13542=VERTEX_POINT('',#48146);
#13543=VERTEX_POINT('',#48147);
#13544=VERTEX_POINT('',#48149);
#13545=VERTEX_POINT('',#48200);
#13546=VERTEX_POINT('',#48246);
#13547=VERTEX_POINT('',#48247);
#13548=VERTEX_POINT('',#48332);
#13549=VERTEX_POINT('',#48333);
#13550=VERTEX_POINT('',#48335);
#13551=VERTEX_POINT('',#48431);
#13552=VERTEX_POINT('',#48433);
#13553=VERTEX_POINT('',#48435);
#13554=VERTEX_POINT('',#48482);
#13555=VERTEX_POINT('',#48532);
#13556=VERTEX_POINT('',#48534);
#13557=VERTEX_POINT('',#48557);
#13558=VERTEX_POINT('',#48582);
#13559=VERTEX_POINT('',#48631);
#13560=VERTEX_POINT('',#48666);
#13561=VERTEX_POINT('',#48671);
#13562=VERTEX_POINT('',#48687);
#13563=VERTEX_POINT('',#48688);
#13564=VERTEX_POINT('',#48692);
#13565=VERTEX_POINT('',#48693);
#13566=VERTEX_POINT('',#48700);
#13567=VERTEX_POINT('',#48702);
#13568=VERTEX_POINT('',#49448);
#13569=VERTEX_POINT('',#49678);
#13570=VERTEX_POINT('',#68983);
#13571=VERTEX_POINT('',#68986);
#13572=VERTEX_POINT('',#68990);
#13573=VERTEX_POINT('',#68995);
#13574=VERTEX_POINT('',#68999);
#13575=VERTEX_POINT('',#69002);
#13576=VERTEX_POINT('',#69006);
#16562=EDGE_CURVE('',#13390,#13391,#7223,.T.);
#16563=EDGE_CURVE('',#13391,#13391,#12814,.T.);
#16564=EDGE_CURVE('',#13390,#13392,#617,.T.);
#16565=EDGE_CURVE('',#13392,#13393,#618,.T.);
#16566=EDGE_CURVE('',#13393,#13394,#7224,.T.);
#16567=EDGE_CURVE('',#13394,#13395,#619,.T.);
#16568=EDGE_CURVE('',#13395,#13396,#620,.T.);
#16569=EDGE_CURVE('',#13396,#13397,#7225,.T.);
#16570=EDGE_CURVE('',#13397,#13390,#621,.T.);
#16571=EDGE_CURVE('',#13398,#13399,#7226,.T.);
#16572=EDGE_CURVE('',#13399,#13394,#622,.T.);
#16573=EDGE_CURVE('',#13393,#13400,#623,.T.);
#16574=EDGE_CURVE('',#13400,#13398,#624,.T.);
#16575=EDGE_CURVE('',#13401,#13402,#7227,.T.);
#16576=EDGE_CURVE('',#13402,#13399,#625,.T.);
#16577=EDGE_CURVE('',#13398,#13401,#626,.T.);
#16578=EDGE_CURVE('',#13403,#13404,#7228,.T.);
#16579=EDGE_CURVE('',#13404,#13405,#627,.T.);
#16580=EDGE_CURVE('',#13405,#13402,#628,.T.);
#16581=EDGE_CURVE('',#13401,#13406,#629,.T.);
#16582=EDGE_CURVE('',#13406,#13403,#630,.T.);
#16583=EDGE_CURVE('',#13407,#13408,#7229,.T.);
#16584=EDGE_CURVE('',#13408,#13409,#631,.T.);
#16585=EDGE_CURVE('',#13409,#13404,#632,.T.);
#16586=EDGE_CURVE('',#13403,#13407,#633,.T.);
#16587=EDGE_CURVE('',#13410,#13411,#7230,.T.);
#16588=EDGE_CURVE('',#13411,#13412,#634,.T.);
#16589=EDGE_CURVE('',#13412,#13408,#635,.T.);
#16590=EDGE_CURVE('',#13407,#13410,#636,.T.);
#16591=EDGE_CURVE('',#13413,#13414,#7231,.T.);
#16592=EDGE_CURVE('',#13414,#13415,#637,.T.);
#16593=EDGE_CURVE('',#13415,#13411,#638,.T.);
#16594=EDGE_CURVE('',#13410,#13416,#639,.T.);
#16595=EDGE_CURVE('',#13416,#13413,#640,.T.);
#16596=EDGE_CURVE('',#13417,#13418,#7232,.T.);
#16597=EDGE_CURVE('',#13418,#13414,#641,.T.);
#16598=EDGE_CURVE('',#13413,#13419,#642,.T.);
#16599=EDGE_CURVE('',#13419,#13417,#643,.T.);
#16600=EDGE_CURVE('',#13417,#13420,#644,.T.);
#16601=EDGE_CURVE('',#13420,#13421,#645,.T.);
#16602=EDGE_CURVE('',#13421,#13422,#7233,.T.);
#16603=EDGE_CURVE('',#13422,#13423,#646,.T.);
#16604=EDGE_CURVE('',#13423,#13418,#647,.T.);
#16605=EDGE_CURVE('',#13424,#13425,#7234,.T.);
#16606=EDGE_CURVE('',#13425,#13422,#648,.T.);
#16607=EDGE_CURVE('',#13421,#13426,#649,.T.);
#16608=EDGE_CURVE('',#13426,#13427,#650,.T.);
#16609=EDGE_CURVE('',#13427,#13424,#651,.T.);
#16610=EDGE_CURVE('',#13428,#13429,#7235,.T.);
#16611=EDGE_CURVE('',#13429,#13430,#652,.T.);
#16612=EDGE_CURVE('',#13430,#13425,#653,.T.);
#16613=EDGE_CURVE('',#13424,#13428,#654,.T.);
#16614=EDGE_CURVE('',#13431,#13432,#7236,.T.);
#16615=EDGE_CURVE('',#13432,#13433,#655,.T.);
#16616=EDGE_CURVE('',#13433,#13429,#656,.T.);
#16617=EDGE_CURVE('',#13428,#13434,#657,.T.);
#16618=EDGE_CURVE('',#13434,#13435,#658,.T.);
#16619=EDGE_CURVE('',#13435,#13431,#659,.T.);
#16620=EDGE_CURVE('',#13436,#13437,#7237,.T.);
#16621=EDGE_CURVE('',#13437,#13438,#660,.T.);
#16622=EDGE_CURVE('',#13438,#13432,#661,.T.);
#16623=EDGE_CURVE('',#13431,#13436,#662,.T.);
#16624=EDGE_CURVE('',#13439,#13440,#663,.T.);
#16625=EDGE_CURVE('',#13440,#13437,#664,.T.);
#16626=EDGE_CURVE('',#13436,#13441,#665,.T.);
#16627=EDGE_CURVE('',#13441,#13439,#7238,.T.);
#16628=EDGE_CURVE('',#13442,#13443,#7239,.T.);
#16629=EDGE_CURVE('',#13443,#13444,#666,.T.);
#16630=EDGE_CURVE('',#13444,#13439,#667,.T.);
#16631=EDGE_CURVE('',#13441,#13445,#668,.T.);
#16632=EDGE_CURVE('',#13445,#13442,#669,.T.);
#16633=EDGE_CURVE('',#13446,#13447,#7240,.T.);
#16634=EDGE_CURVE('',#13447,#13443,#670,.T.);
#16635=EDGE_CURVE('',#13442,#13446,#671,.T.);
#16636=EDGE_CURVE('',#13448,#13449,#7241,.T.);
#16637=EDGE_CURVE('',#13449,#13450,#672,.T.);
#16638=EDGE_CURVE('',#13450,#13447,#673,.T.);
#16639=EDGE_CURVE('',#13446,#13451,#674,.T.);
#16640=EDGE_CURVE('',#13451,#13448,#675,.T.);
#16641=EDGE_CURVE('',#13452,#13453,#7242,.T.);
#16642=EDGE_CURVE('',#13453,#13449,#676,.T.);
#16643=EDGE_CURVE('',#13448,#13454,#677,.T.);
#16644=EDGE_CURVE('',#13454,#13452,#678,.T.);
#16645=EDGE_CURVE('',#13455,#13456,#7243,.T.);
#16646=EDGE_CURVE('',#13456,#13453,#679,.T.);
#16647=EDGE_CURVE('',#13452,#13455,#680,.T.);
#16648=EDGE_CURVE('',#13455,#13457,#681,.T.);
#16649=EDGE_CURVE('',#13457,#13458,#682,.T.);
#16650=EDGE_CURVE('',#13458,#13459,#7244,.T.);
#16651=EDGE_CURVE('',#13459,#13460,#683,.T.);
#16652=EDGE_CURVE('',#13460,#13456,#684,.T.);
#16653=EDGE_CURVE('',#13461,#13462,#7245,.T.);
#16654=EDGE_CURVE('',#13462,#13459,#685,.T.);
#16655=EDGE_CURVE('',#13458,#13463,#686,.T.);
#16656=EDGE_CURVE('',#13463,#13461,#687,.T.);
#16657=EDGE_CURVE('',#13464,#13465,#7246,.T.);
#16658=EDGE_CURVE('',#13465,#13466,#688,.T.);
#16659=EDGE_CURVE('',#13466,#13467,#689,.T.);
#16660=EDGE_CURVE('',#13467,#13462,#690,.T.);
#16661=EDGE_CURVE('',#13461,#13468,#691,.T.);
#16662=EDGE_CURVE('',#13468,#13464,#692,.T.);
#16663=EDGE_CURVE('',#13469,#13470,#7247,.T.);
#16664=EDGE_CURVE('',#13470,#13471,#693,.T.);
#16665=EDGE_CURVE('',#13471,#13465,#694,.T.);
#16666=EDGE_CURVE('',#13464,#13472,#695,.T.);
#16667=EDGE_CURVE('',#13472,#13469,#696,.T.);
#16668=EDGE_CURVE('',#13473,#13474,#7248,.T.);
#16669=EDGE_CURVE('',#13474,#13470,#697,.T.);
#16670=EDGE_CURVE('',#13469,#13473,#698,.T.);
#16671=EDGE_CURVE('',#13475,#13476,#7249,.T.);
#16672=EDGE_CURVE('',#13476,#13477,#699,.T.);
#16673=EDGE_CURVE('',#13477,#13478,#700,.T.);
#16674=EDGE_CURVE('',#13478,#13474,#701,.T.);
#16675=EDGE_CURVE('',#13473,#13479,#702,.T.);
#16676=EDGE_CURVE('',#13479,#13475,#703,.T.);
#16677=EDGE_CURVE('',#13475,#13480,#704,.T.);
#16678=EDGE_CURVE('',#13480,#13481,#705,.T.);
#16679=EDGE_CURVE('',#13481,#13482,#7250,.T.);
#16680=EDGE_CURVE('',#13482,#13476,#706,.T.);
#16681=EDGE_CURVE('',#13483,#13484,#7251,.T.);
#16682=EDGE_CURVE('',#13484,#13482,#707,.T.);
#16683=EDGE_CURVE('',#13481,#13483,#708,.T.);
#16684=EDGE_CURVE('',#13485,#13486,#7252,.T.);
#16685=EDGE_CURVE('',#13486,#13487,#709,.T.);
#16686=EDGE_CURVE('',#13487,#13484,#710,.T.);
#16687=EDGE_CURVE('',#13483,#13488,#711,.T.);
#16688=EDGE_CURVE('',#13488,#13485,#712,.T.);
#16689=EDGE_CURVE('',#13489,#13490,#7253,.T.);
#16690=EDGE_CURVE('',#13490,#13486,#713,.T.);
#16691=EDGE_CURVE('',#13485,#13489,#714,.T.);
#16692=EDGE_CURVE('',#13491,#13492,#7254,.T.);
#16693=EDGE_CURVE('',#13492,#13493,#715,.T.);
#16694=EDGE_CURVE('',#13493,#13490,#716,.T.);
#16695=EDGE_CURVE('',#13489,#13491,#717,.T.);
#16696=EDGE_CURVE('',#13491,#13494,#718,.T.);
#16697=EDGE_CURVE('',#13494,#13495,#719,.T.);
#16698=EDGE_CURVE('',#13495,#13496,#7255,.T.);
#16699=EDGE_CURVE('',#13496,#13497,#720,.T.);
#16700=EDGE_CURVE('',#13497,#13492,#721,.T.);
#16701=EDGE_CURVE('',#13498,#13499,#7256,.T.);
#16702=EDGE_CURVE('',#13499,#13496,#722,.T.);
#16703=EDGE_CURVE('',#13495,#13500,#723,.T.);
#16704=EDGE_CURVE('',#13500,#13498,#724,.T.);
#16705=EDGE_CURVE('',#13501,#13502,#7257,.T.);
#16706=EDGE_CURVE('',#13502,#13499,#725,.T.);
#16707=EDGE_CURVE('',#13498,#13503,#726,.T.);
#16708=EDGE_CURVE('',#13503,#13501,#727,.T.);
#16709=EDGE_CURVE('',#13504,#13505,#7258,.T.);
#16710=EDGE_CURVE('',#13505,#13506,#728,.T.);
#16711=EDGE_CURVE('',#13506,#13507,#729,.T.);
#16712=EDGE_CURVE('',#13507,#13502,#730,.T.);
#16713=EDGE_CURVE('',#13501,#13508,#731,.T.);
#16714=EDGE_CURVE('',#13508,#13504,#732,.T.);
#16715=EDGE_CURVE('',#13509,#13510,#7259,.T.);
#16716=EDGE_CURVE('',#13510,#13511,#733,.T.);
#16717=EDGE_CURVE('',#13511,#13505,#734,.T.);
#16718=EDGE_CURVE('',#13504,#13509,#735,.T.);
#16719=EDGE_CURVE('',#13512,#13513,#7260,.T.);
#16720=EDGE_CURVE('',#13513,#13514,#736,.T.);
#16721=EDGE_CURVE('',#13514,#13510,#737,.T.);
#16722=EDGE_CURVE('',#13509,#13515,#738,.T.);
#16723=EDGE_CURVE('',#13515,#13512,#739,.T.);
#16724=EDGE_CURVE('',#13512,#13516,#740,.T.);
#16725=EDGE_CURVE('',#13516,#13517,#7261,.T.);
#16726=EDGE_CURVE('',#13517,#13513,#741,.T.);
#16727=EDGE_CURVE('',#13518,#13519,#7262,.T.);
#16728=EDGE_CURVE('',#13519,#13520,#742,.T.);
#16729=EDGE_CURVE('',#13520,#13521,#743,.T.);
#16730=EDGE_CURVE('',#13521,#13517,#744,.T.);
#16731=EDGE_CURVE('',#13516,#13518,#745,.T.);
#16732=EDGE_CURVE('',#13522,#13523,#7263,.T.);
#16733=EDGE_CURVE('',#13523,#13519,#746,.T.);
#16734=EDGE_CURVE('',#13518,#13524,#747,.T.);
#16735=EDGE_CURVE('',#13524,#13522,#748,.T.);
#16736=EDGE_CURVE('',#13525,#13526,#7264,.T.);
#16737=EDGE_CURVE('',#13526,#13527,#749,.T.);
#16738=EDGE_CURVE('',#13527,#13528,#750,.T.);
#16739=EDGE_CURVE('',#13528,#13523,#751,.T.);
#16740=EDGE_CURVE('',#13522,#13525,#752,.T.);
#16741=EDGE_CURVE('',#13529,#13530,#7265,.T.);
#16742=EDGE_CURVE('',#13530,#13526,#753,.T.);
#16743=EDGE_CURVE('',#13525,#13531,#754,.T.);
#16744=EDGE_CURVE('',#13531,#13529,#755,.T.);
#16745=EDGE_CURVE('',#13532,#13533,#7266,.T.);
#16746=EDGE_CURVE('',#13533,#13534,#756,.T.);
#16747=EDGE_CURVE('',#13534,#13535,#757,.T.);
#16748=EDGE_CURVE('',#13535,#13536,#758,.T.);
#16749=EDGE_CURVE('',#13536,#13530,#759,.T.);
#16750=EDGE_CURVE('',#13529,#13537,#760,.T.);
#16751=EDGE_CURVE('',#13537,#13538,#761,.T.);
#16752=EDGE_CURVE('',#13538,#13532,#762,.T.);
#16753=EDGE_CURVE('',#13539,#13540,#7267,.T.);
#16754=EDGE_CURVE('',#13540,#13541,#763,.T.);
#16755=EDGE_CURVE('',#13541,#13533,#764,.T.);
#16756=EDGE_CURVE('',#13532,#13539,#765,.T.);
#16757=EDGE_CURVE('',#13542,#13543,#7268,.T.);
#16758=EDGE_CURVE('',#13543,#13544,#766,.T.);
#16759=EDGE_CURVE('',#13544,#13540,#767,.T.);
#16760=EDGE_CURVE('',#13539,#13545,#768,.T.);
#16761=EDGE_CURVE('',#13545,#13542,#769,.T.);
#16762=EDGE_CURVE('',#13546,#13547,#7269,.T.);
#16763=EDGE_CURVE('',#13547,#13543,#770,.T.);
#16764=EDGE_CURVE('',#13542,#13546,#771,.T.);
#16765=EDGE_CURVE('',#13548,#13549,#7270,.T.);
#16766=EDGE_CURVE('',#13549,#13550,#772,.T.);
#16767=EDGE_CURVE('',#13550,#13547,#773,.T.);
#16768=EDGE_CURVE('',#13546,#13548,#774,.T.);
#16769=EDGE_CURVE('',#13551,#13551,#12815,.T.);
#16770=EDGE_CURVE('',#13551,#13552,#7271,.T.);
#16771=EDGE_CURVE('',#13552,#13553,#775,.F.);
#16772=EDGE_CURVE('',#13553,#13554,#776,.T.);
#16773=EDGE_CURVE('',#13555,#13554,#7272,.T.);
#16774=EDGE_CURVE('',#13555,#13556,#777,.T.);
#16775=EDGE_CURVE('',#13556,#13557,#7273,.T.);
#16776=EDGE_CURVE('',#13557,#13552,#778,.F.);
#16777=EDGE_CURVE('',#13554,#13558,#779,.T.);
#16778=EDGE_CURVE('',#13558,#13549,#780,.T.);
#16779=EDGE_CURVE('',#13548,#13559,#781,.T.);
#16780=EDGE_CURVE('',#13560,#13559,#782,.T.);
#16781=EDGE_CURVE('',#13560,#13561,#783,.T.);
#16782=EDGE_CURVE('',#13561,#13555,#784,.T.);
#16783=EDGE_CURVE('',#13562,#13563,#12816,.T.);
#16784=EDGE_CURVE('',#13563,#13562,#7274,.T.);
#16785=EDGE_CURVE('',#13564,#13565,#12817,.T.);
#16786=EDGE_CURVE('',#13565,#13564,#7275,.T.);
#16787=EDGE_CURVE('',#13565,#13562,#7276,.T.);
#16788=EDGE_CURVE('',#13563,#13564,#7277,.T.);
#16789=EDGE_CURVE('',#13566,#13396,#7278,.T.);
#16790=EDGE_CURVE('',#13567,#13566,#7279,.T.);
#16791=EDGE_CURVE('',#13397,#13567,#7280,.T.);
#16792=EDGE_CURVE('',#13392,#13567,#785,.T.);
#16793=EDGE_CURVE('',#13400,#13566,#786,.T.);
#16794=EDGE_CURVE('',#13568,#13553,#787,.T.);
#16795=EDGE_CURVE('',#13569,#13568,#7281,.T.);
#16796=EDGE_CURVE('',#13569,#13558,#788,.T.);
#16797=EDGE_CURVE('',#13537,#13527,#789,.T.);
#16798=EDGE_CURVE('',#13531,#13521,#790,.T.);
#16799=EDGE_CURVE('',#13508,#13497,#791,.T.);
#16800=EDGE_CURVE('',#13503,#13493,#792,.T.);
#16801=EDGE_CURVE('',#13480,#13471,#793,.T.);
#16802=EDGE_CURVE('',#13479,#13466,#794,.T.);
#16803=EDGE_CURVE('',#13454,#13444,#795,.T.);
#16804=EDGE_CURVE('',#13451,#13440,#796,.T.);
#16805=EDGE_CURVE('',#13406,#13395,#797,.T.);
#16806=EDGE_CURVE('',#13568,#13557,#7282,.T.);
#16807=EDGE_CURVE('',#13545,#13535,#798,.T.);
#16808=EDGE_CURVE('',#13515,#13506,#799,.T.);
#16809=EDGE_CURVE('',#13488,#13477,#800,.T.);
#16810=EDGE_CURVE('',#13457,#13450,#801,.T.);
#16811=EDGE_CURVE('',#13435,#13423,#802,.T.);
#16812=EDGE_CURVE('',#13426,#13415,#803,.T.);
#16813=EDGE_CURVE('',#13559,#13544,#804,.T.);
#16814=EDGE_CURVE('',#13524,#13514,#805,.T.);
#16815=EDGE_CURVE('',#13494,#13487,#806,.T.);
#16816=EDGE_CURVE('',#13472,#13460,#807,.T.);
#16817=EDGE_CURVE('',#13445,#13433,#808,.T.);
#16818=EDGE_CURVE('',#13556,#13569,#7283,.T.);
#16819=EDGE_CURVE('',#13420,#13412,#809,.T.);
#16820=EDGE_CURVE('',#13416,#13405,#810,.T.);
#16821=EDGE_CURVE('',#13570,#13570,#12818,.T.);
#16822=EDGE_CURVE('',#13571,#13571,#12819,.T.);
#16823=EDGE_CURVE('',#13571,#13570,#7284,.T.);
#16824=EDGE_CURVE('',#13572,#13572,#12820,.T.);
#16825=EDGE_CURVE('',#13572,#13571,#7285,.T.);
#16826=EDGE_CURVE('',#13551,#13573,#7286,.T.);
#16827=EDGE_CURVE('',#13573,#13573,#12821,.T.);
#16828=EDGE_CURVE('',#13574,#13574,#12822,.T.);
#16829=EDGE_CURVE('',#13575,#13575,#12823,.T.);
#16830=EDGE_CURVE('',#13575,#13574,#7287,.T.);
#16831=EDGE_CURVE('',#13575,#13576,#7288,.T.);
#16832=EDGE_CURVE('',#13576,#13576,#12824,.T.);
#21422=ORIENTED_EDGE('',*,*,#16562,.T.);
#21423=ORIENTED_EDGE('',*,*,#16563,.T.);
#21424=ORIENTED_EDGE('',*,*,#16562,.F.);
#21425=ORIENTED_EDGE('',*,*,#16564,.T.);
#21426=ORIENTED_EDGE('',*,*,#16565,.T.);
#21427=ORIENTED_EDGE('',*,*,#16566,.T.);
#21428=ORIENTED_EDGE('',*,*,#16567,.T.);
#21429=ORIENTED_EDGE('',*,*,#16568,.T.);
#21430=ORIENTED_EDGE('',*,*,#16569,.T.);
#21431=ORIENTED_EDGE('',*,*,#16570,.T.);
#21432=ORIENTED_EDGE('',*,*,#16571,.T.);
#21433=ORIENTED_EDGE('',*,*,#16572,.T.);
#21434=ORIENTED_EDGE('',*,*,#16566,.F.);
#21435=ORIENTED_EDGE('',*,*,#16573,.T.);
#21436=ORIENTED_EDGE('',*,*,#16574,.T.);
#21437=ORIENTED_EDGE('',*,*,#16575,.T.);
#21438=ORIENTED_EDGE('',*,*,#16576,.T.);
#21439=ORIENTED_EDGE('',*,*,#16571,.F.);
#21440=ORIENTED_EDGE('',*,*,#16577,.T.);
#21441=ORIENTED_EDGE('',*,*,#16578,.T.);
#21442=ORIENTED_EDGE('',*,*,#16579,.T.);
#21443=ORIENTED_EDGE('',*,*,#16580,.T.);
#21444=ORIENTED_EDGE('',*,*,#16575,.F.);
#21445=ORIENTED_EDGE('',*,*,#16581,.T.);
#21446=ORIENTED_EDGE('',*,*,#16582,.T.);
#21447=ORIENTED_EDGE('',*,*,#16583,.T.);
#21448=ORIENTED_EDGE('',*,*,#16584,.T.);
#21449=ORIENTED_EDGE('',*,*,#16585,.T.);
#21450=ORIENTED_EDGE('',*,*,#16578,.F.);
#21451=ORIENTED_EDGE('',*,*,#16586,.T.);
#21452=ORIENTED_EDGE('',*,*,#16587,.T.);
#21453=ORIENTED_EDGE('',*,*,#16588,.T.);
#21454=ORIENTED_EDGE('',*,*,#16589,.T.);
#21455=ORIENTED_EDGE('',*,*,#16583,.F.);
#21456=ORIENTED_EDGE('',*,*,#16590,.T.);
#21457=ORIENTED_EDGE('',*,*,#16591,.T.);
#21458=ORIENTED_EDGE('',*,*,#16592,.T.);
#21459=ORIENTED_EDGE('',*,*,#16593,.T.);
#21460=ORIENTED_EDGE('',*,*,#16587,.F.);
#21461=ORIENTED_EDGE('',*,*,#16594,.T.);
#21462=ORIENTED_EDGE('',*,*,#16595,.T.);
#21463=ORIENTED_EDGE('',*,*,#16596,.T.);
#21464=ORIENTED_EDGE('',*,*,#16597,.T.);
#21465=ORIENTED_EDGE('',*,*,#16591,.F.);
#21466=ORIENTED_EDGE('',*,*,#16598,.T.);
#21467=ORIENTED_EDGE('',*,*,#16599,.T.);
#21468=ORIENTED_EDGE('',*,*,#16596,.F.);
#21469=ORIENTED_EDGE('',*,*,#16600,.T.);
#21470=ORIENTED_EDGE('',*,*,#16601,.T.);
#21471=ORIENTED_EDGE('',*,*,#16602,.T.);
#21472=ORIENTED_EDGE('',*,*,#16603,.T.);
#21473=ORIENTED_EDGE('',*,*,#16604,.T.);
#21474=ORIENTED_EDGE('',*,*,#16605,.T.);
#21475=ORIENTED_EDGE('',*,*,#16606,.T.);
#21476=ORIENTED_EDGE('',*,*,#16602,.F.);
#21477=ORIENTED_EDGE('',*,*,#16607,.T.);
#21478=ORIENTED_EDGE('',*,*,#16608,.T.);
#21479=ORIENTED_EDGE('',*,*,#16609,.T.);
#21480=ORIENTED_EDGE('',*,*,#16610,.T.);
#21481=ORIENTED_EDGE('',*,*,#16611,.T.);
#21482=ORIENTED_EDGE('',*,*,#16612,.T.);
#21483=ORIENTED_EDGE('',*,*,#16605,.F.);
#21484=ORIENTED_EDGE('',*,*,#16613,.T.);
#21485=ORIENTED_EDGE('',*,*,#16614,.T.);
#21486=ORIENTED_EDGE('',*,*,#16615,.T.);
#21487=ORIENTED_EDGE('',*,*,#16616,.T.);
#21488=ORIENTED_EDGE('',*,*,#16610,.F.);
#21489=ORIENTED_EDGE('',*,*,#16617,.T.);
#21490=ORIENTED_EDGE('',*,*,#16618,.T.);
#21491=ORIENTED_EDGE('',*,*,#16619,.T.);
#21492=ORIENTED_EDGE('',*,*,#16620,.T.);
#21493=ORIENTED_EDGE('',*,*,#16621,.T.);
#21494=ORIENTED_EDGE('',*,*,#16622,.T.);
#21495=ORIENTED_EDGE('',*,*,#16614,.F.);
#21496=ORIENTED_EDGE('',*,*,#16623,.T.);
#21497=ORIENTED_EDGE('',*,*,#16624,.T.);
#21498=ORIENTED_EDGE('',*,*,#16625,.T.);
#21499=ORIENTED_EDGE('',*,*,#16620,.F.);
#21500=ORIENTED_EDGE('',*,*,#16626,.T.);
#21501=ORIENTED_EDGE('',*,*,#16627,.T.);
#21502=ORIENTED_EDGE('',*,*,#16628,.T.);
#21503=ORIENTED_EDGE('',*,*,#16629,.T.);
#21504=ORIENTED_EDGE('',*,*,#16630,.T.);
#21505=ORIENTED_EDGE('',*,*,#16627,.F.);
#21506=ORIENTED_EDGE('',*,*,#16631,.T.);
#21507=ORIENTED_EDGE('',*,*,#16632,.T.);
#21508=ORIENTED_EDGE('',*,*,#16633,.T.);
#21509=ORIENTED_EDGE('',*,*,#16634,.T.);
#21510=ORIENTED_EDGE('',*,*,#16628,.F.);
#21511=ORIENTED_EDGE('',*,*,#16635,.T.);
#21512=ORIENTED_EDGE('',*,*,#16636,.T.);
#21513=ORIENTED_EDGE('',*,*,#16637,.T.);
#21514=ORIENTED_EDGE('',*,*,#16638,.T.);
#21515=ORIENTED_EDGE('',*,*,#16633,.F.);
#21516=ORIENTED_EDGE('',*,*,#16639,.T.);
#21517=ORIENTED_EDGE('',*,*,#16640,.T.);
#21518=ORIENTED_EDGE('',*,*,#16641,.T.);
#21519=ORIENTED_EDGE('',*,*,#16642,.T.);
#21520=ORIENTED_EDGE('',*,*,#16636,.F.);
#21521=ORIENTED_EDGE('',*,*,#16643,.T.);
#21522=ORIENTED_EDGE('',*,*,#16644,.T.);
#21523=ORIENTED_EDGE('',*,*,#16645,.T.);
#21524=ORIENTED_EDGE('',*,*,#16646,.T.);
#21525=ORIENTED_EDGE('',*,*,#16641,.F.);
#21526=ORIENTED_EDGE('',*,*,#16647,.T.);
#21527=ORIENTED_EDGE('',*,*,#16645,.F.);
#21528=ORIENTED_EDGE('',*,*,#16648,.T.);
#21529=ORIENTED_EDGE('',*,*,#16649,.T.);
#21530=ORIENTED_EDGE('',*,*,#16650,.T.);
#21531=ORIENTED_EDGE('',*,*,#16651,.T.);
#21532=ORIENTED_EDGE('',*,*,#16652,.T.);
#21533=ORIENTED_EDGE('',*,*,#16653,.T.);
#21534=ORIENTED_EDGE('',*,*,#16654,.T.);
#21535=ORIENTED_EDGE('',*,*,#16650,.F.);
#21536=ORIENTED_EDGE('',*,*,#16655,.T.);
#21537=ORIENTED_EDGE('',*,*,#16656,.T.);
#21538=ORIENTED_EDGE('',*,*,#16657,.T.);
#21539=ORIENTED_EDGE('',*,*,#16658,.T.);
#21540=ORIENTED_EDGE('',*,*,#16659,.T.);
#21541=ORIENTED_EDGE('',*,*,#16660,.T.);
#21542=ORIENTED_EDGE('',*,*,#16653,.F.);
#21543=ORIENTED_EDGE('',*,*,#16661,.T.);
#21544=ORIENTED_EDGE('',*,*,#16662,.T.);
#21545=ORIENTED_EDGE('',*,*,#16663,.T.);
#21546=ORIENTED_EDGE('',*,*,#16664,.T.);
#21547=ORIENTED_EDGE('',*,*,#16665,.T.);
#21548=ORIENTED_EDGE('',*,*,#16657,.F.);
#21549=ORIENTED_EDGE('',*,*,#16666,.T.);
#21550=ORIENTED_EDGE('',*,*,#16667,.T.);
#21551=ORIENTED_EDGE('',*,*,#16668,.T.);
#21552=ORIENTED_EDGE('',*,*,#16669,.T.);
#21553=ORIENTED_EDGE('',*,*,#16663,.F.);
#21554=ORIENTED_EDGE('',*,*,#16670,.T.);
#21555=ORIENTED_EDGE('',*,*,#16671,.T.);
#21556=ORIENTED_EDGE('',*,*,#16672,.T.);
#21557=ORIENTED_EDGE('',*,*,#16673,.T.);
#21558=ORIENTED_EDGE('',*,*,#16674,.T.);
#21559=ORIENTED_EDGE('',*,*,#16668,.F.);
#21560=ORIENTED_EDGE('',*,*,#16675,.T.);
#21561=ORIENTED_EDGE('',*,*,#16676,.T.);
#21562=ORIENTED_EDGE('',*,*,#16671,.F.);
#21563=ORIENTED_EDGE('',*,*,#16677,.T.);
#21564=ORIENTED_EDGE('',*,*,#16678,.T.);
#21565=ORIENTED_EDGE('',*,*,#16679,.T.);
#21566=ORIENTED_EDGE('',*,*,#16680,.T.);
#21567=ORIENTED_EDGE('',*,*,#16681,.T.);
#21568=ORIENTED_EDGE('',*,*,#16682,.T.);
#21569=ORIENTED_EDGE('',*,*,#16679,.F.);
#21570=ORIENTED_EDGE('',*,*,#16683,.T.);
#21571=ORIENTED_EDGE('',*,*,#16684,.T.);
#21572=ORIENTED_EDGE('',*,*,#16685,.T.);
#21573=ORIENTED_EDGE('',*,*,#16686,.T.);
#21574=ORIENTED_EDGE('',*,*,#16681,.F.);
#21575=ORIENTED_EDGE('',*,*,#16687,.T.);
#21576=ORIENTED_EDGE('',*,*,#16688,.T.);
#21577=ORIENTED_EDGE('',*,*,#16689,.T.);
#21578=ORIENTED_EDGE('',*,*,#16690,.T.);
#21579=ORIENTED_EDGE('',*,*,#16684,.F.);
#21580=ORIENTED_EDGE('',*,*,#16691,.T.);
#21581=ORIENTED_EDGE('',*,*,#16692,.T.);
#21582=ORIENTED_EDGE('',*,*,#16693,.T.);
#21583=ORIENTED_EDGE('',*,*,#16694,.T.);
#21584=ORIENTED_EDGE('',*,*,#16689,.F.);
#21585=ORIENTED_EDGE('',*,*,#16695,.T.);
#21586=ORIENTED_EDGE('',*,*,#16692,.F.);
#21587=ORIENTED_EDGE('',*,*,#16696,.T.);
#21588=ORIENTED_EDGE('',*,*,#16697,.T.);
#21589=ORIENTED_EDGE('',*,*,#16698,.T.);
#21590=ORIENTED_EDGE('',*,*,#16699,.T.);
#21591=ORIENTED_EDGE('',*,*,#16700,.T.);
#21592=ORIENTED_EDGE('',*,*,#16701,.T.);
#21593=ORIENTED_EDGE('',*,*,#16702,.T.);
#21594=ORIENTED_EDGE('',*,*,#16698,.F.);
#21595=ORIENTED_EDGE('',*,*,#16703,.T.);
#21596=ORIENTED_EDGE('',*,*,#16704,.T.);
#21597=ORIENTED_EDGE('',*,*,#16705,.T.);
#21598=ORIENTED_EDGE('',*,*,#16706,.T.);
#21599=ORIENTED_EDGE('',*,*,#16701,.F.);
#21600=ORIENTED_EDGE('',*,*,#16707,.T.);
#21601=ORIENTED_EDGE('',*,*,#16708,.T.);
#21602=ORIENTED_EDGE('',*,*,#16709,.T.);
#21603=ORIENTED_EDGE('',*,*,#16710,.T.);
#21604=ORIENTED_EDGE('',*,*,#16711,.T.);
#21605=ORIENTED_EDGE('',*,*,#16712,.T.);
#21606=ORIENTED_EDGE('',*,*,#16705,.F.);
#21607=ORIENTED_EDGE('',*,*,#16713,.T.);
#21608=ORIENTED_EDGE('',*,*,#16714,.T.);
#21609=ORIENTED_EDGE('',*,*,#16715,.T.);
#21610=ORIENTED_EDGE('',*,*,#16716,.T.);
#21611=ORIENTED_EDGE('',*,*,#16717,.T.);
#21612=ORIENTED_EDGE('',*,*,#16709,.F.);
#21613=ORIENTED_EDGE('',*,*,#16718,.T.);
#21614=ORIENTED_EDGE('',*,*,#16719,.T.);
#21615=ORIENTED_EDGE('',*,*,#16720,.T.);
#21616=ORIENTED_EDGE('',*,*,#16721,.T.);
#21617=ORIENTED_EDGE('',*,*,#16715,.F.);
#21618=ORIENTED_EDGE('',*,*,#16722,.T.);
#21619=ORIENTED_EDGE('',*,*,#16723,.T.);
#21620=ORIENTED_EDGE('',*,*,#16724,.T.);
#21621=ORIENTED_EDGE('',*,*,#16725,.T.);
#21622=ORIENTED_EDGE('',*,*,#16726,.T.);
#21623=ORIENTED_EDGE('',*,*,#16719,.F.);
#21624=ORIENTED_EDGE('',*,*,#16727,.T.);
#21625=ORIENTED_EDGE('',*,*,#16728,.T.);
#21626=ORIENTED_EDGE('',*,*,#16729,.T.);
#21627=ORIENTED_EDGE('',*,*,#16730,.T.);
#21628=ORIENTED_EDGE('',*,*,#16725,.F.);
#21629=ORIENTED_EDGE('',*,*,#16731,.T.);
#21630=ORIENTED_EDGE('',*,*,#16732,.T.);
#21631=ORIENTED_EDGE('',*,*,#16733,.T.);
#21632=ORIENTED_EDGE('',*,*,#16727,.F.);
#21633=ORIENTED_EDGE('',*,*,#16734,.T.);
#21634=ORIENTED_EDGE('',*,*,#16735,.T.);
#21635=ORIENTED_EDGE('',*,*,#16736,.T.);
#21636=ORIENTED_EDGE('',*,*,#16737,.T.);
#21637=ORIENTED_EDGE('',*,*,#16738,.T.);
#21638=ORIENTED_EDGE('',*,*,#16739,.T.);
#21639=ORIENTED_EDGE('',*,*,#16732,.F.);
#21640=ORIENTED_EDGE('',*,*,#16740,.T.);
#21641=ORIENTED_EDGE('',*,*,#16741,.T.);
#21642=ORIENTED_EDGE('',*,*,#16742,.T.);
#21643=ORIENTED_EDGE('',*,*,#16736,.F.);
#21644=ORIENTED_EDGE('',*,*,#16743,.T.);
#21645=ORIENTED_EDGE('',*,*,#16744,.T.);
#21646=ORIENTED_EDGE('',*,*,#16745,.T.);
#21647=ORIENTED_EDGE('',*,*,#16746,.T.);
#21648=ORIENTED_EDGE('',*,*,#16747,.T.);
#21649=ORIENTED_EDGE('',*,*,#16748,.T.);
#21650=ORIENTED_EDGE('',*,*,#16749,.T.);
#21651=ORIENTED_EDGE('',*,*,#16741,.F.);
#21652=ORIENTED_EDGE('',*,*,#16750,.T.);
#21653=ORIENTED_EDGE('',*,*,#16751,.T.);
#21654=ORIENTED_EDGE('',*,*,#16752,.T.);
#21655=ORIENTED_EDGE('',*,*,#16753,.T.);
#21656=ORIENTED_EDGE('',*,*,#16754,.T.);
#21657=ORIENTED_EDGE('',*,*,#16755,.T.);
#21658=ORIENTED_EDGE('',*,*,#16745,.F.);
#21659=ORIENTED_EDGE('',*,*,#16756,.T.);
#21660=ORIENTED_EDGE('',*,*,#16757,.T.);
#21661=ORIENTED_EDGE('',*,*,#16758,.T.);
#21662=ORIENTED_EDGE('',*,*,#16759,.T.);
#21663=ORIENTED_EDGE('',*,*,#16753,.F.);
#21664=ORIENTED_EDGE('',*,*,#16760,.T.);
#21665=ORIENTED_EDGE('',*,*,#16761,.T.);
#21666=ORIENTED_EDGE('',*,*,#16762,.T.);
#21667=ORIENTED_EDGE('',*,*,#16763,.T.);
#21668=ORIENTED_EDGE('',*,*,#16757,.F.);
#21669=ORIENTED_EDGE('',*,*,#16764,.T.);
#21670=ORIENTED_EDGE('',*,*,#16765,.T.);
#21671=ORIENTED_EDGE('',*,*,#16766,.T.);
#21672=ORIENTED_EDGE('',*,*,#16767,.T.);
#21673=ORIENTED_EDGE('',*,*,#16762,.F.);
#21674=ORIENTED_EDGE('',*,*,#16768,.T.);
#21675=ORIENTED_EDGE('',*,*,#16769,.F.);
#21676=ORIENTED_EDGE('',*,*,#16770,.T.);
#21677=ORIENTED_EDGE('',*,*,#16771,.T.);
#21678=ORIENTED_EDGE('',*,*,#16772,.T.);
#21679=ORIENTED_EDGE('',*,*,#16773,.F.);
#21680=ORIENTED_EDGE('',*,*,#16774,.T.);
#21681=ORIENTED_EDGE('',*,*,#16775,.T.);
#21682=ORIENTED_EDGE('',*,*,#16776,.T.);
#21683=ORIENTED_EDGE('',*,*,#16770,.F.);
#21684=ORIENTED_EDGE('',*,*,#16773,.T.);
#21685=ORIENTED_EDGE('',*,*,#16777,.T.);
#21686=ORIENTED_EDGE('',*,*,#16778,.T.);
#21687=ORIENTED_EDGE('',*,*,#16765,.F.);
#21688=ORIENTED_EDGE('',*,*,#16779,.T.);
#21689=ORIENTED_EDGE('',*,*,#16780,.F.);
#21690=ORIENTED_EDGE('',*,*,#16781,.T.);
#21691=ORIENTED_EDGE('',*,*,#16782,.T.);
#21692=ORIENTED_EDGE('',*,*,#16783,.F.);
#21693=ORIENTED_EDGE('',*,*,#16784,.F.);
#21694=ORIENTED_EDGE('',*,*,#16785,.F.);
#21695=ORIENTED_EDGE('',*,*,#16786,.F.);
#21696=ORIENTED_EDGE('',*,*,#16787,.F.);
#21697=ORIENTED_EDGE('',*,*,#16786,.T.);
#21698=ORIENTED_EDGE('',*,*,#16788,.F.);
#21699=ORIENTED_EDGE('',*,*,#16784,.T.);
#21700=ORIENTED_EDGE('',*,*,#16569,.F.);
#21701=ORIENTED_EDGE('',*,*,#16789,.F.);
#21702=ORIENTED_EDGE('',*,*,#16790,.F.);
#21703=ORIENTED_EDGE('',*,*,#16791,.F.);
#21704=ORIENTED_EDGE('',*,*,#16565,.F.);
#21705=ORIENTED_EDGE('',*,*,#16792,.T.);
#21706=ORIENTED_EDGE('',*,*,#16790,.T.);
#21707=ORIENTED_EDGE('',*,*,#16793,.F.);
#21708=ORIENTED_EDGE('',*,*,#16573,.F.);
#21709=ORIENTED_EDGE('',*,*,#16772,.F.);
#21710=ORIENTED_EDGE('',*,*,#16794,.F.);
#21711=ORIENTED_EDGE('',*,*,#16795,.F.);
#21712=ORIENTED_EDGE('',*,*,#16796,.T.);
#21713=ORIENTED_EDGE('',*,*,#16777,.F.);
#21714=ORIENTED_EDGE('',*,*,#16738,.F.);
#21715=ORIENTED_EDGE('',*,*,#16797,.F.);
#21716=ORIENTED_EDGE('',*,*,#16750,.F.);
#21717=ORIENTED_EDGE('',*,*,#16744,.F.);
#21718=ORIENTED_EDGE('',*,*,#16798,.T.);
#21719=ORIENTED_EDGE('',*,*,#16729,.F.);
#21720=ORIENTED_EDGE('',*,*,#16728,.F.);
#21721=ORIENTED_EDGE('',*,*,#16733,.F.);
#21722=ORIENTED_EDGE('',*,*,#16739,.F.);
#21723=ORIENTED_EDGE('',*,*,#16700,.F.);
#21724=ORIENTED_EDGE('',*,*,#16799,.F.);
#21725=ORIENTED_EDGE('',*,*,#16713,.F.);
#21726=ORIENTED_EDGE('',*,*,#16708,.F.);
#21727=ORIENTED_EDGE('',*,*,#16800,.T.);
#21728=ORIENTED_EDGE('',*,*,#16693,.F.);
#21729=ORIENTED_EDGE('',*,*,#16665,.F.);
#21730=ORIENTED_EDGE('',*,*,#16801,.F.);
#21731=ORIENTED_EDGE('',*,*,#16677,.F.);
#21732=ORIENTED_EDGE('',*,*,#16676,.F.);
#21733=ORIENTED_EDGE('',*,*,#16802,.T.);
#21734=ORIENTED_EDGE('',*,*,#16658,.F.);
#21735=ORIENTED_EDGE('',*,*,#16630,.F.);
#21736=ORIENTED_EDGE('',*,*,#16803,.F.);
#21737=ORIENTED_EDGE('',*,*,#16643,.F.);
#21738=ORIENTED_EDGE('',*,*,#16640,.F.);
#21739=ORIENTED_EDGE('',*,*,#16804,.T.);
#21740=ORIENTED_EDGE('',*,*,#16624,.F.);
#21741=ORIENTED_EDGE('',*,*,#16568,.F.);
#21742=ORIENTED_EDGE('',*,*,#16805,.F.);
#21743=ORIENTED_EDGE('',*,*,#16581,.F.);
#21744=ORIENTED_EDGE('',*,*,#16577,.F.);
#21745=ORIENTED_EDGE('',*,*,#16574,.F.);
#21746=ORIENTED_EDGE('',*,*,#16793,.T.);
#21747=ORIENTED_EDGE('',*,*,#16789,.T.);
#21748=ORIENTED_EDGE('',*,*,#16776,.F.);
#21749=ORIENTED_EDGE('',*,*,#16806,.F.);
#21750=ORIENTED_EDGE('',*,*,#16794,.T.);
#21751=ORIENTED_EDGE('',*,*,#16771,.F.);
#21752=ORIENTED_EDGE('',*,*,#16748,.F.);
#21753=ORIENTED_EDGE('',*,*,#16807,.F.);
#21754=ORIENTED_EDGE('',*,*,#16760,.F.);
#21755=ORIENTED_EDGE('',*,*,#16756,.F.);
#21756=ORIENTED_EDGE('',*,*,#16752,.F.);
#21757=ORIENTED_EDGE('',*,*,#16751,.F.);
#21758=ORIENTED_EDGE('',*,*,#16797,.T.);
#21759=ORIENTED_EDGE('',*,*,#16737,.F.);
#21760=ORIENTED_EDGE('',*,*,#16742,.F.);
#21761=ORIENTED_EDGE('',*,*,#16749,.F.);
#21762=ORIENTED_EDGE('',*,*,#16711,.F.);
#21763=ORIENTED_EDGE('',*,*,#16808,.F.);
#21764=ORIENTED_EDGE('',*,*,#16722,.F.);
#21765=ORIENTED_EDGE('',*,*,#16718,.F.);
#21766=ORIENTED_EDGE('',*,*,#16714,.F.);
#21767=ORIENTED_EDGE('',*,*,#16799,.T.);
#21768=ORIENTED_EDGE('',*,*,#16699,.F.);
#21769=ORIENTED_EDGE('',*,*,#16702,.F.);
#21770=ORIENTED_EDGE('',*,*,#16706,.F.);
#21771=ORIENTED_EDGE('',*,*,#16712,.F.);
#21772=ORIENTED_EDGE('',*,*,#16673,.F.);
#21773=ORIENTED_EDGE('',*,*,#16809,.F.);
#21774=ORIENTED_EDGE('',*,*,#16687,.F.);
#21775=ORIENTED_EDGE('',*,*,#16683,.F.);
#21776=ORIENTED_EDGE('',*,*,#16678,.F.);
#21777=ORIENTED_EDGE('',*,*,#16801,.T.);
#21778=ORIENTED_EDGE('',*,*,#16664,.F.);
#21779=ORIENTED_EDGE('',*,*,#16669,.F.);
#21780=ORIENTED_EDGE('',*,*,#16674,.F.);
#21781=ORIENTED_EDGE('',*,*,#16638,.F.);
#21782=ORIENTED_EDGE('',*,*,#16810,.F.);
#21783=ORIENTED_EDGE('',*,*,#16648,.F.);
#21784=ORIENTED_EDGE('',*,*,#16647,.F.);
#21785=ORIENTED_EDGE('',*,*,#16644,.F.);
#21786=ORIENTED_EDGE('',*,*,#16803,.T.);
#21787=ORIENTED_EDGE('',*,*,#16629,.F.);
#21788=ORIENTED_EDGE('',*,*,#16634,.F.);
#21789=ORIENTED_EDGE('',*,*,#16604,.F.);
#21790=ORIENTED_EDGE('',*,*,#16811,.F.);
#21791=ORIENTED_EDGE('',*,*,#16618,.F.);
#21792=ORIENTED_EDGE('',*,*,#16617,.F.);
#21793=ORIENTED_EDGE('',*,*,#16613,.F.);
#21794=ORIENTED_EDGE('',*,*,#16609,.F.);
#21795=ORIENTED_EDGE('',*,*,#16608,.F.);
#21796=ORIENTED_EDGE('',*,*,#16812,.T.);
#21797=ORIENTED_EDGE('',*,*,#16592,.F.);
#21798=ORIENTED_EDGE('',*,*,#16597,.F.);
#21799=ORIENTED_EDGE('',*,*,#16813,.F.);
#21800=ORIENTED_EDGE('',*,*,#16779,.F.);
#21801=ORIENTED_EDGE('',*,*,#16768,.F.);
#21802=ORIENTED_EDGE('',*,*,#16764,.F.);
#21803=ORIENTED_EDGE('',*,*,#16761,.F.);
#21804=ORIENTED_EDGE('',*,*,#16807,.T.);
#21805=ORIENTED_EDGE('',*,*,#16747,.F.);
#21806=ORIENTED_EDGE('',*,*,#16746,.F.);
#21807=ORIENTED_EDGE('',*,*,#16755,.F.);
#21808=ORIENTED_EDGE('',*,*,#16754,.F.);
#21809=ORIENTED_EDGE('',*,*,#16759,.F.);
#21810=ORIENTED_EDGE('',*,*,#16723,.F.);
#21811=ORIENTED_EDGE('',*,*,#16808,.T.);
#21812=ORIENTED_EDGE('',*,*,#16710,.F.);
#21813=ORIENTED_EDGE('',*,*,#16717,.F.);
#21814=ORIENTED_EDGE('',*,*,#16716,.F.);
#21815=ORIENTED_EDGE('',*,*,#16721,.F.);
#21816=ORIENTED_EDGE('',*,*,#16814,.F.);
#21817=ORIENTED_EDGE('',*,*,#16734,.F.);
#21818=ORIENTED_EDGE('',*,*,#16731,.F.);
#21819=ORIENTED_EDGE('',*,*,#16724,.F.);
#21820=ORIENTED_EDGE('',*,*,#16680,.F.);
#21821=ORIENTED_EDGE('',*,*,#16682,.F.);
#21822=ORIENTED_EDGE('',*,*,#16686,.F.);
#21823=ORIENTED_EDGE('',*,*,#16815,.F.);
#21824=ORIENTED_EDGE('',*,*,#16696,.F.);
#21825=ORIENTED_EDGE('',*,*,#16695,.F.);
#21826=ORIENTED_EDGE('',*,*,#16691,.F.);
#21827=ORIENTED_EDGE('',*,*,#16688,.F.);
#21828=ORIENTED_EDGE('',*,*,#16809,.T.);
#21829=ORIENTED_EDGE('',*,*,#16672,.F.);
#21830=ORIENTED_EDGE('',*,*,#16652,.F.);
#21831=ORIENTED_EDGE('',*,*,#16816,.F.);
#21832=ORIENTED_EDGE('',*,*,#16666,.F.);
#21833=ORIENTED_EDGE('',*,*,#16662,.F.);
#21834=ORIENTED_EDGE('',*,*,#16661,.F.);
#21835=ORIENTED_EDGE('',*,*,#16656,.F.);
#21836=ORIENTED_EDGE('',*,*,#16655,.F.);
#21837=ORIENTED_EDGE('',*,*,#16649,.F.);
#21838=ORIENTED_EDGE('',*,*,#16810,.T.);
#21839=ORIENTED_EDGE('',*,*,#16637,.F.);
#21840=ORIENTED_EDGE('',*,*,#16642,.F.);
#21841=ORIENTED_EDGE('',*,*,#16646,.F.);
#21842=ORIENTED_EDGE('',*,*,#16616,.F.);
#21843=ORIENTED_EDGE('',*,*,#16817,.F.);
#21844=ORIENTED_EDGE('',*,*,#16631,.F.);
#21845=ORIENTED_EDGE('',*,*,#16626,.F.);
#21846=ORIENTED_EDGE('',*,*,#16623,.F.);
#21847=ORIENTED_EDGE('',*,*,#16619,.F.);
#21848=ORIENTED_EDGE('',*,*,#16811,.T.);
#21849=ORIENTED_EDGE('',*,*,#16603,.F.);
#21850=ORIENTED_EDGE('',*,*,#16606,.F.);
#21851=ORIENTED_EDGE('',*,*,#16612,.F.);
#21852=ORIENTED_EDGE('',*,*,#16611,.F.);
#21853=ORIENTED_EDGE('',*,*,#16570,.F.);
#21854=ORIENTED_EDGE('',*,*,#16791,.T.);
#21855=ORIENTED_EDGE('',*,*,#16792,.F.);
#21856=ORIENTED_EDGE('',*,*,#16564,.F.);
#21857=ORIENTED_EDGE('',*,*,#16778,.F.);
#21858=ORIENTED_EDGE('',*,*,#16796,.F.);
#21859=ORIENTED_EDGE('',*,*,#16818,.F.);
#21860=ORIENTED_EDGE('',*,*,#16774,.F.);
#21861=ORIENTED_EDGE('',*,*,#16782,.F.);
#21862=ORIENTED_EDGE('',*,*,#16781,.F.);
#21863=ORIENTED_EDGE('',*,*,#16780,.T.);
#21864=ORIENTED_EDGE('',*,*,#16813,.T.);
#21865=ORIENTED_EDGE('',*,*,#16758,.F.);
#21866=ORIENTED_EDGE('',*,*,#16763,.F.);
#21867=ORIENTED_EDGE('',*,*,#16767,.F.);
#21868=ORIENTED_EDGE('',*,*,#16766,.F.);
#21869=ORIENTED_EDGE('',*,*,#16730,.F.);
#21870=ORIENTED_EDGE('',*,*,#16798,.F.);
#21871=ORIENTED_EDGE('',*,*,#16743,.F.);
#21872=ORIENTED_EDGE('',*,*,#16740,.F.);
#21873=ORIENTED_EDGE('',*,*,#16735,.F.);
#21874=ORIENTED_EDGE('',*,*,#16814,.T.);
#21875=ORIENTED_EDGE('',*,*,#16720,.F.);
#21876=ORIENTED_EDGE('',*,*,#16726,.F.);
#21877=ORIENTED_EDGE('',*,*,#16694,.F.);
#21878=ORIENTED_EDGE('',*,*,#16800,.F.);
#21879=ORIENTED_EDGE('',*,*,#16707,.F.);
#21880=ORIENTED_EDGE('',*,*,#16704,.F.);
#21881=ORIENTED_EDGE('',*,*,#16703,.F.);
#21882=ORIENTED_EDGE('',*,*,#16697,.F.);
#21883=ORIENTED_EDGE('',*,*,#16815,.T.);
#21884=ORIENTED_EDGE('',*,*,#16685,.F.);
#21885=ORIENTED_EDGE('',*,*,#16690,.F.);
#21886=ORIENTED_EDGE('',*,*,#16659,.F.);
#21887=ORIENTED_EDGE('',*,*,#16802,.F.);
#21888=ORIENTED_EDGE('',*,*,#16675,.F.);
#21889=ORIENTED_EDGE('',*,*,#16670,.F.);
#21890=ORIENTED_EDGE('',*,*,#16667,.F.);
#21891=ORIENTED_EDGE('',*,*,#16816,.T.);
#21892=ORIENTED_EDGE('',*,*,#16651,.F.);
#21893=ORIENTED_EDGE('',*,*,#16654,.F.);
#21894=ORIENTED_EDGE('',*,*,#16660,.F.);
#21895=ORIENTED_EDGE('',*,*,#16635,.F.);
#21896=ORIENTED_EDGE('',*,*,#16632,.F.);
#21897=ORIENTED_EDGE('',*,*,#16817,.T.);
#21898=ORIENTED_EDGE('',*,*,#16615,.F.);
#21899=ORIENTED_EDGE('',*,*,#16622,.F.);
#21900=ORIENTED_EDGE('',*,*,#16621,.F.);
#21901=ORIENTED_EDGE('',*,*,#16625,.F.);
#21902=ORIENTED_EDGE('',*,*,#16804,.F.);
#21903=ORIENTED_EDGE('',*,*,#16639,.F.);
#21904=ORIENTED_EDGE('',*,*,#16593,.F.);
#21905=ORIENTED_EDGE('',*,*,#16812,.F.);
#21906=ORIENTED_EDGE('',*,*,#16607,.F.);
#21907=ORIENTED_EDGE('',*,*,#16601,.F.);
#21908=ORIENTED_EDGE('',*,*,#16819,.T.);
#21909=ORIENTED_EDGE('',*,*,#16588,.F.);
#21910=ORIENTED_EDGE('',*,*,#16589,.F.);
#21911=ORIENTED_EDGE('',*,*,#16819,.F.);
#21912=ORIENTED_EDGE('',*,*,#16600,.F.);
#21913=ORIENTED_EDGE('',*,*,#16599,.F.);
#21914=ORIENTED_EDGE('',*,*,#16598,.F.);
#21915=ORIENTED_EDGE('',*,*,#16595,.F.);
#21916=ORIENTED_EDGE('',*,*,#16820,.T.);
#21917=ORIENTED_EDGE('',*,*,#16579,.F.);
#21918=ORIENTED_EDGE('',*,*,#16585,.F.);
#21919=ORIENTED_EDGE('',*,*,#16584,.F.);
#21920=ORIENTED_EDGE('',*,*,#16580,.F.);
#21921=ORIENTED_EDGE('',*,*,#16820,.F.);
#21922=ORIENTED_EDGE('',*,*,#16594,.F.);
#21923=ORIENTED_EDGE('',*,*,#16590,.F.);
#21924=ORIENTED_EDGE('',*,*,#16586,.F.);
#21925=ORIENTED_EDGE('',*,*,#16582,.F.);
#21926=ORIENTED_EDGE('',*,*,#16805,.T.);
#21927=ORIENTED_EDGE('',*,*,#16567,.F.);
#21928=ORIENTED_EDGE('',*,*,#16572,.F.);
#21929=ORIENTED_EDGE('',*,*,#16576,.F.);
#21930=ORIENTED_EDGE('',*,*,#16775,.F.);
#21931=ORIENTED_EDGE('',*,*,#16818,.T.);
#21932=ORIENTED_EDGE('',*,*,#16795,.T.);
#21933=ORIENTED_EDGE('',*,*,#16806,.T.);
#21934=ORIENTED_EDGE('',*,*,#16821,.F.);
#21935=ORIENTED_EDGE('',*,*,#16822,.F.);
#21936=ORIENTED_EDGE('',*,*,#16823,.T.);
#21937=ORIENTED_EDGE('',*,*,#16821,.T.);
#21938=ORIENTED_EDGE('',*,*,#16823,.F.);
#21939=ORIENTED_EDGE('',*,*,#16824,.F.);
#21940=ORIENTED_EDGE('',*,*,#16825,.T.);
#21941=ORIENTED_EDGE('',*,*,#16822,.T.);
#21942=ORIENTED_EDGE('',*,*,#16825,.F.);
#21943=ORIENTED_EDGE('',*,*,#16785,.T.);
#21944=ORIENTED_EDGE('',*,*,#16787,.T.);
#21945=ORIENTED_EDGE('',*,*,#16783,.T.);
#21946=ORIENTED_EDGE('',*,*,#16788,.T.);
#21947=ORIENTED_EDGE('',*,*,#16563,.F.);
#21948=ORIENTED_EDGE('',*,*,#16824,.T.);
#21949=ORIENTED_EDGE('',*,*,#16769,.T.);
#21950=ORIENTED_EDGE('',*,*,#16826,.T.);
#21951=ORIENTED_EDGE('',*,*,#16827,.F.);
#21952=ORIENTED_EDGE('',*,*,#16826,.F.);
#21953=ORIENTED_EDGE('',*,*,#16827,.T.);
#21954=ORIENTED_EDGE('',*,*,#16828,.F.);
#21955=ORIENTED_EDGE('',*,*,#16829,.F.);
#21956=ORIENTED_EDGE('',*,*,#16830,.T.);
#21957=ORIENTED_EDGE('',*,*,#16828,.T.);
#21958=ORIENTED_EDGE('',*,*,#16830,.F.);
#21959=ORIENTED_EDGE('',*,*,#16829,.T.);
#21960=ORIENTED_EDGE('',*,*,#16831,.T.);
#21961=ORIENTED_EDGE('',*,*,#16832,.F.);
#21962=ORIENTED_EDGE('',*,*,#16831,.F.);
#21963=ORIENTED_EDGE('',*,*,#16832,.T.);
#30286=CONICAL_SURFACE('',#32463,1.85,0.78539816339743);
#30287=CONICAL_SURFACE('',#32468,2.35,0.785398163397451);
#30288=CONICAL_SURFACE('',#32474,1.85,0.785398163397448);
#30418=ADVANCED_FACE('',(#3443),#1786,.T.);
#30419=ADVANCED_FACE('',(#3444),#1787,.T.);
#30420=ADVANCED_FACE('',(#3445),#1788,.T.);
#30421=ADVANCED_FACE('',(#3446),#1789,.T.);
#30422=ADVANCED_FACE('',(#3447),#1790,.T.);
#30423=ADVANCED_FACE('',(#3448),#1791,.T.);
#30424=ADVANCED_FACE('',(#3449),#1792,.T.);
#30425=ADVANCED_FACE('',(#3450),#1793,.T.);
#30426=ADVANCED_FACE('',(#3451),#1794,.T.);
#30427=ADVANCED_FACE('',(#3452),#1795,.T.);
#30428=ADVANCED_FACE('',(#3453),#1796,.T.);
#30429=ADVANCED_FACE('',(#3454),#1797,.T.);
#30430=ADVANCED_FACE('',(#3455),#1798,.T.);
#30431=ADVANCED_FACE('',(#3456),#1799,.T.);
#30432=ADVANCED_FACE('',(#3457),#1800,.T.);
#30433=ADVANCED_FACE('',(#3458),#1801,.T.);
#30434=ADVANCED_FACE('',(#3459),#1802,.T.);
#30435=ADVANCED_FACE('',(#3460),#1803,.T.);
#30436=ADVANCED_FACE('',(#3461),#1804,.T.);
#30437=ADVANCED_FACE('',(#3462),#1805,.T.);
#30438=ADVANCED_FACE('',(#3463),#1806,.T.);
#30439=ADVANCED_FACE('',(#3464),#1807,.T.);
#30440=ADVANCED_FACE('',(#3465),#1808,.T.);
#30441=ADVANCED_FACE('',(#3466),#1809,.T.);
#30442=ADVANCED_FACE('',(#3467),#1810,.T.);
#30443=ADVANCED_FACE('',(#3468),#1811,.T.);
#30444=ADVANCED_FACE('',(#3469),#1812,.T.);
#30445=ADVANCED_FACE('',(#3470),#1813,.T.);
#30446=ADVANCED_FACE('',(#3471),#1814,.T.);
#30447=ADVANCED_FACE('',(#3472),#1815,.T.);
#30448=ADVANCED_FACE('',(#3473),#1816,.T.);
#30449=ADVANCED_FACE('',(#3474),#1817,.T.);
#30450=ADVANCED_FACE('',(#3475),#1818,.T.);
#30451=ADVANCED_FACE('',(#3476),#1819,.T.);
#30452=ADVANCED_FACE('',(#3477),#1820,.T.);
#30453=ADVANCED_FACE('',(#3478),#1821,.T.);
#30454=ADVANCED_FACE('',(#3479),#1822,.T.);
#30455=ADVANCED_FACE('',(#3480),#1823,.T.);
#30456=ADVANCED_FACE('',(#3481),#1824,.T.);
#30457=ADVANCED_FACE('',(#3482),#1825,.T.);
#30458=ADVANCED_FACE('',(#3483),#1826,.T.);
#30459=ADVANCED_FACE('',(#3484),#1827,.T.);
#30460=ADVANCED_FACE('',(#3485),#1828,.T.);
#30461=ADVANCED_FACE('',(#3486),#1829,.T.);
#30462=ADVANCED_FACE('',(#3487),#1830,.T.);
#30463=ADVANCED_FACE('',(#3488),#1831,.T.);
#30464=ADVANCED_FACE('',(#3489),#1832,.T.);
#30465=ADVANCED_FACE('',(#3490),#1833,.T.);
#30466=ADVANCED_FACE('',(#3491),#2272,.F.);
#30467=ADVANCED_FACE('',(#3492),#2273,.F.);
#30468=ADVANCED_FACE('',(#3493),#2274,.T.);
#30469=ADVANCED_FACE('',(#3494),#2275,.F.);
#30470=ADVANCED_FACE('',(#3495),#304,.F.);
#30471=ADVANCED_FACE('',(#3496),#305,.F.);
#30472=ADVANCED_FACE('',(#3497),#306,.F.);
#30473=ADVANCED_FACE('',(#3498),#307,.F.);
#30474=ADVANCED_FACE('',(#3499),#308,.F.);
#30475=ADVANCED_FACE('',(#3500),#309,.F.);
#30476=ADVANCED_FACE('',(#3501),#310,.F.);
#30477=ADVANCED_FACE('',(#3502),#311,.F.);
#30478=ADVANCED_FACE('',(#3503),#312,.F.);
#30479=ADVANCED_FACE('',(#3504),#313,.F.);
#30480=ADVANCED_FACE('',(#3505),#314,.F.);
#30481=ADVANCED_FACE('',(#3506),#315,.F.);
#30482=ADVANCED_FACE('',(#3507),#316,.F.);
#30483=ADVANCED_FACE('',(#3508),#317,.F.);
#30484=ADVANCED_FACE('',(#3509),#318,.F.);
#30485=ADVANCED_FACE('',(#3510),#319,.F.);
#30486=ADVANCED_FACE('',(#3511),#320,.F.);
#30487=ADVANCED_FACE('',(#3512),#321,.F.);
#30488=ADVANCED_FACE('',(#3513),#322,.F.);
#30489=ADVANCED_FACE('',(#3514),#323,.F.);
#30490=ADVANCED_FACE('',(#3515),#324,.F.);
#30491=ADVANCED_FACE('',(#3516),#325,.F.);
#30492=ADVANCED_FACE('',(#3517),#326,.F.);
#30493=ADVANCED_FACE('',(#3518),#327,.F.);
#30494=ADVANCED_FACE('',(#3519),#328,.F.);
#30495=ADVANCED_FACE('',(#3520),#329,.F.);
#30496=ADVANCED_FACE('',(#3521),#330,.F.);
#30497=ADVANCED_FACE('',(#3522),#2276,.T.);
#30498=ADVANCED_FACE('',(#3523),#2277,.T.);
#30499=ADVANCED_FACE('',(#3524),#30286,.T.);
#30500=ADVANCED_FACE('',(#3525,#2034),#1834,.T.);
#30501=ADVANCED_FACE('',(#3526,#2035),#2278,.T.);
#30502=ADVANCED_FACE('',(#3527),#30287,.T.);
#30503=ADVANCED_FACE('',(#3528,#2036),#2279,.T.);
#30504=ADVANCED_FACE('',(#3529),#1835,.T.);
#30505=ADVANCED_FACE('',(#3530),#30288,.T.);
#30506=ADVANCED_FACE('',(#3531),#2280,.T.);
#32078=CLOSED_SHELL('',(#30418,#30419,#30420,#30421,#30422,#30423,#30424,
#30425,#30426,#30427,#30428,#30429,#30430,#30431,#30432,#30433,#30434,#30435,
#30436,#30437,#30438,#30439,#30440,#30441,#30442,#30443,#30444,#30445,#30446,
#30447,#30448,#30449,#30450,#30451,#30452,#30453,#30454,#30455,#30456,#30457,
#30458,#30459,#30460,#30461,#30462,#30463,#30464,#30465,#30466,#30467,#30468,
#30469,#30470,#30471,#30472,#30473,#30474,#30475,#30476,#30477,#30478,#30479,
#30480,#30481,#30482,#30483,#30484,#30485,#30486,#30487,#30488,#30489,#30490,
#30491,#30492,#30493,#30494,#30495,#30496,#30497,#30498,#30499,#30500,#30501,
#30502,#30503,#30504,#30505,#30506));
#32403=AXIS2_PLACEMENT_3D('',#41515,#34719,#34720);
#32404=AXIS2_PLACEMENT_3D('',#41516,#34721,#34722);
#32405=AXIS2_PLACEMENT_3D('',#41520,#34724,#34725);
#32406=AXIS2_PLACEMENT_3D('',#41832,#34728,#34729);
#32407=AXIS2_PLACEMENT_3D('',#42030,#34731,#34732);
#32408=AXIS2_PLACEMENT_3D('',#42130,#34734,#34735);
#32409=AXIS2_PLACEMENT_3D('',#42296,#34737,#34738);
#32410=AXIS2_PLACEMENT_3D('',#42403,#34740,#34741);
#32411=AXIS2_PLACEMENT_3D('',#42498,#34743,#34744);
#32412=AXIS2_PLACEMENT_3D('',#42929,#34746,#34747);
#32413=AXIS2_PLACEMENT_3D('',#43020,#34749,#34750);
#32414=AXIS2_PLACEMENT_3D('',#43116,#34752,#34753);
#32415=AXIS2_PLACEMENT_3D('',#43308,#34755,#34756);
#32416=AXIS2_PLACEMENT_3D('',#43407,#34758,#34759);
#32417=AXIS2_PLACEMENT_3D('',#43583,#34761,#34762);
#32418=AXIS2_PLACEMENT_3D('',#43678,#34764,#34765);
#32419=AXIS2_PLACEMENT_3D('',#43771,#34767,#34768);
#32420=AXIS2_PLACEMENT_3D('',#43865,#34770,#34771);
#32421=AXIS2_PLACEMENT_3D('',#43951,#34773,#34774);
#32422=AXIS2_PLACEMENT_3D('',#44157,#34776,#34777);
#32423=AXIS2_PLACEMENT_3D('',#44313,#34779,#34780);
#32424=AXIS2_PLACEMENT_3D('',#44403,#34782,#34783);
#32425=AXIS2_PLACEMENT_3D('',#44503,#34785,#34786);
#32426=AXIS2_PLACEMENT_3D('',#44606,#34788,#34789);
#32427=AXIS2_PLACEMENT_3D('',#44898,#34791,#34792);
#32428=AXIS2_PLACEMENT_3D('',#45341,#34794,#34795);
#32429=AXIS2_PLACEMENT_3D('',#45429,#34797,#34798);
#32430=AXIS2_PLACEMENT_3D('',#45824,#34800,#34801);
#32431=AXIS2_PLACEMENT_3D('',#45917,#34803,#34804);
#32432=AXIS2_PLACEMENT_3D('',#46003,#34806,#34807);
#32433=AXIS2_PLACEMENT_3D('',#46103,#34809,#34810);
#32434=AXIS2_PLACEMENT_3D('',#46191,#34812,#34813);
#32435=AXIS2_PLACEMENT_3D('',#46511,#34815,#34816);
#32436=AXIS2_PLACEMENT_3D('',#46699,#34818,#34819);
#32437=AXIS2_PLACEMENT_3D('',#46794,#34821,#34822);
#32438=AXIS2_PLACEMENT_3D('',#46881,#34824,#34825);
#32439=AXIS2_PLACEMENT_3D('',#46991,#34827,#34828);
#32440=AXIS2_PLACEMENT_3D('',#47084,#34830,#34831);
#32441=AXIS2_PLACEMENT_3D('',#47184,#34833,#34834);
#32442=AXIS2_PLACEMENT_3D('',#47270,#34836,#34837);
#32443=AXIS2_PLACEMENT_3D('',#47614,#34839,#34840);
#32444=AXIS2_PLACEMENT_3D('',#47703,#34842,#34843);
#32445=AXIS2_PLACEMENT_3D('',#47823,#34845,#34846);
#32446=AXIS2_PLACEMENT_3D('',#47916,#34848,#34849);
#32447=AXIS2_PLACEMENT_3D('',#48050,#34851,#34852);
#32448=AXIS2_PLACEMENT_3D('',#48145,#34854,#34855);
#32449=AXIS2_PLACEMENT_3D('',#48245,#34857,#34858);
#32450=AXIS2_PLACEMENT_3D('',#48331,#34860,#34861);
#32451=AXIS2_PLACEMENT_3D('',#48430,#34863,#34864);
#32452=AXIS2_PLACEMENT_3D('',#48432,#34865,#34866);
#32453=AXIS2_PLACEMENT_3D('',#48581,#34870,#34871);
#32454=AXIS2_PLACEMENT_3D('',#48686,#34872,#34873);
#32455=AXIS2_PLACEMENT_3D('',#48689,#34874,#34875);
#32456=AXIS2_PLACEMENT_3D('',#48691,#34877,#34878);
#32457=AXIS2_PLACEMENT_3D('',#48694,#34879,#34880);
#32458=AXIS2_PLACEMENT_3D('',#48696,#34882,#34883);
#32459=AXIS2_PLACEMENT_3D('',#48699,#34886,#34887);
#32460=AXIS2_PLACEMENT_3D('',#68981,#34894,#34895);
#32461=AXIS2_PLACEMENT_3D('',#68982,#34896,#34897);
#32462=AXIS2_PLACEMENT_3D('',#68984,#34898,#34899);
#32463=AXIS2_PLACEMENT_3D('',#68985,#34900,#34901);
#32464=AXIS2_PLACEMENT_3D('',#68987,#34902,#34903);
#32465=AXIS2_PLACEMENT_3D('',#68989,#34905,#34906);
#32466=AXIS2_PLACEMENT_3D('',#68991,#34907,#34908);
#32467=AXIS2_PLACEMENT_3D('',#68993,#34910,#34911);
#32468=AXIS2_PLACEMENT_3D('',#68994,#34912,#34913);
#32469=AXIS2_PLACEMENT_3D('',#68997,#34915,#34916);
#32470=AXIS2_PLACEMENT_3D('',#68998,#34917,#34918);
#32471=AXIS2_PLACEMENT_3D('',#69000,#34919,#34920);
#32472=AXIS2_PLACEMENT_3D('',#69001,#34921,#34922);
#32473=AXIS2_PLACEMENT_3D('',#69003,#34923,#34924);
#32474=AXIS2_PLACEMENT_3D('',#69005,#34926,#34927);
#32475=AXIS2_PLACEMENT_3D('',#69008,#34929,#34930);
#32476=AXIS2_PLACEMENT_3D('',#69009,#34931,#34932);
#34719=DIRECTION('axis',(0.,0.,1.));
#34720=DIRECTION('refdir',(1.,0.,0.));
#34721=DIRECTION('center_axis',(0.,-1.,0.));
#34722=DIRECTION('ref_axis',(1.,0.,0.));
#34723=DIRECTION('',(0.,1.,0.));
#34724=DIRECTION('center_axis',(0.,-1.,0.));
#34725=DIRECTION('ref_axis',(1.,0.,0.));
#34726=DIRECTION('',(0.,1.,0.));
#34727=DIRECTION('',(-0.0016684081382487,0.99998546068423,-0.00512784890894562));
#34728=DIRECTION('center_axis',(0.,-1.,0.));
#34729=DIRECTION('ref_axis',(1.,0.,0.));
#34730=DIRECTION('',(0.,1.,0.));
#34731=DIRECTION('center_axis',(0.,-1.,0.));
#34732=DIRECTION('ref_axis',(1.,0.,0.));
#34733=DIRECTION('',(0.,1.,0.));
#34734=DIRECTION('center_axis',(0.,-1.,0.));
#34735=DIRECTION('ref_axis',(1.,0.,0.));
#34736=DIRECTION('',(0.,1.,0.));
#34737=DIRECTION('center_axis',(0.,-1.,0.));
#34738=DIRECTION('ref_axis',(1.,0.,0.));
#34739=DIRECTION('',(0.,1.,0.));
#34740=DIRECTION('center_axis',(0.,-1.,0.));
#34741=DIRECTION('ref_axis',(1.,0.,0.));
#34742=DIRECTION('',(0.,1.,0.));
#34743=DIRECTION('center_axis',(0.,-1.,0.));
#34744=DIRECTION('ref_axis',(1.,0.,0.));
#34745=DIRECTION('',(0.,1.,0.));
#34746=DIRECTION('center_axis',(0.,-1.,0.));
#34747=DIRECTION('ref_axis',(1.,0.,0.));
#34748=DIRECTION('',(0.,1.,0.));
#34749=DIRECTION('center_axis',(0.,-1.,0.));
#34750=DIRECTION('ref_axis',(1.,0.,0.));
#34751=DIRECTION('',(0.,1.,0.));
#34752=DIRECTION('center_axis',(0.,-1.,0.));
#34753=DIRECTION('ref_axis',(1.,0.,0.));
#34754=DIRECTION('',(0.,1.,0.));
#34755=DIRECTION('center_axis',(0.,-1.,0.));
#34756=DIRECTION('ref_axis',(1.,0.,0.));
#34757=DIRECTION('',(0.,1.,0.));
#34758=DIRECTION('center_axis',(0.,-1.,0.));
#34759=DIRECTION('ref_axis',(1.,0.,0.));
#34760=DIRECTION('',(0.,1.,0.));
#34761=DIRECTION('center_axis',(0.,-1.,0.));
#34762=DIRECTION('ref_axis',(1.,0.,0.));
#34763=DIRECTION('',(0.,1.,0.));
#34764=DIRECTION('center_axis',(0.,-1.,0.));
#34765=DIRECTION('ref_axis',(1.,0.,0.));
#34766=DIRECTION('',(0.,1.,0.));
#34767=DIRECTION('center_axis',(0.,-1.,0.));
#34768=DIRECTION('ref_axis',(1.,0.,0.));
#34769=DIRECTION('',(0.,1.,0.));
#34770=DIRECTION('center_axis',(0.,-1.,0.));
#34771=DIRECTION('ref_axis',(1.,0.,0.));
#34772=DIRECTION('',(0.,1.,0.));
#34773=DIRECTION('center_axis',(0.,-1.,0.));
#34774=DIRECTION('ref_axis',(1.,0.,0.));
#34775=DIRECTION('',(0.,1.,0.));
#34776=DIRECTION('center_axis',(0.,-1.,0.));
#34777=DIRECTION('ref_axis',(1.,0.,0.));
#34778=DIRECTION('',(0.,1.,0.));
#34779=DIRECTION('center_axis',(0.,-1.,0.));
#34780=DIRECTION('ref_axis',(1.,0.,0.));
#34781=DIRECTION('',(0.,1.,0.));
#34782=DIRECTION('center_axis',(0.,-1.,0.));
#34783=DIRECTION('ref_axis',(1.,0.,0.));
#34784=DIRECTION('',(0.,1.,0.));
#34785=DIRECTION('center_axis',(0.,-1.,0.));
#34786=DIRECTION('ref_axis',(1.,0.,0.));
#34787=DIRECTION('',(0.,1.,0.));
#34788=DIRECTION('center_axis',(0.,-1.,0.));
#34789=DIRECTION('ref_axis',(1.,0.,0.));
#34790=DIRECTION('',(0.,1.,0.));
#34791=DIRECTION('center_axis',(0.,-1.,0.));
#34792=DIRECTION('ref_axis',(1.,0.,0.));
#34793=DIRECTION('',(0.,1.,0.));
#34794=DIRECTION('center_axis',(0.,-1.,0.));
#34795=DIRECTION('ref_axis',(1.,0.,0.));
#34796=DIRECTION('',(0.,1.,0.));
#34797=DIRECTION('center_axis',(0.,-1.,0.));
#34798=DIRECTION('ref_axis',(1.,0.,0.));
#34799=DIRECTION('',(0.,1.,0.));
#34800=DIRECTION('center_axis',(0.,-1.,0.));
#34801=DIRECTION('ref_axis',(1.,0.,0.));
#34802=DIRECTION('',(0.,1.,0.));
#34803=DIRECTION('center_axis',(0.,-1.,0.));
#34804=DIRECTION('ref_axis',(1.,0.,0.));
#34805=DIRECTION('',(0.,1.,0.));
#34806=DIRECTION('center_axis',(0.,-1.,0.));
#34807=DIRECTION('ref_axis',(1.,0.,0.));
#34808=DIRECTION('',(0.,1.,0.));
#34809=DIRECTION('center_axis',(0.,-1.,0.));
#34810=DIRECTION('ref_axis',(1.,0.,0.));
#34811=DIRECTION('',(0.,1.,0.));
#34812=DIRECTION('center_axis',(0.,-1.,0.));
#34813=DIRECTION('ref_axis',(1.,0.,0.));
#34814=DIRECTION('',(0.,1.,0.));
#34815=DIRECTION('center_axis',(0.,-1.,0.));
#34816=DIRECTION('ref_axis',(1.,0.,0.));
#34817=DIRECTION('',(0.,1.,0.));
#34818=DIRECTION('center_axis',(0.,-1.,0.));
#34819=DIRECTION('ref_axis',(1.,0.,0.));
#34820=DIRECTION('',(0.,1.,0.));
#34821=DIRECTION('center_axis',(0.,-1.,0.));
#34822=DIRECTION('ref_axis',(1.,0.,0.));
#34823=DIRECTION('',(0.,1.,0.));
#34824=DIRECTION('center_axis',(0.,-1.,0.));
#34825=DIRECTION('ref_axis',(1.,0.,0.));
#34826=DIRECTION('',(0.,1.,0.));
#34827=DIRECTION('center_axis',(0.,-1.,0.));
#34828=DIRECTION('ref_axis',(1.,0.,0.));
#34829=DIRECTION('',(0.,1.,0.));
#34830=DIRECTION('center_axis',(0.,-1.,0.));
#34831=DIRECTION('ref_axis',(1.,0.,0.));
#34832=DIRECTION('',(0.,1.,0.));
#34833=DIRECTION('center_axis',(0.,-1.,0.));
#34834=DIRECTION('ref_axis',(1.,0.,0.));
#34835=DIRECTION('',(0.,1.,0.));
#34836=DIRECTION('center_axis',(0.,-1.,0.));
#34837=DIRECTION('ref_axis',(1.,0.,0.));
#34838=DIRECTION('',(0.,1.,0.));
#34839=DIRECTION('center_axis',(0.,-1.,0.));
#34840=DIRECTION('ref_axis',(1.,0.,0.));
#34841=DIRECTION('',(0.,1.,0.));
#34842=DIRECTION('center_axis',(0.,-1.,0.));
#34843=DIRECTION('ref_axis',(1.,0.,0.));
#34844=DIRECTION('',(0.,1.,0.));
#34845=DIRECTION('center_axis',(0.,-1.,0.));
#34846=DIRECTION('ref_axis',(1.,0.,0.));
#34847=DIRECTION('',(0.,1.,0.));
#34848=DIRECTION('center_axis',(0.,-1.,0.));
#34849=DIRECTION('ref_axis',(1.,0.,0.));
#34850=DIRECTION('',(0.,1.,0.));
#34851=DIRECTION('center_axis',(0.,-1.,0.));
#34852=DIRECTION('ref_axis',(1.,0.,0.));
#34853=DIRECTION('',(0.,1.,0.));
#34854=DIRECTION('center_axis',(0.,-1.,0.));
#34855=DIRECTION('ref_axis',(1.,0.,0.));
#34856=DIRECTION('',(0.,1.,0.));
#34857=DIRECTION('center_axis',(0.,-1.,0.));
#34858=DIRECTION('ref_axis',(1.,0.,0.));
#34859=DIRECTION('',(0.,1.,0.));
#34860=DIRECTION('center_axis',(0.,-1.,0.));
#34861=DIRECTION('ref_axis',(1.,0.,0.));
#34862=DIRECTION('',(0.,1.,0.));
#34863=DIRECTION('center_axis',(0.,-1.,0.));
#34864=DIRECTION('ref_axis',(1.,0.,0.));
#34865=DIRECTION('center_axis',(0.,-1.,0.));
#34866=DIRECTION('ref_axis',(1.,0.,0.));
#34867=DIRECTION('',(0.,1.,0.));
#34868=DIRECTION('',(0.,1.,0.));
#34869=DIRECTION('',(0.,-1.,0.));
#34870=DIRECTION('center_axis',(0.,-1.,0.));
#34871=DIRECTION('ref_axis',(1.,0.,0.));
#34872=DIRECTION('center_axis',(0.,1.,0.));
#34873=DIRECTION('ref_axis',(0.,0.,1.));
#34874=DIRECTION('center_axis',(0.,1.,0.));
#34875=DIRECTION('ref_axis',(1.,0.,0.));
#34876=DIRECTION('',(0.,0.,1.));
#34877=DIRECTION('center_axis',(0.,-1.,0.));
#34878=DIRECTION('ref_axis',(0.,0.,-1.));
#34879=DIRECTION('center_axis',(0.,-1.,0.));
#34880=DIRECTION('ref_axis',(1.,0.,0.));
#34881=DIRECTION('',(0.,0.,-1.));
#34882=DIRECTION('center_axis',(1.,0.,0.));
#34883=DIRECTION('ref_axis',(0.,0.,-1.));
#34884=DIRECTION('',(0.,1.,0.));
#34885=DIRECTION('',(0.,-1.,0.));
#34886=DIRECTION('center_axis',(0.282244511485419,0.0053902631593721,0.959327358517117));
#34887=DIRECTION('ref_axis',(0.891452264496529,-0.370963252076271,-0.260190556579225));
#34888=DIRECTION('',(0.743330576824897,-0.633384321745291,-0.215137059858184));
#34889=DIRECTION('',(-0.354472701149703,-0.928631902678381,0.109507504160964));
#34890=DIRECTION('',(-0.956816275612035,0.0741039314181457,0.281089348912921));
#34891=DIRECTION('',(0.,-1.,0.));
#34892=DIRECTION('',(0.953582665134141,-0.3011313679371,0.));
#34893=DIRECTION('',(-0.953582665134141,-0.3011313679371,0.));
#34894=DIRECTION('center_axis',(0.,0.,1.));
#34895=DIRECTION('ref_axis',(1.,0.,0.));
#34896=DIRECTION('center_axis',(0.,1.,0.));
#34897=DIRECTION('ref_axis',(0.,0.,1.));
#34898=DIRECTION('center_axis',(0.,-1.,0.));
#34899=DIRECTION('ref_axis',(1.,0.,0.));
#34900=DIRECTION('center_axis',(0.,-1.,0.));
#34901=DIRECTION('ref_axis',(1.,0.,0.));
#34902=DIRECTION('center_axis',(0.,-1.,0.));
#34903=DIRECTION('ref_axis',(1.,0.,0.));
#34904=DIRECTION('',(0.707106781186534,0.707106781186561,8.65956056235478E-17));
#34905=DIRECTION('center_axis',(0.,-1.,0.));
#34906=DIRECTION('ref_axis',(1.,0.,0.));
#34907=DIRECTION('center_axis',(0.,-1.,0.));
#34908=DIRECTION('ref_axis',(1.,0.,0.));
#34909=DIRECTION('',(0.,1.,0.));
#34910=DIRECTION('center_axis',(0.,1.,0.));
#34911=DIRECTION('ref_axis',(0.,0.,1.));
#34912=DIRECTION('center_axis',(0.,1.,0.));
#34913=DIRECTION('ref_axis',(1.,0.,0.));
#34914=DIRECTION('',(0.707106781186549,-0.707106781186546,-8.65956056235496E-17));
#34915=DIRECTION('center_axis',(0.,-1.,0.));
#34916=DIRECTION('ref_axis',(1.,0.,0.));
#34917=DIRECTION('center_axis',(0.,-1.,0.));
#34918=DIRECTION('ref_axis',(0.,0.,-1.));
#34919=DIRECTION('center_axis',(0.,-1.,0.));
#34920=DIRECTION('ref_axis',(1.,0.,0.));
#34921=DIRECTION('center_axis',(0.,-1.,0.));
#34922=DIRECTION('ref_axis',(1.,0.,0.));
#34923=DIRECTION('center_axis',(0.,-1.,0.));
#34924=DIRECTION('ref_axis',(1.,0.,0.));
#34925=DIRECTION('',(0.,1.,0.));
#34926=DIRECTION('center_axis',(0.,1.,0.));
#34927=DIRECTION('ref_axis',(1.,0.,0.));
#34928=DIRECTION('',(0.707106781186547,-0.707106781186548,-8.65956056235493E-17));
#34929=DIRECTION('center_axis',(0.,-1.,0.));
#34930=DIRECTION('ref_axis',(1.,0.,0.));
#34931=DIRECTION('center_axis',(0.,-1.,0.));
#34932=DIRECTION('ref_axis',(0.,0.,-1.));
#41515=CARTESIAN_POINT('',(0.,0.,0.));
#41516=CARTESIAN_POINT('Origin',(0.,70.2,13.3));
#41517=CARTESIAN_POINT('',(-2.49999999985264,117.652418880134,13.2999728563934));
#41518=CARTESIAN_POINT('',(-2.5,120.,13.3));
#41519=CARTESIAN_POINT('',(-2.5,70.2,13.3));
#41520=CARTESIAN_POINT('Origin',(0.,120.,13.3));
#41521=CARTESIAN_POINT('',(2.31548671935009,116.940942573699,14.2367878010894));
#41522=CARTESIAN_POINT('Ctrl Pts',(-2.5,117.652415863143,13.2999999999964));
#41523=CARTESIAN_POINT('Ctrl Pts',(-2.50000000000024,117.633767919634,13.4677740226832));
#41524=CARTESIAN_POINT('Ctrl Pts',(-2.48311159749416,117.615475457,13.6351341300433));
#41525=CARTESIAN_POINT('Ctrl Pts',(-2.41467031439132,117.578040264004,13.970738634694));
#41526=CARTESIAN_POINT('Ctrl Pts',(-2.36192374370731,117.558925190662,14.1377499846458));
#41527=CARTESIAN_POINT('Ctrl Pts',(-2.15914690247099,117.50166870114,14.6035341083317));
#41528=CARTESIAN_POINT('Ctrl Pts',(-1.96622718300721,117.463802365995,14.8796290223583));
#41529=CARTESIAN_POINT('Ctrl Pts',(-1.49981270374707,117.394137936618,15.3241315427021));
#41530=CARTESIAN_POINT('Ctrl Pts',(-1.23689840087897,117.362604344116,15.4946851089548));
#41531=CARTESIAN_POINT('Ctrl Pts',(-0.797897943810747,117.311924098983,
15.6749091698224));
#41532=CARTESIAN_POINT('Ctrl Pts',(-0.640607813401521,117.294176141788,
15.7220777314919));
#41533=CARTESIAN_POINT('Ctrl Pts',(-0.192100260886219,117.245478021646,
15.8097910077299));
#41534=CARTESIAN_POINT('Ctrl Pts',(0.103385439683299,117.215867900195,15.8150373826655));
#41535=CARTESIAN_POINT('Ctrl Pts',(0.547510877878541,117.172003103533,15.7443114965582));
#41536=CARTESIAN_POINT('Ctrl Pts',(0.699199333265182,117.157044512303,15.7053151288251));
#41537=CARTESIAN_POINT('Ctrl Pts',(1.1602968287484,117.108884869839,15.5394426026382));
#41538=CARTESIAN_POINT('Ctrl Pts',(1.44852396879158,117.073855997147,15.3647510728443));
#41539=CARTESIAN_POINT('Ctrl Pts',(1.83412146311951,117.023015998026,15.0094727975578));
#41540=CARTESIAN_POINT('Ctrl Pts',(1.95905169782132,117.005486607079,14.8647559879435));
#41541=CARTESIAN_POINT('Ctrl Pts',(2.16656823945866,116.972514041558,14.5600305887085));
#41542=CARTESIAN_POINT('Ctrl Pts',(2.2507575437618,116.957083588901,14.4026200111203));
#41543=CARTESIAN_POINT('Ctrl Pts',(2.31751248124682,116.940955446993,14.2376224716085));
#41544=CARTESIAN_POINT('',(-2.50000780325734,115.753171725698,13.2992871105637));
#41545=CARTESIAN_POINT('Ctrl Pts',(2.31558471872693,116.940912503669,14.2365676273829));
#41546=CARTESIAN_POINT('Ctrl Pts',(2.31659029782528,116.940603919617,14.2343081169145));
#41547=CARTESIAN_POINT('Ctrl Pts',(2.31755492533272,116.940306937475,14.2321321519896));
#41548=CARTESIAN_POINT('Ctrl Pts',(2.31856222833977,116.939995783467,14.2298508630467));
#41549=CARTESIAN_POINT('Ctrl Pts',(2.32625422732343,116.937619739418,14.2124304124893));
#41550=CARTESIAN_POINT('Ctrl Pts',(2.33371980469038,116.935252897235,14.1949902343915));
#41551=CARTESIAN_POINT('Ctrl Pts',(2.34047657787375,116.932574974244,14.1772308598749));
#41552=CARTESIAN_POINT('Ctrl Pts',(2.3410009256349,116.932367158637,14.175852674162));
#41553=CARTESIAN_POINT('Ctrl Pts',(2.34152098933304,116.932157472739,14.1744725868393));
#41554=CARTESIAN_POINT('Ctrl Pts',(2.34203653579483,116.931945768446,14.1730904684601));
#41555=CARTESIAN_POINT('Ctrl Pts',(2.35633192712406,116.926075500808,14.1347662347449));
#41556=CARTESIAN_POINT('Ctrl Pts',(2.36967758476892,116.920203373036,14.096091830941));
#41557=CARTESIAN_POINT('Ctrl Pts',(2.38206951868707,116.914333784119,14.0571084522397));
#41558=CARTESIAN_POINT('Ctrl Pts',(2.40895222770159,116.901600464852,13.9725390191753));
#41559=CARTESIAN_POINT('Ctrl Pts',(2.43130345019459,116.888898275388,13.8866537464038));
#41560=CARTESIAN_POINT('Ctrl Pts',(2.44903453897375,116.876229637983,13.7998201531797));
#41561=CARTESIAN_POINT('Ctrl Pts',(2.45662057711109,116.870809510223,13.7626694199108));
#41562=CARTESIAN_POINT('Ctrl Pts',(2.46336092360456,116.8653957767,13.7253447121415));
#41563=CARTESIAN_POINT('Ctrl Pts',(2.46924841009455,116.859989647685,13.6878728787018));
#41564=CARTESIAN_POINT('Ctrl Pts',(2.46926386831748,116.859975453317,13.6877744924115));
#41565=CARTESIAN_POINT('Ctrl Pts',(2.46927932066003,116.859961259002,13.6876761051061));
#41566=CARTESIAN_POINT('Ctrl Pts',(2.46929476712233,116.859947064739,13.6875777167863));
#41567=CARTESIAN_POINT('Ctrl Pts',(2.47479064415234,116.854896722356,13.6525709886025));
#41568=CARTESIAN_POINT('Ctrl Pts',(2.47954223469556,116.849852988345,13.6174357226674));
#41569=CARTESIAN_POINT('Ctrl Pts',(2.48354560772627,116.844812250552,13.5821956513399));
#41570=CARTESIAN_POINT('Ctrl Pts',(2.49342863155305,116.83236831107,13.4951993954539));
#41571=CARTESIAN_POINT('Ctrl Pts',(2.49871470380525,116.819988043894,13.4078942964491));
#41572=CARTESIAN_POINT('Ctrl Pts',(2.49944034464196,116.807632739007,13.3206537489573));
#41573=CARTESIAN_POINT('Ctrl Pts',(2.50017539447477,116.795117229498,13.2322820000103));
#41574=CARTESIAN_POINT('Ctrl Pts',(2.49623080101212,116.782627493706,13.1439770724103));
#41575=CARTESIAN_POINT('Ctrl Pts',(2.48763810528317,116.770145896355,13.0561199186723));
#41576=CARTESIAN_POINT('Ctrl Pts',(2.47905530371016,116.75767867108,12.9683639290402));
#41577=CARTESIAN_POINT('Ctrl Pts',(2.46583555096674,116.745219851162,12.881055195064));
#41578=CARTESIAN_POINT('Ctrl Pts',(2.44800189138904,116.732770812033,12.7945577675241));
#41579=CARTESIAN_POINT('Ctrl Pts',(2.43642053850014,116.724686284309,12.738385492397));
#41580=CARTESIAN_POINT('Ctrl Pts',(2.42289321852048,116.7166062611,12.6825550060511));
#41581=CARTESIAN_POINT('Ctrl Pts',(2.40742217001043,116.708534470064,12.6271612767138));
#41582=CARTESIAN_POINT('Ctrl Pts',(2.40317285018602,116.706317450212,12.6119466859207));
#41583=CARTESIAN_POINT('Ctrl Pts',(2.39878073164306,116.704103078828,12.5967788316271));
#41584=CARTESIAN_POINT('Ctrl Pts',(2.39424657911186,116.701891450801,12.5816593997127));
#41585=CARTESIAN_POINT('Ctrl Pts',(2.39422205165848,116.701879487021,12.5815776112949));
#41586=CARTESIAN_POINT('Ctrl Pts',(2.39419752004866,116.701867523321,12.581495824294));
#41587=CARTESIAN_POINT('Ctrl Pts',(2.3941729842827,116.701855559702,12.5814140387102));
#41588=CARTESIAN_POINT('Ctrl Pts',(2.36913525351378,116.689647182624,12.4979552450586));
#41589=CARTESIAN_POINT('Ctrl Pts',(2.33976991854307,116.677520410264,12.4159705665369));
#41590=CARTESIAN_POINT('Ctrl Pts',(2.30624651142751,116.66542454348,12.3357854461982));
#41591=CARTESIAN_POINT('Ctrl Pts',(2.27221433430887,116.653145103045,12.2543833915609));
#41592=CARTESIAN_POINT('Ctrl Pts',(2.23389660514796,116.640897607304,12.1748367615522));
#41593=CARTESIAN_POINT('Ctrl Pts',(2.19146914410303,116.628652174829,12.0974947553472));
#41594=CARTESIAN_POINT('Ctrl Pts',(2.14893240047266,116.616375201165,12.0199535353737));
#41595=CARTESIAN_POINT('Ctrl Pts',(2.10226509706415,116.60410053041,11.9446289849932));
#41596=CARTESIAN_POINT('Ctrl Pts',(2.0516424135292,116.591818631987,11.8718700282806));
#41597=CARTESIAN_POINT('Ctrl Pts',(2.02733790787834,116.585921957832,11.836937655062));
#41598=CARTESIAN_POINT('Ctrl Pts',(2.00212159864347,116.580023900124,11.8025965566306));
#41599=CARTESIAN_POINT('Ctrl Pts',(1.97601207576289,116.574124817132,11.7688845677729));
#41600=CARTESIAN_POINT('Ctrl Pts',(1.93528800816622,116.564923781341,11.7163026297826));
#41601=CARTESIAN_POINT('Ctrl Pts',(1.89254740546535,116.555755273503,11.6654526254126));
#41602=CARTESIAN_POINT('Ctrl Pts',(1.84790062309802,116.546623642951,11.6164344471128));
#41603=CARTESIAN_POINT('Ctrl Pts',(1.84785790318654,116.546614905425,11.6163875444666));
#41604=CARTESIAN_POINT('Ctrl Pts',(1.84781518152816,116.546606167932,11.6163406434974));
#41605=CARTESIAN_POINT('Ctrl Pts',(1.84777245812297,116.546597430472,11.6162937442053));
#41606=CARTESIAN_POINT('Ctrl Pts',(1.78880671836136,116.534538214999,11.5515645531837));
#41607=CARTESIAN_POINT('Ctrl Pts',(1.72651412330931,116.522542000416,11.4900271582674));
#41608=CARTESIAN_POINT('Ctrl Pts',(1.66117508174235,116.510564512528,11.4319174966237));
#41609=CARTESIAN_POINT('Ctrl Pts',(1.59497422136402,116.498429042151,11.3730413713416));
#41610=CARTESIAN_POINT('Ctrl Pts',(1.52564613907004,116.48631290844,11.3176849042504));
#41611=CARTESIAN_POINT('Ctrl Pts',(1.45348844373583,116.474190351703,11.2661036490813));
#41612=CARTESIAN_POINT('Ctrl Pts',(1.38834739291626,116.463246597461,11.2195381767676));
#41613=CARTESIAN_POINT('Ctrl Pts',(1.3209007494497,116.452297992488,11.1760497257851));
#41614=CARTESIAN_POINT('Ctrl Pts',(1.2513674883898,116.441337882707,11.1358262063494));
#41615=CARTESIAN_POINT('Ctrl Pts',(1.17929482046512,116.429977501493,11.0941336938041));
#41616=CARTESIAN_POINT('Ctrl Pts',(1.10532794360825,116.418659279662,11.0561498523986));
#41617=CARTESIAN_POINT('Ctrl Pts',(1.02975113129391,116.407385635209,11.0219720448883));
#41618=CARTESIAN_POINT('Ctrl Pts',(1.02486966711646,116.406657476798,11.0197645193534));
#41619=CARTESIAN_POINT('Ctrl Pts',(1.01998147000137,116.405929503522,11.0175728786915));
#41620=CARTESIAN_POINT('Ctrl Pts',(1.01508660977429,116.405201715687,11.0153971521677));
#41621=CARTESIAN_POINT('Ctrl Pts',(0.989532427173145,116.401402215322,11.0040385208075));
#41622=CARTESIAN_POINT('Ctrl Pts',(0.963796808589488,116.39760786875,10.9931133169629));
#41623=CARTESIAN_POINT('Ctrl Pts',(0.937889563447039,116.393818941974,10.9826251250953));
#41624=CARTESIAN_POINT('Ctrl Pts',(0.937876528580895,116.393817035628,10.982619848109));
#41625=CARTESIAN_POINT('Ctrl Pts',(0.937863493671292,116.393815129285,10.9826145712334));
#41626=CARTESIAN_POINT('Ctrl Pts',(0.937850458718229,116.393813222942,10.9826092944684));
#41627=CARTESIAN_POINT('Ctrl Pts',(0.856558251270879,116.38192435854,10.9497008617622));
#41628=CARTESIAN_POINT('Ctrl Pts',(0.773574022102526,116.370087314127,10.9210938611651));
#41629=CARTESIAN_POINT('Ctrl Pts',(0.689246936165983,116.358259657402,10.8969044369372));
#41630=CARTESIAN_POINT('Ctrl Pts',(0.604144768993149,116.346323288338,10.8724926788217));
#41631=CARTESIAN_POINT('Ctrl Pts',(0.517675482596711,116.334396606344,10.8525809850961));
#41632=CARTESIAN_POINT('Ctrl Pts',(0.430216206818991,116.322454369358,10.8372950323008));
#41633=CARTESIAN_POINT('Ctrl Pts',(0.400085229039446,116.31834009704,10.8320288018191));
#41634=CARTESIAN_POINT('Ctrl Pts',(0.369836865368955,116.314224127933,10.827311598678));
#41635=CARTESIAN_POINT('Ctrl Pts',(0.339486805344473,116.310105876929,10.8231485103331));
#41636=CARTESIAN_POINT('Ctrl Pts',(0.251592673824735,116.298179373486,10.8110921574225));
#41637=CARTESIAN_POINT('Ctrl Pts',(0.163299503256435,116.286294065945,10.8037453205576));
#41638=CARTESIAN_POINT('Ctrl Pts',(0.0749915624963321,116.274444109565,
10.801084345815));
#41639=CARTESIAN_POINT('Ctrl Pts',(-0.00218809746395864,116.264087446324,
10.7987586984946));
#41640=CARTESIAN_POINT('Ctrl Pts',(-0.0793792441935915,116.253758137179,
10.8000117096716));
#41641=CARTESIAN_POINT('Ctrl Pts',(-0.156350655397556,116.243457913992,
10.8048298747349));
#41642=CARTESIAN_POINT('Ctrl Pts',(-0.156400196120542,116.243451284512,
10.8048329758262));
#41643=CARTESIAN_POINT('Ctrl Pts',(-0.156449736753255,116.243444655042,
10.804836078396));
#41644=CARTESIAN_POINT('Ctrl Pts',(-0.156499277295674,116.243438025585,
10.8048391824442));
#41645=CARTESIAN_POINT('Ctrl Pts',(-0.24456415739787,116.231653286752,10.8103570394452));
#41646=CARTESIAN_POINT('Ctrl Pts',(-0.332346265444591,116.219905715678,
10.820542262043));
#41647=CARTESIAN_POINT('Ctrl Pts',(-0.419477796327602,116.20816041902,10.8353707649117));
#41648=CARTESIAN_POINT('Ctrl Pts',(-0.488449146412123,116.198863107709,
10.847108672558));
#41649=CARTESIAN_POINT('Ctrl Pts',(-0.557012073175496,116.189567578866,
10.8617562465931));
#41650=CARTESIAN_POINT('Ctrl Pts',(-0.624975132408264,116.180262954861,
10.8793013943141));
#41651=CARTESIAN_POINT('Ctrl Pts',(-0.65193249278898,116.176572301359,10.8862606288657));
#41652=CARTESIAN_POINT('Ctrl Pts',(-0.678751888420746,116.172886231536,
10.8936644806514));
#41653=CARTESIAN_POINT('Ctrl Pts',(-0.705422444723274,116.169204265486,
10.9015078227887));
#41654=CARTESIAN_POINT('Ctrl Pts',(-0.705495663032793,116.169194157435,
10.9015293550075));
#41655=CARTESIAN_POINT('Ctrl Pts',(-0.705568880219835,116.169184049415,
10.9015508905417));
#41656=CARTESIAN_POINT('Ctrl Pts',(-0.705642096283931,116.169173941425,
10.9015724293912));
#41657=CARTESIAN_POINT('Ctrl Pts',(-0.790078629159663,116.157516887221,
10.926412139052));
#41658=CARTESIAN_POINT('Ctrl Pts',(-0.873021144427934,116.145900151257,
10.9556566826382));
#41659=CARTESIAN_POINT('Ctrl Pts',(-0.954125624468592,116.134312207952,
10.989140873903));
#41660=CARTESIAN_POINT('Ctrl Pts',(-1.03160398465552,116.123242352812,11.0211280123456));
#41661=CARTESIAN_POINT('Ctrl Pts',(-1.10740468305274,116.112199021028,11.0569836383265));
#41662=CARTESIAN_POINT('Ctrl Pts',(-1.18125236023816,116.101179283222,11.0965733416553));
#41663=CARTESIAN_POINT('Ctrl Pts',(-1.1854452336852,116.100553612005,11.0988211390429));
#41664=CARTESIAN_POINT('Ctrl Pts',(-1.18963181315389,116.099928016101,11.1010809876576));
#41665=CARTESIAN_POINT('Ctrl Pts',(-1.19381204878256,116.099302494702,11.1033528679144));
#41666=CARTESIAN_POINT('Ctrl Pts',(-1.20234052067155,116.098026312654,11.1079879336443));
#41667=CARTESIAN_POINT('Ctrl Pts',(-1.21084260999004,116.096750449632,11.1126730392948));
#41668=CARTESIAN_POINT('Ctrl Pts',(-1.21931791193801,116.095474904488,11.1174079983053));
#41669=CARTESIAN_POINT('Ctrl Pts',(-1.21941892058687,116.095459702541,11.1174644295469));
#41670=CARTESIAN_POINT('Ctrl Pts',(-1.21951992542756,116.095444500638,11.1175208678753));
#41671=CARTESIAN_POINT('Ctrl Pts',(-1.21962092645903,116.095429298779,11.1175773132903));
#41672=CARTESIAN_POINT('Ctrl Pts',(-1.29230581112784,116.084489357145,11.1581979725452));
#41673=CARTESIAN_POINT('Ctrl Pts',(-1.36302191930873,116.073571818357,11.2024869421495));
#41674=CARTESIAN_POINT('Ctrl Pts',(-1.43148894550428,116.062648657739,11.2503077186718));
#41675=CARTESIAN_POINT('Ctrl Pts',(-1.43561009700005,116.061991173367,11.2531861358552));
#41676=CARTESIAN_POINT('Ctrl Pts',(-1.43972308545627,116.061333669725,11.2560773547882));
#41677=CARTESIAN_POINT('Ctrl Pts',(-1.44382784410453,116.060676141123,11.2589813477688));
#41678=CARTESIAN_POINT('Ctrl Pts',(-1.46186642054003,116.057786597312,11.2717430967139));
#41679=CARTESIAN_POINT('Ctrl Pts',(-1.4797462227181,116.054896613924,11.2847513374824));
#41680=CARTESIAN_POINT('Ctrl Pts',(-1.49746176129706,116.052005801828,11.2980033881251));
#41681=CARTESIAN_POINT('Ctrl Pts',(-1.56781347313938,116.040525847175,11.3506297558742));
#41682=CARTESIAN_POINT('Ctrl Pts',(-1.63521555084676,116.029090470488,11.4068327759038));
#41683=CARTESIAN_POINT('Ctrl Pts',(-1.69941062671312,116.017681713284,11.4663298991271));
#41684=CARTESIAN_POINT('Ctrl Pts',(-1.76448188855156,116.006117240194,11.5266390868903));
#41685=CARTESIAN_POINT('Ctrl Pts',(-1.82625756826401,115.994580378614,11.5903320231517));
#41686=CARTESIAN_POINT('Ctrl Pts',(-1.88448516423124,115.983060855372,11.6571244196917));
#41687=CARTESIAN_POINT('Ctrl Pts',(-1.94054639750562,115.971969916979,11.7214317994002));
#41688=CARTESIAN_POINT('Ctrl Pts',(-1.99331901776561,115.960895321955,11.7886113724769));
#41689=CARTESIAN_POINT('Ctrl Pts',(-2.04259213004864,115.949831653556,11.858432055086));
#41690=CARTESIAN_POINT('Ctrl Pts',(-2.04268247864119,115.949811366897,11.8585600802931));
#41691=CARTESIAN_POINT('Ctrl Pts',(-2.04277281546547,115.949791080273,11.8586881143922));
#41692=CARTESIAN_POINT('Ctrl Pts',(-2.04286314051931,115.949770793686,11.8588161573824));
#41693=CARTESIAN_POINT('Ctrl Pts',(-2.07925508584214,115.941597331938,11.9104046513913));
#41694=CARTESIAN_POINT('Ctrl Pts',(-2.11373782549542,115.933429652993,11.9634365047525));
#41695=CARTESIAN_POINT('Ctrl Pts',(-2.14621742886547,115.92525735781,12.017807968242));
#41696=CARTESIAN_POINT('Ctrl Pts',(-2.19103295219095,115.913981183,12.0928299924489));
#41697=CARTESIAN_POINT('Ctrl Pts',(-2.23180572449633,115.902753224868,12.1700199717333));
#41698=CARTESIAN_POINT('Ctrl Pts',(-2.26840497157125,115.891554051651,12.2490219104932));
#41699=CARTESIAN_POINT('Ctrl Pts',(-2.28335615916443,115.886979068474,12.2812950554627));
#41700=CARTESIAN_POINT('Ctrl Pts',(-2.29761095150448,115.882408989736,12.3138705897435));
#41701=CARTESIAN_POINT('Ctrl Pts',(-2.3111608945923,115.877842846099,12.3467244888677));
#41702=CARTESIAN_POINT('Ctrl Pts',(-2.31122345482284,115.877821764166,12.3468761756674));
#41703=CARTESIAN_POINT('Ctrl Pts',(-2.31128600001604,115.877800682315,12.3470278684067));
#41704=CARTESIAN_POINT('Ctrl Pts',(-2.31134853017173,115.877779600547,12.3471795670829));
#41705=CARTESIAN_POINT('Ctrl Pts',(-2.34169064308544,115.86754989006,12.4207897846128));
#41706=CARTESIAN_POINT('Ctrl Pts',(-2.36849361581318,115.857339984831,12.4957938787982));
#41707=CARTESIAN_POINT('Ctrl Pts',(-2.39167540751614,115.847146677697,12.5719549633683));
#41708=CARTESIAN_POINT('Ctrl Pts',(-2.39554800156618,115.845443852434,12.5846779214006));
#41709=CARTESIAN_POINT('Ctrl Pts',(-2.39931949254203,115.843741481025,12.5974332747695));
#41710=CARTESIAN_POINT('Ctrl Pts',(-2.40298943501363,115.842039537261,12.6102200465974));
#41711=CARTESIAN_POINT('Ctrl Pts',(-2.40303577089737,115.842018048894,12.6103814895566));
#41712=CARTESIAN_POINT('Ctrl Pts',(-2.40308209060529,115.841996560598,12.6105429375206));
#41713=CARTESIAN_POINT('Ctrl Pts',(-2.40312839413032,115.841975072369,12.610704390489));
#41714=CARTESIAN_POINT('Ctrl Pts',(-2.41590288462029,115.836046772837,12.6552469908212));
#41715=CARTESIAN_POINT('Ctrl Pts',(-2.42744647790313,115.830123446056,12.7001724516602));
#41716=CARTESIAN_POINT('Ctrl Pts',(-2.43773795250823,115.824192790862,12.7454148170031));
#41717=CARTESIAN_POINT('Ctrl Pts',(-2.43777476533889,115.824171576778,12.7455766499374));
#41718=CARTESIAN_POINT('Ctrl Pts',(-2.43781156212925,115.824150362603,12.7457384869042));
#41719=CARTESIAN_POINT('Ctrl Pts',(-2.43784834289122,115.824129148337,12.7459003278972));
#41720=CARTESIAN_POINT('Ctrl Pts',(-2.44811410441784,115.818208102025,12.7910712528639));
#41721=CARTESIAN_POINT('Ctrl Pts',(-2.45713095097772,115.8122803864,12.8365526619577));
#41722=CARTESIAN_POINT('Ctrl Pts',(-2.46488253727775,115.806358415083,12.8823025199197));
#41723=CARTESIAN_POINT('Ctrl Pts',(-2.46491177598373,115.80633607762,12.8824750867459));
#41724=CARTESIAN_POINT('Ctrl Pts',(-2.46494099670432,115.806313740233,12.8826476574335));
#41725=CARTESIAN_POINT('Ctrl Pts',(-2.46497019942748,115.806291402924,12.8828202319817));
#41726=CARTESIAN_POINT('Ctrl Pts',(-2.46774729796264,115.804167186348,12.8992315961665));
#41727=CARTESIAN_POINT('Ctrl Pts',(-2.47036163655441,115.802043666934,12.9156778827472));
#41728=CARTESIAN_POINT('Ctrl Pts',(-2.47281230648096,115.799920717301,12.9321560233193));
#41729=CARTESIAN_POINT('Ctrl Pts',(-2.48403796215045,115.790196232858,13.0076365807501));
#41730=CARTESIAN_POINT('Ctrl Pts',(-2.49178559071337,115.780521771062,13.0834875586044));
#41731=CARTESIAN_POINT('Ctrl Pts',(-2.49606163842758,115.770873778594,13.1594975034073));
#41732=CARTESIAN_POINT('Ctrl Pts',(-2.49665765041311,115.769529004276,13.170092062016));
#41733=CARTESIAN_POINT('Ctrl Pts',(-2.49718615364143,115.768184753474,13.180689656827));
#41734=CARTESIAN_POINT('Ctrl Pts',(-2.49764710684871,115.76684097141,13.1912896626918));
#41735=CARTESIAN_POINT('Ctrl Pts',(-2.49921172934089,115.762279745649,13.2272694700374));
#41736=CARTESIAN_POINT('Ctrl Pts',(-2.49999871575296,115.757723936595,13.2632771489192));
#41737=CARTESIAN_POINT('Ctrl Pts',(-2.50000780325734,115.753171725698,13.2992871105637));
#41738=CARTESIAN_POINT('',(-2.5,116.590949403176,13.3));
#41739=CARTESIAN_POINT('',(-2.5,70.2,13.3));
#41740=CARTESIAN_POINT('',(-0.113189986264273,116.915604014531,10.8025547582574));
#41741=CARTESIAN_POINT('Ctrl Pts',(-2.5,116.590949403176,13.3));
#41742=CARTESIAN_POINT('Ctrl Pts',(-2.5,116.620953768662,12.9872092797494));
#41743=CARTESIAN_POINT('Ctrl Pts',(-2.44132738978406,116.653364211068,12.6770829675089));
#41744=CARTESIAN_POINT('Ctrl Pts',(-2.22541193652053,116.708445952147,12.1276873243219));
#41745=CARTESIAN_POINT('Ctrl Pts',(-2.08195957546983,116.731312087827,11.8885330538203));
#41746=CARTESIAN_POINT('Ctrl Pts',(-1.68507892689696,116.782726034039,11.4231982379589));
#41747=CARTESIAN_POINT('Ctrl Pts',(-1.41928106560156,116.814133195958,11.2149293621363));
#41748=CARTESIAN_POINT('Ctrl Pts',(-0.953296569348058,116.856517921123,
10.981356754033));
#41749=CARTESIAN_POINT('Ctrl Pts',(-0.77746724983857,116.870233032691,10.9166232730901));
#41750=CARTESIAN_POINT('Ctrl Pts',(-0.43764187396164,116.89413879085,10.8332135767708));
#41751=CARTESIAN_POINT('Ctrl Pts',(-0.275985400295147,116.9045269682,10.8099444629497));
#41752=CARTESIAN_POINT('Ctrl Pts',(-0.113227701620156,116.915647816343,
10.8025654187575));
#41753=CARTESIAN_POINT('',(2.37817680705653,117.418248384963,12.5291084093352));
#41754=CARTESIAN_POINT('Ctrl Pts',(-0.11318991391854,116.91570063764,10.8025637058401));
#41755=CARTESIAN_POINT('Ctrl Pts',(-0.0267483415987858,116.929017161337,
10.7986459626117));
#41756=CARTESIAN_POINT('Ctrl Pts',(0.0596926633871199,116.942504266172,
10.7992268895155));
#41757=CARTESIAN_POINT('Ctrl Pts',(0.145739837161053,116.956081811018,10.8042516353077));
#41758=CARTESIAN_POINT('Ctrl Pts',(0.231953820853551,116.969685677113,10.809286122006));
#41759=CARTESIAN_POINT('Ctrl Pts',(0.317771656242895,116.983380328598,10.8187801658181));
#41760=CARTESIAN_POINT('Ctrl Pts',(0.402846612778607,116.997089241994,10.8326705516748));
#41761=CARTESIAN_POINT('Ctrl Pts',(0.486360317026859,117.010546576391,10.8463060282423));
#41762=CARTESIAN_POINT('Ctrl Pts',(0.569158212026128,117.024017660618,10.8641761280544));
#41763=CARTESIAN_POINT('Ctrl Pts',(0.650964467559707,117.037434010971,10.8862383585004));
#41764=CARTESIAN_POINT('Ctrl Pts',(0.721054977793133,117.048928961273,10.9051409837185));
#41765=CARTESIAN_POINT('Ctrl Pts',(0.790418663365023,117.06038379259,10.9271204666373));
#41766=CARTESIAN_POINT('Ctrl Pts',(0.858910376226253,117.071757742589,10.9521769731066));
#41767=CARTESIAN_POINT('Ctrl Pts',(0.861120381724083,117.072124743077,10.9529854653276));
#41768=CARTESIAN_POINT('Ctrl Pts',(0.863329073610727,117.072491648114,10.9537970150146));
#41769=CARTESIAN_POINT('Ctrl Pts',(0.86553645088459,117.072858459449,10.954611620181));
#41770=CARTESIAN_POINT('Ctrl Pts',(0.935076433748151,117.084414279223,10.9802744871416));
#41771=CARTESIAN_POINT('Ctrl Pts',(1.00331537275581,117.095877243229,11.0089698285396));
#41772=CARTESIAN_POINT('Ctrl Pts',(1.07010181240248,117.10730088397,11.0406013828691));
#41773=CARTESIAN_POINT('Ctrl Pts',(1.13672507294348,117.118696613364,11.0721556519178));
#41774=CARTESIAN_POINT('Ctrl Pts',(1.20190196549986,117.130053212562,11.1066325777123));
#41775=CARTESIAN_POINT('Ctrl Pts',(1.26544711283963,117.141422144751,11.1439286643049));
#41776=CARTESIAN_POINT('Ctrl Pts',(1.32922572009029,117.152832845509,11.1813617738084));
#41777=CARTESIAN_POINT('Ctrl Pts',(1.39135968082058,117.16425597846,11.221635184068));
#41778=CARTESIAN_POINT('Ctrl Pts',(1.45164008493825,117.175741809776,11.2646275368374));
#41779=CARTESIAN_POINT('Ctrl Pts',(1.51192048905591,117.187227641092,11.3076198896069));
#41780=CARTESIAN_POINT('Ctrl Pts',(1.57034651217938,117.198776184031,11.3533311812538));
#41781=CARTESIAN_POINT('Ctrl Pts',(1.62670074151225,117.210435781116,11.401620507495));
#41782=CARTESIAN_POINT('Ctrl Pts',(1.67550891578635,117.220534111858,11.4434437012226));
#41783=CARTESIAN_POINT('Ctrl Pts',(1.72274007319172,117.230657724238,11.4871857180797));
#41784=CARTESIAN_POINT('Ctrl Pts',(1.76816646432715,117.240762291144,11.5326326487035));
#41785=CARTESIAN_POINT('Ctrl Pts',(1.78004664653425,117.243404898073,11.5445182025207));
#41786=CARTESIAN_POINT('Ctrl Pts',(1.79180358181125,117.24604620237,11.5565201652442));
#41787=CARTESIAN_POINT('Ctrl Pts',(1.8034336175365,117.248685411144,11.5686342999992));
#41788=CARTESIAN_POINT('Ctrl Pts',(1.8581769435127,117.261108336546,11.6256563112365));
#41789=CARTESIAN_POINT('Ctrl Pts',(1.9101109785362,117.273484663151,11.6851578292605));
#41790=CARTESIAN_POINT('Ctrl Pts',(1.95917679036972,117.285737949046,11.747058821437));
#41791=CARTESIAN_POINT('Ctrl Pts',(1.98646034826758,117.292551516837,11.7814795156205));
#41792=CARTESIAN_POINT('Ctrl Pts',(2.01285694050732,117.299327138072,11.8166436662805));
#41793=CARTESIAN_POINT('Ctrl Pts',(2.03835233884761,117.306052387535,11.8525471535437));
#41794=CARTESIAN_POINT('Ctrl Pts',(2.07762546147216,117.316411964715,11.9078529008443));
#41795=CARTESIAN_POINT('Ctrl Pts',(2.11456156585197,117.326577774003,11.9646335879006));
#41796=CARTESIAN_POINT('Ctrl Pts',(2.14911406704124,117.336628105394,12.0227730323684));
#41797=CARTESIAN_POINT('Ctrl Pts',(2.18321742229141,117.346547793116,12.0801567256029));
#41798=CARTESIAN_POINT('Ctrl Pts',(2.21499884773677,117.356354970737,12.1388654478325));
#41799=CARTESIAN_POINT('Ctrl Pts',(2.24439421061938,117.366121279219,12.1987758505471));
#41800=CARTESIAN_POINT('Ctrl Pts',(2.27355623419998,117.375810063106,12.2582106867036));
#41801=CARTESIAN_POINT('Ctrl Pts',(2.30036947417557,117.385458589752,12.3188293335521));
#41802=CARTESIAN_POINT('Ctrl Pts',(2.32475484863219,117.395133573531,12.3804811618237));
#41803=CARTESIAN_POINT('Ctrl Pts',(2.34410593556398,117.402811185885,12.4294051547896));
#41804=CARTESIAN_POINT('Ctrl Pts',(2.36192759828503,117.41050538556,12.4789793027436));
#41805=CARTESIAN_POINT('Ctrl Pts',(2.37817704323118,117.418248311024,12.5291083402655));
#41806=CARTESIAN_POINT('',(2.37639371954888,118.486854168824,12.5236287354052));
#41807=CARTESIAN_POINT('',(2.37732998843941,117.925623783712,12.5265067145218));
#41808=CARTESIAN_POINT('Ctrl Pts',(2.37639382411024,118.486854164655,12.5236287017601));
#41809=CARTESIAN_POINT('Ctrl Pts',(2.29237449868435,118.455071882635,12.2664540657314));
#41810=CARTESIAN_POINT('Ctrl Pts',(2.16719785357465,118.422212612927,12.0247183887063));
#41811=CARTESIAN_POINT('Ctrl Pts',(1.84820554614646,118.35618592643,11.5959234906477));
#41812=CARTESIAN_POINT('Ctrl Pts',(1.65797254561086,118.323870392737,11.4103165284456));
#41813=CARTESIAN_POINT('Ctrl Pts',(1.17168681790221,118.251443979973,11.0668784972995));
#41814=CARTESIAN_POINT('Ctrl Pts',(0.865841333419305,118.211595169798,10.9314448594032));
#41815=CARTESIAN_POINT('Ctrl Pts',(0.388388355687752,118.153118629885,10.8253143118232));
#41816=CARTESIAN_POINT('Ctrl Pts',(0.231386992078417,118.134476740984,10.8057288724813));
#41817=CARTESIAN_POINT('Ctrl Pts',(-0.0819192501568569,118.09774354819,
10.7965051430853));
#41818=CARTESIAN_POINT('Ctrl Pts',(-0.23750455082634,118.079729277626,10.8064492283048));
#41819=CARTESIAN_POINT('Ctrl Pts',(-0.540961868585215,118.044110016183,
10.8545219930496));
#41820=CARTESIAN_POINT('Ctrl Pts',(-0.688276731890548,118.026578242465,
10.8918327871561));
#41821=CARTESIAN_POINT('Ctrl Pts',(-1.06771232274408,117.979320612286,11.0256130190422));
#41822=CARTESIAN_POINT('Ctrl Pts',(-1.29025443117006,117.949427715848,11.1440578220645));
#41823=CARTESIAN_POINT('Ctrl Pts',(-1.73483039841509,117.884058903072,11.4745320778206));
#41824=CARTESIAN_POINT('Ctrl Pts',(-1.94332056132931,117.849380326021,11.6982671554484));
#41825=CARTESIAN_POINT('Ctrl Pts',(-2.16869487811854,117.801600611764,12.0509879017169));
#41826=CARTESIAN_POINT('Ctrl Pts',(-2.22393087527522,117.788485405148,12.1522204186784));
#41827=CARTESIAN_POINT('Ctrl Pts',(-2.34892858865178,117.754045018187,12.4244783697562));
#41828=CARTESIAN_POINT('Ctrl Pts',(-2.40709440953146,117.732674965509,12.6000681821379));
#41829=CARTESIAN_POINT('Ctrl Pts',(-2.48169828832362,117.691521844839,12.951217002664));
#41830=CARTESIAN_POINT('Ctrl Pts',(-2.49999810368946,117.671830201486,13.1253310693141));
#41831=CARTESIAN_POINT('Ctrl Pts',(-2.49999999985264,117.652418880134,13.2999728563934));
#41832=CARTESIAN_POINT('Origin',(0.,70.2,13.3));
#41833=CARTESIAN_POINT('',(-2.50002326288683,113.63543715375,13.3006174987927));
#41834=CARTESIAN_POINT('',(-2.5,114.793997579998,13.3000000010378));
#41835=CARTESIAN_POINT('',(-2.5,70.2,13.3));
#41836=CARTESIAN_POINT('Ctrl Pts',(-2.5,114.793997579998,13.3000000020756));
#41837=CARTESIAN_POINT('Ctrl Pts',(-2.50000000002252,114.797385889231,13.2728777046832));
#41838=CARTESIAN_POINT('Ctrl Pts',(-2.49955862869347,114.800774717604,13.2457529010415));
#41839=CARTESIAN_POINT('Ctrl Pts',(-2.49190150031146,114.830166814656,13.0106026288428));
#41840=CARTESIAN_POINT('Ctrl Pts',(-2.45917284392043,114.856049634189,12.8042153754441));
#41841=CARTESIAN_POINT('Ctrl Pts',(-2.35146918787085,114.904049605931,12.4324861684175));
#41842=CARTESIAN_POINT('Ctrl Pts',(-2.28340152883787,114.926045267411,12.2665224602698));
#41843=CARTESIAN_POINT('Ctrl Pts',(-2.05669318098404,114.984410429985,11.8480094363152));
#41844=CARTESIAN_POINT('Ctrl Pts',(-1.86974559343431,115.02018752997,11.6140809587873));
#41845=CARTESIAN_POINT('Ctrl Pts',(-1.39300455220041,115.097611737711,11.1969877167693));
#41846=CARTESIAN_POINT('Ctrl Pts',(-1.0977401884382,115.138312755489,11.0288491360474));
#41847=CARTESIAN_POINT('Ctrl Pts',(-0.479917790473351,115.216913456915,
10.8265213203945));
#41848=CARTESIAN_POINT('Ctrl Pts',(-0.166029962590372,115.254399332085,
10.7858645153009));
#41849=CARTESIAN_POINT('Ctrl Pts',(0.298014978088405,115.310102267509,10.8132316813518));
#41850=CARTESIAN_POINT('Ctrl Pts',(0.447726592942345,115.328138530198,10.8357825773864));
#41851=CARTESIAN_POINT('Ctrl Pts',(0.887437456843971,115.382620288385,10.9434296106405));
#41852=CARTESIAN_POINT('Ctrl Pts',(1.16505368337756,115.419006550745,11.0675878969932));
#41853=CARTESIAN_POINT('Ctrl Pts',(1.64964681615153,115.488688629676,11.3998934724379));
#41854=CARTESIAN_POINT('Ctrl Pts',(1.85596666936301,115.521525836049,11.6008398262939));
#41855=CARTESIAN_POINT('Ctrl Pts',(2.21975084583485,115.594032687924,12.1024705868506));
#41856=CARTESIAN_POINT('Ctrl Pts',(2.35959987421961,115.633928398604,12.4091249040404));
#41857=CARTESIAN_POINT('Ctrl Pts',(2.49930674860258,115.70608305261,13.0103911353894));
#41858=CARTESIAN_POINT('Ctrl Pts',(2.51603037566584,115.738004574514,13.2955135399316));
#41859=CARTESIAN_POINT('Ctrl Pts',(2.44754858026923,115.808810143904,13.9089612556534));
#41860=CARTESIAN_POINT('Ctrl Pts',(2.34452701964057,115.848357358424,14.2297832668353));
#41861=CARTESIAN_POINT('Ctrl Pts',(2.11048949387997,115.9035194425,14.6479741892287));
#41862=CARTESIAN_POINT('Ctrl Pts',(2.02840636605182,115.919980245341,14.768599183933));
#41863=CARTESIAN_POINT('Ctrl Pts',(1.83699748384671,115.95379355059,15.0029588351278));
#41864=CARTESIAN_POINT('Ctrl Pts',(1.72650133924465,115.971036476695,15.1148894878823));
#41865=CARTESIAN_POINT('Ctrl Pts',(1.34988225547283,116.02560205963,15.4306657198259));
#41866=CARTESIAN_POINT('Ctrl Pts',(1.05299152127506,116.063637079497,15.5919691090266));
#41867=CARTESIAN_POINT('Ctrl Pts',(0.439708259853296,116.134956646751,15.7800962773638));
#41868=CARTESIAN_POINT('Ctrl Pts',(0.132191672253177,116.167781256259,15.8153000771159));
#41869=CARTESIAN_POINT('Ctrl Pts',(-0.507456022132339,116.238328474224,
15.7706726198806));
#41870=CARTESIAN_POINT('Ctrl Pts',(-0.832956242345116,116.276364335092,
15.6807642589591));
#41871=CARTESIAN_POINT('Ctrl Pts',(-1.38386970925306,116.342148183849,15.4012326146894));
#41872=CARTESIAN_POINT('Ctrl Pts',(-1.61286175207875,116.370129562098,15.2310486178901));
#41873=CARTESIAN_POINT('Ctrl Pts',(-2.03856336916099,116.433471672011,14.7850290700612));
#41874=CARTESIAN_POINT('Ctrl Pts',(-2.21813157489942,116.469971070782,14.5004154086595));
#41875=CARTESIAN_POINT('Ctrl Pts',(-2.4365058001107,116.531934314149,13.9263584664292));
#41876=CARTESIAN_POINT('Ctrl Pts',(-2.49140634538486,116.557734397389,13.648972460494));
#41877=CARTESIAN_POINT('Ctrl Pts',(-2.49969015735141,116.586599767941,13.3454626860678));
#41878=CARTESIAN_POINT('Ctrl Pts',(-2.5,116.588769567576,13.3227244381384));
#41879=CARTESIAN_POINT('Ctrl Pts',(-2.5,116.590949403176,13.3));
#41880=CARTESIAN_POINT('',(2.40669191446942,114.731988374668,12.6249749337064));
#41881=CARTESIAN_POINT('Ctrl Pts',(-2.49999989834126,115.75317125154,13.2992870528137));
#41882=CARTESIAN_POINT('Ctrl Pts',(-2.50008184411521,115.716846549025,13.5866357239191));
#41883=CARTESIAN_POINT('Ctrl Pts',(-2.4506214260268,115.68099481083,13.8718771511382));
#41884=CARTESIAN_POINT('Ctrl Pts',(-2.27148199259844,115.614307807583,14.3723863367816));
#41885=CARTESIAN_POINT('Ctrl Pts',(-2.15593128189566,115.583903092524,14.5890356131345));
#41886=CARTESIAN_POINT('Ctrl Pts',(-1.83762731193967,115.517060933905,15.0199042209758));
#41887=CARTESIAN_POINT('Ctrl Pts',(-1.62476569711639,115.481067765976,15.222266975671));
#41888=CARTESIAN_POINT('Ctrl Pts',(-1.11286078002683,115.405310811968,15.5617954833605));
#41889=CARTESIAN_POINT('Ctrl Pts',(-0.811821305593659,115.366328837562,
15.6864587765518));
#41890=CARTESIAN_POINT('Ctrl Pts',(-0.220822194139709,115.293507807071,
15.8059308778056));
#41891=CARTESIAN_POINT('Ctrl Pts',(0.0611000182903552,115.260078353759,
15.814898816406));
#41892=CARTESIAN_POINT('Ctrl Pts',(0.646198561619679,115.188655291391,15.73491437931));
#41893=CARTESIAN_POINT('Ctrl Pts',(0.943342589834492,115.151546914754,15.6359278686744));
#41894=CARTESIAN_POINT('Ctrl Pts',(1.47010395231188,115.080581081869,15.3430692761423));
#41895=CARTESIAN_POINT('Ctrl Pts',(1.69861033226413,115.047205451045,15.15744647314));
#41896=CARTESIAN_POINT('Ctrl Pts',(2.10719160069082,114.975377847186,14.6856154627772));
#41897=CARTESIAN_POINT('Ctrl Pts',(2.27235073686159,114.937009102848,14.3938971371417));
#41898=CARTESIAN_POINT('Ctrl Pts',(2.4547506584159,114.869659507586,13.8372419312285));
#41899=CARTESIAN_POINT('Ctrl Pts',(2.49660250556101,114.840873704305,13.5853658481135));
#41900=CARTESIAN_POINT('Ctrl Pts',(2.50281009642801,114.785206180601,13.0927502466165));
#41901=CARTESIAN_POINT('Ctrl Pts',(2.4716000689058,114.758700075465,12.8547783578521));
#41902=CARTESIAN_POINT('Ctrl Pts',(2.40710702503148,114.732100473491,12.624843892093));
#41903=CARTESIAN_POINT('Ctrl Pts',(2.40671107393509,114.732017803112,12.6249492691423));
#41904=CARTESIAN_POINT('Ctrl Pts',(2.38603655571224,114.719000108274,12.550738421636));
#41905=CARTESIAN_POINT('Ctrl Pts',(2.36192028942924,114.705932228044,12.4776884630487));
#41906=CARTESIAN_POINT('Ctrl Pts',(2.33452665970069,114.692929106293,12.4060060713853));
#41907=CARTESIAN_POINT('Ctrl Pts',(2.33039701405768,114.690968859126,12.3951998044048));
#41908=CARTESIAN_POINT('Ctrl Pts',(2.32619281813754,114.689010075427,12.3844245493953));
#41909=CARTESIAN_POINT('Ctrl Pts',(2.32191456017635,114.68705314018,12.373680944972));
#41910=CARTESIAN_POINT('Ctrl Pts',(2.28917399573477,114.672077146412,12.2914625102381));
#41911=CARTESIAN_POINT('Ctrl Pts',(2.2521012679024,114.657209864433,12.2110977667261));
#41912=CARTESIAN_POINT('Ctrl Pts',(2.21077820277219,114.6424849766,12.1329078564742));
#41913=CARTESIAN_POINT('Ctrl Pts',(2.21077697653088,114.642484539647,12.1329055362277));
#41914=CARTESIAN_POINT('Ctrl Pts',(2.2107757502859,114.642484102693,12.1329032159833));
#41915=CARTESIAN_POINT('Ctrl Pts',(2.2107745240371,114.64248366574,12.1329008957406));
#41916=CARTESIAN_POINT('Ctrl Pts',(2.1698507369237,114.627901152448,12.0554670850472));
#41917=CARTESIAN_POINT('Ctrl Pts',(2.12475641430129,114.613457757854,11.9801627370877));
#41918=CARTESIAN_POINT('Ctrl Pts',(2.07571785117442,114.599065288004,11.9072896599852));
#41919=CARTESIAN_POINT('Ctrl Pts',(2.03735758410725,114.587806822177,11.8502849167503));
#41920=CARTESIAN_POINT('Ctrl Pts',(1.99658309629734,114.576579921931,11.7947685263937));
#41921=CARTESIAN_POINT('Ctrl Pts',(1.95349531511491,114.565353621623,11.7408980764147));
#41922=CARTESIAN_POINT('Ctrl Pts',(1.8986874944664,114.551073725166,11.6723746602703));
#41923=CARTESIAN_POINT('Ctrl Pts',(1.84042639462137,114.536869361689,11.606874339813));
#41924=CARTESIAN_POINT('Ctrl Pts',(1.7790153456993,114.522703384979,11.5446440296108));
#41925=CARTESIAN_POINT('Ctrl Pts',(1.71698406067292,114.508394335478,11.4817852089721));
#41926=CARTESIAN_POINT('Ctrl Pts',(1.6517389305043,114.494124544484,11.4222627597994));
#41927=CARTESIAN_POINT('Ctrl Pts',(1.58356346547917,114.479885790931,11.3663342036022));
#41928=CARTESIAN_POINT('Ctrl Pts',(1.51591781669985,114.465757691892,11.3108402884841));
#41929=CARTESIAN_POINT('Ctrl Pts',(1.44538739137413,114.451660416136,11.2588842683477));
#41930=CARTESIAN_POINT('Ctrl Pts',(1.37221876351566,114.437612544851,11.2107234020551));
#41931=CARTESIAN_POINT('Ctrl Pts',(1.31353379465473,114.426345436076,11.1720959325861));
#41932=CARTESIAN_POINT('Ctrl Pts',(1.2531511881548,114.415110690171,11.1359097259345));
#41933=CARTESIAN_POINT('Ctrl Pts',(1.19118238541695,114.403928443348,11.1023038300403));
#41934=CARTESIAN_POINT('Ctrl Pts',(1.18018643235601,114.401944227811,11.0963406866924));
#41935=CARTESIAN_POINT('Ctrl Pts',(1.16914870734806,114.39996316254,11.0904632670091));
#41936=CARTESIAN_POINT('Ctrl Pts',(1.15806998550336,114.397985378393,11.0846719975152));
#41937=CARTESIAN_POINT('Ctrl Pts',(1.15806078809735,114.397983736463,11.084667189681));
#41938=CARTESIAN_POINT('Ctrl Pts',(1.15805159066309,114.397982094536,11.0846623819063));
#41939=CARTESIAN_POINT('Ctrl Pts',(1.15804239320057,114.39798045261,11.0846575741909));
#41940=CARTESIAN_POINT('Ctrl Pts',(1.08167856283755,114.384348029017,11.0447405253777));
#41941=CARTESIAN_POINT('Ctrl Pts',(1.00336763378465,114.370869434528,11.0089137747217));
#41942=CARTESIAN_POINT('Ctrl Pts',(0.923470403547197,114.357462176603,10.9772313192681));
#41943=CARTESIAN_POINT('Ctrl Pts',(0.842120924938991,114.343811222264,10.9449729891043));
#41944=CARTESIAN_POINT('Ctrl Pts',(0.759126514312415,114.330233992969,10.9170115020167));
#41945=CARTESIAN_POINT('Ctrl Pts',(0.674860844878216,114.316671171922,10.8934318208214));
#41946=CARTESIAN_POINT('Ctrl Pts',(0.589942358421628,114.303003277949,10.8696694647909));
#41947=CARTESIAN_POINT('Ctrl Pts',(0.503732788690918,114.289349949821,10.8503574469222));
#41948=CARTESIAN_POINT('Ctrl Pts',(0.416611040688116,114.275680587882,10.8356037522074));
#41949=CARTESIAN_POINT('Ctrl Pts',(0.358168881629512,114.266511040175,10.8257068229907));
#41950=CARTESIAN_POINT('Ctrl Pts',(0.299316209581032,114.257334914046,10.8178614586516));
#41951=CARTESIAN_POINT('Ctrl Pts',(0.240166277877519,114.248150523747,10.8121047457223));
#41952=CARTESIAN_POINT('Ctrl Pts',(0.155211410934926,114.23495932245,10.8038365911049));
#41953=CARTESIAN_POINT('Ctrl Pts',(0.0700788031493985,114.221816744476,
10.799919257017));
#41954=CARTESIAN_POINT('Ctrl Pts',(-0.0149028882690931,114.208738362147,
10.8003417600113));
#41955=CARTESIAN_POINT('Ctrl Pts',(-0.0208006222667158,114.207830721704,
10.800371081742));
#41956=CARTESIAN_POINT('Ctrl Pts',(-0.0266976415687111,114.206923389794,
10.8004213225244));
#41957=CARTESIAN_POINT('Ctrl Pts',(-0.0325938415091329,114.206016371328,
10.8004924863282));
#41958=CARTESIAN_POINT('Ctrl Pts',(-0.115617731118418,114.193244721498,
10.8014945377932));
#41959=CARTESIAN_POINT('Ctrl Pts',(-0.198477037236091,114.18053572853,10.8066410517021));
#41960=CARTESIAN_POINT('Ctrl Pts',(-0.280897820046986,114.167922066076,
10.8159439136147));
#41961=CARTESIAN_POINT('Ctrl Pts',(-0.288667161823087,114.166733047344,
10.8168208418751));
#41962=CARTESIAN_POINT('Ctrl Pts',(-0.296432625531919,114.165544873754,
10.8177347359478));
#41963=CARTESIAN_POINT('Ctrl Pts',(-0.304193992661227,114.164357571456,
10.8186856271663));
#41964=CARTESIAN_POINT('Ctrl Pts',(-0.304199649362122,114.164356706117,
10.8186863202023));
#41965=CARTESIAN_POINT('Ctrl Pts',(-0.304205306060841,114.164355840778,
10.818687013258));
#41966=CARTESIAN_POINT('Ctrl Pts',(-0.304210962757384,114.16435497544,10.8186877063334));
#41967=CARTESIAN_POINT('Ctrl Pts',(-0.391348216434744,114.151025077656,
10.8293640228845));
#41968=CARTESIAN_POINT('Ctrl Pts',(-0.477972035296507,114.13780468443,10.8446995212591));
#41969=CARTESIAN_POINT('Ctrl Pts',(-0.563722922960105,114.124609062505,
10.8646086883252));
#41970=CARTESIAN_POINT('Ctrl Pts',(-0.62561406599761,114.115085054693,10.8789782317809));
#41971=CARTESIAN_POINT('Ctrl Pts',(-0.687049844929214,114.105574437132,
10.8957310521915));
#41972=CARTESIAN_POINT('Ctrl Pts',(-0.747885721084445,114.096054101726,
10.9148412182077));
#41973=CARTESIAN_POINT('Ctrl Pts',(-0.831713446375473,114.082935723041,
10.9411737352735));
#41974=CARTESIAN_POINT('Ctrl Pts',(-0.913961186335416,114.069866479222,
10.9718430192832));
#41975=CARTESIAN_POINT('Ctrl Pts',(-0.994286798253288,114.056811004444,
11.0066559216147));
#41976=CARTESIAN_POINT('Ctrl Pts',(-1.07540901325354,114.043626056248,11.0418140695614));
#41977=CARTESIAN_POINT('Ctrl Pts',(-1.15457050931461,114.030455293469,11.0811982831899));
#41978=CARTESIAN_POINT('Ctrl Pts',(-1.23142813047825,114.017291787493,11.1246288716901));
#41979=CARTESIAN_POINT('Ctrl Pts',(-1.30769828236307,114.004228898154,11.1677274939373));
#41980=CARTESIAN_POINT('Ctrl Pts',(-1.3816996941409,113.991173464214,11.2148103537045));
#41981=CARTESIAN_POINT('Ctrl Pts',(-1.45310796354058,113.978144094454,11.2657257295881));
#41982=CARTESIAN_POINT('Ctrl Pts',(-1.50981508815594,113.967797140231,11.306158925762));
#41983=CARTESIAN_POINT('Ctrl Pts',(-1.56488724741967,113.957467187443,11.349009316401));
#41984=CARTESIAN_POINT('Ctrl Pts',(-1.61816535072865,113.947172949771,11.3942159583652));
#41985=CARTESIAN_POINT('Ctrl Pts',(-1.63206269290655,113.944487746385,11.4060078978877));
#41986=CARTESIAN_POINT('Ctrl Pts',(-1.6458229034023,113.941807941329,11.4179474284215));
#41987=CARTESIAN_POINT('Ctrl Pts',(-1.65944402960632,113.939133916623,11.4300326652617));
#41988=CARTESIAN_POINT('Ctrl Pts',(-1.65944918529116,113.939132904487,11.4300372396024));
#41989=CARTESIAN_POINT('Ctrl Pts',(-1.65945434095606,113.939131892352,11.430041813964));
#41990=CARTESIAN_POINT('Ctrl Pts',(-1.65945949660102,113.939130880218,11.4300463883465));
#41991=CARTESIAN_POINT('Ctrl Pts',(-1.72416273610041,113.926428617768,11.487454795743));
#41992=CARTESIAN_POINT('Ctrl Pts',(-1.78572985027925,113.913854680771,11.5481503010416));
#41993=CARTESIAN_POINT('Ctrl Pts',(-1.84396740565358,113.901329775944,11.6118290328535));
#41994=CARTESIAN_POINT('Ctrl Pts',(-1.90321619869904,113.888587388506,11.6766134829952));
#41995=CARTESIAN_POINT('Ctrl Pts',(-1.9590181108991,113.875895587199,11.7444861696485));
#41996=CARTESIAN_POINT('Ctrl Pts',(-2.01114658435125,113.863199429364,11.8151322313827));
#41997=CARTESIAN_POINT('Ctrl Pts',(-2.06359350863811,113.850425711191,11.8862098671846));
#41998=CARTESIAN_POINT('Ctrl Pts',(-2.11232137609723,113.837647590056,11.960094833088));
#41999=CARTESIAN_POINT('Ctrl Pts',(-2.15708658914897,113.824838879979,12.0364679833058));
#42000=CARTESIAN_POINT('Ctrl Pts',(-2.18365740274702,113.817236149539,12.0817999855458));
#42001=CARTESIAN_POINT('Ctrl Pts',(-2.20883194412841,113.809623213022,12.128008616839));
#42002=CARTESIAN_POINT('Ctrl Pts',(-2.23255814550346,113.801999384522,12.1750278963945));
#42003=CARTESIAN_POINT('Ctrl Pts',(-2.272374403431,113.789205413959,12.2539335641311));
#42004=CARTESIAN_POINT('Ctrl Pts',(-2.30790217841304,113.776446866853,12.3347046854354));
#42005=CARTESIAN_POINT('Ctrl Pts',(-2.33902960370211,113.763740361142,12.4169872092265));
#42006=CARTESIAN_POINT('Ctrl Pts',(-2.36798167871121,113.751921853732,12.4935193919757));
#42007=CARTESIAN_POINT('Ctrl Pts',(-2.39312741066382,113.74014868853,12.5713592310076));
#42008=CARTESIAN_POINT('Ctrl Pts',(-2.41437667314438,113.728449496644,12.6502582010047));
#42009=CARTESIAN_POINT('Ctrl Pts',(-2.41607055463293,113.727516897473,12.6565476195136));
#42010=CARTESIAN_POINT('Ctrl Pts',(-2.41773966055965,113.7265847667,12.662843790757));
#42011=CARTESIAN_POINT('Ctrl Pts',(-2.41938393675111,113.725653117961,12.6691466003444));
#42012=CARTESIAN_POINT('Ctrl Pts',(-2.42234077420046,113.723977770536,12.6804806958697));
#42013=CARTESIAN_POINT('Ctrl Pts',(-2.42521736162318,113.722304009972,12.6918362489259));
#42014=CARTESIAN_POINT('Ctrl Pts',(-2.42801341001787,113.720631938887,12.7032126026095));
#42015=CARTESIAN_POINT('Ctrl Pts',(-2.42801894130329,113.72062863111,12.7032351078921));
#42016=CARTESIAN_POINT('Ctrl Pts',(-2.42802447227337,113.720625323341,12.7032576132562));
#42017=CARTESIAN_POINT('Ctrl Pts',(-2.42803000292807,113.720622015577,12.7032801187016));
#42018=CARTESIAN_POINT('Ctrl Pts',(-2.44761689028156,113.708907528007,12.7829834538748));
#42019=CARTESIAN_POINT('Ctrl Pts',(-2.46325232600675,113.697274312845,12.863709368401));
#42020=CARTESIAN_POINT('Ctrl Pts',(-2.47488540907793,113.685656562519,12.9451701077313));
#42021=CARTESIAN_POINT('Ctrl Pts',(-2.47571690509852,113.684826162434,12.950992663985));
#42022=CARTESIAN_POINT('Ctrl Pts',(-2.47652793341817,113.68399584297,12.9568189651233));
#42023=CARTESIAN_POINT('Ctrl Pts',(-2.47731846642314,113.683165580842,12.9626489014737));
#42024=CARTESIAN_POINT('Ctrl Pts',(-2.48494713330537,113.67515352674,13.0189079597056));
#42025=CARTESIAN_POINT('Ctrl Pts',(-2.49066846227995,113.667147117449,13.0755059584162));
#42026=CARTESIAN_POINT('Ctrl Pts',(-2.49445986057212,113.659131020065,13.1323371808067));
#42027=CARTESIAN_POINT('Ctrl Pts',(-2.4982010969503,113.651220979274,13.1884165004242));
#42028=CARTESIAN_POINT('Ctrl Pts',(-2.50005122341816,113.643325754841,13.2445504344204));
#42029=CARTESIAN_POINT('Ctrl Pts',(-2.50002326288683,113.63543715375,13.3006174987927));
#42030=CARTESIAN_POINT('Origin',(0.,70.2,13.3));
#42031=CARTESIAN_POINT('',(-2.5,111.608333038426,13.3));
#42032=CARTESIAN_POINT('',(-2.5,112.746400080882,13.3));
#42033=CARTESIAN_POINT('',(-2.5,70.2,13.3));
#42034=CARTESIAN_POINT('Ctrl Pts',(-2.5,112.746400080882,13.2999999999999));
#42035=CARTESIAN_POINT('Ctrl Pts',(-2.5,112.753815786924,13.2504512721242));
#42036=CARTESIAN_POINT('Ctrl Pts',(-2.49852698225489,112.761198580106,13.2008614963978));
#42037=CARTESIAN_POINT('Ctrl Pts',(-2.48028274540318,112.806419689986,12.8946851924858));
#42038=CARTESIAN_POINT('Ctrl Pts',(-2.42555695618829,112.84118494686,12.6420817968267));
#42039=CARTESIAN_POINT('Ctrl Pts',(-2.21899081222048,112.919059926422,12.1053950897869));
#42040=CARTESIAN_POINT('Ctrl Pts',(-2.04929591841819,112.962172914944,11.8332456817295));
#42041=CARTESIAN_POINT('Ctrl Pts',(-1.60442086699413,113.050703854793,11.3534413243468));
#42042=CARTESIAN_POINT('Ctrl Pts',(-1.32811556445397,113.094201856163,11.1553801417068));
#42043=CARTESIAN_POINT('Ctrl Pts',(-0.879925922177475,113.160160743817,
10.9548829918448));
#42044=CARTESIAN_POINT('Ctrl Pts',(-0.733439588801397,113.181027151995,
10.9050249548889));
#42045=CARTESIAN_POINT('Ctrl Pts',(-0.284824237775757,113.24324131313,10.797382739653));
#42046=CARTESIAN_POINT('Ctrl Pts',(0.024324916665919,113.282911646403,10.78133244488));
#42047=CARTESIAN_POINT('Ctrl Pts',(0.652270566389332,113.366151142462,10.8646194126178));
#42048=CARTESIAN_POINT('Ctrl Pts',(0.964289224234859,113.409690487182,10.9704902790412));
#42049=CARTESIAN_POINT('Ctrl Pts',(1.38203089680102,113.473742733204,11.2109255478757));
#42050=CARTESIAN_POINT('Ctrl Pts',(1.50943061924174,113.494103088808,11.3010326495817));
#42051=CARTESIAN_POINT('Ctrl Pts',(1.86959923854331,113.556243189497,11.6099642513656));
#42052=CARTESIAN_POINT('Ctrl Pts',(2.06966085364777,113.597807703668,11.8618964340852));
#42053=CARTESIAN_POINT('Ctrl Pts',(2.29488090205699,113.661365951993,12.2940574152866));
#42054=CARTESIAN_POINT('Ctrl Pts',(2.35745257094803,113.683239454434,12.4509914927382));
#42055=CARTESIAN_POINT('Ctrl Pts',(2.48859592421676,113.745564407196,12.9098662641539));
#42056=CARTESIAN_POINT('Ctrl Pts',(2.51772212539333,113.785664064245,13.2198960333267));
#42057=CARTESIAN_POINT('Ctrl Pts',(2.46033119197494,113.867377867542,13.8482550563151));
#42058=CARTESIAN_POINT('Ctrl Pts',(2.36926741833782,113.908887818044,14.1604597562973));
#42059=CARTESIAN_POINT('Ctrl Pts',(2.14519752951451,113.971987167063,14.5945166550251));
#42060=CARTESIAN_POINT('Ctrl Pts',(2.05437536733974,113.993303992244,14.7342912266888));
#42061=CARTESIAN_POINT('Ctrl Pts',(1.84927709341868,114.035494934116,14.9900518678522));
#42062=CARTESIAN_POINT('Ctrl Pts',(1.73622571015375,114.056263044081,15.1059958276731));
#42063=CARTESIAN_POINT('Ctrl Pts',(1.35751648450548,114.120075409954,15.4257370132797));
#42064=CARTESIAN_POINT('Ctrl Pts',(1.06160829432475,114.162309883462,15.587929557014));
#42065=CARTESIAN_POINT('Ctrl Pts',(0.590639130471669,114.225336214171,15.7344326429001));
#42066=CARTESIAN_POINT('Ctrl Pts',(0.434537905454778,114.245626749545,15.7670825428223));
#42067=CARTESIAN_POINT('Ctrl Pts',(0.112837426690217,114.286850657165,15.8028681481862));
#42068=CARTESIAN_POINT('Ctrl Pts',(-0.0521207760547313,114.307672043328,
15.8048689549461));
#42069=CARTESIAN_POINT('Ctrl Pts',(-0.520815329524812,114.367317752154,
15.7642065263245));
#42070=CARTESIAN_POINT('Ctrl Pts',(-0.818140092689986,114.405780165051,
15.682063214996));
#42071=CARTESIAN_POINT('Ctrl Pts',(-1.24044431316074,114.464991016743,15.4767150278274));
#42072=CARTESIAN_POINT('Ctrl Pts',(-1.3802617770565,114.485534910198,15.390854010734));
#42073=CARTESIAN_POINT('Ctrl Pts',(-1.76464981009766,114.546171400412,15.0993354063904));
#42074=CARTESIAN_POINT('Ctrl Pts',(-1.97946570119846,114.585773662872,14.8599139110405));
#42075=CARTESIAN_POINT('Ctrl Pts',(-2.22891130005095,114.646316726717,14.444328010222));
#42076=CARTESIAN_POINT('Ctrl Pts',(-2.29993057925986,114.666982413506,14.2939082640419));
#42077=CARTESIAN_POINT('Ctrl Pts',(-2.39934061676893,114.703943623379,14.0143321805558));
#42078=CARTESIAN_POINT('Ctrl Pts',(-2.4334205579743,114.720134853252,13.8878527112955));
#42079=CARTESIAN_POINT('Ctrl Pts',(-2.47361631768746,114.747333541985,13.6727824881431));
#42080=CARTESIAN_POINT('Ctrl Pts',(-2.48520435230191,114.75829395106,13.5854870139385));
#42081=CARTESIAN_POINT('Ctrl Pts',(-2.49738731604369,114.777513152509,13.4319620063582));
#42082=CARTESIAN_POINT('Ctrl Pts',(-2.49999999994521,114.78575383967,13.3659884232862));
#42083=CARTESIAN_POINT('Ctrl Pts',(-2.5,114.793997579998,13.3000000020756));
#42084=CARTESIAN_POINT('Ctrl Pts',(-2.49999992423213,113.635422974112,13.300615499269));
#42085=CARTESIAN_POINT('Ctrl Pts',(-2.49993703972846,113.599525349135,13.5560361997111));
#42086=CARTESIAN_POINT('Ctrl Pts',(-2.46072864461712,113.563484692851,13.8099450047488));
#42087=CARTESIAN_POINT('Ctrl Pts',(-2.30125078341498,113.489021137123,14.3144855223787));
#42088=CARTESIAN_POINT('Ctrl Pts',(-2.17642926892917,113.451620898376,14.5602141872255));
#42089=CARTESIAN_POINT('Ctrl Pts',(-1.91840788023706,113.391588607151,14.9111734902358));
#42090=CARTESIAN_POINT('Ctrl Pts',(-1.81015694310975,113.369367075414,15.0319084127732));
#42091=CARTESIAN_POINT('Ctrl Pts',(-1.45341965586932,113.303011864418,15.3595181248978));
#42092=CARTESIAN_POINT('Ctrl Pts',(-1.1758217445381,113.25950062641,15.5296935957019));
#42093=CARTESIAN_POINT('Ctrl Pts',(-0.575113398708736,113.172776977878,
15.753707228805));
#42094=CARTESIAN_POINT('Ctrl Pts',(-0.258131681584966,113.130256384498,
15.8069594504734));
#42095=CARTESIAN_POINT('Ctrl Pts',(0.225640896538735,113.065624474727,15.7952814337151));
#42096=CARTESIAN_POINT('Ctrl Pts',(0.390155687127908,113.043696451551,15.7748992481072));
#42097=CARTESIAN_POINT('Ctrl Pts',(0.709368130684422,113.000177211355,15.7027087118395));
#42098=CARTESIAN_POINT('Ctrl Pts',(0.863446950582938,112.978695790749,15.6517389144345));
#42099=CARTESIAN_POINT('Ctrl Pts',(1.16118397455973,112.935601926959,15.5200083080719));
#42100=CARTESIAN_POINT('Ctrl Pts',(1.30399495537044,112.914070477901,15.4392491879532));
#42101=CARTESIAN_POINT('Ctrl Pts',(1.70549608395798,112.849440648973,15.1569591150295));
#42102=CARTESIAN_POINT('Ctrl Pts',(1.93360969618146,112.80698865331,14.9180853483908));
#42103=CARTESIAN_POINT('Ctrl Pts',(2.25740820833291,112.728316740063,14.4091821727227));
#42104=CARTESIAN_POINT('Ctrl Pts',(2.36601508132898,112.692603330238,14.1533448227506));
#42105=CARTESIAN_POINT('Ctrl Pts',(2.50850694176593,112.614544139567,13.5612253178054));
#42106=CARTESIAN_POINT('Ctrl Pts',(2.52096213046626,112.572601534465,13.2252118158867));
#42107=CARTESIAN_POINT('Ctrl Pts',(2.41709491232301,112.489920817314,12.5898799708317));
#42108=CARTESIAN_POINT('Ctrl Pts',(2.31016801046288,112.450069933046,12.2951335602315));
#42109=CARTESIAN_POINT('Ctrl Pts',(2.07260478440973,112.390452895359,11.8933692380529));
#42110=CARTESIAN_POINT('Ctrl Pts',(1.98087889419261,112.370731470586,11.766889657077));
#42111=CARTESIAN_POINT('Ctrl Pts',(1.65779674484082,112.30887275318,11.3992217548214));
#42112=CARTESIAN_POINT('Ctrl Pts',(1.38968520537882,112.267366551738,11.1952314586677));
#42113=CARTESIAN_POINT('Ctrl Pts',(0.81345988725467,112.187108651779,10.9162411771611));
#42114=CARTESIAN_POINT('Ctrl Pts',(0.515214082937537,112.14909830415,10.8345182190889));
#42115=CARTESIAN_POINT('Ctrl Pts',(0.0426735369502148,112.090135804759,
10.7947556834444));
#42116=CARTESIAN_POINT('Ctrl Pts',(-0.125275961184913,112.069417461386,
10.7975249440082));
#42117=CARTESIAN_POINT('Ctrl Pts',(-0.450578970442157,112.028950133878,
10.8357408701125));
#42118=CARTESIAN_POINT('Ctrl Pts',(-0.607317692404308,112.009294118061,
10.8696164886111));
#42119=CARTESIAN_POINT('Ctrl Pts',(-0.910150655858293,111.97024560837,10.9662157634045));
#42120=CARTESIAN_POINT('Ctrl Pts',(-1.05567456213932,111.950940981782,11.0283319576753));
#42121=CARTESIAN_POINT('Ctrl Pts',(-1.48650189218199,111.890811950433,11.2626256411866));
#42122=CARTESIAN_POINT('Ctrl Pts',(-1.74405103235562,111.850495529867,11.4782126146685));
#42123=CARTESIAN_POINT('Ctrl Pts',(-2.0521156317544,111.790817004304,11.8631430548332));
#42124=CARTESIAN_POINT('Ctrl Pts',(-2.14007229732545,111.771531826763,11.9977590917231));
#42125=CARTESIAN_POINT('Ctrl Pts',(-2.29138224948472,111.732301509873,12.2865903534652));
#42126=CARTESIAN_POINT('Ctrl Pts',(-2.3534748359072,111.712448014133,12.4405854442097));
#42127=CARTESIAN_POINT('Ctrl Pts',(-2.46639860400545,111.664286612685,12.8275089131858));
#42128=CARTESIAN_POINT('Ctrl Pts',(-2.5,111.636366988851,13.0633546777397));
#42129=CARTESIAN_POINT('Ctrl Pts',(-2.5,111.608333038426,13.3000000000001));
#42130=CARTESIAN_POINT('Origin',(0.,70.2,13.3));
#42131=CARTESIAN_POINT('',(-2.50004052090194,109.508185544341,13.2983771895099));
#42132=CARTESIAN_POINT('',(-2.5,110.560415842511,13.3));
#42133=CARTESIAN_POINT('',(-2.5,70.2,13.3));
#42134=CARTESIAN_POINT('',(2.08929110769117,111.244289249369,11.9274842264238));
#42135=CARTESIAN_POINT('Ctrl Pts',(-2.5,110.560415842511,13.3));
#42136=CARTESIAN_POINT('Ctrl Pts',(-2.5,110.584370683036,13.0920730468922));
#42137=CARTESIAN_POINT('Ctrl Pts',(-2.47405787245171,110.608200817813,12.8844414018608));
#42138=CARTESIAN_POINT('Ctrl Pts',(-2.34533043690075,110.666949896553,12.3798636818324));
#42139=CARTESIAN_POINT('Ctrl Pts',(-2.21240249612852,110.700901144954,12.0947971695117));
#42140=CARTESIAN_POINT('Ctrl Pts',(-1.93504890783741,110.754245183841,11.7086651471274));
#42141=CARTESIAN_POINT('Ctrl Pts',(-1.82679420764696,110.77260141554,11.5854759040186));
#42142=CARTESIAN_POINT('Ctrl Pts',(-1.49275364881193,110.82329675654,11.2731990013751));
#42143=CARTESIAN_POINT('Ctrl Pts',(-1.24455563837577,110.854538016865,11.1119955566233));
#42144=CARTESIAN_POINT('Ctrl Pts',(-0.666284738689302,110.921965062839,
10.8673635729908));
#42145=CARTESIAN_POINT('Ctrl Pts',(-0.335518588013175,110.958559556211,
10.8001728934193));
#42146=CARTESIAN_POINT('Ctrl Pts',(0.304137976284174,111.025977192425,10.7998426418367));
#42147=CARTESIAN_POINT('Ctrl Pts',(0.607020187212292,111.056459374609,10.85565220922));
#42148=CARTESIAN_POINT('Ctrl Pts',(1.15445527186085,111.117362606322,11.0648367239618));
#42149=CARTESIAN_POINT('Ctrl Pts',(1.39792202246711,111.146470397471,11.2084369697607));
#42150=CARTESIAN_POINT('Ctrl Pts',(1.79660522546318,111.198230322861,11.5449307811442));
#42151=CARTESIAN_POINT('Ctrl Pts',(1.95729847396441,111.2210116332,11.7261365923488));
#42152=CARTESIAN_POINT('Ctrl Pts',(2.08958333087649,111.244414321256,11.9275418027047));
#42153=CARTESIAN_POINT('Ctrl Pts',(2.09091184280958,111.244255274751,11.9295666139507));
#42154=CARTESIAN_POINT('Ctrl Pts',(2.21253054010004,111.284970005518,12.1151239544681));
#42155=CARTESIAN_POINT('Ctrl Pts',(2.30900676795492,111.322684435055,12.3161256252589));
#42156=CARTESIAN_POINT('Ctrl Pts',(2.4335077814834,111.396411513387,12.699475347969));
#42157=CARTESIAN_POINT('Ctrl Pts',(2.47041201735562,111.430872891983,12.8763747611042));
#42158=CARTESIAN_POINT('Ctrl Pts',(2.51455206744934,111.52046245954,13.3255314183865));
#42159=CARTESIAN_POINT('Ctrl Pts',(2.49698051169547,111.576796334274,13.5981174230396));
#42160=CARTESIAN_POINT('Ctrl Pts',(2.37858078191885,111.673883613869,14.1105762969879));
#42161=CARTESIAN_POINT('Ctrl Pts',(2.28459425240552,111.711900278876,14.3464732099622));
#42162=CARTESIAN_POINT('Ctrl Pts',(1.99690981083706,111.799221855829,14.8366222558941));
#42163=CARTESIAN_POINT('Ctrl Pts',(1.78845502181753,111.84947094421,15.0747534766737));
#42164=CARTESIAN_POINT('Ctrl Pts',(1.30072923679471,111.95792292333,15.4567854333267));
#42165=CARTESIAN_POINT('Ctrl Pts',(1.02715427425439,112.014195572234,15.5997573803887));
#42166=CARTESIAN_POINT('Ctrl Pts',(0.460068335352404,112.107566443777,15.7739788484136));
#42167=CARTESIAN_POINT('Ctrl Pts',(0.173105402682947,112.145123549888,15.8105554982885));
#42168=CARTESIAN_POINT('Ctrl Pts',(-0.400038856030687,112.226856181371,
15.7842923455795));
#42169=CARTESIAN_POINT('Ctrl Pts',(-0.680788012692494,112.270155761364,
15.7223579870173));
#42170=CARTESIAN_POINT('Ctrl Pts',(-1.17642460918943,112.355810486072,15.5200529135176));
#42171=CARTESIAN_POINT('Ctrl Pts',(-1.39271240502498,112.396836001962,15.3912018963467));
#42172=CARTESIAN_POINT('Ctrl Pts',(-1.78057712168394,112.471085378176,15.0727642185427));
#42173=CARTESIAN_POINT('Ctrl Pts',(-1.94979358068073,112.503478099725,14.8848190501461));
#42174=CARTESIAN_POINT('Ctrl Pts',(-2.2108818967367,112.56679614799,14.4881925581217));
#42175=CARTESIAN_POINT('Ctrl Pts',(-2.3079716862597,112.597127401879,14.2863784741139));
#42176=CARTESIAN_POINT('Ctrl Pts',(-2.45861922979916,112.667161857475,13.8240036655302));
#42177=CARTESIAN_POINT('Ctrl Pts',(-2.50000000000002,112.707104458557,13.5625573460289));
#42178=CARTESIAN_POINT('Ctrl Pts',(-2.5,112.746400080882,13.2999999999999));
#42179=CARTESIAN_POINT('',(2.02616441126019,110.570072536149,11.8332575276011));
#42180=CARTESIAN_POINT('Ctrl Pts',(-2.5,111.608333038426,13.3000000000001));
#42181=CARTESIAN_POINT('Ctrl Pts',(-2.5,111.599099972718,13.3779398471102));
#42182=CARTESIAN_POINT('Ctrl Pts',(-2.49635527151303,111.589849429157,13.4559658240946));
#42183=CARTESIAN_POINT('Ctrl Pts',(-2.45782573638485,111.540839411838,13.8661148409415));
#42184=CARTESIAN_POINT('Ctrl Pts',(-2.36038044542047,111.500725318644,14.188839459168));
#42185=CARTESIAN_POINT('Ctrl Pts',(-2.07403389666084,111.429575424823,14.7219765098093));
#42186=CARTESIAN_POINT('Ctrl Pts',(-1.90754689405118,111.398723164012,14.938585373499));
#42187=CARTESIAN_POINT('Ctrl Pts',(-1.60894576554472,111.352314194306,15.2184023803056));
#42188=CARTESIAN_POINT('Ctrl Pts',(-1.50082700824554,111.336760607205,15.3041176577776));
#42189=CARTESIAN_POINT('Ctrl Pts',(-1.10869991052263,111.282813234414,15.5653884913637));
#42190=CARTESIAN_POINT('Ctrl Pts',(-0.797013834972896,111.243261016893,
15.6928940675935));
#42191=CARTESIAN_POINT('Ctrl Pts',(-0.20644117228775,111.174112361976,15.8058178927713));
#42192=CARTESIAN_POINT('Ctrl Pts',(0.0630844876198906,111.144594308231,
15.8135337508679));
#42193=CARTESIAN_POINT('Ctrl Pts',(0.468275405891716,111.100142798027,15.7597809139009));
#42194=CARTESIAN_POINT('Ctrl Pts',(0.605959960202172,111.084978704884,15.7295292123011));
#42195=CARTESIAN_POINT('Ctrl Pts',(1.05860852404524,111.033049732935,15.5891847846559));
#42196=CARTESIAN_POINT('Ctrl Pts',(1.35384735043083,110.994368749858,15.4279096556827));
#42197=CARTESIAN_POINT('Ctrl Pts',(1.81164290653522,110.927253643264,15.0430450286317));
#42198=CARTESIAN_POINT('Ctrl Pts',(1.98618968804743,110.898960372943,14.841242264169));
#42199=CARTESIAN_POINT('Ctrl Pts',(2.2986154924933,110.837435784167,14.3364359854441));
#42200=CARTESIAN_POINT('Ctrl Pts',(2.41469370167995,110.804257223341,14.0259655219129));
#42201=CARTESIAN_POINT('Ctrl Pts',(2.51465739242552,110.736456998861,13.4123130466841));
#42202=CARTESIAN_POINT('Ctrl Pts',(2.51050112902319,110.704723726827,13.1164427349614));
#42203=CARTESIAN_POINT('Ctrl Pts',(2.41984859048833,110.656429980299,12.6449855490945));
#42204=CARTESIAN_POINT('Ctrl Pts',(2.36432368622815,110.638620572774,12.4664997137897));
#42205=CARTESIAN_POINT('Ctrl Pts',(2.21797786032354,110.604334355112,12.1328542246681));
#42206=CARTESIAN_POINT('Ctrl Pts',(2.12933557305595,110.587912623738,11.9780460502149));
#42207=CARTESIAN_POINT('Ctrl Pts',(2.02504033628985,110.570623332967,11.8339810245433));
#42208=CARTESIAN_POINT('Ctrl Pts',(2.0259834028522,110.570059235584,11.8329696480696));
#42209=CARTESIAN_POINT('Ctrl Pts',(1.97582883419295,110.552650219366,11.7640425834076));
#42210=CARTESIAN_POINT('Ctrl Pts',(1.92223002912362,110.535504701489,11.6978035383405));
#42211=CARTESIAN_POINT('Ctrl Pts',(1.86548929155874,110.518551901166,11.6344613355438));
#42212=CARTESIAN_POINT('Ctrl Pts',(1.80790616229344,110.501347413978,11.570178733517));
#42213=CARTESIAN_POINT('Ctrl Pts',(1.74708657362578,110.484341204005,11.508879272392));
#42214=CARTESIAN_POINT('Ctrl Pts',(1.68330635111696,110.467480210923,11.4508013479066));
#42215=CARTESIAN_POINT('Ctrl Pts',(1.61950186928453,110.450612804625,11.3927013330129));
#42216=CARTESIAN_POINT('Ctrl Pts',(1.55273409637837,110.43389064751,11.3378249928812));
#42217=CARTESIAN_POINT('Ctrl Pts',(1.48324649033605,110.417283438422,11.2864357495786));
#42218=CARTESIAN_POINT('Ctrl Pts',(1.42375348366725,110.403064891299,11.2424379668282));
#42219=CARTESIAN_POINT('Ctrl Pts',(1.36226614263345,110.388930975654,11.2009965189817));
#42220=CARTESIAN_POINT('Ctrl Pts',(1.29892115578174,110.374876370531,11.1622943661129));
#42221=CARTESIAN_POINT('Ctrl Pts',(1.22445648225379,110.358354596133,11.1167983715373));
#42222=CARTESIAN_POINT('Ctrl Pts',(1.14782225782505,110.342029277239,11.0753299337114));
#42223=CARTESIAN_POINT('Ctrl Pts',(1.06928416796316,110.325917111898,11.0380836744721));
#42224=CARTESIAN_POINT('Ctrl Pts',(1.02577658878568,110.316991489814,11.0174504431856));
#42225=CARTESIAN_POINT('Ctrl Pts',(0.981683939057707,110.308131636343,10.9981133110716));
#42226=CARTESIAN_POINT('Ctrl Pts',(0.937046037671465,110.299342770227,10.9801092332557));
#42227=CARTESIAN_POINT('Ctrl Pts',(0.858005356480925,110.28378025624,10.9482292718198));
#42228=CARTESIAN_POINT('Ctrl Pts',(0.777257832873348,110.268440135178,10.9205269907542));
#42229=CARTESIAN_POINT('Ctrl Pts',(0.695160321559169,110.253234098766,10.897021913865));
#42230=CARTESIAN_POINT('Ctrl Pts',(0.611789196225796,110.237792164568,10.8731521926038));
#42231=CARTESIAN_POINT('Ctrl Pts',(0.527024854495964,110.222488069096,10.8536110550817));
#42232=CARTESIAN_POINT('Ctrl Pts',(0.441234528753111,110.20724710615,10.8384635423577));
#42233=CARTESIAN_POINT('Ctrl Pts',(0.417057286598754,110.202951931274,10.8341947034181));
#42234=CARTESIAN_POINT('Ctrl Pts',(0.392798569153779,110.198661898692,10.8302750711374));
#42235=CARTESIAN_POINT('Ctrl Pts',(0.368466654843724,110.194375653523,10.826706696421));
#42236=CARTESIAN_POINT('Ctrl Pts',(0.282443181651797,110.179221987779,10.8140910023639));
#42237=CARTESIAN_POINT('Ctrl Pts',(0.19595745502032,110.164192193344,10.8059297038895));
#42238=CARTESIAN_POINT('Ctrl Pts',(0.109387378581065,110.149245055312,10.8021945677738));
#42239=CARTESIAN_POINT('Ctrl Pts',(0.0220758111051781,110.134169891877,
10.7984274394264));
#42240=CARTESIAN_POINT('Ctrl Pts',(-0.0653219079878356,110.119178777285,
10.7991625921094));
#42241=CARTESIAN_POINT('Ctrl Pts',(-0.152435635049384,110.104255973227,
10.8044063858373));
#42242=CARTESIAN_POINT('Ctrl Pts',(-0.238684278608216,110.089481360184,
10.8095981060334));
#42243=CARTESIAN_POINT('Ctrl Pts',(-0.324654979384985,110.074773830453,
10.8192092014915));
#42244=CARTESIAN_POINT('Ctrl Pts',(-0.409999891052358,110.060143180545,
10.8332816511376));
#42245=CARTESIAN_POINT('Ctrl Pts',(-0.4809571128161,110.047979007546,10.8449817268748));
#42246=CARTESIAN_POINT('Ctrl Pts',(-0.551482154344233,110.03586847296,10.8597662429117));
#42247=CARTESIAN_POINT('Ctrl Pts',(-0.621377267313918,110.023829482762,
10.877680368726));
#42248=CARTESIAN_POINT('Ctrl Pts',(-0.63996173885094,110.020628425332,10.8824435710039));
#42249=CARTESIAN_POINT('Ctrl Pts',(-0.658480264399054,110.017436224663,
10.8874226251331));
#42250=CARTESIAN_POINT('Ctrl Pts',(-0.676929533158853,110.014253319914,
10.8926171017569));
#42251=CARTESIAN_POINT('Ctrl Pts',(-0.759203825065035,110.000059194509,
10.9157818077194));
#42252=CARTESIAN_POINT('Ctrl Pts',(-0.840100886012136,109.986048767545,
10.9432268422863));
#42253=CARTESIAN_POINT('Ctrl Pts',(-0.919344599337146,109.972139976636,
10.974720389118));
#42254=CARTESIAN_POINT('Ctrl Pts',(-0.999967450718988,109.957989120558,
11.0067620418771));
#42255=CARTESIAN_POINT('Ctrl Pts',(-1.07887934449036,109.943943116139,11.0429950496292));
#42256=CARTESIAN_POINT('Ctrl Pts',(-1.1557750062517,109.929936373207,11.083214494394));
#42257=CARTESIAN_POINT('Ctrl Pts',(-1.23323378236241,109.915827057545,11.1237284700328));
#42258=CARTESIAN_POINT('Ctrl Pts',(-1.30864686734369,109.901757368578,11.1682879839491));
#42259=CARTESIAN_POINT('Ctrl Pts',(-1.38168314252135,109.887685442195,11.2167136948761));
#42260=CARTESIAN_POINT('Ctrl Pts',(-1.4264895574882,109.879052573509,11.2464219801574));
#42261=CARTESIAN_POINT('Ctrl Pts',(-1.4704010521126,109.870419374408,11.2775858824778));
#42262=CARTESIAN_POINT('Ctrl Pts',(-1.51333730239647,109.861781232391,11.3101686399619));
#42263=CARTESIAN_POINT('Ctrl Pts',(-1.58329352947783,109.847707068475,11.3632558743251));
#42264=CARTESIAN_POINT('Ctrl Pts',(-1.65029388636087,109.833693403166,11.419828104897));
#42265=CARTESIAN_POINT('Ctrl Pts',(-1.71407378502022,109.819743665232,11.4796389819029));
#42266=CARTESIAN_POINT('Ctrl Pts',(-1.77788889059502,109.805786226951,11.5394828748986));
#42267=CARTESIAN_POINT('Ctrl Pts',(-1.83848059659025,109.791893020877,11.6025689225187));
#42268=CARTESIAN_POINT('Ctrl Pts',(-1.89558038405761,109.778091251272,11.6686926200149));
#42269=CARTESIAN_POINT('Ctrl Pts',(-1.93576271336663,109.768378653802,11.7152252658578));
#42270=CARTESIAN_POINT('Ctrl Pts',(-1.97421575088245,109.758711851372,11.7632631138));
#42271=CARTESIAN_POINT('Ctrl Pts',(-2.01084182042605,109.749106280255,11.8127476638983));
#42272=CARTESIAN_POINT('Ctrl Pts',(-2.06270050352498,109.735505796372,11.8828126103645));
#42273=CARTESIAN_POINT('Ctrl Pts',(-2.11089855002028,109.722027164445,11.9557779476345));
#42274=CARTESIAN_POINT('Ctrl Pts',(-2.15524570805872,109.708587080166,12.0313151593601));
#42275=CARTESIAN_POINT('Ctrl Pts',(-2.15963214624348,109.707257703009,12.0387866485049));
#42276=CARTESIAN_POINT('Ctrl Pts',(-2.16398087591946,109.705928721963,12.0462833028258));
#42277=CARTESIAN_POINT('Ctrl Pts',(-2.16829169123313,109.704600069358,12.0538048056359));
#42278=CARTESIAN_POINT('Ctrl Pts',(-2.21145628653423,109.691296147059,12.1291183139242));
#42279=CARTESIAN_POINT('Ctrl Pts',(-2.25059811686777,109.678091178631,12.2065321513085));
#42280=CARTESIAN_POINT('Ctrl Pts',(-2.28561957442646,109.664932737475,12.2856685751055));
#42281=CARTESIAN_POINT('Ctrl Pts',(-2.32106659166802,109.651614402858,12.365766617115));
#42282=CARTESIAN_POINT('Ctrl Pts',(-2.35229235428514,109.638343638471,12.4476295826256));
#42283=CARTESIAN_POINT('Ctrl Pts',(-2.37917363327936,109.6250968897,12.5308869451382));
#42284=CARTESIAN_POINT('Ctrl Pts',(-2.40595432564599,109.611899708726,12.6138327682587));
#42285=CARTESIAN_POINT('Ctrl Pts',(-2.4284230937876,109.598726455936,12.6981626291549));
#42286=CARTESIAN_POINT('Ctrl Pts',(-2.4464367953254,109.585584108856,12.7835290813987));
#42287=CARTESIAN_POINT('Ctrl Pts',(-2.45800778408427,109.577142204232,12.8383636892235));
#42288=CARTESIAN_POINT('Ctrl Pts',(-2.46774018617838,109.568713666937,12.8936263828342));
#42289=CARTESIAN_POINT('Ctrl Pts',(-2.47559063569568,109.560306591779,12.9492290970707));
#42290=CARTESIAN_POINT('Ctrl Pts',(-2.47775855570292,109.557984958299,12.9645839167385));
#42291=CARTESIAN_POINT('Ctrl Pts',(-2.47978290586993,109.555664992123,12.9799646820784));
#42292=CARTESIAN_POINT('Ctrl Pts',(-2.4816630983293,109.553346874686,12.9953658093138));
#42293=CARTESIAN_POINT('Ctrl Pts',(-2.49395830740612,109.538187927313,13.0960789455856));
#42294=CARTESIAN_POINT('Ctrl Pts',(-2.50004583450027,109.523164566333,13.1972739658029));
#42295=CARTESIAN_POINT('Ctrl Pts',(-2.50004052090194,109.508185544341,13.2983771895099));
#42296=CARTESIAN_POINT('Origin',(0.,70.2,13.3));
#42297=CARTESIAN_POINT('',(-2.5,107.398963164072,13.3));
#42298=CARTESIAN_POINT('',(-2.5,108.597702566458,13.299999999993));
#42299=CARTESIAN_POINT('',(-2.5,70.2,13.3));
#42300=CARTESIAN_POINT('',(-2.49999996234878,108.597761318563,13.2995661151097));
#42301=CARTESIAN_POINT('Ctrl Pts',(-2.5,108.597702566458,13.2999999999859));
#42302=CARTESIAN_POINT('Ctrl Pts',(-2.5,108.597723045119,13.2998487659079));
#42303=CARTESIAN_POINT('Ctrl Pts',(-2.49999998745624,108.597742181868,13.2997074408026));
#42304=CARTESIAN_POINT('Ctrl Pts',(-2.4999999606093,108.597762660402,13.2995562055454));
#42305=CARTESIAN_POINT('Ctrl Pts',(-2.49999996234878,108.597761318563,13.2995661151097));
#42306=CARTESIAN_POINT('Ctrl Pts',(-2.49996127400753,108.627272326748,13.0816254657993));
#42307=CARTESIAN_POINT('Ctrl Pts',(-2.47142480948102,108.656429210505,12.8646035671895));
#42308=CARTESIAN_POINT('Ctrl Pts',(-2.35878302773443,108.715080836125,12.4434629014955));
#42309=CARTESIAN_POINT('Ctrl Pts',(-2.27515727800989,108.744218171731,12.2411369514137));
#42310=CARTESIAN_POINT('Ctrl Pts',(-2.00804038715987,108.815466700751,11.7773812837939));
#42311=CARTESIAN_POINT('Ctrl Pts',(-1.79885867136011,108.857325226278,11.5351391029824));
#42312=CARTESIAN_POINT('Ctrl Pts',(-1.41973717840134,108.921060982191,11.2355641456908));
#42313=CARTESIAN_POINT('Ctrl Pts',(-1.27957677521832,108.942797951022,11.1458790846607));
#42314=CARTESIAN_POINT('Ctrl Pts',(-0.986031723585365,108.986018769111,
10.9968767095871));
#42315=CARTESIAN_POINT('Ctrl Pts',(-0.833613895820597,109.007394625194,
10.9374322248134));
#42316=CARTESIAN_POINT('Ctrl Pts',(-0.518255591179365,109.050243261842,
10.8487906492423));
#42317=CARTESIAN_POINT('Ctrl Pts',(-0.356013778143492,109.071585227966,
10.8200251510171));
#42318=CARTESIAN_POINT('Ctrl Pts',(-0.0310359412977735,109.113974241321,
10.7949773096619));
#42319=CARTESIAN_POINT('Ctrl Pts',(0.130877516573796,109.134921306702,10.7982053575935));
#42320=CARTESIAN_POINT('Ctrl Pts',(0.623673653758929,109.199183677247,10.8560294543235));
#42321=CARTESIAN_POINT('Ctrl Pts',(0.94483595807269,109.241569698108,10.9613507794186));
#42322=CARTESIAN_POINT('Ctrl Pts',(1.37356403589125,109.304782593515,11.2051359347462));
#42323=CARTESIAN_POINT('Ctrl Pts',(1.50361457831467,109.325059272149,11.2964334774443));
#42324=CARTESIAN_POINT('Ctrl Pts',(1.87842726030939,109.388089661664,11.6167319908891));
#42325=CARTESIAN_POINT('Ctrl Pts',(2.08655389220884,109.430035043802,11.8828873049376));
#42326=CARTESIAN_POINT('Ctrl Pts',(2.30710833395787,109.492416408326,12.3240707169627));
#42327=CARTESIAN_POINT('Ctrl Pts',(2.36439699616986,109.512421640674,12.472463658104));
#42328=CARTESIAN_POINT('Ctrl Pts',(2.49719917562092,109.574437830974,12.9462728999172));
#42329=CARTESIAN_POINT('Ctrl Pts',(2.52207078606059,109.615761043397,13.2820615962384));
#42330=CARTESIAN_POINT('Ctrl Pts',(2.46015235542664,109.677429094164,13.772962846743));
#42331=CARTESIAN_POINT('Ctrl Pts',(2.42450068824604,109.697451690676,13.9307479769561));
#42332=CARTESIAN_POINT('Ctrl Pts',(2.26886088138479,109.759062269446,14.4020150172217));
#42333=CARTESIAN_POINT('Ctrl Pts',(2.10098182948669,109.800109140089,14.6957355776455));
#42334=CARTESIAN_POINT('Ctrl Pts',(1.68267620470091,109.878046746828,15.1730827795599));
#42335=CARTESIAN_POINT('Ctrl Pts',(1.44618714468181,109.914280049486,15.3611640261789));
#42336=CARTESIAN_POINT('Ctrl Pts',(1.03611523545117,109.97105894972,15.5812048451219));
#42337=CARTESIAN_POINT('Ctrl Pts',(0.882749733962537,109.991209696826,15.6448214532444));
#42338=CARTESIAN_POINT('Ctrl Pts',(0.577555683805002,110.029900944934,15.7371929611169));
#42339=CARTESIAN_POINT('Ctrl Pts',(0.427113075503393,110.048367266475,15.7680074854576));
#42340=CARTESIAN_POINT('Ctrl Pts',(0.116823992327557,110.085886237418,15.8023209407108));
#42341=CARTESIAN_POINT('Ctrl Pts',(-0.0424516464144428,110.104848827156,
15.8046874082007));
#42342=CARTESIAN_POINT('Ctrl Pts',(-0.534757737709349,110.163928021299,
15.7650022335554));
#42343=CARTESIAN_POINT('Ctrl Pts',(-0.859875376778409,110.203875710064,
15.6712549565493));
#42344=CARTESIAN_POINT('Ctrl Pts',(-1.43277381060917,110.280367266776,15.3722037298678));
#42345=CARTESIAN_POINT('Ctrl Pts',(-1.67938483606652,110.316287342787,15.1779110623556));
#42346=CARTESIAN_POINT('Ctrl Pts',(-2.09144447462872,110.390048498595,14.7055117149096));
#42347=CARTESIAN_POINT('Ctrl Pts',(-2.25203633660929,110.426789327045,14.4304877623833));
#42348=CARTESIAN_POINT('Ctrl Pts',(-2.40975463661823,110.481207127063,13.984080209621));
#42349=CARTESIAN_POINT('Ctrl Pts',(-2.44810946395696,110.499150595612,13.8307031217425));
#42350=CARTESIAN_POINT('Ctrl Pts',(-2.49060203845772,110.531575425718,13.5504203653099));
#42351=CARTESIAN_POINT('Ctrl Pts',(-2.5,110.545997076194,13.4251542520052));
#42352=CARTESIAN_POINT('Ctrl Pts',(-2.5,110.560415842511,13.3));
#42353=CARTESIAN_POINT('Ctrl Pts',(-2.49999946874101,109.50813782114,13.2983701856957));
#42354=CARTESIAN_POINT('Ctrl Pts',(-2.50014743099999,109.47470183367,13.5253319738356));
#42355=CARTESIAN_POINT('Ctrl Pts',(-2.46938886651776,109.440797156689,13.7512018334646));
#42356=CARTESIAN_POINT('Ctrl Pts',(-2.36318482247125,109.382484222952,14.1331322874585));
#42357=CARTESIAN_POINT('Ctrl Pts',(-2.30127816868861,109.358753517347,14.2914353476029));
#42358=CARTESIAN_POINT('Ctrl Pts',(-2.07118790625412,109.290656635913,14.7392882519759));
#42359=CARTESIAN_POINT('Ctrl Pts',(-1.86090928673608,109.247048972379,15.0024460208004));
#42360=CARTESIAN_POINT('Ctrl Pts',(-1.35980338407567,109.153226386204,15.4221056702417));
#42361=CARTESIAN_POINT('Ctrl Pts',(-1.07736098827051,109.104562298503,15.5784834082954));
#42362=CARTESIAN_POINT('Ctrl Pts',(-0.479117324911624,109.012092543446,
15.7730932116796));
#42363=CARTESIAN_POINT('Ctrl Pts',(-0.169891597185701,108.971233355369,
15.8133531162263));
#42364=CARTESIAN_POINT('Ctrl Pts',(0.297431111595153,108.906425226583,15.7873004866538));
#42365=CARTESIAN_POINT('Ctrl Pts',(0.454547365927925,108.884460358984,15.7634386301251));
#42366=CARTESIAN_POINT('Ctrl Pts',(0.767729463762711,108.840092224318,15.6848675151351));
#42367=CARTESIAN_POINT('Ctrl Pts',(0.922787692247484,108.817669590434,15.6292634571929));
#42368=CARTESIAN_POINT('Ctrl Pts',(1.2187766126299,108.772826789759,15.4888892061383));
#42369=CARTESIAN_POINT('Ctrl Pts',(1.35908275732209,108.750560573587,15.4046496363571));
#42370=CARTESIAN_POINT('Ctrl Pts',(1.75766305512708,108.682865954791,15.1087570784973));
#42371=CARTESIAN_POINT('Ctrl Pts',(1.9827987061679,108.638676048485,14.858694122639));
#42372=CARTESIAN_POINT('Ctrl Pts',(2.23407575843589,108.572044204741,14.4334636244901));
#42373=CARTESIAN_POINT('Ctrl Pts',(2.30231004488894,108.55030637558,14.2875230706927));
#42374=CARTESIAN_POINT('Ctrl Pts',(2.40924604020111,108.507167369673,13.9861680929474));
#42375=CARTESIAN_POINT('Ctrl Pts',(2.44801163505166,108.485966866797,13.8315454927465));
#42376=CARTESIAN_POINT('Ctrl Pts',(2.51860834899393,108.423068640535,13.3653015499732));
#42377=CARTESIAN_POINT('Ctrl Pts',(2.50705167997413,108.381664188897,13.0502553988117));
#42378=CARTESIAN_POINT('Ctrl Pts',(2.4005401620259,108.31816355143,12.5820011505177));
#42379=CARTESIAN_POINT('Ctrl Pts',(2.34699396469652,108.296160270614,12.4226532248292));
#42380=CARTESIAN_POINT('Ctrl Pts',(2.15206948111612,108.233728377247,11.9916235638509));
#42381=CARTESIAN_POINT('Ctrl Pts',(1.97630606161899,108.193578333358,11.7387499853495));
#42382=CARTESIAN_POINT('Ctrl Pts',(1.53221773170734,108.111950150126,11.2988824867021));
#42383=CARTESIAN_POINT('Ctrl Pts',(1.26407436406757,108.070456391872,11.1195683870759));
#42384=CARTESIAN_POINT('Ctrl Pts',(0.824114986157931,108.008260926605,10.9344777583247));
#42385=CARTESIAN_POINT('Ctrl Pts',(0.673313458835044,107.987932630849,10.8872181441702));
#42386=CARTESIAN_POINT('Ctrl Pts',(0.194063553655871,107.92465414115,10.7854985471525));
#42387=CARTESIAN_POINT('Ctrl Pts',(-0.141442500289415,107.882026430039,
10.7819903818547));
#42388=CARTESIAN_POINT('Ctrl Pts',(-0.627082419382444,107.818166943961,
10.8744986208313));
#42389=CARTESIAN_POINT('Ctrl Pts',(-0.783030632525979,107.797270221791,
10.9202620179646));
#42390=CARTESIAN_POINT('Ctrl Pts',(-1.13257268861168,107.748631656285,11.0609479751009));
#42391=CARTESIAN_POINT('Ctrl Pts',(-1.32058333814669,107.721062016685,11.1664198722666));
#42392=CARTESIAN_POINT('Ctrl Pts',(-1.60728945842999,107.675792686956,11.3798476374749));
#42393=CARTESIAN_POINT('Ctrl Pts',(-1.71426404682308,107.657941223723,11.4747135352435));
#42394=CARTESIAN_POINT('Ctrl Pts',(-1.90423831957223,107.623402092554,11.6747019854949));
#42395=CARTESIAN_POINT('Ctrl Pts',(-1.98805520560998,107.606773674294,11.7783719607084));
#42396=CARTESIAN_POINT('Ctrl Pts',(-2.14135866623276,107.572660840051,12.0024138083965));
#42397=CARTESIAN_POINT('Ctrl Pts',(-2.20987733010779,107.555228240195,12.1228920186611));
#42398=CARTESIAN_POINT('Ctrl Pts',(-2.40063239072227,107.497679759308,12.5343124453017));
#42399=CARTESIAN_POINT('Ctrl Pts',(-2.47793576315712,107.457483744812,12.8427016530759));
#42400=CARTESIAN_POINT('Ctrl Pts',(-2.49864139718994,107.41110563653,13.2048244838333));
#42401=CARTESIAN_POINT('Ctrl Pts',(-2.5,107.405028168214,13.252414849999));
#42402=CARTESIAN_POINT('Ctrl Pts',(-2.5,107.398963164072,13.3));
#42403=CARTESIAN_POINT('Origin',(0.,70.2,13.3));
#42404=CARTESIAN_POINT('',(-2.5,105.533497732924,13.3000000000002));
#42405=CARTESIAN_POINT('',(-2.50000333388702,106.437958303058,13.3001965898202));
#42406=CARTESIAN_POINT('',(-2.5,70.2,13.3));
#42407=CARTESIAN_POINT('',(1.45735612640718,107.079506406801,11.2679629878995));
#42408=CARTESIAN_POINT('Ctrl Pts',(-2.49999999227335,106.437958007126,13.3001965534331));
#42409=CARTESIAN_POINT('Ctrl Pts',(-2.50001798642019,106.465898559144,13.0713256237538));
#42410=CARTESIAN_POINT('Ctrl Pts',(-2.46860680580814,106.493594969784,12.8435143817534));
#42411=CARTESIAN_POINT('Ctrl Pts',(-2.34842960455445,106.547184092487,12.4162042342614));
#42412=CARTESIAN_POINT('Ctrl Pts',(-2.26377157410827,106.572863318266,12.2176117785873));
#42413=CARTESIAN_POINT('Ctrl Pts',(-2.07813421178431,106.616731300532,11.902077945352));
#42414=CARTESIAN_POINT('Ctrl Pts',(-1.98986892198254,106.63477730416,11.7790615650358));
#42415=CARTESIAN_POINT('Ctrl Pts',(-1.68153582826976,106.690900301041,11.4224960813028));
#42416=CARTESIAN_POINT('Ctrl Pts',(-1.42740292158903,106.728163934818,11.2227080745087));
#42417=CARTESIAN_POINT('Ctrl Pts',(-0.995223984362087,106.785184092776,
11.0006671495818));
#42418=CARTESIAN_POINT('Ctrl Pts',(-0.840824854642511,106.804547713125,
10.9398258010325));
#42419=CARTESIAN_POINT('Ctrl Pts',(-0.382829581973324,106.859949198179,
10.8100535828494));
#42420=CARTESIAN_POINT('Ctrl Pts',(-0.0709278463260396,106.895164958428,
10.781787400615));
#42421=CARTESIAN_POINT('Ctrl Pts',(0.465570512213512,106.956956057592,10.8331351265117));
#42422=CARTESIAN_POINT('Ctrl Pts',(0.688930644507382,106.98296512778,10.8859626872702));
#42423=CARTESIAN_POINT('Ctrl Pts',(1.09893413324957,107.032530831421,11.0445790864913));
#42424=CARTESIAN_POINT('Ctrl Pts',(1.2854182595164,107.05593391797,11.1454026727805));
#42425=CARTESIAN_POINT('Ctrl Pts',(1.45701176931329,107.079469279784,11.2684693691498));
#42426=CARTESIAN_POINT('Ctrl Pts',(1.45691314277681,107.080279081049,11.2683986379203));
#42427=CARTESIAN_POINT('Ctrl Pts',(1.62602378470569,107.115794291604,11.389672191585));
#42428=CARTESIAN_POINT('Ctrl Pts',(1.7793776066286,107.15046473624,11.5316147053649));
#42429=CARTESIAN_POINT('Ctrl Pts',(2.05462324138204,107.22120768442,11.8589364513814));
#42430=CARTESIAN_POINT('Ctrl Pts',(2.17314512138307,107.257330168275,12.0447646756983));
#42431=CARTESIAN_POINT('Ctrl Pts',(2.40216586590629,107.345457840436,12.5360399190128));
#42432=CARTESIAN_POINT('Ctrl Pts',(2.48063478144839,107.395677705901,12.8520967298161));
#42433=CARTESIAN_POINT('Ctrl Pts',(2.5130889845337,107.49750342118,13.4974568467129));
#42434=CARTESIAN_POINT('Ctrl Pts',(2.46650567299891,107.546631730194,13.8206323311975));
#42435=CARTESIAN_POINT('Ctrl Pts',(2.25539462242128,107.644707133605,14.4236686416826));
#42436=CARTESIAN_POINT('Ctrl Pts',(2.09580227720739,107.691798446146,14.6989862592695));
#42437=CARTESIAN_POINT('Ctrl Pts',(1.68105237624616,107.786334762015,15.1775017715823));
#42438=CARTESIAN_POINT('Ctrl Pts',(1.42903676626015,107.832842343291,15.375786349681));
#42439=CARTESIAN_POINT('Ctrl Pts',(0.849619493980127,107.928189837091,15.6748306721696));
#42440=CARTESIAN_POINT('Ctrl Pts',(0.524851876498055,107.97624700749,15.7670445384718));
#42441=CARTESIAN_POINT('Ctrl Pts',(-0.13419844394631,108.070733519944,15.8176769949132));
#42442=CARTESIAN_POINT('Ctrl Pts',(-0.461719755941352,108.117147165353,
15.7786256839406));
#42443=CARTESIAN_POINT('Ctrl Pts',(-1.08299346969568,108.209251354498,15.5767776770374));
#42444=CARTESIAN_POINT('Ctrl Pts',(-1.37080309473312,108.254946622623,15.4160212472238));
#42445=CARTESIAN_POINT('Ctrl Pts',(-1.74653250618216,108.323596181201,15.0964960092678));
#42446=CARTESIAN_POINT('Ctrl Pts',(-1.86238445182696,108.346567621202,14.9760981856762));
#42447=CARTESIAN_POINT('Ctrl Pts',(-2.13505286930052,108.407606029766,14.6292511053334));
#42448=CARTESIAN_POINT('Ctrl Pts',(-2.26803346760061,108.445269726053,14.386932257422));
#42449=CARTESIAN_POINT('Ctrl Pts',(-2.45230623455293,108.521241908179,13.8618389889636));
#42450=CARTESIAN_POINT('Ctrl Pts',(-2.50000000000159,108.559525276668,13.5819377266705));
#42451=CARTESIAN_POINT('Ctrl Pts',(-2.5,108.597702566458,13.2999999999859));
#42452=CARTESIAN_POINT('Ctrl Pts',(-2.5,107.398963164072,13.3));
#42453=CARTESIAN_POINT('Ctrl Pts',(-2.5,107.388587973973,13.3814022489794));
#42454=CARTESIAN_POINT('Ctrl Pts',(-2.49602417443423,107.378253537848,13.462789778904));
#42455=CARTESIAN_POINT('Ctrl Pts',(-2.47821031759599,107.355161879218,13.6445350202945));
#42456=CARTESIAN_POINT('Ctrl Pts',(-2.46224293867941,107.342441498577,13.7445140910394));
#42457=CARTESIAN_POINT('Ctrl Pts',(-2.41181399250324,107.313307970256,13.9710369640909));
#42458=CARTESIAN_POINT('Ctrl Pts',(-2.37337316566617,107.29695349493,14.0963916290613));
#42459=CARTESIAN_POINT('Ctrl Pts',(-2.2813654615178,107.265649596051,14.3294058349301));
#42460=CARTESIAN_POINT('Ctrl Pts',(-2.22951262688311,107.25074202421,14.4373561312345));
#42461=CARTESIAN_POINT('Ctrl Pts',(-2.07417327432608,107.211714841503,14.7089580026402));
#42462=CARTESIAN_POINT('Ctrl Pts',(-1.95907952149779,107.187708358492,14.865045300933));
#42463=CARTESIAN_POINT('Ctrl Pts',(-1.67039468351634,107.135041185485,15.1741757722895));
#42464=CARTESIAN_POINT('Ctrl Pts',(-1.49124220078996,107.106610164872,15.3196416303595));
#42465=CARTESIAN_POINT('Ctrl Pts',(-1.04993368060304,107.042470588755,15.5868208327022));
#42466=CARTESIAN_POINT('Ctrl Pts',(-0.781452470515746,107.00715018963,15.6919146642682));
#42467=CARTESIAN_POINT('Ctrl Pts',(-0.200041920490081,106.933773294451,
15.8108508768705));
#42468=CARTESIAN_POINT('Ctrl Pts',(0.10974706912583,106.896361534273,15.8164168905719));
#42469=CARTESIAN_POINT('Ctrl Pts',(0.716563545998488,106.820564402393,15.7148315686896));
#42470=CARTESIAN_POINT('Ctrl Pts',(1.00837663178938,106.782922632074,15.6082628215899));
#42471=CARTESIAN_POINT('Ctrl Pts',(1.55683602445739,106.70510839167,15.2836056075017));
#42472=CARTESIAN_POINT('Ctrl Pts',(1.804287188546,106.665485186369,15.0615259766754));
#42473=CARTESIAN_POINT('Ctrl Pts',(2.17104976337721,106.590690820608,14.5714349524458));
#42474=CARTESIAN_POINT('Ctrl Pts',(2.30089102815796,106.556612477708,14.3178170038338));
#42475=CARTESIAN_POINT('Ctrl Pts',(2.43296860039397,106.503752799261,13.8965039837913));
#42476=CARTESIAN_POINT('Ctrl Pts',(2.46590292276778,106.484922098114,13.7409956117158));
#42477=CARTESIAN_POINT('Ctrl Pts',(2.52171257568214,106.426112166352,13.251876296912));
#42478=CARTESIAN_POINT('Ctrl Pts',(2.49278335522221,106.386359418917,12.9160821442861));
#42479=CARTESIAN_POINT('Ctrl Pts',(2.31119325403085,106.309567356957,12.2974392628104));
#42480=CARTESIAN_POINT('Ctrl Pts',(2.16865671539812,106.27323487974,12.0179348538109));
#42481=CARTESIAN_POINT('Ctrl Pts',(1.87727006989814,106.216993599097,11.6406986597147));
#42482=CARTESIAN_POINT('Ctrl Pts',(1.76326224051283,106.197451366672,11.5200185245298));
#42483=CARTESIAN_POINT('Ctrl Pts',(1.4062358441955,106.141937833872,11.2103203415651));
#42484=CARTESIAN_POINT('Ctrl Pts',(1.13919984286605,106.106598416615,11.0535522118528));
#42485=CARTESIAN_POINT('Ctrl Pts',(0.705936943052217,106.053440846938,10.8968226522371));
#42486=CARTESIAN_POINT('Ctrl Pts',(0.556949731090647,106.035801919639,10.8579907344719));
#42487=CARTESIAN_POINT('Ctrl Pts',(0.0972717715450301,105.981491291937,
10.7824586441877));
#42488=CARTESIAN_POINT('Ctrl Pts',(-0.217687028212233,105.944831568633,
10.7899816313777));
#42489=CARTESIAN_POINT('Ctrl Pts',(-0.808106094379333,105.876435302433,
10.9163297644695));
#42490=CARTESIAN_POINT('Ctrl Pts',(-1.0801857468759,105.845039753081,11.0266526925972));
#42491=CARTESIAN_POINT('Ctrl Pts',(-1.61218472171108,105.774757757908,11.3598969928922));
#42492=CARTESIAN_POINT('Ctrl Pts',(-1.8583483329386,105.735794988364,11.5941963304945));
#42493=CARTESIAN_POINT('Ctrl Pts',(-2.21631095716883,105.666924364116,12.1076374659539));
#42494=CARTESIAN_POINT('Ctrl Pts',(-2.33932955088605,105.636981418308,12.3719473583166));
#42495=CARTESIAN_POINT('Ctrl Pts',(-2.47134358727144,105.582009656608,12.8633873336436));
#42496=CARTESIAN_POINT('Ctrl Pts',(-2.5,105.557440002256,13.0814498945321));
#42497=CARTESIAN_POINT('Ctrl Pts',(-2.5,105.533497732924,13.3000000000004));
#42498=CARTESIAN_POINT('Origin',(0.,70.2,13.3));
#42499=CARTESIAN_POINT('',(-2.50003871369437,103.603837493162,13.2999999833246));
#42500=CARTESIAN_POINT('',(-2.5,104.491842419534,13.3));
#42501=CARTESIAN_POINT('',(-2.5,70.2,13.3));
#42502=CARTESIAN_POINT('',(-0.0771081494294188,104.870757121609,10.8023559268293));
#42503=CARTESIAN_POINT('Ctrl Pts',(-2.5,104.491842419534,13.3));
#42504=CARTESIAN_POINT('Ctrl Pts',(-2.5,104.515014746024,13.0770988191812));
#42505=CARTESIAN_POINT('Ctrl Pts',(-2.47018808345436,104.537763921925,12.8547935006237));
#42506=CARTESIAN_POINT('Ctrl Pts',(-2.36817301427408,104.578231563052,12.4826513121143));
#42507=CARTESIAN_POINT('Ctrl Pts',(-2.31017230605444,104.595256815441,12.3307634735551));
#42508=CARTESIAN_POINT('Ctrl Pts',(-2.10833292898536,104.641830880163,11.9254613436518));
#42509=CARTESIAN_POINT('Ctrl Pts',(-1.93445262603939,104.669970953774,11.6899135363534));
#42510=CARTESIAN_POINT('Ctrl Pts',(-1.48578658328471,104.730245552284,11.262700707031));
#42511=CARTESIAN_POINT('Ctrl Pts',(-1.20518080907228,104.763270768522,11.0851054799438));
#42512=CARTESIAN_POINT('Ctrl Pts',(-0.635850580826999,104.820912496787,
10.8659274407985));
#42513=CARTESIAN_POINT('Ctrl Pts',(-0.358400677651412,104.84553105741,10.8099051765678));
#42514=CARTESIAN_POINT('Ctrl Pts',(-0.0774247329654312,104.870995320611,
10.8011992054737));
#42515=CARTESIAN_POINT('Ctrl Pts',(-0.0767123097838143,104.870816751188,
10.8022856266005));
#42516=CARTESIAN_POINT('Ctrl Pts',(-0.0223177348150291,104.878477929272,
10.8001035155528));
#42517=CARTESIAN_POINT('Ctrl Pts',(0.0320873656158203,104.886295266453,
10.7999829501676));
#42518=CARTESIAN_POINT('Ctrl Pts',(0.0863615600831533,104.894160010526,
10.8017387475656));
#42519=CARTESIAN_POINT('Ctrl Pts',(0.120678810323465,104.899132841409,10.8028489278138));
#42520=CARTESIAN_POINT('Ctrl Pts',(0.154944755651476,104.904124748766,10.8047090968772));
#42521=CARTESIAN_POINT('Ctrl Pts',(0.189134306212569,104.909109517031,10.8072718680335));
#42522=CARTESIAN_POINT('Ctrl Pts',(0.269346731325135,104.920804328593,10.8132844094704));
#42523=CARTESIAN_POINT('Ctrl Pts',(0.349139807491138,104.932459741272,10.8231604950264));
#42524=CARTESIAN_POINT('Ctrl Pts',(0.428273375004075,104.944050329601,10.8368704813559));
#42525=CARTESIAN_POINT('Ctrl Pts',(0.436481208700324,104.945252520081,10.8382924984759));
#42526=CARTESIAN_POINT('Ctrl Pts',(0.444681975098596,104.946454016347,10.8397557979769));
#42527=CARTESIAN_POINT('Ctrl Pts',(0.452875424696013,104.94765479224,10.8412603731459));
#42528=CARTESIAN_POINT('Ctrl Pts',(0.478581129502685,104.951422044393,10.8459807494289));
#42529=CARTESIAN_POINT('Ctrl Pts',(0.504214836405781,104.955182106315,10.8511071745682));
#42530=CARTESIAN_POINT('Ctrl Pts',(0.529769172972489,104.958933982361,10.8566393738351));
#42531=CARTESIAN_POINT('Ctrl Pts',(0.529797434998153,104.958938131779,10.8566454922158));
#42532=CARTESIAN_POINT('Ctrl Pts',(0.52982569692664,104.958942281187,10.8566516110931));
#42533=CARTESIAN_POINT('Ctrl Pts',(0.529853958757947,104.958946430585,10.8566577304671));
#42534=CARTESIAN_POINT('Ctrl Pts',(0.609649687591697,104.970662028134,10.8739354470389));
#42535=CARTESIAN_POINT('Ctrl Pts',(0.688673893735166,104.982299532234,10.8951699354422));
#42536=CARTESIAN_POINT('Ctrl Pts',(0.766635019018041,104.993914622409,10.9202985827422));
#42537=CARTESIAN_POINT('Ctrl Pts',(0.77264163974443,104.994809522799,10.9222346534845));
#42538=CARTESIAN_POINT('Ctrl Pts',(0.778641930049558,104.995704288225,10.9241938566037));
#42539=CARTESIAN_POINT('Ctrl Pts',(0.784635746401502,104.996598943195,10.926176171165));
#42540=CARTESIAN_POINT('Ctrl Pts',(0.826373752028617,105.002828882849,10.9399800402623));
#42541=CARTESIAN_POINT('Ctrl Pts',(0.867798332419425,105.009053175507,10.9549038079222));
#42542=CARTESIAN_POINT('Ctrl Pts',(0.908860953515595,105.015278002027,10.9709380285799));
#42543=CARTESIAN_POINT('Ctrl Pts',(0.991712109179066,105.027837698833,11.0032899261498));
#42544=CARTESIAN_POINT('Ctrl Pts',(1.07264720441223,105.040334468887,11.039989888498));
#42545=CARTESIAN_POINT('Ctrl Pts',(1.15131842734291,105.052799988542,11.0808198028244));
#42546=CARTESIAN_POINT('Ctrl Pts',(1.22998965027359,105.065265508198,11.1216497171509));
#42547=CARTESIAN_POINT('Ctrl Pts',(1.3063963941909,105.07769946929,11.1666090994476));
#42548=CARTESIAN_POINT('Ctrl Pts',(1.3802058218432,105.09010954104,11.2154881414483));
#42549=CARTESIAN_POINT('Ctrl Pts',(1.38021285402431,105.090110723407,11.215492798391));
#42550=CARTESIAN_POINT('Ctrl Pts',(1.38021988618185,105.090111905775,11.2154974553693));
#42551=CARTESIAN_POINT('Ctrl Pts',(1.38022691831581,105.090113088142,11.2155021123832));
#42552=CARTESIAN_POINT('Ctrl Pts',(1.45391807892792,105.102503353383,11.2643039077924));
#42553=CARTESIAN_POINT('Ctrl Pts',(1.52502286575103,105.114869774911,11.3170138546018));
#42554=CARTESIAN_POINT('Ctrl Pts',(1.59323035299045,105.127242949573,11.3734193901038));
#42555=CARTESIAN_POINT('Ctrl Pts',(1.64632972673284,105.136875437915,11.417330971251));
#42556=CARTESIAN_POINT('Ctrl Pts',(1.69767277560963,105.146511559921,11.4634822423969));
#42557=CARTESIAN_POINT('Ctrl Pts',(1.74710941870683,105.156157570951,11.5117740752752));
#42558=CARTESIAN_POINT('Ctrl Pts',(1.81048733976164,105.168523785306,11.5736843462808));
#42559=CARTESIAN_POINT('Ctrl Pts',(1.87039492239607,105.180841025181,11.6387822943887));
#42560=CARTESIAN_POINT('Ctrl Pts',(1.92662844542012,105.193108828271,11.7067719615592));
#42561=CARTESIAN_POINT('Ctrl Pts',(1.96714642331521,105.201948156624,11.7557606018463));
#42562=CARTESIAN_POINT('Ctrl Pts',(2.00575746861655,105.210761464845,11.8062510992187));
#42563=CARTESIAN_POINT('Ctrl Pts',(2.04238978974739,105.219544953973,11.8581462872837));
#42564=CARTESIAN_POINT('Ctrl Pts',(2.04240145913173,105.219547751992,11.8581628187203));
#42565=CARTESIAN_POINT('Ctrl Pts',(2.04241312831511,105.219550550007,11.8581793502997));
#42566=CARTESIAN_POINT('Ctrl Pts',(2.04242479729753,105.21955334802,11.8581958820219));
#42567=CARTESIAN_POINT('Ctrl Pts',(2.09087546388037,105.231170948197,11.9268370822175));
#42568=CARTESIAN_POINT('Ctrl Pts',(2.13586585416883,105.242737817032,11.9979391885498));
#42569=CARTESIAN_POINT('Ctrl Pts',(2.17721560855768,105.254298993246,12.0712284238331));
#42570=CARTESIAN_POINT('Ctrl Pts',(2.18047416711808,105.255210069268,12.0770039663617));
#42571=CARTESIAN_POINT('Ctrl Pts',(2.18371008994331,105.256121107944,12.082793091901));
#42572=CARTESIAN_POINT('Ctrl Pts',(2.18692327512376,105.257032130292,12.0885956662356));
#42573=CARTESIAN_POINT('Ctrl Pts',(2.23092026546228,105.269506432018,12.168048232023));
#42574=CARTESIAN_POINT('Ctrl Pts',(2.27065881057391,105.281977987509,12.2500219681585));
#42575=CARTESIAN_POINT('Ctrl Pts',(2.30589542182622,105.294478480049,12.3341511912473));
#42576=CARTESIAN_POINT('Ctrl Pts',(2.33996226830475,105.306563988421,12.4154875407277));
#42577=CARTESIAN_POINT('Ctrl Pts',(2.36964148514218,105.318612847026,12.4984093401656));
#42578=CARTESIAN_POINT('Ctrl Pts',(2.39485288630369,105.330634405139,12.5825331581062));
#42579=CARTESIAN_POINT('Ctrl Pts',(2.42034091503532,105.342787867638,12.6675800095266));
#42580=CARTESIAN_POINT('Ctrl Pts',(2.44126312560911,105.354913086582,12.7538544208005));
#42581=CARTESIAN_POINT('Ctrl Pts',(2.4575459223763,105.367004861023,12.8409935595597));
#42582=CARTESIAN_POINT('Ctrl Pts',(2.46751060912787,105.374404741172,12.8943206528073));
#42583=CARTESIAN_POINT('Ctrl Pts',(2.475737958404,105.381791826925,12.9479723280063));
#42584=CARTESIAN_POINT('Ctrl Pts',(2.48221055097361,105.389163087704,13.0018737295152));
#42585=CARTESIAN_POINT('Ctrl Pts',(2.48221345153975,105.389166390991,13.0018978843772));
#42586=CARTESIAN_POINT('Ctrl Pts',(2.4822163517532,105.389169694274,13.0019220392895));
#42587=CARTESIAN_POINT('Ctrl Pts',(2.48221925161395,105.389172997555,13.001946194252));
#42588=CARTESIAN_POINT('Ctrl Pts',(2.49200947540987,105.40032520752,13.083495795978));
#42589=CARTESIAN_POINT('Ctrl Pts',(2.49778328797554,105.411442318619,13.1656207611822));
#42590=CARTESIAN_POINT('Ctrl Pts',(2.49948722327461,105.422563640583,13.2480287371168));
#42591=CARTESIAN_POINT('Ctrl Pts',(2.4996162514713,105.423405787652,13.2542689696737));
#42592=CARTESIAN_POINT('Ctrl Pts',(2.49972192247862,105.424247957049,13.2605108108624));
#42593=CARTESIAN_POINT('Ctrl Pts',(2.49980420337392,105.425090164947,13.2667541264527));
#42594=CARTESIAN_POINT('Ctrl Pts',(2.49997792983122,105.426868388118,13.27993615486));
#42595=CARTESIAN_POINT('Ctrl Pts',(2.50004746740122,105.428646758056,13.2931247595324));
#42596=CARTESIAN_POINT('Ctrl Pts',(2.50001257456669,105.43042539916,13.3063186690347));
#42597=CARTESIAN_POINT('Ctrl Pts',(2.49978032346598,105.442264258336,13.3941389921994));
#42598=CARTESIAN_POINT('Ctrl Pts',(2.49492252226676,105.454055084379,13.4817379211726));
#42599=CARTESIAN_POINT('Ctrl Pts',(2.48551198524104,105.465824827408,13.5687387848905));
#42600=CARTESIAN_POINT('Ctrl Pts',(2.47598579827656,105.477739213622,13.6568088378094));
#42601=CARTESIAN_POINT('Ctrl Pts',(2.46179440573668,105.489631756767,13.7442651823317));
#42602=CARTESIAN_POINT('Ctrl Pts',(2.44301432508079,105.501514401093,13.8307279010647));
#42603=CARTESIAN_POINT('Ctrl Pts',(2.42427314145891,105.513372434257,13.9170115394533));
#42604=CARTESIAN_POINT('Ctrl Pts',(2.40096309316782,105.525220298167,14.0023050920439));
#42605=CARTESIAN_POINT('Ctrl Pts',(2.37315395086311,105.537058232586,14.0862526435496));
#42606=CARTESIAN_POINT('Ctrl Pts',(2.3585587874749,105.543271174544,14.13031111241));
#42607=CARTESIAN_POINT('Ctrl Pts',(2.34272417772455,105.549481216242,14.1739992488483));
#42608=CARTESIAN_POINT('Ctrl Pts',(2.32565797445764,105.555687556788,14.2172685452003));
#42609=CARTESIAN_POINT('Ctrl Pts',(2.32565424479426,105.555688913127,14.2172780013111));
#42610=CARTESIAN_POINT('Ctrl Pts',(2.32565051507209,105.555690269466,14.2172874574019));
#42611=CARTESIAN_POINT('Ctrl Pts',(2.32564678529104,105.555691625805,14.2172969134728));
#42612=CARTESIAN_POINT('Ctrl Pts',(2.3181041697723,105.558434506029,14.2364196196085));
#42613=CARTESIAN_POINT('Ctrl Pts',(2.3103209622381,105.56117666083,14.2554605617107));
#42614=CARTESIAN_POINT('Ctrl Pts',(2.30229812250341,105.563918672576,14.2744151213525));
#42615=CARTESIAN_POINT('Ctrl Pts',(2.26825350326511,105.575554296482,14.354848083642));
#42616=CARTESIAN_POINT('Ctrl Pts',(2.23006911326562,105.587128688416,14.4333113867564));
#42617=CARTESIAN_POINT('Ctrl Pts',(2.18795192015606,105.598676768125,14.5094947206022));
#42618=CARTESIAN_POINT('Ctrl Pts',(2.14520393250849,105.610397804888,14.5868190618925));
#42619=CARTESIAN_POINT('Ctrl Pts',(2.09840447483234,105.622091544948,14.6617935829058));
#42620=CARTESIAN_POINT('Ctrl Pts',(2.04777528699326,105.633778478258,14.7340913729177));
#42621=CARTESIAN_POINT('Ctrl Pts',(1.99706699511466,105.645483671462,14.8065021224197));
#42622=CARTESIAN_POINT('Ctrl Pts',(1.94251772866277,105.657181761271,14.8762271029557));
#42623=CARTESIAN_POINT('Ctrl Pts',(1.88434978160436,105.668880968815,14.9429486422004));
#42624=CARTESIAN_POINT('Ctrl Pts',(1.84060283042637,105.677679709137,14.9931285792183));
#42625=CARTESIAN_POINT('Ctrl Pts',(1.79480924101796,105.686478796312,15.0416099965999));
#42626=CARTESIAN_POINT('Ctrl Pts',(1.74705831743356,105.695278621781,15.0882638213829));
#42627=CARTESIAN_POINT('Ctrl Pts',(1.70289359002632,105.703417561593,15.1314138444479));
#42628=CARTESIAN_POINT('Ctrl Pts',(1.65721598349889,105.711527384435,15.1728430380111));
#42629=CARTESIAN_POINT('Ctrl Pts',(1.6101210606777,105.719607721275,15.2124907827542));
#42630=CARTESIAN_POINT('Ctrl Pts',(1.61009827249629,105.71961163117,15.2125099674125));
#42631=CARTESIAN_POINT('Ctrl Pts',(1.61007548398255,105.719615541058,15.2125291516533));
#42632=CARTESIAN_POINT('Ctrl Pts',(1.61005269513633,105.719619450939,15.2125483354769));
#42633=CARTESIAN_POINT('Ctrl Pts',(1.5467607321213,105.730478449014,15.2658279899057));
#42634=CARTESIAN_POINT('Ctrl Pts',(1.4809054610739,105.741285214015,15.3158927283671));
#42635=CARTESIAN_POINT('Ctrl Pts',(1.41273687818421,105.752072263208,15.3625790913589));
#42636=CARTESIAN_POINT('Ctrl Pts',(1.40908368282409,105.752650347662,15.3650810416332));
#42637=CARTESIAN_POINT('Ctrl Pts',(1.40542384247143,105.753228374396,15.3675732771162));
#42638=CARTESIAN_POINT('Ctrl Pts',(1.40175739531424,105.753806348042,15.3700557685084));
#42639=CARTESIAN_POINT('Ctrl Pts',(1.32696265084648,105.765596887837,15.4206980664509));
#42640=CARTESIAN_POINT('Ctrl Pts',(1.24941903782708,105.777365741811,15.4672896711794));
#42641=CARTESIAN_POINT('Ctrl Pts',(1.16947577736157,105.789139938805,15.5095991769402));
#42642=CARTESIAN_POINT('Ctrl Pts',(1.08953251689606,105.800914135799,15.5519086827011));
#42643=CARTESIAN_POINT('Ctrl Pts',(1.00719045863905,105.812693416674,15.5899352425771));
#42644=CARTESIAN_POINT('Ctrl Pts',(0.922814149414468,105.824492674449,15.6234487947611));
#42645=CARTESIAN_POINT('Ctrl Pts',(0.840494140845276,105.83600437732,15.656145601819));
#42646=CARTESIAN_POINT('Ctrl Pts',(0.756669532738083,105.847474872144,15.6843759250257));
#42647=CARTESIAN_POINT('Ctrl Pts',(0.671717354500609,105.858911300001,15.708074851585));
#42648=CARTESIAN_POINT('Ctrl Pts',(0.593676842397612,105.869417265889,15.7298456454992));
#42649=CARTESIAN_POINT('Ctrl Pts',(0.514684904131195,105.879894301432,15.7477928776352));
#42650=CARTESIAN_POINT('Ctrl Pts',(0.434999958783847,105.890345964829,15.7618732428008));
#42651=CARTESIAN_POINT('Ctrl Pts',(0.4272820147099,105.891358268386,15.7632370069398));
#42652=CARTESIAN_POINT('Ctrl Pts',(0.41955753635055,105.892370336641,15.7645644729712));
#42653=CARTESIAN_POINT('Ctrl Pts',(0.411826737618222,105.893382174577,15.7658555860788));
#42654=CARTESIAN_POINT('Ctrl Pts',(0.392933753176928,105.895854964135,15.7690108848645));
#42655=CARTESIAN_POINT('Ctrl Pts',(0.374003051985269,105.898326358889,15.7719492196747));
#42656=CARTESIAN_POINT('Ctrl Pts',(0.355037683276059,105.900796413385,15.7746699389306));
#42657=CARTESIAN_POINT('Ctrl Pts',(0.355009411215707,105.900800095545,15.7746739947621));
#42658=CARTESIAN_POINT('Ctrl Pts',(0.35498113907849,105.900803777703,15.7746780501095));
#42659=CARTESIAN_POINT('Ctrl Pts',(0.354952866863997,105.900807459857,15.7746821049729));
#42660=CARTESIAN_POINT('Ctrl Pts',(0.275362966415399,105.91117319594,15.7860970640957));
#42661=CARTESIAN_POINT('Ctrl Pts',(0.195159535661565,105.921516126916,15.7936796314266));
#42662=CARTESIAN_POINT('Ctrl Pts',(0.114613373662538,105.931860908419,15.7973747524082));
#42663=CARTESIAN_POINT('Ctrl Pts',(0.106607492758985,105.932889127351,15.7977420287348));
#42664=CARTESIAN_POINT('Ctrl Pts',(0.0985982516142945,105.933917360959,
15.798070866006));
#42665=CARTESIAN_POINT('Ctrl Pts',(0.0905859339165349,105.934945631065,
15.7983611885636));
#42666=CARTESIAN_POINT('Ctrl Pts',(0.0466598291122464,105.940582938786,
15.7999528302801));
#42667=CARTESIAN_POINT('Ctrl Pts',(0.00264108292224348,105.946221279131,
15.8003879064293));
#42668=CARTESIAN_POINT('Ctrl Pts',(-0.0414220991200776,105.951863558129,
15.7996569773884));
#42669=CARTESIAN_POINT('Ctrl Pts',(-0.129649252143588,105.963161022121,
15.7981934473992));
#42670=CARTESIAN_POINT('Ctrl Pts',(-0.217598499637906,105.974416486348,
15.7920619921095));
#42671=CARTESIAN_POINT('Ctrl Pts',(-0.304876011434223,105.985647005872,
15.7813383723747));
#42672=CARTESIAN_POINT('Ctrl Pts',(-0.393111830651169,105.997000836545,
15.7704970072533));
#42673=CARTESIAN_POINT('Ctrl Pts',(-0.480659965460766,106.00832890011,15.7549624067265));
#42674=CARTESIAN_POINT('Ctrl Pts',(-0.567127395333113,106.019642960363,
15.7348227819865));
#42675=CARTESIAN_POINT('Ctrl Pts',(-0.653120786905656,106.030894993817,
15.7147935682241));
#42676=CARTESIAN_POINT('Ctrl Pts',(-0.738044605572204,106.042132906577,
15.6902108041284));
#42677=CARTESIAN_POINT('Ctrl Pts',(-0.82153966473669,106.053366615165,15.661159983255));
#42678=CARTESIAN_POINT('Ctrl Pts',(-0.880797051696853,106.061339305087,
15.6405422874149));
#42679=CARTESIAN_POINT('Ctrl Pts',(-0.939335435527555,106.06930983994,15.6176741808237));
#42680=CARTESIAN_POINT('Ctrl Pts',(-0.997036660975464,106.077282331523,
15.5925799698115));
#42681=CARTESIAN_POINT('Ctrl Pts',(-1.00076673224388,106.077797709863,15.5909577651742));
#42682=CARTESIAN_POINT('Ctrl Pts',(-1.00449242144962,106.078312974203,15.5893266403852));
#42683=CARTESIAN_POINT('Ctrl Pts',(-1.00821370359685,106.078828125878,15.5876866136242));
#42684=CARTESIAN_POINT('Ctrl Pts',(-1.00822934511551,106.078830291195,15.5876797201643));
#42685=CARTESIAN_POINT('Ctrl Pts',(-1.00824498655625,106.07883245651,15.587672826547));
#42686=CARTESIAN_POINT('Ctrl Pts',(-1.00826062791905,106.078834621822,15.5876659327723));
#42687=CARTESIAN_POINT('Ctrl Pts',(-1.08779081575265,106.089844387037,15.5526137953467));
#42688=CARTESIAN_POINT('Ctrl Pts',(-1.16531048809033,106.100803409767,15.5134950297588));
#42689=CARTESIAN_POINT('Ctrl Pts',(-1.24053283900543,106.111734164408,15.4705020308001));
#42690=CARTESIAN_POINT('Ctrl Pts',(-1.31708027702335,106.122857470888,15.4267516842214));
#42691=CARTESIAN_POINT('Ctrl Pts',(-1.39124746951981,106.133951294818,15.378989002505));
#42692=CARTESIAN_POINT('Ctrl Pts',(-1.46271281470655,106.145032236782,15.3274294926996));
#42693=CARTESIAN_POINT('Ctrl Pts',(-1.53466997760064,106.156189436735,15.2755151552525));
#42694=CARTESIAN_POINT('Ctrl Pts',(-1.60388692214073,106.167333327671,15.2197519602795));
#42695=CARTESIAN_POINT('Ctrl Pts',(-1.67003393079078,106.178477253816,15.1603726532369));
#42696=CARTESIAN_POINT('Ctrl Pts',(-1.71410383774848,106.185901804047,15.1208116724761));
#42697=CARTESIAN_POINT('Ctrl Pts',(-1.75681112493626,106.193326301304,15.079645902846));
#42698=CARTESIAN_POINT('Ctrl Pts',(-1.79806070250911,106.200754649183,15.0369449333695));
#42699=CARTESIAN_POINT('Ctrl Pts',(-1.85480992413589,106.210974219538,14.978198955275));
#42700=CARTESIAN_POINT('Ctrl Pts',(-1.90852777793187,106.221152183826,14.9168293454672));
#42701=CARTESIAN_POINT('Ctrl Pts',(-1.95906553464639,106.231300987436,14.8530814438934));
#42702=CARTESIAN_POINT('Ctrl Pts',(-1.96366259469882,106.232224151872,14.8472827509794));
#42703=CARTESIAN_POINT('Ctrl Pts',(-1.96823334005503,106.233147077082,14.8414643440128));
#42704=CARTESIAN_POINT('Ctrl Pts',(-1.97277765705257,106.234069773669,14.835626386468));
#42705=CARTESIAN_POINT('Ctrl Pts',(-2.00522579949362,106.240658176343,14.7939411611458));
#42706=CARTESIAN_POINT('Ctrl Pts',(-2.03632730304487,106.247234868703,14.7512605436525));
#42707=CARTESIAN_POINT('Ctrl Pts',(-2.06604550345792,106.253804188614,14.7076421634946));
#42708=CARTESIAN_POINT('Ctrl Pts',(-2.06605822524938,106.253807000814,14.7076234913029));
#42709=CARTESIAN_POINT('Ctrl Pts',(-2.06607094678712,106.253809813013,14.707604818939));
#42710=CARTESIAN_POINT('Ctrl Pts',(-2.06608366807114,106.25381262521,14.707586146403));
#42711=CARTESIAN_POINT('Ctrl Pts',(-2.11184912614115,106.263929645628,14.6404107604048));
#42712=CARTESIAN_POINT('Ctrl Pts',(-2.15433513971328,106.27402966425,14.5710071336948));
#42713=CARTESIAN_POINT('Ctrl Pts',(-2.19338512292969,106.284124772629,14.4996089412343));
#42714=CARTESIAN_POINT('Ctrl Pts',(-2.19856502698409,106.285463869052,14.4901381103622));
#42715=CARTESIAN_POINT('Ctrl Pts',(-2.20368439823283,106.286802872529,14.4806321937328));
#42716=CARTESIAN_POINT('Ctrl Pts',(-2.2087428039534,106.288141805273,14.4710917482332));
#42717=CARTESIAN_POINT('Ctrl Pts',(-2.24920320147823,106.298851454537,14.3947811004121));
#42718=CARTESIAN_POINT('Ctrl Pts',(-2.28576704144237,106.309556811497,14.3162608832952));
#42719=CARTESIAN_POINT('Ctrl Pts',(-2.31823081051596,106.320268892542,14.2358441526627));
#42720=CARTESIAN_POINT('Ctrl Pts',(-2.32043139778229,106.320995021079,14.2303930285795));
#42721=CARTESIAN_POINT('Ctrl Pts',(-2.32261312579945,106.321721179361,14.2249331926951));
#42722=CARTESIAN_POINT('Ctrl Pts',(-2.32477592260554,106.322447370315,14.2194647439171));
#42723=CARTESIAN_POINT('Ctrl Pts',(-2.35733730491164,106.333380335086,14.1371360430508));
#42724=CARTESIAN_POINT('Ctrl Pts',(-2.38544381125838,106.344264515039,14.0532814442699));
#42725=CARTESIAN_POINT('Ctrl Pts',(-2.40901979147983,106.355112883126,13.9682972962322));
#42726=CARTESIAN_POINT('Ctrl Pts',(-2.43282223960327,106.366065459272,13.882496801153));
#42727=CARTESIAN_POINT('Ctrl Pts',(-2.45200715117387,106.376981311971,13.7955461667228));
#42728=CARTESIAN_POINT('Ctrl Pts',(-2.46651155076268,106.387878306611,13.707829504449));
#42729=CARTESIAN_POINT('Ctrl Pts',(-2.47985710950783,106.397904676971,13.627121036502));
#42730=CARTESIAN_POINT('Ctrl Pts',(-2.48924077358504,106.407915006875,13.5457643076491));
#42731=CARTESIAN_POINT('Ctrl Pts',(-2.49461608659223,106.417928770086,13.4640288581122));
#42732=CARTESIAN_POINT('Ctrl Pts',(-2.49505233826781,106.418741470849,13.4573953417444));
#42733=CARTESIAN_POINT('Ctrl Pts',(-2.49546216787465,106.419554196303,13.4507593110106));
#42734=CARTESIAN_POINT('Ctrl Pts',(-2.49584553938309,106.420366957959,13.4441208997767));
#42735=CARTESIAN_POINT('Ctrl Pts',(-2.49668113576872,106.42213845294,13.4296518213207));
#42736=CARTESIAN_POINT('Ctrl Pts',(-2.49739112856075,106.423910126733,13.4151714419338));
#42737=CARTESIAN_POINT('Ctrl Pts',(-2.4979752113352,106.425682110233,13.4006811231117));
#42738=CARTESIAN_POINT('Ctrl Pts',(-2.49797622340333,106.425685180634,13.400656015044));
#42739=CARTESIAN_POINT('Ctrl Pts',(-2.49797723509339,106.425688251035,13.4006309069463));
#42740=CARTESIAN_POINT('Ctrl Pts',(-2.49797824640536,106.425691321437,13.4006057988189));
#42741=CARTESIAN_POINT('Ctrl Pts',(-2.49932446808026,106.429778529246,13.3671827735883));
#42742=CARTESIAN_POINT('Ctrl Pts',(-2.50000082507155,106.433867394332,13.3337067595297));
#42743=CARTESIAN_POINT('Ctrl Pts',(-2.50000333388702,106.437958303058,13.3001965898202));
#42744=CARTESIAN_POINT('',(2.31220144791066,104.895136985459,14.2499282950331));
#42745=CARTESIAN_POINT('Ctrl Pts',(-2.5,105.533497732924,13.3000000000004));
#42746=CARTESIAN_POINT('Ctrl Pts',(-2.5,105.520804033348,13.4158707782706));
#42747=CARTESIAN_POINT('Ctrl Pts',(-2.49194405837885,105.508271404854,13.5318769342806));
#42748=CARTESIAN_POINT('Ctrl Pts',(-2.43550168616906,105.465234432574,13.9343938651791));
#42749=CARTESIAN_POINT('Ctrl Pts',(-2.3455711156717,105.436725695498,14.2123538901486));
#42750=CARTESIAN_POINT('Ctrl Pts',(-2.05347068002038,105.372146357901,14.764712314317));
#42751=CARTESIAN_POINT('Ctrl Pts',(-1.83899158460821,105.335631760271,15.0263806357197));
#42752=CARTESIAN_POINT('Ctrl Pts',(-1.35535144233529,105.273294634429,15.4204772199161));
#42753=CARTESIAN_POINT('Ctrl Pts',(-1.10166774143074,105.247108937262,15.562670083002));
#42754=CARTESIAN_POINT('Ctrl Pts',(-0.513772393234898,105.187016003129,
15.7693959782354));
#42755=CARTESIAN_POINT('Ctrl Pts',(-0.179028915558743,105.152249943282,
15.8159540487419));
#42756=CARTESIAN_POINT('Ctrl Pts',(0.437597169497571,105.09541965019,15.777623767016));
#42757=CARTESIAN_POINT('Ctrl Pts',(0.71488641944579,105.072598380658,15.712260395868));
#42758=CARTESIAN_POINT('Ctrl Pts',(1.28240255117051,105.020050748162,15.4717752588311));
#42759=CARTESIAN_POINT('Ctrl Pts',(1.56033530811733,104.988672482657,15.2815924355496));
#42760=CARTESIAN_POINT('Ctrl Pts',(2.01516254243393,104.936876652781,14.8135517832682));
#42761=CARTESIAN_POINT('Ctrl Pts',(2.19136165007833,104.91683004046,14.5447676063188));
#42762=CARTESIAN_POINT('Ctrl Pts',(2.31244118192445,104.894682621471,14.2500609349615));
#42763=CARTESIAN_POINT('Ctrl Pts',(2.31132717531622,104.894586489788,14.2495818126787));
#42764=CARTESIAN_POINT('Ctrl Pts',(2.31640301832098,104.893034510998,14.2382227802811));
#42765=CARTESIAN_POINT('Ctrl Pts',(2.32096538576457,104.891223989443,14.2271257782176));
#42766=CARTESIAN_POINT('Ctrl Pts',(2.325494703813,104.889232143616,14.2155903870854));
#42767=CARTESIAN_POINT('Ctrl Pts',(2.32796599272174,104.888145351643,14.2092964408758));
#42768=CARTESIAN_POINT('Ctrl Pts',(2.33045581922597,104.887039290589,14.2028797622965));
#42769=CARTESIAN_POINT('Ctrl Pts',(2.33288880610748,104.885944438163,14.1965283732465));
#42770=CARTESIAN_POINT('Ctrl Pts',(2.3547237778565,104.876118626125,14.139527490288));
#42771=CARTESIAN_POINT('Ctrl Pts',(2.37442302242763,104.866334600622,14.0819364577489));
#42772=CARTESIAN_POINT('Ctrl Pts',(2.39201877324852,104.856560092324,14.0237517623631));
#42773=CARTESIAN_POINT('Ctrl Pts',(2.39344183757104,104.855769574536,14.0190460487528));
#42774=CARTESIAN_POINT('Ctrl Pts',(2.39485111735034,104.854979119164,14.0143364410787));
#42775=CARTESIAN_POINT('Ctrl Pts',(2.39624661586076,104.854188709229,14.0096229320215));
#42776=CARTESIAN_POINT('Ctrl Pts',(2.40063533255731,104.851702941418,13.994799372022));
#42777=CARTESIAN_POINT('Ctrl Pts',(2.40488779415261,104.849217659616,13.9799372376659));
#42778=CARTESIAN_POINT('Ctrl Pts',(2.40900402591882,104.846732403914,13.9650362751071));
#42779=CARTESIAN_POINT('Ctrl Pts',(2.4324637763532,104.832568119238,13.8801108183507));
#42780=CARTESIAN_POINT('Ctrl Pts',(2.45142542935255,104.81844640189,13.7941923937425));
#42781=CARTESIAN_POINT('Ctrl Pts',(2.46583912706641,104.804367050333,13.7076472505981));
#42782=CARTESIAN_POINT('Ctrl Pts',(2.48028545759541,104.790255822925,13.6209061680276));
#42783=CARTESIAN_POINT('Ctrl Pts',(2.49016380420976,104.776187456513,13.53353550939));
#42784=CARTESIAN_POINT('Ctrl Pts',(2.49540428284792,104.762186058041,13.4458706150948));
#42785=CARTESIAN_POINT('Ctrl Pts',(2.50002756423327,104.749833673956,13.3685304517379));
#42786=CARTESIAN_POINT('Ctrl Pts',(2.50104126814055,104.737533941667,13.2909606583303));
#42787=CARTESIAN_POINT('Ctrl Pts',(2.49837750332954,104.725315874626,13.2133711356687));
#42788=CARTESIAN_POINT('Ctrl Pts',(2.498377401564,104.725315407851,13.2133681714659));
#42789=CARTESIAN_POINT('Ctrl Pts',(2.4983772997931,104.725314941076,13.2133652072631));
#42790=CARTESIAN_POINT('Ctrl Pts',(2.49837719801682,104.725314474302,13.2133622430602));
#42791=CARTESIAN_POINT('Ctrl Pts',(2.49631991527468,104.715879199737,13.153444513395));
#42792=CARTESIAN_POINT('Ctrl Pts',(2.49206892984282,104.706492629584,13.0935136045211));
#42793=CARTESIAN_POINT('Ctrl Pts',(2.48563118019984,104.697127684045,13.0336903597452));
#42794=CARTESIAN_POINT('Ctrl Pts',(2.47641510401865,104.68372112798,12.9480493187237));
#42795=CARTESIAN_POINT('Ctrl Pts',(2.4627635801708,104.670422904911,12.8630447898128));
#42796=CARTESIAN_POINT('Ctrl Pts',(2.44480596284123,104.657174972098,12.779027106201));
#42797=CARTESIAN_POINT('Ctrl Pts',(2.42644199360434,104.643627259939,12.6931082379634));
#42798=CARTESIAN_POINT('Ctrl Pts',(2.40357459222705,104.630132057815,12.6082215059131));
#42799=CARTESIAN_POINT('Ctrl Pts',(2.37631958811954,104.616658055251,12.5247395636468));
#42800=CARTESIAN_POINT('Ctrl Pts',(2.3633671507341,104.610254784357,12.4850663122411));
#42801=CARTESIAN_POINT('Ctrl Pts',(2.34942349741903,104.603856751717,12.44571028307));
#42802=CARTESIAN_POINT('Ctrl Pts',(2.33449942248738,104.597462983089,12.4067111690843));
#42803=CARTESIAN_POINT('Ctrl Pts',(2.33449551723172,104.597461310001,12.4067009639954));
#42804=CARTESIAN_POINT('Ctrl Pts',(2.33449161190891,104.597459636912,12.406690758931));
#42805=CARTESIAN_POINT('Ctrl Pts',(2.33448770651895,104.597457963824,12.406680553891));
#42806=CARTESIAN_POINT('Ctrl Pts',(2.30308731779963,104.584005884054,12.3246292797908));
#42807=CARTESIAN_POINT('Ctrl Pts',(2.26734814612602,104.570570846415,12.2441570905773));
#42808=CARTESIAN_POINT('Ctrl Pts',(2.22738543114158,104.557133161751,12.1656287552845));
#42809=CARTESIAN_POINT('Ctrl Pts',(2.22232079896839,104.555430151079,12.1556765502458));
#42810=CARTESIAN_POINT('Ctrl Pts',(2.21718830623773,104.553727135036,12.1457555765282));
#42811=CARTESIAN_POINT('Ctrl Pts',(2.21198816619355,104.552024105675,12.1358665851468));
#42812=CARTESIAN_POINT('Ctrl Pts',(2.1707674646652,104.53852445674,12.0574780881662));
#42813=CARTESIAN_POINT('Ctrl Pts',(2.125504413121,104.525088923967,11.9814918736891));
#42814=CARTESIAN_POINT('Ctrl Pts',(2.07641083093898,104.511727763851,11.908206254754));
#42815=CARTESIAN_POINT('Ctrl Pts',(2.03007312716373,104.499116635225,11.8390345392209));
#42816=CARTESIAN_POINT('Ctrl Pts',(1.98032290342944,104.486572082576,11.7722682983247));
#42817=CARTESIAN_POINT('Ctrl Pts',(1.92730470099957,104.474120826965,11.7081458826343));
#42818=CARTESIAN_POINT('Ctrl Pts',(1.92415675167142,104.473381535176,11.7043386219928));
#42819=CARTESIAN_POINT('Ctrl Pts',(1.92099726632121,104.472642571576,11.7005406836093));
#42820=CARTESIAN_POINT('Ctrl Pts',(1.91782626945823,104.471903941485,11.6967521182203));
#42821=CARTESIAN_POINT('Ctrl Pts',(1.91782098748062,104.471902711138,11.6967458075494));
#42822=CARTESIAN_POINT('Ctrl Pts',(1.91781570547112,104.471901480791,11.6967394969046));
#42823=CARTESIAN_POINT('Ctrl Pts',(1.91781042342962,104.471900250446,11.6967331862858));
#42824=CARTESIAN_POINT('Ctrl Pts',(1.86438918186872,104.459456844901,11.6329091713746));
#42825=CARTESIAN_POINT('Ctrl Pts',(1.8077021726804,104.447107763815,11.5717411172208));
#42826=CARTESIAN_POINT('Ctrl Pts',(1.74797526072607,104.434777066512,11.5134449880751));
#42827=CARTESIAN_POINT('Ctrl Pts',(1.74475125556711,104.434111466527,11.5102982152894));
#42828=CARTESIAN_POINT('Ctrl Pts',(1.741518389665,104.433445920956,11.5071598226906));
#42829=CARTESIAN_POINT('Ctrl Pts',(1.73827669757747,104.432780418149,11.504029848421));
#42830=CARTESIAN_POINT('Ctrl Pts',(1.70142992194142,104.425215963545,11.4684529162061));
#42831=CARTESIAN_POINT('Ctrl Pts',(1.66344318122168,104.417657370591,11.4339626861876));
#42832=CARTESIAN_POINT('Ctrl Pts',(1.6243690138553,104.410091315338,11.4006152189792));
#42833=CARTESIAN_POINT('Ctrl Pts',(1.55770811423271,104.397183553415,11.3437241240672));
#42834=CARTESIAN_POINT('Ctrl Pts',(1.48821400032916,104.384316116825,11.2904416042935));
#42835=CARTESIAN_POINT('Ctrl Pts',(1.41623247776679,104.371446188938,11.2409555225195));
#42836=CARTESIAN_POINT('Ctrl Pts',(1.34343741829754,104.358430804815,11.1909101478539));
#42837=CARTESIAN_POINT('Ctrl Pts',(1.26809865033967,104.345412964124,11.1447478606375));
#42838=CARTESIAN_POINT('Ctrl Pts',(1.19055875363133,104.332378863251,11.1026664096893));
#42839=CARTESIAN_POINT('Ctrl Pts',(1.11337774917425,104.319405090519,11.060779732107));
#42840=CARTESIAN_POINT('Ctrl Pts',(1.03401642885747,104.306415474085,11.0229360815388));
#42841=CARTESIAN_POINT('Ctrl Pts',(0.952792154383874,104.293423606679,10.9893319930855));
#42842=CARTESIAN_POINT('Ctrl Pts',(0.903417989526645,104.285526181835,10.9689049247747));
#42843=CARTESIAN_POINT('Ctrl Pts',(0.853355014458621,104.277628441397,10.9500444244177));
#42844=CARTESIAN_POINT('Ctrl Pts',(0.802669533287437,104.269737670569,10.9327957675765));
#42845=CARTESIAN_POINT('Ctrl Pts',(0.726683416410001,104.25790806926,10.9069371109271));
#42846=CARTESIAN_POINT('Ctrl Pts',(0.649647541024132,104.246147920313,10.8848185904926));
#42847=CARTESIAN_POINT('Ctrl Pts',(0.571791164490983,104.234490979685,10.8664973794054));
#42848=CARTESIAN_POINT('Ctrl Pts',(0.563722196810629,104.233282864417,10.864598584898));
#42849=CARTESIAN_POINT('Ctrl Pts',(0.5556443763029,104.232075854953,10.8627406008586));
#42850=CARTESIAN_POINT('Ctrl Pts',(0.547557931073244,104.230869986947,10.8609235080037));
#42851=CARTESIAN_POINT('Ctrl Pts',(0.54067397443229,104.229843436612,10.8593766245376));
#42852=CARTESIAN_POINT('Ctrl Pts',(0.533783769571032,104.228817722253,10.8578593633675));
#42853=CARTESIAN_POINT('Ctrl Pts',(0.526887455256306,104.227792869948,10.856371770479));
#42854=CARTESIAN_POINT('Ctrl Pts',(0.526880753065446,104.227791873945,10.8563703247601));
#42855=CARTESIAN_POINT('Ctrl Pts',(0.526874050868816,104.227790877942,10.8563688790693));
#42856=CARTESIAN_POINT('Ctrl Pts',(0.526867348666415,104.227789881939,10.8563674334065));
#42857=CARTESIAN_POINT('Ctrl Pts',(0.446620824989185,104.21586459042,10.8390582854445));
#42858=CARTESIAN_POINT('Ctrl Pts',(0.365545409459377,104.204054184164,10.8257640866501));
#42859=CARTESIAN_POINT('Ctrl Pts',(0.283937999466609,104.192283089781,10.8164921772243));
#42860=CARTESIAN_POINT('Ctrl Pts',(0.279486886488785,104.191641058978,10.8159864594668));
#42861=CARTESIAN_POINT('Ctrl Pts',(0.275034195464569,104.190999146129,10.8154927196941));
#42862=CARTESIAN_POINT('Ctrl Pts',(0.270579976289946,104.190357339318,10.8150109631338));
#42863=CARTESIAN_POINT('Ctrl Pts',(0.18293327300947,104.177728357924,10.8055313276145));
#42864=CARTESIAN_POINT('Ctrl Pts',(0.0946927161389826,104.165139746534,
10.8006875338495));
#42865=CARTESIAN_POINT('Ctrl Pts',(0.00625065803806539,104.152526195187,
10.8005145466055));
#42866=CARTESIAN_POINT('Ctrl Pts',(-0.0411532060176732,104.145765485563,
10.8004218275533));
#42867=CARTESIAN_POINT('Ctrl Pts',(-0.0886145178237575,104.138998111239,
10.8016712486707));
#42868=CARTESIAN_POINT('Ctrl Pts',(-0.136070138901457,104.13221754998,10.8042694897761));
#42869=CARTESIAN_POINT('Ctrl Pts',(-0.224250527438516,104.119618146311,
10.8090974512478));
#42870=CARTESIAN_POINT('Ctrl Pts',(-0.311967947992333,104.107034634962,
10.8185579744082));
#42871=CARTESIAN_POINT('Ctrl Pts',(-0.398827613518663,104.094448735194,
10.8325581551025));
#42872=CARTESIAN_POINT('Ctrl Pts',(-0.486276333258706,104.081777481916,
10.8466532805031));
#42873=CARTESIAN_POINT('Ctrl Pts',(-0.572855093604851,104.069104083644,
10.8653494072166));
#42874=CARTESIAN_POINT('Ctrl Pts',(-0.658183909257249,104.056437260993,
10.8885601179806));
#42875=CARTESIAN_POINT('Ctrl Pts',(-0.742515312981924,104.043918501337,
10.9114995178212));
#42876=CARTESIAN_POINT('Ctrl Pts',(-0.825625721850992,104.03140657265,10.9388476503207));
#42877=CARTESIAN_POINT('Ctrl Pts',(-0.907175381067747,104.0189312925,10.9705395440152));
#42878=CARTESIAN_POINT('Ctrl Pts',(-0.958033605417957,104.011151117785,
10.9903041077801));
#42879=CARTESIAN_POINT('Ctrl Pts',(-1.00828537816385,104.00338560235,11.0117585033029));
#42880=CARTESIAN_POINT('Ctrl Pts',(-1.05785344363349,103.995645155671,11.0348935660898));
#42881=CARTESIAN_POINT('Ctrl Pts',(-1.06777998612567,103.994095047307,11.0395266132269));
#42882=CARTESIAN_POINT('Ctrl Pts',(-1.07767292081435,103.992546915427,11.0442241955565));
#42883=CARTESIAN_POINT('Ctrl Pts',(-1.08753176128416,103.991000846838,11.0489860266477));
#42884=CARTESIAN_POINT('Ctrl Pts',(-1.087533256854,103.991000612302,11.0489867490096));
#42885=CARTESIAN_POINT('Ctrl Pts',(-1.08753475242305,103.991000377766,11.048987471373));
#42886=CARTESIAN_POINT('Ctrl Pts',(-1.08753624799132,103.99100014323,11.0489881937379));
#42887=CARTESIAN_POINT('Ctrl Pts',(-1.16515019883,103.978828674469,11.0864760125203));
#42888=CARTESIAN_POINT('Ctrl Pts',(-1.24065394406993,103.96678307826,11.1279448232097));
#42889=CARTESIAN_POINT('Ctrl Pts',(-1.31378826137423,103.95478369176,11.1731703264622));
#42890=CARTESIAN_POINT('Ctrl Pts',(-1.38825593575194,103.942565537006,11.2192203638989));
#42891=CARTESIAN_POINT('Ctrl Pts',(-1.46026623719515,103.930395143374,11.2691661804705));
#42892=CARTESIAN_POINT('Ctrl Pts',(-1.5295177582202,103.918214907366,11.3227748642695));
#42893=CARTESIAN_POINT('Ctrl Pts',(-1.59937234241708,103.905928602182,11.3768503886868));
#42894=CARTESIAN_POINT('Ctrl Pts',(-1.66641902509694,103.893632283652,11.4346530706847));
#42895=CARTESIAN_POINT('Ctrl Pts',(-1.7303331345939,103.881294620168,11.4959394971383));
#42896=CARTESIAN_POINT('Ctrl Pts',(-1.7639922823914,103.874797224804,11.5282148257351));
#42897=CARTESIAN_POINT('Ctrl Pts',(-1.79678247358277,103.868288827152,11.5614562326876));
#42898=CARTESIAN_POINT('Ctrl Pts',(-1.82865573339812,103.861767840413,11.5956277512324));
#42899=CARTESIAN_POINT('Ctrl Pts',(-1.88899623687624,103.849422707682,11.6603191773855));
#42900=CARTESIAN_POINT('Ctrl Pts',(-1.945743259724,103.83709370184,11.7280142267784));
#42901=CARTESIAN_POINT('Ctrl Pts',(-1.99868685669959,103.82478831317,11.7983868957619));
#42902=CARTESIAN_POINT('Ctrl Pts',(-2.04833708423673,103.813248384222,11.8643820156069));
#42903=CARTESIAN_POINT('Ctrl Pts',(-2.0946426725136,103.801729546487,11.9327316991028));
#42904=CARTESIAN_POINT('Ctrl Pts',(-2.1374460831665,103.790253046683,12.0031971503753));
#42905=CARTESIAN_POINT('Ctrl Pts',(-2.14033658080241,103.789478043125,12.0079556548311));
#42906=CARTESIAN_POINT('Ctrl Pts',(-2.14321110172861,103.788703231404,12.0127238265024));
#42907=CARTESIAN_POINT('Ctrl Pts',(-2.14606959460474,103.787928617525,12.0175015999515));
#42908=CARTESIAN_POINT('Ctrl Pts',(-2.18042621706528,103.77861842584,12.0749263218966));
#42909=CARTESIAN_POINT('Ctrl Pts',(-2.21246904706033,103.769337440822,12.1337357121099));
#42910=CARTESIAN_POINT('Ctrl Pts',(-2.24211581456284,103.760101711445,12.1938232382963));
#42911=CARTESIAN_POINT('Ctrl Pts',(-2.24211903410285,103.760100708475,12.1938297636011));
#42912=CARTESIAN_POINT('Ctrl Pts',(-2.24212225361458,103.760099705506,12.193836288921));
#42913=CARTESIAN_POINT('Ctrl Pts',(-2.24212547309804,103.760098702538,12.193842814256));
#42914=CARTESIAN_POINT('Ctrl Pts',(-2.27620049792537,103.749483282059,12.2629069839777));
#42915=CARTESIAN_POINT('Ctrl Pts',(-2.30711203979563,103.738926878711,12.3336636236315));
#42916=CARTESIAN_POINT('Ctrl Pts',(-2.3347431690348,103.728375426866,12.4059037896928));
#42917=CARTESIAN_POINT('Ctrl Pts',(-2.36583191082452,103.716503622457,12.4871837059092));
#42918=CARTESIAN_POINT('Ctrl Pts',(-2.39261160021939,103.704696711206,12.5699347703841));
#42919=CARTESIAN_POINT('Ctrl Pts',(-2.415018825915,103.692899317101,12.6537855449586));
#42920=CARTESIAN_POINT('Ctrl Pts',(-2.43777757189232,103.680916847728,12.738951754487));
#42921=CARTESIAN_POINT('Ctrl Pts',(-2.45602467618214,103.668944244274,12.825251955648));
#42922=CARTESIAN_POINT('Ctrl Pts',(-2.46968963992784,103.656949702055,12.9122873766021));
#42923=CARTESIAN_POINT('Ctrl Pts',(-2.48340027960736,103.644915067384,12.9996137184984));
#42924=CARTESIAN_POINT('Ctrl Pts',(-2.49249782364295,103.632858547501,13.0876793361628));
#42925=CARTESIAN_POINT('Ctrl Pts',(-2.49691617211707,103.620772247152,13.1760824234444));
#42926=CARTESIAN_POINT('Ctrl Pts',(-2.49897760899693,103.615133229445,13.2173280122618));
#42927=CARTESIAN_POINT('Ctrl Pts',(-2.50002056844956,103.609488051128,13.2586471582004));
#42928=CARTESIAN_POINT('Ctrl Pts',(-2.50003871369437,103.603837493162,13.2999999833247));
#42929=CARTESIAN_POINT('Origin',(0.,70.2,13.3));
#42930=CARTESIAN_POINT('',(-2.5,101.637207465761,13.3));
#42931=CARTESIAN_POINT('',(-2.49999999983267,102.618167926383,13.3000182966029));
#42932=CARTESIAN_POINT('',(-2.5,70.2,13.3));
#42933=CARTESIAN_POINT('Ctrl Pts',(-2.50000000000001,102.618170270812,13.3000000000108));
#42934=CARTESIAN_POINT('Ctrl Pts',(-2.50000000000002,102.640241818529,13.1277477261055));
#42935=CARTESIAN_POINT('Ctrl Pts',(-2.48219754881853,102.662175662565,12.9559557473048));
#42936=CARTESIAN_POINT('Ctrl Pts',(-2.41878394951985,102.701806833258,12.6532752530091));
#42937=CARTESIAN_POINT('Ctrl Pts',(-2.37971848431703,102.719380382371,12.5217291795141));
#42938=CARTESIAN_POINT('Ctrl Pts',(-2.24627692491632,102.766817117034,12.1785203162223));
#42939=CARTESIAN_POINT('Ctrl Pts',(-2.13297412252146,102.796604688506,11.9756503729151));
#42940=CARTESIAN_POINT('Ctrl Pts',(-1.83035194125583,102.861030204594,11.5758152281744));
#42941=CARTESIAN_POINT('Ctrl Pts',(-1.63342316382879,102.894998152686,11.3882017433834));
#42942=CARTESIAN_POINT('Ctrl Pts',(-1.15105626067604,102.968551686843,11.0586572424382));
#42943=CARTESIAN_POINT('Ctrl Pts',(-0.860793368550738,103.007629514266,
10.9319652280881));
#42944=CARTESIAN_POINT('Ctrl Pts',(-0.333393964031027,103.075601944804,
10.8119578523735));
#42945=CARTESIAN_POINT('Ctrl Pts',(-0.106267156973827,103.103980854947,
10.7919692630349));
#42946=CARTESIAN_POINT('Ctrl Pts',(0.454543715130937,103.174286282485,10.8190159216283));
#42947=CARTESIAN_POINT('Ctrl Pts',(0.782084388962346,103.215561131113,10.9020257305053));
#42948=CARTESIAN_POINT('Ctrl Pts',(1.37852094509146,103.297314979055,11.1888903374276));
#42949=CARTESIAN_POINT('Ctrl Pts',(1.64277116966911,103.336961893884,11.3872937983161));
#42950=CARTESIAN_POINT('Ctrl Pts',(2.06252832963449,103.413649002816,11.855411703839));
#42951=CARTESIAN_POINT('Ctrl Pts',(2.22153308461144,103.450236068805,12.1143937399292));
#42952=CARTESIAN_POINT('Ctrl Pts',(2.44745506784865,103.526009143805,12.6964692631386));
#42953=CARTESIAN_POINT('Ctrl Pts',(2.50488005028318,103.564342939622,13.017348411793));
#42954=CARTESIAN_POINT('Ctrl Pts',(2.49428563828586,103.643210285286,13.6747076658831));
#42955=CARTESIAN_POINT('Ctrl Pts',(2.42183817645359,103.68304824667,14.004707900806));
#42956=CARTESIAN_POINT('Ctrl Pts',(2.168328900386,103.757209567566,14.5782519913845));
#42957=CARTESIAN_POINT('Ctrl Pts',(2.00401103259475,103.79118499957,14.8229973609931));
#42958=CARTESIAN_POINT('Ctrl Pts',(1.68844924596043,103.844936016636,15.1508213560995));
#42959=CARTESIAN_POINT('Ctrl Pts',(1.56461454068236,103.864070384638,15.2566270723523));
#42960=CARTESIAN_POINT('Ctrl Pts',(1.18864626693842,103.917695431997,15.5191834086683));
#42961=CARTESIAN_POINT('Ctrl Pts',(0.917703892648551,103.951315705915,15.6442495189771));
#42962=CARTESIAN_POINT('Ctrl Pts',(0.307417210611317,104.023796487592,15.8034880093659));
#42963=CARTESIAN_POINT('Ctrl Pts',(-0.030061686814792,104.062479500167,
15.8221220763861));
#42964=CARTESIAN_POINT('Ctrl Pts',(-0.67340724325193,104.136138283098,15.7281808403738));
#42965=CARTESIAN_POINT('Ctrl Pts',(-0.974166239719262,104.170745060693,
15.6239078966338));
#42966=CARTESIAN_POINT('Ctrl Pts',(-1.3875139716866,104.224606338278,15.3858760299509));
#42967=CARTESIAN_POINT('Ctrl Pts',(-1.51932294290106,104.242802123662,15.291919144752));
#42968=CARTESIAN_POINT('Ctrl Pts',(-1.86263044979247,104.293459772383,14.9931640649498));
#42969=CARTESIAN_POINT('Ctrl Pts',(-2.04844768197224,104.324808370143,14.7629080256152));
#42970=CARTESIAN_POINT('Ctrl Pts',(-2.35110813356646,104.392648284681,14.2131243018626));
#42971=CARTESIAN_POINT('Ctrl Pts',(-2.45193861624832,104.429337759002,13.8912436478308));
#42972=CARTESIAN_POINT('Ctrl Pts',(-2.49552480648441,104.4738137519,13.4728195719713));
#42973=CARTESIAN_POINT('Ctrl Pts',(-2.5,104.482864048722,13.3863654953521));
#42974=CARTESIAN_POINT('Ctrl Pts',(-2.5,104.491842419534,13.3));
#42975=CARTESIAN_POINT('',(-2.49999935789722,103.603575436303,13.3017917905773));
#42976=CARTESIAN_POINT('Ctrl Pts',(-2.50003871369437,103.603837493162,13.2999999833247));
#42977=CARTESIAN_POINT('Ctrl Pts',(-2.50003897610844,103.60375577556,13.3005980222681));
#42978=CARTESIAN_POINT('Ctrl Pts',(-2.50003902414661,103.603674056831,13.3011960682681));
#42979=CARTESIAN_POINT('Ctrl Pts',(-2.50003885778613,103.603592336976,13.3017941212051));
#42980=CARTESIAN_POINT('Ctrl Pts',(-2.49999935789722,103.603575436303,13.3017917905773));
#42981=CARTESIAN_POINT('Ctrl Pts',(-2.49987384567273,103.579612808251,13.4769129708106));
#42982=CARTESIAN_POINT('Ctrl Pts',(-2.48134822948507,103.55566875521,13.6515591459021));
#42983=CARTESIAN_POINT('Ctrl Pts',(-2.40206796913163,103.504501247821,14.022253028833));
#42984=CARTESIAN_POINT('Ctrl Pts',(-2.33517777320684,103.477508758949,14.2157209686054));
#42985=CARTESIAN_POINT('Ctrl Pts',(-2.10502101028616,103.407673700546,14.6860208714818));
#42986=CARTESIAN_POINT('Ctrl Pts',(-1.91075366020395,103.365019951847,14.9435301765248));
#42987=CARTESIAN_POINT('Ctrl Pts',(-1.42414626749157,103.277997202902,15.3818808592167));
#42988=CARTESIAN_POINT('Ctrl Pts',(-1.13238691184991,103.234822206233,15.5539218284624));
#42989=CARTESIAN_POINT('Ctrl Pts',(-0.662935492327526,103.169600803758,
15.715888693799));
#42990=CARTESIAN_POINT('Ctrl Pts',(-0.50576891308823,103.148428990443,15.7536098285557));
#42991=CARTESIAN_POINT('Ctrl Pts',(-0.0383727463709212,103.086589344291,
15.818938681796));
#42992=CARTESIAN_POINT('Ctrl Pts',(0.274691269532586,103.046981194232,15.8042209450093));
#42993=CARTESIAN_POINT('Ctrl Pts',(0.898423530583375,102.964585598428,15.6562504400845));
#42994=CARTESIAN_POINT('Ctrl Pts',(1.20151545297683,102.922364417971,15.5170816790616));
#42995=CARTESIAN_POINT('Ctrl Pts',(1.6012205823757,102.859086283876,15.2268823182098));
#42996=CARTESIAN_POINT('Ctrl Pts',(1.72389772965701,102.838265461855,15.1179560911702));
#42997=CARTESIAN_POINT('Ctrl Pts',(2.0570403779814,102.775777062402,14.7578862647492));
#42998=CARTESIAN_POINT('Ctrl Pts',(2.22984811558075,102.734636828213,14.4767125247071));
#42999=CARTESIAN_POINT('Ctrl Pts',(2.45981529442251,102.651181647567,13.8573876576525));
#43000=CARTESIAN_POINT('Ctrl Pts',(2.51217994755866,102.60966780587,13.5243963862876));
#43001=CARTESIAN_POINT('Ctrl Pts',(2.48301168831486,102.525953791866,12.8563736488223));
#43002=CARTESIAN_POINT('Ctrl Pts',(2.40132308282432,102.484624019053,12.5280985190173));
#43003=CARTESIAN_POINT('Ctrl Pts',(2.18792875470781,102.423077012594,12.0797160517702));
#43004=CARTESIAN_POINT('Ctrl Pts',(2.10447650457136,102.403142545388,11.940843048404));
#43005=CARTESIAN_POINT('Ctrl Pts',(1.81921790746521,102.344073768843,11.5561181098551));
#43006=CARTESIAN_POINT('Ctrl Pts',(1.5834170617546,102.305532688792,11.3395174198834));
#43007=CARTESIAN_POINT('Ctrl Pts',(1.02873179768248,102.225802055474,10.9970361940603));
#43008=CARTESIAN_POINT('Ctrl Pts',(0.711624302200728,102.185327693338,10.8801721773681));
#43009=CARTESIAN_POINT('Ctrl Pts',(0.227552725347762,102.126239798956,10.8055471516363));
#43010=CARTESIAN_POINT('Ctrl Pts',(0.0723278330722858,102.107652599778,
10.7962332615171));
#43011=CARTESIAN_POINT('Ctrl Pts',(-0.417079563898204,102.048926960579,
10.8124438502513));
#43012=CARTESIAN_POINT('Ctrl Pts',(-0.745819897061609,102.008947356071,
10.8905043375096));
#43013=CARTESIAN_POINT('Ctrl Pts',(-1.32291415776129,101.933310958461,11.1574142746825));
#43014=CARTESIAN_POINT('Ctrl Pts',(-1.57128153623215,101.898363766591,11.3322930818985));
#43015=CARTESIAN_POINT('Ctrl Pts',(-2.018280835674,101.823342126679,11.7868652511051));
#43016=CARTESIAN_POINT('Ctrl Pts',(-2.20328270803896,101.783936534117,12.0717320386843));
#43017=CARTESIAN_POINT('Ctrl Pts',(-2.44116137868579,101.708842047491,12.6763330895868));
#43018=CARTESIAN_POINT('Ctrl Pts',(-2.5,101.673389006817,12.986866730166));
#43019=CARTESIAN_POINT('Ctrl Pts',(-2.5,101.637207465761,13.3));
#43020=CARTESIAN_POINT('Origin',(0.,70.2,13.3));
#43021=CARTESIAN_POINT('',(2.49284186651808,100.7945130522,13.1110770588995));
#43022=CARTESIAN_POINT('Ctrl Pts',(-2.5,101.637207465761,13.3));
#43023=CARTESIAN_POINT('Ctrl Pts',(-2.5,101.635397107763,13.3156677494368));
#43024=CARTESIAN_POINT('Ctrl Pts',(-2.4998527135231,101.633586332796,13.3313421699356));
#43025=CARTESIAN_POINT('Ctrl Pts',(-2.49397575294634,101.597501416344,13.6437498288163));
#43026=CARTESIAN_POINT('Ctrl Pts',(-2.43559995242375,101.563958202291,13.9371851059678));
#43027=CARTESIAN_POINT('Ctrl Pts',(-2.26975677891009,101.513235154397,14.3596381439182));
#43028=CARTESIAN_POINT('Ctrl Pts',(-2.19878289690343,101.495853589453,14.4999917288581));
#43029=CARTESIAN_POINT('Ctrl Pts',(-1.93995342605789,101.441357413942,14.9107605021292));
#43030=CARTESIAN_POINT('Ctrl Pts',(-1.71162696691703,101.404443533433,15.1515939579269));
#43031=CARTESIAN_POINT('Ctrl Pts',(-1.177653286629,101.333066457237,15.5291010900195));
#43032=CARTESIAN_POINT('Ctrl Pts',(-0.877994267335959,101.298563133645,
15.6632353312194));
#43033=CARTESIAN_POINT('Ctrl Pts',(-0.272708342417149,101.230749095566,
15.8026397347157));
#43034=CARTESIAN_POINT('Ctrl Pts',(0.0252665497621781,101.199320408508,
15.8173478379036));
#43035=CARTESIAN_POINT('Ctrl Pts',(0.476193706233752,101.152163356072,15.75934411446));
#43036=CARTESIAN_POINT('Ctrl Pts',(0.631147494318057,101.135950172377,15.7242077588106));
#43037=CARTESIAN_POINT('Ctrl Pts',(1.09075440636581,101.085495612883,15.5729065029533));
#43038=CARTESIAN_POINT('Ctrl Pts',(1.37712231785397,101.051274244471,15.4117616857425));
#43039=CARTESIAN_POINT('Ctrl Pts',(1.86579795875028,100.98715374067,14.9939624038972));
#43040=CARTESIAN_POINT('Ctrl Pts',(2.06556533212102,100.956976682237,14.7436608799853));
#43041=CARTESIAN_POINT('Ctrl Pts',(2.32950750604381,100.900678241366,14.2412607707093));
#43042=CARTESIAN_POINT('Ctrl Pts',(2.41199748374071,100.876406442244,14.0035179645452));
#43043=CARTESIAN_POINT('Ctrl Pts',(2.49744258256006,100.833213788839,13.5443911621765));
#43044=CARTESIAN_POINT('Ctrl Pts',(2.50922496440789,100.814139396728,13.3271443744556));
#43045=CARTESIAN_POINT('Ctrl Pts',(2.49285252681543,100.794505242158,13.1110918753734));
#43046=CARTESIAN_POINT('',(-2.5,99.7536786153901,13.299999999524));
#43047=CARTESIAN_POINT('Ctrl Pts',(2.49285672356711,100.794015874192,13.11114726434));
#43048=CARTESIAN_POINT('Ctrl Pts',(2.47466985079183,100.759178937447,12.8710804846872));
#43049=CARTESIAN_POINT('Ctrl Pts',(2.42189355944945,100.724522436754,12.6348159025486));
#43050=CARTESIAN_POINT('Ctrl Pts',(2.23933715036676,100.652368551319,12.1557982714085));
#43051=CARTESIAN_POINT('Ctrl Pts',(2.10182163062156,100.615009546234,11.9193494988057));
#43052=CARTESIAN_POINT('Ctrl Pts',(1.73674877950707,100.534417987845,11.4765436645856));
#43053=CARTESIAN_POINT('Ctrl Pts',(1.50385865512308,100.491692324512,11.2801668860126));
#43054=CARTESIAN_POINT('Ctrl Pts',(0.950019201125868,100.403244092737,10.9632725006471));
#43055=CARTESIAN_POINT('Ctrl Pts',(0.627745662968607,100.358727928871,10.8568762769735));
#43056=CARTESIAN_POINT('Ctrl Pts',(-0.00524379688189826,100.271984632209,
10.7819049015937));
#43057=CARTESIAN_POINT('Ctrl Pts',(-0.308510598960716,100.230841405672,
10.8008641585676));
#43058=CARTESIAN_POINT('Ctrl Pts',(-0.926964154886148,100.145111588349,
10.9540581475074));
#43059=CARTESIAN_POINT('Ctrl Pts',(-1.23330514807368,100.101369766984,11.099607941249));
#43060=CARTESIAN_POINT('Ctrl Pts',(-1.74232012171602,100.016726577802,11.4820747650571));
#43061=CARTESIAN_POINT('Ctrl Pts',(-1.94829914608007,99.9768076775756,11.7047881115834));
#43062=CARTESIAN_POINT('Ctrl Pts',(-2.19621809152953,99.9161437038351,12.0947622126472));
#43063=CARTESIAN_POINT('Ctrl Pts',(-2.26933440606012,99.8952175210238,12.2388200231824));
#43064=CARTESIAN_POINT('Ctrl Pts',(-2.44169468599849,99.8337959262168,12.6792526037952));
#43065=CARTESIAN_POINT('Ctrl Pts',(-2.49999999988129,99.7937512872206,12.9882722440034));
#43066=CARTESIAN_POINT('Ctrl Pts',(-2.5,99.7536786153901,13.299999999048));
#43067=CARTESIAN_POINT('',(-2.5,100.556030878907,13.3000000000001));
#43068=CARTESIAN_POINT('',(-2.5,70.2,13.3));
#43069=CARTESIAN_POINT('',(-1.18065793506841,100.775168925174,11.0950388653619));
#43070=CARTESIAN_POINT('Ctrl Pts',(-2.5,100.556030878907,13.3000000000002));
#43071=CARTESIAN_POINT('Ctrl Pts',(-2.5,100.575712858969,13.0805393351909));
#43072=CARTESIAN_POINT('Ctrl Pts',(-2.47110612339189,100.593966114938,12.8617403493646));
#43073=CARTESIAN_POINT('Ctrl Pts',(-2.32687792948211,100.640854367325,12.3267623410781));
#43074=CARTESIAN_POINT('Ctrl Pts',(-2.17625108057745,100.672093072887,12.0250388790023));
#43075=CARTESIAN_POINT('Ctrl Pts',(-1.85782227860843,100.714049821671,11.6171010726225));
#43076=CARTESIAN_POINT('Ctrl Pts',(-1.72936686120991,100.727548384298,11.4853389758269));
#43077=CARTESIAN_POINT('Ctrl Pts',(-1.46093464308142,100.751543479388,11.2646786927412));
#43078=CARTESIAN_POINT('Ctrl Pts',(-1.32443223706636,100.762177989808,11.1733302526813));
#43079=CARTESIAN_POINT('Ctrl Pts',(-1.17998685155049,100.773580099726,11.0959965902549));
#43080=CARTESIAN_POINT('Ctrl Pts',(-1.18027058595304,100.77645823042,11.0961485204456));
#43081=CARTESIAN_POINT('Ctrl Pts',(-0.938059961197377,100.81973254846,10.9664328482887));
#43082=CARTESIAN_POINT('Ctrl Pts',(-0.67611969418476,100.863378555888,10.8775428772392));
#43083=CARTESIAN_POINT('Ctrl Pts',(-0.104371428946291,100.955455344403,
10.7836577628089));
#43084=CARTESIAN_POINT('Ctrl Pts',(0.20286109498074,101.001180411669,10.7896541673622));
#43085=CARTESIAN_POINT('Ctrl Pts',(0.800542765702973,101.09424520677,10.9120623848384));
#43086=CARTESIAN_POINT('Ctrl Pts',(1.08576786172926,101.14129542265,11.0275030476426));
#43087=CARTESIAN_POINT('Ctrl Pts',(1.62644534730514,101.237426863056,11.3719205629185));
#43088=CARTESIAN_POINT('Ctrl Pts',(1.87054137050352,101.284952813534,11.607661578119));
#43089=CARTESIAN_POINT('Ctrl Pts',(2.15217581987885,101.358294704342,12.017738384329));
#43090=CARTESIAN_POINT('Ctrl Pts',(2.23045716296475,101.38221229061,12.1593346989988));
#43091=CARTESIAN_POINT('Ctrl Pts',(2.4225117340961,101.453320984913,12.6033369942959));
#43092=CARTESIAN_POINT('Ctrl Pts',(2.49208268306385,101.498027246709,12.9211553592237));
#43093=CARTESIAN_POINT('Ctrl Pts',(2.5062718767786,101.587230943087,13.5495308111175));
#43094=CARTESIAN_POINT('Ctrl Pts',(2.45694119476446,101.631158355497,13.8541715994227));
#43095=CARTESIAN_POINT('Ctrl Pts',(2.29943054260782,101.696909554085,14.2943245697655));
#43096=CARTESIAN_POINT('Ctrl Pts',(2.23042958462874,101.719162545749,14.4407293777322));
#43097=CARTESIAN_POINT('Ctrl Pts',(2.06791841338335,101.763145315154,14.7135286666381));
#43098=CARTESIAN_POINT('Ctrl Pts',(1.975686937057,101.78476497561,14.8398065251242));
#43099=CARTESIAN_POINT('Ctrl Pts',(1.65122715615705,101.853115961513,15.2065003343976));
#43100=CARTESIAN_POINT('Ctrl Pts',(1.38230114422013,101.899447507771,15.4096596098744));
#43101=CARTESIAN_POINT('Ctrl Pts',(0.937253820472456,101.966521739436,15.6231650612652));
#43102=CARTESIAN_POINT('Ctrl Pts',(0.786868930602964,101.98811492698,15.6783138108469));
#43103=CARTESIAN_POINT('Ctrl Pts',(0.33232613258465,102.052110240557,15.7971308868413));
#43104=CARTESIAN_POINT('Ctrl Pts',(0.0204033351471258,102.094634362746,
15.8190696730077));
#43105=CARTESIAN_POINT('Ctrl Pts',(-0.619763219661474,102.1816384624,15.7449368552534));
#43106=CARTESIAN_POINT('Ctrl Pts',(-0.940905829217929,102.225509644986,
15.6402058495464));
#43107=CARTESIAN_POINT('Ctrl Pts',(-1.37113130501076,102.291810297129,15.3965651763402));
#43108=CARTESIAN_POINT('Ctrl Pts',(-1.50243774962431,102.313262476999,15.3045623869997));
#43109=CARTESIAN_POINT('Ctrl Pts',(-1.87849937890772,102.379344657656,14.983226876065));
#43110=CARTESIAN_POINT('Ctrl Pts',(-2.08673312877407,102.422754265075,14.7168978275346));
#43111=CARTESIAN_POINT('Ctrl Pts',(-2.31214659148409,102.489286959397,14.2657781400346));
#43112=CARTESIAN_POINT('Ctrl Pts',(-2.37231105861528,102.511632157536,14.1067798584379));
#43113=CARTESIAN_POINT('Ctrl Pts',(-2.47172208006199,102.562390571945,13.7332170211324));
#43114=CARTESIAN_POINT('Ctrl Pts',(-2.49999602821008,102.590349238264,13.5171226284436));
#43115=CARTESIAN_POINT('Ctrl Pts',(-2.49999999958163,102.61816441031,13.300045736922));
#43116=CARTESIAN_POINT('Origin',(0.,70.2,13.3));
#43117=CARTESIAN_POINT('',(-2.5,97.6537365388727,13.300000000061));
#43118=CARTESIAN_POINT('',(-2.5,98.7897650553754,13.3000000423409));
#43119=CARTESIAN_POINT('',(-2.5,70.2,13.3));
#43120=CARTESIAN_POINT('Ctrl Pts',(-2.5,98.7897650605138,13.3000000429739));
#43121=CARTESIAN_POINT('Ctrl Pts',(-2.50000000214343,98.8051272660355,13.1753065631474));
#43122=CARTESIAN_POINT('Ctrl Pts',(-2.4906708580659,98.8204518455014,13.0507235054539));
#43123=CARTESIAN_POINT('Ctrl Pts',(-2.44826568409266,98.855360827728,12.7694578365237));
#43124=CARTESIAN_POINT('Ctrl Pts',(-2.40940571355738,98.8748469893923,12.6142545421071));
#43125=CARTESIAN_POINT('Ctrl Pts',(-2.30198530466049,98.9141082339661,12.3115894708146));
#43126=CARTESIAN_POINT('Ctrl Pts',(-2.23333073527477,98.9338116246053,12.1649550451765));
#43127=CARTESIAN_POINT('Ctrl Pts',(-1.99098648642878,98.9918312786834,11.7557924829878));
#43128=CARTESIAN_POINT('Ctrl Pts',(-1.78147653231448,99.0295221164529,11.5181582930845));
#43129=CARTESIAN_POINT('Ctrl Pts',(-1.40529604856019,99.0873156968289,11.226000277956));
#43130=CARTESIAN_POINT('Ctrl Pts',(-1.26774449724101,99.1069517428578,11.1391760757682));
#43131=CARTESIAN_POINT('Ctrl Pts',(-0.841826558727321,99.1644754720802,
10.9250932985549));
#43132=CARTESIAN_POINT('Ctrl Pts',(-0.536762726704051,99.2017539995856,
10.8381397520154));
#43133=CARTESIAN_POINT('Ctrl Pts',(0.090611532668975,99.277260929085,10.781805010844));
#43134=CARTESIAN_POINT('Ctrl Pts',(0.407349129855685,99.3145103836881,10.8133136781569));
#43135=CARTESIAN_POINT('Ctrl Pts',(0.86206129970444,99.3707717314157,10.947970020182));
#43136=CARTESIAN_POINT('Ctrl Pts',(1.00962443647151,99.3894664737536,11.0074343217137));
#43137=CARTESIAN_POINT('Ctrl Pts',(1.44812432265774,99.4476893050727,11.2347451963873));
#43138=CARTESIAN_POINT('Ctrl Pts',(1.7116809425071,99.4870872328887,11.447291758789));
#43139=CARTESIAN_POINT('Ctrl Pts',(2.12328411387118,99.5622800556226,11.9443326462106));
#43140=CARTESIAN_POINT('Ctrl Pts',(2.27491957300927,99.5974259474615,12.2179098821064));
#43141=CARTESIAN_POINT('Ctrl Pts',(2.47778820378074,99.6717334494876,12.8289243550386));
#43142=CARTESIAN_POINT('Ctrl Pts',(2.51848056897162,99.7111296876756,13.1634850240867));
#43143=CARTESIAN_POINT('Ctrl Pts',(2.47008131417638,99.7815387857339,13.7783123624695));
#43144=CARTESIAN_POINT('Ctrl Pts',(2.40013715673431,99.8123662283287,14.0546164279131));
#43145=CARTESIAN_POINT('Ctrl Pts',(2.1502067743619,99.8811201682489,14.6182859862622));
#43146=CARTESIAN_POINT('Ctrl Pts',(1.9553652950623,99.9198991317864,14.8930460892253));
#43147=CARTESIAN_POINT('Ctrl Pts',(1.50949062916033,99.9882133066538,15.3122017106855));
#43148=CARTESIAN_POINT('Ctrl Pts',(1.27619852477342,100.017630055568,15.467689370579));
#43149=CARTESIAN_POINT('Ctrl Pts',(0.717247206038844,100.083273518722,15.7180768763258));
#43150=CARTESIAN_POINT('Ctrl Pts',(0.388176065348154,100.119902847992,15.7921610004401));
#43151=CARTESIAN_POINT('Ctrl Pts',(-0.271248184284303,100.19020796814,15.8064786470139));
#43152=CARTESIAN_POINT('Ctrl Pts',(-0.595071393621657,100.22463495625,15.749887798597));
#43153=CARTESIAN_POINT('Ctrl Pts',(-1.05125249761847,100.275694322305,15.5740946185112));
#43154=CARTESIAN_POINT('Ctrl Pts',(-1.19744680120775,100.292753612668,15.5006286895925));
#43155=CARTESIAN_POINT('Ctrl Pts',(-1.59818476697444,100.341714161852,15.2474094550559));
#43156=CARTESIAN_POINT('Ctrl Pts',(-1.82772321634462,100.37297117758,15.0338042070319));
#43157=CARTESIAN_POINT('Ctrl Pts',(-2.1933156268446,100.434384186937,14.5379426114997));
#43158=CARTESIAN_POINT('Ctrl Pts',(-2.32794606981634,100.463422938872,14.2611769303796));
#43159=CARTESIAN_POINT('Ctrl Pts',(-2.45202071822513,100.508032718833,13.8129609280056));
#43160=CARTESIAN_POINT('Ctrl Pts',(-2.47979654466681,100.523353891658,13.6551931589905));
#43161=CARTESIAN_POINT('Ctrl Pts',(-2.49744451782718,100.544218754017,13.4305894947812));
#43162=CARTESIAN_POINT('Ctrl Pts',(-2.5,100.550177730551,13.3652645630937));
#43163=CARTESIAN_POINT('Ctrl Pts',(-2.5,100.556030878907,13.3000000000002));
#43164=CARTESIAN_POINT('',(1.85693809316476,98.5858197253477,11.6266881416021));
#43165=CARTESIAN_POINT('Ctrl Pts',(-2.5,99.7536786153901,13.299999999048));
#43166=CARTESIAN_POINT('Ctrl Pts',(-2.50000000000205,99.7529871031884,13.3053793145855));
#43167=CARTESIAN_POINT('Ctrl Pts',(-2.49998263778621,99.7522955829396,13.3107594365981));
#43168=CARTESIAN_POINT('Ctrl Pts',(-2.49886417546877,99.7300314983695,13.4839966483087));
#43169=CARTESIAN_POINT('Ctrl Pts',(-2.48087730636317,99.708595350066,13.6513255859644));
#43170=CARTESIAN_POINT('Ctrl Pts',(-2.4130122730618,99.6665343858624,13.9733155581015));
#43171=CARTESIAN_POINT('Ctrl Pts',(-2.36459163132424,99.6460111796206,14.1274611634218));
#43172=CARTESIAN_POINT('Ctrl Pts',(-2.17142198877263,99.5830262880744,14.5830657591208));
#43173=CARTESIAN_POINT('Ctrl Pts',(-1.98097237446091,99.5413281492994,14.8611303351601));
#43174=CARTESIAN_POINT('Ctrl Pts',(-1.50488730504586,99.4580955184984,15.3233915873593));
#43175=CARTESIAN_POINT('Ctrl Pts',(-1.22506645736199,99.4173386990936,15.5040984827822));
#43176=CARTESIAN_POINT('Ctrl Pts',(-0.770752212604174,99.356807626939,15.6835012772582));
#43177=CARTESIAN_POINT('Ctrl Pts',(-0.618072616570848,99.3372697100055,
15.7275767246838));
#43178=CARTESIAN_POINT('Ctrl Pts',(-0.140620197266651,99.2774807068649,
15.8174051103642));
#43179=CARTESIAN_POINT('Ctrl Pts',(0.189803133257262,99.2378372422568,15.8141821376149));
#43180=CARTESIAN_POINT('Ctrl Pts',(0.665595919586561,99.1787152582534,15.7149884669689));
#43181=CARTESIAN_POINT('Ctrl Pts',(0.817533069576632,99.1595297038779,15.6678752431131));
#43182=CARTESIAN_POINT('Ctrl Pts',(1.1118761690379,99.1210583390881,15.544866071418));
#43183=CARTESIAN_POINT('Ctrl Pts',(1.25348934389529,99.101862958593,15.4689770455246));
#43184=CARTESIAN_POINT('Ctrl Pts',(1.66685831342957,99.0423367829859,15.1933650357196));
#43185=CARTESIAN_POINT('Ctrl Pts',(1.90632908056946,99.0025134688997,14.9520317040624));
#43186=CARTESIAN_POINT('Ctrl Pts',(2.179981716146,98.9436737025004,14.5345489450462));
#43187=CARTESIAN_POINT('Ctrl Pts',(2.25563508912969,98.9246597486341,14.3902042183656));
#43188=CARTESIAN_POINT('Ctrl Pts',(2.43966574363723,98.8672341310013,13.9364148628871));
#43189=CARTESIAN_POINT('Ctrl Pts',(2.5019341340693,98.8293628637644,13.6120529936428));
#43190=CARTESIAN_POINT('Ctrl Pts',(2.49903474331672,98.7742921815908,13.1329263785518));
#43191=CARTESIAN_POINT('Ctrl Pts',(2.48426450572032,98.7569600705699,12.9813778565468));
#43192=CARTESIAN_POINT('Ctrl Pts',(2.41162109407947,98.712498421881,12.6000940934995));
#43193=CARTESIAN_POINT('Ctrl Pts',(2.33475495555389,98.6855918690322,12.3754851169304));
#43194=CARTESIAN_POINT('Ctrl Pts',(2.12817714561673,98.6342832714491,11.9700655205455));
#43195=CARTESIAN_POINT('Ctrl Pts',(2.00368739954201,98.6100544090427,11.7890026644713));
#43196=CARTESIAN_POINT('Ctrl Pts',(1.85721457609527,98.5856828656957,11.6264546560253));
#43197=CARTESIAN_POINT('',(-2.49956101882259,97.6535864963121,13.298861354865));
#43198=CARTESIAN_POINT('Ctrl Pts',(1.85690960710508,98.5856773324862,11.6267152159055));
#43199=CARTESIAN_POINT('Ctrl Pts',(1.8077250499098,98.5731300683111,11.5720968634514));
#43200=CARTESIAN_POINT('Ctrl Pts',(1.75634066847637,98.560755922621,11.5196760589334));
#43201=CARTESIAN_POINT('Ctrl Pts',(1.70281770841323,98.5483499926756,11.4697088541542));
#43202=CARTESIAN_POINT('Ctrl Pts',(1.69221343839639,98.5458920600277,11.4598090703821));
#43203=CARTESIAN_POINT('Ctrl Pts',(1.68152525336647,98.5434329006297,11.4500057589624));
#43204=CARTESIAN_POINT('Ctrl Pts',(1.67075368875989,98.5409709520606,11.4403011455887));
#43205=CARTESIAN_POINT('Ctrl Pts',(1.60526395387986,98.5260026196997,11.3812983377171));
#43206=CARTESIAN_POINT('Ctrl Pts',(1.53678119562569,98.5111050743696,11.3258301785802));
#43207=CARTESIAN_POINT('Ctrl Pts',(1.46555679140617,98.4962988036746,11.2741434922838));
#43208=CARTESIAN_POINT('Ctrl Pts',(1.39433238718665,98.4814925329796,11.2224568059874));
#43209=CARTESIAN_POINT('Ctrl Pts',(1.32036646695919,98.466777901265,11.1745506420625));
#43210=CARTESIAN_POINT('Ctrl Pts',(1.24386760259586,98.4521967174326,11.1306839680054));
#43211=CARTESIAN_POINT('Ctrl Pts',(1.24384665438821,98.4521927245672,11.1306719556938));
#43212=CARTESIAN_POINT('Ctrl Pts',(1.24382570599033,98.4521887317119,11.1306599436852));
#43213=CARTESIAN_POINT('Ctrl Pts',(1.24380475740234,98.4521847388666,11.1306479319799));
#43214=CARTESIAN_POINT('Ctrl Pts',(1.18362787507212,98.4407148975493,11.0961431253399));
#43215=CARTESIAN_POINT('Ctrl Pts',(1.12188171434896,98.4293278778844,11.0641378362799));
#43216=CARTESIAN_POINT('Ctrl Pts',(1.05873497356869,98.4179752887785,11.034710939003));
#43217=CARTESIAN_POINT('Ctrl Pts',(0.980190438086826,98.4038544675482,10.9981085435549));
#43218=CARTESIAN_POINT('Ctrl Pts',(0.899887840407072,98.3898595702403,10.9656844771038));
#43219=CARTESIAN_POINT('Ctrl Pts',(0.81820808033838,98.3759192694801,10.9374911360008));
#43220=CARTESIAN_POINT('Ctrl Pts',(0.735155417917374,98.3617446552048,10.9088239112295));
#43221=CARTESIAN_POINT('Ctrl Pts',(0.650678671048983,98.3476263482223,10.8845311962933));
#43222=CARTESIAN_POINT('Ctrl Pts',(0.56516518123011,98.3335200054256,10.8646907338479));
#43223=CARTESIAN_POINT('Ctrl Pts',(0.479335393357447,98.3193614859631,10.8447768853243));
#43224=CARTESIAN_POINT('Ctrl Pts',(0.392461224071964,98.305215056977,10.8293484093262));
#43225=CARTESIAN_POINT('Ctrl Pts',(0.304922580453783,98.2910671650078,10.8185025756208));
#43226=CARTESIAN_POINT('Ctrl Pts',(0.23434772347413,98.2796609401565,10.8097585155012));
#43227=CARTESIAN_POINT('Ctrl Pts',(0.163340782647186,98.2682544039755,10.803993323425));
#43228=CARTESIAN_POINT('Ctrl Pts',(0.0920946306619685,98.2568545880395,
10.8012672213045));
#43229=CARTESIAN_POINT('Ctrl Pts',(0.0087673670571682,98.2435217210554,
10.7980788578116));
#43230=CARTESIAN_POINT('Ctrl Pts',(-0.0744698003503501,98.230263849956,
10.7990633229069));
#43231=CARTESIAN_POINT('Ctrl Pts',(-0.157327380642784,98.2171110235674,
10.8042089214701));
#43232=CARTESIAN_POINT('Ctrl Pts',(-0.162465995246597,98.2162953190112,
10.8045280382948));
#43233=CARTESIAN_POINT('Ctrl Pts',(-0.167603159750644,98.2154800177744,
10.8048631728795));
#43234=CARTESIAN_POINT('Ctrl Pts',(-0.172738808847055,98.2146651267462,
10.8052143278411));
#43235=CARTESIAN_POINT('Ctrl Pts',(-0.231902192624619,98.2052774700482,
10.8092596812852));
#43236=CARTESIAN_POINT('Ctrl Pts',(-0.290863988911329,98.1959448621742,
10.8154295879729));
#43237=CARTESIAN_POINT('Ctrl Pts',(-0.349529404896252,98.186682902991,10.8237293448082));
#43238=CARTESIAN_POINT('Ctrl Pts',(-0.349566423542153,98.1866770585734,
10.8237345820635));
#43239=CARTESIAN_POINT('Ctrl Pts',(-0.349603442069974,98.1866712141838,
10.8237398201674));
#43240=CARTESIAN_POINT('Ctrl Pts',(-0.349640460479707,98.1866653698222,
10.8237450591199));
#43241=CARTESIAN_POINT('Ctrl Pts',(-0.435420835414029,98.173122607364,10.8358849460904));
#43242=CARTESIAN_POINT('Ctrl Pts',(-0.520569872626937,98.1597297385198,
10.8525773729019));
#43243=CARTESIAN_POINT('Ctrl Pts',(-0.604757739420849,98.1463938881941,
10.8737062199925));
#43244=CARTESIAN_POINT('Ctrl Pts',(-0.690177587505622,98.1328628848288,
10.8951442606201));
#43245=CARTESIAN_POINT('Ctrl Pts',(-0.774608104153329,98.1193902428782,
10.9211504533214));
#43246=CARTESIAN_POINT('Ctrl Pts',(-0.857675979165781,98.1059045094002,
10.9516283315024));
#43247=CARTESIAN_POINT('Ctrl Pts',(-0.867543590611796,98.1043025425988,
10.95524879079));
#43248=CARTESIAN_POINT('Ctrl Pts',(-0.877391939972514,98.1027004235435,
10.9589323693656));
#43249=CARTESIAN_POINT('Ctrl Pts',(-0.8872203744183,98.1010980591305,10.9626789196573));
#43250=CARTESIAN_POINT('Ctrl Pts',(-0.969282088609672,98.0877192477634,
10.9939604366615));
#43251=CARTESIAN_POINT('Ctrl Pts',(-1.04952459558973,98.0743905233542,11.0294665444871));
#43252=CARTESIAN_POINT('Ctrl Pts',(-1.12761912194777,98.0610745687717,11.0689869248279));
#43253=CARTESIAN_POINT('Ctrl Pts',(-1.20649254011099,98.0476258047801,11.1089014698024));
#43254=CARTESIAN_POINT('Ctrl Pts',(-1.28317473152672,98.0341901899186,11.1529106546193));
#43255=CARTESIAN_POINT('Ctrl Pts',(-1.35733332410368,98.0207589852649,11.2008200181214));
#43256=CARTESIAN_POINT('Ctrl Pts',(-1.43093441808567,98.0074287517525,11.2483692156344));
#43257=CARTESIAN_POINT('Ctrl Pts',(-1.50204983803708,97.9941031558961,11.2997597484355));
#43258=CARTESIAN_POINT('Ctrl Pts',(-1.57036148504395,97.9807995009096,11.3548272860642));
#43259=CARTESIAN_POINT('Ctrl Pts',(-1.62464458227933,97.9702278981324,11.3985860977835));
#43260=CARTESIAN_POINT('Ctrl Pts',(-1.6771575261111,97.9596707221894,11.4446671003648));
#43261=CARTESIAN_POINT('Ctrl Pts',(-1.72774177335385,97.9491463647847,11.4930030452226));
#43262=CARTESIAN_POINT('Ctrl Pts',(-1.75106323781302,97.9442941935941,11.5152879477672));
#43263=CARTESIAN_POINT('Ctrl Pts',(-1.77392982658307,97.9394584790718,11.5380094279285));
#43264=CARTESIAN_POINT('Ctrl Pts',(-1.79633105271662,97.9346413679592,11.56115692621));
#43265=CARTESIAN_POINT('Ctrl Pts',(-1.79633402503211,97.934640728799,11.5611599975449));
#43266=CARTESIAN_POINT('Ctrl Pts',(-1.79633699733939,97.934640089639,11.5611630688873));
#43267=CARTESIAN_POINT('Ctrl Pts',(-1.79633996963847,97.9346394504794,11.5611661402372));
#43268=CARTESIAN_POINT('Ctrl Pts',(-1.85648744176362,97.9217054101724,11.6233180056473));
#43269=CARTESIAN_POINT('Ctrl Pts',(-1.91328231390543,97.908903295095,11.6885410519733));
#43270=CARTESIAN_POINT('Ctrl Pts',(-1.96654495350802,97.8961492911077,11.7565102147902));
#43271=CARTESIAN_POINT('Ctrl Pts',(-2.02072536299437,97.8831755225567,11.8256505559625));
#43272=CARTESIAN_POINT('Ctrl Pts',(-2.07125007841324,97.8702513400781,11.8976329408409));
#43273=CARTESIAN_POINT('Ctrl Pts',(-2.11790735285553,97.8573194023268,11.9721188703281));
#43274=CARTESIAN_POINT('Ctrl Pts',(-2.16480499076845,97.8443208433362,12.046988527685));
#43275=CARTESIAN_POINT('Ctrl Pts',(-2.20779465421926,97.8313144343512,12.1243875209184));
#43276=CARTESIAN_POINT('Ctrl Pts',(-2.24664854939422,97.8182743953918,12.2039727074303));
#43277=CARTESIAN_POINT('Ctrl Pts',(-2.26366933039734,97.8125619270177,12.2388367030377));
#43278=CARTESIAN_POINT('Ctrl Pts',(-2.27989631894334,97.8068434236944,12.2741202603897));
#43279=CARTESIAN_POINT('Ctrl Pts',(-2.29530993377528,97.8011186409183,12.3097947551504));
#43280=CARTESIAN_POINT('Ctrl Pts',(-2.33044684477994,97.7880684132385,12.391118413566));
#43281=CARTESIAN_POINT('Ctrl Pts',(-2.3611719920498,97.7750529178162,12.4740419297995));
#43282=CARTESIAN_POINT('Ctrl Pts',(-2.38739168035197,97.7620898280361,12.5581907883444));
#43283=CARTESIAN_POINT('Ctrl Pts',(-2.41181656453723,97.7500140946059,12.6365794442504));
#43284=CARTESIAN_POINT('Ctrl Pts',(-2.43233211720112,97.7379841771657,12.7160315578295));
#43285=CARTESIAN_POINT('Ctrl Pts',(-2.44886153498619,97.7260327698438,12.7962804586082));
#43286=CARTESIAN_POINT('Ctrl Pts',(-2.45007079496971,97.7251584281816,12.8021513117559));
#43287=CARTESIAN_POINT('Ctrl Pts',(-2.4512587063564,97.7242845053269,12.8080264474667));
#43288=CARTESIAN_POINT('Ctrl Pts',(-2.45242523195955,97.7234110134226,12.8139057696976));
#43289=CARTESIAN_POINT('Ctrl Pts',(-2.46681732935069,97.7126342413359,12.8864423500451));
#43290=CARTESIAN_POINT('Ctrl Pts',(-2.47795721570267,97.7019238513227,12.9596138246261));
#43291=CARTESIAN_POINT('Ctrl Pts',(-2.48577639666548,97.6913126183989,13.033253105027));
#43292=CARTESIAN_POINT('Ctrl Pts',(-2.48577675208907,97.6913121360617,13.0332564523261));
#43293=CARTESIAN_POINT('Ctrl Pts',(-2.48577710750579,97.6913116537246,13.0332597996261));
#43294=CARTESIAN_POINT('Ctrl Pts',(-2.48577746291565,97.6913111713877,13.0332631469272));
#43295=CARTESIAN_POINT('Ctrl Pts',(-2.49401981843078,97.680125235194,13.110890833956));
#43296=CARTESIAN_POINT('Ctrl Pts',(-2.49857267927591,97.6690489749956,13.1890433458736));
#43297=CARTESIAN_POINT('Ctrl Pts',(-2.49941994343173,97.6580017020404,13.2674859930955));
#43298=CARTESIAN_POINT('Ctrl Pts',(-2.49946891720529,97.6573631448202,13.2720201545092));
#43299=CARTESIAN_POINT('Ctrl Pts',(-2.49950549973951,97.6567246856369,13.2765552753999));
#43300=CARTESIAN_POINT('Ctrl Pts',(-2.49952968419203,97.6560863093464,13.2810913066838));
#43301=CARTESIAN_POINT('Ctrl Pts',(-2.49956126834484,97.6552526095017,13.2870152243378));
#43302=CARTESIAN_POINT('Ctrl Pts',(-2.49957170282008,97.6544193477551,13.2929386213973));
#43303=CARTESIAN_POINT('Ctrl Pts',(-2.49956101882259,97.6535864963121,13.298861354865));
#43304=CARTESIAN_POINT('Ctrl Pts',(-2.49999975973186,97.6538889287948,13.2989039431398));
#43305=CARTESIAN_POINT('Ctrl Pts',(-2.49999991991164,97.6538381304678,13.2992692977425));
#43306=CARTESIAN_POINT('Ctrl Pts',(-2.50000000000002,97.6537873338306,13.2996346500787));
#43307=CARTESIAN_POINT('Ctrl Pts',(-2.5,97.6537365388727,13.3000000001219));
#43308=CARTESIAN_POINT('Origin',(0.,70.2,13.3));
#43309=CARTESIAN_POINT('',(-2.5,95.5986983740631,13.2999999999961));
#43310=CARTESIAN_POINT('',(-2.5,96.7549279855909,13.2999999999447));
#43311=CARTESIAN_POINT('',(-2.5,70.2,13.3));
#43312=CARTESIAN_POINT('',(-2.49999986066494,96.7550430853858,13.2991653292544));
#43313=CARTESIAN_POINT('Ctrl Pts',(-2.5,96.7549279855909,13.2999999998894));
#43314=CARTESIAN_POINT('Ctrl Pts',(-2.49999999999999,96.7549668066987,13.2997184759693));
#43315=CARTESIAN_POINT('Ctrl Pts',(-2.499999954658,96.7550042625919,13.2994468565905));
#43316=CARTESIAN_POINT('Ctrl Pts',(-2.49999986066494,96.7550430853858,13.2991653292544));
#43317=CARTESIAN_POINT('Ctrl Pts',(-2.49999986066494,96.7550430853858,13.2991653292544));
#43318=CARTESIAN_POINT('Ctrl Pts',(-2.4999048220303,96.7942977431784,13.0145062890155));
#43319=CARTESIAN_POINT('Ctrl Pts',(-2.45119641016012,96.8342362093599,12.7319672350244));
#43320=CARTESIAN_POINT('Ctrl Pts',(-2.24580299791176,96.9182776615934,12.1533329620363));
#43321=CARTESIAN_POINT('Ctrl Pts',(-2.07536145657939,96.961638181301,11.867721059664));
#43322=CARTESIAN_POINT('Ctrl Pts',(-1.70534736711559,97.0370430385601,11.4584834123906));
#43323=CARTESIAN_POINT('Ctrl Pts',(-1.53496590298137,97.0676330581365,11.3142279371448));
#43324=CARTESIAN_POINT('Ctrl Pts',(-1.06376103659421,97.1429442871494,11.0126211563722));
#43325=CARTESIAN_POINT('Ctrl Pts',(-0.745874945772812,97.1864051895193,
10.890136629139));
#43326=CARTESIAN_POINT('Ctrl Pts',(-0.2614463808509,97.2520668212153,10.808950743721));
#43327=CARTESIAN_POINT('Ctrl Pts',(-0.107656360007522,97.2727323842445,
10.7975835750841));
#43328=CARTESIAN_POINT('Ctrl Pts',(0.368999568794703,97.3366120753734,10.8063924363503));
#43329=CARTESIAN_POINT('Ctrl Pts',(0.687640674119482,97.3784385152547,10.8748312297851));
#43330=CARTESIAN_POINT('Ctrl Pts',(1.12953003033371,97.4416803229475,11.0641423801631));
#43331=CARTESIAN_POINT('Ctrl Pts',(1.26836582571434,97.4624317716116,11.1398730102519));
#43332=CARTESIAN_POINT('Ctrl Pts',(1.53637440812764,97.5047924201444,11.320864607133));
#43333=CARTESIAN_POINT('Ctrl Pts',(1.66407019271966,97.5262914635495,11.4269549133227));
#43334=CARTESIAN_POINT('Ctrl Pts',(1.89442578477539,97.5691004210316,11.6606219903953));
#43335=CARTESIAN_POINT('Ctrl Pts',(1.99695763875969,97.5903017820097,11.7871985510204));
#43336=CARTESIAN_POINT('Ctrl Pts',(2.26999867043505,97.6550460335004,12.2008667524305));
#43337=CARTESIAN_POINT('Ctrl Pts',(2.396117148237,97.6975554606845,12.5128257932262));
#43338=CARTESIAN_POINT('Ctrl Pts',(2.48662776819297,97.7612196066646,12.9967060763603));
#43339=CARTESIAN_POINT('Ctrl Pts',(2.50088558516876,97.7817796272842,13.1555073472334));
#43340=CARTESIAN_POINT('Ctrl Pts',(2.49900506359339,97.8233510810348,13.4778209951536));
#43341=CARTESIAN_POINT('Ctrl Pts',(2.48206732363548,97.844233587277,13.6405767748455));
#43342=CARTESIAN_POINT('Ctrl Pts',(2.38754758700351,97.9048166049424,14.1031239518931));
#43343=CARTESIAN_POINT('Ctrl Pts',(2.27016509505655,97.9442452537162,14.3916775207734));
#43344=CARTESIAN_POINT('Ctrl Pts',(2.01166848824739,98.0052587730919,14.7939351977878));
#43345=CARTESIAN_POINT('Ctrl Pts',(1.90593033739705,98.0267429784756,14.9266787869341));
#43346=CARTESIAN_POINT('Ctrl Pts',(1.67387596686174,98.0690202143734,15.1640275240825));
#43347=CARTESIAN_POINT('Ctrl Pts',(1.54907843914706,98.0897042238692,15.268963261203));
#43348=CARTESIAN_POINT('Ctrl Pts',(1.28379776255734,98.1306363590377,15.4510883205238));
#43349=CARTESIAN_POINT('Ctrl Pts',(1.14431833258083,98.1507581395254,15.5284202670932));
#43350=CARTESIAN_POINT('Ctrl Pts',(0.695788205789993,98.21269066934,15.7238097878825));
#43351=CARTESIAN_POINT('Ctrl Pts',(0.369995281367472,98.2540823150316,15.7944124734551));
#43352=CARTESIAN_POINT('Ctrl Pts',(-0.124078022263904,98.3163559804903,
15.8022990562058));
#43353=CARTESIAN_POINT('Ctrl Pts',(-0.287921324138257,98.3369323485032,
15.7887747607542));
#43354=CARTESIAN_POINT('Ctrl Pts',(-0.777776827461194,98.3994949808555,
15.6992892043637));
#43355=CARTESIAN_POINT('Ctrl Pts',(-1.09097785132098,98.4409096251606,15.5740518226424));
#43356=CARTESIAN_POINT('Ctrl Pts',(-1.62791708018648,98.5211033674332,15.2221710225551));
#43357=CARTESIAN_POINT('Ctrl Pts',(-1.85212484969452,98.5591586581678,15.0071914751938));
#43358=CARTESIAN_POINT('Ctrl Pts',(-2.12518501545708,98.6174049447581,14.626411606301));
#43359=CARTESIAN_POINT('Ctrl Pts',(-2.20596720111262,98.6372923791233,14.4872196738139));
#43360=CARTESIAN_POINT('Ctrl Pts',(-2.40442423974478,98.696314506151,14.0540238557462));
#43361=CARTESIAN_POINT('Ctrl Pts',(-2.48038171310186,98.7349138964142,13.7444405524168));
#43362=CARTESIAN_POINT('Ctrl Pts',(-2.49889197968721,98.7791722189695,13.3859597485197));
#43363=CARTESIAN_POINT('Ctrl Pts',(-2.49999999926131,98.7844707629695,13.3429733245846));
#43364=CARTESIAN_POINT('Ctrl Pts',(-2.5,98.7897650605139,13.3000000429739));
#43365=CARTESIAN_POINT('Ctrl Pts',(-2.5,97.6537365388727,13.3000000001219));
#43366=CARTESIAN_POINT('Ctrl Pts',(-2.49999999999076,97.627401975356,13.4894151372761));
#43367=CARTESIAN_POINT('Ctrl Pts',(-2.4784747780135,97.6014402125008,13.67820302557));
#43368=CARTESIAN_POINT('Ctrl Pts',(-2.40177725317404,97.5536409027924,14.0101859651423));
#43369=CARTESIAN_POINT('Ctrl Pts',(-2.35441017643867,97.5321493679576,14.1541811575294));
#43370=CARTESIAN_POINT('Ctrl Pts',(-2.192399226816,97.4733058212946,14.5285183068175));
#43371=CARTESIAN_POINT('Ctrl Pts',(-2.05480027994648,97.4355934204874,14.7469513949122));
#43372=CARTESIAN_POINT('Ctrl Pts',(-1.67493578681359,97.3527118660193,15.1837187278098));
#43373=CARTESIAN_POINT('Ctrl Pts',(-1.41852849998166,97.3100120024059,15.3836717135531));
#43374=CARTESIAN_POINT('Ctrl Pts',(-0.836152786389093,97.2206086767106,
15.6791168348764));
#43375=CARTESIAN_POINT('Ctrl Pts',(-0.514540246449376,97.174495855927,15.7687012573328));
#43376=CARTESIAN_POINT('Ctrl Pts',(0.0509460299849206,97.0952246912926,
15.8106474016969));
#43377=CARTESIAN_POINT('Ctrl Pts',(0.288229664456515,97.0630785404824,15.7945929786411));
#43378=CARTESIAN_POINT('Ctrl Pts',(0.847849911368506,96.9875772773639,15.6756260792212));
#43379=CARTESIAN_POINT('Ctrl Pts',(1.15847714094599,96.9444677987102,15.540619152968));
#43380=CARTESIAN_POINT('Ctrl Pts',(1.70390832761623,96.8557277708046,15.1589874242792));
#43381=CARTESIAN_POINT('Ctrl Pts',(1.93442436709792,96.8112368601696,14.9177806471101));
#43382=CARTESIAN_POINT('Ctrl Pts',(2.19482873235114,96.747557840951,14.5070674152662));
#43383=CARTESIAN_POINT('Ctrl Pts',(2.26579713673052,96.7274806900131,14.3679232083318));
#43384=CARTESIAN_POINT('Ctrl Pts',(2.43940956666114,96.6667595832406,13.9309409165425));
#43385=CARTESIAN_POINT('Ctrl Pts',(2.49932457427662,96.6263279190135,13.6195785155601));
#43386=CARTESIAN_POINT('Ctrl Pts',(2.50071024216123,96.5409121595066,12.9694116703955));
#43387=CARTESIAN_POINT('Ctrl Pts',(2.43371445754413,96.4970067633686,12.6367081648662));
#43388=CARTESIAN_POINT('Ctrl Pts',(2.17706364847366,96.412042208916,12.0291557188249));
#43389=CARTESIAN_POINT('Ctrl Pts',(1.99451233046105,96.3711267612373,11.7583759989667));
#43390=CARTESIAN_POINT('Ctrl Pts',(1.53615472367558,96.2884946343016,11.3012299239407));
#43391=CARTESIAN_POINT('Ctrl Pts',(1.26461108592141,96.2475172110001,11.1192575230292));
#43392=CARTESIAN_POINT('Ctrl Pts',(0.659213540111815,96.1644262521489,10.8656613387087));
#43393=CARTESIAN_POINT('Ctrl Pts',(0.329919297730919,96.1231293188218,10.7996487205787));
#43394=CARTESIAN_POINT('Ctrl Pts',(-0.271650992945435,96.0477807689548,
10.8002866753478));
#43395=CARTESIAN_POINT('Ctrl Pts',(-0.53886072686419,96.0143725009609,10.8439866649088));
#43396=CARTESIAN_POINT('Ctrl Pts',(-0.930947777987851,95.9628533577763,
10.9753046607155));
#43397=CARTESIAN_POINT('Ctrl Pts',(-1.06370987554998,95.9449175566548,11.0329764389628));
#43398=CARTESIAN_POINT('Ctrl Pts',(-1.4856031535675,95.8853573127292,11.2615121404549));
#43399=CARTESIAN_POINT('Ctrl Pts',(-1.74536023738308,95.8443779661622,11.4789526737075));
#43400=CARTESIAN_POINT('Ctrl Pts',(-2.12607564347549,95.7696574029082,11.9563022019608));
#43401=CARTESIAN_POINT('Ctrl Pts',(-2.26097034795487,95.7363966300211,12.1983000332855));
#43402=CARTESIAN_POINT('Ctrl Pts',(-2.40424892457855,95.6845807834732,12.5985295102163));
#43403=CARTESIAN_POINT('Ctrl Pts',(-2.44198066924691,95.6663679720158,12.7439353615846));
#43404=CARTESIAN_POINT('Ctrl Pts',(-2.48878040304612,95.6316250583232,13.0267460608703));
#43405=CARTESIAN_POINT('Ctrl Pts',(-2.49999999999958,95.6151461118388,13.1632543090288));
#43406=CARTESIAN_POINT('Ctrl Pts',(-2.5,95.5986983740631,13.2999999999923));
#43407=CARTESIAN_POINT('Origin',(0.,70.2,13.3));
#43408=CARTESIAN_POINT('',(-2.49986749706851,93.5355013981268,13.3002300840465));
#43409=CARTESIAN_POINT('',(-2.5,94.5443074868315,13.3));
#43410=CARTESIAN_POINT('',(-2.5,70.2,13.3));
#43411=CARTESIAN_POINT('',(1.26263430499969,95.0979194610116,11.1414618660017));
#43412=CARTESIAN_POINT('Ctrl Pts',(-2.5,94.5443074868315,13.3000000000001));
#43413=CARTESIAN_POINT('Ctrl Pts',(-2.5,94.5644680475081,13.1186486447222));
#43414=CARTESIAN_POINT('Ctrl Pts',(-2.48026874018247,94.5847545601826,12.9374339113955));
#43415=CARTESIAN_POINT('Ctrl Pts',(-2.37654233467327,94.6386548782938,12.4689486065813));
#43416=CARTESIAN_POINT('Ctrl Pts',(-2.26079321829323,94.6713476130852,12.1920715749935));
#43417=CARTESIAN_POINT('Ctrl Pts',(-2.01323785574154,94.7204442407306,11.8094242032686));
#43418=CARTESIAN_POINT('Ctrl Pts',(-1.91508090445217,94.7372444910322,11.6852537477538));
#43419=CARTESIAN_POINT('Ctrl Pts',(-1.5772741532493,94.7899797268026,11.3323920717047));
#43420=CARTESIAN_POINT('Ctrl Pts',(-1.30348816183964,94.8259667526053,11.1412239424654));
#43421=CARTESIAN_POINT('Ctrl Pts',(-0.708934834990189,94.8936466630685,
10.8816245350023));
#43422=CARTESIAN_POINT('Ctrl Pts',(-0.395859301737226,94.9254859523938,
10.8111388947139));
#43423=CARTESIAN_POINT('Ctrl Pts',(0.17199246902843,94.9845464046267,10.7934137226392));
#43424=CARTESIAN_POINT('Ctrl Pts',(0.42181962795496,95.0100858075626,10.8231668857346));
#43425=CARTESIAN_POINT('Ctrl Pts',(0.87298920622079,95.0561559175267,10.9472851876794));
#43426=CARTESIAN_POINT('Ctrl Pts',(1.07440374312525,95.0767567093663,11.0321747618983));
#43427=CARTESIAN_POINT('Ctrl Pts',(1.26227923984204,95.0978944889888,11.142072494113));
#43428=CARTESIAN_POINT('Ctrl Pts',(1.26203730190332,95.0995873533355,11.1419309907687));
#43429=CARTESIAN_POINT('Ctrl Pts',(1.46842430378966,95.1476613657154,11.262625970352));
#43430=CARTESIAN_POINT('Ctrl Pts',(1.65668516861459,95.1947410746065,11.4124842588553));
#43431=CARTESIAN_POINT('Ctrl Pts',(2.01414687277796,95.2959850342644,11.7923979876296));
#43432=CARTESIAN_POINT('Ctrl Pts',(2.17133982784043,95.3467602996658,12.0291119103098));
#43433=CARTESIAN_POINT('Ctrl Pts',(2.40258858417271,95.4497714527187,12.5511821660518));
#43434=CARTESIAN_POINT('Ctrl Pts',(2.47302861188947,95.5011569869884,12.8334108037426));
#43435=CARTESIAN_POINT('Ctrl Pts',(2.51582245316482,95.6026152339085,13.4321460196188));
#43436=CARTESIAN_POINT('Ctrl Pts',(2.47984647037667,95.6545025759123,13.7441960487413));
#43437=CARTESIAN_POINT('Ctrl Pts',(2.34060727965609,95.7315276322284,14.1924901756862));
#43438=CARTESIAN_POINT('Ctrl Pts',(2.27953083918698,95.7565976643406,14.3386250518416));
#43439=CARTESIAN_POINT('Ctrl Pts',(2.0632840803951,95.8295088394741,14.7433714554592));
#43440=CARTESIAN_POINT('Ctrl Pts',(1.87477882323332,95.8775947323833,14.9810074047945));
#43441=CARTESIAN_POINT('Ctrl Pts',(1.52582791384189,95.9494024363869,15.2870786508213));
#43442=CARTESIAN_POINT('Ctrl Pts',(1.39287000270935,95.9741138758102,15.3824433696164));
#43443=CARTESIAN_POINT('Ctrl Pts',(0.962236362152568,96.0499931698765,15.6314762132584));
#43444=CARTESIAN_POINT('Ctrl Pts',(0.64220285034896,96.100642312423,15.7391436704674));
#43445=CARTESIAN_POINT('Ctrl Pts',(-0.0128182161629909,96.1981843631053,
15.8210933592527));
#43446=CARTESIAN_POINT('Ctrl Pts',(-0.340864458137898,96.246576201709,15.7979887443412));
#43447=CARTESIAN_POINT('Ctrl Pts',(-0.978260935330136,96.3424149658101,
15.6248722001714));
#43448=CARTESIAN_POINT('Ctrl Pts',(-1.2804779668322,96.3894533056691,15.4731330420803));
#43449=CARTESIAN_POINT('Ctrl Pts',(-1.80705279880308,96.4856715391894,15.0596972143874));
#43450=CARTESIAN_POINT('Ctrl Pts',(-2.02611260905865,96.5323773074924,14.8022897964918));
#43451=CARTESIAN_POINT('Ctrl Pts',(-2.28083439937312,96.6072885286814,14.3414471807324));
#43452=CARTESIAN_POINT('Ctrl Pts',(-2.35405458842808,96.6344178644481,14.1633121593938));
#43453=CARTESIAN_POINT('Ctrl Pts',(-2.46842584453599,96.6924053719844,13.757701351164));
#43454=CARTESIAN_POINT('Ctrl Pts',(-2.50000000001015,96.7232936431479,13.5294067478282));
#43455=CARTESIAN_POINT('Ctrl Pts',(-2.5,96.7549279855909,13.2999999998894));
#43456=CARTESIAN_POINT('',(-2.49999982739251,95.5985866352558,13.3009289980743));
#43457=CARTESIAN_POINT('Ctrl Pts',(-2.5,95.5986983740631,13.2999999999923));
#43458=CARTESIAN_POINT('Ctrl Pts',(-2.5,95.5986607295953,13.3003129742643));
#43459=CARTESIAN_POINT('Ctrl Pts',(-2.49999994369443,95.5986242794474,13.3006160213367));
#43460=CARTESIAN_POINT('Ctrl Pts',(-2.49999982739251,95.5985866352558,13.3009289980743));
#43461=CARTESIAN_POINT('',(1.16384208806484,94.4245814674342,11.0879031093561));
#43462=CARTESIAN_POINT('Ctrl Pts',(-2.49999982739251,95.5985866352558,13.3009289980743));
#43463=CARTESIAN_POINT('Ctrl Pts',(-2.49991594077752,95.5714345148425,13.5266738395382));
#43464=CARTESIAN_POINT('Ctrl Pts',(-2.46925785809366,95.544573295601,13.7513636778397));
#43465=CARTESIAN_POINT('Ctrl Pts',(-2.34196456797705,95.4874583805173,14.2097856729491));
#43466=CARTESIAN_POINT('Ctrl Pts',(-2.2393043135814,95.4576130445069,14.4393195495366));
#43467=CARTESIAN_POINT('Ctrl Pts',(-1.94095249925456,95.392167000552,14.9044377699575));
#43468=CARTESIAN_POINT('Ctrl Pts',(-1.73274263558696,95.3572435285814,15.1273299475365));
#43469=CARTESIAN_POINT('Ctrl Pts',(-1.35662187133884,95.3021398289391,15.4064365280348));
#43470=CARTESIAN_POINT('Ctrl Pts',(-1.21394946922444,95.2826120965141,15.4917637903386));
#43471=CARTESIAN_POINT('Ctrl Pts',(-0.762885317374347,95.2242495326819,
15.703879635277));
#43472=CARTESIAN_POINT('Ctrl Pts',(-0.436626489655097,95.1865739351268,
15.7839558464747));
#43473=CARTESIAN_POINT('Ctrl Pts',(0.0537123919130964,95.1303100478708,
15.8044169864406));
#43474=CARTESIAN_POINT('Ctrl Pts',(0.211919055482687,95.1120638801406,15.796011968289));
#43475=CARTESIAN_POINT('Ctrl Pts',(0.694474064943877,95.055886535,15.7241452126201));
#43476=CARTESIAN_POINT('Ctrl Pts',(1.00792883989179,95.019068419798,15.6114805376621));
#43477=CARTESIAN_POINT('Ctrl Pts',(1.57641306123172,94.9452865667945,15.2688456076683));
#43478=CARTESIAN_POINT('Ctrl Pts',(1.82493765431576,94.9078033833975,15.04099045924));
#43479=CARTESIAN_POINT('Ctrl Pts',(2.19572368194789,94.8381420569224,14.5314986521421));
#43480=CARTESIAN_POINT('Ctrl Pts',(2.32610993023979,94.80677869421,14.2628269382608));
#43481=CARTESIAN_POINT('Ctrl Pts',(2.4968400964955,94.7389319078162,13.6564681884161));
#43482=CARTESIAN_POINT('Ctrl Pts',(2.52209192413947,94.7024607771091,13.3204391869547));
#43483=CARTESIAN_POINT('Ctrl Pts',(2.4417562244427,94.6346841393199,12.6790173972034));
#43484=CARTESIAN_POINT('Ctrl Pts',(2.34501599305682,94.6034267524288,12.378746960768));
#43485=CARTESIAN_POINT('Ctrl Pts',(2.12961663849431,94.5565354597433,11.9833175548818));
#43486=CARTESIAN_POINT('Ctrl Pts',(2.05395544128919,94.54222843125,11.868149916199));
#43487=CARTESIAN_POINT('Ctrl Pts',(1.85605096969357,94.5093535416532,11.6151254287725));
#43488=CARTESIAN_POINT('Ctrl Pts',(1.72729025550136,94.4910953114638,11.4833471580103));
#43489=CARTESIAN_POINT('Ctrl Pts',(1.45461349282513,94.456731209407,11.2597487954932));
#43490=CARTESIAN_POINT('Ctrl Pts',(1.31350356515208,94.4406468431525,11.1661698056949));
#43491=CARTESIAN_POINT('Ctrl Pts',(1.16404056044746,94.424229722102,11.0875331474499));
#43492=CARTESIAN_POINT('Ctrl Pts',(1.16347235681021,94.4241522805232,11.0886093503689));
#43493=CARTESIAN_POINT('Ctrl Pts',(1.09886931445663,94.4095786870534,11.0546714886086));
#43494=CARTESIAN_POINT('Ctrl Pts',(1.03286394719834,94.3949382050941,11.0237518795221));
#43495=CARTESIAN_POINT('Ctrl Pts',(0.965698223793783,94.3804123520948,10.9957715840715));
#43496=CARTESIAN_POINT('Ctrl Pts',(0.954625997705913,94.3780177746172,10.9911590504527));
#43497=CARTESIAN_POINT('Ctrl Pts',(0.943522128381032,94.3756263044254,10.9866264249625));
#43498=CARTESIAN_POINT('Ctrl Pts',(0.932387570777659,94.3732387453768,10.9821733941901));
#43499=CARTESIAN_POINT('Ctrl Pts',(0.852355593053961,94.3560776618925,10.9501662977006));
#43500=CARTESIAN_POINT('Ctrl Pts',(0.770739886231872,94.3391183146964,10.9222676418242));
#43501=CARTESIAN_POINT('Ctrl Pts',(0.687895202432596,94.3223048946047,10.898563720722));
#43502=CARTESIAN_POINT('Ctrl Pts',(0.604906261470646,94.3054621973625,10.8748185240635));
#43503=CARTESIAN_POINT('Ctrl Pts',(0.520683550444595,94.2887658382801,10.8552826098449));
#43504=CARTESIAN_POINT('Ctrl Pts',(0.435566099291187,94.2721823223814,10.8400796637549));
#43505=CARTESIAN_POINT('Ctrl Pts',(0.362494535345656,94.2579457184182,10.8270282502984));
#43506=CARTESIAN_POINT('Ctrl Pts',(0.288763106090426,94.2437926396513,10.8171706621563));
#43507=CARTESIAN_POINT('Ctrl Pts',(0.214580045610659,94.2297157102005,10.8106081683442));
#43508=CARTESIAN_POINT('Ctrl Pts',(0.127661799560024,94.2132221601941,10.8029190753331));
#43509=CARTESIAN_POINT('Ctrl Pts',(0.040587175047819,94.1969195527311,10.799794064794));
#43510=CARTESIAN_POINT('Ctrl Pts',(-0.046315175775073,94.1808216686268,
10.8012845181134));
#43511=CARTESIAN_POINT('Ctrl Pts',(-0.0895357882538338,94.172815436298,
10.8020257904118));
#43512=CARTESIAN_POINT('Ctrl Pts',(-0.132714256012658,94.1648601554613,
10.8039093396504));
#43513=CARTESIAN_POINT('Ctrl Pts',(-0.175812361638747,94.1569592270527,
10.8069454866206));
#43514=CARTESIAN_POINT('Ctrl Pts',(-0.175818529435711,94.1569580963459,
10.8069459211255));
#43515=CARTESIAN_POINT('Ctrl Pts',(-0.175824697231117,94.1569569656401,
10.806946355654));
#43516=CARTESIAN_POINT('Ctrl Pts',(-0.175830865024881,94.1569558349355,
10.8069467902062));
#43517=CARTESIAN_POINT('Ctrl Pts',(-0.260944759189729,94.1413524153915,
10.8129434927071));
#43518=CARTESIAN_POINT('Ctrl Pts',(-0.345746873428532,94.1259600022047,
10.8234327177893));
#43519=CARTESIAN_POINT('Ctrl Pts',(-0.429909388036926,94.1106936244754,
10.8382787893713));
#43520=CARTESIAN_POINT('Ctrl Pts',(-0.51533239086428,94.0951986047032,10.8533472081399));
#43521=CARTESIAN_POINT('Ctrl Pts',(-0.600097272709715,94.0798330160529,
10.8729045032887));
#43522=CARTESIAN_POINT('Ctrl Pts',(-0.683848059130618,94.0645257074691,
10.8968512447243));
#43523=CARTESIAN_POINT('Ctrl Pts',(-0.712115171912877,94.0593592674078,
10.904933619468));
#43524=CARTESIAN_POINT('Ctrl Pts',(-0.740266604201373,94.0541996398609,
10.9135163387467));
#43525=CARTESIAN_POINT('Ctrl Pts',(-0.768288134706657,94.0490446490367,
10.9225964879163));
#43526=CARTESIAN_POINT('Ctrl Pts',(-0.851089486853107,94.0338120688441,
10.9494275929764));
#43527=CARTESIAN_POINT('Ctrl Pts',(-0.932321208706402,94.018697261967,10.9804584999919));
#43528=CARTESIAN_POINT('Ctrl Pts',(-1.01165869703274,94.0036631570407,11.0155028541458));
#43529=CARTESIAN_POINT('Ctrl Pts',(-1.09159427871556,93.9885157160553,11.0508113935651));
#43530=CARTESIAN_POINT('Ctrl Pts',(-1.16960731629625,93.9734501950163,11.0901942032906));
#43531=CARTESIAN_POINT('Ctrl Pts',(-1.24536692198904,93.9584541936714,11.1335007446988));
#43532=CARTESIAN_POINT('Ctrl Pts',(-1.32029170007773,93.9436234397001,11.176330072744));
#43533=CARTESIAN_POINT('Ctrl Pts',(-1.39301295184137,93.9288608246002,11.2229971636614));
#43534=CARTESIAN_POINT('Ctrl Pts',(-1.46320530897308,93.914178040055,11.2733945537142));
#43535=CARTESIAN_POINT('Ctrl Pts',(-1.52151896162447,93.9019800339911,11.3152631561969));
#43536=CARTESIAN_POINT('Ctrl Pts',(-1.57808737847907,93.8898376016107,11.3597069807771));
#43537=CARTESIAN_POINT('Ctrl Pts',(-1.63271644490332,93.8777688222159,11.4066848110243));
#43538=CARTESIAN_POINT('Ctrl Pts',(-1.64362384817868,93.8753591335187,11.4160645455329));
#43539=CARTESIAN_POINT('Ctrl Pts',(-1.65444449801962,93.8729545265953,11.4255372421034));
#43540=CARTESIAN_POINT('Ctrl Pts',(-1.66517723864454,93.8705551820243,11.4351021586842));
#43541=CARTESIAN_POINT('Ctrl Pts',(-1.66517859425571,93.8705548789724,11.435103366792));
#43542=CARTESIAN_POINT('Ctrl Pts',(-1.66517994986548,93.8705545759205,11.4351045749013));
#43543=CARTESIAN_POINT('Ctrl Pts',(-1.66518130547384,93.8705542728687,11.4351057830121));
#43544=CARTESIAN_POINT('Ctrl Pts',(-1.72884031212494,93.8563230407208,11.4918383411191));
#43545=CARTESIAN_POINT('Ctrl Pts',(-1.78940844538948,93.8422753331869,11.5518122614757));
#43546=CARTESIAN_POINT('Ctrl Pts',(-1.84671790514911,93.8283371097907,11.6146958222387));
#43547=CARTESIAN_POINT('Ctrl Pts',(-1.90503232073465,93.8141544712689,11.6786820840393));
#43548=CARTESIAN_POINT('Ctrl Pts',(-1.95997290070592,93.8000848809414,11.745681602123));
#43549=CARTESIAN_POINT('Ctrl Pts',(-2.01133759587612,93.7860740938722,11.8153752450508));
#43550=CARTESIAN_POINT('Ctrl Pts',(-2.06307838930044,93.7719607181954,11.8855791929135));
#43551=CARTESIAN_POINT('Ctrl Pts',(-2.11119079150021,93.7579068496475,11.9585172775703));
#43552=CARTESIAN_POINT('Ctrl Pts',(-2.15544179716195,93.7438844347746,12.0338854754219));
#43553=CARTESIAN_POINT('Ctrl Pts',(-2.16356185472066,93.741311322273,12.0477155363549));
#43554=CARTESIAN_POINT('Ctrl Pts',(-2.17155181739915,93.7387393459551,12.0616274759162));
#43555=CARTESIAN_POINT('Ctrl Pts',(-2.17941014585818,93.7361684369155,12.0756194824366));
#43556=CARTESIAN_POINT('Ctrl Pts',(-2.17941197753976,93.7361678376677,12.0756227438045));
#43557=CARTESIAN_POINT('Ctrl Pts',(-2.17941380921418,93.7361672384198,12.0756260051768));
#43558=CARTESIAN_POINT('Ctrl Pts',(-2.17941564088145,93.7361666391721,12.0756292665535));
#43559=CARTESIAN_POINT('Ctrl Pts',(-2.20057589852894,93.7292438549686,12.1133061804977));
#43560=CARTESIAN_POINT('Ctrl Pts',(-2.22078186132525,93.7223287096649,12.1515636262624));
#43561=CARTESIAN_POINT('Ctrl Pts',(-2.24000847350861,93.7154167765929,12.1903652844855));
#43562=CARTESIAN_POINT('Ctrl Pts',(-2.27868382590507,93.7015130558151,12.2684168825014));
#43563=CARTESIAN_POINT('Ctrl Pts',(-2.31319724593064,93.687694207725,12.3482620836716));
#43564=CARTESIAN_POINT('Ctrl Pts',(-2.34345309249078,93.6739428144898,12.4295605374583));
#43565=CARTESIAN_POINT('Ctrl Pts',(-2.37395208550431,93.6600809102998,12.5115123337541));
#43566=CARTESIAN_POINT('Ctrl Pts',(-2.4001251281991,93.64628764271,12.5949410687129));
#43567=CARTESIAN_POINT('Ctrl Pts',(-2.42184839166118,93.6325683170609,12.6795286142253));
#43568=CARTESIAN_POINT('Ctrl Pts',(-2.43619340691957,93.6235087235926,12.7353862266492));
#43569=CARTESIAN_POINT('Ctrl Pts',(-2.4485975138681,93.6144818559146,12.7917497827169));
#43570=CARTESIAN_POINT('Ctrl Pts',(-2.45901752505367,93.6054942738369,12.8485340711388));
#43571=CARTESIAN_POINT('Ctrl Pts',(-2.45901797260607,93.6054938878092,12.8485365100944));
#43572=CARTESIAN_POINT('Ctrl Pts',(-2.4590184201548,93.6054935017815,12.8485389490507));
#43573=CARTESIAN_POINT('Ctrl Pts',(-2.45901886769987,93.6054931157538,12.8485413880079));
#43574=CARTESIAN_POINT('Ctrl Pts',(-2.47477860185115,93.5918996400528,12.9344261810042));
#43575=CARTESIAN_POINT('Ctrl Pts',(-2.4860015256015,93.5783948820527,13.0212750778943));
#43576=CARTESIAN_POINT('Ctrl Pts',(-2.49264976786009,93.5649076679167,13.1087174910619));
#43577=CARTESIAN_POINT('Ctrl Pts',(-2.49364658064142,93.5628854450626,13.1218282821078));
#43578=CARTESIAN_POINT('Ctrl Pts',(-2.49454047246715,93.5608636596275,13.1349523938354));
#43579=CARTESIAN_POINT('Ctrl Pts',(-2.49533116854958,93.5588423848586,13.1480868187036));
#43580=CARTESIAN_POINT('Ctrl Pts',(-2.49838372369694,93.5510390672033,13.1987934772166));
#43581=CARTESIAN_POINT('Ctrl Pts',(-2.4998915056308,93.5432607996176,13.249540054876));
#43582=CARTESIAN_POINT('Ctrl Pts',(-2.49986749706851,93.5355013981268,13.3002300840465));
#43583=CARTESIAN_POINT('Origin',(0.,70.2,13.3));
#43584=CARTESIAN_POINT('',(-2.5,91.3980900981106,13.3));
#43585=CARTESIAN_POINT('',(-2.5,92.6061264662692,13.2999999996171));
#43586=CARTESIAN_POINT('',(-2.5,70.2,13.3));
#43587=CARTESIAN_POINT('',(-2.49999761486117,92.6065892681553,13.296546640986));
#43588=CARTESIAN_POINT('Ctrl Pts',(-2.5,92.6061264662692,13.2999999992341));
#43589=CARTESIAN_POINT('Ctrl Pts',(-2.49999999999965,92.6062811709464,13.2988456033981));
#43590=CARTESIAN_POINT('Ctrl Pts',(-2.49999920955526,92.6064345527048,13.2977010913065));
#43591=CARTESIAN_POINT('Ctrl Pts',(-2.49999761486117,92.6065892681553,13.2965466409861));
#43592=CARTESIAN_POINT('Ctrl Pts',(-2.49999761486117,92.6065892681554,13.296546640986));
#43593=CARTESIAN_POINT('Ctrl Pts',(-2.49974231312978,92.6313583587562,13.1117255097472));
#43594=CARTESIAN_POINT('Ctrl Pts',(-2.47899380873915,92.6561286709599,12.9275123025644));
#43595=CARTESIAN_POINT('Ctrl Pts',(-2.39276586348267,92.708439349742,12.5471553898367));
#43596=CARTESIAN_POINT('Ctrl Pts',(-2.32292262850757,92.735726442814,12.3533322714901));
#43597=CARTESIAN_POINT('Ctrl Pts',(-2.07920141723139,92.8061179400166,11.872248794433));
#43598=CARTESIAN_POINT('Ctrl Pts',(-1.87007179557902,92.8484792603454,11.6075450979363));
#43599=CARTESIAN_POINT('Ctrl Pts',(-1.38183916875315,92.9319131617122,11.1943129302899));
#43600=CARTESIAN_POINT('Ctrl Pts',(-1.11433355745884,92.9719818863433,11.0413153212106));
#43601=CARTESIAN_POINT('Ctrl Pts',(-0.551537143215495,93.049648231513,10.8443344521761));
#43602=CARTESIAN_POINT('Ctrl Pts',(-0.262503619937133,93.086277995738,10.7968748032867));
#43603=CARTESIAN_POINT('Ctrl Pts',(0.339914036160982,93.1628043721513,10.8036806691249));
#43604=CARTESIAN_POINT('Ctrl Pts',(0.648180826792544,93.202181931772,10.8654578372114));
#43605=CARTESIAN_POINT('Ctrl Pts',(1.15749934761066,93.2723831415024,11.0713900277499));
#43606=CARTESIAN_POINT('Ctrl Pts',(1.36406727805913,93.3026013245646,11.1914822077757));
#43607=CARTESIAN_POINT('Ctrl Pts',(1.81248982774957,93.3748889939285,11.5460405876667));
#43608=CARTESIAN_POINT('Ctrl Pts',(2.03031177981672,93.4163034018027,11.8035488170692));
#43609=CARTESIAN_POINT('Ctrl Pts',(2.34680804312831,93.4984737524834,12.379648598209));
#43610=CARTESIAN_POINT('Ctrl Pts',(2.44605820800887,93.5383907596061,12.6905942134514));
#43611=CARTESIAN_POINT('Ctrl Pts',(2.52108852552984,93.6191936511323,13.3371554665366));
#43612=CARTESIAN_POINT('Ctrl Pts',(2.49454822643192,93.6593295731743,13.6667888607161));
#43613=CARTESIAN_POINT('Ctrl Pts',(2.36211807527856,93.7188889609086,14.1338678288279));
#43614=CARTESIAN_POINT('Ctrl Pts',(2.30474237838344,93.7381450405329,14.2813787102134));
#43615=CARTESIAN_POINT('Ctrl Pts',(2.0864230926269,93.7974474462361,14.7158477760113));
#43616=CARTESIAN_POINT('Ctrl Pts',(1.88265177494184,93.837158538839,14.9773285460213));
#43617=CARTESIAN_POINT('Ctrl Pts',(1.51509361740658,93.8959651658159,15.2948053030737));
#43618=CARTESIAN_POINT('Ctrl Pts',(1.38656789723429,93.9148813552297,15.3861908873483));
#43619=CARTESIAN_POINT('Ctrl Pts',(1.11642368411619,93.9523260924595,15.5422084446643));
#43620=CARTESIAN_POINT('Ctrl Pts',(0.975663561710984,93.9707753732465,15.606942167965));
#43621=CARTESIAN_POINT('Ctrl Pts',(0.514260502639939,94.0293900601284,15.76930134143));
#43622=CARTESIAN_POINT('Ctrl Pts',(0.179556580620323,94.0692542741921,15.8158937237312));
#43623=CARTESIAN_POINT('Ctrl Pts',(-0.477623044706271,94.1469936864816,
15.7752256425953));
#43624=CARTESIAN_POINT('Ctrl Pts',(-0.793897270724776,94.1844054736309,
15.6926131546135));
#43625=CARTESIAN_POINT('Ctrl Pts',(-1.22976491031325,94.2414202920349,15.482495961809));
#43626=CARTESIAN_POINT('Ctrl Pts',(-1.36692753001275,94.26019774854,15.3993159874602));
#43627=CARTESIAN_POINT('Ctrl Pts',(-1.73569019541523,94.3138047017912,15.1241221320101));
#43628=CARTESIAN_POINT('Ctrl Pts',(-1.94192177052931,94.347720696045,14.9028112140539));
#43629=CARTESIAN_POINT('Ctrl Pts',(-2.2853474559415,94.4207917580665,14.3676691921534));
#43630=CARTESIAN_POINT('Ctrl Pts',(-2.40795052875896,94.4594073953375,14.0513863627676));
#43631=CARTESIAN_POINT('Ctrl Pts',(-2.48815000607631,94.5130391481474,13.5811380584742));
#43632=CARTESIAN_POINT('Ctrl Pts',(-2.5,94.5286845898386,13.4405334697025));
#43633=CARTESIAN_POINT('Ctrl Pts',(-2.5,94.5443074868315,13.3000000000001));
#43634=CARTESIAN_POINT('Ctrl Pts',(-2.49999998683747,93.5356742584249,13.3002565397127));
#43635=CARTESIAN_POINT('Ctrl Pts',(-2.4999789695336,93.5044243811101,13.5050718444085));
#43636=CARTESIAN_POINT('Ctrl Pts',(-2.47478881885302,93.473058246009,13.7091015875136));
#43637=CARTESIAN_POINT('Ctrl Pts',(-2.37018635660125,93.4074962166809,14.1264723750432));
#43638=CARTESIAN_POINT('Ctrl Pts',(-2.28604298265964,93.3743391483411,14.3367685729446));
#43639=CARTESIAN_POINT('Ctrl Pts',(-2.09910870413749,93.3182242719682,14.666488622868));
#43640=CARTESIAN_POINT('Ctrl Pts',(-2.0112932659589,93.295470102,14.7927312450222));
#43641=CARTESIAN_POINT('Ctrl Pts',(-1.70571042301175,93.225223893868,15.1556957769451));
#43642=CARTESIAN_POINT('Ctrl Pts',(-1.45356321019058,93.1798227443927,15.3591995454538));
#43643=CARTESIAN_POINT('Ctrl Pts',(-1.02913288799724,93.1107249653846,15.5838978624607));
#43644=CARTESIAN_POINT('Ctrl Pts',(-0.881759653757164,93.0877777099911,
15.644740430157));
#43645=CARTESIAN_POINT('Ctrl Pts',(-0.407882395044307,93.0169384538345,
15.789331411237));
#43646=CARTESIAN_POINT('Ctrl Pts',(-0.0695863349327156,92.9706330455138,
15.8215770818348));
#43647=CARTESIAN_POINT('Ctrl Pts',(0.586698011167412,92.8775518437506,15.7516272646382));
#43648=CARTESIAN_POINT('Ctrl Pts',(0.898782601217875,92.8334217271977,15.6551959751661));
#43649=CARTESIAN_POINT('Ctrl Pts',(1.44938353103509,92.7469448940478,15.3591678880462));
#43650=CARTESIAN_POINT('Ctrl Pts',(1.68695879439215,92.7054565987242,15.1695231302102));
#43651=CARTESIAN_POINT('Ctrl Pts',(2.0931268316993,92.6213899195092,14.7032713845275));
#43652=CARTESIAN_POINT('Ctrl Pts',(2.25393486896684,92.5783071985329,14.4269993422804));
#43653=CARTESIAN_POINT('Ctrl Pts',(2.41344537190869,92.5131072267778,13.972630544522));
#43654=CARTESIAN_POINT('Ctrl Pts',(2.45252514690124,92.491087068295,13.8121318364526));
#43655=CARTESIAN_POINT('Ctrl Pts',(2.4983191341392,92.4469569051383,13.4872558846521));
#43656=CARTESIAN_POINT('Ctrl Pts',(2.50521404251146,92.4249607365414,13.3237244353476));
#43657=CARTESIAN_POINT('Ctrl Pts',(2.47773093742526,92.358445213497,12.8312603077648));
#43658=CARTESIAN_POINT('Ctrl Pts',(2.3943083060055,92.3152377297702,12.5086723216436));
#43659=CARTESIAN_POINT('Ctrl Pts',(2.18178654562703,92.2502850745213,12.0692238051173));
#43660=CARTESIAN_POINT('Ctrl Pts',(2.09959281497549,92.2292337984681,11.9337219735002));
#43661=CARTESIAN_POINT('Ctrl Pts',(1.80543284066672,92.1639854018535,11.5386840176256));
#43662=CARTESIAN_POINT('Ctrl Pts',(1.55390552563549,92.120684412765,11.3132384200328));
#43663=CARTESIAN_POINT('Ctrl Pts',(0.977159926933571,92.0325181691515,10.9747194087218));
#43664=CARTESIAN_POINT('Ctrl Pts',(0.657777013696649,91.9894311947502,10.8650191560993));
#43665=CARTESIAN_POINT('Ctrl Pts',(0.168672586084107,91.924970656387,10.8006368228099));
#43666=CARTESIAN_POINT('Ctrl Pts',(0.00945374552732607,91.9042037078517,
10.7949691397534));
#43667=CARTESIAN_POINT('Ctrl Pts',(-0.482974831005797,91.8399479630952,
10.8244147096595));
#43668=CARTESIAN_POINT('Ctrl Pts',(-0.809373468747169,91.797310972374,10.9111249870723));
#43669=CARTESIAN_POINT('Ctrl Pts',(-1.40949449292844,91.7106124885981,11.2081802334211));
#43670=CARTESIAN_POINT('Ctrl Pts',(-1.67699636792964,91.6680289632479,11.4158307318775));
#43671=CARTESIAN_POINT('Ctrl Pts',(-2.0000838690445,91.6043552699173,11.7915732168463));
#43672=CARTESIAN_POINT('Ctrl Pts',(-2.09265142535013,91.5837847170907,11.9228658205572));
#43673=CARTESIAN_POINT('Ctrl Pts',(-2.33749113353084,91.5203917769293,12.3524654527532));
#43674=CARTESIAN_POINT('Ctrl Pts',(-2.44308933652245,91.4783101504844,12.6730853904379));
#43675=CARTESIAN_POINT('Ctrl Pts',(-2.49419079729861,91.423136710787,13.1030884670158));
#43676=CARTESIAN_POINT('Ctrl Pts',(-2.5,91.4105921947178,13.2016002889944));
#43677=CARTESIAN_POINT('Ctrl Pts',(-2.5,91.3980900981106,13.3));
#43678=CARTESIAN_POINT('Origin',(0.,70.2,13.3));
#43679=CARTESIAN_POINT('',(-2.5,90.4307847167281,13.2999999999841));
#43680=CARTESIAN_POINT('',(0.400974295891035,90.9332096597013,10.8309447386746));
#43681=CARTESIAN_POINT('Ctrl Pts',(-2.49999999944397,90.430791038424,13.2999472726946));
#43682=CARTESIAN_POINT('Ctrl Pts',(-2.49999398616684,90.4649743170265,13.0148351718446));
#43683=CARTESIAN_POINT('Ctrl Pts',(-2.45121672545614,90.4988744454463,12.7317974299723));
#43684=CARTESIAN_POINT('Ctrl Pts',(-2.26557142946895,90.5645414565702,12.209239581071));
#43685=CARTESIAN_POINT('Ctrl Pts',(-2.13494258436756,90.5959008943449,11.9716138177145));
#43686=CARTESIAN_POINT('Ctrl Pts',(-1.86512631626832,90.6472524747142,11.6267783216932));
#43687=CARTESIAN_POINT('Ctrl Pts',(-1.7481912546364,90.6669116085519,11.5049506339109));
#43688=CARTESIAN_POINT('Ctrl Pts',(-1.37991318202436,90.7230418962365,11.1916588423971));
#43689=CARTESIAN_POINT('Ctrl Pts',(-1.1034811920457,90.7587209515757,11.0346917762158));
#43690=CARTESIAN_POINT('Ctrl Pts',(-0.604712400799047,90.8190948670444,
10.8650145562887));
#43691=CARTESIAN_POINT('Ctrl Pts',(-0.396384515693903,90.8431506187802,
10.8225555507897));
#43692=CARTESIAN_POINT('Ctrl Pts',(0.0104683070707311,90.8890917529299,
10.79233544841));
#43693=CARTESIAN_POINT('Ctrl Pts',(0.207159199743011,90.9108543330795,10.8008836601677));
#43694=CARTESIAN_POINT('Ctrl Pts',(0.400828488760919,90.9327222859085,10.8323418951164));
#43695=CARTESIAN_POINT('Ctrl Pts',(0.400506739468218,90.9349782296111,10.8322896540233));
#43696=CARTESIAN_POINT('Ctrl Pts',(0.621120297389946,90.9723564264929,10.868094997592));
#43697=CARTESIAN_POINT('Ctrl Pts',(0.835904576484284,91.0101623910831,10.9333148711372));
#43698=CARTESIAN_POINT('Ctrl Pts',(1.27168608214601,91.090069164932,11.1324708489373));
#43699=CARTESIAN_POINT('Ctrl Pts',(1.48652387690573,91.1303415091947,11.2737468407469));
#43700=CARTESIAN_POINT('Ctrl Pts',(1.90760374097452,91.2207085299562,11.654329613527));
#43701=CARTESIAN_POINT('Ctrl Pts',(2.09775190589845,91.2708175203025,11.904784414362));
#43702=CARTESIAN_POINT('Ctrl Pts',(2.38675839750348,91.3723506393853,12.483941804229));
#43703=CARTESIAN_POINT('Ctrl Pts',(2.4746364372273,91.4213334522488,12.8112648400754));
#43704=CARTESIAN_POINT('Ctrl Pts',(2.51293821602994,91.5162567229141,13.4331618947545));
#43705=CARTESIAN_POINT('Ctrl Pts',(2.48102245615064,91.5605504977297,13.7210305117836));
#43706=CARTESIAN_POINT('Ctrl Pts',(2.35523589392042,91.6271019915223,14.1541369467785));
#43707=CARTESIAN_POINT('Ctrl Pts',(2.29439915178092,91.6506768742613,14.3062005804627));
#43708=CARTESIAN_POINT('Ctrl Pts',(2.070561381475,91.7213524525443,14.7376635081236));
#43709=CARTESIAN_POINT('Ctrl Pts',(1.8679142149634,91.7687807293572,14.9926178470517));
#43710=CARTESIAN_POINT('Ctrl Pts',(1.36693704679103,91.8645588470098,15.4199816748156));
#43711=CARTESIAN_POINT('Ctrl Pts',(1.0700285034486,91.9109157335291,15.5842830755364));
#43712=CARTESIAN_POINT('Ctrl Pts',(0.432339885058854,92.0063423998576,15.7846688280913));
#43713=CARTESIAN_POINT('Ctrl Pts',(0.0983981470253122,92.0538541595564,
15.8201114951091));
#43714=CARTESIAN_POINT('Ctrl Pts',(-0.394684796713186,92.1225632368531,
15.7739974665974));
#43715=CARTESIAN_POINT('Ctrl Pts',(-0.554718205591719,92.1449255734657,
15.7430981435197));
#43716=CARTESIAN_POINT('Ctrl Pts',(-1.005229486078,92.2101441446002,15.6095322692099));
#43717=CARTESIAN_POINT('Ctrl Pts',(-1.281214846687,92.2532119422054,15.4686190485525));
#43718=CARTESIAN_POINT('Ctrl Pts',(-1.79048026572708,92.3419207642284,15.0766916589386));
#43719=CARTESIAN_POINT('Ctrl Pts',(-2.01242440125496,92.386502596009,14.8207462284203));
#43720=CARTESIAN_POINT('Ctrl Pts',(-2.27816469537492,92.4603043242833,14.3498147510431));
#43721=CARTESIAN_POINT('Ctrl Pts',(-2.35665279172611,92.4883709713848,14.1592674280451));
#43722=CARTESIAN_POINT('Ctrl Pts',(-2.47004890104903,92.5465142950431,13.7458294206398));
#43723=CARTESIAN_POINT('Ctrl Pts',(-2.50000000006845,92.576184132504,13.5234276683856));
#43724=CARTESIAN_POINT('Ctrl Pts',(-2.5,92.6061264662693,13.2999999992341));
#43725=CARTESIAN_POINT('',(-2.5,89.5119815300394,13.3));
#43726=CARTESIAN_POINT('Ctrl Pts',(-2.5,91.3980900981106,13.3));
#43727=CARTESIAN_POINT('Ctrl Pts',(-2.5,91.368530213291,13.5326557068775));
#43728=CARTESIAN_POINT('Ctrl Pts',(-2.46751960634584,91.3392038081443,13.7646842113909));
#43729=CARTESIAN_POINT('Ctrl Pts',(-2.35870962296507,91.2892893951694,14.1440491200089));
#43730=CARTESIAN_POINT('Ctrl Pts',(-2.29946141539159,91.2689712778199,14.294187482627));
#43731=CARTESIAN_POINT('Ctrl Pts',(-2.15320190902688,91.228398632862,14.5804091252095));
#43732=CARTESIAN_POINT('Ctrl Pts',(-2.06663970281822,91.2082547569972,14.7158846723123));
#43733=CARTESIAN_POINT('Ctrl Pts',(-1.7693061928053,91.1476526070444,15.0952690068056));
#43734=CARTESIAN_POINT('Ctrl Pts',(-1.52391373605851,91.1076480466686,15.3077696040993));
#43735=CARTESIAN_POINT('Ctrl Pts',(-1.09880992681705,91.0463439344429,15.5518957636767));
#43736=CARTESIAN_POINT('Ctrl Pts',(-0.944503984613686,91.0253561873975,
15.6208474375327));
#43737=CARTESIAN_POINT('Ctrl Pts',(-0.510700700564446,90.9684073479455,
15.7642031784739));
#43738=CARTESIAN_POINT('Ctrl Pts',(-0.223365419072312,90.9328095634411,
15.8066368307339));
#43739=CARTESIAN_POINT('Ctrl Pts',(0.222638075959661,90.8773771355885,15.795064762925));
#43740=CARTESIAN_POINT('Ctrl Pts',(0.379695990862955,90.8578382908325,15.7760351590646));
#43741=CARTESIAN_POINT('Ctrl Pts',(0.815486743500037,90.8026557974328,15.680767658675));
#43742=CARTESIAN_POINT('Ctrl Pts',(1.08431846596642,90.7674865422745,15.5709778776648));
#43743=CARTESIAN_POINT('Ctrl Pts',(1.61292582457286,90.6907519849497,15.2393819932704));
#43744=CARTESIAN_POINT('Ctrl Pts',(1.8585328820173,90.6497316053036,15.0054664287502));
#43745=CARTESIAN_POINT('Ctrl Pts',(2.23051708143503,90.5704271973385,14.4720539524885));
#43746=CARTESIAN_POINT('Ctrl Pts',(2.36013642592417,90.5327665798079,14.1824274811899));
#43747=CARTESIAN_POINT('Ctrl Pts',(2.46991719189685,90.4748120053061,13.7190918867424));
#43748=CARTESIAN_POINT('Ctrl Pts',(2.4918439325536,90.4551884526585,13.5585498160198));
#43749=CARTESIAN_POINT('Ctrl Pts',(2.50939685205833,90.4004998753436,13.1065462481498));
#43750=CARTESIAN_POINT('Ctrl Pts',(2.46993224947177,90.3661374484165,12.8163155338604));
#43751=CARTESIAN_POINT('Ctrl Pts',(2.27992584186872,90.2914072336011,12.2214092042317));
#43752=CARTESIAN_POINT('Ctrl Pts',(2.1157069097961,90.2511386130339,11.9269655469924));
#43753=CARTESIAN_POINT('Ctrl Pts',(1.71056651076189,90.1770821018749,11.4540824290684));
#43754=CARTESIAN_POINT('Ctrl Pts',(1.48600950333078,90.1437499762508,11.2689315344893));
#43755=CARTESIAN_POINT('Ctrl Pts',(0.944518588190801,90.0705024688197,10.9613368573605));
#43756=CARTESIAN_POINT('Ctrl Pts',(0.624138639742351,90.0303394185647,10.8562509154152));
#43757=CARTESIAN_POINT('Ctrl Pts',(0.0186310933730435,89.9586948956865,
10.7848971646399));
#43758=CARTESIAN_POINT('Ctrl Pts',(-0.258796694907511,89.9274633674728,
10.7981706303626));
#43759=CARTESIAN_POINT('Ctrl Pts',(-0.854485046668086,89.8576522359491,
10.9270035879568));
#43760=CARTESIAN_POINT('Ctrl Pts',(-1.16308185270574,89.8183984118701,11.0620356140602));
#43761=CARTESIAN_POINT('Ctrl Pts',(-1.6640759599315,89.748234413936,11.4136213894974));
#43762=CARTESIAN_POINT('Ctrl Pts',(-1.86374161376017,89.7176791650614,11.610597051237));
#43763=CARTESIAN_POINT('Ctrl Pts',(-2.22196856512738,89.6497716042869,12.1067014844785));
#43764=CARTESIAN_POINT('Ctrl Pts',(-2.36107557540821,89.6112869974941,12.4132200524645));
#43765=CARTESIAN_POINT('Ctrl Pts',(-2.46887032142857,89.5576028964703,12.8804083992387));
#43766=CARTESIAN_POINT('Ctrl Pts',(-2.48918706775228,89.5415776841612,13.0255115769856));
#43767=CARTESIAN_POINT('Ctrl Pts',(-2.49890211709861,89.5211630832979,13.2144071673686));
#43768=CARTESIAN_POINT('Ctrl Pts',(-2.5,89.516563021389,13.2572235679475));
#43769=CARTESIAN_POINT('Ctrl Pts',(-2.5,89.5119815300394,13.3));
#43770=CARTESIAN_POINT('',(-2.5,70.2,13.3));
#43771=CARTESIAN_POINT('Origin',(0.,70.2,13.3));
#43772=CARTESIAN_POINT('',(-2.5,87.6157001716672,13.3000000000001));
#43773=CARTESIAN_POINT('',(-2.5,88.464609916907,13.2999999999998));
#43774=CARTESIAN_POINT('',(-2.5,70.2,13.3));
#43775=CARTESIAN_POINT('',(-1.18108807079192,88.7245239333106,11.0963559860755));
#43776=CARTESIAN_POINT('Ctrl Pts',(-2.5,88.464609916907,13.2999999999997));
#43777=CARTESIAN_POINT('Ctrl Pts',(-2.49999999999999,88.4763169599804,13.1863620604698));
#43778=CARTESIAN_POINT('Ctrl Pts',(-2.49225149769818,88.4878609695849,13.0725943974306));
#43779=CARTESIAN_POINT('Ctrl Pts',(-2.43361199552928,88.5308384828477,12.6460598539817));
#43780=CARTESIAN_POINT('Ctrl Pts',(-2.33139820322754,88.5609011878374,12.3436028049079));
#43781=CARTESIAN_POINT('Ctrl Pts',(-2.05119861166652,88.6173290833032,11.8487106482045));
#43782=CARTESIAN_POINT('Ctrl Pts',(-1.89432399303536,88.6418420705692,11.6491554750665));
#43783=CARTESIAN_POINT('Ctrl Pts',(-1.55107956884997,88.6853869978468,11.3272581236237));
#43784=CARTESIAN_POINT('Ctrl Pts',(-1.3731860005449,88.7045813073607,11.1995430462422));
#43785=CARTESIAN_POINT('Ctrl Pts',(-1.1809717498647,88.7243316451192,11.096524171673));
#43786=CARTESIAN_POINT('Ctrl Pts',(-1.18100228905586,88.7246337621387,11.0965405396866));
#43787=CARTESIAN_POINT('Ctrl Pts',(-0.912279497684443,88.768490042615,10.9525114629338));
#43788=CARTESIAN_POINT('Ctrl Pts',(-0.619420463177039,88.8119324096701,
10.8588259010574));
#43789=CARTESIAN_POINT('Ctrl Pts',(0.0110562175630186,88.9019754116573,
10.7782565527367));
#43790=CARTESIAN_POINT('Ctrl Pts',(0.344128588636148,88.9474058964649,10.8018106969851));
#43791=CARTESIAN_POINT('Ctrl Pts',(0.985082241119456,89.0399859110188,10.9781053204488));
#43792=CARTESIAN_POINT('Ctrl Pts',(1.28619087413887,89.0858470553435,11.1303608395587));
#43793=CARTESIAN_POINT('Ctrl Pts',(1.76740341983592,89.1703846349364,11.5100161694327));
#43794=CARTESIAN_POINT('Ctrl Pts',(1.95593217319766,89.2087799324138,11.7181829468283));
#43795=CARTESIAN_POINT('Ctrl Pts',(2.28641800458696,89.2915244201812,12.2350168643086));
#43796=CARTESIAN_POINT('Ctrl Pts',(2.40826581514484,89.3349110408818,12.5501922024444));
#43797=CARTESIAN_POINT('Ctrl Pts',(2.51969689321026,89.4234811092858,13.2041022431543));
#43798=CARTESIAN_POINT('Ctrl Pts',(2.5104565071361,89.4676960780469,13.535874451767));
#43799=CARTESIAN_POINT('Ctrl Pts',(2.37940547667574,89.5470239663889,14.1100374774523));
#43800=CARTESIAN_POINT('Ctrl Pts',(2.28221157497402,89.5812808781357,14.3532486116256));
#43801=CARTESIAN_POINT('Ctrl Pts',(2.06661474240068,89.6359562540811,14.716058017857));
#43802=CARTESIAN_POINT('Ctrl Pts',(1.97077728174789,89.6567147310476,14.8466599521433));
#43803=CARTESIAN_POINT('Ctrl Pts',(1.76006132626174,89.6975160446304,15.0821379882182));
#43804=CARTESIAN_POINT('Ctrl Pts',(1.64668519347369,89.7174882555832,15.1873941516935));
#43805=CARTESIAN_POINT('Ctrl Pts',(1.25926540288717,89.7807712394764,15.4854270935864));
#43806=CARTESIAN_POINT('Ctrl Pts',(0.955928569384893,89.8230556129854,15.6341153718328));
#43807=CARTESIAN_POINT('Ctrl Pts',(0.47588115623038,89.8862569233562,15.7596088273576));
#43808=CARTESIAN_POINT('Ctrl Pts',(0.315858414766504,89.9067645785581,15.7852316710863));
#43809=CARTESIAN_POINT('Ctrl Pts',(-0.178758489715751,89.9695384933718,
15.8158534419732));
#43810=CARTESIAN_POINT('Ctrl Pts',(-0.5128089107048,90.0110951020614,15.7695224754184));
#43811=CARTESIAN_POINT('Ctrl Pts',(-0.980914054595601,90.0731649428838,
15.6052339635061));
#43812=CARTESIAN_POINT('Ctrl Pts',(-1.12834413828788,90.093352382921,15.536770055282));
#43813=CARTESIAN_POINT('Ctrl Pts',(-1.41087701492271,90.1341263072552,15.3704759451092));
#43814=CARTESIAN_POINT('Ctrl Pts',(-1.54494897055453,90.1546113378598,15.2724561154334));
#43815=CARTESIAN_POINT('Ctrl Pts',(-1.9010443501359,90.2136559253285,14.9533779167191));
#43816=CARTESIAN_POINT('Ctrl Pts',(-2.09262623372159,90.2516155141937,14.7030592156736));
#43817=CARTESIAN_POINT('Ctrl Pts',(-2.32357225104417,90.3143298066315,14.2441900446282));
#43818=CARTESIAN_POINT('Ctrl Pts',(-2.39200606433039,90.3387228604655,14.0541889532507));
#43819=CARTESIAN_POINT('Ctrl Pts',(-2.47883854408009,90.3857630654534,13.6749938333432));
#43820=CARTESIAN_POINT('Ctrl Pts',(-2.5000000000012,90.4082684462306,13.4878011326208));
#43821=CARTESIAN_POINT('Ctrl Pts',(-2.5,90.4307847167281,13.2999999999841));
#43822=CARTESIAN_POINT('',(2.49380022861477,88.7482468790765,13.1242986243742));
#43823=CARTESIAN_POINT('Ctrl Pts',(-2.5,89.5119815300394,13.3));
#43824=CARTESIAN_POINT('Ctrl Pts',(-2.5,89.4810423796734,13.5888724134592));
#43825=CARTESIAN_POINT('Ctrl Pts',(-2.44993209699204,89.4503589471884,13.8758588946447));
#43826=CARTESIAN_POINT('Ctrl Pts',(-2.25550598041351,89.386723099465,14.4149652188788));
#43827=CARTESIAN_POINT('Ctrl Pts',(-2.1145205937211,89.3558894266671,14.6636012356151));
#43828=CARTESIAN_POINT('Ctrl Pts',(-1.72695518427293,89.2925059282761,15.1371816758764));
#43829=CARTESIAN_POINT('Ctrl Pts',(-1.4712854181974,89.2600761614001,15.347657900266));
#43830=CARTESIAN_POINT('Ctrl Pts',(-1.0437449082664,89.2082805972365,15.5771293245674));
#43831=CARTESIAN_POINT('Ctrl Pts',(-0.898470128396195,89.1915201595237,
15.6382673932665));
#43832=CARTESIAN_POINT('Ctrl Pts',(-0.489441669287295,89.1472260303795,
15.7665965143056));
#43833=CARTESIAN_POINT('Ctrl Pts',(-0.218986886119816,89.1213352670832,
15.8051510850134));
#43834=CARTESIAN_POINT('Ctrl Pts',(0.386695141988435,89.0641691849577,15.7924291495129));
#43835=CARTESIAN_POINT('Ctrl Pts',(0.716050772460616,89.0303875130934,15.7184560611734));
#43836=CARTESIAN_POINT('Ctrl Pts',(1.26825396004202,88.9727120554833,15.4713748099971));
#43837=CARTESIAN_POINT('Ctrl Pts',(1.49584007436802,88.9494664761161,15.321362199537));
#43838=CARTESIAN_POINT('Ctrl Pts',(1.80937824712612,88.9140270927264,15.0321509241068));
#43839=CARTESIAN_POINT('Ctrl Pts',(1.91357251849696,88.9011856658873,14.9163063922395));
#43840=CARTESIAN_POINT('Ctrl Pts',(2.19258967471724,88.8598586562317,14.5409534548794));
#43841=CARTESIAN_POINT('Ctrl Pts',(2.33049526736143,88.8312407626482,14.2574036472055));
#43842=CARTESIAN_POINT('Ctrl Pts',(2.48608381650137,88.7854658454611,13.6848348898527));
#43843=CARTESIAN_POINT('Ctrl Pts',(2.513521888597,88.7677049407441,13.4039429441296));
#43844=CARTESIAN_POINT('Ctrl Pts',(2.49381725504168,88.7482160582468,13.1242857477141));
#43845=CARTESIAN_POINT('Ctrl Pts',(2.49381566113763,88.7484607548506,13.12426312776));
#43846=CARTESIAN_POINT('Ctrl Pts',(2.47565534574513,88.7070000631215,12.8665569425994));
#43847=CARTESIAN_POINT('Ctrl Pts',(2.41765147496816,88.6651844459182,12.6132136321295));
#43848=CARTESIAN_POINT('Ctrl Pts',(2.21301696079434,88.5761995865008,12.1004754446969));
#43849=CARTESIAN_POINT('Ctrl Pts',(2.05689746380474,88.5315830003039,11.8489259991677));
#43850=CARTESIAN_POINT('Ctrl Pts',(1.65040665773457,88.4384387277635,11.3960303305365));
#43851=CARTESIAN_POINT('Ctrl Pts',(1.39802601746336,88.3896655340998,11.2037090144886));
#43852=CARTESIAN_POINT('Ctrl Pts',(0.819588758961109,88.2914320737367,10.9149417394812));
#43853=CARTESIAN_POINT('Ctrl Pts',(0.495955679782436,88.2444147965749,10.8272734506959));
#43854=CARTESIAN_POINT('Ctrl Pts',(0.00453787822132061,88.1721718799112,
10.7948703357809));
#43855=CARTESIAN_POINT('Ctrl Pts',(-0.156050830368948,88.148541850119,10.799732329503));
#43856=CARTESIAN_POINT('Ctrl Pts',(-0.635349229729586,88.0774445711616,
10.8606198763144));
#43857=CARTESIAN_POINT('Ctrl Pts',(-0.944788939378858,88.0320309903952,
10.962969055852));
#43858=CARTESIAN_POINT('Ctrl Pts',(-1.48429869501355,87.9435592292897,11.2666467041139));
#43859=CARTESIAN_POINT('Ctrl Pts',(-1.71448532938947,87.9008458484831,11.4565718891768));
#43860=CARTESIAN_POINT('Ctrl Pts',(-2.1228309313702,87.8120499511084,11.93772816208));
#43861=CARTESIAN_POINT('Ctrl Pts',(-2.28605336365111,87.768145174016,12.2340625425692));
#43862=CARTESIAN_POINT('Ctrl Pts',(-2.46172645703544,87.6871063806446,12.7958318505116));
#43863=CARTESIAN_POINT('Ctrl Pts',(-2.5,87.6515555495105,13.0474641705025));
#43864=CARTESIAN_POINT('Ctrl Pts',(-2.5,87.6157001716673,13.3000000000002));
#43865=CARTESIAN_POINT('Origin',(0.,70.2,13.3));
#43866=CARTESIAN_POINT('',(-2.49999998851479,85.6233212596494,13.299784549362));
#43867=CARTESIAN_POINT('',(-2.5,86.6193069507268,13.3));
#43868=CARTESIAN_POINT('',(-2.5,70.2,13.3));
#43869=CARTESIAN_POINT('Ctrl Pts',(-2.5,86.6193069507268,13.3));
#43870=CARTESIAN_POINT('Ctrl Pts',(-2.5,86.6466224285355,13.0882700909667));
#43871=CARTESIAN_POINT('Ctrl Pts',(-2.47310162020712,86.6739408747903,12.8769977869022));
#43872=CARTESIAN_POINT('Ctrl Pts',(-2.33717304474614,86.7432060272066,12.3538430071535));
#43873=CARTESIAN_POINT('Ctrl Pts',(-2.19299741241983,86.7842030767294,12.0556505314509));
#43874=CARTESIAN_POINT('Ctrl Pts',(-1.89845883436738,86.8458435419989,11.665464747059));
#43875=CARTESIAN_POINT('Ctrl Pts',(-1.78943257350458,86.8660433988868,11.5467786512888));
#43876=CARTESIAN_POINT('Ctrl Pts',(-1.42031476505742,86.9283745224802,11.215522845001));
#43877=CARTESIAN_POINT('Ctrl Pts',(-1.12835965609482,86.9698982400417,11.0440809091017));
#43878=CARTESIAN_POINT('Ctrl Pts',(-0.660044278587822,87.0316091782384,
10.8834095432661));
#43879=CARTESIAN_POINT('Ctrl Pts',(-0.504163353457166,87.0514528251636,
10.8461478125476));
#43880=CARTESIAN_POINT('Ctrl Pts',(-0.0148979909304198,87.1127595257338,
10.7778177517056));
#43881=CARTESIAN_POINT('Ctrl Pts',(0.321954960890778,87.1535939154995,10.7983984756532));
#43882=CARTESIAN_POINT('Ctrl Pts',(0.796401612334706,87.2137847940213,10.925055463053));
#43883=CARTESIAN_POINT('Ctrl Pts',(0.943848795692934,87.2329188398661,10.9797050512545));
#43884=CARTESIAN_POINT('Ctrl Pts',(1.38639000358212,87.2929515301836,11.1929405664258));
#43885=CARTESIAN_POINT('Ctrl Pts',(1.65545708382981,87.3334111575162,11.3970342209617));
#43886=CARTESIAN_POINT('Ctrl Pts',(2.09063920004624,87.4129023369536,11.8913397762962));
#43887=CARTESIAN_POINT('Ctrl Pts',(2.2555061197234,87.4513297701916,12.1740337493058));
#43888=CARTESIAN_POINT('Ctrl Pts',(2.4142692291858,87.5095085883815,12.631487104091));
#43889=CARTESIAN_POINT('Ctrl Pts',(2.45210320271859,87.5286452993377,12.7873574458279));
#43890=CARTESIAN_POINT('Ctrl Pts',(2.51725670542116,87.5833614208896,13.2425587142243));
#43891=CARTESIAN_POINT('Ctrl Pts',(2.50600923919744,87.6181536114473,13.5445853195605));
#43892=CARTESIAN_POINT('Ctrl Pts',(2.36975068982988,87.6926827888213,14.1636264460045));
#43893=CARTESIAN_POINT('Ctrl Pts',(2.23328414475215,87.7318659425395,14.4722059293934));
#43894=CARTESIAN_POINT('Ctrl Pts',(1.85248841510107,87.8080604517333,15.0099025973434));
#43895=CARTESIAN_POINT('Ctrl Pts',(1.61491793120646,87.8447442584537,15.2358519541843));
#43896=CARTESIAN_POINT('Ctrl Pts',(1.08764544573736,87.9168828566478,15.5709007560183));
#43897=CARTESIAN_POINT('Ctrl Pts',(0.807547217265582,87.9508570739586,15.6849329705292));
#43898=CARTESIAN_POINT('Ctrl Pts',(0.360424704205339,88.0019452544041,15.7788475805645));
#43899=CARTESIAN_POINT('Ctrl Pts',(0.204268234737293,88.0193065650425,15.7965704328218));
#43900=CARTESIAN_POINT('Ctrl Pts',(-0.287258966713611,88.0743739751298,
15.8059084464013));
#43901=CARTESIAN_POINT('Ctrl Pts',(-0.619978172706541,88.1120388035939,
15.7449568493119));
#43902=CARTESIAN_POINT('Ctrl Pts',(-1.23105190151795,88.1839341142793,15.4998057128026));
#43903=CARTESIAN_POINT('Ctrl Pts',(-1.50506596143497,88.2181948120678,15.322228590379));
#43904=CARTESIAN_POINT('Ctrl Pts',(-1.95150383951295,88.2859948112912,14.8906373921834));
#43905=CARTESIAN_POINT('Ctrl Pts',(-2.12682915700285,88.3176526285759,14.6472925207583));
#43906=CARTESIAN_POINT('Ctrl Pts',(-2.32365163721931,88.3649981698067,14.2358180576044));
#43907=CARTESIAN_POINT('Ctrl Pts',(-2.37828215497575,88.3812051966122,14.0866910105076));
#43908=CARTESIAN_POINT('Ctrl Pts',(-2.47269020647712,88.4200082290749,13.7262271340283));
#43909=CARTESIAN_POINT('Ctrl Pts',(-2.50000000000002,88.4426309223165,13.5133457306453));
#43910=CARTESIAN_POINT('Ctrl Pts',(-2.5,88.464609916907,13.2999999999997));
#43911=CARTESIAN_POINT('Ctrl Pts',(-2.5,87.6157001716673,13.3000000000002));
#43912=CARTESIAN_POINT('Ctrl Pts',(-2.5,87.6048906897737,13.3761331114224));
#43913=CARTESIAN_POINT('Ctrl Pts',(-2.4965224112813,87.5940677933037,13.452350368579));
#43914=CARTESIAN_POINT('Ctrl Pts',(-2.46510757798474,87.5454743782036,13.7947448174624));
#43915=CARTESIAN_POINT('Ctrl Pts',(-2.39809759648182,87.5092925209849,14.0554947378149));
#43916=CARTESIAN_POINT('Ctrl Pts',(-2.16102875337192,87.4299927646321,14.5981855066975));
#43917=CARTESIAN_POINT('Ctrl Pts',(-1.97446098492741,87.3867291938527,14.8674059211297));
#43918=CARTESIAN_POINT('Ctrl Pts',(-1.50179762651519,87.2964549886563,15.3264396930274));
#43919=CARTESIAN_POINT('Ctrl Pts',(-1.21741653480531,87.2508484855315,15.5090665624559));
#43920=CARTESIAN_POINT('Ctrl Pts',(-0.594089858313682,87.163389292783,15.751238717163));
#43921=CARTESIAN_POINT('Ctrl Pts',(-0.261716373756765,87.121006090775,15.8085929817085));
#43922=CARTESIAN_POINT('Ctrl Pts',(0.369495063987766,87.0383197382512,15.7903782250777));
#43923=CARTESIAN_POINT('Ctrl Pts',(0.662968954884288,86.999087228789,15.7287824581235));
#43924=CARTESIAN_POINT('Ctrl Pts',(1.24884474031079,86.9165904250011,15.4914280926614));
#43925=CARTESIAN_POINT('Ctrl Pts',(1.53065417503801,86.8746009812092,15.3047763718407));
#43926=CARTESIAN_POINT('Ctrl Pts',(1.95169418101603,86.7983425328552,14.8839200494221));
#43927=CARTESIAN_POINT('Ctrl Pts',(2.10605889778836,86.7649315937189,14.6720095011498));
#43928=CARTESIAN_POINT('Ctrl Pts',(2.29093548057867,86.7125650457084,14.3112312392637));
#43929=CARTESIAN_POINT('Ctrl Pts',(2.34566095004559,86.693892675126,14.1768424648627));
#43930=CARTESIAN_POINT('Ctrl Pts',(2.48729441704505,86.6323240198447,13.7187538256714));
#43931=CARTESIAN_POINT('Ctrl Pts',(2.52096433896476,86.590453325082,13.3823820847822));
#43932=CARTESIAN_POINT('Ctrl Pts',(2.47170635126602,86.5285024519331,12.8935881743819));
#43933=CARTESIAN_POINT('Ctrl Pts',(2.44141781072855,86.5088471240641,12.7396567590519));
#43934=CARTESIAN_POINT('Ctrl Pts',(2.30300644825099,86.4476390572762,12.2726692707813));
#43935=CARTESIAN_POINT('Ctrl Pts',(2.14715563849133,86.4065960985094,11.9775063735307));
#43936=CARTESIAN_POINT('Ctrl Pts',(1.74658059918022,86.3273664067261,11.4856900616074));
#43937=CARTESIAN_POINT('Ctrl Pts',(1.51341345441157,86.2898878339531,11.2870727723557));
#43938=CARTESIAN_POINT('Ctrl Pts',(1.01354676556786,86.2186284722799,10.9983712063086));
#43939=CARTESIAN_POINT('Ctrl Pts',(0.755899027584269,86.1853458203392,10.9013730834781));
#43940=CARTESIAN_POINT('Ctrl Pts',(0.164164177956732,86.111639338047,10.7836844551613));
#43941=CARTESIAN_POINT('Ctrl Pts',(-0.168912606911206,86.0716259537327,
10.783994787668));
#43942=CARTESIAN_POINT('Ctrl Pts',(-0.783423096808428,85.9955451571676,
10.9074267337659));
#43943=CARTESIAN_POINT('Ctrl Pts',(-1.06181458238947,85.9602116328655,11.0172961032343));
#43944=CARTESIAN_POINT('Ctrl Pts',(-1.59892393627267,85.8845224624073,11.3492801308928));
#43945=CARTESIAN_POINT('Ctrl Pts',(-1.8452892123725,85.8446071613234,11.5804625622087));
#43946=CARTESIAN_POINT('Ctrl Pts',(-2.18010727624499,85.7760126044956,12.0523224408078));
#43947=CARTESIAN_POINT('Ctrl Pts',(-2.2914420907559,85.7475533148643,12.2709867692661));
#43948=CARTESIAN_POINT('Ctrl Pts',(-2.45582760355662,85.6868482894876,12.7592485550244));
#43949=CARTESIAN_POINT('Ctrl Pts',(-2.49997107572636,85.6548921126602,13.0285721308173));
#43950=CARTESIAN_POINT('Ctrl Pts',(-2.49999998579136,85.6233272066706,13.2997334606593));
#43951=CARTESIAN_POINT('Origin',(0.,70.2,13.3));
#43952=CARTESIAN_POINT('',(-2.50006911666048,83.7560733610116,13.3003763888455));
#43953=CARTESIAN_POINT('',(-2.5,84.5087322051727,13.3000000000001));
#43954=CARTESIAN_POINT('',(-2.5,70.2,13.3));
#43955=CARTESIAN_POINT('',(-2.03459967169508,84.6272597203354,11.8472323735682));
#43956=CARTESIAN_POINT('Ctrl Pts',(-2.5,84.5087322051727,13.3000000000002));
#43957=CARTESIAN_POINT('Ctrl Pts',(-2.5,84.5296744575748,13.0655280982184));
#43958=CARTESIAN_POINT('Ctrl Pts',(-2.46699906006975,84.5500080722109,12.8315998676825));
#43959=CARTESIAN_POINT('Ctrl Pts',(-2.32292977670388,84.5897770551703,12.3335388726652));
#43960=CARTESIAN_POINT('Ctrl Pts',(-2.19886900509429,84.6076007678664,12.0773365066594));
#43961=CARTESIAN_POINT('Ctrl Pts',(-2.03458002190507,84.6272882767454,11.8472494589694));
#43962=CARTESIAN_POINT('Ctrl Pts',(-2.03458055730488,84.627288638924,11.8472502087982));
#43963=CARTESIAN_POINT('Ctrl Pts',(-1.89450969771275,84.6662409459504,11.6510805384963));
#43964=CARTESIAN_POINT('Ctrl Pts',(-1.72676167686059,84.70488524973,11.4761414012548));
#43965=CARTESIAN_POINT('Ctrl Pts',(-1.33323554888588,84.7839203668059,11.1695331444189));
#43966=CARTESIAN_POINT('Ctrl Pts',(-1.10663251548048,84.824181403158,11.043490787527));
#43967=CARTESIAN_POINT('Ctrl Pts',(-0.713279434127413,84.8891603374553,
10.8984823803338));
#43968=CARTESIAN_POINT('Ctrl Pts',(-0.556769167311561,84.9137340255325,
10.8574444566412));
#43969=CARTESIAN_POINT('Ctrl Pts',(-0.0920359549528423,84.9854951466048,
10.7826265481142));
#43970=CARTESIAN_POINT('Ctrl Pts',(0.219863619697767,85.0323990958273,10.7905367664575));
#43971=CARTESIAN_POINT('Ctrl Pts',(0.829912779101551,85.1254292919659,10.9209057582261));
#43972=CARTESIAN_POINT('Ctrl Pts',(1.12231417855182,85.1718960945836,11.0440446262694));
#43973=CARTESIAN_POINT('Ctrl Pts',(1.6507300087735,85.2648134431928,11.3953957464715));
#43974=CARTESIAN_POINT('Ctrl Pts',(1.88082541594596,85.3108255938684,11.6222047214489));
#43975=CARTESIAN_POINT('Ctrl Pts',(2.154729054646,85.3805730708179,12.0216790741474));
#43976=CARTESIAN_POINT('Ctrl Pts',(2.23401550940231,85.4037764216242,12.1659173450706));
#43977=CARTESIAN_POINT('Ctrl Pts',(2.36216169616374,85.4501613860974,12.4655396180094));
#43978=CARTESIAN_POINT('Ctrl Pts',(2.41115940395367,85.4734047411207,12.6199789466383));
#43979=CARTESIAN_POINT('Ctrl Pts',(2.50542927385025,85.5380651617574,13.0615369731934));
#43980=CARTESIAN_POINT('Ctrl Pts',(2.51620520654007,85.5771720580018,13.3534227472839));
#43981=CARTESIAN_POINT('Ctrl Pts',(2.43286997623803,85.660417934164,13.9590573673342));
#43982=CARTESIAN_POINT('Ctrl Pts',(2.32815364430273,85.7046699769092,14.2658043051374));
#43983=CARTESIAN_POINT('Ctrl Pts',(2.04326879523016,85.7853727884209,14.7622662765919));
#43984=CARTESIAN_POINT('Ctrl Pts',(1.88594571676374,85.8206545389477,14.9602761163235));
#43985=CARTESIAN_POINT('Ctrl Pts',(1.45672746521806,85.8996631696703,15.3590473678497));
#43986=CARTESIAN_POINT('Ctrl Pts',(1.16867617371516,85.9429996836769,15.5351669355018));
#43987=CARTESIAN_POINT('Ctrl Pts',(0.567290294484066,86.0294344701491,15.7538890334455));
#43988=CARTESIAN_POINT('Ctrl Pts',(0.263389568511162,86.0713280760463,15.80479544449));
#43989=CARTESIAN_POINT('Ctrl Pts',(-0.347063720854757,86.153708880797,15.7945044066049));
#43990=CARTESIAN_POINT('Ctrl Pts',(-0.648508246571967,86.1927479533828,
15.7336233250396));
#43991=CARTESIAN_POINT('Ctrl Pts',(-1.22704950937592,86.2739753109181,15.5012940046377));
#43992=CARTESIAN_POINT('Ctrl Pts',(-1.49705895641803,86.3156531362169,15.3273375546511));
#43993=CARTESIAN_POINT('Ctrl Pts',(-1.90384652058772,86.3902653546794,14.9386270062663));
#43994=CARTESIAN_POINT('Ctrl Pts',(-2.05487870899703,86.4223406009384,14.744737410521));
#43995=CARTESIAN_POINT('Ctrl Pts',(-2.33984399672216,86.4969198229823,14.2415511770626));
#43996=CARTESIAN_POINT('Ctrl Pts',(-2.44450868436423,86.5389635819673,13.9211140722652));
#43997=CARTESIAN_POINT('Ctrl Pts',(-2.49440148476151,86.5943813575555,13.4932888285128));
#43998=CARTESIAN_POINT('Ctrl Pts',(-2.5,86.6068448891404,13.3965969251772));
#43999=CARTESIAN_POINT('Ctrl Pts',(-2.5,86.6193069507268,13.3));
#44000=CARTESIAN_POINT('',(2.14925682029349,84.6483054938945,12.0236057114313));
#44001=CARTESIAN_POINT('Ctrl Pts',(-2.5,85.6232961799494,13.299999999995));
#44002=CARTESIAN_POINT('Ctrl Pts',(-2.50000000000055,85.5917227576639,13.5712372036452));
#44003=CARTESIAN_POINT('Ctrl Pts',(-2.45585968378062,85.560975556195,13.8406868646292));
#44004=CARTESIAN_POINT('Ctrl Pts',(-2.27504200781115,85.4958832560464,14.3776917079628));
#44005=CARTESIAN_POINT('Ctrl Pts',(-2.13192098994924,85.4617229481704,14.6387221943466));
#44006=CARTESIAN_POINT('Ctrl Pts',(-1.75410765777896,85.3933213928303,15.1075309435492));
#44007=CARTESIAN_POINT('Ctrl Pts',(-1.51934906495187,85.3597252797142,15.3088945812207));
#44008=CARTESIAN_POINT('Ctrl Pts',(-1.10894810382751,85.3063223822594,15.5468531123579));
#44009=CARTESIAN_POINT('Ctrl Pts',(-0.955788647789875,85.2873824496154,
15.6161583606504));
#44010=CARTESIAN_POINT('Ctrl Pts',(-0.480112309063621,85.231316508119,15.7761164643413));
#44011=CARTESIAN_POINT('Ctrl Pts',(-0.145206934044905,85.1957537821981,
15.8180608233535));
#44012=CARTESIAN_POINT('Ctrl Pts',(0.347176162967513,85.1423661766384,15.7809117293853));
#44013=CARTESIAN_POINT('Ctrl Pts',(0.504742999838479,85.1248905459983,15.7537076929526));
#44014=CARTESIAN_POINT('Ctrl Pts',(0.940608188461335,85.0756692072896,15.6346732045655));
#44015=CARTESIAN_POINT('Ctrl Pts',(1.20697524144371,85.0448924842423,15.5087888422649));
#44016=CARTESIAN_POINT('Ctrl Pts',(1.57582668150888,84.9981323686656,15.2473704104133));
#44017=CARTESIAN_POINT('Ctrl Pts',(1.69691114033394,84.9817729703862,15.1428161339116));
#44018=CARTESIAN_POINT('Ctrl Pts',(2.02477759993649,84.9321002195505,14.7998083454098));
#44019=CARTESIAN_POINT('Ctrl Pts',(2.19749443666729,84.8992477097675,14.5330108934588));
#44020=CARTESIAN_POINT('Ctrl Pts',(2.37516628231922,84.8523744181851,14.0957358404697));
#44021=CARTESIAN_POINT('Ctrl Pts',(2.42041100154623,84.8371809870098,13.9451571559582));
#44022=CARTESIAN_POINT('Ctrl Pts',(2.51630609195442,84.7896560808508,13.4667250924553));
#44023=CARTESIAN_POINT('Ctrl Pts',(2.51626066285438,84.7563533960887,13.132390406575));
#44024=CARTESIAN_POINT('Ctrl Pts',(2.39548609200373,84.6982962618345,12.5310518927434));
#44025=CARTESIAN_POINT('Ctrl Pts',(2.29349171899702,84.6735589749346,12.2658148578631));
#44026=CARTESIAN_POINT('Ctrl Pts',(2.14935917264751,84.64798408829,12.0231855471698));
#44027=CARTESIAN_POINT('Ctrl Pts',(2.14849826856341,84.6481217304052,12.0232892114969));
#44028=CARTESIAN_POINT('Ctrl Pts',(2.11917051097377,84.6398957178875,11.9731483588035));
#44029=CARTESIAN_POINT('Ctrl Pts',(2.0879409562537,84.6315456703781,11.9242313897563));
#44030=CARTESIAN_POINT('Ctrl Pts',(2.05503530279454,84.6231699387726,11.8765751353672));
#44031=CARTESIAN_POINT('Ctrl Pts',(2.03758851112758,84.6187290713526,11.8513074790665));
#44032=CARTESIAN_POINT('Ctrl Pts',(2.01967012324788,84.6142808813125,11.8263934597074));
#44033=CARTESIAN_POINT('Ctrl Pts',(2.0013105791726,84.6098393338709,11.8018336082256));
#44034=CARTESIAN_POINT('Ctrl Pts',(1.95360166998468,84.598297577568,11.7380126484452));
#44035=CARTESIAN_POINT('Ctrl Pts',(1.90291702693478,84.5868009686769,11.6765816365097));
#44036=CARTESIAN_POINT('Ctrl Pts',(1.84940702252334,84.5753758491209,11.617721034844));
#44037=CARTESIAN_POINT('Ctrl Pts',(1.84334032278039,84.5740805255522,11.6110477108381));
#44038=CARTESIAN_POINT('Ctrl Pts',(1.83723725127936,84.5727861170242,11.6044074219133));
#44039=CARTESIAN_POINT('Ctrl Pts',(1.83109798478322,84.571492658943,11.597800428888));
#44040=CARTESIAN_POINT('Ctrl Pts',(1.81083540127987,84.5672236143602,11.5759941189706));
#44041=CARTESIAN_POINT('Ctrl Pts',(1.79017879691286,84.5629650561677,11.554550327143));
#44042=CARTESIAN_POINT('Ctrl Pts',(1.76913427802234,84.5587185485681,11.5334779347543));
#44043=CARTESIAN_POINT('Ctrl Pts',(1.76912118729655,84.5587159070315,11.5334648266898));
#44044=CARTESIAN_POINT('Ctrl Pts',(1.76910809642049,84.5587132654995,11.5334517187691));
#44045=CARTESIAN_POINT('Ctrl Pts',(1.76909500539423,84.5587106239721,11.5334386109921));
#44046=CARTESIAN_POINT('Ctrl Pts',(1.71326467222136,84.5474450935846,11.4775368399679));
#44047=CARTESIAN_POINT('Ctrl Pts',(1.65470244751872,84.5362629238947,11.4242464012593));
#44048=CARTESIAN_POINT('Ctrl Pts',(1.5935912865466,84.5251013315194,11.3737476542726));
#44049=CARTESIAN_POINT('Ctrl Pts',(1.58663034186001,84.5238299561126,11.3679955301282));
#44050=CARTESIAN_POINT('Ctrl Pts',(1.57963632720324,84.5225588525222,11.362279682546));
#44051=CARTESIAN_POINT('Ctrl Pts',(1.57260951578204,84.5212879316989,11.3566004206128));
#44052=CARTESIAN_POINT('Ctrl Pts',(1.54114987390819,84.5155979093606,11.3311738742295));
#44053=CARTESIAN_POINT('Ctrl Pts',(1.50903308308831,84.5099117604085,11.306480011195));
#44054=CARTESIAN_POINT('Ctrl Pts',(1.47628533748555,84.5042229325365,11.2825462510708));
#44055=CARTESIAN_POINT('Ctrl Pts',(1.40560170972749,84.4919440112159,11.2308869700934));
#44056=CARTESIAN_POINT('Ctrl Pts',(1.33234814011117,84.4797149402549,11.1830393232752));
#44057=CARTESIAN_POINT('Ctrl Pts',(1.25688466188294,84.4674885153415,11.1391740063337));
#44058=CARTESIAN_POINT('Ctrl Pts',(1.18024233305996,84.4550710956764,11.0946234485819));
#44059=CARTESIAN_POINT('Ctrl Pts',(1.10132102455115,84.4426565425067,11.0541814524054));
#44060=CARTESIAN_POINT('Ctrl Pts',(1.02050057260668,84.4302220882334,11.0180230316069));
#44061=CARTESIAN_POINT('Ctrl Pts',(0.939565585508334,84.417770012404,10.9818133687009));
#44062=CARTESIAN_POINT('Ctrl Pts',(0.856727000365074,84.4052982698638,10.9498996271201));
#44063=CARTESIAN_POINT('Ctrl Pts',(0.772357774959221,84.3928072041311,10.9224457497855));
#44064=CARTESIAN_POINT('Ctrl Pts',(0.705646887261843,84.3829304975559,10.9007379230404));
#44065=CARTESIAN_POINT('Ctrl Pts',(0.637979060749295,84.3730422331464,10.8818180164808));
#44066=CARTESIAN_POINT('Ctrl Pts',(0.569528632595271,84.3631508286921,10.8657628186098));
#44067=CARTESIAN_POINT('Ctrl Pts',(0.492890482829709,84.3520762604768,10.8477871726987));
#44068=CARTESIAN_POINT('Ctrl Pts',(0.415633948246713,84.3410498064073,10.8334872949032));
#44069=CARTESIAN_POINT('Ctrl Pts',(0.337996328823612,84.3300902367718,10.8228666141398));
#44070=CARTESIAN_POINT('Ctrl Pts',(0.327737236966226,84.3286420312183,10.82146318961));
#44071=CARTESIAN_POINT('Ctrl Pts',(0.317471425880949,84.3271949884746,10.820124044175));
#44072=CARTESIAN_POINT('Ctrl Pts',(0.307199384886591,84.3257491472112,10.8188492206551));
#44073=CARTESIAN_POINT('Ctrl Pts',(0.241293251306034,84.3164725285242,10.8106698637737));
#44074=CARTESIAN_POINT('Ctrl Pts',(0.17513263978019,84.3072459085532,10.8051360337245));
#44075=CARTESIAN_POINT('Ctrl Pts',(0.108833704360324,84.2980823991264,10.8022584452339));
#44076=CARTESIAN_POINT('Ctrl Pts',(0.108796485092262,84.2980772548642,10.8022568297971));
#44077=CARTESIAN_POINT('Ctrl Pts',(0.108759265780064,84.2980721106215,10.8022552151983));
#44078=CARTESIAN_POINT('Ctrl Pts',(0.108722046423735,84.2980669663986,10.8022536014376));
#44079=CARTESIAN_POINT('Ctrl Pts',(0.0315282094793017,84.2873977248123,
10.798906622949));
#44080=CARTESIAN_POINT('Ctrl Pts',(-0.0458583482863662,84.2768127737701,
10.7991611830844));
#44081=CARTESIAN_POINT('Ctrl Pts',(-0.123206969103929,84.2662556267233,
10.8030205706221));
#44082=CARTESIAN_POINT('Ctrl Pts',(-0.134614841424897,84.2646985907437,
10.8035897779305));
#44083=CARTESIAN_POINT('Ctrl Pts',(-0.146021823490824,84.2631421683135,
10.8042374633925));
#44084=CARTESIAN_POINT('Ctrl Pts',(-0.157427105394915,84.2615861873139,
10.8049637018818));
#44085=CARTESIAN_POINT('Ctrl Pts',(-0.238209670080459,84.2505653167376,
10.8101075824304));
#44086=CARTESIAN_POINT('Ctrl Pts',(-0.318910181397317,84.2395660218492,
10.8191901541463));
#44087=CARTESIAN_POINT('Ctrl Pts',(-0.399221905405393,84.2285423329785,
10.832224058259));
#44088=CARTESIAN_POINT('Ctrl Pts',(-0.40716638935307,84.2274518630582,10.8335133798777));
#44089=CARTESIAN_POINT('Ctrl Pts',(-0.415107035160441,84.2263611579551,
10.8348413913814));
#44090=CARTESIAN_POINT('Ctrl Pts',(-0.423043523069841,84.2252701754968,
10.8362081206935));
#44091=CARTESIAN_POINT('Ctrl Pts',(-0.509827441306192,84.2133404991037,
10.8511530341395));
#44092=CARTESIAN_POINT('Ctrl Pts',(-0.595661334196555,84.2014396006435,
10.8706460978654));
#44093=CARTESIAN_POINT('Ctrl Pts',(-0.680151385509904,84.1895334035807,
10.8945522574904));
#44094=CARTESIAN_POINT('Ctrl Pts',(-0.765810754833279,84.1774624281748,
10.918789271489));
#44095=CARTESIAN_POINT('Ctrl Pts',(-0.850087656711938,84.1653862403638,
10.9475623001945));
#44096=CARTESIAN_POINT('Ctrl Pts',(-0.932579965822,84.1532917784,10.980718122263));
#44097=CARTESIAN_POINT('Ctrl Pts',(-1.01489871165712,84.1412227631045,11.0138041847003));
#44098=CARTESIAN_POINT('Ctrl Pts',(-1.0954395486111,84.1291359036723,11.0512537216435));
#44099=CARTESIAN_POINT('Ctrl Pts',(-1.17382631390194,84.117035886723,11.0929096144844));
#44100=CARTESIAN_POINT('Ctrl Pts',(-1.23349316200181,84.1078255325178,11.1246174649281));
#44101=CARTESIAN_POINT('Ctrl Pts',(-1.29191246367207,84.0986079596607,11.158762141708));
#44102=CARTESIAN_POINT('Ctrl Pts',(-1.34893047897793,84.0893901288936,11.1952788927209));
#44103=CARTESIAN_POINT('Ctrl Pts',(-1.41374684242227,84.0789115763525,11.2367900360457));
#44104=CARTESIAN_POINT('Ctrl Pts',(-1.47645562641417,84.0684804861339,11.2811758377148));
#44105=CARTESIAN_POINT('Ctrl Pts',(-1.53690793086315,84.0581102114262,11.3282811495333));
#44106=CARTESIAN_POINT('Ctrl Pts',(-1.54661344555603,84.0564452814544,11.3358438272531));
#44107=CARTESIAN_POINT('Ctrl Pts',(-1.55626083141933,84.0547819109094,11.3434767058554));
#44108=CARTESIAN_POINT('Ctrl Pts',(-1.56584950640497,84.0531201457002,11.3511792634875));
#44109=CARTESIAN_POINT('Ctrl Pts',(-1.58076085088466,84.050535935315,11.3631575076555));
#44110=CARTESIAN_POINT('Ctrl Pts',(-1.5955302851023,84.0479556411926,11.3753041619004));
#44111=CARTESIAN_POINT('Ctrl Pts',(-1.61015577184586,84.0453794715716,11.3876173081328));
#44112=CARTESIAN_POINT('Ctrl Pts',(-1.61017318706277,84.0453764040119,11.3876319699432));
#44113=CARTESIAN_POINT('Ctrl Pts',(-1.61019060207545,84.0453733364582,11.3876466319895));
#44114=CARTESIAN_POINT('Ctrl Pts',(-1.61020801688417,84.0453702689102,11.387661294272));
#44115=CARTESIAN_POINT('Ctrl Pts',(-1.6702222848764,84.0347989989563,11.4381899084481));
#44116=CARTESIAN_POINT('Ctrl Pts',(-1.72781534394189,84.0242960017743,11.491523535541));
#44117=CARTESIAN_POINT('Ctrl Pts',(-1.78281861963694,84.0138159666427,11.5474935888694));
#44118=CARTESIAN_POINT('Ctrl Pts',(-1.78873192186358,84.0126892771083,11.5535108276027));
#44119=CARTESIAN_POINT('Ctrl Pts',(-1.79461524224577,84.0115628577759,11.5595585424526));
#44120=CARTESIAN_POINT('Ctrl Pts',(-1.80046833598367,84.01043665582,11.5656365256758));
#44121=CARTESIAN_POINT('Ctrl Pts',(-1.85778274524969,83.9994087101373,11.6251530879525));
#44122=CARTESIAN_POINT('Ctrl Pts',(-1.91220264883735,83.9884010673625,11.6875723068517));
#44123=CARTESIAN_POINT('Ctrl Pts',(-1.96349678520254,83.9773768953035,11.7526753058382));
#44124=CARTESIAN_POINT('Ctrl Pts',(-1.96727297368631,83.9765653142043,11.7574680796805));
#44125=CARTESIAN_POINT('Ctrl Pts',(-1.97103219826863,83.975753645517,11.7622753979488));
#44126=CARTESIAN_POINT('Ctrl Pts',(-1.97477435558608,83.974941875499,11.7670971725773));
#44127=CARTESIAN_POINT('Ctrl Pts',(-2.00390860505308,83.9686219086436,11.8046366913581));
#44128=CARTESIAN_POINT('Ctrl Pts',(-2.03200944070001,83.9622959963989,11.8430519541797));
#44129=CARTESIAN_POINT('Ctrl Pts',(-2.05903053186209,83.9559594509966,11.8822977714207));
#44130=CARTESIAN_POINT('Ctrl Pts',(-2.10927629639763,83.9441766341466,11.9552754346937));
#44131=CARTESIAN_POINT('Ctrl Pts',(-2.15552457366351,83.9324176323788,12.0307431773993));
#44132=CARTESIAN_POINT('Ctrl Pts',(-2.19760450671408,83.9206653708732,12.1083180328222));
#44133=CARTESIAN_POINT('Ctrl Pts',(-2.24010370136137,83.9087960162172,12.1866658019689));
#44134=CARTESIAN_POINT('Ctrl Pts',(-2.27835082976822,83.8969338428497,12.2671617205543));
#44135=CARTESIAN_POINT('Ctrl Pts',(-2.31219177387408,83.8850748620298,12.3494225010224));
#44136=CARTESIAN_POINT('Ctrl Pts',(-2.34577947277736,83.8733046266654,12.431067691454));
#44137=CARTESIAN_POINT('Ctrl Pts',(-2.37502734172382,83.8615378834169,12.5144502354414));
#44138=CARTESIAN_POINT('Ctrl Pts',(-2.39980300275635,83.8497790893336,12.5992242626934));
#44139=CARTESIAN_POINT('Ctrl Pts',(-2.41793252873578,83.8411746221292,12.661257438213));
#44140=CARTESIAN_POINT('Ctrl Pts',(-2.43366789394612,83.8325746030936,12.7240362618047));
#44141=CARTESIAN_POINT('Ctrl Pts',(-2.44695834901582,83.8239824445497,12.7874374646912));
#44142=CARTESIAN_POINT('Ctrl Pts',(-2.460347233552,83.8153266522494,12.8513082185857));
#44143=CARTESIAN_POINT('Ctrl Pts',(-2.471204606091,83.8067116911319,12.9155681000887));
#44144=CARTESIAN_POINT('Ctrl Pts',(-2.47953240888263,83.7981397773589,12.9801030274514));
#44145=CARTESIAN_POINT('Ctrl Pts',(-2.47954663266533,83.7981251366377,12.9802132522978));
#44146=CARTESIAN_POINT('Ctrl Pts',(-2.4795608490606,83.7981104960407,12.9803234779527));
#44147=CARTESIAN_POINT('Ctrl Pts',(-2.47957505806789,83.7980958555679,12.980433704416));
#44148=CARTESIAN_POINT('Ctrl Pts',(-2.48978104680403,83.7875799554521,13.0596067261839));
#44149=CARTESIAN_POINT('Ctrl Pts',(-2.49617918219035,83.7771276545593,13.1391989483178));
#44150=CARTESIAN_POINT('Ctrl Pts',(-2.49876087430341,83.7667036850347,13.2189438316804));
#44151=CARTESIAN_POINT('Ctrl Pts',(-2.49899788354894,83.7657467246211,13.2262647180652));
#44152=CARTESIAN_POINT('Ctrl Pts',(-2.49920269802926,83.7647900065606,13.2335868711549));
#44153=CARTESIAN_POINT('Ctrl Pts',(-2.49937529352148,83.763833505736,13.240910072088));
#44154=CARTESIAN_POINT('Ctrl Pts',(-2.49984232063202,83.7612453047894,13.2607259625703));
#44155=CARTESIAN_POINT('Ctrl Pts',(-2.50007366146133,83.7586587303504,13.2805495321041));
#44156=CARTESIAN_POINT('Ctrl Pts',(-2.50006911666048,83.7560733610116,13.3003763888455));
#44157=CARTESIAN_POINT('Origin',(0.,70.2,13.3));
#44158=CARTESIAN_POINT('',(-2.49945695676299,81.6745745895027,13.3008703539627));
#44159=CARTESIAN_POINT('',(-2.5,82.7842705339798,13.3000000461456));
#44160=CARTESIAN_POINT('',(-2.5,70.2,13.3));
#44161=CARTESIAN_POINT('Ctrl Pts',(-2.5,82.7842705395179,13.30000004682));
#44162=CARTESIAN_POINT('Ctrl Pts',(-2.50000000474803,82.8151486489161,13.0464743231556));
#44163=CARTESIAN_POINT('Ctrl Pts',(-2.46143312520029,82.8456950881806,12.7942093261388));
#44164=CARTESIAN_POINT('Ctrl Pts',(-2.29559019350917,82.913307429788,12.2653750201076));
#44165=CARTESIAN_POINT('Ctrl Pts',(-2.15481793884933,82.9496162619464,11.9973154498993));
#44166=CARTESIAN_POINT('Ctrl Pts',(-1.77133732543768,83.0243684274161,11.5065918089598));
#44167=CARTESIAN_POINT('Ctrl Pts',(-1.52552718495303,83.0624000292781,11.2933314358174));
#44168=CARTESIAN_POINT('Ctrl Pts',(-0.978817042207699,83.1380165311215,
10.979029248912));
#44169=CARTESIAN_POINT('Ctrl Pts',(-0.685479661821654,83.1744000363931,
10.876129893064));
#44170=CARTESIAN_POINT('Ctrl Pts',(-0.230925991395841,83.2286768540928,
10.8060729843433));
#44171=CARTESIAN_POINT('Ctrl Pts',(-0.0792523874947042,83.246459573482,
10.7966588088363));
#44172=CARTESIAN_POINT('Ctrl Pts',(0.40597672983133,83.3037729097049,10.8107043539447));
#44173=CARTESIAN_POINT('Ctrl Pts',(0.734341271195505,83.343726567668,10.887079955444));
#44174=CARTESIAN_POINT('Ctrl Pts',(1.29290248867132,83.415501730351,11.1420161353982));
#44175=CARTESIAN_POINT('Ctrl Pts',(1.52642631860712,83.4470317637685,11.3003642432778));
#44176=CARTESIAN_POINT('Ctrl Pts',(1.96977200461063,83.5172201949765,11.7248012931862));
#44177=CARTESIAN_POINT('Ctrl Pts',(2.16210557071182,83.5565757583034,12.0013363632263));
#44178=CARTESIAN_POINT('Ctrl Pts',(2.40434668893103,83.6266132227551,12.5613249417336));
#44179=CARTESIAN_POINT('Ctrl Pts',(2.47128925112929,83.6569863242284,12.8317076339978));
#44180=CARTESIAN_POINT('Ctrl Pts',(2.51847633634278,83.7249975186905,13.4430164826046));
#44181=CARTESIAN_POINT('Ctrl Pts',(2.47639648335978,83.7638242349361,13.7801922505863));
#44182=CARTESIAN_POINT('Ctrl Pts',(2.32211632612132,83.8179195687182,14.2376694798723));
#44183=CARTESIAN_POINT('Ctrl Pts',(2.26320478544772,83.8339892328385,14.3720869380744));
#44184=CARTESIAN_POINT('Ctrl Pts',(2.03327647388433,83.8857476511911,14.7920409828922));
#44185=CARTESIAN_POINT('Ctrl Pts',(1.8172110944513,83.9206614450298,15.0487405805084));
#44186=CARTESIAN_POINT('Ctrl Pts',(1.33675906134119,83.988904671192,15.4313357697943));
#44187=CARTESIAN_POINT('Ctrl Pts',(1.08792744616513,84.0195314593032,15.5684976495056));
#44188=CARTESIAN_POINT('Ctrl Pts',(0.512447306626639,84.0825800153206,15.7686752409219));
#44189=CARTESIAN_POINT('Ctrl Pts',(0.18549286044068,84.1148658541091,15.8144637113446));
#44190=CARTESIAN_POINT('Ctrl Pts',(-0.297842385271882,84.1663760915718,
15.7871608483506));
#44191=CARTESIAN_POINT('Ctrl Pts',(-0.453540252969198,84.183059015621,15.7635344772117));
#44192=CARTESIAN_POINT('Ctrl Pts',(-0.87086652634696,84.2273370307914,15.659261624922));
#44193=CARTESIAN_POINT('Ctrl Pts',(-1.12309700629158,84.2532555468506,15.5501672836693));
#44194=CARTESIAN_POINT('Ctrl Pts',(-1.63403978386678,84.3106087880742,15.2213979897503));
#44195=CARTESIAN_POINT('Ctrl Pts',(-1.87603810873575,84.3447079772851,14.9858870711083));
#44196=CARTESIAN_POINT('Ctrl Pts',(-2.2161326393584,84.4028897048695,14.4878602816455));
#44197=CARTESIAN_POINT('Ctrl Pts',(-2.33095487771852,84.4263308146894,14.2428805823425));
#44198=CARTESIAN_POINT('Ctrl Pts',(-2.44762140903683,84.4620722812837,13.8328188645868));
#44199=CARTESIAN_POINT('Ctrl Pts',(-2.47628360372299,84.4751148756247,13.677856235399));
#44200=CARTESIAN_POINT('Ctrl Pts',(-2.49673874376048,84.4955310389552,13.447508993848));
#44201=CARTESIAN_POINT('Ctrl Pts',(-2.5,84.502147214964,13.3737263188229));
#44202=CARTESIAN_POINT('Ctrl Pts',(-2.5,84.5087322051727,13.3000000000002));
#44203=CARTESIAN_POINT('',(0.920533865651003,82.4393565600724,10.9761000835092));
#44204=CARTESIAN_POINT('Ctrl Pts',(-2.49999997190418,83.756061301239,13.3003748053845));
#44205=CARTESIAN_POINT('Ctrl Pts',(-2.49997053707063,83.7304625818255,13.4967089193153));
#44206=CARTESIAN_POINT('Ctrl Pts',(-2.47681278101998,83.7050876939534,13.6923701395223));
#44207=CARTESIAN_POINT('Ctrl Pts',(-2.386442493329,83.6549243393185,14.0689985510949));
#44208=CARTESIAN_POINT('Ctrl Pts',(-2.3207540989909,83.6303163479419,14.2489869525319));
#44209=CARTESIAN_POINT('Ctrl Pts',(-2.17540180662083,83.588603526226,14.5391361695074));
#44210=CARTESIAN_POINT('Ctrl Pts',(-2.10611992772313,83.5715210295465,14.6535483090943));
#44211=CARTESIAN_POINT('Ctrl Pts',(-1.84384754758448,83.5141396907722,15.0173918612513));
#44212=CARTESIAN_POINT('Ctrl Pts',(-1.61301034700003,83.4742903313108,15.2358304578918));
#44213=CARTESIAN_POINT('Ctrl Pts',(-1.06657348378726,83.3921894241131,15.5855651570229));
#44214=CARTESIAN_POINT('Ctrl Pts',(-0.752239937707715,83.3507172289968,
15.7073982634096));
#44215=CARTESIAN_POINT('Ctrl Pts',(-0.100607888244321,83.2681416610412,
15.8193341419016));
#44216=CARTESIAN_POINT('Ctrl Pts',(0.229826195854046,83.2278622845284,15.8108536590563));
#44217=CARTESIAN_POINT('Ctrl Pts',(0.854323629728798,83.1489218889708,15.6702154373954));
#44218=CARTESIAN_POINT('Ctrl Pts',(1.14383932493661,83.1109645118561,15.544872369784));
#44219=CARTESIAN_POINT('Ctrl Pts',(1.53687818274458,83.0530562323332,15.278451413705));
#44220=CARTESIAN_POINT('Ctrl Pts',(1.6618751448833,83.0333993710254,15.1746844222207));
#44221=CARTESIAN_POINT('Ctrl Pts',(1.99964754439797,82.9753386868527,14.8337623860049));
#44222=CARTESIAN_POINT('Ctrl Pts',(2.17826535959274,82.9375944425982,14.567362465926));
#44223=CARTESIAN_POINT('Ctrl Pts',(2.42372800150795,82.8622912527412,13.9875530584655));
#44224=CARTESIAN_POINT('Ctrl Pts',(2.49051521068362,82.8256643283977,13.6802215306031));
#44225=CARTESIAN_POINT('Ctrl Pts',(2.50820308507383,82.749883453198,13.0350558370635));
#44226=CARTESIAN_POINT('Ctrl Pts',(2.45051170429726,82.7110712531846,12.7030768183537));
#44227=CARTESIAN_POINT('Ctrl Pts',(2.21264451975073,82.6353142833311,12.0927269729288));
#44228=CARTESIAN_POINT('Ctrl Pts',(2.03926080643865,82.5989342728309,11.8185321005017));
#44229=CARTESIAN_POINT('Ctrl Pts',(1.68967717139366,82.5407258716454,11.4478785655612));
#44230=CARTESIAN_POINT('Ctrl Pts',(1.54561286613422,82.5194619873994,11.3260548274809));
#44231=CARTESIAN_POINT('Ctrl Pts',(1.24219839653513,82.4785013781746,11.1232543168828));
#44232=CARTESIAN_POINT('Ctrl Pts',(1.08514199867268,82.4588978683154,11.0408518241034));
#44233=CARTESIAN_POINT('Ctrl Pts',(0.920701682247921,82.439197125928,10.9757133541007));
#44234=CARTESIAN_POINT('Ctrl Pts',(0.920507210407054,82.4391691851521,10.9761469785899));
#44235=CARTESIAN_POINT('Ctrl Pts',(0.84976445037318,82.426381971998,10.948000104283));
#44236=CARTESIAN_POINT('Ctrl Pts',(0.777916166713806,82.4135085909658,10.9232354764272));
#44237=CARTESIAN_POINT('Ctrl Pts',(0.705230255075198,82.4006744273682,10.9018091529748));
#44238=CARTESIAN_POINT('Ctrl Pts',(0.694119454342045,82.398712591421,10.8985339156563));
#44239=CARTESIAN_POINT('Ctrl Pts',(0.6829889829655,82.3967516629018,10.8953366906903));
#44240=CARTESIAN_POINT('Ctrl Pts',(0.671839691847331,82.3947920799437,10.8922173334976));
#44241=CARTESIAN_POINT('Ctrl Pts',(0.586872667320551,82.3798584010672,10.8684451944179));
#44242=CARTESIAN_POINT('Ctrl Pts',(0.500815373266157,82.3650031047442,10.8491915008198));
#44243=CARTESIAN_POINT('Ctrl Pts',(0.413984558834269,82.3502424772814,10.8345517612444));
#44244=CARTESIAN_POINT('Ctrl Pts',(0.327154114489939,82.3354819127309,10.8199120840661));
#44245=CARTESIAN_POINT('Ctrl Pts',(0.239549777812097,82.3208163506725,10.8098854974778));
#44246=CARTESIAN_POINT('Ctrl Pts',(0.151457802439923,82.3062793032402,10.804602088381));
#44247=CARTESIAN_POINT('Ctrl Pts',(0.151457426975483,82.3062792412806,10.8046020658621));
#44248=CARTESIAN_POINT('Ctrl Pts',(0.151457051511035,82.306279179321,10.8046020433433));
#44249=CARTESIAN_POINT('Ctrl Pts',(0.151456676046577,82.3062791173614,10.8046020208246));
#44250=CARTESIAN_POINT('Ctrl Pts',(0.0822104397887709,82.2948520186583,
10.800448936811));
#44251=CARTESIAN_POINT('Ctrl Pts',(0.0126607245485073,82.2835043155213,
10.7992276341647));
#44252=CARTESIAN_POINT('Ctrl Pts',(-0.0570059073669244,82.2721873246359,
10.8009360103044));
#44253=CARTESIAN_POINT('Ctrl Pts',(-0.14371378961836,82.258102069096,10.8030622746734));
#44254=CARTESIAN_POINT('Ctrl Pts',(-0.230151663471033,82.2441367908506,
10.8097146479824));
#44255=CARTESIAN_POINT('Ctrl Pts',(-0.315952706456719,82.2302199268284,
10.8207744957541));
#44256=CARTESIAN_POINT('Ctrl Pts',(-0.403178153725669,82.2160720255131,
10.8320179507872));
#44257=CARTESIAN_POINT('Ctrl Pts',(-0.489745485313005,82.2019740268762,
10.8478168688112));
#44258=CARTESIAN_POINT('Ctrl Pts',(-0.575270617001006,82.1878816168917,
10.8680721652291));
#44259=CARTESIAN_POINT('Ctrl Pts',(-0.661074709200265,82.173743241168,10.8883935291027));
#44260=CARTESIAN_POINT('Ctrl Pts',(-0.745829681226131,82.1596105377005,
10.9132004739449));
#44261=CARTESIAN_POINT('Ctrl Pts',(-0.829149800122876,82.1454701158155,
10.9424143426831));
#44262=CARTESIAN_POINT('Ctrl Pts',(-0.896122525388783,82.1341040423798,
10.9658964551772));
#44263=CARTESIAN_POINT('Ctrl Pts',(-0.96216825856647,82.1227336268377,10.9922261462949));
#44264=CARTESIAN_POINT('Ctrl Pts',(-1.02708814866811,82.1113658868256,11.0213733111377));
#44265=CARTESIAN_POINT('Ctrl Pts',(-1.10336977519159,82.0980086599932,11.0556215690949));
#44266=CARTESIAN_POINT('Ctrl Pts',(-1.17771424808106,82.0847211261591,11.0935876798491));
#44267=CARTESIAN_POINT('Ctrl Pts',(-1.24986448583372,82.0715335632568,11.1351336081243));
#44268=CARTESIAN_POINT('Ctrl Pts',(-1.25422160535989,82.0707371724254,11.1376425475396));
#44269=CARTESIAN_POINT('Ctrl Pts',(-1.25857072555773,82.0699411455125,11.1401645576712));
#44270=CARTESIAN_POINT('Ctrl Pts',(-1.26291179071775,82.0691454889291,11.1426996141131));
#44271=CARTESIAN_POINT('Ctrl Pts',(-1.31412432639877,82.0597589467627,11.1726062530819));
#44272=CARTESIAN_POINT('Ctrl Pts',(-1.36421607654112,82.0504245494676,11.2043270087693));
#44273=CARTESIAN_POINT('Ctrl Pts',(-1.41309955253088,82.0411578054689,11.2378252182875));
#44274=CARTESIAN_POINT('Ctrl Pts',(-1.41310394086109,82.0411569735818,11.2378282254633));
#44275=CARTESIAN_POINT('Ctrl Pts',(-1.41310832918156,82.0411561416953,11.2378312326534));
#44276=CARTESIAN_POINT('Ctrl Pts',(-1.41311271749229,82.0411553098093,11.2378342398578));
#44277=CARTESIAN_POINT('Ctrl Pts',(-1.48469698971785,82.0275851782536,11.2868892303627));
#44278=CARTESIAN_POINT('Ctrl Pts',(-1.5536938241786,82.0141586954001,11.3397565966466));
#44279=CARTESIAN_POINT('Ctrl Pts',(-1.61985078000212,82.0007828283404,11.3961809425237));
#44280=CARTESIAN_POINT('Ctrl Pts',(-1.68693280121697,81.987219928012,11.4533942637844));
#44281=CARTESIAN_POINT('Ctrl Pts',(-1.75109465428362,81.9737087318884,11.5142656241143));
#44282=CARTESIAN_POINT('Ctrl Pts',(-1.81203792615991,81.9601793605005,11.5785368018034));
#44283=CARTESIAN_POINT('Ctrl Pts',(-1.81926383290583,81.958575213349,11.5861572908605));
#44284=CARTESIAN_POINT('Ctrl Pts',(-1.82644445540145,81.956970844803,11.593825576645));
#44285=CARTESIAN_POINT('Ctrl Pts',(-1.8335792678427,81.9553661663048,11.6015412284807));
#44286=CARTESIAN_POINT('Ctrl Pts',(-1.89327644268047,81.9419397765216,11.666098302744));
#44287=CARTESIAN_POINT('Ctrl Pts',(-1.94945332063817,81.9285591200788,11.7336311899609));
#44288=CARTESIAN_POINT('Ctrl Pts',(-2.00190495204929,81.915190002813,11.8037989156827));
#44289=CARTESIAN_POINT('Ctrl Pts',(-2.05486837504321,81.9016904377135,11.8746512960177));
#44290=CARTESIAN_POINT('Ctrl Pts',(-2.1040333896945,81.8882027779552,11.9481899398141));
#44291=CARTESIAN_POINT('Ctrl Pts',(-2.14918746491882,81.8747225855896,12.0240873143052));
#44292=CARTESIAN_POINT('Ctrl Pts',(-2.19396401610349,81.8613550983708,12.0993501262838));
#44293=CARTESIAN_POINT('Ctrl Pts',(-2.23479676132122,81.84799526694,12.1769320227064));
#44294=CARTESIAN_POINT('Ctrl Pts',(-2.27147531358765,81.8346653241564,12.2565413372964));
#44295=CARTESIAN_POINT('Ctrl Pts',(-2.30066318307058,81.8240576909174,12.3198924277921));
#44296=CARTESIAN_POINT('Ctrl Pts',(-2.32722053987198,81.813469572234,12.384527860221));
#44297=CARTESIAN_POINT('Ctrl Pts',(-2.35103612877134,81.8029222000041,12.4503155687124));
#44298=CARTESIAN_POINT('Ctrl Pts',(-2.36200624994732,81.798063787645,12.4806192129805));
#44299=CARTESIAN_POINT('Ctrl Pts',(-2.37237341924686,81.7932235389059,12.5111090934759));
#44300=CARTESIAN_POINT('Ctrl Pts',(-2.38213316408953,81.7884038266734,12.5417713279222));
#44301=CARTESIAN_POINT('Ctrl Pts',(-2.38213497126972,81.788402934223,12.5417770055484));
#44302=CARTESIAN_POINT('Ctrl Pts',(-2.38213677842907,81.7884020417733,12.5417826831804));
#44303=CARTESIAN_POINT('Ctrl Pts',(-2.38213858556761,81.7884011493242,12.5417883608184));
#44304=CARTESIAN_POINT('Ctrl Pts',(-2.40822063813608,81.7755206192219,12.6237325227086));
#44305=CARTESIAN_POINT('Ctrl Pts',(-2.42996705299851,81.7627848366969,12.7069088786412));
#44306=CARTESIAN_POINT('Ctrl Pts',(-2.44737300812834,81.7501066243246,12.7909657542522));
#44307=CARTESIAN_POINT('Ctrl Pts',(-2.46525102449264,81.7370845702879,12.8773023089828));
#44308=CARTESIAN_POINT('Ctrl Pts',(-2.4785491035503,81.724122963737,12.9645680884214));
#44309=CARTESIAN_POINT('Ctrl Pts',(-2.48723432530795,81.7111558284396,13.0523726633709));
#44310=CARTESIAN_POINT('Ctrl Pts',(-2.49539167600486,81.698976810666,13.1348406452648));
#44311=CARTESIAN_POINT('Ctrl Pts',(-2.49947918835398,81.6867931450403,13.2177836784269));
#44312=CARTESIAN_POINT('Ctrl Pts',(-2.49945695676299,81.6745745895027,13.3008703539627));
#44313=CARTESIAN_POINT('Origin',(0.,70.2,13.3));
#44314=CARTESIAN_POINT('',(-2.5,79.5915676097122,13.3));
#44315=CARTESIAN_POINT('',(-2.49999989869882,80.7678846556286,13.3006754269486));
#44316=CARTESIAN_POINT('',(-2.5,70.2,13.3));
#44317=CARTESIAN_POINT('Ctrl Pts',(-2.5,80.7679766722356,13.2999999999636));
#44318=CARTESIAN_POINT('Ctrl Pts',(-2.49999999999743,80.7919940503135,13.1237066736875));
#44319=CARTESIAN_POINT('Ctrl Pts',(-2.48135257898582,80.8160657376386,12.9479000631705));
#44320=CARTESIAN_POINT('Ctrl Pts',(-2.40449147928125,80.8656754101913,12.5896891044419));
#44321=CARTESIAN_POINT('Ctrl Pts',(-2.34355439399043,80.8910969426707,12.4089970768672));
#44322=CARTESIAN_POINT('Ctrl Pts',(-2.1323483554941,80.9578859740607,11.9594402169915));
#44323=CARTESIAN_POINT('Ctrl Pts',(-1.95200779379245,80.9986680773843,11.7082328251797));
#44324=CARTESIAN_POINT('Ctrl Pts',(-1.50005750782899,81.0816867594947,11.2746672404786));
#44325=CARTESIAN_POINT('Ctrl Pts',(-1.22910592695524,81.1239888242985,11.0996727640186));
#44326=CARTESIAN_POINT('Ctrl Pts',(-0.622132238241597,81.2105497801797,
10.85563754211));
#44327=CARTESIAN_POINT('Ctrl Pts',(-0.289742232557924,81.2537155668831,
10.7943997868315));
#44328=CARTESIAN_POINT('Ctrl Pts',(0.378906709372972,81.3416969560312,10.8063952796647));
#44329=CARTESIAN_POINT('Ctrl Pts',(0.708421464602578,81.3847548048629,10.8792982086031));
#44330=CARTESIAN_POINT('Ctrl Pts',(1.15920293187042,81.4492114126598,11.0792950433409));
#44331=CARTESIAN_POINT('Ctrl Pts',(1.29806394747014,81.46999271598,11.1574981473877));
#44332=CARTESIAN_POINT('Ctrl Pts',(1.56092802817003,81.5117258795864,11.3405303600909));
#44333=CARTESIAN_POINT('Ctrl Pts',(1.68407459372433,81.5325267391818,11.4452989666089));
#44334=CARTESIAN_POINT('Ctrl Pts',(2.01344849481162,81.593772627866,11.7855611220864));
#44335=CARTESIAN_POINT('Ctrl Pts',(2.18668992149707,81.6339977394226,12.0486394497486));
#44336=CARTESIAN_POINT('Ctrl Pts',(2.37206751090576,81.6959212714359,12.4926489676096));
#44337=CARTESIAN_POINT('Ctrl Pts',(2.42117567545926,81.7175292392572,12.6546859991923));
#44338=CARTESIAN_POINT('Ctrl Pts',(2.51301675488385,81.7790396248975,13.1245661496585));
#44339=CARTESIAN_POINT('Ctrl Pts',(2.51540170769641,81.8185577968828,13.4371340404721));
#44340=CARTESIAN_POINT('Ctrl Pts',(2.40386216979899,81.8990292788653,14.0578293187524));
#44341=CARTESIAN_POINT('Ctrl Pts',(2.28691982456896,81.9396181738109,14.3596549603516));
#44342=CARTESIAN_POINT('Ctrl Pts',(2.02796594347174,82.0014185968546,14.7713185529014));
#44343=CARTESIAN_POINT('Ctrl Pts',(1.92607653879892,82.0223329024532,14.9023909362485));
#44344=CARTESIAN_POINT('Ctrl Pts',(1.70024326424352,82.0638260203644,15.1399653104941));
#44345=CARTESIAN_POINT('Ctrl Pts',(1.57733880143946,82.0843029246184,15.2463562682276));
#44346=CARTESIAN_POINT('Ctrl Pts',(1.17233692727742,82.1470572328373,15.5332193050472));
#44347=CARTESIAN_POINT('Ctrl Pts',(0.863690510392055,82.1886808319658,15.6697476837293));
#44348=CARTESIAN_POINT('Ctrl Pts',(0.379503208853912,82.250929777162,15.7763067879642));
#44349=CARTESIAN_POINT('Ctrl Pts',(0.218669114029323,82.2711547840977,15.7956570620044));
#44350=CARTESIAN_POINT('Ctrl Pts',(-0.109131336955512,82.3122024257939,
15.8031451044184));
#44351=CARTESIAN_POINT('Ctrl Pts',(-0.275325575811793,82.332920868852,15.7903501656056));
#44352=CARTESIAN_POINT('Ctrl Pts',(-0.600564073168092,82.3741292333048,
15.7323342732206));
#44353=CARTESIAN_POINT('Ctrl Pts',(-0.75888333096764,82.3945175299687,15.6876819955936));
#44354=CARTESIAN_POINT('Ctrl Pts',(-1.21607316545537,82.4556116920922,15.5086263790366));
#44355=CARTESIAN_POINT('Ctrl Pts',(-1.49415858908143,82.4958887774955,15.3308551159289));
#44356=CARTESIAN_POINT('Ctrl Pts',(-1.94913799063012,82.5738694127342,14.8946466969535));
#44357=CARTESIAN_POINT('Ctrl Pts',(-2.12809954443533,82.6108546906218,14.646566811081));
#44358=CARTESIAN_POINT('Ctrl Pts',(-2.40253056499088,82.6895940267774,14.0687282670974));
#44359=CARTESIAN_POINT('Ctrl Pts',(-2.48404468206299,82.7306970300942,13.738917591953));
#44360=CARTESIAN_POINT('Ctrl Pts',(-2.49929532159507,82.7759165854465,13.3685641927628));
#44361=CARTESIAN_POINT('Ctrl Pts',(-2.49999999935818,82.780096565306,13.3342705981348));
#44362=CARTESIAN_POINT('Ctrl Pts',(-2.5,82.7842705395179,13.30000004682));
#44363=CARTESIAN_POINT('Ctrl Pts',(-2.4999998261115,81.6749952458184,13.3009324389811));
#44364=CARTESIAN_POINT('Ctrl Pts',(-2.49991253633163,81.6405605469028,13.5349685946262));
#44365=CARTESIAN_POINT('Ctrl Pts',(-2.46696346326491,81.6058284433278,13.7678210047342));
#44366=CARTESIAN_POINT('Ctrl Pts',(-2.32746234213115,81.5318384401283,14.2515934989957));
#44367=CARTESIAN_POINT('Ctrl Pts',(-2.21144212941816,81.4940422500614,14.4967445953751));
#44368=CARTESIAN_POINT('Ctrl Pts',(-1.87818185910071,81.4105339024537,14.9802831866022));
#44369=CARTESIAN_POINT('Ctrl Pts',(-1.64970720082521,81.3649212471221,15.2050888306269));
#44370=CARTESIAN_POINT('Ctrl Pts',(-1.10617480949064,81.2723301938908,15.5668922268197));
#44371=CARTESIAN_POINT('Ctrl Pts',(-0.792482881520969,81.2269863668739,
15.694674443377));
#44372=CARTESIAN_POINT('Ctrl Pts',(-0.305885222944733,81.1579877356795,
15.7863540338617));
#44373=CARTESIAN_POINT('Ctrl Pts',(-0.14641747304618,81.1356671061898,15.8008166872527));
#44374=CARTESIAN_POINT('Ctrl Pts',(0.33631647022864,81.068466064175,15.7982413847432));
#44375=CARTESIAN_POINT('Ctrl Pts',(0.655951788470225,81.025363460793,15.7339520439778));
#44376=CARTESIAN_POINT('Ctrl Pts',(1.23977630781376,80.9396868701814,15.4927558358357));
#44377=CARTESIAN_POINT('Ctrl Pts',(1.50071189510592,80.8976116253231,15.3231388991448));
#44378=CARTESIAN_POINT('Ctrl Pts',(1.9671157445643,80.8107550473978,14.8789293715332));
#44379=CARTESIAN_POINT('Ctrl Pts',(2.16104664137428,80.7670092557745,14.6009593608744));
#44380=CARTESIAN_POINT('Ctrl Pts',(2.39439141454417,80.6886729004306,14.0618027257703));
#44381=CARTESIAN_POINT('Ctrl Pts',(2.45894886565495,80.6550316744386,13.8167865804675));
#44382=CARTESIAN_POINT('Ctrl Pts',(2.52138635184131,80.5782689387822,13.2338126945466));
#44383=CARTESIAN_POINT('Ctrl Pts',(2.48995284914939,80.5358865949142,12.8975853572706));
#44384=CARTESIAN_POINT('Ctrl Pts',(2.30089390179739,80.4505903893889,12.2713312541675));
#44385=CARTESIAN_POINT('Ctrl Pts',(2.15057778183786,80.4086501158078,11.9857418823028));
#44386=CARTESIAN_POINT('Ctrl Pts',(1.74537905123426,80.32403380283,11.4803167972005));
#44387=CARTESIAN_POINT('Ctrl Pts',(1.49180752192044,80.2827027831265,11.2672255635697));
#44388=CARTESIAN_POINT('Ctrl Pts',(1.07427192245701,80.2218625597934,11.0377125497692));
#44389=CARTESIAN_POINT('Ctrl Pts',(0.938178420999734,80.20293185114,10.9779699547945));
#44390=CARTESIAN_POINT('Ctrl Pts',(0.524495277091662,80.1470038199357,10.8387113041414));
#44391=CARTESIAN_POINT('Ctrl Pts',(0.237531674435638,80.1101825354509,10.7946798827699));
#44392=CARTESIAN_POINT('Ctrl Pts',(-0.358844376929671,80.0341640202705,
10.8067514790922));
#44393=CARTESIAN_POINT('Ctrl Pts',(-0.663334875007,79.9957531567254,10.8699603612868));
#44394=CARTESIAN_POINT('Ctrl Pts',(-1.24016568033655,79.9176729412342,11.1065420209301));
#44395=CARTESIAN_POINT('Ctrl Pts',(-1.50647293035896,79.8787046039393,11.2801417129448));
#44396=CARTESIAN_POINT('Ctrl Pts',(-1.8363841577928,79.8217387609598,11.5976268567848));
#44397=CARTESIAN_POINT('Ctrl Pts',(-1.93058492742045,79.8040343036143,11.7052509341366));
#44398=CARTESIAN_POINT('Ctrl Pts',(-2.21401866602675,79.744612481632,12.0912436803229));
#44399=CARTESIAN_POINT('Ctrl Pts',(-2.3563070459151,79.7034678779596,12.3995407202117));
#44400=CARTESIAN_POINT('Ctrl Pts',(-2.47774027658423,79.6385375323126,12.9150157743823));
#44401=CARTESIAN_POINT('Ctrl Pts',(-2.5,79.6150595569346,13.1073924341113));
#44402=CARTESIAN_POINT('Ctrl Pts',(-2.5,79.5915676097122,13.3));
#44403=CARTESIAN_POINT('Origin',(0.,70.2,13.3));
#44404=CARTESIAN_POINT('',(0.0622069118415443,78.2779999202659,10.8008522795397));
#44405=CARTESIAN_POINT('Ctrl Pts',(-2.5,79.5915676097122,13.3));
#44406=CARTESIAN_POINT('Ctrl Pts',(-2.5,79.5765893471849,13.4228049194608));
#44407=CARTESIAN_POINT('Ctrl Pts',(-2.49095183244887,79.5615902451076,13.5457018584579));
#44408=CARTESIAN_POINT('Ctrl Pts',(-2.42905647899425,79.5103106867224,13.9619631225716));
#44409=CARTESIAN_POINT('Ctrl Pts',(-2.33311627520834,79.4745828864616,14.2461061930075));
#44410=CARTESIAN_POINT('Ctrl Pts',(-2.11483283458189,79.4203135727282,14.6421625210424));
#44411=CARTESIAN_POINT('Ctrl Pts',(-2.02777490876142,79.4018575879159,14.7703903323516));
#44412=CARTESIAN_POINT('Ctrl Pts',(-1.71700853519764,79.3432769354389,15.1475574324335));
#44413=CARTESIAN_POINT('Ctrl Pts',(-1.45502808785973,79.3035168530704,15.3602269930674));
#44414=CARTESIAN_POINT('Ctrl Pts',(-0.870536320458681,79.2257575529658,
15.6660382611492));
#44415=CARTESIAN_POINT('Ctrl Pts',(-0.555372805189541,79.1881784743964,
15.7591739433774));
#44416=CARTESIAN_POINT('Ctrl Pts',(0.0689547438071552,79.1144225712145,
15.8171677303455));
#44417=CARTESIAN_POINT('Ctrl Pts',(0.37177162559577,79.0795738596712,15.7905292092738));
#44418=CARTESIAN_POINT('Ctrl Pts',(0.813737634667213,79.0270165160454,15.6690525947261));
#44419=CARTESIAN_POINT('Ctrl Pts',(0.960662794940438,79.0091851413643,15.6133751578383));
#44420=CARTESIAN_POINT('Ctrl Pts',(1.39918978441872,78.9530842841364,15.3981666218593));
#44421=CARTESIAN_POINT('Ctrl Pts',(1.66500041743212,78.9150325480588,15.1941727241333));
#44422=CARTESIAN_POINT('Ctrl Pts',(2.0978478448116,78.8411758699274,14.6983952064093));
#44423=CARTESIAN_POINT('Ctrl Pts',(2.26227010865142,78.8054826369546,14.4129268163996));
#44424=CARTESIAN_POINT('Ctrl Pts',(2.46292419306783,78.7354421192179,13.8221142684528));
#44425=CARTESIAN_POINT('Ctrl Pts',(2.50756858043878,78.7028085987227,13.5253606679568));
#44426=CARTESIAN_POINT('Ctrl Pts',(2.49438845861115,78.6537286585241,13.0699291846091));
#44427=CARTESIAN_POINT('Ctrl Pts',(2.47489621447307,78.6369255806952,12.9129704408489));
#44428=CARTESIAN_POINT('Ctrl Pts',(2.36985034709022,78.5844124596717,12.4391366042795));
#44429=CARTESIAN_POINT('Ctrl Pts',(2.23677091053079,78.5487737055021,12.1362737650858));
#44430=CARTESIAN_POINT('Ctrl Pts',(1.86562405784736,78.4811260038381,11.6053326362498));
#44431=CARTESIAN_POINT('Ctrl Pts',(1.633539081042,78.4489573179972,11.3806244304195));
#44432=CARTESIAN_POINT('Ctrl Pts',(1.15875266219343,78.3898965509339,11.0710637806197));
#44433=CARTESIAN_POINT('Ctrl Pts',(0.933219124018623,78.3646789547675,10.9676100711174));
#44434=CARTESIAN_POINT('Ctrl Pts',(0.489884079549194,78.319165331666,10.8390810709257));
#44435=CARTESIAN_POINT('Ctrl Pts',(0.276813594715694,78.298799748681,10.8061106932887));
#44436=CARTESIAN_POINT('Ctrl Pts',(0.0621484015592424,78.2779284766691,
10.8007726041467));
#44437=CARTESIAN_POINT('',(-2.5,77.5741002924676,13.3000000003379));
#44438=CARTESIAN_POINT('Ctrl Pts',(0.0619821551910609,78.2789454186495,
10.8007684756234));
#44439=CARTESIAN_POINT('Ctrl Pts',(-0.104887459920181,78.2455091533278,
10.7966300281528));
#44440=CARTESIAN_POINT('Ctrl Pts',(-0.271922990360639,78.2128217158413,
10.8092189380874));
#44441=CARTESIAN_POINT('Ctrl Pts',(-0.614414187643506,78.1449976468288,
10.8699487483443));
#44442=CARTESIAN_POINT('Ctrl Pts',(-0.788656239572891,78.1101407315737,
10.920744664503));
#44443=CARTESIAN_POINT('Ctrl Pts',(-1.24864492292068,78.0183993180752,11.1111327255881));
#44444=CARTESIAN_POINT('Ctrl Pts',(-1.51604373609959,77.9626022477322,11.2869701050732));
#44445=CARTESIAN_POINT('Ctrl Pts',(-1.96838320015796,77.8511640306151,11.7271156654777));
#44446=CARTESIAN_POINT('Ctrl Pts',(-2.15010403125278,77.7996110206432,11.986333026704));
#44447=CARTESIAN_POINT('Ctrl Pts',(-2.34743372797686,77.7191456011658,12.4241322392309));
#44448=CARTESIAN_POINT('Ctrl Pts',(-2.40044283594966,77.6913034022843,12.582023844553));
#44449=CARTESIAN_POINT('Ctrl Pts',(-2.47898775590883,77.6335137307816,12.9263758145357));
#44450=CARTESIAN_POINT('Ctrl Pts',(-2.5000000000506,77.6039710225773,13.1128609741768));
#44451=CARTESIAN_POINT('Ctrl Pts',(-2.5,77.5741002924676,13.3000000006759));
#44452=CARTESIAN_POINT('',(-2.5,78.5257776763231,13.3));
#44453=CARTESIAN_POINT('',(-2.5,70.2,13.3));
#44454=CARTESIAN_POINT('',(0.171877485205294,78.9529403329783,10.8041890652845));
#44455=CARTESIAN_POINT('Ctrl Pts',(-2.5,78.5257776763231,13.2999999999999));
#44456=CARTESIAN_POINT('Ctrl Pts',(-2.5,78.5374921201612,13.192701393122));
#44457=CARTESIAN_POINT('Ctrl Pts',(-2.49309211256744,78.5491001278162,13.08530859238));
#44458=CARTESIAN_POINT('Ctrl Pts',(-2.45895306334767,78.5776320699999,12.8220488663969));
#44459=CARTESIAN_POINT('Ctrl Pts',(-2.42390357232428,78.5944012804548,12.6678797589494));
#44460=CARTESIAN_POINT('Ctrl Pts',(-2.27266321667134,78.6466887304271,12.2086072991207));
#44461=CARTESIAN_POINT('Ctrl Pts',(-2.11120649888306,78.6820619745369,11.9219325597868));
#44462=CARTESIAN_POINT('Ctrl Pts',(-1.69032400712601,78.7495267532703,11.4302392127342));
#44463=CARTESIAN_POINT('Ctrl Pts',(-1.43630710763509,78.7818015743182,11.2287147601134));
#44464=CARTESIAN_POINT('Ctrl Pts',(-0.934258717810192,78.8406692098519,
10.9682936273892));
#44465=CARTESIAN_POINT('Ctrl Pts',(-0.70198902852392,78.8655951332596,10.8881584393048));
#44466=CARTESIAN_POINT('Ctrl Pts',(-0.252925044443173,78.9105886366888,
10.8037701643773));
#44467=CARTESIAN_POINT('Ctrl Pts',(-0.0399939993924468,78.9307258166804,
10.7913084605993));
#44468=CARTESIAN_POINT('Ctrl Pts',(0.171947635724521,78.9513559607842,10.805920207658));
#44469=CARTESIAN_POINT('Ctrl Pts',(0.171303481418846,78.9553621611337,10.8058758817465));
#44470=CARTESIAN_POINT('Ctrl Pts',(0.505867271394403,79.0245516761969,10.8288546667877));
#44471=CARTESIAN_POINT('Ctrl Pts',(0.831929165199084,79.0863319292476,10.9187702898156));
#44472=CARTESIAN_POINT('Ctrl Pts',(1.23052217204385,79.1735020953802,11.1209408397906));
#44473=CARTESIAN_POINT('Ctrl Pts',(1.32665033278514,79.1958273401737,11.1780930678944));
#44474=CARTESIAN_POINT('Ctrl Pts',(1.63536937636204,79.2662723917822,11.3908566956994));
#44475=CARTESIAN_POINT('Ctrl Pts',(1.82722107710317,79.3063688325274,11.5735409813187));
#44476=CARTESIAN_POINT('Ctrl Pts',(2.18172934994433,79.3983318517819,12.0378802394338));
#44477=CARTESIAN_POINT('Ctrl Pts',(2.32519576174729,79.450561402491,12.327446655297));
#44478=CARTESIAN_POINT('Ctrl Pts',(2.48050030556733,79.5526871729,12.8911251762962));
#44479=CARTESIAN_POINT('Ctrl Pts',(2.50992648690821,79.6001223886286,13.1561574926153));
#44480=CARTESIAN_POINT('Ctrl Pts',(2.4817442154734,79.6944068751355,13.736713999312));
#44481=CARTESIAN_POINT('Ctrl Pts',(2.4067385701941,79.7409703630377,14.0470738747417));
#44482=CARTESIAN_POINT('Ctrl Pts',(2.14174192637851,79.8388252292017,14.6293068551095));
#44483=CARTESIAN_POINT('Ctrl Pts',(1.95245057245882,79.8890169503679,14.8943553326399));
#44484=CARTESIAN_POINT('Ctrl Pts',(1.47484138064917,79.9899104232987,15.3462248317479));
#44485=CARTESIAN_POINT('Ctrl Pts',(1.18771380609895,80.0383247134631,15.5252268585384));
#44486=CARTESIAN_POINT('Ctrl Pts',(0.726853310411885,80.111607156897,15.6971359724758));
#44487=CARTESIAN_POINT('Ctrl Pts',(0.575091912529377,80.1348851208563,15.7380072204676));
#44488=CARTESIAN_POINT('Ctrl Pts',(0.255105968301367,80.1821333282104,15.7926001852218));
#44489=CARTESIAN_POINT('Ctrl Pts',(0.0873214593971162,80.2061723419182,
15.8041013366678));
#44490=CARTESIAN_POINT('Ctrl Pts',(-0.239383543702946,80.2533509862687,
15.7935933724892));
#44491=CARTESIAN_POINT('Ctrl Pts',(-0.397551125899607,80.2763502649642,
15.7733109938813));
#44492=CARTESIAN_POINT('Ctrl Pts',(-0.879279426513901,80.3473941635615,
15.6641045728957));
#44493=CARTESIAN_POINT('Ctrl Pts',(-1.18767938229527,80.3936092227799,15.5252178632953));
#44494=CARTESIAN_POINT('Ctrl Pts',(-1.58750127644831,80.4632663793177,15.2376943353219));
#44495=CARTESIAN_POINT('Ctrl Pts',(-1.70645156282528,80.4855189044681,15.1338111519495));
#44496=CARTESIAN_POINT('Ctrl Pts',(-1.92132795902574,80.5289745915201,14.9070061206651));
#44497=CARTESIAN_POINT('Ctrl Pts',(-2.01714654831655,80.5502304891351,14.7849571867929));
#44498=CARTESIAN_POINT('Ctrl Pts',(-2.22411274682521,80.6029904129379,14.4639924109367));
#44499=CARTESIAN_POINT('Ctrl Pts',(-2.32059410452609,80.6344752592051,14.2572888175016));
#44500=CARTESIAN_POINT('Ctrl Pts',(-2.46210955022574,80.7001052591825,13.8008974785368));
#44501=CARTESIAN_POINT('Ctrl Pts',(-2.49992465432316,80.7337057411103,13.5515590982602));
#44502=CARTESIAN_POINT('Ctrl Pts',(-2.49999988752857,80.7678745091697,13.300749904748));
#44503=CARTESIAN_POINT('Origin',(0.,70.2,13.3));
#44504=CARTESIAN_POINT('',(-2.5,75.3973313149984,13.3000000121208));
#44505=CARTESIAN_POINT('',(-2.5,76.6135035584265,13.2999999999132));
#44506=CARTESIAN_POINT('',(-2.5,70.2,13.3));
#44507=CARTESIAN_POINT('Ctrl Pts',(-2.5,76.6135035584265,13.2999999998264));
#44508=CARTESIAN_POINT('Ctrl Pts',(-2.49999999998539,76.640902869312,13.0895322308419));
#44509=CARTESIAN_POINT('Ctrl Pts',(-2.47342120095586,76.6677737652282,12.8798774831044));
#44510=CARTESIAN_POINT('Ctrl Pts',(-2.3781118132781,76.7170204228158,12.5100973809186));
#44511=CARTESIAN_POINT('Ctrl Pts',(-2.31840169439709,76.7391589961369,12.3490188539065));
#44512=CARTESIAN_POINT('Ctrl Pts',(-2.12608432661687,76.7959052654627,11.9585769422093));
#44513=CARTESIAN_POINT('Ctrl Pts',(-1.97271400315806,76.8304637746989,11.7417801334845));
#44514=CARTESIAN_POINT('Ctrl Pts',(-1.55432352359324,76.9084499187077,11.3135007781829));
#44515=CARTESIAN_POINT('Ctrl Pts',(-1.2745885757433,76.9505294341588,11.1233999946634));
#44516=CARTESIAN_POINT('Ctrl Pts',(-0.665469047182266,77.0347972873928,
10.8683177235145));
#44517=CARTESIAN_POINT('Ctrl Pts',(-0.343592375749612,77.0761912654679,
10.8024294587727));
#44518=CARTESIAN_POINT('Ctrl Pts',(0.224305597109283,77.1489271621091,10.7983050157087));
#44519=CARTESIAN_POINT('Ctrl Pts',(0.465768942230109,77.1796327922307,10.8318265258157));
#44520=CARTESIAN_POINT('Ctrl Pts',(1.01810755224723,77.2521309194086,10.992584925399));
#44521=CARTESIAN_POINT('Ctrl Pts',(1.31585192842238,77.2933169768907,11.1484246196224));
#44522=CARTESIAN_POINT('Ctrl Pts',(1.80560651333131,77.3719347136821,11.5454611603937));
#44523=CARTESIAN_POINT('Ctrl Pts',(2.0015333900107,77.4086412486526,11.772746904296));
#44524=CARTESIAN_POINT('Ctrl Pts',(2.23186471364254,77.4647845442123,12.1629328237427));
#44525=CARTESIAN_POINT('Ctrl Pts',(2.29820690462181,77.4839667178163,12.3038123258275));
#44526=CARTESIAN_POINT('Ctrl Pts',(2.46448498400187,77.5443102571003,12.7636937113607));
#44527=CARTESIAN_POINT('Ctrl Pts',(2.51399035998698,77.5848542874368,13.0970293775363));
#44528=CARTESIAN_POINT('Ctrl Pts',(2.4792250272564,77.6663169874103,13.7633551740978));
#44529=CARTESIAN_POINT('Ctrl Pts',(2.39535655664669,77.7065267839996,14.0896555908775));
#44530=CARTESIAN_POINT('Ctrl Pts',(2.11692598939642,77.7836716415707,14.664438237422));
#44531=CARTESIAN_POINT('Ctrl Pts',(1.93478729252063,77.819908957663,14.9123521587681));
#44532=CARTESIAN_POINT('Ctrl Pts',(1.48376859601782,77.8942561289083,15.3364222407047));
#44533=CARTESIAN_POINT('Ctrl Pts',(1.21650442379957,77.9315662180476,15.5065256145283));
#44534=CARTESIAN_POINT('Ctrl Pts',(0.616914435544194,78.0076284594651,15.7452344837372));
#44535=CARTESIAN_POINT('Ctrl Pts',(0.287797030902772,78.045956589178,15.8053804108854));
#44536=CARTESIAN_POINT('Ctrl Pts',(-0.340078085170195,78.1198400621924,
15.7944661472727));
#44537=CARTESIAN_POINT('Ctrl Pts',(-0.633483617053071,78.1540624494793,
15.7365500538306));
#44538=CARTESIAN_POINT('Ctrl Pts',(-1.05594351327345,78.2059808555621,15.5714678825535));
#44539=CARTESIAN_POINT('Ctrl Pts',(-1.19628421432258,78.223787946904,15.5007919969388));
#44540=CARTESIAN_POINT('Ctrl Pts',(-1.60741510921896,78.2795230211215,15.2427330232083));
#44541=CARTESIAN_POINT('Ctrl Pts',(-1.84865373409124,78.3171641432396,15.0148046712996));
#44542=CARTESIAN_POINT('Ctrl Pts',(-2.22847037713956,78.390763227938,14.4795104962304));
#44543=CARTESIAN_POINT('Ctrl Pts',(-2.36369876141874,78.4266339789996,14.1776392558598));
#44544=CARTESIAN_POINT('Ctrl Pts',(-2.47888946444884,78.4844613579317,13.6748672499996));
#44545=CARTESIAN_POINT('Ctrl Pts',(-2.5,78.5052984944755,13.4875793432979));
#44546=CARTESIAN_POINT('Ctrl Pts',(-2.5,78.5257776763231,13.2999999999999));
#44547=CARTESIAN_POINT('',(-2.49999942824129,77.573830409475,13.3016907966184));
#44548=CARTESIAN_POINT('Ctrl Pts',(-2.5,77.5741002924675,13.3000000006759));
#44549=CARTESIAN_POINT('Ctrl Pts',(-2.49999999999985,77.5740103330377,13.300563593198));
#44550=CARTESIAN_POINT('Ctrl Pts',(-2.49999980941778,77.5739203720443,13.301127191876));
#44551=CARTESIAN_POINT('Ctrl Pts',(-2.49999942824129,77.573830409475,13.3016907966182));
#44552=CARTESIAN_POINT('Ctrl Pts',(-2.49999942824129,77.573830409475,13.3016907966184));
#44553=CARTESIAN_POINT('Ctrl Pts',(-2.4998505811012,77.5387005635294,13.5217750817969));
#44554=CARTESIAN_POINT('Ctrl Pts',(-2.47064091555273,77.5033825159943,13.740893541864));
#44555=CARTESIAN_POINT('Ctrl Pts',(-2.3483376565198,77.429789750783,14.192603555114));
#44556=CARTESIAN_POINT('Ctrl Pts',(-2.24832776289067,77.3922965656205,14.4209456127892));
#44557=CARTESIAN_POINT('Ctrl Pts',(-2.03244148026049,77.3297355802073,14.7642416633179));
#44558=CARTESIAN_POINT('Ctrl Pts',(-1.93614254553577,77.3053765968394,14.8893973342427));
#44559=CARTESIAN_POINT('Ctrl Pts',(-1.71980881159253,77.2570344446502,15.1214711922229));
#44560=CARTESIAN_POINT('Ctrl Pts',(-1.59998907477998,77.2333548279477,15.2275763340365));
#44561=CARTESIAN_POINT('Ctrl Pts',(-1.21985180740028,77.1633293695089,15.5041530681793));
#44562=CARTESIAN_POINT('Ctrl Pts',(-0.937023136788006,77.1167539272231,
15.6384551993766));
#44563=CARTESIAN_POINT('Ctrl Pts',(-0.325696562787157,77.0237243318469,
15.7994850398668));
#44564=CARTESIAN_POINT('Ctrl Pts',(-0.00157318768005031,76.9774958228247,
15.8206327412019));
#44565=CARTESIAN_POINT('Ctrl Pts',(0.63174975682301,76.8851664667259,15.7394987781402));
#44566=CARTESIAN_POINT('Ctrl Pts',(0.935374303226106,76.8404184465601,15.6399543789379));
#44567=CARTESIAN_POINT('Ctrl Pts',(1.3028941703547,76.7808548813591,15.4361609030548));
#44568=CARTESIAN_POINT('Ctrl Pts',(1.39009367686082,76.7665074340061,15.3804588353565));
#44569=CARTESIAN_POINT('Ctrl Pts',(1.50535157950659,76.7463205190376,15.2963636060073));
#44570=CARTESIAN_POINT('Ctrl Pts',(1.53659892243022,76.7406681422641,15.2724126513246));
#44571=CARTESIAN_POINT('Ctrl Pts',(1.81904613870801,76.6889073900605,15.0451420920796));
#44572=CARTESIAN_POINT('Ctrl Pts',(2.02897514010295,76.6484341445869,14.7959177014732));
#44573=CARTESIAN_POINT('Ctrl Pts',(2.3044125404054,76.5736698642684,14.2996769558068));
#44574=CARTESIAN_POINT('Ctrl Pts',(2.39094677284079,76.5407430138779,14.0700120180514));
#44575=CARTESIAN_POINT('Ctrl Pts',(2.47192341580842,76.4874477557849,13.6978860278733));
#44576=CARTESIAN_POINT('Ctrl Pts',(2.48998737661861,76.4680577676827,13.5620527966633));
#44577=CARTESIAN_POINT('Ctrl Pts',(2.50731994501945,76.4191333719729,13.2170661773746));
#44578=CARTESIAN_POINT('Ctrl Pts',(2.49167006960422,76.3900369387755,13.0080606890604));
#44579=CARTESIAN_POINT('Ctrl Pts',(2.38327009156406,76.3168584472652,12.4733323875626));
#44580=CARTESIAN_POINT('Ctrl Pts',(2.25040410413921,76.2732649774488,12.160223554131));
#44581=CARTESIAN_POINT('Ctrl Pts',(1.88165383932843,76.1858267344357,11.6243497016782));
#44582=CARTESIAN_POINT('Ctrl Pts',(1.65673297807875,76.143246252331,11.4016782761849));
#44583=CARTESIAN_POINT('Ctrl Pts',(1.27826868862348,76.081701869475,11.1467762890589));
#44584=CARTESIAN_POINT('Ctrl Pts',(1.15331478493064,76.0627282967789,11.0773335725986));
#44585=CARTESIAN_POINT('Ctrl Pts',(0.880737790828388,76.0240851784733,10.9550845003908));
#44586=CARTESIAN_POINT('Ctrl Pts',(0.732726750098576,76.0044524348387,10.9047007074389));
#44587=CARTESIAN_POINT('Ctrl Pts',(0.454796393228603,75.9683176029859,10.8382959519578));
#44588=CARTESIAN_POINT('Ctrl Pts',(0.32649122453168,75.9519074811869,10.8180203891146));
#44589=CARTESIAN_POINT('Ctrl Pts',(0.0277475536918095,75.913455920915,10.7943811013704));
#44590=CARTESIAN_POINT('Ctrl Pts',(-0.142584306677741,75.8913396507178,
10.7982939050615));
#44591=CARTESIAN_POINT('Ctrl Pts',(-0.623538156815243,75.8270074461982,
10.8586237557184));
#44592=CARTESIAN_POINT('Ctrl Pts',(-0.925689021952383,75.7841518592404,
10.9564564924502));
#44593=CARTESIAN_POINT('Ctrl Pts',(-1.31863331537763,75.7247675861707,11.1718601340145));
#44594=CARTESIAN_POINT('Ctrl Pts',(-1.43023064939628,75.7075147965054,11.2451938153252));
#44595=CARTESIAN_POINT('Ctrl Pts',(-1.68474483337432,75.6661869413406,11.4432798817047));
#44596=CARTESIAN_POINT('Ctrl Pts',(-1.82034970448806,75.6423350379601,11.576019380759));
#44597=CARTESIAN_POINT('Ctrl Pts',(-2.07068845605139,75.5917233173125,11.8838908761042));
#44598=CARTESIAN_POINT('Ctrl Pts',(-2.18108506264707,75.56510243921,12.0606627621888));
#44599=CARTESIAN_POINT('Ctrl Pts',(-2.327449747465,75.5198200222404,12.3765606150119));
#44600=CARTESIAN_POINT('Ctrl Pts',(-2.37568238161733,75.5014569409713,12.5088664258353));
#44601=CARTESIAN_POINT('Ctrl Pts',(-2.46990638762609,75.4544805658895,12.8556620039472));
#44602=CARTESIAN_POINT('Ctrl Pts',(-2.49932241759073,75.4261114405848,13.0734822739441));
#44603=CARTESIAN_POINT('Ctrl Pts',(-2.49999614356494,75.3979755132803,13.2949294639965));
#44604=CARTESIAN_POINT('Ctrl Pts',(-2.50000000001249,75.3976534070846,13.2974647744158));
#44605=CARTESIAN_POINT('Ctrl Pts',(-2.5,75.3973313165138,13.3000000123134));
#44606=CARTESIAN_POINT('Origin',(0.,70.2,13.3));
#44607=CARTESIAN_POINT('',(-2.5,73.4944230382101,13.2999999999644));
#44608=CARTESIAN_POINT('',(-2.49999273450874,74.4211783466184,13.3001428234969));
#44609=CARTESIAN_POINT('',(-2.5,70.2,13.3));
#44610=CARTESIAN_POINT('',(-0.733503873481175,74.78666297405,10.9114679132036));
#44611=CARTESIAN_POINT('Ctrl Pts',(-2.49999999591027,74.4211798314431,13.3001429987339));
#44612=CARTESIAN_POINT('Ctrl Pts',(-2.50000751449558,74.436651893318,13.1686980360196));
#44613=CARTESIAN_POINT('Ctrl Pts',(-2.48964837222459,74.4520432857278,13.0374544083168));
#44614=CARTESIAN_POINT('Ctrl Pts',(-2.44723124009369,74.4837556590281,12.7705393309274));
#44615=CARTESIAN_POINT('Ctrl Pts',(-2.41406352581613,74.5000213738019,12.6354931731809));
#44616=CARTESIAN_POINT('Ctrl Pts',(-2.28678011758541,74.5466895483705,12.256593581168));
#44617=CARTESIAN_POINT('Ctrl Pts',(-2.16549504303506,74.5765971772256,12.0237856397495));
#44618=CARTESIAN_POINT('Ctrl Pts',(-1.84691883962062,74.6380215390291,11.5928048072836));
#44619=CARTESIAN_POINT('Ctrl Pts',(-1.64806494295363,74.669433844371,11.4001236101956));
#44620=CARTESIAN_POINT('Ctrl Pts',(-1.21099616275154,74.7296273166173,11.0979110585496));
#44621=CARTESIAN_POINT('Ctrl Pts',(-0.978969412809463,74.7580078043688,
10.9854055233531));
#44622=CARTESIAN_POINT('Ctrl Pts',(-0.733888726014597,74.7865824538561,
10.9101449127973));
#44623=CARTESIAN_POINT('',(-2.5002953309371,76.6131570886756,13.3019903645843));
#44624=CARTESIAN_POINT('Ctrl Pts',(-0.733451012361657,74.7865480661225,
10.9113467541027));
#44625=CARTESIAN_POINT('Ctrl Pts',(-0.673432073149203,74.7969027271255,
10.8925765472324));
#44626=CARTESIAN_POINT('Ctrl Pts',(-0.61279267897203,74.8074995342543,10.8762898556838));
#44627=CARTESIAN_POINT('Ctrl Pts',(-0.55172135071725,74.8181371867223,10.8623636258165));
#44628=CARTESIAN_POINT('Ctrl Pts',(-0.527242737521253,74.8224009711776,
10.8567817135846));
#44629=CARTESIAN_POINT('Ctrl Pts',(-0.502694159786421,74.8266713837145,
10.8515789143186));
#44630=CARTESIAN_POINT('Ctrl Pts',(-0.478085440360247,74.830935728438,10.8467469881344));
#44631=CARTESIAN_POINT('Ctrl Pts',(-0.391690881824103,74.8459066894804,
10.8297834020844));
#44632=CARTESIAN_POINT('Ctrl Pts',(-0.304556382645288,74.8608026951908,
10.8173866950697));
#44633=CARTESIAN_POINT('Ctrl Pts',(-0.217002215176073,74.8756018342364,
10.8096373887802));
#44634=CARTESIAN_POINT('Ctrl Pts',(-0.130399267725503,74.8902401901037,
10.8019722737461));
#44635=CARTESIAN_POINT('Ctrl Pts',(-0.0433852286454588,74.9047833866685,
10.7988533364698));
#44636=CARTESIAN_POINT('Ctrl Pts',(0.043758486802499,74.91919374792,10.8003936725185));
#44637=CARTESIAN_POINT('Ctrl Pts',(0.0566968067092791,74.9213332695468,
10.8006223678462));
#44638=CARTESIAN_POINT('Ctrl Pts',(0.0696380283409227,74.9234698394944,
10.8009538476554));
#44639=CARTESIAN_POINT('Ctrl Pts',(0.0825812731339249,74.9256033117317,
10.8013885670833));
#44640=CARTESIAN_POINT('Ctrl Pts',(0.0825820740862332,74.925603443755,10.8013885939845));
#44641=CARTESIAN_POINT('Ctrl Pts',(0.0825828750384656,74.9256035757782,
10.8013886208862));
#44642=CARTESIAN_POINT('Ctrl Pts',(0.0825836759907892,74.9256037078014,
10.8013886477882));
#44643=CARTESIAN_POINT('Ctrl Pts',(0.139654244730043,74.9350108117913,10.80330550976));
#44644=CARTESIAN_POINT('Ctrl Pts',(0.19676461313113,74.944358023619,10.8072290409036));
#44645=CARTESIAN_POINT('Ctrl Pts',(0.25380981250971,74.9536749586842,10.8131490801754));
#44646=CARTESIAN_POINT('Ctrl Pts',(0.339677955557163,74.9676994151093,10.8220603081942));
#44647=CARTESIAN_POINT('Ctrl Pts',(0.424954184620481,74.9815844407113,10.8354479249586));
#44648=CARTESIAN_POINT('Ctrl Pts',(0.50928181401435,74.995410860137,10.8531618287097));
#44649=CARTESIAN_POINT('Ctrl Pts',(0.595136153633828,75.0094876000813,10.8711964339697));
#44650=CARTESIAN_POINT('Ctrl Pts',(0.680007269306105,75.0235037767173,10.8937159352084));
#44651=CARTESIAN_POINT('Ctrl Pts',(0.76351528770202,75.0375128666789,10.9205871965277));
#44652=CARTESIAN_POINT('Ctrl Pts',(0.847496371018082,75.0516013167924,10.9476106809668));
#44653=CARTESIAN_POINT('Ctrl Pts',(0.93009870104371,75.0656826032932,10.979035547205));
#44654=CARTESIAN_POINT('Ctrl Pts',(1.01093371845271,75.0797779001705,11.0147460566196));
#44655=CARTESIAN_POINT('Ctrl Pts',(1.07649638558958,75.0912101394027,11.0437096953629));
#44656=CARTESIAN_POINT('Ctrl Pts',(1.14089641483889,75.1026509275967,11.0754928204192));
#44657=CARTESIAN_POINT('Ctrl Pts',(1.20392643847574,75.1140960024377,11.1100433369972));
#44658=CARTESIAN_POINT('Ctrl Pts',(1.27764029228284,75.1274810612552,11.1504502983314));
#44659=CARTESIAN_POINT('Ctrl Pts',(1.34910819872983,75.1408056987181,11.1944383492081));
#44660=CARTESIAN_POINT('Ctrl Pts',(1.41807234911295,75.1540415193412,11.2418370124753));
#44661=CARTESIAN_POINT('Ctrl Pts',(1.42188026116491,75.1547723460184,11.2444541684919));
#44662=CARTESIAN_POINT('Ctrl Pts',(1.42568054105983,75.1555029024436,11.2470817358406));
#44663=CARTESIAN_POINT('Ctrl Pts',(1.42947314570352,75.1562331840236,11.2497196904154));
#44664=CARTESIAN_POINT('Ctrl Pts',(1.48821328401066,75.1675438385859,11.2905765239462));
#44665=CARTESIAN_POINT('Ctrl Pts',(1.5451127816376,75.178787796999,11.3339221191132));
#44666=CARTESIAN_POINT('Ctrl Pts',(1.60001966060966,75.1899372720086,11.3796743104618));
#44667=CARTESIAN_POINT('Ctrl Pts',(1.60003342207554,75.189940066433,11.3796857774625));
#44668=CARTESIAN_POINT('Ctrl Pts',(1.60004718341631,75.1899428608514,11.3796972446146));
#44669=CARTESIAN_POINT('Ctrl Pts',(1.60006094463184,75.1899456552639,11.3797087119179));
#44670=CARTESIAN_POINT('Ctrl Pts',(1.6673443291717,75.2036085130715,11.4357763595104));
#44671=CARTESIAN_POINT('Ctrl Pts',(1.73163979777147,75.2171305775013,11.4954600813728));
#44672=CARTESIAN_POINT('Ctrl Pts',(1.79271504775094,75.2306050483382,11.5584796061301));
#44673=CARTESIAN_POINT('Ctrl Pts',(1.85244431910617,75.243782568287,11.6201103042635));
#44674=CARTESIAN_POINT('Ctrl Pts',(1.90909317913172,75.2569147376254,11.6849322179067));
#44675=CARTESIAN_POINT('Ctrl Pts',(1.96241051268122,75.270064831468,11.7526874122898));
#44676=CARTESIAN_POINT('Ctrl Pts',(2.01669904148912,75.2834544592096,11.8216767929899));
#44677=CARTESIAN_POINT('Ctrl Pts',(2.06724717224374,75.2967928725989,11.8933439766623));
#44678=CARTESIAN_POINT('Ctrl Pts',(2.1138843007413,75.3101179829707,11.9673353415709));
#44679=CARTESIAN_POINT('Ctrl Pts',(2.16101009854242,75.3235827154123,12.0421019966811));
#44680=CARTESIAN_POINT('Ctrl Pts',(2.20414236768937,75.3370337554537,12.1192416034528));
#44681=CARTESIAN_POINT('Ctrl Pts',(2.24309946485785,75.3504800299476,12.198411352111));
#44682=CARTESIAN_POINT('Ctrl Pts',(2.28179120955321,75.3638347164523,12.2770418437369));
#44683=CARTESIAN_POINT('Ctrl Pts',(2.31636476395523,75.377184419459,12.357674599306));
#44684=CARTESIAN_POINT('Ctrl Pts',(2.34663557544729,75.390511346333,12.4399993181984));
#44685=CARTESIAN_POINT('Ctrl Pts',(2.37076686222032,75.4011353064566,12.505626941053));
#44686=CARTESIAN_POINT('Ctrl Pts',(2.39216386483685,75.4117442086223,12.5723302337242));
#44687=CARTESIAN_POINT('Ctrl Pts',(2.41072662863896,75.4223188535665,12.6399658222181));
#44688=CARTESIAN_POINT('Ctrl Pts',(2.42243215395167,75.4289871372007,12.6826162648782));
#44689=CARTESIAN_POINT('Ctrl Pts',(2.43297973302564,75.435623911314,12.7255250621973));
#44690=CARTESIAN_POINT('Ctrl Pts',(2.44236065948483,75.4422232969214,12.7686548293934));
#44691=CARTESIAN_POINT('Ctrl Pts',(2.44236584688118,75.4422269462016,12.7686786789778));
#44692=CARTESIAN_POINT('Ctrl Pts',(2.44237103392073,75.4422305954703,12.7687025286298));
#44693=CARTESIAN_POINT('Ctrl Pts',(2.44237622060347,75.4422342447276,12.7687263783495));
#44694=CARTESIAN_POINT('Ctrl Pts',(2.46072654712334,75.4551452065906,12.853105964497));
#44695=CARTESIAN_POINT('Ctrl Pts',(2.47461400085036,75.4679150002155,12.9383338657672));
#44696=CARTESIAN_POINT('Ctrl Pts',(2.48406042479723,75.4806324337433,13.0240546792843));
#44697=CARTESIAN_POINT('Ctrl Pts',(2.49367121346562,75.4935711465014,13.1112670072327));
#44698=CARTESIAN_POINT('Ctrl Pts',(2.49868415566037,75.5064559074555,13.1989897404089));
#44699=CARTESIAN_POINT('Ctrl Pts',(2.49909641203807,75.5193519910899,13.2868352131255));
#44700=CARTESIAN_POINT('Ctrl Pts',(2.49951140053525,75.5323335400882,13.3752628583458));
#44701=CARTESIAN_POINT('Ctrl Pts',(2.495263900863,75.5453266418256,13.4638146101252));
#44702=CARTESIAN_POINT('Ctrl Pts',(2.48633709196862,75.5583670927344,13.5520823114472));
#44703=CARTESIAN_POINT('Ctrl Pts',(2.48364724855088,75.5622964667646,13.5786793068808));
#44704=CARTESIAN_POINT('Ctrl Pts',(2.4805324830723,75.5662299259216,13.6052504431002));
#44705=CARTESIAN_POINT('Ctrl Pts',(2.47699218299231,75.5701678989593,13.6317844060255));
#44706=CARTESIAN_POINT('Ctrl Pts',(2.46528649345273,75.5831884590115,13.7195166109914));
#44707=CARTESIAN_POINT('Ctrl Pts',(2.44899149821608,75.5961919028125,13.806378913221));
#44708=CARTESIAN_POINT('Ctrl Pts',(2.42822322194485,75.6091743378299,13.8919968916897));
#44709=CARTESIAN_POINT('Ctrl Pts',(2.40740031121669,75.6221909253344,13.9778401027052));
#44710=CARTESIAN_POINT('Ctrl Pts',(2.38208137503915,75.6351860176116,14.0624323536811));
#44711=CARTESIAN_POINT('Ctrl Pts',(2.35236220815066,75.6481314832766,14.1454285113532));
#44712=CARTESIAN_POINT('Ctrl Pts',(2.32489555181246,75.6600957707647,14.2221341252329));
#44713=CARTESIAN_POINT('Ctrl Pts',(2.29367077963975,75.6720172721161,14.2974769611409));
#44714=CARTESIAN_POINT('Ctrl Pts',(2.25873663231306,75.6838596094595,14.3712075534845));
#44715=CARTESIAN_POINT('Ctrl Pts',(2.25685841419233,75.6844963071977,14.375171644358));
#44716=CARTESIAN_POINT('Ctrl Pts',(2.25496946130733,75.6851327769405,14.3791310771119));
#44717=CARTESIAN_POINT('Ctrl Pts',(2.25306977696079,75.6857690133209,14.3830858136331));
#44718=CARTESIAN_POINT('Ctrl Pts',(2.25306658016676,75.6857700839812,14.3830924686746));
#44719=CARTESIAN_POINT('Ctrl Pts',(2.25306338334234,75.6857711546408,14.3830991237028));
#44720=CARTESIAN_POINT('Ctrl Pts',(2.25306018648752,75.6857722252999,14.3831057787176));
#44721=CARTESIAN_POINT('Ctrl Pts',(2.22243593725604,75.6960285960637,14.4468574490815));
#44722=CARTESIAN_POINT('Ctrl Pts',(2.18902432755426,75.7062241969384,14.5093912418138));
#44723=CARTESIAN_POINT('Ctrl Pts',(2.15290592708741,75.7164060231917,14.5705373831612));
#44724=CARTESIAN_POINT('Ctrl Pts',(2.10866139269601,75.7288786176589,14.6454405493805));
#44725=CARTESIAN_POINT('Ctrl Pts',(2.06058442629697,75.741267291856,14.7178723154643));
#44726=CARTESIAN_POINT('Ctrl Pts',(2.00893945857773,75.7536364929604,14.78756381264));
#44727=CARTESIAN_POINT('Ctrl Pts',(1.95648556985937,75.7661994342675,14.8583468956568));
#44728=CARTESIAN_POINT('Ctrl Pts',(1.90035073741023,75.7787423214424,14.9263025021805));
#44729=CARTESIAN_POINT('Ctrl Pts',(1.84080541521727,75.7913032226803,14.9911382774124));
#44730=CARTESIAN_POINT('Ctrl Pts',(1.78111316121511,75.8038951187281,15.0561340389775));
#44731=CARTESIAN_POINT('Ctrl Pts',(1.71799383596212,75.8165049741781,15.117994034378));
#44732=CARTESIAN_POINT('Ctrl Pts',(1.6517134736397,75.8291427017163,15.1764225844277));
#44733=CARTESIAN_POINT('Ctrl Pts',(1.5990675273059,75.8391807446968,15.2228319008903));
#44734=CARTESIAN_POINT('Ctrl Pts',(1.54442734183659,75.8492357618664,15.2670763422543));
#44735=CARTESIAN_POINT('Ctrl Pts',(1.4879202749969,75.8593011931669,15.3090092861084));
#44736=CARTESIAN_POINT('Ctrl Pts',(1.42231117942937,75.8709879410563,15.3576966923855));
#44737=CARTESIAN_POINT('Ctrl Pts',(1.3545068213907,75.8826320789913,15.4030297515981));
#44738=CARTESIAN_POINT('Ctrl Pts',(1.28475077245473,75.8942095722137,15.444881694988));
#44739=CARTESIAN_POINT('Ctrl Pts',(1.27871108705053,75.8952119858811,15.4485053602541));
#44740=CARTESIAN_POINT('Ctrl Pts',(1.27265673912055,75.8962139017588,15.4521029219175));
#44741=CARTESIAN_POINT('Ctrl Pts',(1.26658786902862,75.8972153052834,15.4556742931523));
#44742=CARTESIAN_POINT('Ctrl Pts',(1.21572309807101,75.9056083274014,15.4856068797972));
#44743=CARTESIAN_POINT('Ctrl Pts',(1.16383977803469,75.9139648112094,15.5137008071853));
#44744=CARTESIAN_POINT('Ctrl Pts',(1.11101530300954,75.9222723589206,15.5399090451328));
#44745=CARTESIAN_POINT('Ctrl Pts',(1.11099275017228,75.9222759057381,15.539920234456));
#44746=CARTESIAN_POINT('Ctrl Pts',(1.11097019716324,75.9222794525467,15.5399314234353));
#44747=CARTESIAN_POINT('Ctrl Pts',(1.1109476439824,75.9222829993466,15.5399426120706));
#44748=CARTESIAN_POINT('Ctrl Pts',(1.03849226736117,75.933677610141,15.5758877317773));
#44749=CARTESIAN_POINT('Ctrl Pts',(0.964263053763198,75.9449815130845,15.6082870623993));
#44750=CARTESIAN_POINT('Ctrl Pts',(0.888522792730374,75.9562620121927,15.6370424190572));
#44751=CARTESIAN_POINT('Ctrl Pts',(0.882729811883871,75.9571247992281,15.6392417675686));
#44752=CARTESIAN_POINT('Ctrl Pts',(0.876927997441459,75.9579874472851,15.6414197746847));
#44753=CARTESIAN_POINT('Ctrl Pts',(0.871117470341167,75.9588499854481,15.6435763845172));
#44754=CARTESIAN_POINT('Ctrl Pts',(0.788277248438114,75.9711471233134,15.6743229990672));
#44755=CARTESIAN_POINT('Ctrl Pts',(0.703664325561586,75.983422613545,15.7007248351678));
#44756=CARTESIAN_POINT('Ctrl Pts',(0.617648796075465,75.995736457179,15.7226245731082));
#44757=CARTESIAN_POINT('Ctrl Pts',(0.608067858723901,75.9971080486244,15.7250639002678));
#44758=CARTESIAN_POINT('Ctrl Pts',(0.598469549791323,75.9984800870089,15.7274473540847));
#44759=CARTESIAN_POINT('Ctrl Pts',(0.588854403214788,75.9998526334047,15.729774706648));
#44760=CARTESIAN_POINT('Ctrl Pts',(0.503102455857692,76.0120935831757,15.7505310219989));
#44761=CARTESIAN_POINT('Ctrl Pts',(0.416463419919644,76.0243127067554,15.766715883117));
#44762=CARTESIAN_POINT('Ctrl Pts',(0.32934856527692,76.03653712927,15.7783111241274));
#44763=CARTESIAN_POINT('Ctrl Pts',(0.241430789949471,76.0488742219112,15.7900132362207));
#44764=CARTESIAN_POINT('Ctrl Pts',(0.153029212895176,76.0612164676254,15.7970407405293));
#44765=CARTESIAN_POINT('Ctrl Pts',(0.0645493278428554,76.0735649869199,
15.7993796972489));
#44766=CARTESIAN_POINT('Ctrl Pts',(-0.0230985086592275,76.0857973830122,
15.80169665885));
#44767=CARTESIAN_POINT('Ctrl Pts',(-0.110822535722874,76.0980355546637,
15.7994135583182));
#44768=CARTESIAN_POINT('Ctrl Pts',(-0.198256686777905,76.1102592735339,
15.7925159596017));
#44769=CARTESIAN_POINT('Ctrl Pts',(-0.269506223325971,76.1202203047086,
15.7868951500448));
#44770=CARTESIAN_POINT('Ctrl Pts',(-0.340563746673898,76.1301712481095,
15.7782104512091));
#44771=CARTESIAN_POINT('Ctrl Pts',(-0.411248703774869,76.1400932863411,
15.7664465105473));
#44772=CARTESIAN_POINT('Ctrl Pts',(-0.44133857644335,76.1443169978527,15.7614387197653));
#44773=CARTESIAN_POINT('Ctrl Pts',(-0.471306198061353,76.1485276771993,
15.755881959445));
#44774=CARTESIAN_POINT('Ctrl Pts',(-0.501139789789567,76.1527237137163,
15.7497803106777));
#44775=CARTESIAN_POINT('Ctrl Pts',(-0.501197011215927,76.1527317617984,
15.7497686075932));
#44776=CARTESIAN_POINT('Ctrl Pts',(-0.501254232148938,76.1527398098271,
15.7497569025029));
#44777=CARTESIAN_POINT('Ctrl Pts',(-0.501311452588403,76.1527478578024,
15.7497451954068));
#44778=CARTESIAN_POINT('Ctrl Pts',(-0.580947228216661,76.1639485190249,
15.7334520021067));
#44779=CARTESIAN_POINT('Ctrl Pts',(-0.659630015256989,76.1750462039147,
15.7132769711695));
#44780=CARTESIAN_POINT('Ctrl Pts',(-0.737114781406418,76.1861013148928,
15.6893371215363));
#44781=CARTESIAN_POINT('Ctrl Pts',(-0.741951721823921,76.186791423617,15.687842690669));
#44782=CARTESIAN_POINT('Ctrl Pts',(-0.746783982146367,76.1874813649855,
15.6863335770746));
#44783=CARTESIAN_POINT('Ctrl Pts',(-0.751611498013482,76.1881711531107,
15.684809804654));
#44784=CARTESIAN_POINT('Ctrl Pts',(-0.835239102038435,76.2001204309129,
15.6584133224633));
#44785=CARTESIAN_POINT('Ctrl Pts',(-0.917446329446927,76.2120243199748,
15.6276207561274));
#44786=CARTESIAN_POINT('Ctrl Pts',(-0.997890138365169,76.2239362109078,
15.5925692869216));
#44787=CARTESIAN_POINT('Ctrl Pts',(-1.0789228246198,76.2359353011256,15.5572612284754));
#44788=CARTESIAN_POINT('Ctrl Pts',(-1.15816533534941,76.2479424786977,15.5176311885102));
#44789=CARTESIAN_POINT('Ctrl Pts',(-1.23524624877195,76.2599888541402,15.4738223576914));
#44790=CARTESIAN_POINT('Ctrl Pts',(-1.27100436126527,76.2655772109601,15.4534992837804));
#44791=CARTESIAN_POINT('Ctrl Pts',(-1.30629707352708,76.2711736775701,15.4322769955763));
#44792=CARTESIAN_POINT('Ctrl Pts',(-1.34108657282719,76.2767797302698,15.4101702111085));
#44793=CARTESIAN_POINT('Ctrl Pts',(-1.415759134045,76.2888126230056,15.3627199675086));
#44794=CARTESIAN_POINT('Ctrl Pts',(-1.48771758185659,76.300827454443,15.3114463334864));
#44795=CARTESIAN_POINT('Ctrl Pts',(-1.55667988000077,76.3128244045749,15.2566116217886));
#44796=CARTESIAN_POINT('Ctrl Pts',(-1.62213921269428,76.3242119651859,15.2045622595606));
#44797=CARTESIAN_POINT('Ctrl Pts',(-1.68489918208202,76.3355831139414,15.1493048957895));
#44798=CARTESIAN_POINT('Ctrl Pts',(-1.74474088032925,76.3469255124351,15.0910409012296));
#44799=CARTESIAN_POINT('Ctrl Pts',(-1.74812837979167,76.3475675792535,15.0877427119062));
#44800=CARTESIAN_POINT('Ctrl Pts',(-1.75150652690978,76.3482095547653,15.0844348742236));
#44801=CARTESIAN_POINT('Ctrl Pts',(-1.75487528148195,76.3488514370288,15.0811174197373));
#44802=CARTESIAN_POINT('Ctrl Pts',(-1.80561391389885,76.358519172545,15.0311514456266));
#44803=CARTESIAN_POINT('Ctrl Pts',(-1.85422289573364,76.3681651830346,14.9790071471326));
#44804=CARTESIAN_POINT('Ctrl Pts',(-1.90057536777064,76.3777775107188,14.9247866797692));
#44805=CARTESIAN_POINT('Ctrl Pts',(-1.90062224681902,76.3777872322451,14.924731843343));
#44806=CARTESIAN_POINT('Ctrl Pts',(-1.90066912355759,76.3777969537375,14.9246770047901));
#44807=CARTESIAN_POINT('Ctrl Pts',(-1.9007159979862,76.3778066751962,14.9246221641105));
#44808=CARTESIAN_POINT('Ctrl Pts',(-1.95231041277473,76.3885070289554,14.8642593424878));
#44809=CARTESIAN_POINT('Ctrl Pts',(-2.00111051102113,76.3991667756396,14.8013195262346));
#44810=CARTESIAN_POINT('Ctrl Pts',(-2.04691567528589,76.4098334589787,14.7360005086112));
#44811=CARTESIAN_POINT('Ctrl Pts',(-2.05012799429443,76.4105815141423,14.7314196818573));
#44812=CARTESIAN_POINT('Ctrl Pts',(-2.05332556257768,76.4113296017097,14.7268271568184));
#44813=CARTESIAN_POINT('Ctrl Pts',(-2.05650830149135,76.4120777373028,14.7222230034536));
#44814=CARTESIAN_POINT('Ctrl Pts',(-2.10629072825319,76.4237796099294,14.6502076940295));
#44815=CARTESIAN_POINT('Ctrl Pts',(-2.1521892024876,76.4354331050823,14.5757230003587));
#44816=CARTESIAN_POINT('Ctrl Pts',(-2.19403695991354,76.4470776657862,14.4991364969011));
#44817=CARTESIAN_POINT('Ctrl Pts',(-2.23643541816,76.4588754645494,14.4215421437309));
#44818=CARTESIAN_POINT('Ctrl Pts',(-2.27467494882356,76.4706638994492,14.341791060917));
#44819=CARTESIAN_POINT('Ctrl Pts',(-2.30859138972386,76.4824603329568,14.2602705222529));
#44820=CARTESIAN_POINT('Ctrl Pts',(-2.34239086443858,76.4942160846065,14.1790311199994));
#44821=CARTESIAN_POINT('Ctrl Pts',(-2.37189690399192,76.5059794565488,14.0960355989326));
#44822=CARTESIAN_POINT('Ctrl Pts',(-2.39696388450254,76.5177482893823,14.0116574646967));
#44823=CARTESIAN_POINT('Ctrl Pts',(-2.41650145088532,76.5269210875434,13.9458919291074));
#44824=CARTESIAN_POINT('Ctrl Pts',(-2.4333428481211,76.5360967607975,13.8792864653539));
#44825=CARTESIAN_POINT('Ctrl Pts',(-2.4474244211088,76.5452678718641,13.8120084540209));
#44826=CARTESIAN_POINT('Ctrl Pts',(-2.46306349950581,76.5554533621558,13.7372890959951));
#44827=CARTESIAN_POINT('Ctrl Pts',(-2.47522838680595,76.5655876315513,13.6620766505065));
#44828=CARTESIAN_POINT('Ctrl Pts',(-2.48392759067115,76.5756563141987,13.5865868434683));
#44829=CARTESIAN_POINT('Ctrl Pts',(-2.48540853634816,76.5773703988748,13.5737355176317));
#44830=CARTESIAN_POINT('Ctrl Pts',(-2.48678898196702,76.5790825920282,13.5608760472049));
#44831=CARTESIAN_POINT('Ctrl Pts',(-2.48806889087532,76.5807928342119,13.5480093684867));
#44832=CARTESIAN_POINT('Ctrl Pts',(-2.49254950722509,76.5867799314504,13.502966591881));
#44833=CARTESIAN_POINT('Ctrl Pts',(-2.49579901758045,76.5927428739485,13.4578359689247));
#44834=CARTESIAN_POINT('Ctrl Pts',(-2.49781663356568,76.59867840509,13.412654387648));
#44835=CARTESIAN_POINT('Ctrl Pts',(-2.49782108997901,76.5986915152062,13.4125545927402));
#44836=CARTESIAN_POINT('Ctrl Pts',(-2.49782554038138,76.5987046251887,13.4124547975822));
#44837=CARTESIAN_POINT('Ctrl Pts',(-2.49782998477221,76.5987177350374,13.4123550021743));
#44838=CARTESIAN_POINT('Ctrl Pts',(-2.49946714175907,76.6035469413954,13.3755938901972));
#44839=CARTESIAN_POINT('Ctrl Pts',(-2.50028876863852,76.6083580330503,13.3387986941934));
#44840=CARTESIAN_POINT('Ctrl Pts',(-2.5002953309371,76.6131570886756,13.3019903645843));
#44841=CARTESIAN_POINT('Ctrl Pts',(-2.49999919892924,76.6132430042317,13.3020013378422));
#44842=CARTESIAN_POINT('Ctrl Pts',(-2.49999973298295,76.613329861406,13.3013342171668));
#44843=CARTESIAN_POINT('Ctrl Pts',(-2.50000000000005,76.6134167127929,13.3006671044415));
#44844=CARTESIAN_POINT('Ctrl Pts',(-2.5,76.6135035584265,13.2999999998264));
#44845=CARTESIAN_POINT('',(-2.4999999270496,73.494492116903,13.2993960529866));
#44846=CARTESIAN_POINT('Ctrl Pts',(-2.5,75.3973313165138,13.3000000123134));
#44847=CARTESIAN_POINT('Ctrl Pts',(-2.49999999930815,75.3794855759421,13.4404673277535));
#44848=CARTESIAN_POINT('Ctrl Pts',(-2.48816179457868,75.3615006572095,13.5806882486726));
#44849=CARTESIAN_POINT('Ctrl Pts',(-2.45095445436725,75.3332520774929,13.7994517894063));
#44850=CARTESIAN_POINT('Ctrl Pts',(-2.43338834493185,75.3229050248894,13.8790088385834));
#44851=CARTESIAN_POINT('Ctrl Pts',(-2.36938303214634,75.2919598298753,14.1137818437225));
#44852=CARTESIAN_POINT('Ctrl Pts',(-2.31171814593751,75.2714156745673,14.2654938052394));
#44853=CARTESIAN_POINT('Ctrl Pts',(-2.0948220817595,75.2094987503269,14.7029305970115));
#44854=CARTESIAN_POINT('Ctrl Pts',(-1.89399762693792,75.1686958122473,14.9641156730433));
#44855=CARTESIAN_POINT('Ctrl Pts',(-1.39769529827426,75.085326161972,15.3995014584683));
#44856=CARTESIAN_POINT('Ctrl Pts',(-1.10513603679065,75.0437866196789,15.5671908650294));
#44857=CARTESIAN_POINT('Ctrl Pts',(-0.635224349127472,74.9816679945857,
15.7233247668668));
#44858=CARTESIAN_POINT('Ctrl Pts',(-0.477601342132093,74.96149582157,15.759250211776));
#44859=CARTESIAN_POINT('Ctrl Pts',(0.00557082576147318,74.9005214840376,
15.8211373284657));
#44860=CARTESIAN_POINT('Ctrl Pts',(0.333770523264666,74.8602562950338,15.7989557265504));
#44861=CARTESIAN_POINT('Ctrl Pts',(0.806534464814458,74.7993341183018,15.6719796575195));
#44862=CARTESIAN_POINT('Ctrl Pts',(0.960047577135318,74.7790364042287,15.6141079638523));
#44863=CARTESIAN_POINT('Ctrl Pts',(1.25098845094371,74.7387396892959,15.470457553408));
#44864=CARTESIAN_POINT('Ctrl Pts',(1.38797483721028,74.7188438722729,15.3855183534228));
#44865=CARTESIAN_POINT('Ctrl Pts',(1.64125378238698,74.6794328915327,15.1923936235826));
#44866=CARTESIAN_POINT('Ctrl Pts',(1.75732842027187,74.6600066475558,15.0851237520893));
#44867=CARTESIAN_POINT('Ctrl Pts',(2.08631059955819,74.5991786079486,14.7176946522855));
#44868=CARTESIAN_POINT('Ctrl Pts',(2.25752652155513,74.5582589250647,14.4252330328735));
#44869=CARTESIAN_POINT('Ctrl Pts',(2.41834594181126,74.4973362844201,13.9541606773706));
#44870=CARTESIAN_POINT('Ctrl Pts',(2.45569313558712,74.4775627525761,13.7958778664999));
#44871=CARTESIAN_POINT('Ctrl Pts',(2.49926677107777,74.4377923045067,13.473728490575));
#44872=CARTESIAN_POINT('Ctrl Pts',(2.50527587115069,74.4179256063479,13.3106077671179));
#44873=CARTESIAN_POINT('Ctrl Pts',(2.48591052115193,74.3791271198315,12.9925618485189));
#44874=CARTESIAN_POINT('Ctrl Pts',(2.46192808661686,74.3602767894519,12.8382814999868));
#44875=CARTESIAN_POINT('Ctrl Pts',(2.3429262047644,74.3015459577404,12.3675809227022));
#44876=CARTESIAN_POINT('Ctrl Pts',(2.19966323029684,74.2621185759085,12.0670280133111));
#44877=CARTESIAN_POINT('Ctrl Pts',(1.91062036874315,74.2042817750153,11.6804578957822));
#44878=CARTESIAN_POINT('Ctrl Pts',(1.80800134049828,74.1860362191448,11.5666463778398));
#44879=CARTESIAN_POINT('Ctrl Pts',(1.48995679492643,74.1339292109434,11.2730881712845));
#44880=CARTESIAN_POINT('Ctrl Pts',(1.25382301214976,74.1001662766046,11.119104232612));
#44881=CARTESIAN_POINT('Ctrl Pts',(0.737991110913591,74.0333338360369,10.8947554316624));
#44882=CARTESIAN_POINT('Ctrl Pts',(0.461640395918053,74.0007827039911,10.8267945107951));
#44883=CARTESIAN_POINT('Ctrl Pts',(-0.152956009339652,73.9287428698101,
10.7824824854762));
#44884=CARTESIAN_POINT('Ctrl Pts',(-0.487134590031164,73.8888815077343,
10.8253330033193));
#44885=CARTESIAN_POINT('Ctrl Pts',(-1.06689216198579,73.8171841973809,11.0219812491073));
#44886=CARTESIAN_POINT('Ctrl Pts',(-1.31395600857547,73.7857292972642,11.1549625923103));
#44887=CARTESIAN_POINT('Ctrl Pts',(-1.79978338394291,73.7154979029411,11.5324961074332));
#44888=CARTESIAN_POINT('Ctrl Pts',(-2.02110396006483,73.675917157806,11.7905658659855));
#44889=CARTESIAN_POINT('Ctrl Pts',(-2.28838954888656,73.6126840262612,12.2710378854155));
#44890=CARTESIAN_POINT('Ctrl Pts',(-2.36781510497411,73.5888336856356,12.4699536848605));
#44891=CARTESIAN_POINT('Ctrl Pts',(-2.47342243415319,73.5417658505072,12.8800744979288));
#44892=CARTESIAN_POINT('Ctrl Pts',(-2.49994917427196,73.518521429244,13.0893081850669));
#44893=CARTESIAN_POINT('Ctrl Pts',(-2.4999999270496,73.494492116903,13.2993960529866));
#44894=CARTESIAN_POINT('Ctrl Pts',(-2.4999999270496,73.494492116903,13.2993960529867));
#44895=CARTESIAN_POINT('Ctrl Pts',(-2.49999997648352,73.4944687120149,13.2996006815233));
#44896=CARTESIAN_POINT('Ctrl Pts',(-2.49999999999999,73.4944464433691,13.2997953736906));
#44897=CARTESIAN_POINT('Ctrl Pts',(-2.5,73.4944230382101,13.2999999999289));
#44898=CARTESIAN_POINT('Origin',(0.,70.2,13.3));
#44899=CARTESIAN_POINT('',(-2.50070443670409,71.6262534957662,13.2983067811559));
#44900=CARTESIAN_POINT('',(-2.5,72.4321658751541,13.2999999555149));
#44901=CARTESIAN_POINT('',(-2.5,70.2,13.3));
#44902=CARTESIAN_POINT('',(-2.03416539392586,72.5775385913636,11.8488729526678));
#44903=CARTESIAN_POINT('Ctrl Pts',(-2.5,72.4321658707887,13.2999999550827));
#44904=CARTESIAN_POINT('Ctrl Pts',(-2.49999999988434,72.4328037665143,13.2935626169879));
#44905=CARTESIAN_POINT('Ctrl Pts',(-2.49997513620357,72.4334420042849,13.2871241387266));
#44906=CARTESIAN_POINT('Ctrl Pts',(-2.49779794714823,72.4613839629548,13.0053373066117));
#44907=CARTESIAN_POINT('Ctrl Pts',(-2.45019055606489,72.4884964690398,12.7321056106144));
#44908=CARTESIAN_POINT('Ctrl Pts',(-2.28095458285056,72.5360659243848,12.2499098292762));
#44909=CARTESIAN_POINT('Ctrl Pts',(-2.171990881226,72.556756728809,12.0398803308066));
#44910=CARTESIAN_POINT('Ctrl Pts',(-2.03524748958403,72.5780861924427,11.8481847031589));
#44911=CARTESIAN_POINT('Ctrl Pts',(-2.03353780881959,72.5776812861837,11.8479182461381));
#44912=CARTESIAN_POINT('Ctrl Pts',(-2.00233517851855,72.5853459213617,11.8033339758466));
#44913=CARTESIAN_POINT('Ctrl Pts',(-1.96948569089566,72.593167016327,11.7599905332146));
#44914=CARTESIAN_POINT('Ctrl Pts',(-1.93522193281923,72.6010356435396,11.717886377818));
#44915=CARTESIAN_POINT('Ctrl Pts',(-1.91356637909698,72.6060088131185,11.6912754965163));
#44916=CARTESIAN_POINT('Ctrl Pts',(-1.89134540088026,72.6110010933063,11.665158731078));
#44917=CARTESIAN_POINT('Ctrl Pts',(-1.86861172784556,72.6159862597669,11.6395268720491));
#44918=CARTESIAN_POINT('Ctrl Pts',(-1.81493788397145,72.6277561592409,11.5790104567026));
#44919=CARTESIAN_POINT('Ctrl Pts',(-1.75840840698191,72.6394863199071,11.5211937322117));
#44920=CARTESIAN_POINT('Ctrl Pts',(-1.69919068199487,72.6511529581679,11.466250439536));
#44921=CARTESIAN_POINT('Ctrl Pts',(-1.69344502147043,72.6522849257152,11.4609195101922));
#44922=CARTESIAN_POINT('Ctrl Pts',(-1.6876740131914,72.6534162979526,11.4556156325558));
#44923=CARTESIAN_POINT('Ctrl Pts',(-1.68187778389141,72.6545470548966,11.4503389668807));
#44924=CARTESIAN_POINT('Ctrl Pts',(-1.6625817125446,72.6583114274805,11.4327725608484));
#44925=CARTESIAN_POINT('Ctrl Pts',(-1.64300627854001,72.6620688900243,11.4155075965675));
#44926=CARTESIAN_POINT('Ctrl Pts',(-1.62315600409785,72.665818536364,11.3985497211438));
#44927=CARTESIAN_POINT('Ctrl Pts',(-1.62315110236485,72.665819462284,11.3985455336461));
#44928=CARTESIAN_POINT('Ctrl Pts',(-1.62314620061507,72.6658203882035,11.3985413461672));
#44929=CARTESIAN_POINT('Ctrl Pts',(-1.62314129884852,72.6658213141225,11.3985371587071));
#44930=CARTESIAN_POINT('Ctrl Pts',(-1.56082317157978,72.6775928945893,11.3453002953787));
#44931=CARTESIAN_POINT('Ctrl Pts',(-1.4957944859709,72.6892892859298,11.2950882784085));
#44932=CARTESIAN_POINT('Ctrl Pts',(-1.42828733292841,72.7009656441407,11.248104005016));
#44933=CARTESIAN_POINT('Ctrl Pts',(-1.42332600423477,72.7018237791445,11.2446509720673));
#44934=CARTESIAN_POINT('Ctrl Pts',(-1.41835128774641,72.7026818042154,11.2412153962897));
#44935=CARTESIAN_POINT('Ctrl Pts',(-1.41336327554541,72.7035397404235,11.2377973692778));
#44936=CARTESIAN_POINT('Ctrl Pts',(-1.37712182632814,72.7097732559532,11.2129629768617));
#44937=CARTESIAN_POINT('Ctrl Pts',(-1.34017883736149,72.7160017706803,11.1890540941832));
#44938=CARTESIAN_POINT('Ctrl Pts',(-1.30257161362189,72.7222311870257,11.1661042373544));
#44939=CARTESIAN_POINT('Ctrl Pts',(-1.22666037836876,72.7348054385303,11.1197793080582));
#44940=CARTESIAN_POINT('Ctrl Pts',(-1.14844789582755,72.7473182678509,11.0776095001034));
#44941=CARTESIAN_POINT('Ctrl Pts',(-1.06832128165793,72.7597986771855,11.0397427669342));
#44942=CARTESIAN_POINT('Ctrl Pts',(-0.988194667488308,72.77227908652,11.0018760337651));
#44943=CARTESIAN_POINT('Ctrl Pts',(-0.906154741620227,72.7847267457644,
10.9683124889373));
#44944=CARTESIAN_POINT('Ctrl Pts',(-0.822570907356569,72.797146478726,10.9391908917457));
#44945=CARTESIAN_POINT('Ctrl Pts',(-0.822568759051828,72.7971467979429,
10.9391901432509));
#44946=CARTESIAN_POINT('Ctrl Pts',(-0.822566610745908,72.7971471171598,
10.939189394759));
#44947=CARTESIAN_POINT('Ctrl Pts',(-0.822564462439122,72.7971474363766,
10.9391886462701));
#44948=CARTESIAN_POINT('Ctrl Pts',(-0.739122321522642,72.8095461018663,
10.9101166724656));
#44949=CARTESIAN_POINT('Ctrl Pts',(-0.654138804942838,72.8219169139849,
10.8854698603914));
#44950=CARTESIAN_POINT('Ctrl Pts',(-0.567970639269384,72.834291747492,10.8653654129984));
#44951=CARTESIAN_POINT('Ctrl Pts',(-0.500847214011987,72.843931516489,10.8497044161397));
#44952=CARTESIAN_POINT('Ctrl Pts',(-0.433005218202936,72.8535732672548,
10.8368000881515));
#44953=CARTESIAN_POINT('Ctrl Pts',(-0.364614729086927,72.8632238157735,
10.8267114737518));
#44954=CARTESIAN_POINT('Ctrl Pts',(-0.277028957441099,72.8755830012354,
10.8137912696642));
#44955=CARTESIAN_POINT('Ctrl Pts',(-0.18900998836863,72.8878915084906,10.8055572567933));
#44956=CARTESIAN_POINT('Ctrl Pts',(-0.10091689812988,72.9001498719571,10.801991568242));
#44957=CARTESIAN_POINT('Ctrl Pts',(-0.0373380391023907,72.9089970217237,
10.7994181267937));
#44958=CARTESIAN_POINT('Ctrl Pts',(0.0262801750454052,72.9178176922334,
10.799276294681));
#44959=CARTESIAN_POINT('Ctrl Pts',(0.0898160120563695,72.9266083378267,
10.8015639694048));
#44960=CARTESIAN_POINT('Ctrl Pts',(0.0898329310713154,72.9266106786955,
10.8015645785917));
#44961=CARTESIAN_POINT('Ctrl Pts',(0.089849850080472,72.9266130195624,10.8015651879512));
#44962=CARTESIAN_POINT('Ctrl Pts',(0.0898667690838388,72.9266153604271,
10.801565797483));
#44963=CARTESIAN_POINT('Ctrl Pts',(0.173797377113533,72.9382277583191,10.8045895205693));
#44964=CARTESIAN_POINT('Ctrl Pts',(0.257587847717748,72.949789154405,10.8118537130972));
#44965=CARTESIAN_POINT('Ctrl Pts',(0.340913817027985,72.961344531577,10.8233359098749));
#44966=CARTESIAN_POINT('Ctrl Pts',(0.347489815953519,72.9622564699379,10.8242420729151));
#44967=CARTESIAN_POINT('Ctrl Pts',(0.354062906104864,72.9631683688201,10.825174528162));
#44968=CARTESIAN_POINT('Ctrl Pts',(0.360632919580723,72.9640802493081,10.8261332753483));
#44969=CARTESIAN_POINT('Ctrl Pts',(0.450469841210252,72.9765491028715,10.8392429738528));
#44970=CARTESIAN_POINT('Ctrl Pts',(0.539734065831612,72.9890148357778,10.8572646821544));
#44971=CARTESIAN_POINT('Ctrl Pts',(0.627990142466835,73.0015094525903,10.880171520626));
#44972=CARTESIAN_POINT('Ctrl Pts',(0.713329773984111,73.0135911815249,10.9023213966338));
#44973=CARTESIAN_POINT('Ctrl Pts',(0.797276335746133,73.0256362234166,10.9289218151932));
#44974=CARTESIAN_POINT('Ctrl Pts',(0.879477830991702,73.0376544768961,10.9598058078935));
#44975=CARTESIAN_POINT('Ctrl Pts',(0.962586973041719,73.0498054326986,10.9910308133356));
#44976=CARTESIAN_POINT('Ctrl Pts',(1.04391188025697,73.0619286698602,11.0266334838925));
#44977=CARTESIAN_POINT('Ctrl Pts',(1.12311984382727,73.0740196943337,11.0664543810062));
#44978=CARTESIAN_POINT('Ctrl Pts',(1.17162970886691,73.0814246816476,11.0908421604374));
#44979=CARTESIAN_POINT('Ctrl Pts',(1.21934622802924,73.0888173197235,11.1168123983187));
#44980=CARTESIAN_POINT('Ctrl Pts',(1.26619905011251,73.0961947466003,11.144333929718));
#44981=CARTESIAN_POINT('Ctrl Pts',(1.2662122340189,73.096196822533,11.1443416739963));
#44982=CARTESIAN_POINT('Ctrl Pts',(1.26622541785702,73.0961988984646,11.1443494183977));
#44983=CARTESIAN_POINT('Ctrl Pts',(1.26623860162657,73.0962009743949,11.1443571629219));
#44984=CARTESIAN_POINT('Ctrl Pts',(1.33721083186637,73.1073763371073,11.1860482858601));
#44985=CARTESIAN_POINT('Ctrl Pts',(1.40620421057854,73.118517965937,11.2313013178963));
#44986=CARTESIAN_POINT('Ctrl Pts',(1.47294802842284,73.129664939284,11.2799795122737));
#44987=CARTESIAN_POINT('Ctrl Pts',(1.47787170560366,73.1304872491259,11.2835704922715));
#44988=CARTESIAN_POINT('Ctrl Pts',(1.48278311839773,73.1313095863343,11.2871801191278));
#44989=CARTESIAN_POINT('Ctrl Pts',(1.48768214735287,73.1321319657744,11.2908083410286));
#44990=CARTESIAN_POINT('Ctrl Pts',(1.49825461608264,73.1339067217503,11.2986383136501));
#44991=CARTESIAN_POINT('Ctrl Pts',(1.50876946429231,73.1356816487118,11.3065548228557));
#44992=CARTESIAN_POINT('Ctrl Pts',(1.51922552872597,73.1374568675363,11.3145572867525));
#44993=CARTESIAN_POINT('Ctrl Pts',(1.58901016748647,73.1493048247839,11.367966392614));
#44994=CARTESIAN_POINT('Ctrl Pts',(1.6558133367778,73.1611056721388,11.4249265632611));
#44995=CARTESIAN_POINT('Ctrl Pts',(1.71937633086119,73.1728854036747,11.4851486463954));
#44996=CARTESIAN_POINT('Ctrl Pts',(1.78370884880155,73.1848077462468,11.5460998067287));
#44997=CARTESIAN_POINT('Ctrl Pts',(1.84472166146891,73.1967082083627,11.6103916638963));
#44998=CARTESIAN_POINT('Ctrl Pts',(1.90215787333205,73.2085975648045,11.6777304363509));
#44999=CARTESIAN_POINT('Ctrl Pts',(1.95944319604363,73.2204556870329,11.7448923048993));
#45000=CARTESIAN_POINT('Ctrl Pts',(2.01317077029276,73.2323024404982,11.8150840358726));
#45001=CARTESIAN_POINT('Ctrl Pts',(2.06310091360915,73.2441369028791,11.8880333691187));
#45002=CARTESIAN_POINT('Ctrl Pts',(2.08930829682315,73.2503485872474,11.9263230876054));
#45003=CARTESIAN_POINT('Ctrl Pts',(2.11446974771244,73.2565567214177,11.9653729420136));
#45004=CARTESIAN_POINT('Ctrl Pts',(2.13855173663704,73.2627603494946,12.0051473198796));
#45005=CARTESIAN_POINT('Ctrl Pts',(2.13855545002762,73.2627613060806,12.0051534530026));
#45006=CARTESIAN_POINT('Ctrl Pts',(2.13855916339253,73.2627622626665,12.0051595861428));
#45007=CARTESIAN_POINT('Ctrl Pts',(2.13856287673177,73.2627632192523,12.0051657193003));
#45008=CARTESIAN_POINT('Ctrl Pts',(2.14921639855088,73.2655076514524,12.0227616679975));
#45009=CARTESIAN_POINT('Ctrl Pts',(2.15965867181997,73.2682511993657,12.0404994742902));
#45010=CARTESIAN_POINT('Ctrl Pts',(2.16988667557105,73.2709944723947,12.0583756525207));
#45011=CARTESIAN_POINT('Ctrl Pts',(2.21320796727965,73.2826137613602,12.134091222304));
#45012=CARTESIAN_POINT('Ctrl Pts',(2.25246284353253,73.2941696184544,12.2119000238158));
#45013=CARTESIAN_POINT('Ctrl Pts',(2.28753354557419,73.3056990189531,12.2914562562454));
#45014=CARTESIAN_POINT('Ctrl Pts',(2.32315205883524,73.3174085109408,12.3722551725723));
#45015=CARTESIAN_POINT('Ctrl Pts',(2.35445375262732,73.3290905463094,12.4548560009577));
#45016=CARTESIAN_POINT('Ctrl Pts',(2.38131295547122,73.3407678264489,12.5388879834489));
#45017=CARTESIAN_POINT('Ctrl Pts',(2.4082565505562,73.3524817968746,12.6231839963867));
#45018=CARTESIAN_POINT('Ctrl Pts',(2.43072946898995,73.3641907263945,12.7089192493945));
#45019=CARTESIAN_POINT('Ctrl Pts',(2.44861131043191,73.3759047830073,12.7957222680304));
#45020=CARTESIAN_POINT('Ctrl Pts',(2.46205090276032,73.384708806122,12.8609614765945));
#45021=CARTESIAN_POINT('Ctrl Pts',(2.47289742868133,73.3935154323392,12.9268037870214));
#45022=CARTESIAN_POINT('Ctrl Pts',(2.48110148774651,73.4023256647204,12.9930975741823));
#45023=CARTESIAN_POINT('Ctrl Pts',(2.48868454997462,73.410469016671,13.0543733291939));
#45024=CARTESIAN_POINT('Ctrl Pts',(2.4939825627341,73.4185856930003,13.1158109652438));
#45025=CARTESIAN_POINT('Ctrl Pts',(2.49700513073167,73.4266755909545,13.1772949549708));
#45026=CARTESIAN_POINT('Ctrl Pts',(2.49700633378398,73.4266788109219,13.1773194270277));
#45027=CARTESIAN_POINT('Ctrl Pts',(2.49700753647547,73.4266820308852,13.1773438990924));
#45028=CARTESIAN_POINT('Ctrl Pts',(2.49700873880609,73.4266852508442,13.1773683711644));
#45029=CARTESIAN_POINT('Ctrl Pts',(2.50129482405442,73.4381638064985,13.2646067605123));
#45030=CARTESIAN_POINT('Ctrl Pts',(2.50099985775013,73.4495894794228,13.351942076957));
#45031=CARTESIAN_POINT('Ctrl Pts',(2.49614920214244,73.4609924753731,13.4390156985328));
#45032=CARTESIAN_POINT('Ctrl Pts',(2.49123082008854,73.4725546836968,13.5273050706022));
#45033=CARTESIAN_POINT('Ctrl Pts',(2.48162827059325,73.4840933815966,13.615324511331));
#45034=CARTESIAN_POINT('Ctrl Pts',(2.46736827501081,73.4956279218977,13.7026915579614));
#45035=CARTESIAN_POINT('Ctrl Pts',(2.45828319561121,73.5029766068162,13.758353325243));
#45036=CARTESIAN_POINT('Ctrl Pts',(2.44730774964432,73.5103233663213,13.8137501608377));
#45037=CARTESIAN_POINT('Ctrl Pts',(2.43444902403012,73.5176713013572,13.8687838814702));
#45038=CARTESIAN_POINT('Ctrl Pts',(2.43444379905134,73.5176742870967,13.868806243719));
#45039=CARTESIAN_POINT('Ctrl Pts',(2.43443857376157,73.5176772728363,13.8688286059079));
#45040=CARTESIAN_POINT('Ctrl Pts',(2.4344333481608,73.5176802585762,13.8688509680369));
#45041=CARTESIAN_POINT('Ctrl Pts',(2.42629390065555,73.5223308765159,13.9036824415316));
#45042=CARTESIAN_POINT('Ctrl Pts',(2.41740001942849,73.5269819505898,13.9383685490922));
#45043=CARTESIAN_POINT('Ctrl Pts',(2.40775379177636,73.5316350026151,13.97288380081));
#45044=CARTESIAN_POINT('Ctrl Pts',(2.3841740531368,73.5430091640584,14.0572546703289));
#45045=CARTESIAN_POINT('Ctrl Pts',(2.35622043358093,73.5543371678204,14.1401690110613));
#45046=CARTESIAN_POINT('Ctrl Pts',(2.32406085243493,73.5656353612939,14.2212942630802));
#45047=CARTESIAN_POINT('Ctrl Pts',(2.2913907848197,73.5771128971186,14.3037072602124));
#45048=CARTESIAN_POINT('Ctrl Pts',(2.25438096393225,73.5885594153825,14.3842733082134));
#45049=CARTESIAN_POINT('Ctrl Pts',(2.21319922707366,73.5999856891628,14.4626643216925));
#45050=CARTESIAN_POINT('Ctrl Pts',(2.20371695763857,73.6026166371239,14.480714184758));
#45051=CARTESIAN_POINT('Ctrl Pts',(2.19401343862176,73.605246494746,14.4986488374847));
#45052=CARTESIAN_POINT('Ctrl Pts',(2.18409057163531,73.6078753689123,14.5164644639377));
#45053=CARTESIAN_POINT('Ctrl Pts',(2.1840784998516,73.607878567101,14.5164861377533));
#45054=CARTESIAN_POINT('Ctrl Pts',(2.18406642774296,73.6078817652882,14.5165078113925));
#45055=CARTESIAN_POINT('Ctrl Pts',(2.18405435530939,73.607884963474,14.5165294848555));
#45056=CARTESIAN_POINT('Ctrl Pts',(2.14099860687478,73.619291137893,14.5938268385608));
#45057=CARTESIAN_POINT('Ctrl Pts',(2.09381259199541,73.6306795804414,14.6688854275725));
#45058=CARTESIAN_POINT('Ctrl Pts',(2.04266511848951,73.6420734746669,14.7413688003259));
#45059=CARTESIAN_POINT('Ctrl Pts',(2.01737742112873,73.6477067020619,14.7772051274842));
#45060=CARTESIAN_POINT('Ctrl Pts',(1.99112157182045,73.6533411159011,14.8124116242157));
#45061=CARTESIAN_POINT('Ctrl Pts',(1.96391898866646,73.6589787854801,14.8469461788497));
#45062=CARTESIAN_POINT('Ctrl Pts',(1.90940688591095,73.6702762869583,14.9161510473789));
#45063=CARTESIAN_POINT('Ctrl Pts',(1.85137529467586,73.6815288812977,14.9822992683596));
#45064=CARTESIAN_POINT('Ctrl Pts',(1.79010475237028,73.6927498506299,15.0451480084304));
#45065=CARTESIAN_POINT('Ctrl Pts',(1.78185427612238,73.6942608269893,15.0536109992519));
#45066=CARTESIAN_POINT('Ctrl Pts',(1.77354504249908,73.6957712246937,15.0620141917625));
#45067=CARTESIAN_POINT('Ctrl Pts',(1.76517770766173,73.69728107206,15.0703570203222));
#45068=CARTESIAN_POINT('Ctrl Pts',(1.76516281634345,73.6972837591304,15.0703718680267));
#45069=CARTESIAN_POINT('Ctrl Pts',(1.76514792484096,73.6972864461991,15.0703867155399));
#45070=CARTESIAN_POINT('Ctrl Pts',(1.76513303315425,73.697289133266,15.0704015628617));
#45071=CARTESIAN_POINT('Ctrl Pts',(1.7025265980138,73.7085858846769,15.1328214825145));
#45072=CARTESIAN_POINT('Ctrl Pts',(1.63666761921622,73.7198522934615,15.191861541058));
#45073=CARTESIAN_POINT('Ctrl Pts',(1.56784913211618,73.7311046927559,15.2472707152904));
#45074=CARTESIAN_POINT('Ctrl Pts',(1.49913127904375,73.7423406375436,15.3025988640804));
#45075=CARTESIAN_POINT('Ctrl Pts',(1.42746360530328,73.7535623546263,15.3543065322117));
#45076=CARTESIAN_POINT('Ctrl Pts',(1.35312935194537,73.7647828589483,15.4021541708615));
#45077=CARTESIAN_POINT('Ctrl Pts',(1.3098499907358,73.7713157322547,15.4300123269955));
#45078=CARTESIAN_POINT('Ctrl Pts',(1.26566646222046,73.7778481545506,15.4565622280442));
#45079=CARTESIAN_POINT('Ctrl Pts',(1.22063096628485,73.7843827064178,15.4817579816506));
#45080=CARTESIAN_POINT('Ctrl Pts',(1.21708536945061,73.7848971647563,15.4837416166116));
#45081=CARTESIAN_POINT('Ctrl Pts',(1.21353533127665,73.7854115143304,15.4857163878051));
#45082=CARTESIAN_POINT('Ctrl Pts',(1.20998088303043,73.7859257565345,15.4876822852714));
#45083=CARTESIAN_POINT('Ctrl Pts',(1.20995800480846,73.7859290664568,15.4876949387792));
#45084=CARTESIAN_POINT('Ctrl Pts',(1.20993512640368,73.7859323763746,15.487707591919));
#45085=CARTESIAN_POINT('Ctrl Pts',(1.20991224781601,73.7859356862879,15.4877202446908));
#45086=CARTESIAN_POINT('Ctrl Pts',(1.13371903175926,73.796958785634,15.5298581332995));
#45087=CARTESIAN_POINT('Ctrl Pts',(1.05549763345003,73.8079332466301,15.5679199945778));
#45088=CARTESIAN_POINT('Ctrl Pts',(0.975580932636508,73.8188805221497,15.6017912055059));
#45089=CARTESIAN_POINT('Ctrl Pts',(0.894288616358889,73.8300162343958,15.6362454455264));
#45090=CARTESIAN_POINT('Ctrl Pts',(0.81124264483813,73.8411236031648,15.666362331274));
#45091=CARTESIAN_POINT('Ctrl Pts',(0.726813507581337,73.8522184547178,15.6920161130511));
#45092=CARTESIAN_POINT('Ctrl Pts',(0.641886281410767,73.8633787602448,15.7178212390764));
#45093=CARTESIAN_POINT('Ctrl Pts',(0.55556052045207,73.874526150366,15.7391099440483));
#45094=CARTESIAN_POINT('Ctrl Pts',(0.46822177286561,73.8856735115328,15.7557622194446));
#45095=CARTESIAN_POINT('Ctrl Pts',(0.410327112081077,73.8930628170957,15.7668005943011));
#45096=CARTESIAN_POINT('Ctrl Pts',(0.351987503949557,73.9004520504417,15.7758019757087));
#45097=CARTESIAN_POINT('Ctrl Pts',(0.293313731830431,73.9078450103692,15.7827337846194));
#45098=CARTESIAN_POINT('Ctrl Pts',(0.212594966547678,73.9180156637221,15.7922700226392));
#45099=CARTESIAN_POINT('Ctrl Pts',(0.1316293840294,73.9281449406435,15.7978439249359));
#45100=CARTESIAN_POINT('Ctrl Pts',(0.050695235931738,73.938245163729,15.7994858904266));
#45101=CARTESIAN_POINT('Ctrl Pts',(0.0428563290129143,73.9392234245804,
15.7996449236029));
#45102=CARTESIAN_POINT('Ctrl Pts',(0.0350176857552271,73.9402014153011,
15.7997670460444));
#45103=CARTESIAN_POINT('Ctrl Pts',(0.0271795394711455,73.9411791486449,
15.7998522684778));
#45104=CARTESIAN_POINT('Ctrl Pts',(-0.0255788911773204,73.9477602553177,
15.8004258992424));
#45105=CARTESIAN_POINT('Ctrl Pts',(-0.0783141785358755,73.9543296457411,
15.7993291913896));
#45106=CARTESIAN_POINT('Ctrl Pts',(-0.130959639856642,73.9608916989189,
15.796567664907));
#45107=CARTESIAN_POINT('Ctrl Pts',(-0.13098453186807,73.9608948016119,15.7965663591924));
#45108=CARTESIAN_POINT('Ctrl Pts',(-0.131009423859538,73.9608979043032,
15.7965650531051));
#45109=CARTESIAN_POINT('Ctrl Pts',(-0.131034315831042,73.9609010069929,
15.7965637466453));
#45110=CARTESIAN_POINT('Ctrl Pts',(-0.211918936036267,73.9709829677021,
15.7923185018661));
#45111=CARTESIAN_POINT('Ctrl Pts',(-0.292595669761997,73.9810480981651,
15.7841419162165));
#45112=CARTESIAN_POINT('Ctrl Pts',(-0.372786814204804,73.9911084885637,
15.772049757157));
#45113=CARTESIAN_POINT('Ctrl Pts',(-0.383722757406466,73.9924804587326,
15.7704007076818));
#45114=CARTESIAN_POINT('Ctrl Pts',(-0.394649613821351,73.9938523337729,
15.7686787817984));
#45115=CARTESIAN_POINT('Ctrl Pts',(-0.405566624343431,73.9952241377399,
15.76688396919));
#45116=CARTESIAN_POINT('Ctrl Pts',(-0.490543523113661,74.0059021201968,
15.7529133305225));
#45117=CARTESIAN_POINT('Ctrl Pts',(-0.574926649123603,74.0165760349966,
15.7345293361135));
#45118=CARTESIAN_POINT('Ctrl Pts',(-0.658346101382832,74.0272568189175,
15.7117584487786));
#45119=CARTESIAN_POINT('Ctrl Pts',(-0.664252883748156,74.0280131061431,
15.7101460829322));
#45120=CARTESIAN_POINT('Ctrl Pts',(-0.670154819025069,74.0287694265211,
15.708511706861));
#45121=CARTESIAN_POINT('Ctrl Pts',(-0.676051768597265,74.0295257833444,
15.7068553232257));
#45122=CARTESIAN_POINT('Ctrl Pts',(-0.761266198022221,74.0404555893987,
15.682919594309));
#45123=CARTESIAN_POINT('Ctrl Pts',(-0.845001135821688,74.0513368367019,
15.6545158815446));
#45124=CARTESIAN_POINT('Ctrl Pts',(-0.926893964906226,74.0621824056608,
15.6218235710098));
#45125=CARTESIAN_POINT('Ctrl Pts',(-1.0095880665815,74.0731340920568,15.5888113856745));
#45126=CARTESIAN_POINT('Ctrl Pts',(-1.09040311035051,74.0840491747836,15.551427350259));
#45127=CARTESIAN_POINT('Ctrl Pts',(-1.16899335196819,74.0949453898928,15.5098545427027));
#45128=CARTESIAN_POINT('Ctrl Pts',(-1.2413646583252,74.1049793750996,15.4715714387212));
#45129=CARTESIAN_POINT('Ctrl Pts',(-1.31184946361676,74.1149972811528,15.4297368908981));
#45130=CARTESIAN_POINT('Ctrl Pts',(-1.38020314453495,74.1250185438341,15.3844786621361));
#45131=CARTESIAN_POINT('Ctrl Pts',(-1.38570105997187,74.1258245875476,15.3808383912507));
#45132=CARTESIAN_POINT('Ctrl Pts',(-1.39118519146044,74.1266306550172,15.3771759430737));
#45133=CARTESIAN_POINT('Ctrl Pts',(-1.39665541301641,74.1274367574286,15.3734913694022));
#45134=CARTESIAN_POINT('Ctrl Pts',(-1.40873566158579,74.1292169261846,15.3653544840187));
#45135=CARTESIAN_POINT('Ctrl Pts',(-1.42074812250748,74.1309972723805,15.3571097738254));
#45136=CARTESIAN_POINT('Ctrl Pts',(-1.43269150113015,74.1327779285501,15.3487578372105));
#45137=CARTESIAN_POINT('Ctrl Pts',(-1.43270814395231,74.1327804098533,15.3487461989798));
#45138=CARTESIAN_POINT('Ctrl Pts',(-1.4327247866403,74.1327828911572,15.3487345605409));
#45139=CARTESIAN_POINT('Ctrl Pts',(-1.43274142919412,74.1327853724616,15.3487229218937));
#45140=CARTESIAN_POINT('Ctrl Pts',(-1.46975856779551,74.1383044046323,15.3228357039874));
#45141=CARTESIAN_POINT('Ctrl Pts',(-1.5061123792386,74.1438264387456,15.2959182353033));
#45142=CARTESIAN_POINT('Ctrl Pts',(-1.54175964813545,74.1493524052715,15.2679911113879));
#45143=CARTESIAN_POINT('Ctrl Pts',(-1.6106533329589,74.1600321630191,15.2140177627249));
#45144=CARTESIAN_POINT('Ctrl Pts',(-1.67655905716899,74.1706724236108,15.1565460532155));
#45145=CARTESIAN_POINT('Ctrl Pts',(-1.73922926765431,74.181279657172,15.0958498312479));
#45146=CARTESIAN_POINT('Ctrl Pts',(-1.8028790531229,74.1920526884952,15.0342048889847));
#45147=CARTESIAN_POINT('Ctrl Pts',(-1.86319023395297,74.2027913948432,14.9692341759712));
#45148=CARTESIAN_POINT('Ctrl Pts',(-1.91989961078423,74.2135052070296,14.901238251256));
#45149=CARTESIAN_POINT('Ctrl Pts',(-1.97679002714856,74.2242532220879,14.833025255729));
#45150=CARTESIAN_POINT('Ctrl Pts',(-2.03005504931108,74.2349759582558,14.761768665622));
#45151=CARTESIAN_POINT('Ctrl Pts',(-2.07943829573419,74.2456892501053,14.6877755540771));
#45152=CARTESIAN_POINT('Ctrl Pts',(-2.11265888379711,74.2528961852727,14.6379996714415));
#45153=CARTESIAN_POINT('Ctrl Pts',(-2.14412311571905,74.2600989861902,14.5869855056616));
#45154=CARTESIAN_POINT('Ctrl Pts',(-2.17375607155748,74.2673047803565,14.5348235657417));
#45155=CARTESIAN_POINT('Ctrl Pts',(-2.21313294035364,74.2768799848351,14.4655097289588));
#45156=CARTESIAN_POINT('Ctrl Pts',(-2.24909377318838,74.2864160170156,14.3944911231243));
#45157=CARTESIAN_POINT('Ctrl Pts',(-2.28156343766963,74.2959360987337,14.3220077550171));
#45158=CARTESIAN_POINT('Ctrl Pts',(-2.28538296352163,74.2970559809011,14.313481270289));
#45159=CARTESIAN_POINT('Ctrl Pts',(-2.28915416434354,74.2981756461493,14.3049344595523));
#45160=CARTESIAN_POINT('Ctrl Pts',(-2.29287690406189,74.2992951353138,14.2963676683204));
#45161=CARTESIAN_POINT('Ctrl Pts',(-2.29532894250337,74.3000325036698,14.2907250225784));
#45162=CARTESIAN_POINT('Ctrl Pts',(-2.29775996884127,74.3007697977115,14.2850737138729));
#45163=CARTESIAN_POINT('Ctrl Pts',(-2.30016994868297,74.3015070301832,14.2794138407622));
#45164=CARTESIAN_POINT('Ctrl Pts',(-2.30017588511715,74.3015088461868,14.2793998989592));
#45165=CARTESIAN_POINT('Ctrl Pts',(-2.30018182142352,74.30151066219,14.2793859571042));
#45166=CARTESIAN_POINT('Ctrl Pts',(-2.30018775760206,74.3015124781928,14.2793720151971));
#45167=CARTESIAN_POINT('Ctrl Pts',(-2.33233849075179,74.3113480687414,14.2038617303245));
#45168=CARTESIAN_POINT('Ctrl Pts',(-2.36074405274654,74.3211725286144,14.1268246655189));
#45169=CARTESIAN_POINT('Ctrl Pts',(-2.38530971244953,74.3309847983196,14.0485327517548));
#45170=CARTESIAN_POINT('Ctrl Pts',(-2.38694554546875,74.3316381996519,14.0433192749249));
#45171=CARTESIAN_POINT('Ctrl Pts',(-2.38856433300727,74.3322915452213,14.0381002387581));
#45172=CARTESIAN_POINT('Ctrl Pts',(-2.3901660393656,74.3329448339845,14.0328757259305));
#45173=CARTESIAN_POINT('Ctrl Pts',(-2.41620504186434,74.3435653747897,13.9479406179044));
#45174=CARTESIAN_POINT('Ctrl Pts',(-2.43773388193084,74.3541711231403,13.8615570689893));
#45175=CARTESIAN_POINT('Ctrl Pts',(-2.45462226753716,74.3647649634114,13.774103436091));
#45176=CARTESIAN_POINT('Ctrl Pts',(-2.46450513939925,74.3709643461332,13.7229266647905));
#45177=CARTESIAN_POINT('Ctrl Pts',(-2.47279885746805,74.3771597574519,13.6713840314169));
#45178=CARTESIAN_POINT('Ctrl Pts',(-2.47947793825715,74.3833528359836,13.619556771821));
#45179=CARTESIAN_POINT('Ctrl Pts',(-2.49102244893907,74.3940573121714,13.529975529894));
#45180=CARTESIAN_POINT('Ctrl Pts',(-2.49768369321288,74.4046996691395,13.4400022552948));
#45181=CARTESIAN_POINT('Ctrl Pts',(-2.49948904565975,74.4152986643673,13.3500644366634));
#45182=CARTESIAN_POINT('Ctrl Pts',(-2.49982311671675,74.4172599531699,13.3334219122705));
#45183=CARTESIAN_POINT('Ctrl Pts',(-2.49999094463134,74.4192197919804,13.3167805118867));
#45184=CARTESIAN_POINT('Ctrl Pts',(-2.49999273450874,74.4211783466184,13.3001428234969));
#45185=CARTESIAN_POINT('',(2.15550409125805,72.6022418966679,12.0345911582846));
#45186=CARTESIAN_POINT('Ctrl Pts',(-2.5,73.4944230382101,13.2999999999288));
#45187=CARTESIAN_POINT('Ctrl Pts',(-2.50000000000897,73.4583731784959,13.6151761185301));
#45188=CARTESIAN_POINT('Ctrl Pts',(-2.44039283535546,73.4225014456294,13.9276778727858));
#45189=CARTESIAN_POINT('Ctrl Pts',(-2.23465482786394,73.3616757179031,14.446910667989));
#45190=CARTESIAN_POINT('Ctrl Pts',(-2.11265258757116,73.3362988716897,14.6585864733192));
#45191=CARTESIAN_POINT('Ctrl Pts',(-1.75550076090336,73.2733885901009,15.1108832337171));
#45192=CARTESIAN_POINT('Ctrl Pts',(-1.49860366585412,73.2355210576777,15.3286502061438));
#45193=CARTESIAN_POINT('Ctrl Pts',(-0.939078089956608,73.1675993626938,
15.636954284236));
#45194=CARTESIAN_POINT('Ctrl Pts',(-0.647003862542713,73.1376911885021,
15.7340470175276));
#45195=CARTESIAN_POINT('Ctrl Pts',(-0.0128277743704004,73.0709254514597,
15.8223130833006));
#45196=CARTESIAN_POINT('Ctrl Pts',(0.325221648481027,73.0349016869927,15.8013488882042));
#45197=CARTESIAN_POINT('Ctrl Pts',(0.939142011172969,72.9724547021774,15.63627649858));
#45198=CARTESIAN_POINT('Ctrl Pts',(1.21262516272004,72.9457745378757,15.5067371850223));
#45199=CARTESIAN_POINT('Ctrl Pts',(1.72046847219534,72.8845201048941,15.1426523782178));
#45200=CARTESIAN_POINT('Ctrl Pts',(1.945263761033,72.8512055310555,14.9036470538047));
#45201=CARTESIAN_POINT('Ctrl Pts',(2.27198004299956,72.7954271071532,14.3826338374693));
#45202=CARTESIAN_POINT('Ctrl Pts',(2.38199997869102,72.7725349973656,14.1123955096302));
#45203=CARTESIAN_POINT('Ctrl Pts',(2.5119201936499,72.7193307811069,13.5126520122323));
#45204=CARTESIAN_POINT('Ctrl Pts',(2.51837495144558,72.6893801651482,13.1851696111672));
#45205=CARTESIAN_POINT('Ctrl Pts',(2.41016238116982,72.6410772644571,12.5720763393092));
#45206=CARTESIAN_POINT('Ctrl Pts',(2.30646714388487,72.6223614865806,12.2906341890378));
#45207=CARTESIAN_POINT('Ctrl Pts',(2.15571927943544,72.6016597320381,12.0339532440426));
#45208=CARTESIAN_POINT('Ctrl Pts',(2.15445813049926,72.6018264157545,12.0336790882568));
#45209=CARTESIAN_POINT('Ctrl Pts',(2.12210370708062,72.591658948342,11.9780546956726));
#45210=CARTESIAN_POINT('Ctrl Pts',(2.08752077496568,72.5813095705524,11.9238853360025));
#45211=CARTESIAN_POINT('Ctrl Pts',(2.0509269321179,72.5709431692347,11.8712295010138));
#45212=CARTESIAN_POINT('Ctrl Pts',(2.03728749051808,72.5670793518718,11.8516033527242));
#45213=CARTESIAN_POINT('Ctrl Pts',(2.02336834487594,72.5632131129879,11.8321870798604));
#45214=CARTESIAN_POINT('Ctrl Pts',(2.00917947777018,72.5593527877987,11.8129823910257));
#45215=CARTESIAN_POINT('Ctrl Pts',(1.96030681681733,72.5460561403124,11.7468330473801));
#45216=CARTESIAN_POINT('Ctrl Pts',(1.90823764456952,72.5328301919631,11.6831924744939));
#45217=CARTESIAN_POINT('Ctrl Pts',(1.85312925906669,72.5197047773732,11.6223047551265));
#45218=CARTESIAN_POINT('Ctrl Pts',(1.85312527945052,72.51970382953,11.6223003581595));
#45219=CARTESIAN_POINT('Ctrl Pts',(1.85312129981847,72.5197028816872,11.6222959612069));
#45220=CARTESIAN_POINT('Ctrl Pts',(1.85311732017056,72.519701933845,11.6222915642686));
#45221=CARTESIAN_POINT('Ctrl Pts',(1.7942232423232,72.5056749910705,11.5572220828988));
#45222=CARTESIAN_POINT('Ctrl Pts',(1.73185568354955,72.4917632956444,11.4952916200479));
#45223=CARTESIAN_POINT('Ctrl Pts',(1.66629232202317,72.477862964003,11.436689910296));
#45224=CARTESIAN_POINT('Ctrl Pts',(1.61017157037369,72.4659645951316,11.3865281747984));
#45225=CARTESIAN_POINT('Ctrl Pts',(1.55170855157011,72.4540746396689,11.3388064413359));
#45226=CARTESIAN_POINT('Ctrl Pts',(1.49107618687501,72.4421388638591,11.2936704800694));
#45227=CARTESIAN_POINT('Ctrl Pts',(1.47473442913998,72.4389219093886,11.2815053443722));
#45228=CARTESIAN_POINT('Ctrl Pts',(1.45825494632662,72.4357055846102,11.2695429552899));
#45229=CARTESIAN_POINT('Ctrl Pts',(1.44164222522493,72.4324890061798,11.2577849739746));
#45230=CARTESIAN_POINT('Ctrl Pts',(1.44163802710613,72.4324881933341,11.2577820026732));
#45231=CARTESIAN_POINT('Ctrl Pts',(1.44163382897881,72.4324873804884,11.2577790313848));
#45232=CARTESIAN_POINT('Ctrl Pts',(1.44162963084299,72.4324865676427,11.2577760601094));
#45233=CARTESIAN_POINT('Ctrl Pts',(1.37521144133417,72.4196266359719,11.2107678789212));
#45234=CARTESIAN_POINT('Ctrl Pts',(1.30666667510322,72.4067598510506,11.1670299991077));
#45235=CARTESIAN_POINT('Ctrl Pts',(1.23625365020321,72.3939459221504,11.1267718668503));
#45236=CARTESIAN_POINT('Ctrl Pts',(1.22694982289881,72.3922527896405,11.1214524716013));
#45237=CARTESIAN_POINT('Ctrl Pts',(1.21761330386815,72.3905605750161,11.1161938360422));
#45238=CARTESIAN_POINT('Ctrl Pts',(1.2082446220452,72.3888694115082,11.1109964525919));
#45239=CARTESIAN_POINT('Ctrl Pts',(1.14036038558841,72.3766154631266,11.0733368955954));
#45240=CARTESIAN_POINT('Ctrl Pts',(1.07079149767844,72.3644175511415,11.038891524946));
#45241=CARTESIAN_POINT('Ctrl Pts',(0.999720811602757,72.3523496936735,11.0078290960524));
#45242=CARTESIAN_POINT('Ctrl Pts',(0.986751010578721,72.3501474114277,11.0021604646613));
#45243=CARTESIAN_POINT('Ctrl Pts',(0.973731061205759,72.3479494491451,10.9966045351065));
#45244=CARTESIAN_POINT('Ctrl Pts',(0.960661896435918,72.345756241502,10.9911623947048));
#45245=CARTESIAN_POINT('Ctrl Pts',(0.9606449335591,72.3457533948694,10.991155331181));
#45246=CARTESIAN_POINT('Ctrl Pts',(0.960627970599397,72.3457505482448,10.9911482678487));
#45247=CARTESIAN_POINT('Ctrl Pts',(0.960611007556961,72.3457477016284,10.9911412047082));
#45248=CARTESIAN_POINT('Ctrl Pts',(0.886022931418177,72.333230864126,10.9600839185077));
#45249=CARTESIAN_POINT('Ctrl Pts',(0.809832831377722,72.3208701164345,10.9327281948738));
#45250=CARTESIAN_POINT('Ctrl Pts',(0.7323055728732,72.3085740050782,10.9091238268088));
#45251=CARTESIAN_POINT('Ctrl Pts',(0.726075529266496,72.307585897006,10.9072269940665));
#45252=CARTESIAN_POINT('Ctrl Pts',(0.719836858514145,72.3065982083406,10.9053544128214));
#45253=CARTESIAN_POINT('Ctrl Pts',(0.713589702597001,72.3056108926817,10.9035061226376));
#45254=CARTESIAN_POINT('Ctrl Pts',(0.673379385175608,72.2992559566807,10.8916094554244));
#45255=CARTESIAN_POINT('Ctrl Pts',(0.632817383828258,72.2929166400686,10.8807186627525));
#45256=CARTESIAN_POINT('Ctrl Pts',(0.591942311665562,72.2865819985053,10.8708446832849));
#45257=CARTESIAN_POINT('Ctrl Pts',(0.507625532162543,72.2735149493805,10.8504767155837));
#45258=CARTESIAN_POINT('Ctrl Pts',(0.422412951260775,72.2605329770767,10.8345398594402));
#45259=CARTESIAN_POINT('Ctrl Pts',(0.33668559964136,72.2475589406759,10.8230152507945));
#45260=CARTESIAN_POINT('Ctrl Pts',(0.249438792457217,72.2343549488239,10.8112863767608));
#45261=CARTESIAN_POINT('Ctrl Pts',(0.161658859339895,72.2211590214262,10.8041282715558));
#45262=CARTESIAN_POINT('Ctrl Pts',(0.0737499573133302,72.2079216664521,
10.8015392279642));
#45263=CARTESIAN_POINT('Ctrl Pts',(-0.0146879078865501,72.1946046600078,
10.7989346056463));
#45264=CARTESIAN_POINT('Ctrl Pts',(-0.103255890545628,72.1812457512613,
10.8009545224982));
#45265=CARTESIAN_POINT('Ctrl Pts',(-0.191543702703014,72.1678273720905,
10.8076072262273));
#45266=CARTESIAN_POINT('Ctrl Pts',(-0.261945025597524,72.1571274620844,
10.8129121390109));
#45267=CARTESIAN_POINT('Ctrl Pts',(-0.332168127949612,72.1463904176932,
10.8211629270956));
#45268=CARTESIAN_POINT('Ctrl Pts',(-0.402008476277773,72.1356216272196,
10.8323678267623));
#45269=CARTESIAN_POINT('Ctrl Pts',(-0.484673496677335,72.1228753808808,
10.8456302643317));
#45270=CARTESIAN_POINT('Ctrl Pts',(-0.566386256195227,72.1101482039065,
10.8629640088588));
#45271=CARTESIAN_POINT('Ctrl Pts',(-0.646852322776328,72.0974697133191,
10.884271690602));
#45272=CARTESIAN_POINT('Ctrl Pts',(-0.651699454506012,72.0967059837543,
10.8855552271864));
#45273=CARTESIAN_POINT('Ctrl Pts',(-0.656542070174611,72.0959424300872,
10.8868531973606));
#45274=CARTESIAN_POINT('Ctrl Pts',(-0.661380108236213,72.0951790584958,
10.8881655851328));
#45275=CARTESIAN_POINT('Ctrl Pts',(-0.739392118190532,72.0828699051925,
10.9093274707255));
#45276=CARTESIAN_POINT('Ctrl Pts',(-0.816212330200092,72.0706085631986,
10.9342339141927));
#45277=CARTESIAN_POINT('Ctrl Pts',(-0.891603421851303,72.0584372139234,
10.9628214631198));
#45278=CARTESIAN_POINT('Ctrl Pts',(-0.901590736687165,72.0568248338062,
10.9666085531495));
#45279=CARTESIAN_POINT('Ctrl Pts',(-0.911552999715001,72.0552140281018,
10.9704603129576));
#45280=CARTESIAN_POINT('Ctrl Pts',(-0.921489682736567,72.0536048903777,
10.9743766598092));
#45281=CARTESIAN_POINT('Ctrl Pts',(-0.994021229411912,72.0418591953921,
11.0029635326968));
#45282=CARTESIAN_POINT('Ctrl Pts',(-1.06518927731977,72.0302031485049,11.0349870929658));
#45283=CARTESIAN_POINT('Ctrl Pts',(-1.13480147812153,72.0186828733091,11.0704289949137));
#45284=CARTESIAN_POINT('Ctrl Pts',(-1.14228992685233,72.0174435935682,11.0742416148654));
#45285=CARTESIAN_POINT('Ctrl Pts',(-1.14976038127993,72.0162058813937,11.0780938409884));
#45286=CARTESIAN_POINT('Ctrl Pts',(-1.15721260825799,72.0149697915856,11.0819856863963));
#45287=CARTESIAN_POINT('Ctrl Pts',(-1.16161711955472,72.0142392218459,11.0842858950607));
#45288=CARTESIAN_POINT('Ctrl Pts',(-1.16601526471472,72.0135092220089,11.0865999397769));
#45289=CARTESIAN_POINT('Ctrl Pts',(-1.17040699608717,72.0127798043756,11.0889278231301));
#45290=CARTESIAN_POINT('Ctrl Pts',(-1.17045349071948,72.0127720821354,11.0889524680984));
#45291=CARTESIAN_POINT('Ctrl Pts',(-1.17049998463185,72.0127643599604,11.0889771146175));
#45292=CARTESIAN_POINT('Ctrl Pts',(-1.17054647782407,72.0127566378507,11.0890017626873));
#45293=CARTESIAN_POINT('Ctrl Pts',(-1.22414151324484,72.0038549744893,11.1174148294504));
#45294=CARTESIAN_POINT('Ctrl Pts',(-1.27678131669416,71.9950398375616,11.1478881495438));
#45295=CARTESIAN_POINT('Ctrl Pts',(-1.32836841847262,71.9862671759764,11.1803669383502));
#45296=CARTESIAN_POINT('Ctrl Pts',(-1.40093940038355,71.9739260937435,11.2260569948508));
#45297=CARTESIAN_POINT('Ctrl Pts',(-1.47105635823873,71.9617309526274,11.2754813921305));
#45298=CARTESIAN_POINT('Ctrl Pts',(-1.5384767452491,71.9495765345888,11.3283759101635));
#45299=CARTESIAN_POINT('Ctrl Pts',(-1.60737156169563,71.9371563092397,11.3824271886046));
#45300=CARTESIAN_POINT('Ctrl Pts',(-1.67344975408167,71.9247783255427,11.4401030369362));
#45301=CARTESIAN_POINT('Ctrl Pts',(-1.73642125199137,71.9123625028405,11.501119461988));
#45302=CARTESIAN_POINT('Ctrl Pts',(-1.80028155331662,71.899771438545,11.5629970958213));
#45303=CARTESIAN_POINT('Ctrl Pts',(-1.86094577837497,71.8871413296168,11.628310602362));
#45304=CARTESIAN_POINT('Ctrl Pts',(-1.91809433407489,71.8744245247237,11.6967512407477));
#45305=CARTESIAN_POINT('Ctrl Pts',(-1.96392142140589,71.8642269944227,11.7516333821051));
#45306=CARTESIAN_POINT('Ctrl Pts',(-2.00748733228005,71.8539744388831,11.8085259627929));
#45307=CARTESIAN_POINT('Ctrl Pts',(-2.04862610987012,71.8436589813961,11.8672641727492));
#45308=CARTESIAN_POINT('Ctrl Pts',(-2.09986880400616,71.8308099891837,11.940428819421));
#45309=CARTESIAN_POINT('Ctrl Pts',(-2.14707274256881,71.8179306430369,12.0160672188127));
#45310=CARTESIAN_POINT('Ctrl Pts',(-2.19005724799498,71.8050374183289,12.0937883678593));
#45311=CARTESIAN_POINT('Ctrl Pts',(-2.23039136752221,71.7929391782466,12.1667173008402));
#45312=CARTESIAN_POINT('Ctrl Pts',(-2.26701071556132,71.7808290987621,12.2414796872062));
#45313=CARTESIAN_POINT('Ctrl Pts',(-2.29978576562082,71.7687423985122,12.317785146074));
#45314=CARTESIAN_POINT('Ctrl Pts',(-2.3019788303873,71.767933645622,12.3228909449371));
#45315=CARTESIAN_POINT('Ctrl Pts',(-2.30415467623841,71.7671249960947,12.3280036706565));
#45316=CARTESIAN_POINT('Ctrl Pts',(-2.30631326117513,71.7663164599153,12.3331232439072));
#45317=CARTESIAN_POINT('Ctrl Pts',(-2.33713893790816,71.7547701573039,12.4062333204906));
#45318=CARTESIAN_POINT('Ctrl Pts',(-2.36444692199442,71.7432476571416,12.4807358856692));
#45319=CARTESIAN_POINT('Ctrl Pts',(-2.38813010461055,71.7317930452142,12.5564168134418));
#45320=CARTESIAN_POINT('Ctrl Pts',(-2.3903252254031,71.7307313527373,12.5634314440701));
#45321=CARTESIAN_POINT('Ctrl Pts',(-2.3924891886415,71.7296702404246,12.5704562304934));
#45322=CARTESIAN_POINT('Ctrl Pts',(-2.39462189759618,71.728609741501,12.5774910220215));
#45323=CARTESIAN_POINT('Ctrl Pts',(-2.41449867855878,71.7187259245978,12.6430550597279));
#45324=CARTESIAN_POINT('Ctrl Pts',(-2.43166303877302,71.7088961288796,12.7094857594791));
#45325=CARTESIAN_POINT('Ctrl Pts',(-2.44603814558137,71.6991533694695,12.776672391503));
#45326=CARTESIAN_POINT('Ctrl Pts',(-2.44771547507019,71.698016555818,12.7845119241514));
#45327=CARTESIAN_POINT('Ctrl Pts',(-2.44935385450317,71.6968815805346,12.7923572810489));
#45328=CARTESIAN_POINT('Ctrl Pts',(-2.45095344119494,71.6957483748995,12.800209101295));
#45329=CARTESIAN_POINT('Ctrl Pts',(-2.45096445588852,71.6957405716882,12.8002631686329));
#45330=CARTESIAN_POINT('Ctrl Pts',(-2.45097546874151,71.6957327685606,12.8003172362761));
#45331=CARTESIAN_POINT('Ctrl Pts',(-2.4509864797539,71.6957249655165,12.8003713042251));
#45332=CARTESIAN_POINT('Ctrl Pts',(-2.4665313781018,71.6847089460218,12.8767022300982));
#45333=CARTESIAN_POINT('Ctrl Pts',(-2.47841178654089,71.6738590388587,12.9536438912108));
#45334=CARTESIAN_POINT('Ctrl Pts',(-2.48665911936036,71.6630936615033,13.0309612316457));
#45335=CARTESIAN_POINT('Ctrl Pts',(-2.48753921184129,71.661944862507,13.0392119487504));
#45336=CARTESIAN_POINT('Ctrl Pts',(-2.48837788944345,71.6607970308485,13.0474669218202));
#45337=CARTESIAN_POINT('Ctrl Pts',(-2.48917516051926,71.6596500707978,13.055725848435));
#45338=CARTESIAN_POINT('Ctrl Pts',(-2.49695389712681,71.6484595229351,13.1363057374423));
#45339=CARTESIAN_POINT('Ctrl Pts',(-2.50079429925675,71.6373514085253,13.2172645178092));
#45340=CARTESIAN_POINT('Ctrl Pts',(-2.50070443670409,71.6262534957662,13.2983067811559));
#45341=CARTESIAN_POINT('Origin',(0.,70.2,13.3));
#45342=CARTESIAN_POINT('',(-2.5,69.6117391960828,13.3));
#45343=CARTESIAN_POINT('',(-2.5,70.6202795746371,13.2999999999956));
#45344=CARTESIAN_POINT('',(-2.5,70.2,13.3));
#45345=CARTESIAN_POINT('Ctrl Pts',(-2.5,70.6202795746371,13.2999999999913));
#45346=CARTESIAN_POINT('Ctrl Pts',(-2.49999999999947,70.6394456460639,13.1486673749071));
#45347=CARTESIAN_POINT('Ctrl Pts',(-2.48625904090408,70.6585193331841,12.9976404384911));
#45348=CARTESIAN_POINT('Ctrl Pts',(-2.43277840039442,70.6958945847908,12.7061947707861));
#45349=CARTESIAN_POINT('Ctrl Pts',(-2.39426039670762,70.7141226191345,12.5661508897012));
#45350=CARTESIAN_POINT('Ctrl Pts',(-2.23708478719293,70.7709350702978,12.1425981655169));
#45351=CARTESIAN_POINT('Ctrl Pts',(-2.07829814092921,70.8090280780769,11.8770361458128));
#45352=CARTESIAN_POINT('Ctrl Pts',(-1.77069185889503,70.8670676595898,11.5280733342784));
#45353=CARTESIAN_POINT('Ctrl Pts',(-1.6549314539226,70.8867415846239,11.4195003937804));
#45354=CARTESIAN_POINT('Ctrl Pts',(-1.26525622213921,70.9479573936792,11.118054283164));
#45355=CARTESIAN_POINT('Ctrl Pts',(-0.962448457501469,70.9889095280149,
10.9685860005634));
#45356=CARTESIAN_POINT('Ctrl Pts',(-0.486186479102335,71.0494139724573,
10.8426287696168));
#45357=CARTESIAN_POINT('Ctrl Pts',(-0.329670559905892,71.0687462970969,
10.8167820739238));
#45358=CARTESIAN_POINT('Ctrl Pts',(0.161889237777242,71.128988982311,10.7829299228129));
#45359=CARTESIAN_POINT('Ctrl Pts',(0.496807426143598,71.1695298547018,10.8271342670815));
#45360=CARTESIAN_POINT('Ctrl Pts',(1.1014511275559,71.2469243672991,11.0350979139091));
#45361=CARTESIAN_POINT('Ctrl Pts',(1.36924285129701,71.2830941470646,11.1861958203389));
#45362=CARTESIAN_POINT('Ctrl Pts',(1.72990593570642,71.3395640352817,11.4876309496461));
#45363=CARTESIAN_POINT('Ctrl Pts',(1.84578861765027,71.3593803596938,11.6057968048365));
#45364=CARTESIAN_POINT('Ctrl Pts',(2.15902370342132,71.4191843054308,11.9958066083007));
#45365=CARTESIAN_POINT('Ctrl Pts',(2.31422879170653,71.4581444197495,12.2966570788982));
#45366=CARTESIAN_POINT('Ctrl Pts',(2.44806458548582,71.5158413414613,12.769531453346));
#45367=CARTESIAN_POINT('Ctrl Pts',(2.47642740497632,71.5342550132755,12.9235405313664));
#45368=CARTESIAN_POINT('Ctrl Pts',(2.51941730600979,71.5915723186385,13.4083478783766));
#45369=CARTESIAN_POINT('Ctrl Pts',(2.48305857205729,71.6295278341907,13.7401103735801));
#45370=CARTESIAN_POINT('Ctrl Pts',(2.28238998188811,71.7056552055624,14.3733326516439));
#45371=CARTESIAN_POINT('Ctrl Pts',(2.1189046935722,71.7440471228116,14.6680650732052));
#45372=CARTESIAN_POINT('Ctrl Pts',(1.71002515174723,71.8159518735498,15.1476277313869));
#45373=CARTESIAN_POINT('Ctrl Pts',(1.47903131089068,71.8486182465415,15.3372565262688));
#45374=CARTESIAN_POINT('Ctrl Pts',(0.928478468424501,71.9190597988017,15.6451304526573));
#45375=CARTESIAN_POINT('Ctrl Pts',(0.606958837930968,71.9567847148786,15.7481355386928));
#45376=CARTESIAN_POINT('Ctrl Pts',(-0.0378388720561457,72.0279255245038,
15.8194089948512));
#45377=CARTESIAN_POINT('Ctrl Pts',(-0.354076081769428,72.0610798581294,
15.7946931162187));
#45378=CARTESIAN_POINT('Ctrl Pts',(-0.813266661607912,72.1130629684333,
15.6695326377008));
#45379=CARTESIAN_POINT('Ctrl Pts',(-0.964634150853069,72.1306784652811,
15.6120511075016));
#45380=CARTESIAN_POINT('Ctrl Pts',(-1.37312510352448,72.1796227011478,15.4097695389725));
#45381=CARTESIAN_POINT('Ctrl Pts',(-1.61173468465016,72.2096798993154,15.2336373042292));
#45382=CARTESIAN_POINT('Ctrl Pts',(-2.04379044445544,72.2747064014632,14.7779134858905));
#45383=CARTESIAN_POINT('Ctrl Pts',(-2.22259154982646,72.310090929242,14.4922558729459));
#45384=CARTESIAN_POINT('Ctrl Pts',(-2.44582943646689,72.3739624854953,13.8985393364112));
#45385=CARTESIAN_POINT('Ctrl Pts',(-2.50000000539873,72.402390189325,13.6004818691382));
#45386=CARTESIAN_POINT('Ctrl Pts',(-2.5,72.4321658707887,13.2999999550827));
#45387=CARTESIAN_POINT('Ctrl Pts',(-2.49999938929793,71.6258524055026,13.2982525704591));
#45388=CARTESIAN_POINT('Ctrl Pts',(-2.50013773453631,71.5989545908592,13.4961792984747));
#45389=CARTESIAN_POINT('Ctrl Pts',(-2.47677199854322,71.5721754987909,13.6933916855558));
#45390=CARTESIAN_POINT('Ctrl Pts',(-2.39349175089188,71.5230701261886,14.0389321059686));
#45391=CARTESIAN_POINT('Ctrl Pts',(-2.34218548439843,71.5010839175006,14.1882422837462));
#45392=CARTESIAN_POINT('Ctrl Pts',(-2.17431598654963,71.4439554442844,14.5587640397383));
#45393=CARTESIAN_POINT('Ctrl Pts',(-2.03801120145824,71.4089634905474,14.7692753447635));
#45394=CARTESIAN_POINT('Ctrl Pts',(-1.65111115326409,71.3302018808504,15.2067576317367));
#45395=CARTESIAN_POINT('Ctrl Pts',(-1.38144107517593,71.2870343870214,15.4103504312543));
#45396=CARTESIAN_POINT('Ctrl Pts',(-0.801244258773137,71.2005757838904,
15.6881556512127));
#45397=CARTESIAN_POINT('Ctrl Pts',(-0.500572500224744,71.1584637136106,
15.7687414164191));
#45398=CARTESIAN_POINT('Ctrl Pts',(0.096429653907802,71.0778933685252,15.8149329684114));
#45399=CARTESIAN_POINT('Ctrl Pts',(0.387429532898798,71.0407407905083,15.7867968746636));
#45400=CARTESIAN_POINT('Ctrl Pts',(0.966568824290719,70.9627806760956,15.6264248990345));
#45401=CARTESIAN_POINT('Ctrl Pts',(1.24784204597565,70.9223411990915,15.4884539371541));
#45402=CARTESIAN_POINT('Ctrl Pts',(1.70024609970173,70.8475039101213,15.1503512405443));
#45403=CARTESIAN_POINT('Ctrl Pts',(1.879538234941,70.8139614360242,14.9679420148664));
#45404=CARTESIAN_POINT('Ctrl Pts',(2.22344387612902,70.737775010458,14.4907052154775));
#45405=CARTESIAN_POINT('Ctrl Pts',(2.3624270599191,70.6956188391405,14.183427827997));
#45406=CARTESIAN_POINT('Ctrl Pts',(2.50678602477161,70.6122113201419,13.5528840412773));
#45407=CARTESIAN_POINT('Ctrl Pts',(2.51873350559229,70.5718831580062,13.2374213908898));
#45408=CARTESIAN_POINT('Ctrl Pts',(2.42603921610482,70.4918509984893,12.6214768694168));
#45409=CARTESIAN_POINT('Ctrl Pts',(2.32331680181175,70.4530237610246,12.3261872834063));
#45410=CARTESIAN_POINT('Ctrl Pts',(2.08831773288123,70.3934112066731,11.9160204105586));
#45411=CARTESIAN_POINT('Ctrl Pts',(1.99384698139257,70.3729742695969,11.7830796893343));
#45412=CARTESIAN_POINT('Ctrl Pts',(1.66783097605583,70.3104879002622,11.4078770028622));
#45413=CARTESIAN_POINT('Ctrl Pts',(1.40010146279125,70.2690377384254,11.2020174536021));
#45414=CARTESIAN_POINT('Ctrl Pts',(0.957195817800658,70.2075114976101,10.9850495059801));
#45415=CARTESIAN_POINT('Ctrl Pts',(0.80824430601015,70.1877820793355,10.9289319082503));
#45416=CARTESIAN_POINT('Ctrl Pts',(0.332182962529846,70.1264957089557,10.7996944176321));
#45417=CARTESIAN_POINT('Ctrl Pts',(-0.00496502799410541,70.0855435982572,
10.7777216544529));
#45418=CARTESIAN_POINT('Ctrl Pts',(-0.631510731345653,70.007928039846,10.862817631781));
#45419=CARTESIAN_POINT('Ctrl Pts',(-0.917058190577315,69.9718426761726,
10.9552867834349));
#45420=CARTESIAN_POINT('Ctrl Pts',(-1.44432109297885,69.8988027482903,11.2374585300552));
#45421=CARTESIAN_POINT('Ctrl Pts',(-1.68138955700855,69.8626524387002,11.4256709683559));
#45422=CARTESIAN_POINT('Ctrl Pts',(-1.98219270859602,69.8077940472495,11.7685943223874));
#45423=CARTESIAN_POINT('Ctrl Pts',(-2.07378868692379,69.7891618773236,11.8951181545654));
#45424=CARTESIAN_POINT('Ctrl Pts',(-2.32283199014498,69.7303498246778,12.3170990858516));
#45425=CARTESIAN_POINT('Ctrl Pts',(-2.43327812336977,69.690515908006,12.6360336866484));
#45426=CARTESIAN_POINT('Ctrl Pts',(-2.49260078235443,69.6378455207597,13.0777903161134));
#45427=CARTESIAN_POINT('Ctrl Pts',(-2.5,69.6247727051849,13.1889492361916));
#45428=CARTESIAN_POINT('Ctrl Pts',(-2.5,69.6117391960828,13.3));
#45429=CARTESIAN_POINT('Origin',(0.,70.2,13.3));
#45430=CARTESIAN_POINT('',(-2.5,67.7617877809656,13.3000000230487));
#45431=CARTESIAN_POINT('',(-2.49999999984276,68.4536941147331,13.3000280391888));
#45432=CARTESIAN_POINT('',(-2.5,70.2,13.3));
#45433=CARTESIAN_POINT('',(-2.46701393303641,68.4808270900767,12.9018894245279));
#45434=CARTESIAN_POINT('Ctrl Pts',(-2.5,68.4536960240567,13.3));
#45435=CARTESIAN_POINT('Ctrl Pts',(-2.49999999999523,68.4582353924442,13.2333373963885));
#45436=CARTESIAN_POINT('Ctrl Pts',(-2.49733364133762,68.4627032333579,13.1666999747746));
#45437=CARTESIAN_POINT('Ctrl Pts',(-2.48667961645755,68.471683031839,13.0337855110735));
#45438=CARTESIAN_POINT('Ctrl Pts',(-2.47869585369853,68.4761914296149,12.967568059918));
#45439=CARTESIAN_POINT('Ctrl Pts',(-2.46807636330827,68.4808334773074,12.9017550190159));
#45440=CARTESIAN_POINT('',(-2.50001628522818,70.6201479917331,13.3010276898172));
#45441=CARTESIAN_POINT('Ctrl Pts',(-2.46710028502621,68.4807253128341,12.9017689911365));
#45442=CARTESIAN_POINT('Ctrl Pts',(-2.45701642861137,68.4909143573078,12.8376991620988));
#45443=CARTESIAN_POINT('Ctrl Pts',(-2.44427557470376,68.5012897672622,12.7741791907651));
#45444=CARTESIAN_POINT('Ctrl Pts',(-2.42907716009975,68.5116874000612,12.7113448092636));
#45445=CARTESIAN_POINT('Ctrl Pts',(-2.42367255572964,68.5153848312162,12.6890007041905));
#45446=CARTESIAN_POINT('Ctrl Pts',(-2.41795702470293,68.51908512482,12.6667428443687));
#45447=CARTESIAN_POINT('Ctrl Pts',(-2.41193893499027,68.5227810738497,12.644575871674));
#45448=CARTESIAN_POINT('Ctrl Pts',(-2.39162414618716,68.5352571962656,12.5697485775994));
#45449=CARTESIAN_POINT('Ctrl Pts',(-2.36786463113725,68.5476833482295,12.4959563733787));
#45450=CARTESIAN_POINT('Ctrl Pts',(-2.34072701070115,68.560051885539,12.4234391530385));
#45451=CARTESIAN_POINT('Ctrl Pts',(-2.34072148492479,68.560054404027,12.4234243870444));
#45452=CARTESIAN_POINT('Ctrl Pts',(-2.34071595900827,68.5600569225126,12.4234096211033));
#45453=CARTESIAN_POINT('Ctrl Pts',(-2.34071043295155,68.5600594409959,12.4233948552149));
#45454=CARTESIAN_POINT('Ctrl Pts',(-2.32462243553839,68.5673914959409,12.3804069552124));
#45455=CARTESIAN_POINT('Ctrl Pts',(-2.307346956239,68.5747029330603,12.3378665568768));
#45456=CARTESIAN_POINT('Ctrl Pts',(-2.28890451365498,68.5820029565785,12.295811501126));
#45457=CARTESIAN_POINT('Ctrl Pts',(-2.28889840876518,68.582005373061,12.2957975798962));
#45458=CARTESIAN_POINT('Ctrl Pts',(-2.28889230374749,68.5820077895422,12.2957836587196));
#45459=CARTESIAN_POINT('Ctrl Pts',(-2.28888619860188,68.5820102060222,12.2957697375963));
#45460=CARTESIAN_POINT('Ctrl Pts',(-2.27045717205942,68.5893046058984,12.2537473570202));
#45461=CARTESIAN_POINT('Ctrl Pts',(-2.25086289904019,68.5965877603358,12.2122098379469));
#45462=CARTESIAN_POINT('Ctrl Pts',(-2.23012083470916,68.6038595070499,12.1712137759273));
#45463=CARTESIAN_POINT('Ctrl Pts',(-2.23011422780498,68.6038618232964,12.1712007175813));
#45464=CARTESIAN_POINT('Ctrl Pts',(-2.23010762078434,68.6038641395417,12.1711876592902));
#45465=CARTESIAN_POINT('Ctrl Pts',(-2.23010101364719,68.6038664557859,12.1711746010541));
#45466=CARTESIAN_POINT('Ctrl Pts',(-2.19557652710775,68.6159696010891,12.102940979198));
#45467=CARTESIAN_POINT('Ctrl Pts',(-2.15787300844718,68.6280416842535,12.03620611478));
#45468=CARTESIAN_POINT('Ctrl Pts',(-2.11708179466995,68.6401060351926,11.9711914617286));
#45469=CARTESIAN_POINT('Ctrl Pts',(-2.10897264785992,68.642504384834,11.9582667821818));
#45470=CARTESIAN_POINT('Ctrl Pts',(-2.10074880264077,68.6449002213517,11.9454218985461));
#45471=CARTESIAN_POINT('Ctrl Pts',(-2.09241156316031,68.647293665484,11.9326581893751));
#45472=CARTESIAN_POINT('Ctrl Pts',(-2.09240410168288,68.6472958075155,11.9326467663941));
#45473=CARTESIAN_POINT('Ctrl Pts',(-2.09239664011459,68.647297949545,11.9326353434781));
#45474=CARTESIAN_POINT('Ctrl Pts',(-2.09238917845551,68.6473000915727,11.9326239206272));
#45475=CARTESIAN_POINT('Ctrl Pts',(-2.04472018782476,68.66098448729,11.859648759465));
#45476=CARTESIAN_POINT('Ctrl Pts',(-1.99334689902953,68.6745928541095,11.7893274485888));
#45477=CARTESIAN_POINT('Ctrl Pts',(-1.93851690543501,68.6881428727038,11.7219296825362));
#45478=CARTESIAN_POINT('Ctrl Pts',(-1.88304016296446,68.7018527209591,11.6537369240611));
#45479=CARTESIAN_POINT('Ctrl Pts',(-1.8240249662701,68.7155026501715,11.588536853598));
#45480=CARTESIAN_POINT('Ctrl Pts',(-1.7616944179658,68.7290851141273,11.5266064023743));
#45481=CARTESIAN_POINT('Ctrl Pts',(-1.75540230636181,68.7304562295978,11.5203546795612));
#45482=CARTESIAN_POINT('Ctrl Pts',(-1.74907637980759,68.7318266376466,11.5141362757948));
#45483=CARTESIAN_POINT('Ctrl Pts',(-1.74271684702026,68.733196317435,11.5079514767474));
#45484=CARTESIAN_POINT('Ctrl Pts',(-1.74270984886747,68.7331978246571,11.507944670875));
#45485=CARTESIAN_POINT('Ctrl Pts',(-1.74270285067398,68.7331993318784,11.5079378650433));
#45486=CARTESIAN_POINT('Ctrl Pts',(-1.7426958524398,68.7332008390987,11.5079310592522));
#45487=CARTESIAN_POINT('Ctrl Pts',(-1.67973330998321,68.7467611777024,11.4466999122221));
#45488=CARTESIAN_POINT('Ctrl Pts',(-1.61347719936441,68.7602523735259,11.3887599843362));
#45489=CARTESIAN_POINT('Ctrl Pts',(-1.54421130510449,68.773735668214,11.3343593984148));
#45490=CARTESIAN_POINT('Ctrl Pts',(-1.5076110920206,68.7808602634268,11.3056140388423));
#45491=CARTESIAN_POINT('Ctrl Pts',(-1.47017041061827,68.7879822034691,11.2778573990232));
#45492=CARTESIAN_POINT('Ctrl Pts',(-1.43193068565022,68.7951074030585,11.2511291391457));
#45493=CARTESIAN_POINT('Ctrl Pts',(-1.36025064822009,68.8084635287549,11.2010272445827));
#45494=CARTESIAN_POINT('Ctrl Pts',(-1.28613928825395,68.8217632664951,11.1548007140498));
#45495=CARTESIAN_POINT('Ctrl Pts',(-1.209937200357,68.8350248467504,11.1126014272649));
#45496=CARTESIAN_POINT('Ctrl Pts',(-1.13286004751762,68.8484387160607,11.0699175459304));
#45497=CARTESIAN_POINT('Ctrl Pts',(-1.05364415253597,68.8618133437034,11.0313536919916));
#45498=CARTESIAN_POINT('Ctrl Pts',(-0.97261117779691,68.875141448303,10.997073095939));
#45499=CARTESIAN_POINT('Ctrl Pts',(-0.919400315590347,68.8838934401879,
10.9745625059134));
#45500=CARTESIAN_POINT('Ctrl Pts',(-0.865405294095551,68.8926248332336,
10.9538989316396));
#45501=CARTESIAN_POINT('Ctrl Pts',(-0.810709125003197,68.9013283155877,
10.9351313915851));
#45502=CARTESIAN_POINT('Ctrl Pts',(-0.810708110977433,68.9013284769437,
10.935131043649));
#45503=CARTESIAN_POINT('Ctrl Pts',(-0.810707096951468,68.9013286382997,
10.9351306957136));
#45504=CARTESIAN_POINT('Ctrl Pts',(-0.810706082925222,68.9013287996557,
10.9351303477789));
#45505=CARTESIAN_POINT('Ctrl Pts',(-0.727629192316671,68.914548332826,10.9066248360828));
#45506=CARTESIAN_POINT('Ctrl Pts',(-0.642932326791323,68.9277049444459,
10.8824915327675));
#45507=CARTESIAN_POINT('Ctrl Pts',(-0.556971403557444,68.9408617620192,
10.8628491960142));
#45508=CARTESIAN_POINT('Ctrl Pts',(-0.544950324965995,68.9427016577777,
10.8601023423865));
#45509=CARTESIAN_POINT('Ctrl Pts',(-0.532904548884078,68.9445415150838,
10.8574433604609));
#45510=CARTESIAN_POINT('Ctrl Pts',(-0.520835071435796,68.9463814646041,
10.8548726168578));
#45511=CARTESIAN_POINT('Ctrl Pts',(-0.435403739039851,68.9594051716974,
10.8366761330245));
#45512=CARTESIAN_POINT('Ctrl Pts',(-0.349231485807851,68.9723675199397,
10.8229937466344));
#45513=CARTESIAN_POINT('Ctrl Pts',(-0.262694614641421,68.985299723341,10.8138246267049));
#45514=CARTESIAN_POINT('Ctrl Pts',(-0.173047108075527,68.9986967848907,
10.8043259156006));
#45515=CARTESIAN_POINT('Ctrl Pts',(-0.0830086539429363,69.0120614483157,
10.7996706163981));
#45516=CARTESIAN_POINT('Ctrl Pts',(0.00702312402538797,69.0253990666962,
10.7998740880398));
#45517=CARTESIAN_POINT('Ctrl Pts',(0.097054901993754,69.0387366850766,10.8000775596816));
#45518=CARTESIAN_POINT('Ctrl Pts',(0.187079837545918,69.0520469299655,10.8051391620622));
#45519=CARTESIAN_POINT('Ctrl Pts',(0.276724728185427,69.0653094366795,10.8150960485874));
#45520=CARTESIAN_POINT('Ctrl Pts',(0.276735596481498,69.0653110445888,10.8150972557325));
#45521=CARTESIAN_POINT('Ctrl Pts',(0.276746464771963,69.0653126524973,10.8150984629496));
#45522=CARTESIAN_POINT('Ctrl Pts',(0.276757333056906,69.0653142604051,10.8150996702387));
#45523=CARTESIAN_POINT('Ctrl Pts',(0.342204847938776,69.0749968894875,10.8223698212616));
#45524=CARTESIAN_POINT('Ctrl Pts',(0.407451436589961,69.0846537569479,10.8322500112889));
#45525=CARTESIAN_POINT('Ctrl Pts',(0.47233765325959,69.0943076633307,10.8447312387675));
#45526=CARTESIAN_POINT('Ctrl Pts',(0.557893594534456,69.1070368543661,10.8611884036326));
#45527=CARTESIAN_POINT('Ctrl Pts',(0.642377866330353,69.1196957004163,10.8820813114099));
#45528=CARTESIAN_POINT('Ctrl Pts',(0.725447266460774,69.1323140128587,10.9072645398335));
#45529=CARTESIAN_POINT('Ctrl Pts',(0.755066709573133,69.1368132314275,10.9162439377888));
#45530=CARTESIAN_POINT('Ctrl Pts',(0.784506363236137,69.1413070512098,10.925768961271));
#45531=CARTESIAN_POINT('Ctrl Pts',(0.813751012452173,69.145796031994,10.9358335828332));
#45532=CARTESIAN_POINT('Ctrl Pts',(0.813763275507918,69.1457979143425,10.9358378031955));
#45533=CARTESIAN_POINT('Ctrl Pts',(0.813775538529388,69.1457997966902,10.9358420236528));
#45534=CARTESIAN_POINT('Ctrl Pts',(0.813787801516542,69.1458016790371,10.935846244205));
#45535=CARTESIAN_POINT('Ctrl Pts',(0.900662829668634,69.1591368425563,10.9657460220978));
#45536=CARTESIAN_POINT('Ctrl Pts',(0.985816994502783,69.1724314404545,11.0004058925232));
#45537=CARTESIAN_POINT('Ctrl Pts',(1.06886499221508,69.1857090128889,11.0396648636248));
#45538=CARTESIAN_POINT('Ctrl Pts',(1.14754780382579,69.1982886868039,11.0768602965348));
#45539=CARTESIAN_POINT('Ctrl Pts',(1.22433976169283,69.2108528675956,11.1181841656645));
#45540=CARTESIAN_POINT('Ctrl Pts',(1.29891555615958,69.2233983758659,11.1635197194307));
#45541=CARTESIAN_POINT('Ctrl Pts',(1.30306400294486,69.224096248062,11.1660416118708));
#45542=CARTESIAN_POINT('Ctrl Pts',(1.3072055878291,69.2247940628451,11.1685759307943));
#45543=CARTESIAN_POINT('Ctrl Pts',(1.31134025317747,69.2254918197984,11.171122660597));
#45544=CARTESIAN_POINT('Ctrl Pts',(1.31135422434589,69.2254941775418,11.1711312660796));
#45545=CARTESIAN_POINT('Ctrl Pts',(1.31136819543531,69.2254965352845,11.1711398717039));
#45546=CARTESIAN_POINT('Ctrl Pts',(1.31138216644577,69.2254988930264,11.1711484774698));
#45547=CARTESIAN_POINT('Ctrl Pts',(1.33813162952027,69.23001312133,11.187625425764));
#45548=CARTESIAN_POINT('Ctrl Pts',(1.36459173541892,69.2345246994819,11.2046215361119));
#45549=CARTESIAN_POINT('Ctrl Pts',(1.39074802582465,69.239038624908,11.2221279654452));
#45550=CARTESIAN_POINT('Ctrl Pts',(1.40280709560774,69.2411197205398,11.2301991119919));
#45551=CARTESIAN_POINT('Ctrl Pts',(1.41479117008784,69.2431995200094,11.2383717723792));
#45552=CARTESIAN_POINT('Ctrl Pts',(1.42669913149396,69.245278482405,11.2466445228467));
#45553=CARTESIAN_POINT('Ctrl Pts',(1.42671293625134,69.2452808925213,11.2466541133475));
#45554=CARTESIAN_POINT('Ctrl Pts',(1.42672674090642,69.2452833026364,11.2466637039829));
#45555=CARTESIAN_POINT('Ctrl Pts',(1.42674054545918,69.2452857127505,11.2466732947528));
#45556=CARTESIAN_POINT('Ctrl Pts',(1.46452159863263,69.2518818444896,11.2729218371295));
#45557=CARTESIAN_POINT('Ctrl Pts',(1.50153584351307,69.2584697485006,11.3001776947919));
#45558=CARTESIAN_POINT('Ctrl Pts',(1.53772885816469,69.265029912732,11.3284086227869));
#45559=CARTESIAN_POINT('Ctrl Pts',(1.53774268781877,69.2650324194257,11.328419410061));
#45560=CARTESIAN_POINT('Ctrl Pts',(1.53775651735298,69.2650349261154,11.3284301974775));
#45561=CARTESIAN_POINT('Ctrl Pts',(1.53777034676736,69.265037432801,11.3284409850364));
#45562=CARTESIAN_POINT('Ctrl Pts',(1.59857550653995,69.2760588262814,11.3758717167935));
#45563=CARTESIAN_POINT('Ctrl Pts',(1.65706798729583,69.2870021977314,11.4260555927558));
#45564=CARTESIAN_POINT('Ctrl Pts',(1.71313960617886,69.2979608857032,11.4788041681358));
#45565=CARTESIAN_POINT('Ctrl Pts',(1.71915879412077,69.2991372812455,11.4844666333046));
#45566=CARTESIAN_POINT('Ctrl Pts',(1.72515003590684,69.3003138478121,11.4901586519967));
#45567=CARTESIAN_POINT('Ctrl Pts',(1.73111316273383,69.3014906969056,11.4958799888797));
#45568=CARTESIAN_POINT('Ctrl Pts',(1.73588764363626,69.3024329615405,11.5004608764705));
#45569=CARTESIAN_POINT('Ctrl Pts',(1.74064410521965,69.3033754035243,11.5050605551194));
#45570=CARTESIAN_POINT('Ctrl Pts',(1.745382460388,69.3043180775947,11.509678901346));
#45571=CARTESIAN_POINT('Ctrl Pts',(1.74539430201747,69.3043204334327,11.509690443061));
#45572=CARTESIAN_POINT('Ctrl Pts',(1.7454061435337,69.3043227892722,11.5097019848927));
#45573=CARTESIAN_POINT('Ctrl Pts',(1.74541798493674,69.3043251451133,11.5097135268411));
#45574=CARTESIAN_POINT('Ctrl Pts',(1.8030488418173,69.3157907747721,11.565886969636));
#45575=CARTESIAN_POINT('Ctrl Pts',(1.8579975848143,69.3272931358038,11.6248206449648));
#45576=CARTESIAN_POINT('Ctrl Pts',(1.91000833396433,69.3387810634638,11.6863106092312));
#45577=CARTESIAN_POINT('Ctrl Pts',(1.91629329806695,69.3401692613678,11.6937410389866));
#45578=CARTESIAN_POINT('Ctrl Pts',(1.92253536353318,69.3415572540476,11.7012088585325));
#45579=CARTESIAN_POINT('Ctrl Pts',(1.92873407884509,69.3429449558,11.7087137596157));
#45580=CARTESIAN_POINT('Ctrl Pts',(1.97669639644135,69.3536822439033,11.7667826385953));
#45581=CARTESIAN_POINT('Ctrl Pts',(2.02206426325868,69.3644013308688,11.827067119155));
#45582=CARTESIAN_POINT('Ctrl Pts',(2.06465495930781,69.3750445556727,11.8894330863254));
#45583=CARTESIAN_POINT('Ctrl Pts',(2.07313001076284,69.3771624331959,11.9018431859444));
#45584=CARTESIAN_POINT('Ctrl Pts',(2.08149507952893,69.3792773231086,11.9143358680576));
#45585=CARTESIAN_POINT('Ctrl Pts',(2.08974868801882,69.3813887954505,11.9269103220508));
#45586=CARTESIAN_POINT('Ctrl Pts',(2.09150796335126,69.3818388605597,11.9295905953829));
#45587=CARTESIAN_POINT('Ctrl Pts',(2.09326185186073,69.3822886730454,11.9322740599648));
#45588=CARTESIAN_POINT('Ctrl Pts',(2.09501033148427,69.3827382384023,11.9349607119884));
#45589=CARTESIAN_POINT('Ctrl Pts',(2.13784276421261,69.3937512222827,12.0007755150414));
#45590=CARTESIAN_POINT('Ctrl Pts',(2.17743371466383,69.4046163067197,12.0685030997901));
#45591=CARTESIAN_POINT('Ctrl Pts',(2.21373045870408,69.4154117303112,12.1379092891655));
#45592=CARTESIAN_POINT('Ctrl Pts',(2.21688249549914,69.4163492130876,12.1439365753175));
#45593=CARTESIAN_POINT('Ctrl Pts',(2.2200096575108,69.4172861675077,12.149976518639));
#45594=CARTESIAN_POINT('Ctrl Pts',(2.22311189218551,69.418222643084,12.1560289641454));
#45595=CARTESIAN_POINT('Ctrl Pts',(2.26053984883482,69.4295210685565,12.2290507345104));
#45596=CARTESIAN_POINT('Ctrl Pts',(2.2943429555824,69.4407507008421,12.3038935424851));
#45597=CARTESIAN_POINT('Ctrl Pts',(2.32442367345173,69.4519815543759,12.3802724719404));
#45598=CARTESIAN_POINT('Ctrl Pts',(2.32626576753546,69.4526693135224,12.3849497929632));
#45599=CARTESIAN_POINT('Ctrl Pts',(2.32809388645792,69.4533570757873,12.389632871055));
#45600=CARTESIAN_POINT('Ctrl Pts',(2.32990800177276,69.4540448566763,12.394321639167));
#45601=CARTESIAN_POINT('Ctrl Pts',(2.36193636236869,69.4661876869281,12.4771022400536));
#45602=CARTESIAN_POINT('Ctrl Pts',(2.38960387102893,69.4783370394601,12.5616579670394));
#45603=CARTESIAN_POINT('Ctrl Pts',(2.41276317008455,69.4905523650869,12.6475996965818));
#45604=CARTESIAN_POINT('Ctrl Pts',(2.43163782306541,69.500507762774,12.717641553971));
#45605=CARTESIAN_POINT('Ctrl Pts',(2.4475174504375,69.5105064253298,12.7886032742458));
#45606=CARTESIAN_POINT('Ctrl Pts',(2.46032036786947,69.5205657976629,12.8602613757723));
#45607=CARTESIAN_POINT('Ctrl Pts',(2.4759832095527,69.5328722393097,12.9479265119019));
#45608=CARTESIAN_POINT('Ctrl Pts',(2.48695700823147,69.5452044792185,13.0361632797939));
#45609=CARTESIAN_POINT('Ctrl Pts',(2.49324964569461,69.5575667617407,13.1245401413933));
#45610=CARTESIAN_POINT('Ctrl Pts',(2.49957447029312,69.569992277917,13.2133690547795));
#45611=CARTESIAN_POINT('Ctrl Pts',(2.50117071942633,69.5824477732759,13.3023385599671));
#45612=CARTESIAN_POINT('Ctrl Pts',(2.49805608672364,69.5949132923211,13.3910440920875));
#45613=CARTESIAN_POINT('Ctrl Pts',(2.49516671437906,69.6064772645221,13.4733341518749));
#45614=CARTESIAN_POINT('Ctrl Pts',(2.48822389015378,69.6180494984437,13.555396980219));
#45615=CARTESIAN_POINT('Ctrl Pts',(2.47723921943366,69.6295996054898,13.6369443361281));
#45616=CARTESIAN_POINT('Ctrl Pts',(2.47656532930736,69.6303081841349,13.6419471222264));
#45617=CARTESIAN_POINT('Ctrl Pts',(2.47587621401331,69.6310166808024,13.6469479777495));
#45618=CARTESIAN_POINT('Ctrl Pts',(2.47517187088532,69.6317250889864,13.6519468397047));
#45619=CARTESIAN_POINT('Ctrl Pts',(2.46537114414571,69.6415823797815,13.7215045284011));
#45620=CARTESIAN_POINT('Ctrl Pts',(2.45262528353376,69.6514218402911,13.7906750536128));
#45621=CARTESIAN_POINT('Ctrl Pts',(2.43692859562038,69.6612194466812,13.8593015173351));
#45622=CARTESIAN_POINT('Ctrl Pts',(2.42200437329576,69.6705348931514,13.924550734724));
#45623=CARTESIAN_POINT('Ctrl Pts',(2.40447319609836,69.6797747920806,13.9890458939864));
#45624=CARTESIAN_POINT('Ctrl Pts',(2.38437526957604,69.6889186140611,14.0526862067553));
#45625=CARTESIAN_POINT('Ctrl Pts',(2.38436632465434,69.6889226836736,14.0527145309515));
#45626=CARTESIAN_POINT('Ctrl Pts',(2.38435737922361,69.6889267532671,14.0527428549785));
#45627=CARTESIAN_POINT('Ctrl Pts',(2.38434843328378,69.6889308228417,14.0527711788364));
#45628=CARTESIAN_POINT('Ctrl Pts',(2.36151035591637,69.6993200342555,14.1250791162566));
#45629=CARTESIAN_POINT('Ctrl Pts',(2.33535676515888,69.7095864886297,14.1962881545291));
#45630=CARTESIAN_POINT('Ctrl Pts',(2.30598464802508,69.7197980582485,14.2662152096127));
#45631=CARTESIAN_POINT('Ctrl Pts',(2.30216951873161,69.721124433811,14.275297999084));
#45632=CARTESIAN_POINT('Ctrl Pts',(2.29830005562725,69.7224498762773,14.2843590964447));
#45633=CARTESIAN_POINT('Ctrl Pts',(2.29437644417292,69.7237745280003,14.2933980431371));
#45634=CARTESIAN_POINT('Ctrl Pts',(2.26276231626872,69.7344477838734,14.3662285005309));
#45635=CARTESIAN_POINT('Ctrl Pts',(2.22763349023853,69.7450704908474,14.4376246046964));
#45636=CARTESIAN_POINT('Ctrl Pts',(2.18910076349599,69.7557017740771,14.5073320387567));
#45637=CARTESIAN_POINT('Ctrl Pts',(2.1837793768327,69.757169959009,14.5169586663354));
#45638=CARTESIAN_POINT('Ctrl Pts',(2.17839304775096,69.7586382998401,14.5265530108488));
#45639=CARTESIAN_POINT('Ctrl Pts',(2.17294204808246,69.7601069449087,14.536114327533));
#45640=CARTESIAN_POINT('Ctrl Pts',(2.13137878965643,69.7713051981162,14.609018290183));
#45641=CARTESIAN_POINT('Ctrl Pts',(2.08605615374757,69.7825217257262,14.680005875772));
#45642=CARTESIAN_POINT('Ctrl Pts',(2.03712301582743,69.7938014659925,14.7487408392039));
#45643=CARTESIAN_POINT('Ctrl Pts',(2.03316839621133,69.7947130585046,14.7542957789901));
#45644=CARTESIAN_POINT('Ctrl Pts',(2.02919018990079,69.7956250616874,14.7598359784257));
#45645=CARTESIAN_POINT('Ctrl Pts',(2.02518847321715,69.7965374980996,14.765361245264));
#45646=CARTESIAN_POINT('Ctrl Pts',(1.97315048731705,69.80840274417,14.8372113487462));
#45647=CARTESIAN_POINT('Ctrl Pts',(1.9174131813531,69.8202791647436,14.9061601506594));
#45648=CARTESIAN_POINT('Ctrl Pts',(1.85829189772205,69.8321897426764,14.9718940227602));
#45649=CARTESIAN_POINT('Ctrl Pts',(1.79861679112262,69.8442118938232,15.0382436617376));
#45650=CARTESIAN_POINT('Ctrl Pts',(1.73549496583036,69.8562685440475,15.101316979798));
#45651=CARTESIAN_POINT('Ctrl Pts',(1.66925420501732,69.8683584881138,15.1608171881416));
#45652=CARTESIAN_POINT('Ctrl Pts',(1.60367188503604,69.8803282567364,15.2197259575254));
#45653=CARTESIAN_POINT('Ctrl Pts',(1.53503370614351,69.8923302386959,15.2751322740645));
#45654=CARTESIAN_POINT('Ctrl Pts',(1.46364342249625,69.9043445863292,15.3267799436083));
#45655=CARTESIAN_POINT('Ctrl Pts',(1.40873436921352,69.9135852899748,15.3665041818943));
#45656=CARTESIAN_POINT('Ctrl Pts',(1.35219717552376,69.9228328780306,15.4040057465273));
#45657=CARTESIAN_POINT('Ctrl Pts',(1.29415591594126,69.9320730965854,15.4391790836035));
#45658=CARTESIAN_POINT('Ctrl Pts',(1.23022248155498,69.9422513544479,15.4779231124942));
#45659=CARTESIAN_POINT('Ctrl Pts',(1.16474992615481,69.9523753930348,15.5136695269958));
#45660=CARTESIAN_POINT('Ctrl Pts',(1.09791606230348,69.9624237368063,15.5463656837148));
#45661=CARTESIAN_POINT('Ctrl Pts',(1.08528489012075,69.9643228094174,15.5525450479088));
#45662=CARTESIAN_POINT('Ctrl Pts',(1.07260494573646,69.9662191904854,15.5586154447488));
#45663=CARTESIAN_POINT('Ctrl Pts',(1.05987722280761,69.9681127520765,15.5645764873251));
#45664=CARTESIAN_POINT('Ctrl Pts',(1.01749693022492,69.9744178621662,15.5844253424497));
#45665=CARTESIAN_POINT('Ctrl Pts',(0.974587743570524,69.9806914853537,15.6030623844121));
#45666=CARTESIAN_POINT('Ctrl Pts',(0.931181893463117,69.9869285085228,15.6204741968846));
#45667=CARTESIAN_POINT('Ctrl Pts',(0.93113646091439,69.986935036764,15.6204924216865));
#45668=CARTESIAN_POINT('Ctrl Pts',(0.93109102782079,69.9869415649654,15.6205106451451));
#45669=CARTESIAN_POINT('Ctrl Pts',(0.931045594182292,69.9869480931269,15.6205288672604));
#45670=CARTESIAN_POINT('Ctrl Pts',(0.862582976136436,69.9967851883703,15.6479872386433));
#45671=CARTESIAN_POINT('Ctrl Pts',(0.792881203027636,70.006532272519,15.6723992841724));
#45672=CARTESIAN_POINT('Ctrl Pts',(0.722111028103673,70.0162431913653,15.6937042086057));
#45673=CARTESIAN_POINT('Ctrl Pts',(0.710197042261118,70.0178780007999,15.6972908405216));
#45674=CARTESIAN_POINT('Ctrl Pts',(0.698252834406958,70.0195117735174,15.7007893095625));
#45675=CARTESIAN_POINT('Ctrl Pts',(0.686279293816833,70.0211447521252,15.7041992031062));
#45676=CARTESIAN_POINT('Ctrl Pts',(0.612265188066109,70.0312389636461,15.7252773645273));
#45677=CARTESIAN_POINT('Ctrl Pts',(0.537127501164212,70.0413034609848,15.7429736632169));
#45678=CARTESIAN_POINT('Ctrl Pts',(0.461100222343306,70.0513841327094,15.7571915589655));
#45679=CARTESIAN_POINT('Ctrl Pts',(0.449893828301642,70.0528700201606,15.7592872717763));
#45680=CARTESIAN_POINT('Ctrl Pts',(0.438668165611532,70.0543562504055,15.7613073401694));
#45681=CARTESIAN_POINT('Ctrl Pts',(0.427424047954188,70.055842961437,15.7632513844396));
#45682=CARTESIAN_POINT('Ctrl Pts',(0.406594269687557,70.0585971002742,15.766852735148));
#45683=CARTESIAN_POINT('Ctrl Pts',(0.385701175003112,70.0613528250924,15.7701934092717));
#45684=CARTESIAN_POINT('Ctrl Pts',(0.364750122956928,70.0641108683095,15.7732712637113));
#45685=CARTESIAN_POINT('Ctrl Pts',(0.277743471818803,70.0755646179105,15.7860531424871));
#45686=CARTESIAN_POINT('Ctrl Pts',(0.19018823497606,70.087000641333,15.7942347475934));
#45687=CARTESIAN_POINT('Ctrl Pts',(0.102510667813711,70.0984565180099,15.7978109533579));
#45688=CARTESIAN_POINT('Ctrl Pts',(0.01358043595333,70.1100760667955,15.8014382529981));
#45689=CARTESIAN_POINT('Ctrl Pts',(-0.0754742851914581,70.1217158403208,
15.8003268962746));
#45690=CARTESIAN_POINT('Ctrl Pts',(-0.164199033821504,70.1333925230572,
15.7944943321978));
#45691=CARTESIAN_POINT('Ctrl Pts',(-0.252756319590444,70.1450471667263,
15.7886727767502));
#45692=CARTESIAN_POINT('Ctrl Pts',(-0.340983424829321,70.1567382485531,
15.7781481170492));
#45693=CARTESIAN_POINT('Ctrl Pts',(-0.428440479512438,70.1684641869835,
15.7629633930642));
#45694=CARTESIAN_POINT('Ctrl Pts',(-0.494062496909083,70.1772625593786,
15.751569775647));
#45695=CARTESIAN_POINT('Ctrl Pts',(-0.559251153861324,70.1860801433988,
15.7375532922927));
#45696=CARTESIAN_POINT('Ctrl Pts',(-0.623831971164928,70.1949113471847,
15.7209379703818));
#45697=CARTESIAN_POINT('Ctrl Pts',(-0.69839193812473,70.2051071652307,15.7017552176011));
#45698=CARTESIAN_POINT('Ctrl Pts',(-0.771800687543043,70.2152748164325,
15.6791962467254));
#45699=CARTESIAN_POINT('Ctrl Pts',(-0.843847806244314,70.2254015817701,
15.6533881351996));
#45700=CARTESIAN_POINT('Ctrl Pts',(-0.855334802569033,70.2270161656467,
15.6492733602081));
#45701=CARTESIAN_POINT('Ctrl Pts',(-0.866787255135574,70.2286297189187,
15.6450759093358));
#45702=CARTESIAN_POINT('Ctrl Pts',(-0.878204386210756,70.2302421999663,
15.6407962017555));
#45703=CARTESIAN_POINT('Ctrl Pts',(-0.947352556727918,70.2400082360834,
15.6148760342825));
#45704=CARTESIAN_POINT('Ctrl Pts',(-1.01520313841598,70.2497344017798,15.585942753797));
#45705=CARTESIAN_POINT('Ctrl Pts',(-1.08160798117368,70.2594089171849,15.5540849648858));
#45706=CARTESIAN_POINT('Ctrl Pts',(-1.0943450491834,70.2612645794462,15.5479743439258));
#45707=CARTESIAN_POINT('Ctrl Pts',(-1.10702900301784,70.2631183551719,15.541755994678));
#45708=CARTESIAN_POINT('Ctrl Pts',(-1.11965889759404,70.2649701808128,15.5354303468635));
#45709=CARTESIAN_POINT('Ctrl Pts',(-1.14794015873828,70.2691168476142,15.5212657553328));
#45710=CARTESIAN_POINT('Ctrl Pts',(-1.17595043962458,70.2732536617004,15.5065635206852));
#45711=CARTESIAN_POINT('Ctrl Pts',(-1.20368003277824,70.2773798529382,15.491327901301));
#45712=CARTESIAN_POINT('Ctrl Pts',(-1.2037229633007,70.277386241043,15.4913043137533));
#45713=CARTESIAN_POINT('Ctrl Pts',(-1.20376589315014,70.2773926291224,15.4912807249264));
#45714=CARTESIAN_POINT('Ctrl Pts',(-1.20380882232651,70.2773990171765,15.4912571348202));
#45715=CARTESIAN_POINT('Ctrl Pts',(-1.26742642944486,70.2868656026444,15.4562984834978));
#45716=CARTESIAN_POINT('Ctrl Pts',(-1.32957019752597,70.2962770242264,15.4185311107454));
#45717=CARTESIAN_POINT('Ctrl Pts',(-1.39009318732037,70.3056726599036,15.3780181758782));
#45718=CARTESIAN_POINT('Ctrl Pts',(-1.40251309408387,70.3076007358214,15.3697045272055));
#45719=CARTESIAN_POINT('Ctrl Pts',(-1.41486457486924,70.3095281303524,15.3612752388359));
#45720=CARTESIAN_POINT('Ctrl Pts',(-1.42714609176254,70.3114551579939,15.3527308358896));
#45721=CARTESIAN_POINT('Ctrl Pts',(-1.45440827917267,70.3157327231484,15.3337641954937));
#45722=CARTESIAN_POINT('Ctrl Pts',(-1.48132603291762,70.3200084353271,15.3142305611203));
#45723=CARTESIAN_POINT('Ctrl Pts',(-1.50788174594805,70.3242853535711,15.2941366208503));
#45724=CARTESIAN_POINT('Ctrl Pts',(-1.57266814708591,70.3347194978424,15.2451146242168));
#45725=CARTESIAN_POINT('Ctrl Pts',(-1.63499119347552,70.3451119765115,15.192990508662));
#45726=CARTESIAN_POINT('Ctrl Pts',(-1.69463638386186,70.3554981699385,15.1379691056813));
#45727=CARTESIAN_POINT('Ctrl Pts',(-1.69878705948321,70.3562209393618,15.1341401968535));
#45728=CARTESIAN_POINT('Ctrl Pts',(-1.70292474658918,70.3569436760685,15.130297254325));
#45729=CARTESIAN_POINT('Ctrl Pts',(-1.70704936373546,70.3576663909591,15.126440346116));
#45730=CARTESIAN_POINT('Ctrl Pts',(-1.77160880991124,70.3689784888895,15.0660711411471));
#45731=CARTESIAN_POINT('Ctrl Pts',(-1.83297023730468,70.3802857665096,15.0022808156671));
#45732=CARTESIAN_POINT('Ctrl Pts',(-1.89083291826391,70.3916163554277,14.9353661169356));
#45733=CARTESIAN_POINT('Ctrl Pts',(-1.94914069489051,70.4030341023543,14.8679366919247));
#45734=CARTESIAN_POINT('Ctrl Pts',(-2.00389420879611,70.4144753004314,14.7973351616577));
#45735=CARTESIAN_POINT('Ctrl Pts',(-2.0547890930373,70.4259538792498,14.7238968456928));
#45736=CARTESIAN_POINT('Ctrl Pts',(-2.09195668421999,70.4343364727312,14.6702662039176));
#45737=CARTESIAN_POINT('Ctrl Pts',(-2.12706653535575,70.4427386678698,14.6151234984332));
#45738=CARTESIAN_POINT('Ctrl Pts',(-2.16000686497024,70.4511621004216,14.5586058797152));
#45739=CARTESIAN_POINT('Ctrl Pts',(-2.20220603956577,70.4619531855476,14.4862023279622));
#45740=CARTESIAN_POINT('Ctrl Pts',(-2.24063570839904,70.4727262416205,14.4118998419532));
#45741=CARTESIAN_POINT('Ctrl Pts',(-2.27519405667041,70.4834798357975,14.3360364825278));
#45742=CARTESIAN_POINT('Ctrl Pts',(-2.27753892085078,70.484209492134,14.3308889774236));
#45743=CARTESIAN_POINT('Ctrl Pts',(-2.27986595804307,70.484939060164,14.3257342667091));
#45744=CARTESIAN_POINT('Ctrl Pts',(-2.2821751346037,70.4856685400044,14.3205724476062));
#45745=CARTESIAN_POINT('Ctrl Pts',(-2.31455928023641,70.4958988453829,14.2481825297417));
#45746=CARTESIAN_POINT('Ctrl Pts',(-2.3434322556813,70.5061113456515,14.174399032633));
#45747=CARTESIAN_POINT('Ctrl Pts',(-2.3687287929498,70.5163037689282,14.099477053488));
#45748=CARTESIAN_POINT('Ctrl Pts',(-2.37182718200157,70.5175521647998,14.0903004046267));
#45749=CARTESIAN_POINT('Ctrl Pts',(-2.37487189986608,70.5188002649376,14.081106614678));
#45750=CARTESIAN_POINT('Ctrl Pts',(-2.37786281017834,70.5200480697423,14.0718961013543));
#45751=CARTESIAN_POINT('Ctrl Pts',(-2.40125907834412,70.5298089695291,13.9998472542915));
#45752=CARTESIAN_POINT('Ctrl Pts',(-2.4213651855868,70.5395513109683,13.9267791929086));
#45753=CARTESIAN_POINT('Ctrl Pts',(-2.43812763170418,70.5492750724892,13.8528720253056));
#45754=CARTESIAN_POINT('Ctrl Pts',(-2.44065479389618,70.5507410591541,13.8417295346228));
#45755=CARTESIAN_POINT('Ctrl Pts',(-2.4431059143404,70.5522066324039,13.8305678847687));
#45756=CARTESIAN_POINT('Ctrl Pts',(-2.44548076118895,70.5536718016633,13.8193876015694));
#45757=CARTESIAN_POINT('Ctrl Pts',(-2.44973892873762,70.5562988915733,13.7993410376688));
#45758=CARTESIAN_POINT('Ctrl Pts',(-2.45375200762531,70.5589246676948,13.7792346069052));
#45759=CARTESIAN_POINT('Ctrl Pts',(-2.45751873206479,70.5615491847454,13.7590711743978));
#45760=CARTESIAN_POINT('Ctrl Pts',(-2.45752562215502,70.5615539855105,13.7590342914584));
#45761=CARTESIAN_POINT('Ctrl Pts',(-2.4575325114208,70.5615587862714,13.7589974083281));
#45762=CARTESIAN_POINT('Ctrl Pts',(-2.45753939986211,70.5615635870281,13.7589605250071));
#45763=CARTESIAN_POINT('Ctrl Pts',(-2.46528867627758,70.5669642849811,13.7174679671417));
#45764=CARTESIAN_POINT('Ctrl Pts',(-2.47199483430321,70.5723597156861,13.6757336645926));
#45765=CARTESIAN_POINT('Ctrl Pts',(-2.47764411293714,70.5777541555775,13.6337938114561));
#45766=CARTESIAN_POINT('Ctrl Pts',(-2.48852935099954,70.5881483609682,13.5529825583252));
#45767=CARTESIAN_POINT('Ctrl Pts',(-2.49544042130253,70.5984920278951,13.471776143099));
#45768=CARTESIAN_POINT('Ctrl Pts',(-2.49838216990339,70.6088101525565,13.3904693114515));
#45769=CARTESIAN_POINT('Ctrl Pts',(-2.49861827024406,70.6096382698018,13.3839437468113));
#45770=CARTESIAN_POINT('Ctrl Pts',(-2.49882877883583,70.6104662196973,13.3774175493841));
#45771=CARTESIAN_POINT('Ctrl Pts',(-2.49901368622386,70.6112940136901,13.3708908792594));
#45772=CARTESIAN_POINT('Ctrl Pts',(-2.49967335126509,70.6142472042803,13.3476067035272));
#45773=CARTESIAN_POINT('Ctrl Pts',(-2.50000751548752,70.6171983845687,13.3243165065547));
#45774=CARTESIAN_POINT('Ctrl Pts',(-2.50001628522819,70.6201479917331,13.3010276898172));
#45775=CARTESIAN_POINT('Ctrl Pts',(-2.49999978870036,70.6201493965427,13.3010278609544));
#45776=CARTESIAN_POINT('Ctrl Pts',(-2.49999992956743,70.6201927897384,13.3006852390838));
#45777=CARTESIAN_POINT('Ctrl Pts',(-2.5,70.620236182436,13.3003426187556));
#45778=CARTESIAN_POINT('Ctrl Pts',(-2.5,70.6202795746371,13.2999999999913));
#45779=CARTESIAN_POINT('',(1.35925139903161,68.5015684297319,11.2018017462371));
#45780=CARTESIAN_POINT('Ctrl Pts',(-2.5,69.6117391960828,13.3));
#45781=CARTESIAN_POINT('Ctrl Pts',(-2.5,69.5868984362623,13.5116533107127));
#45782=CARTESIAN_POINT('Ctrl Pts',(-2.47312159666966,69.5620969687835,13.7229015939511));
#45783=CARTESIAN_POINT('Ctrl Pts',(-2.37956580310906,69.5182587119009,14.083015772128));
#45784=CARTESIAN_POINT('Ctrl Pts',(-2.32476545853278,69.4995523412897,14.2332315126848));
#45785=CARTESIAN_POINT('Ctrl Pts',(-2.12606976051521,69.4458587704588,14.6493637701716));
#45786=CARTESIAN_POINT('Ctrl Pts',(-1.94793740573065,69.4117941420902,14.8957805457345));
#45787=CARTESIAN_POINT('Ctrl Pts',(-1.48832906641449,69.3386088439744,15.3364632396691));
#45788=CARTESIAN_POINT('Ctrl Pts',(-1.20220079857416,69.3001093631724,15.5174526183101));
#45789=CARTESIAN_POINT('Ctrl Pts',(-0.582791217961786,69.2255759157103,
15.7530787964279));
#45790=CARTESIAN_POINT('Ctrl Pts',(-0.256787408095275,69.1896508547796,
15.8082458630207));
#45791=CARTESIAN_POINT('Ctrl Pts',(0.368292389417417,69.119256871216,15.7905983579557));
#45792=CARTESIAN_POINT('Ctrl Pts',(0.662216165928006,69.0864985363696,15.7290484483144));
#45793=CARTESIAN_POINT('Ctrl Pts',(1.08466724944942,69.0372135465817,15.5579615117129));
#45794=CARTESIAN_POINT('Ctrl Pts',(1.22496652487473,69.0203448330629,15.4850279835998));
#45795=CARTESIAN_POINT('Ctrl Pts',(1.63261569660207,68.9676090591445,15.2214417251557));
#45796=CARTESIAN_POINT('Ctrl Pts',(1.87023210697087,68.9318521879707,14.9910721409861));
#45797=CARTESIAN_POINT('Ctrl Pts',(2.24050175203724,68.8634697219996,14.4553092538144));
#45798=CARTESIAN_POINT('Ctrl Pts',(2.37101546223115,68.8306680820086,14.1560772195167));
#45799=CARTESIAN_POINT('Ctrl Pts',(2.50473075109296,68.7656663114431,13.5520242921483));
#45800=CARTESIAN_POINT('Ctrl Pts',(2.516993553084,68.7355808882792,13.254584108532));
#45801=CARTESIAN_POINT('Ctrl Pts',(2.45537931489148,68.6908075740461,12.8033106644488));
#45802=CARTESIAN_POINT('Ctrl Pts',(2.41857985065703,68.6753936489625,12.6472704213994));
#45803=CARTESIAN_POINT('Ctrl Pts',(2.27002573796472,68.6299422017385,12.2099966991114));
#45804=CARTESIAN_POINT('Ctrl Pts',(2.12189734459302,68.5997252687359,11.9439725157658));
#45805=CARTESIAN_POINT('Ctrl Pts',(1.76687834959433,68.5473097365251,11.5128583182058));
#45806=CARTESIAN_POINT('Ctrl Pts',(1.57444119245041,68.5248031972306,11.3412057157747));
#45807=CARTESIAN_POINT('Ctrl Pts',(1.3592513647516,68.5015684831821,11.2018017902446));
#45808=CARTESIAN_POINT('Ctrl Pts',(1.35922685968084,68.5017698542948,11.2017859156125));
#45809=CARTESIAN_POINT('Ctrl Pts',(1.16329772448109,68.4679246869375,11.0748626692483));
#45810=CARTESIAN_POINT('Ctrl Pts',(0.950487220343815,68.4340759749094,10.9759635422888));
#45811=CARTESIAN_POINT('Ctrl Pts',(0.466658774060705,68.3626134545601,10.8289163155397));
#45812=CARTESIAN_POINT('Ctrl Pts',(0.19513354664671,68.3252407491545,10.7928130380239));
#45813=CARTESIAN_POINT('Ctrl Pts',(-0.383778198058173,68.2440015915658,
10.8106250704725));
#45814=CARTESIAN_POINT('Ctrl Pts',(-0.686331796473102,68.2006307553199,
10.8765229155169));
#45815=CARTESIAN_POINT('Ctrl Pts',(-1.2788474602455,68.1114145517084,11.1257719889208));
#45816=CARTESIAN_POINT('Ctrl Pts',(-1.55900536851427,68.0667979413492,11.3169972368763));
#45817=CARTESIAN_POINT('Ctrl Pts',(-2.00124833323174,67.9802453746223,11.7721669464916));
#45818=CARTESIAN_POINT('Ctrl Pts',(-2.16937622326692,67.9393861545933,12.0220700233241));
#45819=CARTESIAN_POINT('Ctrl Pts',(-2.42436824473168,67.8538965558814,12.6033695120974));
#45820=CARTESIAN_POINT('Ctrl Pts',(-2.49595863888419,67.8102147607181,12.9351487417965));
#45821=CARTESIAN_POINT('Ctrl Pts',(-2.49994461778903,67.7643387514265,13.2807826890184));
#45822=CARTESIAN_POINT('Ctrl Pts',(-2.50000000009011,67.7630631808826,13.2903925247493));
#45823=CARTESIAN_POINT('Ctrl Pts',(-2.5,67.7617877839724,13.3000000234479));
#45824=CARTESIAN_POINT('Origin',(0.,70.2,13.3));
#45825=CARTESIAN_POINT('',(-0.20632980674377,66.2927243572952,10.8082436938974));
#45826=CARTESIAN_POINT('Ctrl Pts',(-2.5,67.7617877839724,13.3000000234479));
#45827=CARTESIAN_POINT('Ctrl Pts',(-2.49999999722602,67.7225256620901,13.5957595488635));
#45828=CARTESIAN_POINT('Ctrl Pts',(-2.44751521952288,67.6833209369714,13.8892901188729));
#45829=CARTESIAN_POINT('Ctrl Pts',(-2.28875435858697,67.6232069710623,14.3187295896263));
#45830=CARTESIAN_POINT('Ctrl Pts',(-2.21799892564411,67.6021721375708,14.4647730683009));
#45831=CARTESIAN_POINT('Ctrl Pts',(-1.96868832241002,67.5399978003467,14.8730234644183));
#45832=CARTESIAN_POINT('Ctrl Pts',(-1.7539605333616,67.4993192332267,15.109363162545));
#45833=CARTESIAN_POINT('Ctrl Pts',(-1.36688160654624,67.4370998399759,15.3999264567616));
#45834=CARTESIAN_POINT('Ctrl Pts',(-1.22314933749683,67.4157082165148,15.4867709879815));
#45835=CARTESIAN_POINT('Ctrl Pts',(-0.9256486713516,67.3736180420083,15.6279493782103));
#45836=CARTESIAN_POINT('Ctrl Pts',(-0.773094630311917,67.3530216905194,
15.6829607786152));
#45837=CARTESIAN_POINT('Ctrl Pts',(-0.292696823526602,67.2899391679536,
15.8051584395702));
#45838=CARTESIAN_POINT('Ctrl Pts',(0.0441693313863235,67.2482188913854,
15.8218223071524));
#45839=CARTESIAN_POINT('Ctrl Pts',(0.693875930672618,67.1658110326071,15.7234184875379));
#45840=CARTESIAN_POINT('Ctrl Pts',(1.00101021270645,67.1258696982556,15.6135330787129));
#45841=CARTESIAN_POINT('Ctrl Pts',(1.41651319070852,67.0659308077562,15.366204515324));
#45842=CARTESIAN_POINT('Ctrl Pts',(1.5460938564108,67.0461661417386,15.271118924942));
#45843=CARTESIAN_POINT('Ctrl Pts',(1.90894206626637,66.986267381346,14.9469240839239));
#45844=CARTESIAN_POINT('Ctrl Pts',(2.10734890652499,66.9467409247531,14.6840280321213));
#45845=CARTESIAN_POINT('Ctrl Pts',(2.31887673554413,66.8877298751789,14.2476256427034));
#45846=CARTESIAN_POINT('Ctrl Pts',(2.3743444830329,66.8685386145047,14.0985475386327));
#45847=CARTESIAN_POINT('Ctrl Pts',(2.45661310108357,66.8300830155865,13.790580312074));
#45848=CARTESIAN_POINT('Ctrl Pts',(2.48297741687454,66.8109086574451,13.6323324635222));
#45849=CARTESIAN_POINT('Ctrl Pts',(2.51707300787301,66.7517406660427,13.139792194619));
#45850=CARTESIAN_POINT('Ctrl Pts',(2.47325120089564,66.7122277110131,12.8056304521614));
#45851=CARTESIAN_POINT('Ctrl Pts',(2.31268382373457,66.6537832086372,12.3368425662245));
#45852=CARTESIAN_POINT('Ctrl Pts',(2.2455174742449,66.6348512048037,12.1892192379082));
#45853=CARTESIAN_POINT('Ctrl Pts',(1.9995758508219,66.5772088143333,11.7636354028661));
#45854=CARTESIAN_POINT('Ctrl Pts',(1.77971327059208,66.5389983508999,11.5135514593427));
#45855=CARTESIAN_POINT('Ctrl Pts',(1.39541318339668,66.483385867781,11.2199826808397));
#45856=CARTESIAN_POINT('Ctrl Pts',(1.2648488428219,66.4658426669773,11.1381004340619));
#45857=CARTESIAN_POINT('Ctrl Pts',(0.914284569745283,66.4208540202292,10.9609400434414));
#45858=CARTESIAN_POINT('Ctrl Pts',(0.686598815799409,66.3936233209689,10.8842756362153));
#45859=CARTESIAN_POINT('Ctrl Pts',(0.234623662540332,66.34180468946,10.8012871093587));
#45860=CARTESIAN_POINT('Ctrl Pts',(0.0134371728524807,66.3173924881665,
10.7903300910262));
#45861=CARTESIAN_POINT('Ctrl Pts',(-0.206318250554135,66.2928316028488,
10.8085279894231));
#45862=CARTESIAN_POINT('',(-2.5,65.696789585947,13.2999999999999));
#45863=CARTESIAN_POINT('Ctrl Pts',(-0.206248650970427,66.2923157697828,
10.8085222268756));
#45864=CARTESIAN_POINT('Ctrl Pts',(-0.492720738343416,66.2438642690178,
10.832236860094));
#45865=CARTESIAN_POINT('Ctrl Pts',(-0.772845838683397,66.1937747245436,
10.9051866997659));
#45866=CARTESIAN_POINT('Ctrl Pts',(-1.25578965221234,66.1019374669533,11.1246328414266));
#45867=CARTESIAN_POINT('Ctrl Pts',(-1.46186855298299,66.0616368429323,11.2572875518897));
#45868=CARTESIAN_POINT('Ctrl Pts',(-1.89948718136495,65.9727967771414,11.6400300826565));
#45869=CARTESIAN_POINT('Ctrl Pts',(-2.10569846836433,65.9238380940771,11.9108527376458));
#45870=CARTESIAN_POINT('Ctrl Pts',(-2.37726386591633,65.8260764030656,12.4743249644652));
#45871=CARTESIAN_POINT('Ctrl Pts',(-2.45656126657527,65.7795732932735,12.7537071211792));
#45872=CARTESIAN_POINT('Ctrl Pts',(-2.49550840758641,65.7223041543191,13.1268508588702));
#45873=CARTESIAN_POINT('Ctrl Pts',(-2.49999999999999,65.709424128047,13.213474844254));
#45874=CARTESIAN_POINT('Ctrl Pts',(-2.5,65.696789585947,13.2999999999997));
#45875=CARTESIAN_POINT('',(-2.5,66.7778885669818,13.3));
#45876=CARTESIAN_POINT('',(-2.5,70.2,13.3));
#45877=CARTESIAN_POINT('Ctrl Pts',(-2.5,66.7778885669818,13.3));
#45878=CARTESIAN_POINT('Ctrl Pts',(-2.5,66.7918413044886,13.1852589379609));
#45879=CARTESIAN_POINT('Ctrl Pts',(-2.49210079537757,66.8057580925441,13.0703921209457));
#45880=CARTESIAN_POINT('Ctrl Pts',(-2.43495215129586,66.8558636094013,12.6587480632189));
#45881=CARTESIAN_POINT('Ctrl Pts',(-2.34038603459958,66.8912358567461,12.3711285140565));
#45882=CARTESIAN_POINT('Ctrl Pts',(-2.04271380146662,66.9660389016043,11.8228429549495));
#45883=CARTESIAN_POINT('Ctrl Pts',(-1.8345944822031,67.0044353555049,11.5711348115867));
#45884=CARTESIAN_POINT('Ctrl Pts',(-1.32734782214467,67.0820580522804,11.1555986421081));
#45885=CARTESIAN_POINT('Ctrl Pts',(-1.0310556023197,67.1205391368846,10.998432575161));
#45886=CARTESIAN_POINT('Ctrl Pts',(-0.560974796121357,67.1790585878968,
10.8586114429367));
#45887=CARTESIAN_POINT('Ctrl Pts',(-0.405248485500008,67.1979261353801,
10.827985950135));
#45888=CARTESIAN_POINT('Ctrl Pts',(0.0215944749802646,67.2485059398258,
10.78549190141));
#45889=CARTESIAN_POINT('Ctrl Pts',(0.293465307249012,67.2793701113925,10.8025706557839));
#45890=CARTESIAN_POINT('Ctrl Pts',(0.700935861631911,67.3269947439867,10.8957568463845));
#45891=CARTESIAN_POINT('Ctrl Pts',(0.841319429460069,67.3437349888158,10.9412140832751));
#45892=CARTESIAN_POINT('Ctrl Pts',(1.28520168748909,67.3997086012979,11.1296436413456));
#45893=CARTESIAN_POINT('Ctrl Pts',(1.56421133847712,67.4389649266098,11.3212222920514));
#45894=CARTESIAN_POINT('Ctrl Pts',(2.01027649080665,67.5113508665155,11.7825148298095));
#45895=CARTESIAN_POINT('Ctrl Pts',(2.18101087549921,67.5442913843132,12.0401744489584));
#45896=CARTESIAN_POINT('Ctrl Pts',(2.4240201399684,67.6148620195753,12.6120683372072));
#45897=CARTESIAN_POINT('Ctrl Pts',(2.49135655174185,67.6509290513449,12.9226361181987));
#45898=CARTESIAN_POINT('Ctrl Pts',(2.50682470755549,67.7187639505598,13.5421114795545));
#45899=CARTESIAN_POINT('Ctrl Pts',(2.45871982272519,67.750186200484,13.8454189862729));
#45900=CARTESIAN_POINT('Ctrl Pts',(2.251745196374,67.8185899091536,14.4313842011514));
#45901=CARTESIAN_POINT('Ctrl Pts',(2.0903038501426,67.8540092266959,14.7075513449628));
#45902=CARTESIAN_POINT('Ctrl Pts',(1.68396679177138,67.9188317723156,15.1719572106393));
#45903=CARTESIAN_POINT('Ctrl Pts',(1.44748494170992,67.9480240235824,15.3602784316105));
#45904=CARTESIAN_POINT('Ctrl Pts',(0.899674880587149,68.0132688187001,15.654619675979));
#45905=CARTESIAN_POINT('Ctrl Pts',(0.589032099880397,68.0479853858131,15.7509057350415));
#45906=CARTESIAN_POINT('Ctrl Pts',(-0.0270692607296119,68.109375633073,
15.8174764530437));
#45907=CARTESIAN_POINT('Ctrl Pts',(-0.325929982479385,68.1360588846597,
15.7964296452563));
#45908=CARTESIAN_POINT('Ctrl Pts',(-0.927580749741263,68.1969626388315,
15.6439618401786));
#45909=CARTESIAN_POINT('Ctrl Pts',(-1.22304781389004,68.230108754567,15.504328224522));
#45910=CARTESIAN_POINT('Ctrl Pts',(-1.71691579141469,68.2857881259515,15.1401472128048));
#45911=CARTESIAN_POINT('Ctrl Pts',(-1.91827023404044,68.3087014678107,14.9291326085142));
#45912=CARTESIAN_POINT('Ctrl Pts',(-2.2326618221574,68.3577384042391,14.4583269641961));
#45913=CARTESIAN_POINT('Ctrl Pts',(-2.34717466342319,68.3834492539409,14.2041450269218));
#45914=CARTESIAN_POINT('Ctrl Pts',(-2.47231368909138,68.4235361610872,13.7286746008922));
#45915=CARTESIAN_POINT('Ctrl Pts',(-2.49999759002584,68.4390631270895,13.5148895441053));
#45916=CARTESIAN_POINT('Ctrl Pts',(-2.49999999984276,68.453694114733,13.3000280391888));
#45917=CARTESIAN_POINT('Origin',(0.,70.2,13.3));
#45918=CARTESIAN_POINT('',(-2.5,63.5861738118246,13.3));
#45919=CARTESIAN_POINT('',(-2.5,64.7766865736815,13.2999999985417));
#45920=CARTESIAN_POINT('',(-2.5,70.2,13.3));
#45921=CARTESIAN_POINT('Ctrl Pts',(-2.5,64.7766865736815,13.2999999970835));
#45922=CARTESIAN_POINT('Ctrl Pts',(-2.49999999965576,64.8164008365653,13.0049246949997));
#45923=CARTESIAN_POINT('Ctrl Pts',(-2.44775725432166,64.855896686039,12.7120539935902));
#45924=CARTESIAN_POINT('Ctrl Pts',(-2.23481454245837,64.9376441713423,12.1346235687608));
#45925=CARTESIAN_POINT('Ctrl Pts',(-2.06735487938246,64.9800658702118,11.8582854382355));
#45926=CARTESIAN_POINT('Ctrl Pts',(-1.62784326520881,65.0667847652865,11.373375077376));
#45927=CARTESIAN_POINT('Ctrl Pts',(-1.35589850308388,65.1101015735457,11.1731892740713));
#45928=CARTESIAN_POINT('Ctrl Pts',(-0.749236115015228,65.1982470950867,
10.8915700195959));
#45929=CARTESIAN_POINT('Ctrl Pts',(-0.420611491999876,65.241294996556,10.8130324822582));
#45930=CARTESIAN_POINT('Ctrl Pts',(0.0722700300150027,65.3056861833212,
10.7960151635174));
#45931=CARTESIAN_POINT('Ctrl Pts',(0.230969399305698,65.3263938329972,10.8056426584217));
#45932=CARTESIAN_POINT('Ctrl Pts',(0.717892393503333,65.390532821863,10.8820766748746));
#45933=CARTESIAN_POINT('Ctrl Pts',(1.03439191845666,65.433173265611,10.9996139717914));
#45934=CARTESIAN_POINT('Ctrl Pts',(1.60248948455939,65.519743013992,11.3522268419152));
#45935=CARTESIAN_POINT('Ctrl Pts',(1.84834766112784,65.5621883103019,11.5837742387333));
#45936=CARTESIAN_POINT('Ctrl Pts',(2.13372005689657,65.625678982509,11.9874361549427));
#45937=CARTESIAN_POINT('Ctrl Pts',(2.21331029422729,65.6461981821876,12.1266098265435));
#45938=CARTESIAN_POINT('Ctrl Pts',(2.4164263685598,65.7095121501173,12.5771040557331));
#45939=CARTESIAN_POINT('Ctrl Pts',(2.4913221117068,65.7515893489608,12.906264654977));
#45940=CARTESIAN_POINT('Ctrl Pts',(2.50725549696481,65.8367710959168,13.5744797604832));
#45941=CARTESIAN_POINT('Ctrl Pts',(2.44815922708852,65.8786796610131,13.906802360106));
#45942=CARTESIAN_POINT('Ctrl Pts',(2.26683798631002,65.941188151735,14.3662878980475));
#45943=CARTESIAN_POINT('Ctrl Pts',(2.19408169130771,65.9613563491209,14.5089382612658));
#45944=CARTESIAN_POINT('Ctrl Pts',(1.92866174281978,66.0237002790106,14.9253809960834));
#45945=CARTESIAN_POINT('Ctrl Pts',(1.69444577020903,66.0652338265536,15.1682811507576));
#45946=CARTESIAN_POINT('Ctrl Pts',(1.28307061606148,66.1279136968628,15.4520142477283));
#45947=CARTESIAN_POINT('Ctrl Pts',(1.13770749664708,66.1486105514198,15.5322768763966));
#45948=CARTESIAN_POINT('Ctrl Pts',(0.837972295611676,66.1893788022971,15.660839261364));
#45949=CARTESIAN_POINT('Ctrl Pts',(0.68471636599104,66.2093617375317,15.7097562943906));
#45950=CARTESIAN_POINT('Ctrl Pts',(0.375294234782263,66.2488151249023,15.7765917640375));
#45951=CARTESIAN_POINT('Ctrl Pts',(0.220006241415938,66.2681970853179,15.7951856248744));
#45952=CARTESIAN_POINT('Ctrl Pts',(-0.271061763174914,66.3292938258388,
15.8077609983177));
#45953=CARTESIAN_POINT('Ctrl Pts',(-0.604471184224974,66.3705211903455,
15.7488730727342));
#45954=CARTESIAN_POINT('Ctrl Pts',(-1.21037029596744,66.4509066517408,15.510173913772));
#45955=CARTESIAN_POINT('Ctrl Pts',(-1.47978289942527,66.4893481870635,15.3396352947398));
#45956=CARTESIAN_POINT('Ctrl Pts',(-1.93196083231809,66.5657496062255,14.9155187257816));
#45957=CARTESIAN_POINT('Ctrl Pts',(-2.11389669558551,66.6028166560054,14.6688851926677));
#45958=CARTESIAN_POINT('Ctrl Pts',(-2.31646774840565,66.6591071355653,14.2534227207639));
#45959=CARTESIAN_POINT('Ctrl Pts',(-2.37215638311095,66.678258350027,14.1049304926687));
#45960=CARTESIAN_POINT('Ctrl Pts',(-2.47102083162873,66.7243196319004,13.7390717503395));
#45961=CARTESIAN_POINT('Ctrl Pts',(-2.5,66.7511646065957,13.5197658771335));
#45962=CARTESIAN_POINT('Ctrl Pts',(-2.5,66.7778885669818,13.3));
#45963=CARTESIAN_POINT('Ctrl Pts',(-2.5,65.696789585947,13.2999999999997));
#45964=CARTESIAN_POINT('Ctrl Pts',(-2.50000000000002,65.6606212395657,13.5476917468759));
#45965=CARTESIAN_POINT('Ctrl Pts',(-2.46320526908407,65.6259776293922,13.7945024697698));
#45966=CARTESIAN_POINT('Ctrl Pts',(-2.34675403472998,65.5682504655492,14.174556274757));
#45967=CARTESIAN_POINT('Ctrl Pts',(-2.29062164953506,65.5463543672022,14.312485993215));
#45968=CARTESIAN_POINT('Ctrl Pts',(-2.09627605640216,65.4828785527232,14.6898759582726));
#45969=CARTESIAN_POINT('Ctrl Pts',(-1.93020081276959,65.4407810355203,14.9126111261388));
#45970=CARTESIAN_POINT('Ctrl Pts',(-1.48931269496749,65.3522800206411,15.33573253192));
#45971=CARTESIAN_POINT('Ctrl Pts',(-1.20330963137783,65.3075904348623,15.5168712083578));
#45972=CARTESIAN_POINT('Ctrl Pts',(-0.583806940896402,65.2139673687482,
15.7528477763624));
#45973=CARTESIAN_POINT('Ctrl Pts',(-0.257803732388431,65.1662698905148,
15.8081282301965));
#45974=CARTESIAN_POINT('Ctrl Pts',(0.347315996248517,65.0794127826204,15.7913143648248));
#45975=CARTESIAN_POINT('Ctrl Pts',(0.621957310552961,65.0419753787324,15.737324534739));
#45976=CARTESIAN_POINT('Ctrl Pts',(1.18165338917458,64.9610831563909,15.5262297058993));
#45977=CARTESIAN_POINT('Ctrl Pts',(1.45651850407446,64.9175262604713,15.3568994673308));
#45978=CARTESIAN_POINT('Ctrl Pts',(1.86865997329142,64.8391995882492,14.9780108429671));
#45979=CARTESIAN_POINT('Ctrl Pts',(2.02111302776291,64.8055394947104,14.7909051061706));
#45980=CARTESIAN_POINT('Ctrl Pts',(2.31657298205842,64.7277876819778,14.2977508391837));
#45981=CARTESIAN_POINT('Ctrl Pts',(2.42923108392718,64.6848035235328,13.978942722645));
#45982=CARTESIAN_POINT('Ctrl Pts',(2.52015281979624,64.5977656973278,13.3308689765477));
#45983=CARTESIAN_POINT('Ctrl Pts',(2.50345875413146,64.5547767687459,13.0088120080675));
#45984=CARTESIAN_POINT('Ctrl Pts',(2.35075483869388,64.4700617407981,12.392593825506));
#45985=CARTESIAN_POINT('Ctrl Pts',(2.21768277196079,64.4299216122369,12.1035926913253));
#45986=CARTESIAN_POINT('Ctrl Pts',(1.85229888222638,64.3484960718886,11.5920563535047));
#45987=CARTESIAN_POINT('Ctrl Pts',(1.62401830993652,64.3077502366141,11.3737113160013));
#45988=CARTESIAN_POINT('Ctrl Pts',(1.18147612245848,64.2381881831123,11.0863720959783));
#45989=CARTESIAN_POINT('Ctrl Pts',(0.98719503872063,64.2100366034237,10.99315893442));
#45990=CARTESIAN_POINT('Ctrl Pts',(0.638182294179026,64.1625544867496,10.8779974120894));
#45991=CARTESIAN_POINT('Ctrl Pts',(0.488894506674402,64.1430428931642,10.8435055930678));
#45992=CARTESIAN_POINT('Ctrl Pts',(0.0191928557524364,64.0825479846592,
10.7795332818075));
#45993=CARTESIAN_POINT('Ctrl Pts',(-0.304380293821025,64.0420105464618,
10.7979070045178));
#45994=CARTESIAN_POINT('Ctrl Pts',(-0.937368490865787,63.9585250257917,
10.9587286875582));
#45995=CARTESIAN_POINT('Ctrl Pts',(-1.23968286156801,63.9165679531756,11.1037644527327));
#45996=CARTESIAN_POINT('Ctrl Pts',(-1.76645161829872,63.833499977726,11.5008412785666));
#45997=CARTESIAN_POINT('Ctrl Pts',(-1.98677737394653,63.7928727123624,11.7475622274495));
#45998=CARTESIAN_POINT('Ctrl Pts',(-2.30902557930508,63.7135869421685,12.2938209223983));
#45999=CARTESIAN_POINT('Ctrl Pts',(-2.41491369294374,63.6756793594576,12.5843141463113));
#46000=CARTESIAN_POINT('Ctrl Pts',(-2.48854959505432,63.6203739294691,13.0236138047583));
#46001=CARTESIAN_POINT('Ctrl Pts',(-2.5,63.6032428589473,13.1618533917633));
#46002=CARTESIAN_POINT('Ctrl Pts',(-2.5,63.5861738118246,13.3));
#46003=CARTESIAN_POINT('Origin',(0.,70.2,13.3));
#46004=CARTESIAN_POINT('',(-2.5,61.6106677866271,13.299999999999));
#46005=CARTESIAN_POINT('',(-2.5,62.5034831341457,13.3));
#46006=CARTESIAN_POINT('',(-2.5,70.2,13.3));
#46007=CARTESIAN_POINT('',(-0.95113387948199,62.8051682013071,10.9879645736141));
#46008=CARTESIAN_POINT('Ctrl Pts',(-2.5,62.5034831341457,13.3));
#46009=CARTESIAN_POINT('Ctrl Pts',(-2.5,62.5134432259226,13.2082675133545));
#46010=CARTESIAN_POINT('Ctrl Pts',(-2.49495101965816,62.5233554399033,13.1165445974971));
#46011=CARTESIAN_POINT('Ctrl Pts',(-2.45278266979642,62.5644149407621,12.7351703849783));
#46012=CARTESIAN_POINT('Ctrl Pts',(-2.3701642172966,62.5940975669794,12.4529177587687));
#46013=CARTESIAN_POINT('Ctrl Pts',(-2.0966825207848,62.6573818047408,11.9002278508217));
#46014=CARTESIAN_POINT('Ctrl Pts',(-1.89733435958966,62.691549647966,11.6399939848498));
#46015=CARTESIAN_POINT('Ctrl Pts',(-1.4454503030277,62.7519607742206,11.2414035082826));
#46016=CARTESIAN_POINT('Ctrl Pts',(-1.20800434745213,62.7781618468012,11.0936720557263));
#46017=CARTESIAN_POINT('Ctrl Pts',(-0.951119787994485,62.8051408818796,
10.9879941287087));
#46018=CARTESIAN_POINT('Ctrl Pts',(-0.951158341752456,62.8053674325562,
10.9880099894431));
#46019=CARTESIAN_POINT('Ctrl Pts',(-0.748346167324441,62.8492893880777,
10.904572565131));
#46020=CARTESIAN_POINT('Ctrl Pts',(-0.535268424204013,62.8917771650403,
10.8481154674408));
#46021=CARTESIAN_POINT('Ctrl Pts',(-0.0889495945967942,62.9804306988286,
10.7909909524606));
#46022=CARTESIAN_POINT('Ctrl Pts',(0.142613438430281,63.0260526474146,10.7934352654522));
#46023=CARTESIAN_POINT('Ctrl Pts',(0.699104733539934,63.1294345358272,10.8768801767992));
#46024=CARTESIAN_POINT('Ctrl Pts',(1.01495953001673,63.1833347447265,10.991118965619));
#46025=CARTESIAN_POINT('Ctrl Pts',(1.54273258886205,63.290342160986,11.3123026100822));
#46026=CARTESIAN_POINT('Ctrl Pts',(1.75905112041114,63.3401990429101,11.5008112959782));
#46027=CARTESIAN_POINT('Ctrl Pts',(2.14172120523175,63.4396702711262,11.9710484837984));
#46028=CARTESIAN_POINT('Ctrl Pts',(2.29464284649186,63.4904376972501,12.2569608158226));
#46029=CARTESIAN_POINT('Ctrl Pts',(2.47662564756037,63.5890843688263,12.8478464586179));
#46030=CARTESIAN_POINT('Ctrl Pts',(2.51282222328703,63.6351455260115,13.14498589657));
#46031=CARTESIAN_POINT('Ctrl Pts',(2.47864321403863,63.7269539372175,13.7471624079164));
#46032=CARTESIAN_POINT('Ctrl Pts',(2.40535918588835,63.7738565060348,14.0469516213565));
#46033=CARTESIAN_POINT('Ctrl Pts',(2.21256971785119,63.844126463776,14.4752928707189));
#46034=CARTESIAN_POINT('Ctrl Pts',(2.13090646374222,63.8681490390869,14.6175867503245));
#46035=CARTESIAN_POINT('Ctrl Pts',(1.94168182561234,63.9163656631226,14.8831073813957));
#46036=CARTESIAN_POINT('Ctrl Pts',(1.83480669666587,63.9404276085913,15.0058259153776));
#46037=CARTESIAN_POINT('Ctrl Pts',(1.47875293674026,64.0126768939748,15.3421845921755));
#46038=CARTESIAN_POINT('Ctrl Pts',(1.19884115664813,64.0585668993632,15.5181273955644));
#46039=CARTESIAN_POINT('Ctrl Pts',(0.745927806343105,64.1282335562372,15.691304811016));
#46040=CARTESIAN_POINT('Ctrl Pts',(0.594008037624197,64.1508934864502,15.733496942561));
#46041=CARTESIAN_POINT('Ctrl Pts',(0.277723065736383,64.1966550626599,15.7899295768095));
#46042=CARTESIAN_POINT('Ctrl Pts',(0.113863356180166,64.2196131224913,15.8027837998128));
#46043=CARTESIAN_POINT('Ctrl Pts',(-0.215059461004993,64.2660254171419,
15.7961921332998));
#46044=CARTESIAN_POINT('Ctrl Pts',(-0.379294277305768,64.2893611369709,
15.7765617810483));
#46045=CARTESIAN_POINT('Ctrl Pts',(-0.857227760767255,64.3585474097511,
15.6707529771788));
#46046=CARTESIAN_POINT('Ctrl Pts',(-1.15743174475583,64.4025777893146,15.5395829385504));
#46047=CARTESIAN_POINT('Ctrl Pts',(-1.55565506513275,64.4695488243418,15.263545430248));
#46048=CARTESIAN_POINT('Ctrl Pts',(-1.67804127748925,64.4917087080322,15.1600409967452));
#46049=CARTESIAN_POINT('Ctrl Pts',(-1.90299735637489,64.5360832026101,14.9293956022825));
#46050=CARTESIAN_POINT('Ctrl Pts',(-2.00471820278112,64.5580814761814,14.8024784541755));
#46051=CARTESIAN_POINT('Ctrl Pts',(-2.26248951748846,64.6223594959449,14.4076066676219));
#46052=CARTESIAN_POINT('Ctrl Pts',(-2.38204455263811,64.6646992209118,14.11947654915));
#46053=CARTESIAN_POINT('Ctrl Pts',(-2.47995802895167,64.728787571935,13.6560923109532));
#46054=CARTESIAN_POINT('Ctrl Pts',(-2.49799735875449,64.750796444763,13.4923763989412));
#46055=CARTESIAN_POINT('Ctrl Pts',(-2.49994748911428,64.7741681509402,13.3187124487616));
#46056=CARTESIAN_POINT('Ctrl Pts',(-2.50000000001091,64.7754274660069,13.3093551141232));
#46057=CARTESIAN_POINT('Ctrl Pts',(-2.5,64.7766865736815,13.2999999970835));
#46058=CARTESIAN_POINT('',(-1.05593533999082,62.1312800345432,11.0339552088038));
#46059=CARTESIAN_POINT('Ctrl Pts',(-2.5,63.5861738118246,13.3));
#46060=CARTESIAN_POINT('Ctrl Pts',(-2.5,63.5618355279943,13.4969794410489));
#46061=CARTESIAN_POINT('Ctrl Pts',(-2.47671861934085,63.5376308222105,13.6937707697339));
#46062=CARTESIAN_POINT('Ctrl Pts',(-2.35237461690196,63.4726961590915,14.209267299241));
#46063=CARTESIAN_POINT('Ctrl Pts',(-2.21081146089628,63.4326027026238,14.5135737800926));
#46064=CARTESIAN_POINT('Ctrl Pts',(-1.83677979572786,63.3557031742944,15.0220899791508));
#46065=CARTESIAN_POINT('Ctrl Pts',(-1.61788509968431,63.3198464727878,15.2292071572241));
#46066=CARTESIAN_POINT('Ctrl Pts',(-1.23633831161108,63.2651741875956,15.4785444763662));
#46067=CARTESIAN_POINT('Ctrl Pts',(-1.09729487286071,63.2464608355503,15.5517842501154));
#46068=CARTESIAN_POINT('Ctrl Pts',(-0.65304333740367,63.1888084607364,15.7348093327135));
#46069=CARTESIAN_POINT('Ctrl Pts',(-0.332619401530084,63.1503506761926,
15.7988360913035));
#46070=CARTESIAN_POINT('Ctrl Pts',(0.149764845495188,63.0935063297738,15.8005468611102));
#46071=CARTESIAN_POINT('Ctrl Pts',(0.308094869727977,63.0749797054085,15.7860098994124));
#46072=CARTESIAN_POINT('Ctrl Pts',(0.793028183159608,63.0171521241753,15.6944185410486));
#46073=CARTESIAN_POINT('Ctrl Pts',(1.10628083734864,62.9778276726596,15.5667840736932));
#46074=CARTESIAN_POINT('Ctrl Pts',(1.6421354944158,62.9032050294953,15.2101635679604));
#46075=CARTESIAN_POINT('Ctrl Pts',(1.86528134142054,62.868495484353,14.992948509786));
#46076=CARTESIAN_POINT('Ctrl Pts',(2.22589220972072,62.796441996323,14.4814847880212));
#46077=CARTESIAN_POINT('Ctrl Pts',(2.35766988115371,62.7602485560122,14.18993062246));
#46078=CARTESIAN_POINT('Ctrl Pts',(2.46841211352946,62.7069325753515,13.7268655699382));
#46079=CARTESIAN_POINT('Ctrl Pts',(2.49055727223028,62.6893607887676,13.5690734070085));
#46080=CARTESIAN_POINT('Ctrl Pts',(2.51231105272378,62.6345021586197,13.0762421278448));
#46081=CARTESIAN_POINT('Ctrl Pts',(2.4599096092195,62.596869803934,12.7426248548224));
#46082=CARTESIAN_POINT('Ctrl Pts',(2.23536643917119,62.5263208200567,12.1383733469182));
#46083=CARTESIAN_POINT('Ctrl Pts',(2.07411883505748,62.4938036036167,11.8702147044956));
#46084=CARTESIAN_POINT('Ctrl Pts',(1.66115536010345,62.4262744560102,11.4059731185847));
#46085=CARTESIAN_POINT('Ctrl Pts',(1.4127414065054,62.3927876344703,11.2140810921841));
#46086=CARTESIAN_POINT('Ctrl Pts',(0.994382633338479,62.3440182625655,11.0008126638597));
#46087=CARTESIAN_POINT('Ctrl Pts',(0.846837094673137,62.3278983183272,10.9424737002965));
#46088=CARTESIAN_POINT('Ctrl Pts',(0.384509880431944,62.278476354872,10.8087226587651));
#46089=CARTESIAN_POINT('Ctrl Pts',(0.059763906012211,62.2444794544955,10.7799212919263));
#46090=CARTESIAN_POINT('Ctrl Pts',(-0.536687791893848,62.1843125767197,
10.8426602317689));
#46091=CARTESIAN_POINT('Ctrl Pts',(-0.80512551759084,62.1581728462725,10.9170737303865));
#46092=CARTESIAN_POINT('Ctrl Pts',(-1.0559353435001,62.1312734393566,11.0339460398421));
#46093=CARTESIAN_POINT('Ctrl Pts',(-1.05588007528467,62.1309604529623,11.0339202867911));
#46094=CARTESIAN_POINT('Ctrl Pts',(-1.28187597354016,62.0803724841633,11.1392230988119));
#46095=CARTESIAN_POINT('Ctrl Pts',(-1.49124228115003,62.031193003458,11.2779710600194));
#46096=CARTESIAN_POINT('Ctrl Pts',(-1.90685064701863,61.9225543060576,11.6536992054081));
#46097=CARTESIAN_POINT('Ctrl Pts',(-2.09635136197059,61.8672490886137,11.902875871808));
#46098=CARTESIAN_POINT('Ctrl Pts',(-2.36481197668388,61.7591668280173,12.4391365608076));
#46099=CARTESIAN_POINT('Ctrl Pts',(-2.44852088510863,61.7086069741114,12.7181463211823));
#46100=CARTESIAN_POINT('Ctrl Pts',(-2.4942115345676,61.6434985370641,13.1034831108955));
#46101=CARTESIAN_POINT('Ctrl Pts',(-2.49999999999992,61.6270837917359,13.2017877758211));
#46102=CARTESIAN_POINT('Ctrl Pts',(-2.5,61.6106677866271,13.299999999998));
#46103=CARTESIAN_POINT('Origin',(0.,70.2,13.3));
#46104=CARTESIAN_POINT('',(-2.5,59.3994433450696,13.3));
#46105=CARTESIAN_POINT('',(-2.50005097985869,60.6167707974153,13.3003061727703));
#46106=CARTESIAN_POINT('',(-2.5,70.2,13.3));
#46107=CARTESIAN_POINT('Ctrl Pts',(-2.49999998106492,60.6167825252036,13.3003076936568));
#46108=CARTESIAN_POINT('Ctrl Pts',(-2.50003167432271,60.6503069125688,13.0428011051694));
#46109=CARTESIAN_POINT('Ctrl Pts',(-2.46027730575809,60.6836579553173,12.786819843935));
#46110=CARTESIAN_POINT('Ctrl Pts',(-2.29644321278257,60.7536512825819,12.2723264854255));
#46111=CARTESIAN_POINT('Ctrl Pts',(-2.16575661142914,60.7895694189813,12.0196521562626));
#46112=CARTESIAN_POINT('Ctrl Pts',(-1.89997952644266,60.8460870435028,11.6674296411658));
#46113=CARTESIAN_POINT('Ctrl Pts',(-1.79248929773588,60.8663775023704,11.5500881844077));
#46114=CARTESIAN_POINT('Ctrl Pts',(-1.43354632066325,60.9282128096194,11.2262737701675));
#46115=CARTESIAN_POINT('Ctrl Pts',(-1.15240914753211,60.9691002371946,11.0578176679183));
#46116=CARTESIAN_POINT('Ctrl Pts',(-0.555685804014866,61.0493877044964,
10.8429651857453));
#46117=CARTESIAN_POINT('Ctrl Pts',(-0.247484298851549,61.0881331015775,
10.7930928430669));
#46118=CARTESIAN_POINT('Ctrl Pts',(0.231228210956693,61.1482337357571,10.8049662505859));
#46119=CARTESIAN_POINT('Ctrl Pts',(0.399612079283944,61.1693637168444,10.826343877124));
#46120=CARTESIAN_POINT('Ctrl Pts',(0.862306460298472,61.2286679117027,10.9335989626459));
#46121=CARTESIAN_POINT('Ctrl Pts',(1.14491670061985,61.2663615499773,11.0566516905333));
#46122=CARTESIAN_POINT('Ctrl Pts',(1.53566880802269,61.3248000057025,11.3203091326199));
#46123=CARTESIAN_POINT('Ctrl Pts',(1.66347295866566,61.3452538209656,11.4264160646674));
#46124=CARTESIAN_POINT('Ctrl Pts',(2.0142493549841,61.4068455850894,11.7820336132132));
#46125=CARTESIAN_POINT('Ctrl Pts',(2.19872426078175,61.4472436498982,12.0642538241026));
#46126=CARTESIAN_POINT('Ctrl Pts',(2.37977989143596,61.5068727069176,12.5185127945139));
#46127=CARTESIAN_POINT('Ctrl Pts',(2.42368541458096,61.5257723766018,12.6676831439235));
#46128=CARTESIAN_POINT('Ctrl Pts',(2.51698705120129,61.5849334691689,13.1445457620724));
#46129=CARTESIAN_POINT('Ctrl Pts',(2.51546320204714,61.6244248978137,13.4785687636092));
#46130=CARTESIAN_POINT('Ctrl Pts',(2.38421848069762,61.7025293376362,14.1180243412869));
#46131=CARTESIAN_POINT('Ctrl Pts',(2.25916099771928,61.7408909013013,14.4179751268707));
#46132=CARTESIAN_POINT('Ctrl Pts',(1.91668378618502,61.8144096986113,14.9321171412022));
#46133=CARTESIAN_POINT('Ctrl Pts',(1.71030723496061,61.8487793672088,15.1472590005306));
#46134=CARTESIAN_POINT('Ctrl Pts',(1.20040881389063,61.9226347869468,15.5183592177604));
#46135=CARTESIAN_POINT('Ctrl Pts',(0.892840490250037,61.96191338326,15.6590194630925));
#46136=CARTESIAN_POINT('Ctrl Pts',(0.262417594039295,62.0368102437113,15.8057398815962));
#46137=CARTESIAN_POINT('Ctrl Pts',(-0.0524529815479305,62.0718865390332,
15.8188997708182));
#46138=CARTESIAN_POINT('Ctrl Pts',(-0.671634931442725,62.1439398580234,
15.7283921689737));
#46139=CARTESIAN_POINT('Ctrl Pts',(-0.970482295014021,62.1796355811393,
15.6251724561424));
#46140=CARTESIAN_POINT('Ctrl Pts',(-1.38124944674192,62.232582959014,15.3899086427978));
#46141=CARTESIAN_POINT('Ctrl Pts',(-1.51206128228296,62.250243219615,15.2973084796327));
#46142=CARTESIAN_POINT('Ctrl Pts',(-1.88618394378343,62.3052287457407,14.9745185526001));
#46143=CARTESIAN_POINT('Ctrl Pts',(-2.09292902595285,62.3428443665707,14.7076243431039));
#46144=CARTESIAN_POINT('Ctrl Pts',(-2.37990882752752,62.4136135517456,14.1271384734215));
#46145=CARTESIAN_POINT('Ctrl Pts',(-2.46472935062807,62.446468573607,13.8227282112553));
#46146=CARTESIAN_POINT('Ctrl Pts',(-2.49703912277934,62.4882012010445,13.4405024502384));
#46147=CARTESIAN_POINT('Ctrl Pts',(-2.5,62.4958557361002,13.3702483676872));
#46148=CARTESIAN_POINT('Ctrl Pts',(-2.5,62.5034831341457,13.3));
#46149=CARTESIAN_POINT('Ctrl Pts',(-2.5,61.6106677866271,13.2999999999979));
#46150=CARTESIAN_POINT('Ctrl Pts',(-2.50000000000017,61.5753977216309,13.5110106269549));
#46151=CARTESIAN_POINT('Ctrl Pts',(-2.47328881942191,61.5399743614456,13.7215699957689));
#46152=CARTESIAN_POINT('Ctrl Pts',(-2.34086749087818,61.4536198113013,14.2329923829222));
#46153=CARTESIAN_POINT('Ctrl Pts',(-2.20399523672876,61.4032180149517,14.5217670579512));
#46154=CARTESIAN_POINT('Ctrl Pts',(-1.83146316933345,61.3029540924801,15.0303651257921));
#46155=CARTESIAN_POINT('Ctrl Pts',(-1.60020023359404,61.2571020417161,15.2462503961835));
#46156=CARTESIAN_POINT('Ctrl Pts',(-1.07677625810136,61.1639043490878,15.5767667070598));
#46157=CARTESIAN_POINT('Ctrl Pts',(-0.791217250734542,61.1166318477133,
15.6910244293695));
#46158=CARTESIAN_POINT('Ctrl Pts',(-0.162002177805606,61.0205089410304,
15.8173747927169));
#46159=CARTESIAN_POINT('Ctrl Pts',(0.178249166057133,60.9738822900553,15.8163040584398));
#46160=CARTESIAN_POINT('Ctrl Pts',(0.661210841276149,60.9016095528027,15.716034411891));
#46161=CARTESIAN_POINT('Ctrl Pts',(0.810899553950083,60.8784850141691,15.66999065206));
#46162=CARTESIAN_POINT('Ctrl Pts',(1.2338256231954,60.8110986230562,15.4951128133702));
#46163=CARTESIAN_POINT('Ctrl Pts',(1.48928700482673,60.7690305034994,15.330514957981));
#46164=CARTESIAN_POINT('Ctrl Pts',(1.94055110680696,60.6820145210843,14.9076771002005));
#46165=CARTESIAN_POINT('Ctrl Pts',(2.12846386403743,60.6375835412521,14.6490782544425));
#46166=CARTESIAN_POINT('Ctrl Pts',(2.40528866024503,60.5466316330392,14.0593351017857));
#46167=CARTESIAN_POINT('Ctrl Pts',(2.48523782949149,60.5013429511135,13.730853322367));
#46168=CARTESIAN_POINT('Ctrl Pts',(2.5107276025244,60.4097155920456,13.0701376918266));
#46169=CARTESIAN_POINT('Ctrl Pts',(2.45928938940062,60.3658637000904,12.7445343508971));
#46170=CARTESIAN_POINT('Ctrl Pts',(2.29143638730971,60.299482163651,12.2875788530185));
#46171=CARTESIAN_POINT('Ctrl Pts',(2.22185050580503,60.277588760923,12.1428227299824));
#46172=CARTESIAN_POINT('Ctrl Pts',(1.96568075416499,60.2103221284824,11.7194831123215));
#46173=CARTESIAN_POINT('Ctrl Pts',(1.73674823198205,60.1661649256645,11.4708829128064));
#46174=CARTESIAN_POINT('Ctrl Pts',(1.20107551719154,60.0770022268735,11.0832234339517));
#46175=CARTESIAN_POINT('Ctrl Pts',(0.901469739307313,60.0340434543022,10.9454136203066));
#46176=CARTESIAN_POINT('Ctrl Pts',(0.286501669427965,59.9498332087379,10.7977189146826));
#46177=CARTESIAN_POINT('Ctrl Pts',(-0.0214358916469852,59.9093592186135,
10.7814543511458));
#46178=CARTESIAN_POINT('Ctrl Pts',(-0.639429444520793,59.8273145602628,
10.8623987714831));
#46179=CARTESIAN_POINT('Ctrl Pts',(-0.943485454479146,59.7856405535461,
10.9632049556967));
#46180=CARTESIAN_POINT('Ctrl Pts',(-1.36462591161955,59.722341325843,11.1987964870087));
#46181=CARTESIAN_POINT('Ctrl Pts',(-1.50038760761804,59.7008903977335,11.2934850410936));
#46182=CARTESIAN_POINT('Ctrl Pts',(-1.7495610949226,59.6580734504445,11.5067993877266));
#46183=CARTESIAN_POINT('Ctrl Pts',(-1.86264971926353,59.6368153223749,11.6245694910179));
#46184=CARTESIAN_POINT('Ctrl Pts',(-2.17060216608482,59.5718096871366,12.0153003709833));
#46185=CARTESIAN_POINT('Ctrl Pts',(-2.32288678666953,59.5290983426027,12.3170477084673));
#46186=CARTESIAN_POINT('Ctrl Pts',(-2.45341481384624,59.4651200924951,12.7937991660323));
#46187=CARTESIAN_POINT('Ctrl Pts',(-2.48072617625929,59.4444711572715,12.9514556000494));
#46188=CARTESIAN_POINT('Ctrl Pts',(-2.49761161611624,59.4156963943897,13.1737417293526));
#46189=CARTESIAN_POINT('Ctrl Pts',(-2.5,59.4075609409309,13.2369073430154));
#46190=CARTESIAN_POINT('Ctrl Pts',(-2.5,59.3994433450696,13.3));
#46191=CARTESIAN_POINT('Origin',(0.,70.2,13.3));
#46192=CARTESIAN_POINT('',(-2.5,57.4769927816046,13.3));
#46193=CARTESIAN_POINT('',(-2.49999999761251,58.4092448555943,13.3001092586366));
#46194=CARTESIAN_POINT('',(-2.5,70.2,13.3));
#46195=CARTESIAN_POINT('',(-1.71831766398917,58.6398093087261,11.4856494580447));
#46196=CARTESIAN_POINT('Ctrl Pts',(-2.5,58.4092574955175,13.3000000000002));
#46197=CARTESIAN_POINT('Ctrl Pts',(-2.5,58.4285081348677,13.1335985253904));
#46198=CARTESIAN_POINT('Ctrl Pts',(-2.48338644354128,58.4475613350895,12.9676028553435));
#46199=CARTESIAN_POINT('Ctrl Pts',(-2.41623371863719,58.4863852419782,12.6355231449167));
#46200=CARTESIAN_POINT('Ctrl Pts',(-2.36468214575892,58.5061348190271,12.4705448459811));
#46201=CARTESIAN_POINT('Ctrl Pts',(-2.22765497520508,58.5457343700435,12.1519709352431));
#46202=CARTESIAN_POINT('Ctrl Pts',(-2.14215917281841,58.5654413971552,11.9993906346628));
#46203=CARTESIAN_POINT('Ctrl Pts',(-1.94650672128539,58.6034839248316,11.722604870779));
#46204=CARTESIAN_POINT('Ctrl Pts',(-1.83851610981518,58.6217439894937,11.5979641222271));
#46205=CARTESIAN_POINT('Ctrl Pts',(-1.71906196354253,58.64008093262,11.4848344523154));
#46206=CARTESIAN_POINT('Ctrl Pts',(-1.71827827352178,58.6398165637634,11.4856099157301));
#46207=CARTESIAN_POINT('Ctrl Pts',(-1.67168277133379,58.6506632299144,11.4415863705764));
#46208=CARTESIAN_POINT('Ctrl Pts',(-1.62358535300898,58.6613329356252,11.3993011150436));
#46209=CARTESIAN_POINT('Ctrl Pts',(-1.5740109869715,58.6720612790877,11.3589698018563));
#46210=CARTESIAN_POINT('Ctrl Pts',(-1.55542295036543,58.6760838991824,11.343847471793));
#46211=CARTESIAN_POINT('Ctrl Pts',(-1.53662750959264,58.6801146947408,11.3290003063795));
#46212=CARTESIAN_POINT('Ctrl Pts',(-1.51762695332325,58.6841658372305,11.3144412813472));
#46213=CARTESIAN_POINT('Ctrl Pts',(-1.44725522850215,58.6991699181874,11.2605195072315));
#46214=CARTESIAN_POINT('Ctrl Pts',(-1.37420002501608,58.7141619361767,11.2103505537322));
#46215=CARTESIAN_POINT('Ctrl Pts',(-1.2987892723116,58.7291444985975,11.1641594431883));
#46216=CARTESIAN_POINT('Ctrl Pts',(-1.22407694124179,58.7439882990333,11.1183961346458));
#46217=CARTESIAN_POINT('Ctrl Pts',(-1.14705267636555,58.7588225370595,11.076536897693));
#46218=CARTESIAN_POINT('Ctrl Pts',(-1.06800390276438,58.7736204504448,11.0388066892096));
#46219=CARTESIAN_POINT('Ctrl Pts',(-1.0053145409205,58.7853558854742,11.008884875318));
#46220=CARTESIAN_POINT('Ctrl Pts',(-0.941351322191961,58.7970678425373,
10.9815597990238));
#46221=CARTESIAN_POINT('Ctrl Pts',(-0.876242310501115,58.8087316248811,
10.9569505145643));
#46222=CARTESIAN_POINT('Ctrl Pts',(-0.800964081422921,58.8222171448789,
10.9284975661185));
#46223=CARTESIAN_POINT('Ctrl Pts',(-0.724519456047828,58.8355729945648,
10.9038121138826));
#46224=CARTESIAN_POINT('Ctrl Pts',(-0.647114574550911,58.8487502606411,
10.8829842087397));
#46225=CARTESIAN_POINT('Ctrl Pts',(-0.639468270488092,58.8500519535213,
10.8809267610357));
#46226=CARTESIAN_POINT('Ctrl Pts',(-0.631812560411286,58.8513519060032,
10.8789069777978));
#46227=CARTESIAN_POINT('Ctrl Pts',(-0.624147619917967,58.8526500724191,
10.8769249611432));
#46228=CARTESIAN_POINT('Ctrl Pts',(-0.587811188157204,58.8588041626469,
10.8675290091486));
#46229=CARTESIAN_POINT('Ctrl Pts',(-0.551267549895413,58.8649179004233,
10.8589815057862));
#46230=CARTESIAN_POINT('Ctrl Pts',(-0.514534554199861,58.8709857720265,
10.8512937498166));
#46231=CARTESIAN_POINT('Ctrl Pts',(-0.514459951384814,58.87099809556,10.8512781363817));
#46232=CARTESIAN_POINT('Ctrl Pts',(-0.514385347791356,58.8710104189047,
10.8512625264951));
#46233=CARTESIAN_POINT('Ctrl Pts',(-0.514310743419481,58.8710227420607,
10.8512469201572));
#46234=CARTESIAN_POINT('Ctrl Pts',(-0.430731462675848,58.8848283742604,
10.8337631391232));
#46235=CARTESIAN_POINT('Ctrl Pts',(-0.346173773906837,58.8983975898941,
10.8207279432178));
#46236=CARTESIAN_POINT('Ctrl Pts',(-0.260978977584018,58.911854953297,10.8121073648089));
#46237=CARTESIAN_POINT('Ctrl Pts',(-0.178135598296444,58.9249408870479,
10.8037247184781));
#46238=CARTESIAN_POINT('Ctrl Pts',(-0.094689111867007,58.9379215364864,
10.7995176207406));
#46239=CARTESIAN_POINT('Ctrl Pts',(-0.0109716505076562,58.950890909248,
10.799488647867));
#46240=CARTESIAN_POINT('Ctrl Pts',(-0.00631521864721163,58.9516122760878,
10.7994870363727));
#46241=CARTESIAN_POINT('Ctrl Pts',(-0.00165795546027684,58.9523336071144,
10.7994983620118));
#46242=CARTESIAN_POINT('Ctrl Pts',(0.00300007929513795,58.9530549181748,
10.7995226291543));
#46243=CARTESIAN_POINT('Ctrl Pts',(0.0364730885342065,58.9582383169807,
10.7996970147757));
#46244=CARTESIAN_POINT('Ctrl Pts',(0.0699860464254556,58.9634204505794,
10.8005393829189));
#46245=CARTESIAN_POINT('Ctrl Pts',(0.103516510062052,58.9686061984143,10.8020510141029));
#46246=CARTESIAN_POINT('Ctrl Pts',(0.191067906454456,58.9821467050178,10.8059980344132));
#46247=CARTESIAN_POINT('Ctrl Pts',(0.278280705036573,58.9956442394026,10.814486745742));
#46248=CARTESIAN_POINT('Ctrl Pts',(0.36475353336839,59.0091613741268,10.8274087422704));
#46249=CARTESIAN_POINT('Ctrl Pts',(0.452514906646568,59.0228799297594,10.8405232914613));
#46250=CARTESIAN_POINT('Ctrl Pts',(0.53951370060598,59.036618702049,10.8582045625988));
#46251=CARTESIAN_POINT('Ctrl Pts',(0.625334894065203,59.0504062987958,10.8803525144015));
#46252=CARTESIAN_POINT('Ctrl Pts',(0.711016321799679,59.0641714414916,10.9024643967393));
#46253=CARTESIAN_POINT('Ctrl Pts',(0.795523583189255,59.077985064378,10.9290282286279));
#46254=CARTESIAN_POINT('Ctrl Pts',(0.878454469038144,59.0918405742896,10.959956495412));
#46255=CARTESIAN_POINT('Ctrl Pts',(0.943779983616589,59.1027547024272,10.9843190103184));
#46256=CARTESIAN_POINT('Ctrl Pts',(1.00812761085416,59.113694076328,11.011389659825));
#46257=CARTESIAN_POINT('Ctrl Pts',(1.07130720503626,59.124641521194,11.0411336050755));
#46258=CARTESIAN_POINT('Ctrl Pts',(1.14502710516054,59.1374153376861,11.0758397582497));
#46259=CARTESIAN_POINT('Ctrl Pts',(1.21679595895508,59.1501382469946,11.1140152441909));
#46260=CARTESIAN_POINT('Ctrl Pts',(1.28638304892513,59.1627657238264,11.1555235388176));
#46261=CARTESIAN_POINT('Ctrl Pts',(1.2927845440097,59.1639273578436,11.1593419934208));
#46262=CARTESIAN_POINT('Ctrl Pts',(1.29916758597747,59.1650881863615,11.1631886872241));
#46263=CARTESIAN_POINT('Ctrl Pts',(1.30553200080499,59.166248176004,11.1670635353192));
#46264=CARTESIAN_POINT('Ctrl Pts',(1.37291006161506,59.1785286220133,11.2080853350687));
#46265=CARTESIAN_POINT('Ctrl Pts',(1.43820025096216,59.1907143811178,11.25225816944));
#46266=CARTESIAN_POINT('Ctrl Pts',(1.50121024247637,59.2027530099914,11.2994955979673));
#46267=CARTESIAN_POINT('Ctrl Pts',(1.50839977487922,59.2041266351943,11.3048854578112));
#46268=CARTESIAN_POINT('Ctrl Pts',(1.5155596272048,59.2054983486907,11.3103152715227));
#46269=CARTESIAN_POINT('Ctrl Pts',(1.52268951705691,59.206868075529,11.3157849541186));
#46270=CARTESIAN_POINT('Ctrl Pts',(1.53622473082987,59.2094683324685,11.3261684698169));
#46271=CARTESIAN_POINT('Ctrl Pts',(1.54965199117437,59.2120613804525,11.3366956126132));
#46272=CARTESIAN_POINT('Ctrl Pts',(1.56296939946788,59.2146466487011,11.3473658306531));
#46273=CARTESIAN_POINT('Ctrl Pts',(1.56300888168497,59.2146543132646,11.347397464726));
#46274=CARTESIAN_POINT('Ctrl Pts',(1.56304836293562,59.21466197776,11.3474291000564));
#46275=CARTESIAN_POINT('Ctrl Pts',(1.5630878432197,59.2146696421874,11.3474607366442));
#46276=CARTESIAN_POINT('Ctrl Pts',(1.62498333468977,59.2266856017106,11.3970592184399));
#46277=CARTESIAN_POINT('Ctrl Pts',(1.68450744753681,59.2385345056002,11.4497473619077));
#46278=CARTESIAN_POINT('Ctrl Pts',(1.74149536111069,59.2503104816428,11.5053325961441));
#46279=CARTESIAN_POINT('Ctrl Pts',(1.74713357180979,59.2514755608666,11.5108320300193));
#46280=CARTESIAN_POINT('Ctrl Pts',(1.75274691561814,59.2526399229283,11.5163598294427));
#46281=CARTESIAN_POINT('Ctrl Pts',(1.75833520571778,59.2538036567991,11.5219158116712));
#46282=CARTESIAN_POINT('Ctrl Pts',(1.79515167104113,59.2614705042492,11.5585194280552));
#46283=CARTESIAN_POINT('Ctrl Pts',(1.83088173082515,59.2691099214016,11.5963461675733));
#46284=CARTESIAN_POINT('Ctrl Pts',(1.86546985158908,59.2767442297419,11.6353424213068));
#46285=CARTESIAN_POINT('Ctrl Pts',(1.92317617836415,59.2894812007614,11.7004032141815));
#46286=CARTESIAN_POINT('Ctrl Pts',(1.97740579089471,59.3021394830516,11.7683814677034));
#46287=CARTESIAN_POINT('Ctrl Pts',(2.02797839793939,59.3148007611641,11.8389300574549));
#46288=CARTESIAN_POINT('Ctrl Pts',(2.07947086483033,59.3276923339364,11.9107618481074));
#46289=CARTESIAN_POINT('Ctrl Pts',(2.12717125216542,59.3405871608286,11.9852585855909));
#46290=CARTESIAN_POINT('Ctrl Pts',(2.17087373687153,59.3535372860957,12.0620537631012));
#46291=CARTESIAN_POINT('Ctrl Pts',(2.21483013926339,59.3665626534425,12.1392951315749));
#46292=CARTESIAN_POINT('Ctrl Pts',(2.25474142351539,59.3796439165231,12.2188614005462));
#46293=CARTESIAN_POINT('Ctrl Pts',(2.29039399640346,59.3927990942328,12.300380149045));
#46294=CARTESIAN_POINT('Ctrl Pts',(2.31841991380376,59.4031401690561,12.3644607336126));
#46295=CARTESIAN_POINT('Ctrl Pts',(2.34381422166481,59.4135261815954,12.429747660825));
#46296=CARTESIAN_POINT('Ctrl Pts',(2.36647381168078,59.4239515112605,12.4960633986888));
#46297=CARTESIAN_POINT('Ctrl Pts',(2.39355470089487,59.4364110128439,12.5753185462432));
#46298=CARTESIAN_POINT('Ctrl Pts',(2.41659439458519,59.448864999823,12.6556462291611));
#46299=CARTESIAN_POINT('Ctrl Pts',(2.43554026660505,59.4612821491933,12.7367302669068));
#46300=CARTESIAN_POINT('Ctrl Pts',(2.43677049553403,59.4620884428468,12.7419953678643));
#46301=CARTESIAN_POINT('Ctrl Pts',(2.43798345428773,59.462894582159,12.7472636737242));
#46302=CARTESIAN_POINT('Ctrl Pts',(2.4391791245498,59.4637005589631,12.7525351043601));
#46303=CARTESIAN_POINT('Ctrl Pts',(2.45699519767812,59.4757100085065,12.8310820053568));
#46304=CARTESIAN_POINT('Ctrl Pts',(2.47097570716193,59.4876827505012,12.9103191771994));
#46305=CARTESIAN_POINT('Ctrl Pts',(2.48106971641073,59.4995755236576,12.9900022613495));
#46306=CARTESIAN_POINT('Ctrl Pts',(2.48200456958852,59.500676968733,12.9973820826473));
#46307=CARTESIAN_POINT('Ctrl Pts',(2.48290606404071,59.5017777304834,13.0047657580969));
#46308=CARTESIAN_POINT('Ctrl Pts',(2.48377414493789,59.5028777761427,13.012153111169));
#46309=CARTESIAN_POINT('Ctrl Pts',(2.49281344617476,59.5143325197286,13.0890774047206));
#46310=CARTESIAN_POINT('Ctrl Pts',(2.49823326059392,59.5257089156831,13.1663976070584));
#46311=CARTESIAN_POINT('Ctrl Pts',(2.49996888262786,59.5369602010634,13.2439331579682));
#46312=CARTESIAN_POINT('Ctrl Pts',(2.50014131000419,59.5380779730095,13.2516360168595));
#46313=CARTESIAN_POINT('Ctrl Pts',(2.50027734442346,59.539194513445,13.2593410299962));
#46314=CARTESIAN_POINT('Ctrl Pts',(2.50037690087323,59.5403097787046,13.2670480389967));
#46315=CARTESIAN_POINT('Ctrl Pts',(2.50037737123612,59.5403150478698,13.2670844514136));
#46316=CARTESIAN_POINT('Ctrl Pts',(2.50037784078482,59.5403203170064,13.2671208638747));
#46317=CARTESIAN_POINT('Ctrl Pts',(2.50037830951934,59.5403255861145,13.2671572763801));
#46318=CARTESIAN_POINT('Ctrl Pts',(2.50128601740068,59.550529253138,13.3376703644645));
#46319=CARTESIAN_POINT('Ctrl Pts',(2.49914256466633,59.5606260739844,13.408351690911));
#46320=CARTESIAN_POINT('Ctrl Pts',(2.49395012281287,59.5706793582291,13.4790286814146));
#46321=CARTESIAN_POINT('Ctrl Pts',(2.48764039382557,59.5828958646063,13.5649136404185));
#46322=CARTESIAN_POINT('Ctrl Pts',(2.47686026899674,59.5949868619463,13.6503509074918));
#46323=CARTESIAN_POINT('Ctrl Pts',(2.46172657029248,59.6070473770885,13.7350019088095));
#46324=CARTESIAN_POINT('Ctrl Pts',(2.44627835339879,59.6193585415571,13.8214121812868));
#46325=CARTESIAN_POINT('Ctrl Pts',(2.42629251947667,59.6316381721857,13.907002805738));
#46326=CARTESIAN_POINT('Ctrl Pts',(2.40188227406564,59.6439566260316,13.9913867545134));
#46327=CARTESIAN_POINT('Ctrl Pts',(2.37717338292673,59.6564257892846,14.0768030938027));
#46328=CARTESIAN_POINT('Ctrl Pts',(2.34793048083732,59.6689348013427,14.160982229526));
#46329=CARTESIAN_POINT('Ctrl Pts',(2.31427441934883,59.68152324342,14.2435047244255));
#46330=CARTESIAN_POINT('Ctrl Pts',(2.28751075741139,59.6915337079002,14.3091274995824));
#46331=CARTESIAN_POINT('Ctrl Pts',(2.25795655633981,59.7015937118674,14.3737021478923));
#46332=CARTESIAN_POINT('Ctrl Pts',(2.22567631510524,59.7117083510003,14.4370154482916));
#46333=CARTESIAN_POINT('Ctrl Pts',(2.18511903193608,59.7244165052079,14.5165630400834));
#46334=CARTESIAN_POINT('Ctrl Pts',(2.14047539887216,59.7371441213632,14.5936941839776));
#46335=CARTESIAN_POINT('Ctrl Pts',(2.0920013610226,59.749873529981,14.6680773519142));
#46336=CARTESIAN_POINT('Ctrl Pts',(2.04685992951998,59.7617277874903,14.7373466521275));
#46337=CARTESIAN_POINT('Ctrl Pts',(1.99839712194163,59.7735832333912,14.8042330946931));
#46338=CARTESIAN_POINT('Ctrl Pts',(1.94679834215026,59.7854074525574,14.8685006188011));
#46339=CARTESIAN_POINT('Ctrl Pts',(1.94297012406212,59.7862847153506,14.8732687567157));
#46340=CARTESIAN_POINT('Ctrl Pts',(1.93912462063216,59.7871618079109,14.8780224820268));
#46341=CARTESIAN_POINT('Ctrl Pts',(1.93526189621512,59.7880387177967,14.8827616994595));
#46342=CARTESIAN_POINT('Ctrl Pts',(1.88543794211375,59.7993496768976,14.9438912355979));
#46343=CARTESIAN_POINT('Ctrl Pts',(1.83275345257738,59.8106295757333,15.0026072895304));
#46344=CARTESIAN_POINT('Ctrl Pts',(1.77733724064179,59.8218393754625,15.0587248540365));
#46345=CARTESIAN_POINT('Ctrl Pts',(1.77189331698259,59.8229405928108,15.064237676484));
#46346=CARTESIAN_POINT('Ctrl Pts',(1.76642298929319,59.8240411370812,15.0697254218942));
#46347=CARTESIAN_POINT('Ctrl Pts',(1.76092635230643,59.8251409735031,15.0751879137462));
#46348=CARTESIAN_POINT('Ctrl Pts',(1.71347422013327,59.834635794316,15.1223452730516));
#46349=CARTESIAN_POINT('Ctrl Pts',(1.66406433723682,59.8440772105526,15.1676214971317));
#46350=CARTESIAN_POINT('Ctrl Pts',(1.61274763941038,59.8534385124002,15.2109084390397));
#46351=CARTESIAN_POINT('Ctrl Pts',(1.61271278144252,59.8534448712653,15.2109378426236));
#46352=CARTESIAN_POINT('Ctrl Pts',(1.612677922594,59.8534512300934,15.2109672452895));
#46353=CARTESIAN_POINT('Ctrl Pts',(1.6126430628648,59.8534575888844,15.2109966470373));
#46354=CARTESIAN_POINT('Ctrl Pts',(1.61148134785781,59.853669498245,15.2119764725392));
#46355=CARTESIAN_POINT('Ctrl Pts',(1.61031865478613,59.8538813664654,15.2129552784351));
#46356=CARTESIAN_POINT('Ctrl Pts',(1.60915498477109,59.8540931941773,15.2139330635866));
#46357=CARTESIAN_POINT('Ctrl Pts',(1.55020696078019,59.864823749129,15.2634647193182));
#46358=CARTESIAN_POINT('Ctrl Pts',(1.48902325362349,59.8754021982025,15.3101515096413));
#46359=CARTESIAN_POINT('Ctrl Pts',(1.42581404612227,59.8859070487761,15.353905724036));
#46360=CARTESIAN_POINT('Ctrl Pts',(1.41912316332405,59.887019018484,15.3585372378932));
#46361=CARTESIAN_POINT('Ctrl Pts',(1.41240958468812,59.8881301587286,15.3631358449879));
#46362=CARTESIAN_POINT('Ctrl Pts',(1.40567356052368,59.8892405592113,15.3677014078902));
#46363=CARTESIAN_POINT('Ctrl Pts',(1.33883089404637,59.9002592443159,15.4130062332463));
#46364=CARTESIAN_POINT('Ctrl Pts',(1.26977717227794,59.9112058480364,15.4550610497965));
#46365=CARTESIAN_POINT('Ctrl Pts',(1.19877265293406,59.922150181128,15.4937272790274));
#46366=CARTESIAN_POINT('Ctrl Pts',(1.19324757079086,59.9230017936717,15.4967360183956));
#46367=CARTESIAN_POINT('Ctrl Pts',(1.18771068101699,59.9238533899401,15.4997242146752));
#46368=CARTESIAN_POINT('Ctrl Pts',(1.1821621088393,59.9247050015428,15.5026917897785));
#46369=CARTESIAN_POINT('Ctrl Pts',(1.10377082825718,59.9367367318624,15.5446182539426));
#46370=CARTESIAN_POINT('Ctrl Pts',(1.02304627281204,59.9487723007819,15.5824329766345));
#46371=CARTESIAN_POINT('Ctrl Pts',(0.940367691462049,59.9608733853385,15.6159261158047));
#46372=CARTESIAN_POINT('Ctrl Pts',(0.870834804575598,59.971050426719,15.6440939268552));
#46373=CARTESIAN_POINT('Ctrl Pts',(0.79992069165266,59.9812732470463,15.6692043885178));
#46374=CARTESIAN_POINT('Ctrl Pts',(0.727868067876903,59.9915612181891,15.6911316846438));
#46375=CARTESIAN_POINT('Ctrl Pts',(0.642453056742453,60.0037571261751,15.7171254673072));
#46376=CARTESIAN_POINT('Ctrl Pts',(0.555895002218752,60.0159802616778,15.7385065701487));
#46377=CARTESIAN_POINT('Ctrl Pts',(0.468642151115674,60.0282337224108,15.7552261443502));
#46378=CARTESIAN_POINT('Ctrl Pts',(0.38094541171423,60.0405495211393,15.7720307773577));
#46379=CARTESIAN_POINT('Ctrl Pts',(0.292548020977324,60.052895543025,15.7841268590937));
#46380=CARTESIAN_POINT('Ctrl Pts',(0.203871504215768,60.0652501800661,15.7914861794489));
#46381=CARTESIAN_POINT('Ctrl Pts',(0.122822309657222,60.0765421592486,15.798212503498));
#46382=CARTESIAN_POINT('Ctrl Pts',(0.0415400858558959,60.0878409708304,
15.8009825371921));
#46383=CARTESIAN_POINT('Ctrl Pts',(-0.039689640861549,60.0991162829269,
15.7997813431565));
#46384=CARTESIAN_POINT('Ctrl Pts',(-0.0458630406410711,60.099973198394,
15.7996900532889));
#46385=CARTESIAN_POINT('Ctrl Pts',(-0.0520361549971498,60.1008299802659,
15.7995758086185));
#46386=CARTESIAN_POINT('Ctrl Pts',(-0.0582088671208629,60.1016866162842,
15.7994385936371));
#46387=CARTESIAN_POINT('Ctrl Pts',(-0.12734800021417,60.1112815998986,15.7979016800937));
#46388=CARTESIAN_POINT('Ctrl Pts',(-0.196435023005444,60.1208575677164,
15.7934860962484));
#46389=CARTESIAN_POINT('Ctrl Pts',(-0.265319269215243,60.1303911617268,
15.7861745697976));
#46390=CARTESIAN_POINT('Ctrl Pts',(-0.328785114153774,60.1391748478738,
15.7794381644578));
#46391=CARTESIAN_POINT('Ctrl Pts',(-0.391836588715798,60.1478888811247,
15.7702695356354));
#46392=CARTESIAN_POINT('Ctrl Pts',(-0.454382638560456,60.1565152457386,
15.75869807515));
#46393=CARTESIAN_POINT('Ctrl Pts',(-0.454430746547466,60.1565218808025,
15.758689174833));
#46394=CARTESIAN_POINT('Ctrl Pts',(-0.454478854236144,60.1565285158147,
15.7586802730931));
#46395=CARTESIAN_POINT('Ctrl Pts',(-0.454526961626474,60.1565351507754,
15.7586713699301));
#46396=CARTESIAN_POINT('Ctrl Pts',(-0.52837655333923,60.1667204701915,15.7450041361788));
#46397=CARTESIAN_POINT('Ctrl Pts',(-0.601526523728802,60.1767846212224,
15.7279862217928));
#46398=CARTESIAN_POINT('Ctrl Pts',(-0.673804609387891,60.1867910088178,
15.7076882553179));
#46399=CARTESIAN_POINT('Ctrl Pts',(-0.683827269572054,60.1881785749331,
15.704873576172));
#46400=CARTESIAN_POINT('Ctrl Pts',(-0.693833097284363,60.1895650222819,
15.7019957794827));
#46401=CARTESIAN_POINT('Ctrl Pts',(-0.703821567336172,60.1909505121541,
15.6990550122623));
#46402=CARTESIAN_POINT('Ctrl Pts',(-0.77894100990679,60.2013702487447,15.6769386327583));
#46403=CARTESIAN_POINT('Ctrl Pts',(-0.853082298181796,60.2117366076373,
15.6512616831298));
#46404=CARTESIAN_POINT('Ctrl Pts',(-0.92600381073812,60.2221056842168,15.6220951695599));
#46405=CARTESIAN_POINT('Ctrl Pts',(-0.938161850952179,60.2238344970955,
15.6172323021775));
#46406=CARTESIAN_POINT('Ctrl Pts',(-0.950285876321194,60.2255633742816,
15.6122723851462));
#46407=CARTESIAN_POINT('Ctrl Pts',(-0.962374636235121,60.2272925622388,
15.6072156980307));
#46408=CARTESIAN_POINT('Ctrl Pts',(-1.03842434324269,60.2381707861794,15.575404364503));
#46409=CARTESIAN_POINT('Ctrl Pts',(-1.11308213560497,60.2490619084814,15.5397639548018));
#46410=CARTESIAN_POINT('Ctrl Pts',(-1.18602358418327,60.2600099587645,15.5003883468616));
#46411=CARTESIAN_POINT('Ctrl Pts',(-1.19421937252181,60.2612400947789,15.4959640564935));
#46412=CARTESIAN_POINT('Ctrl Pts',(-1.20239343972178,60.2624709450305,15.4914925952459));
#46413=CARTESIAN_POINT('Ctrl Pts',(-1.21054528533793,60.2637025685625,15.4869740871883));
#46414=CARTESIAN_POINT('Ctrl Pts',(-1.28805374649585,60.2754129528346,15.4440117173443));
#46415=CARTESIAN_POINT('Ctrl Pts',(-1.36314756475987,60.2871320961967,15.397024406493));
#46416=CARTESIAN_POINT('Ctrl Pts',(-1.43548080528418,60.2988870358612,15.3462784106231));
#46417=CARTESIAN_POINT('Ctrl Pts',(-1.50857195784496,60.3107651444892,15.2950006951621));
#46418=CARTESIAN_POINT('Ctrl Pts',(-1.57884328318765,60.3226795409351,15.2398857656068));
#46419=CARTESIAN_POINT('Ctrl Pts',(-1.64595639049583,60.33463524494,15.1812194589559));
#46420=CARTESIAN_POINT('Ctrl Pts',(-1.71256112033185,60.346500385256,15.1229975458054));
#46421=CARTESIAN_POINT('Ctrl Pts',(-1.77605491076421,60.3584058279396,15.0612791137166));
#46422=CARTESIAN_POINT('Ctrl Pts',(-1.83613637053914,60.370339024527,14.9963398423922));
#46423=CARTESIAN_POINT('Ctrl Pts',(-1.88144242810172,60.3793375757193,14.9473706200111));
#46424=CARTESIAN_POINT('Ctrl Pts',(-1.92480886439003,60.3883515105436,14.8965700506351));
#46425=CARTESIAN_POINT('Ctrl Pts',(-1.96611780436083,60.3973708602517,14.8440474848212));
#46426=CARTESIAN_POINT('Ctrl Pts',(-2.01328239313746,60.4076687260482,14.7840797098103));
#46427=CARTESIAN_POINT('Ctrl Pts',(-2.0575505040754,60.4179269682567,14.7221404931659));
#46428=CARTESIAN_POINT('Ctrl Pts',(-2.09883875439965,60.428127898034,14.6584211624251));
#46429=CARTESIAN_POINT('Ctrl Pts',(-2.10585568884355,60.4298615451358,14.6475920678738));
#46430=CARTESIAN_POINT('Ctrl Pts',(-2.11278655893247,60.431593546692,14.6367114369141));
#46431=CARTESIAN_POINT('Ctrl Pts',(-2.11963095313664,60.4333238279332,14.6257800593745));
#46432=CARTESIAN_POINT('Ctrl Pts',(-2.14375367382694,60.4394221165259,14.5872529729325));
#46433=CARTESIAN_POINT('Ctrl Pts',(-2.16680272970016,60.4454988338563,14.5480963312027));
#46434=CARTESIAN_POINT('Ctrl Pts',(-2.18876181863496,60.4515503313939,14.5083413758981));
#46435=CARTESIAN_POINT('Ctrl Pts',(-2.1887828027413,60.4515561142052,14.508303386061));
#46436=CARTESIAN_POINT('Ctrl Pts',(-2.18880378585152,60.4515618969937,14.5082653956769));
#46437=CARTESIAN_POINT('Ctrl Pts',(-2.18882476796558,60.4515676797595,14.5082274047455));
#46438=CARTESIAN_POINT('Ctrl Pts',(-2.22650688805877,60.4619530429175,14.439998872852));
#46439=CARTESIAN_POINT('Ctrl Pts',(-2.26098034919205,60.4722653626783,14.3700047366866));
#46440=CARTESIAN_POINT('Ctrl Pts',(-2.29214000432683,60.4825490008941,14.298457429472));
#46441=CARTESIAN_POINT('Ctrl Pts',(-2.29567845576629,60.4837167979794,14.2903326068092));
#46442=CARTESIAN_POINT('Ctrl Pts',(-2.29917412029052,60.484884220357,14.2821877680779));
#46443=CARTESIAN_POINT('Ctrl Pts',(-2.30262680350284,60.4860513292658,14.2740232358047));
#46444=CARTESIAN_POINT('Ctrl Pts',(-2.33454719484305,60.4968413643812,14.1985413426673));
#46445=CARTESIAN_POINT('Ctrl Pts',(-2.36279750989817,60.5076050639362,14.1213748437473));
#46446=CARTESIAN_POINT('Ctrl Pts',(-2.38723291317746,60.5183775034172,14.0428001666309));
#46447=CARTESIAN_POINT('Ctrl Pts',(-2.38905840304868,60.5191822774959,14.0369301068831));
#46448=CARTESIAN_POINT('Ctrl Pts',(-2.3908625787226,60.5199870986543,14.031052195651));
#46449=CARTESIAN_POINT('Ctrl Pts',(-2.39264536888567,60.5207919806927,14.0251665522838));
#46450=CARTESIAN_POINT('Ctrl Pts',(-2.39886622731632,60.5236005317593,14.0046292198936));
#46451=CARTESIAN_POINT('Ctrl Pts',(-2.40482696298709,60.5264097579991,13.9839978030011));
#46452=CARTESIAN_POINT('Ctrl Pts',(-2.41052510737083,60.5292202247935,13.9632766606078));
#46453=CARTESIAN_POINT('Ctrl Pts',(-2.43381076806375,60.5407052928709,13.8785990079467));
#46454=CARTESIAN_POINT('Ctrl Pts',(-2.45258513433876,60.5521506386081,13.792878745595));
#46455=CARTESIAN_POINT('Ctrl Pts',(-2.4668090159224,60.5635766116674,13.70651223253));
#46456=CARTESIAN_POINT('Ctrl Pts',(-2.48044230741506,60.5745281666553,13.6237317452983));
#46457=CARTESIAN_POINT('Ctrl Pts',(-2.48989536647366,60.5854615711786,13.5403583727911));
#46458=CARTESIAN_POINT('Ctrl Pts',(-2.49514302977644,60.5963827299336,13.4567264576687));
#46459=CARTESIAN_POINT('Ctrl Pts',(-2.49514465071334,60.5963861033416,13.4567006248267));
#46460=CARTESIAN_POINT('Ctrl Pts',(-2.49514627124893,60.5963894767483,13.4566747919598));
#46461=CARTESIAN_POINT('Ctrl Pts',(-2.4951478913832,60.5963928501539,13.4566489590681));
#46462=CARTESIAN_POINT('Ctrl Pts',(-2.49841156595885,60.6031883967148,13.4046099686768));
#46463=CARTESIAN_POINT('Ctrl Pts',(-2.5000472486871,60.6099790432102,13.3524700211784));
#46464=CARTESIAN_POINT('Ctrl Pts',(-2.50005097985869,60.6167707974152,13.3003061727703));
#46465=CARTESIAN_POINT('Ctrl Pts',(-2.5,59.3994433450696,13.3));
#46466=CARTESIAN_POINT('Ctrl Pts',(-2.5,59.3645326518074,13.5713375280958));
#46467=CARTESIAN_POINT('Ctrl Pts',(-2.45582275699131,59.3298728723396,13.8413154973223));
#46468=CARTESIAN_POINT('Ctrl Pts',(-2.26198134694515,59.2520835125909,14.4158398109649));
#46469=CARTESIAN_POINT('Ctrl Pts',(-2.09274908494108,59.2099873435,14.7078640735593));
#46470=CARTESIAN_POINT('Ctrl Pts',(-1.76542759316789,59.147088947621,15.0772629224902));
#46471=CARTESIAN_POINT('Ctrl Pts',(-1.64857013328762,59.1268133617154,15.1861645024256));
#46472=CARTESIAN_POINT('Ctrl Pts',(-1.39232480313582,59.0857511129315,15.3828374172618));
#46473=CARTESIAN_POINT('Ctrl Pts',(-1.25303350586245,59.0650777127863,15.4694908484802));
#46474=CARTESIAN_POINT('Ctrl Pts',(-0.830465451583301,59.0054283505205,
15.6780073168761));
#46475=CARTESIAN_POINT('Ctrl Pts',(-0.53188567776378,58.966814499779,15.762052975899));
#46476=CARTESIAN_POINT('Ctrl Pts',(-0.0632947915091542,58.9075684335156,
15.8045037340727));
#46477=CARTESIAN_POINT('Ctrl Pts',(0.100020462504728,58.8871449597277,15.8033065024178));
#46478=CARTESIAN_POINT('Ctrl Pts',(0.419134632114546,58.8468549178829,15.7696707599079));
#46479=CARTESIAN_POINT('Ctrl Pts',(0.574292788339893,58.8270821187475,15.7382651271886));
#46480=CARTESIAN_POINT('Ctrl Pts',(1.04510008816248,58.7654333506753,15.5955037295384));
#46481=CARTESIAN_POINT('Ctrl Pts',(1.34212244248392,58.7241320994188,15.4354857585171));
#46482=CARTESIAN_POINT('Ctrl Pts',(1.72305534902668,58.6624257125961,15.1185586697063));
#46483=CARTESIAN_POINT('Ctrl Pts',(1.83689407189847,58.6423915696704,15.0034956389685));
#46484=CARTESIAN_POINT('Ctrl Pts',(2.04238469877396,58.6019544913329,14.7510570451429));
#46485=CARTESIAN_POINT('Ctrl Pts',(2.13316363596419,58.5816551435649,14.613970192102));
#46486=CARTESIAN_POINT('Ctrl Pts',(2.35859713029488,58.5219805079189,14.1878064710611));
#46487=CARTESIAN_POINT('Ctrl Pts',(2.45231769902695,58.483116114058,13.8808031272104));
#46488=CARTESIAN_POINT('Ctrl Pts',(2.50271885245684,58.4244300543436,13.4070548963955));
#46489=CARTESIAN_POINT('Ctrl Pts',(2.50447649653974,58.4050121415564,13.2483910766068));
#46490=CARTESIAN_POINT('Ctrl Pts',(2.47775045955394,58.3658932325713,12.9303955960265));
#46491=CARTESIAN_POINT('Ctrl Pts',(2.44885674681256,58.3462843322562,12.7718360701045));
#46492=CARTESIAN_POINT('Ctrl Pts',(2.31576608143569,58.2866967409114,12.3031020865792));
#46493=CARTESIAN_POINT('Ctrl Pts',(2.16593231736754,58.2472017253765,12.0095183875325));
#46494=CARTESIAN_POINT('Ctrl Pts',(1.75727584906853,58.1671523836789,11.4907247669193));
#46495=CARTESIAN_POINT('Ctrl Pts',(1.50017129145475,58.1269675630468,11.2724387051608));
#46496=CARTESIAN_POINT('Ctrl Pts',(1.0689625956934,58.0676891342559,11.0345071919954));
#46497=CARTESIAN_POINT('Ctrl Pts',(0.923165792334853,58.0487401405484,10.9712866142904));
#46498=CARTESIAN_POINT('Ctrl Pts',(0.454178518263113,57.989610193629,10.8189425390981));
#46499=CARTESIAN_POINT('Ctrl Pts',(0.118436411469683,57.9497763461178,10.7804901403219));
#46500=CARTESIAN_POINT('Ctrl Pts',(-0.536725224395779,57.8717130480077,
10.8370236215221));
#46501=CARTESIAN_POINT('Ctrl Pts',(-0.85009979282434,57.8343099805388,10.9268917939241));
#46502=CARTESIAN_POINT('Ctrl Pts',(-1.3840831280269,57.7629396421448,11.1997909007637));
#46503=CARTESIAN_POINT('Ctrl Pts',(-1.60791004167294,57.7297936317739,11.365772965549));
#46504=CARTESIAN_POINT('Ctrl Pts',(-1.99099596710922,57.6651288580241,11.7632217121788));
#46505=CARTESIAN_POINT('Ctrl Pts',(-2.14799101676222,57.6340707102155,11.9915921922629));
#46506=CARTESIAN_POINT('Ctrl Pts',(-2.40621270997693,57.5646689399261,12.5437760893431));
#46507=CARTESIAN_POINT('Ctrl Pts',(-2.4856484868962,57.5259257271973,12.8718967308891));
#46508=CARTESIAN_POINT('Ctrl Pts',(-2.49941036415996,57.4841426208034,13.2372814670857));
#46509=CARTESIAN_POINT('Ctrl Pts',(-2.5,57.4805638506737,13.26865141346));
#46510=CARTESIAN_POINT('Ctrl Pts',(-2.5,57.4769927816046,13.3));
#46511=CARTESIAN_POINT('Origin',(0.,70.2,13.3));
#46512=CARTESIAN_POINT('',(1.36952200671963,56.456522023403,11.210153809184));
#46513=CARTESIAN_POINT('Ctrl Pts',(-2.5,57.4769927816046,13.3));
#46514=CARTESIAN_POINT('Ctrl Pts',(-2.5,57.4459316982446,13.5726693438026));
#46515=CARTESIAN_POINT('Ctrl Pts',(-2.45538841038206,57.4156542366357,13.8437456246808));
#46516=CARTESIAN_POINT('Ctrl Pts',(-2.25976716009472,57.3469461366581,14.4209791769068));
#46517=CARTESIAN_POINT('Ctrl Pts',(-2.08862106037187,57.3078837011561,14.7145146492395));
#46518=CARTESIAN_POINT('Ctrl Pts',(-1.67879428804009,57.2396608994169,15.173327824965));
#46519=CARTESIAN_POINT('Ctrl Pts',(-1.45963520298074,57.2105138890148,15.3487075687647));
#46520=CARTESIAN_POINT('Ctrl Pts',(-0.924771568170676,57.1451182786575,
15.6464691107768));
#46521=CARTESIAN_POINT('Ctrl Pts',(-0.604120811806337,57.1074465471387,
15.7486948490657));
#46522=CARTESIAN_POINT('Ctrl Pts',(0.00103428072363587,57.0419646916788,
15.8151364688876));
#46523=CARTESIAN_POINT('Ctrl Pts',(0.277999449479295,57.0142712095688,15.7997361875592));
#46524=CARTESIAN_POINT('Ctrl Pts',(0.874633747031843,56.9522497055724,15.6659664618541));
#46525=CARTESIAN_POINT('Ctrl Pts',(1.18406779077029,56.9158900746659,15.5272610971029));
#46526=CARTESIAN_POINT('Ctrl Pts',(1.57583850097768,56.8664620514363,15.2463189710605));
#46527=CARTESIAN_POINT('Ctrl Pts',(1.68709219417902,56.8519536134822,15.1507213273601));
#46528=CARTESIAN_POINT('Ctrl Pts',(2.02101231098688,56.8058296438384,14.808485994022));
#46529=CARTESIAN_POINT('Ctrl Pts',(2.20310153977486,56.7752544493422,14.5273228999349));
#46530=CARTESIAN_POINT('Ctrl Pts',(2.42812484038507,56.7140033923145,13.9579751872364));
#46531=CARTESIAN_POINT('Ctrl Pts',(2.48667123778913,56.6869043094238,13.6813465795139));
#46532=CARTESIAN_POINT('Ctrl Pts',(2.51062235352946,56.6347298760345,13.0864889195961));
#46533=CARTESIAN_POINT('Ctrl Pts',(2.46393343806034,56.6097884288235,12.7728566775426));
#46534=CARTESIAN_POINT('Ctrl Pts',(2.30818385936516,56.5675513054282,12.3267067575381));
#46535=CARTESIAN_POINT('Ctrl Pts',(2.24198890991713,56.5533848606566,12.1826241047964));
#46536=CARTESIAN_POINT('Ctrl Pts',(2.05772104536115,56.5224072325291,11.8649117906946));
#46537=CARTESIAN_POINT('Ctrl Pts',(1.93057620891326,56.5064572664569,11.697920368476));
#46538=CARTESIAN_POINT('Ctrl Pts',(1.65862592877859,56.479276351471,11.4209094098465));
#46539=CARTESIAN_POINT('Ctrl Pts',(1.51996586495887,56.4677225622875,11.3070874124032));
#46540=CARTESIAN_POINT('Ctrl Pts',(1.37035622588183,56.455286737476,11.2090375866155));
#46541=CARTESIAN_POINT('',(-2.50125173685429,55.6414517644448,13.3001584307864));
#46542=CARTESIAN_POINT('Ctrl Pts',(1.36944901719983,56.4564965633172,11.2101199336514));
#46543=CARTESIAN_POINT('Ctrl Pts',(1.29603082900563,56.4426908388302,11.1624967982744));
#46544=CARTESIAN_POINT('Ctrl Pts',(1.22027156825106,56.428933734737,11.1187547073001));
#46545=CARTESIAN_POINT('Ctrl Pts',(1.14255504747613,56.4151597343664,11.0790266810285));
#46546=CARTESIAN_POINT('Ctrl Pts',(1.06363597865445,56.4011726017417,11.0386839223947));
#46547=CARTESIAN_POINT('Ctrl Pts',(0.98269862043085,56.3871679761864,11.0024808901664));
#46548=CARTESIAN_POINT('Ctrl Pts',(0.90013272529909,56.373112312793,10.970569505787));
#46549=CARTESIAN_POINT('Ctrl Pts',(0.817545950255569,56.3590530948931,10.9386500514061));
#46550=CARTESIAN_POINT('Ctrl Pts',(0.733330146478969,56.344942943031,10.911024534462));
#46551=CARTESIAN_POINT('Ctrl Pts',(0.647860516769757,56.330782502838,10.8878527637467));
#46552=CARTESIAN_POINT('Ctrl Pts',(0.580271343564073,56.3195844615205,10.8695285843898));
#46553=CARTESIAN_POINT('Ctrl Pts',(0.511897862989226,56.3083556916996,10.8539896154898));
#46554=CARTESIAN_POINT('Ctrl Pts',(0.442916666885505,56.2971105655553,10.8413190935192));
#46555=CARTESIAN_POINT('Ctrl Pts',(0.361629173409385,56.2838593004318,10.8263881408799));
#46556=CARTESIAN_POINT('Ctrl Pts',(0.279900731404808,56.2706501227155,10.8155140490353));
#46557=CARTESIAN_POINT('Ctrl Pts',(0.198010739746884,56.2575256924461,10.8087225081528));
#46558=CARTESIAN_POINT('Ctrl Pts',(0.191809252601509,56.2565317860607,10.8082081882386));
#46559=CARTESIAN_POINT('Ctrl Pts',(0.185606819982153,56.2555383643905,10.8077172973724));
#46560=CARTESIAN_POINT('Ctrl Pts',(0.179403554156247,56.2545454453184,10.8072498547535));
#46561=CARTESIAN_POINT('Ctrl Pts',(0.0994616940672659,56.2417496374696,
10.8012258935873));
#46562=CARTESIAN_POINT('Ctrl Pts',(0.0193841213790183,56.2290379427932,
10.7990925696856));
#46563=CARTESIAN_POINT('Ctrl Pts',(-0.0606086754043837,56.2164626019884,
10.8008947606548));
#46564=CARTESIAN_POINT('Ctrl Pts',(-0.0682721219220201,56.2152578628672,
10.8010674136268));
#46565=CARTESIAN_POINT('Ctrl Pts',(-0.0759348159106824,56.2140543726688,
10.8012762167855));
#46566=CARTESIAN_POINT('Ctrl Pts',(-0.0835965792288266,56.2128521757121,
10.8015212294454));
#46567=CARTESIAN_POINT('Ctrl Pts',(-0.110826037820625,56.2085796380608,
10.8023919901046));
#46568=CARTESIAN_POINT('Ctrl Pts',(-0.138043705741017,56.2043235614105,
10.8037199228905));
#46569=CARTESIAN_POINT('Ctrl Pts',(-0.165241826304231,56.2000861980125,
10.8055077843409));
#46570=CARTESIAN_POINT('Ctrl Pts',(-0.165242864855589,56.2000860362101,
10.8055078526098));
#46571=CARTESIAN_POINT('Ctrl Pts',(-0.165243903406876,56.2000858744078,
10.8055079208794));
#46572=CARTESIAN_POINT('Ctrl Pts',(-0.165244941958176,56.2000857126056,
10.8055079891497));
#46573=CARTESIAN_POINT('Ctrl Pts',(-0.245392444874828,56.1875990410136,
10.8107765684174));
#46574=CARTESIAN_POINT('Ctrl Pts',(-0.325372755007318,56.1752736773837,
10.8200370396293));
#46575=CARTESIAN_POINT('Ctrl Pts',(-0.404926294732208,56.1630147684855,
10.8332229156012));
#46576=CARTESIAN_POINT('Ctrl Pts',(-0.411686604966254,56.1619730294558,
10.83434342655));
#46577=CARTESIAN_POINT('Ctrl Pts',(-0.418443811964095,56.1609317726542,
10.8354923063435));
#46578=CARTESIAN_POINT('Ctrl Pts',(-0.425197744114492,56.1598909411829,
10.836669526147));
#46579=CARTESIAN_POINT('Ctrl Pts',(-0.466390339984701,56.1535428539932,
10.8438494531194));
#46580=CARTESIAN_POINT('Ctrl Pts',(-0.507461483222913,56.1472107569749,
10.8520832082565));
#46581=CARTESIAN_POINT('Ctrl Pts',(-0.548371370921128,56.1408831966229,
10.8613642367384));
#46582=CARTESIAN_POINT('Ctrl Pts',(-0.632916656422052,56.127806519404,10.8805446170056));
#46583=CARTESIAN_POINT('Ctrl Pts',(-0.716335870297029,56.1148144342113,
10.904097743567));
#46584=CARTESIAN_POINT('Ctrl Pts',(-0.798288826299474,56.101825375084,10.9318430111096));
#46585=CARTESIAN_POINT('Ctrl Pts',(-0.881714476844274,56.0886029025764,
10.960086861084));
#46586=CARTESIAN_POINT('Ctrl Pts',(-0.963620305287153,56.0753834070735,
10.9926755305163));
#46587=CARTESIAN_POINT('Ctrl Pts',(-1.04363603309156,56.0621136895825,11.0294319090248));
#46588=CARTESIAN_POINT('Ctrl Pts',(-1.12414277452161,56.0487625429491,11.0664138417234));
#46589=CARTESIAN_POINT('Ctrl Pts',(-1.20273558800698,56.035360582838,11.1076149159066));
#46590=CARTESIAN_POINT('Ctrl Pts',(-1.27903342209982,56.0218874888268,11.1528620961267));
#46591=CARTESIAN_POINT('Ctrl Pts',(-1.33966487582784,56.0111808510065,11.1888185861956));
#46592=CARTESIAN_POINT('Ctrl Pts',(-1.39884693568266,56.0004299968532,11.2273301795414));
#46593=CARTESIAN_POINT('Ctrl Pts',(-1.4563897806272,55.9896392984033,11.2683141868384));
#46594=CARTESIAN_POINT('Ctrl Pts',(-1.5250305535497,55.9767674655509,11.3172025228433));
#46595=CARTESIAN_POINT('Ctrl Pts',(-1.59099181520561,55.9639034410327,11.3693610284727));
#46596=CARTESIAN_POINT('Ctrl Pts',(-1.6540427539691,55.9510765991678,11.4245667677993));
#46597=CARTESIAN_POINT('Ctrl Pts',(-1.65755599969368,55.9503618778928,11.4276428731114));
#46598=CARTESIAN_POINT('Ctrl Pts',(-1.66106021037135,55.9496472714153,11.4307284528359));
#46599=CARTESIAN_POINT('Ctrl Pts',(-1.66455534626192,55.9489327845877,11.4338234731183));
#46600=CARTESIAN_POINT('Ctrl Pts',(-1.72541332248449,55.9364920029623,11.4877145596608));
#46601=CARTESIAN_POINT('Ctrl Pts',(-1.78352031244173,55.9240879815468,11.5444634611635));
#46602=CARTESIAN_POINT('Ctrl Pts',(-1.83868488776429,55.9117632804885,11.6039034913596));
#46603=CARTESIAN_POINT('Ctrl Pts',(-1.84571234650124,55.910193227105,11.6114756036632));
#46604=CARTESIAN_POINT('Ctrl Pts',(-1.85269205021684,55.9086244564431,11.6190914578392));
#46605=CARTESIAN_POINT('Ctrl Pts',(-1.8596235971321,55.9070570525137,11.6267507699646));
#46606=CARTESIAN_POINT('Ctrl Pts',(-1.91219654572504,55.8951689347226,11.6848435200463));
#46607=CARTESIAN_POINT('Ctrl Pts',(-1.96200070672626,55.8833602282237,11.7454318674796));
#46608=CARTESIAN_POINT('Ctrl Pts',(-2.00886749518019,55.871677708519,11.8084100756291));
#46609=CARTESIAN_POINT('Ctrl Pts',(-2.01377586110376,55.8704541964434,11.8150057930018));
#46610=CARTESIAN_POINT('Ctrl Pts',(-2.01865199736498,55.8692320650099,11.8216277691318));
#46611=CARTESIAN_POINT('Ctrl Pts',(-2.02349570117022,55.8680113655344,11.828275914873));
#46612=CARTESIAN_POINT('Ctrl Pts',(-2.02636737027956,55.8672876538632,11.8322173769291));
#46613=CARTESIAN_POINT('Ctrl Pts',(-2.02922764241447,55.8665644486409,11.8361680346309));
#46614=CARTESIAN_POINT('Ctrl Pts',(-2.03207647586611,55.865841761517,11.8401278694902));
#46615=CARTESIAN_POINT('Ctrl Pts',(-2.03211492050008,55.865832008949,11.8401813069425));
#46616=CARTESIAN_POINT('Ctrl Pts',(-2.03215336304922,55.8658222564752,11.8402347460648));
#46617=CARTESIAN_POINT('Ctrl Pts',(-2.03219180351324,55.8658125040956,11.8402881868568));
#46618=CARTESIAN_POINT('Ctrl Pts',(-2.06766621902012,55.8568126136023,11.8896055119599));
#46619=CARTESIAN_POINT('Ctrl Pts',(-2.10136653431973,55.8478927840317,11.9403452179639));
#46620=CARTESIAN_POINT('Ctrl Pts',(-2.13322179210664,55.8390117877274,11.992403401392));
#46621=CARTESIAN_POINT('Ctrl Pts',(-2.1779864217838,55.8265317596772,12.0655582105106));
#46622=CARTESIAN_POINT('Ctrl Pts',(-2.21887907971105,55.8141907353134,12.1409422096651));
#46623=CARTESIAN_POINT('Ctrl Pts',(-2.25578928865405,55.8018972314393,12.218181355777));
#46624=CARTESIAN_POINT('Ctrl Pts',(-2.29350245773508,55.7893362895351,12.2971007946101));
#46625=CARTESIAN_POINT('Ctrl Pts',(-2.32705691767267,55.7768247567593,12.3779571064769));
#46626=CARTESIAN_POINT('Ctrl Pts',(-2.35632092094978,55.7643023245731,12.4603424912428));
#46627=CARTESIAN_POINT('Ctrl Pts',(-2.38592694917522,55.7516335356434,12.5436907605704));
#46628=CARTESIAN_POINT('Ctrl Pts',(-2.41114083119113,55.7389535795631,12.6286035012372));
#46629=CARTESIAN_POINT('Ctrl Pts',(-2.43182710159743,55.7262393017939,12.7146528205441));
#46630=CARTESIAN_POINT('Ctrl Pts',(-2.44241010168477,55.7197347362005,12.7586752535808));
#46631=CARTESIAN_POINT('Ctrl Pts',(-2.45180819335629,55.7132218194797,12.8029951221362));
#46632=CARTESIAN_POINT('Ctrl Pts',(-2.46000407553754,55.7067013018513,12.8475555370706));
#46633=CARTESIAN_POINT('Ctrl Pts',(-2.46001189210237,55.7066950831127,12.8475980351647));
#46634=CARTESIAN_POINT('Ctrl Pts',(-2.46001970757379,55.7066888643674,12.8476405334778));
#46635=CARTESIAN_POINT('Ctrl Pts',(-2.46002752195179,55.7066826456154,12.8476830320098));
#46636=CARTESIAN_POINT('Ctrl Pts',(-2.46481980748636,55.7028689018423,12.8737458997491));
#46637=CARTESIAN_POINT('Ctrl Pts',(-2.46920089563749,55.6990526313445,12.899891090277));
#46638=CARTESIAN_POINT('Ctrl Pts',(-2.47316768476101,55.6952351470767,12.9261138759658));
#46639=CARTESIAN_POINT('Ctrl Pts',(-2.48294489086037,55.6858259424769,12.990746900862));
#46640=CARTESIAN_POINT('Ctrl Pts',(-2.49016872377525,55.6764461520061,13.0556000782221));
#46641=CARTESIAN_POINT('Ctrl Pts',(-2.49483923918304,55.6671113889433,13.1206080688506));
#46642=CARTESIAN_POINT('Ctrl Pts',(-2.49484248107682,55.6671049095063,13.1206531921361));
#46643=CARTESIAN_POINT('Ctrl Pts',(-2.49484572173883,55.6670984300904,13.1206983154964));
#46644=CARTESIAN_POINT('Ctrl Pts',(-2.49484896116907,55.6670919506956,13.1207434389313));
#46645=CARTESIAN_POINT('Ctrl Pts',(-2.49913669539619,55.6585157748956,13.1804691569517));
#46646=CARTESIAN_POINT('Ctrl Pts',(-2.50126743306733,55.6499764118575,13.2403259773289));
#46647=CARTESIAN_POINT('Ctrl Pts',(-2.50125173685429,55.6414517644448,13.3001584307864));
#46648=CARTESIAN_POINT('',(-2.5,56.395745969557,13.3));
#46649=CARTESIAN_POINT('',(-2.5,70.2,13.3));
#46650=CARTESIAN_POINT('',(-2.46826046448302,56.4316304354619,12.9028993853228));
#46651=CARTESIAN_POINT('Ctrl Pts',(-2.5,56.395745969557,13.3));
#46652=CARTESIAN_POINT('Ctrl Pts',(-2.5,56.4077454755149,13.1671729739548));
#46653=CARTESIAN_POINT('Ctrl Pts',(-2.48941435575088,56.4195677315213,13.0343816947313));
#46654=CARTESIAN_POINT('Ctrl Pts',(-2.46825964356923,56.4316313272142,12.9028925436012));
#46655=CARTESIAN_POINT('Ctrl Pts',(-2.46825694932604,56.4314940421042,12.9028757976354));
#46656=CARTESIAN_POINT('Ctrl Pts',(-2.43520383378043,56.461992268376,12.6974398618336));
#46657=CARTESIAN_POINT('Ctrl Pts',(-2.3766228776081,56.4924752322176,12.4968768864496));
#46658=CARTESIAN_POINT('Ctrl Pts',(-2.19111489475908,56.5590511745454,12.0688458864486));
#46659=CARTESIAN_POINT('Ctrl Pts',(-2.0522520440533,56.5945121834133,11.8491177263255));
#46660=CARTESIAN_POINT('Ctrl Pts',(-1.66671822294653,56.6763109067864,11.4081288818872));
#46661=CARTESIAN_POINT('Ctrl Pts',(-1.40497744941339,56.7223224480549,11.2064031416049));
#46662=CARTESIAN_POINT('Ctrl Pts',(-0.972108750619124,56.7897769391544,
10.9914621828345));
#46663=CARTESIAN_POINT('Ctrl Pts',(-0.826166856433883,56.8111836067347,
10.93530015989));
#46664=CARTESIAN_POINT('Ctrl Pts',(-0.369399857416966,56.8761099376736,
10.807029416002));
#46665=CARTESIAN_POINT('Ctrl Pts',(-0.0492021703253953,56.9191676728897,
10.7802800871358));
#46666=CARTESIAN_POINT('Ctrl Pts',(0.433302312139852,56.9847184945054,10.8321902665078));
#46667=CARTESIAN_POINT('Ctrl Pts',(0.596991241850096,57.0070965552408,10.8665986960538));
#46668=CARTESIAN_POINT('Ctrl Pts',(0.91232652892166,57.0515843353888,10.9666447355976));
#46669=CARTESIAN_POINT('Ctrl Pts',(1.06336864643656,57.0735814735889,11.0314900382241));
#46670=CARTESIAN_POINT('Ctrl Pts',(1.34799849265034,57.117101753697,11.188405258786));
#46671=CARTESIAN_POINT('Ctrl Pts',(1.48119110792558,57.138464255273,11.2796006096996));
#46672=CARTESIAN_POINT('Ctrl Pts',(1.84765740379511,57.2018052376995,11.586361653006));
#46673=CARTESIAN_POINT('Ctrl Pts',(2.04977963288396,57.2434055391266,11.8341096808076));
#46674=CARTESIAN_POINT('Ctrl Pts',(2.27874118847686,57.3066143958866,12.2585242906968));
#46675=CARTESIAN_POINT('Ctrl Pts',(2.34261540956501,57.3281056529485,12.4114660491561));
#46676=CARTESIAN_POINT('Ctrl Pts',(2.48230431115144,57.3903420304424,12.8687288980539));
#46677=CARTESIAN_POINT('Ctrl Pts',(2.51675090670696,57.4306842182026,13.1823973446887));
#46678=CARTESIAN_POINT('Ctrl Pts',(2.4795336408618,57.492319675819,13.6598471795062));
#46679=CARTESIAN_POINT('Ctrl Pts',(2.4501631459233,57.5135330746118,13.8237211100322));
#46680=CARTESIAN_POINT('Ctrl Pts',(2.318547542361,57.5750706742593,14.2868005586607));
#46681=CARTESIAN_POINT('Ctrl Pts',(2.17571283375371,57.6149163814681,14.5711198884439));
#46682=CARTESIAN_POINT('Ctrl Pts',(1.88386088806936,57.6755517746152,14.951673850455));
#46683=CARTESIAN_POINT('Ctrl Pts',(1.77134472640245,57.6961843048605,15.0718074279181));
#46684=CARTESIAN_POINT('Ctrl Pts',(1.40788708041656,57.7569018446779,15.3903782784728));
#46685=CARTESIAN_POINT('Ctrl Pts',(1.12982731653552,57.7964293220125,15.552854342033));
#46686=CARTESIAN_POINT('Ctrl Pts',(0.675575006530766,57.8562171006933,15.7124561782358));
#46687=CARTESIAN_POINT('Ctrl Pts',(0.517551642506458,57.8762570492878,15.7512226167826));
#46688=CARTESIAN_POINT('Ctrl Pts',(0.0391949544407114,57.9358455834721,
15.8202158073517));
#46689=CARTESIAN_POINT('Ctrl Pts',(-0.284388345736859,57.9747798850292,
15.8044320481447));
#46690=CARTESIAN_POINT('Ctrl Pts',(-0.899717038167667,58.0520139946708,
15.653341691228));
#46691=CARTESIAN_POINT('Ctrl Pts',(-1.18665887089664,58.0894794143834,15.5225189252697));
#46692=CARTESIAN_POINT('Ctrl Pts',(-1.7146742041079,58.1670655530837,15.1496685883279));
#46693=CARTESIAN_POINT('Ctrl Pts',(-1.94603656445841,58.2066718111652,14.9044838725725));
#46694=CARTESIAN_POINT('Ctrl Pts',(-2.24294382232247,58.2731478789509,14.427480083543));
#46695=CARTESIAN_POINT('Ctrl Pts',(-2.33640446706872,58.2997659432329,14.2182773391564));
#46696=CARTESIAN_POINT('Ctrl Pts',(-2.46638263202234,58.3543009467222,13.7721573370521));
#46697=CARTESIAN_POINT('Ctrl Pts',(-2.49998965566844,58.38186849262,13.5367483102214));
#46698=CARTESIAN_POINT('Ctrl Pts',(-2.49999999761251,58.4092448555942,13.3001092586366));
#46699=CARTESIAN_POINT('Origin',(0.,70.2,13.3));
#46700=CARTESIAN_POINT('',(-2.5,53.601880595513,13.2999999999966));
#46701=CARTESIAN_POINT('',(-2.5,54.6185115759899,13.3));
#46702=CARTESIAN_POINT('',(-2.5,70.2,13.3));
#46703=CARTESIAN_POINT('Ctrl Pts',(-2.5,54.6185115759899,13.3));
#46704=CARTESIAN_POINT('Ctrl Pts',(-2.5,54.6256816081909,13.2428501459448));
#46705=CARTESIAN_POINT('Ctrl Pts',(-2.4980403631648,54.6328527105969,13.1856442401504));
#46706=CARTESIAN_POINT('Ctrl Pts',(-2.48320476460674,54.6599395432761,12.9699132169714));
#46707=CARTESIAN_POINT('Ctrl Pts',(-2.45720238398481,54.6797643890759,12.8127396260848));
#46708=CARTESIAN_POINT('Ctrl Pts',(-2.33302560160475,54.7402005328981,12.3445441614442));
#46709=CARTESIAN_POINT('Ctrl Pts',(-2.18897094356574,54.7802755360276,12.0492654123138));
#46710=CARTESIAN_POINT('Ctrl Pts',(-1.81028555321965,54.8578225681675,11.5496473271837));
#46711=CARTESIAN_POINT('Ctrl Pts',(-1.58622614775164,54.8945743522683,11.3442941017801));
#46712=CARTESIAN_POINT('Ctrl Pts',(-1.04874269305375,54.972199004244,11.0062399209845));
#46713=CARTESIAN_POINT('Ctrl Pts',(-0.733763163302521,55.0124741275843,
10.886948758197));
#46714=CARTESIAN_POINT('Ctrl Pts',(-0.24315258734495,55.0727292892315,10.806475911269));
#46715=CARTESIAN_POINT('Ctrl Pts',(-0.0794297301991653,55.0924802060136,
10.7959072366966));
#46716=CARTESIAN_POINT('Ctrl Pts',(0.247103105746923,55.1318695094133,10.8069049501745));
#46717=CARTESIAN_POINT('Ctrl Pts',(0.409130891528226,55.1514061426414,10.8283208184865));
#46718=CARTESIAN_POINT('Ctrl Pts',(0.727223091315103,55.1906127019791,10.9025211533163));
#46719=CARTESIAN_POINT('Ctrl Pts',(0.882501490435353,55.2101772749367,10.9552283963109));
#46720=CARTESIAN_POINT('Ctrl Pts',(1.32114398037918,55.2676383950357,11.1539172495321));
#46721=CARTESIAN_POINT('Ctrl Pts',(1.58312223767498,55.3048904217772,11.3391714937393));
#46722=CARTESIAN_POINT('Ctrl Pts',(2.03490250559403,55.381797392642,11.809718075388));
#46723=CARTESIAN_POINT('Ctrl Pts',(2.21575623272531,55.421156485849,12.0949124350888));
#46724=CARTESIAN_POINT('Ctrl Pts',(2.44469767641483,55.4957097072909,12.6937526721326));
#46725=CARTESIAN_POINT('Ctrl Pts',(2.50057746437837,55.5302945892199,12.9979890867919));
#46726=CARTESIAN_POINT('Ctrl Pts',(2.49938474111581,55.6028559205025,13.6266753707104));
#46727=CARTESIAN_POINT('Ctrl Pts',(2.43659302018294,55.6397778948392,13.9455522396094));
#46728=CARTESIAN_POINT('Ctrl Pts',(2.25525689348932,55.6937730616882,14.3903531379472));
#46729=CARTESIAN_POINT('Ctrl Pts',(2.1817163323055,55.7113335238116,14.5309230217389));
#46730=CARTESIAN_POINT('Ctrl Pts',(1.9129600563537,55.7662886867816,14.9439075857987));
#46731=CARTESIAN_POINT('Ctrl Pts',(1.67612906556862,55.8040630675707,15.1848021877775));
#46732=CARTESIAN_POINT('Ctrl Pts',(1.14388756487371,55.8747303709051,15.5441473790804));
#46733=CARTESIAN_POINT('Ctrl Pts',(0.859266810832548,55.9071604172506,15.6677742999895));
#46734=CARTESIAN_POINT('Ctrl Pts',(0.253630371974718,55.974891106573,15.8068021057106));
#46735=CARTESIAN_POINT('Ctrl Pts',(-0.0626823167098201,56.008815340953,
15.8188438213752));
#46736=CARTESIAN_POINT('Ctrl Pts',(-0.529596877881329,56.0581367373013,
15.7483874886325));
#46737=CARTESIAN_POINT('Ctrl Pts',(-0.683577128958439,56.074362666002,15.7099378941588));
#46738=CARTESIAN_POINT('Ctrl Pts',(-1.14763743670498,56.1251986327514,15.5459656276796));
#46739=CARTESIAN_POINT('Ctrl Pts',(-1.43697091166929,56.1605841531913,15.372826789526));
#46740=CARTESIAN_POINT('Ctrl Pts',(-1.90876623848562,56.2249845726101,14.9429390715));
#46741=CARTESIAN_POINT('Ctrl Pts',(-2.09442498998999,56.2537431699344,14.6985877607604));
#46742=CARTESIAN_POINT('Ctrl Pts',(-2.35889595293474,56.311807009802,14.1748280973507));
#46743=CARTESIAN_POINT('Ctrl Pts',(-2.44260186386045,56.3397192377136,13.9029365998579));
#46744=CARTESIAN_POINT('Ctrl Pts',(-2.49303031383222,56.3761580991573,13.5155872348193));
#46745=CARTESIAN_POINT('Ctrl Pts',(-2.5,56.3860090119722,13.4077820306317));
#46746=CARTESIAN_POINT('Ctrl Pts',(-2.5,56.395745969557,13.3));
#46747=CARTESIAN_POINT('',(-2.49999996150753,53.6019333424293,13.2995612946774));
#46748=CARTESIAN_POINT('Ctrl Pts',(-2.49999999962317,55.6406441094823,13.3000434069646));
#46749=CARTESIAN_POINT('Ctrl Pts',(-2.49999514856348,55.6008789438551,13.5794374930429));
#46750=CARTESIAN_POINT('Ctrl Pts',(-2.45315110307401,55.561142419573,13.8569861486731));
#46751=CARTESIAN_POINT('Ctrl Pts',(-2.32260733326474,55.506429780821,14.2324084986736));
#46752=CARTESIAN_POINT('Ctrl Pts',(-2.27606908246108,55.4904458047403,14.3408684472124));
#46753=CARTESIAN_POINT('Ctrl Pts',(-2.071826177445,55.4298800450285,14.7370079936151));
#46754=CARTESIAN_POINT('Ctrl Pts',(-1.86581453799125,55.3851594898524,14.9958973400834));
#46755=CARTESIAN_POINT('Ctrl Pts',(-1.4313046639714,55.3051154312028,15.3639385942157));
#46756=CARTESIAN_POINT('Ctrl Pts',(-1.2250133956775,55.2710204191418,15.4926933185702));
#46757=CARTESIAN_POINT('Ctrl Pts',(-0.696699257190743,55.1926776146113,
15.724192593985));
#46758=CARTESIAN_POINT('Ctrl Pts',(-0.366087260910269,55.1495429980827,
15.7956331535918));
#46759=CARTESIAN_POINT('Ctrl Pts',(0.286967813768001,55.0618561944297,15.8037691593593));
#46760=CARTESIAN_POINT('Ctrl Pts',(0.602914036599877,55.0184354138797,15.7469702169358));
#46761=CARTESIAN_POINT('Ctrl Pts',(1.15381366359778,54.938697353611,15.5344819690884));
#46762=CARTESIAN_POINT('Ctrl Pts',(1.39025769175468,54.9035361389359,15.3955795865521));
#46763=CARTESIAN_POINT('Ctrl Pts',(1.84106150969616,54.8274471042439,15.0202170579832));
#46764=CARTESIAN_POINT('Ctrl Pts',(2.04236777153051,54.7867425911399,14.7755761270405));
#46765=CARTESIAN_POINT('Ctrl Pts',(2.31693127172701,54.7110312123163,14.2738426169271));
#46766=CARTESIAN_POINT('Ctrl Pts',(2.40501956916731,54.6768940542676,14.0297055291302));
#46767=CARTESIAN_POINT('Ctrl Pts',(2.48430527144445,54.6228541884747,13.621249360735));
#46768=CARTESIAN_POINT('Ctrl Pts',(2.49964426585912,54.6025971645548,13.4635911560632));
#46769=CARTESIAN_POINT('Ctrl Pts',(2.50059200737536,54.5475880435969,13.035112195922));
#46770=CARTESIAN_POINT('Ctrl Pts',(2.45731107975392,54.5130740518882,12.7663952638752));
#46771=CARTESIAN_POINT('Ctrl Pts',(2.26943700520349,54.4362594902424,12.2024299909904));
#46772=CARTESIAN_POINT('Ctrl Pts',(2.10820642991216,54.394567649508,11.91778419352));
#46773=CARTESIAN_POINT('Ctrl Pts',(1.6792492715809,54.3106503627889,11.4179720115442));
#46774=CARTESIAN_POINT('Ctrl Pts',(1.41260525198989,54.2689477200906,11.2103832946605));
#46775=CARTESIAN_POINT('Ctrl Pts',(0.96464551892134,54.2059927401207,10.9876615128587));
#46776=CARTESIAN_POINT('Ctrl Pts',(0.809319659711741,54.1852240841484,10.9288283632719));
#46777=CARTESIAN_POINT('Ctrl Pts',(0.352595701903903,54.1259154090887,10.8059896289497));
#46778=CARTESIAN_POINT('Ctrl Pts',(0.0436742169096238,54.0878238786443,
10.7815632772995));
#46779=CARTESIAN_POINT('Ctrl Pts',(-0.420033436857514,54.0297578632496,
10.830415860734));
#46780=CARTESIAN_POINT('Ctrl Pts',(-0.576192859075911,54.0100451599276,
10.8621158564814));
#46781=CARTESIAN_POINT('Ctrl Pts',(-0.887017238542555,53.9697638273405,
10.9567687532628));
#46782=CARTESIAN_POINT('Ctrl Pts',(-1.04055054904443,53.9492993877314,11.0207913615787));
#46783=CARTESIAN_POINT('Ctrl Pts',(-1.45642500566705,53.8910929605599,11.2450557000329));
#46784=CARTESIAN_POINT('Ctrl Pts',(-1.69720452912144,53.8539341723211,11.4389556136179));
#46785=CARTESIAN_POINT('Ctrl Pts',(-2.09992975582247,53.7783345828611,11.9080769050163));
#46786=CARTESIAN_POINT('Ctrl Pts',(-2.25696948369581,53.7406047263216,12.1805000813266));
#46787=CARTESIAN_POINT('Ctrl Pts',(-2.45257708898085,53.6690720952781,12.7398788473275));
#46788=CARTESIAN_POINT('Ctrl Pts',(-2.49995067680506,53.6357011960875,13.0187081845893));
#46789=CARTESIAN_POINT('Ctrl Pts',(-2.49999996150753,53.6019333424293,13.2995612946774));
#46790=CARTESIAN_POINT('Ctrl Pts',(-2.49999996150753,53.6019333424293,13.2995612946774));
#46791=CARTESIAN_POINT('Ctrl Pts',(-2.49999998775002,53.6019153621539,13.2997108397542));
#46792=CARTESIAN_POINT('Ctrl Pts',(-2.5,53.6018985756711,13.2998504558639));
#46793=CARTESIAN_POINT('Ctrl Pts',(-2.5,53.601880595513,13.2999999999933));
#46794=CARTESIAN_POINT('Origin',(0.,70.2,13.3));
#46795=CARTESIAN_POINT('',(-2.5,51.768689088129,13.3));
#46796=CARTESIAN_POINT('',(-2.5,52.4544328862007,13.2999999995898));
#46797=CARTESIAN_POINT('',(-2.5,70.2,13.3));
#46798=CARTESIAN_POINT('Ctrl Pts',(-2.5,52.4544328862007,13.2999999991796));
#46799=CARTESIAN_POINT('Ctrl Pts',(-2.49999999992006,52.4942096580698,13.0563895109075));
#46800=CARTESIAN_POINT('Ctrl Pts',(-2.46439545171715,52.5345368483334,12.8140008047215));
#46801=CARTESIAN_POINT('Ctrl Pts',(-2.30070537491682,52.6234500099736,12.2692915759769));
#46802=CARTESIAN_POINT('Ctrl Pts',(-2.147508716278,52.6680607852065,11.9794028432668));
#46803=CARTESIAN_POINT('Ctrl Pts',(-1.84810007490051,52.7375150314633,11.6096789462031));
#46804=CARTESIAN_POINT('Ctrl Pts',(-1.74303612520946,52.7598253545768,11.5015421202317));
#46805=CARTESIAN_POINT('Ctrl Pts',(-1.51675776766793,52.8048938653409,11.3071849715741));
#46806=CARTESIAN_POINT('Ctrl Pts',(-1.39627322822478,52.8275433882984,11.2209922473548));
#46807=CARTESIAN_POINT('Ctrl Pts',(-1.05758175359877,52.8876127463687,11.0214751733709));
#46808=CARTESIAN_POINT('Ctrl Pts',(-0.828886735133715,52.9239955574636,
10.9286382373325));
#46809=CARTESIAN_POINT('Ctrl Pts',(-0.264221855574125,53.0058422648009,
10.7914922772734));
#46810=CARTESIAN_POINT('Ctrl Pts',(0.074144148524351,53.0515521422413,10.778707717533));
#46811=CARTESIAN_POINT('Ctrl Pts',(0.700533014429393,53.1433159233277,10.8815396724768));
#46812=CARTESIAN_POINT('Ctrl Pts',(0.984924941083911,53.1877492055136,10.9827586030877));
#46813=CARTESIAN_POINT('Ctrl Pts',(1.53106617933084,53.2780073671093,11.2962766464776));
#46814=CARTESIAN_POINT('Ctrl Pts',(1.7821939982874,53.322619800311,11.5158993287024));
#46815=CARTESIAN_POINT('Ctrl Pts',(2.08290058941423,53.3912612919028,11.90779082202));
#46816=CARTESIAN_POINT('Ctrl Pts',(2.16945461946802,53.4139721382326,12.0469279035097));
#46817=CARTESIAN_POINT('Ctrl Pts',(2.36753984400065,53.4760439036145,12.4482612832306));
#46818=CARTESIAN_POINT('Ctrl Pts',(2.44895659786436,53.5152035156178,12.7226276688593));
#46819=CARTESIAN_POINT('Ctrl Pts',(2.5220255039177,53.5989556973617,13.3371076043503));
#46820=CARTESIAN_POINT('Ctrl Pts',(2.49442606497016,53.6422366924613,13.6740224821022));
#46821=CARTESIAN_POINT('Ctrl Pts',(2.30976107345451,53.7316145808187,14.3115528646591));
#46822=CARTESIAN_POINT('Ctrl Pts',(2.15675044867975,53.7766768871334,14.6063719814992));
#46823=CARTESIAN_POINT('Ctrl Pts',(1.75355144184725,53.8643022791095,15.1096681853563));
#46824=CARTESIAN_POINT('Ctrl Pts',(1.51099909853781,53.9054716088556,15.3166330063897));
#46825=CARTESIAN_POINT('Ctrl Pts',(1.09610865819898,53.9684124584055,15.552673695711));
#46826=CARTESIAN_POINT('Ctrl Pts',(0.948591906231343,53.9896138414012,15.6186562571482));
#46827=CARTESIAN_POINT('Ctrl Pts',(0.480197868595057,54.0547280313389,15.7759261900835));
#46828=CARTESIAN_POINT('Ctrl Pts',(0.146584506599161,54.0984333203008,15.817814060565));
#46829=CARTESIAN_POINT('Ctrl Pts',(-0.51913771734361,54.1846857779829,15.7682872903183));
#46830=CARTESIAN_POINT('Ctrl Pts',(-0.844472258303415,54.2266669885973,
15.6767307406235));
#46831=CARTESIAN_POINT('Ctrl Pts',(-1.44195705231916,54.3127851301454,15.369868722278));
#46832=CARTESIAN_POINT('Ctrl Pts',(-1.70755417061573,54.3560029992327,15.1568383263904));
#46833=CARTESIAN_POINT('Ctrl Pts',(-2.13458258207599,54.441757663764,14.6428521509289));
#46834=CARTESIAN_POINT('Ctrl Pts',(-2.29353918990075,54.4832145497734,14.3485349460562));
#46835=CARTESIAN_POINT('Ctrl Pts',(-2.46318625238237,54.5563678179391,13.7943353265305));
#46836=CARTESIAN_POINT('Ctrl Pts',(-2.5,54.5874357260752,13.54769488302));
#46837=CARTESIAN_POINT('Ctrl Pts',(-2.5,54.6185115759899,13.3));
#46838=CARTESIAN_POINT('',(0.286897399705336,52.3546462541016,10.8159730008272));
#46839=CARTESIAN_POINT('Ctrl Pts',(-2.5,53.601880595513,13.2999999999933));
#46840=CARTESIAN_POINT('Ctrl Pts',(-2.50000000000064,53.5731131225576,13.5392641191748));
#46841=CARTESIAN_POINT('Ctrl Pts',(-2.46565160583379,53.5445458247303,13.7773194039659));
#46842=CARTESIAN_POINT('Ctrl Pts',(-2.339909469218,53.4918334916248,14.2038876647921));
#46843=CARTESIAN_POINT('Ctrl Pts',(-2.25777010751144,53.467827568561,14.3930116395779));
#46844=CARTESIAN_POINT('Ctrl Pts',(-1.9836209286351,53.4045220441114,14.8578746983225));
#46845=CARTESIAN_POINT('Ctrl Pts',(-1.75778464162242,53.3652473856669,15.1088530205023));
#46846=CARTESIAN_POINT('Ctrl Pts',(-1.24350967275062,53.2908752019447,15.4902761625381));
#46847=CARTESIAN_POINT('Ctrl Pts',(-0.966350613583913,53.2564059017049,
15.6258997525158));
#46848=CARTESIAN_POINT('Ctrl Pts',(-0.511099720078386,53.201969793668,15.7528629360861));
#46849=CARTESIAN_POINT('Ctrl Pts',(-0.346530686780513,53.1827388820718,
15.7814675360167));
#46850=CARTESIAN_POINT('Ctrl Pts',(0.151806240932969,53.125532032502,15.8175089616181));
#46851=CARTESIAN_POINT('Ctrl Pts',(0.4854494957925,53.0888957746755,15.7749317149148));
#46852=CARTESIAN_POINT('Ctrl Pts',(1.11783352102538,53.0144318994423,15.5610460638276));
#46853=CARTESIAN_POINT('Ctrl Pts',(1.41001520366356,52.9767114590674,15.3913618338837));
#46854=CARTESIAN_POINT('Ctrl Pts',(1.89550517844697,52.9055575406695,14.9601614973445));
#46855=CARTESIAN_POINT('Ctrl Pts',(2.08926806752941,52.8723934770927,14.7085612058889));
#46856=CARTESIAN_POINT('Ctrl Pts',(2.30418077339101,52.8203737657069,14.2833087793285));
#46857=CARTESIAN_POINT('Ctrl Pts',(2.36294884427428,52.8027429700754,14.1322437127345));
#46858=CARTESIAN_POINT('Ctrl Pts',(2.48645812186145,52.7537446260197,13.6928781057888));
#46859=CARTESIAN_POINT('Ctrl Pts',(2.51543151191713,52.7236489171256,13.3973254962775));
#46860=CARTESIAN_POINT('Ctrl Pts',(2.46604118017213,52.6585527230857,12.7708822172963));
#46861=CARTESIAN_POINT('Ctrl Pts',(2.37349349969795,52.623144414568,12.4468103461552));
#46862=CARTESIAN_POINT('Ctrl Pts',(2.07867279225929,52.5585387625586,11.8774673299877));
#46863=CARTESIAN_POINT('Ctrl Pts',(1.88820132051613,52.5294443406335,11.6329067702848));
#46864=CARTESIAN_POINT('Ctrl Pts',(1.4522969279502,52.4716038860416,11.2465932927216));
#46865=CARTESIAN_POINT('Ctrl Pts',(1.21767054179381,52.4444919352275,11.0993087674344));
#46866=CARTESIAN_POINT('Ctrl Pts',(0.747444085012265,52.3970136639375,10.9028660147942));
#46867=CARTESIAN_POINT('Ctrl Pts',(0.519589731567782,52.3764011794508,10.8433860242739));
#46868=CARTESIAN_POINT('Ctrl Pts',(0.286774387752517,52.3551642862145,10.8165023755741));
#46869=CARTESIAN_POINT('Ctrl Pts',(0.286877445958826,52.3542721930149,10.816514278076));
#46870=CARTESIAN_POINT('Ctrl Pts',(0.0534685891634007,52.3201799922785,
10.7895522802234));
#46871=CARTESIAN_POINT('Ctrl Pts',(-0.18266081179476,52.2862606553252,10.7956204292661));
#46872=CARTESIAN_POINT('Ctrl Pts',(-0.683558456558155,52.2146770321189,
10.8798405647647));
#46873=CARTESIAN_POINT('Ctrl Pts',(-0.943406753658285,52.1772598924145,
10.9688110113775));
#46874=CARTESIAN_POINT('Ctrl Pts',(-1.4516945793859,52.0964405945036,11.2420579055508));
#46875=CARTESIAN_POINT('Ctrl Pts',(-1.6911231432963,52.0535484484607,11.4338091393431));
#46876=CARTESIAN_POINT('Ctrl Pts',(-2.1101240378482,51.9649275935853,11.9178794987417));
#46877=CARTESIAN_POINT('Ctrl Pts',(-2.276600969804,51.9204574267858,12.2136993571353));
#46878=CARTESIAN_POINT('Ctrl Pts',(-2.45946237885603,51.839359618117,12.781485196561));
#46879=CARTESIAN_POINT('Ctrl Pts',(-2.5,51.8038794390372,13.0400814168076));
#46880=CARTESIAN_POINT('Ctrl Pts',(-2.5,51.768689088129,13.3));
#46881=CARTESIAN_POINT('Origin',(0.,70.2,13.3));
#46882=CARTESIAN_POINT('',(-2.5,49.7250834523465,13.3));
#46883=CARTESIAN_POINT('',(-2.5,50.7693915870611,13.3));
#46884=CARTESIAN_POINT('',(-2.5,70.2,13.3));
#46885=CARTESIAN_POINT('',(-2.38836719431143,52.3345987243418,14.039166525391));
#46886=CARTESIAN_POINT('Ctrl Pts',(-2.5,50.7693915870611,13.3));
#46887=CARTESIAN_POINT('Ctrl Pts',(-2.5,50.7725682780938,13.2734783251166));
#46888=CARTESIAN_POINT('Ctrl Pts',(-2.49957796284895,50.7757476555801,13.2469500982438));
#46889=CARTESIAN_POINT('Ctrl Pts',(-2.48841632301576,50.8177866315958,12.8964628064063));
#46890=CARTESIAN_POINT('Ctrl Pts',(-2.41519323296121,50.8563021021842,12.5775523474777));
#46891=CARTESIAN_POINT('Ctrl Pts',(-2.14875170210609,50.9338853896533,11.9802824721953));
#46892=CARTESIAN_POINT('Ctrl Pts',(-1.95610079506944,50.9720594824519,11.7086364044699));
#46893=CARTESIAN_POINT('Ctrl Pts',(-1.5070040047066,51.045941333298,11.2846108392235));
#46894=CARTESIAN_POINT('Ctrl Pts',(-1.26509151548325,51.0801655353141,11.124574871138));
#46895=CARTESIAN_POINT('Ctrl Pts',(-0.730537283946954,51.147916669297,10.8909381507117));
#46896=CARTESIAN_POINT('Ctrl Pts',(-0.441024149265621,51.1808843734047,
10.8215380968865));
#46897=CARTESIAN_POINT('Ctrl Pts',(0.187481298086497,51.2534729750946,10.7847442286701));
#46898=CARTESIAN_POINT('Ctrl Pts',(0.521694952288247,51.291995383055,10.832296344163));
#46899=CARTESIAN_POINT('Ctrl Pts',(1.14160679155934,51.3666808956943,11.052458057065));
#46900=CARTESIAN_POINT('Ctrl Pts',(1.42259703054374,51.4022470936342,11.2189164682836));
#46901=CARTESIAN_POINT('Ctrl Pts',(1.88099796831056,51.4727552274126,11.6277728686283));
#46902=CARTESIAN_POINT('Ctrl Pts',(2.06262362807787,51.5059263156767,11.8577059227597));
#46903=CARTESIAN_POINT('Ctrl Pts',(2.34314018473742,51.5704941531685,12.378117007052));
#46904=CARTESIAN_POINT('Ctrl Pts',(2.43682352816317,51.6012773454488,12.665924165674));
#46905=CARTESIAN_POINT('Ctrl Pts',(2.52134667315964,51.66994238345,13.2880912876859));
#46906=CARTESIAN_POINT('Ctrl Pts',(2.50122058728866,51.706676664711,13.61847547561));
#46907=CARTESIAN_POINT('Ctrl Pts',(2.34212047022356,51.7723260907281,14.2236805603188));
#46908=CARTESIAN_POINT('Ctrl Pts',(2.21555212298877,51.8012326111194,14.4958383739554));
#46909=CARTESIAN_POINT('Ctrl Pts',(1.85692002585776,51.8662425903497,15.0051465134759));
#46910=CARTESIAN_POINT('Ctrl Pts',(1.61951574509793,51.9012134617866,15.2321217609254));
#46911=CARTESIAN_POINT('Ctrl Pts',(1.0937158446704,51.962859639302,15.5677722942097));
#46912=CARTESIAN_POINT('Ctrl Pts',(0.815636928066772,51.9895830661086,15.6819558533277));
#46913=CARTESIAN_POINT('Ctrl Pts',(0.208048024794138,52.050481122095,15.8121921422632));
#46914=CARTESIAN_POINT('Ctrl Pts',(-0.118429000940584,52.083533541405,15.818077387983));
#46915=CARTESIAN_POINT('Ctrl Pts',(-0.723190307698781,52.1391610915244,
15.7106921402116));
#46916=CARTESIAN_POINT('Ctrl Pts',(-0.998037080650211,52.1620883105981,
15.6104670007487));
#46917=CARTESIAN_POINT('Ctrl Pts',(-1.53285632026417,52.2156576959321,15.3018320883281));
#46918=CARTESIAN_POINT('Ctrl Pts',(-1.78177453963372,52.246149476322,15.0840161997767));
#46919=CARTESIAN_POINT('Ctrl Pts',(-2.16284095185504,52.2949202092249,14.5885950881461));
#46920=CARTESIAN_POINT('Ctrl Pts',(-2.30043496719591,52.3136961116099,14.322847980847));
#46921=CARTESIAN_POINT('Ctrl Pts',(-2.38824601620833,52.3343772023775,14.0391082235133));
#46922=CARTESIAN_POINT('',(-2.49999907835137,52.4541831787799,13.3021466817004));
#46923=CARTESIAN_POINT('Ctrl Pts',(-2.38823974721953,52.3348094618126,14.039128479901));
#46924=CARTESIAN_POINT('Ctrl Pts',(-2.39249209790126,52.3367544905651,14.0253884696141));
#46925=CARTESIAN_POINT('Ctrl Pts',(-2.39661953396157,52.3390485561389,14.0116326761911));
#46926=CARTESIAN_POINT('Ctrl Pts',(-2.40062839257814,52.3413419978795,13.9978419024017));
#46927=CARTESIAN_POINT('Ctrl Pts',(-2.42328041852285,52.3543010734616,13.9199172371658));
#46928=CARTESIAN_POINT('Ctrl Pts',(-2.44212535260044,52.367239303345,13.8409335891714));
#46929=CARTESIAN_POINT('Ctrl Pts',(-2.45709519403956,52.3802030616442,13.761175896408));
#46930=CARTESIAN_POINT('Ctrl Pts',(-2.4721416566318,52.3932331732254,13.6810099744449));
#46931=CARTESIAN_POINT('Ctrl Pts',(-2.48322978256872,52.406256383375,13.6002940375464));
#46932=CARTESIAN_POINT('Ctrl Pts',(-2.49036063219162,52.4192841759952,13.5193260623595));
#46933=CARTESIAN_POINT('Ctrl Pts',(-2.49672451963419,52.4309107577132,13.4470666391785));
#46934=CARTESIAN_POINT('Ctrl Pts',(-2.49993685890941,52.4425409927571,13.374606677753));
#46935=CARTESIAN_POINT('Ctrl Pts',(-2.49999907835137,52.4541831787799,13.3021466817004));
#46936=CARTESIAN_POINT('Ctrl Pts',(-2.49999909203731,52.4540850015726,13.3021306836036));
#46937=CARTESIAN_POINT('Ctrl Pts',(-2.49999969735462,52.4542009600857,13.3014204454813));
#46938=CARTESIAN_POINT('Ctrl Pts',(-2.50000000000023,52.4543169216404,13.3007102172747));
#46939=CARTESIAN_POINT('Ctrl Pts',(-2.5,52.4544328862007,13.2999999991796));
#46940=CARTESIAN_POINT('',(-1.29179640210147,50.1461249705794,11.1593417706458));
#46941=CARTESIAN_POINT('Ctrl Pts',(-2.5,51.768689088129,13.3));
#46942=CARTESIAN_POINT('Ctrl Pts',(-2.5,51.7629474434776,13.3424082199945));
#46943=CARTESIAN_POINT('Ctrl Pts',(-2.49892094169084,51.7572160263818,13.3848519830099));
#46944=CARTESIAN_POINT('Ctrl Pts',(-2.47966187969698,51.7063255121688,13.762610749563));
#46945=CARTESIAN_POINT('Ctrl Pts',(-2.3951862990094,51.6625830605823,14.0911222396105));
#46946=CARTESIAN_POINT('Ctrl Pts',(-2.1164369446295,51.5778134849495,14.6644346748973));
#46947=CARTESIAN_POINT('Ctrl Pts',(-1.93651301242115,51.5377720997179,14.909640372495));
#46948=CARTESIAN_POINT('Ctrl Pts',(-1.60034318458678,51.4770039596661,15.2273759684802));
#46949=CARTESIAN_POINT('Ctrl Pts',(-1.47303267800506,51.4561009033281,15.3263417277534));
#46950=CARTESIAN_POINT('Ctrl Pts',(-1.06878369447911,51.3939318251766,15.5822202654902));
#46951=CARTESIAN_POINT('Ctrl Pts',(-0.770539737270521,51.353141705809,15.6994025429945));
#46952=CARTESIAN_POINT('Ctrl Pts',(-0.293525913282724,51.2907737945221,
15.7883625346195));
#46953=CARTESIAN_POINT('Ctrl Pts',(-0.126038071449243,51.2693639414798,
15.8024438062637));
#46954=CARTESIAN_POINT('Ctrl Pts',(0.203287682843875,51.2272633415639,15.7969629520643));
#46955=CARTESIAN_POINT('Ctrl Pts',(0.364338283359357,51.2066748147378,15.7785905382435));
#46956=CARTESIAN_POINT('Ctrl Pts',(0.849018184601001,51.1435978432017,15.6750074593532));
#46957=CARTESIAN_POINT('Ctrl Pts',(1.15831829398671,51.1018788792346,15.5404999244014));
#46958=CARTESIAN_POINT('Ctrl Pts',(1.69668112210125,51.0195170473709,15.1642659370116));
#46959=CARTESIAN_POINT('Ctrl Pts',(1.92300757144743,50.9796175269159,14.9298133782415));
#46960=CARTESIAN_POINT('Ctrl Pts',(2.18566631018747,50.9197137082865,14.5241669991209));
#46961=CARTESIAN_POINT('Ctrl Pts',(2.25968390187904,50.8999441277541,14.3814601295327));
#46962=CARTESIAN_POINT('Ctrl Pts',(2.44111483740834,50.8400732404914,13.9302334886086));
#46963=CARTESIAN_POINT('Ctrl Pts',(2.50241299235157,50.8005785073798,13.6069190536023));
#46964=CARTESIAN_POINT('Ctrl Pts',(2.49871746097642,50.7416018946686,13.1222708694074));
#46965=CARTESIAN_POINT('Ctrl Pts',(2.48240477128401,50.722412470282,12.96406939397));
#46966=CARTESIAN_POINT('Ctrl Pts',(2.41975546825254,50.6839698686371,12.6516407152287));
#46967=CARTESIAN_POINT('Ctrl Pts',(2.37332527689488,50.6648064992292,12.4981782058203));
#46968=CARTESIAN_POINT('Ctrl Pts',(2.18578563885437,50.6056495927986,12.0415610428059));
#46969=CARTESIAN_POINT('Ctrl Pts',(1.9984932814877,50.5661344829914,11.7613637016388));
#46970=CARTESIAN_POINT('Ctrl Pts',(1.64697059303443,50.5076987274167,11.4122406162932));
#46971=CARTESIAN_POINT('Ctrl Pts',(1.52144957518724,50.4887776532648,11.3096877666298));
#46972=CARTESIAN_POINT('Ctrl Pts',(1.11231307495995,50.4311138012836,11.0368872096299));
#46973=CARTESIAN_POINT('Ctrl Pts',(0.804131611952014,50.3928664901067,10.9099476749318));
#46974=CARTESIAN_POINT('Ctrl Pts',(0.329225561166609,50.3372175099223,10.8170049888917));
#46975=CARTESIAN_POINT('Ctrl Pts',(0.175883705644164,50.319673507889,10.8014562283027));
#46976=CARTESIAN_POINT('Ctrl Pts',(-0.217021322703808,50.2746726455672,
10.7979852562611));
#46977=CARTESIAN_POINT('Ctrl Pts',(-0.455224259394456,50.2474269416367,
10.8301880342919));
#46978=CARTESIAN_POINT('Ctrl Pts',(-0.898164367839591,50.1954873287541,
10.9564291233102));
#46979=CARTESIAN_POINT('Ctrl Pts',(-1.10210590474819,50.1709733136877,11.0451389016571));
#46980=CARTESIAN_POINT('Ctrl Pts',(-1.29169878399524,50.1463083191803,11.159552791722));
#46981=CARTESIAN_POINT('Ctrl Pts',(-1.29163435892636,50.1458351890062,11.1595139143548));
#46982=CARTESIAN_POINT('Ctrl Pts',(-1.46762460773575,50.1105095323541,11.2657117792802));
#46983=CARTESIAN_POINT('Ctrl Pts',(-1.62986516721391,50.0749704644603,11.393219411866));
#46984=CARTESIAN_POINT('Ctrl Pts',(-1.94536507579223,49.9990922641977,11.7112007736914));
#46985=CARTESIAN_POINT('Ctrl Pts',(-2.09010636036623,49.9604708810454,11.9070648993695));
#46986=CARTESIAN_POINT('Ctrl Pts',(-2.35338776298511,49.8708349028971,12.3993094134785));
#46987=CARTESIAN_POINT('Ctrl Pts',(-2.44820394406151,49.8195830419382,12.7033849088837));
#46988=CARTESIAN_POINT('Ctrl Pts',(-2.49465709755074,49.7543437774861,13.1111596643773));
#46989=CARTESIAN_POINT('Ctrl Pts',(-2.5,49.7395751853974,13.2056242711644));
#46990=CARTESIAN_POINT('Ctrl Pts',(-2.5,49.7250834523465,13.2999999999999));
#46991=CARTESIAN_POINT('Origin',(0.,70.2,13.3));
#46992=CARTESIAN_POINT('',(-2.5,47.5828357057113,13.3000000065378));
#46993=CARTESIAN_POINT('',(-2.5,48.7838403868077,13.299999999879));
#46994=CARTESIAN_POINT('',(-2.5,70.2,13.3));
#46995=CARTESIAN_POINT('',(-2.4999999894034,48.7838710165738,13.2997698196152));
#46996=CARTESIAN_POINT('Ctrl Pts',(-2.5,48.7838403868077,13.2999999997579));
#46997=CARTESIAN_POINT('Ctrl Pts',(-2.49999999999999,48.7838510363932,13.2999199689242));
#46998=CARTESIAN_POINT('Ctrl Pts',(-2.49999999615702,48.7838616860023,13.2998399380025));
#46999=CARTESIAN_POINT('Ctrl Pts',(-2.49999998847107,48.7838723356347,13.2997599069931));
#47000=CARTESIAN_POINT('Ctrl Pts',(-2.4999999894034,48.7838710165738,13.2997698196152));
#47001=CARTESIAN_POINT('Ctrl Pts',(-2.49997574528622,48.8189102305316,13.0364533222377));
#47002=CARTESIAN_POINT('Ctrl Pts',(-2.45835285905331,48.8540155824351,12.774780871668));
#47003=CARTESIAN_POINT('Ctrl Pts',(-2.28928258735442,48.9260073663749,12.2566873908404));
#47004=CARTESIAN_POINT('Ctrl Pts',(-2.15729167260878,48.962680734914,12.0056201297113));
#47005=CARTESIAN_POINT('Ctrl Pts',(-1.78503266972356,49.0435148904801,11.5185791184643));
#47006=CARTESIAN_POINT('Ctrl Pts',(-1.53344516837968,49.0862670222244,11.2979060528129));
#47007=CARTESIAN_POINT('Ctrl Pts',(-0.976340908060309,49.1702162853774,
10.9775845227962));
#47008=CARTESIAN_POINT('Ctrl Pts',(-0.679913943215935,49.2106048164309,
10.8741807152196));
#47009=CARTESIAN_POINT('Ctrl Pts',(-0.0538643248561953,49.2926435889597,
10.7799440859284));
#47010=CARTESIAN_POINT('Ctrl Pts',(0.270685388248418,49.3339325108916,10.7939412577153));
#47011=CARTESIAN_POINT('Ctrl Pts',(0.746092934661981,49.3969442602778,10.9080864923979));
#47012=CARTESIAN_POINT('Ctrl Pts',(0.904210893931087,49.4183681529807,10.9632694047121));
#47013=CARTESIAN_POINT('Ctrl Pts',(1.20169591364608,49.4605596397534,11.1018445214737));
#47014=CARTESIAN_POINT('Ctrl Pts',(1.3408343894498,49.4812203909971,11.1838417173814));
#47015=CARTESIAN_POINT('Ctrl Pts',(1.74148294898111,49.5447523390527,11.475429903687));
#47016=CARTESIAN_POINT('Ctrl Pts',(1.96965794407698,49.5866819322116,11.7244709889722));
#47017=CARTESIAN_POINT('Ctrl Pts',(2.3035072345252,49.6690421294183,12.279278766032));
#47018=CARTESIAN_POINT('Ctrl Pts',(2.41311500808524,49.7086718580359,12.5754945777285));
#47019=CARTESIAN_POINT('Ctrl Pts',(2.49255119753986,49.7691462220849,13.0464939837112));
#47020=CARTESIAN_POINT('Ctrl Pts',(2.50383101667476,49.7898790402248,13.2110631978932));
#47021=CARTESIAN_POINT('Ctrl Pts',(2.48876699441618,49.8527914321867,13.7093365956019));
#47022=CARTESIAN_POINT('Ctrl Pts',(2.41189695913903,49.8943888319195,14.0377567516765));
#47023=CARTESIAN_POINT('Ctrl Pts',(2.20582409122037,49.9565519988986,14.4875106276615));
#47024=CARTESIAN_POINT('Ctrl Pts',(2.12492163897261,49.9766894446145,14.6268578607494));
#47025=CARTESIAN_POINT('Ctrl Pts',(1.93541762073261,50.0174132607323,14.8909594056961));
#47026=CARTESIAN_POINT('Ctrl Pts',(1.82670587767699,50.0378968015838,15.0146842823719));
#47027=CARTESIAN_POINT('Ctrl Pts',(1.51696441892292,50.0907830912343,15.3040444892191));
#47028=CARTESIAN_POINT('Ctrl Pts',(1.30083833751125,50.1228859371001,15.4506283318528));
#47029=CARTESIAN_POINT('Ctrl Pts',(0.762507559903441,50.1968745761546,15.7044104100344));
#47030=CARTESIAN_POINT('Ctrl Pts',(0.433230957433051,50.2381038171472,15.7849436110871));
#47031=CARTESIAN_POINT('Ctrl Pts',(-0.1515114467204,50.3102707019366,15.8078546984625));
#47032=CARTESIAN_POINT('Ctrl Pts',(-0.400965222433192,50.3407507399289,
15.7802255237307));
#47033=CARTESIAN_POINT('Ctrl Pts',(-0.966146157028917,50.4128391759118,
15.6300073374752));
#47034=CARTESIAN_POINT('Ctrl Pts',(-1.26954502935261,50.4537469703206,15.4796029785403));
#47035=CARTESIAN_POINT('Ctrl Pts',(-1.76994747238211,50.5309283253864,15.0906410124269));
#47036=CARTESIAN_POINT('Ctrl Pts',(-1.97093128696611,50.5667926990972,14.8666983644878));
#47037=CARTESIAN_POINT('Ctrl Pts',(-2.30115625921089,50.6432443336031,14.3314327480784));
#47038=CARTESIAN_POINT('Ctrl Pts',(-2.41720417231426,50.6827743714643,14.0185729409194));
#47039=CARTESIAN_POINT('Ctrl Pts',(-2.48965734046885,50.7380156454991,13.5624242089609));
#47040=CARTESIAN_POINT('Ctrl Pts',(-2.5,50.7536658271994,13.4312918020845));
#47041=CARTESIAN_POINT('Ctrl Pts',(-2.5,50.7693915870611,13.3));
#47042=CARTESIAN_POINT('Ctrl Pts',(-2.5,49.7250834523465,13.2999999999999));
#47043=CARTESIAN_POINT('Ctrl Pts',(-2.50000000000001,49.6903982705044,13.5258832193953));
#47044=CARTESIAN_POINT('Ctrl Pts',(-2.46939640538158,49.6567888895813,13.7511788687082));
#47045=CARTESIAN_POINT('Ctrl Pts',(-2.32753734732961,49.5766501239402,14.2613220295873));
#47046=CARTESIAN_POINT('Ctrl Pts',(-2.19419348848113,49.5302683919951,14.5357830192452));
#47047=CARTESIAN_POINT('Ctrl Pts',(-1.91789616941836,49.4609289592335,14.9120140623529));
#47048=CARTESIAN_POINT('Ctrl Pts',(-1.80799082825554,49.4370358396022,15.0343884028129));
#47049=CARTESIAN_POINT('Ctrl Pts',(-1.46177996646387,49.3682292374493,15.3509041504178));
#47050=CARTESIAN_POINT('Ctrl Pts',(-1.20093128353508,49.3231151588567,15.5137705746146));
#47051=CARTESIAN_POINT('Ctrl Pts',(-0.604625773530855,49.2303253984791,
15.7489461068489));
#47052=CARTESIAN_POINT('Ctrl Pts',(-0.270477891234554,49.1857501758419,
15.8079524723122));
#47053=CARTESIAN_POINT('Ctrl Pts',(0.211777654371516,49.1186201656644,15.7953058242519));
#47054=CARTESIAN_POINT('Ctrl Pts',(0.357352633227321,49.0980103424572,15.7786439468728));
#47055=CARTESIAN_POINT('Ctrl Pts',(0.78740304282428,49.0351235627537,15.6907506695462));
#47056=CARTESIAN_POINT('Ctrl Pts',(1.06166772416961,48.9921157803747,15.5822247676385));
#47057=CARTESIAN_POINT('Ctrl Pts',(1.59682086504989,48.9029774494922,15.2526649230808));
#47058=CARTESIAN_POINT('Ctrl Pts',(1.8443772937165,48.8589548350079,15.0207937331081));
#47059=CARTESIAN_POINT('Ctrl Pts',(2.22984221920842,48.7677785303737,14.4776143496617));
#47060=CARTESIAN_POINT('Ctrl Pts',(2.36564142860816,48.7216196921004,14.1732696455439));
#47061=CARTESIAN_POINT('Ctrl Pts',(2.49828338508911,48.6375467068815,13.5867578797384));
#47062=CARTESIAN_POINT('Ctrl Pts',(2.5146696928622,48.6010656145741,13.3140065050327));
#47063=CARTESIAN_POINT('Ctrl Pts',(2.45262497002278,48.5203840757889,12.7116469996151));
#47064=CARTESIAN_POINT('Ctrl Pts',(2.3521838591124,48.4765720900617,12.3896289644743));
#47065=CARTESIAN_POINT('Ctrl Pts',(2.11339554843581,48.4106913930493,11.9546869439607));
#47066=CARTESIAN_POINT('Ctrl Pts',(2.02168512650663,48.3891711071079,11.8204398478526));
#47067=CARTESIAN_POINT('Ctrl Pts',(1.7026193999923,48.3232321701159,11.4389836398935));
#47068=CARTESIAN_POINT('Ctrl Pts',(1.4381010366275,48.279843063557,11.2277544124366));
#47069=CARTESIAN_POINT('Ctrl Pts',(0.844613033353298,48.192514944874,10.9237369856404));
#47070=CARTESIAN_POINT('Ctrl Pts',(0.522249665684434,48.1498093742071,10.8327578245077));
#47071=CARTESIAN_POINT('Ctrl Pts',(0.0309148217236938,48.0858638403156,
10.7950069533122));
#47072=CARTESIAN_POINT('Ctrl Pts',(-0.130513606119788,48.0650250082897,
10.7982173017314));
#47073=CARTESIAN_POINT('Ctrl Pts',(-0.451827532153677,48.0232626490109,
10.8358104321365));
#47074=CARTESIAN_POINT('Ctrl Pts',(-0.610925446739087,48.0024123387974,
10.8703596175259));
#47075=CARTESIAN_POINT('Ctrl Pts',(-1.08299660625344,47.9386852182676,11.0222118837479));
#47076=CARTESIAN_POINT('Ctrl Pts',(-1.37684940664384,47.8964615822085,11.1868232541413));
#47077=CARTESIAN_POINT('Ctrl Pts',(-1.73989261239969,47.8354714326538,11.4989253870466));
#47078=CARTESIAN_POINT('Ctrl Pts',(-1.84157450578367,47.8170194101915,11.6030316477075));
#47079=CARTESIAN_POINT('Ctrl Pts',(-2.14516061070636,47.7562049055104,11.9734840618113));
#47080=CARTESIAN_POINT('Ctrl Pts',(-2.30289297602479,47.7146384666952,12.2713687991248));
#47081=CARTESIAN_POINT('Ctrl Pts',(-2.46550448428009,47.6426728931688,12.8215874592548));
#47082=CARTESIAN_POINT('Ctrl Pts',(-2.50000000125408,47.612791848772,13.0602271230663));
#47083=CARTESIAN_POINT('Ctrl Pts',(-2.5,47.5828357057113,13.3000000130757));
#47084=CARTESIAN_POINT('Origin',(0.,70.2,13.3));
#47085=CARTESIAN_POINT('',(-2.4999999974205,45.6622550402693,13.3001106063177));
#47086=CARTESIAN_POINT('',(-2.5,46.4777801864859,13.3));
#47087=CARTESIAN_POINT('',(-2.5,70.2,13.3));
#47088=CARTESIAN_POINT('',(-1.87910183479348,46.6587897073237,11.6508024920329));
#47089=CARTESIAN_POINT('Ctrl Pts',(-2.5,46.4777801864859,13.3));
#47090=CARTESIAN_POINT('Ctrl Pts',(-2.5,46.4830105492051,13.2490202868915));
#47091=CARTESIAN_POINT('Ctrl Pts',(-2.49844064223901,46.4882548457263,13.1980275614499));
#47092=CARTESIAN_POINT('Ctrl Pts',(-2.47718908444389,46.5241995259477,12.8512180824113));
#47093=CARTESIAN_POINT('Ctrl Pts',(-2.40656458679348,46.5551780664903,12.5607941863735));
#47094=CARTESIAN_POINT('Ctrl Pts',(-2.18400029226825,46.6100024289926,12.0571541864303));
#47095=CARTESIAN_POINT('Ctrl Pts',(-2.0465266140265,46.6339946691803,11.8418305389474));
#47096=CARTESIAN_POINT('Ctrl Pts',(-1.87896154964605,46.6586668546072,11.6509082818255));
#47097=CARTESIAN_POINT('Ctrl Pts',(-1.87901788858152,46.6592025379051,11.6509724761573));
#47098=CARTESIAN_POINT('Ctrl Pts',(-1.74699164114983,46.6998851401868,11.500532488286));
#47099=CARTESIAN_POINT('Ctrl Pts',(-1.59720813559193,46.7391955629047,11.3663107355683));
#47100=CARTESIAN_POINT('Ctrl Pts',(-1.25403850047345,46.8210059840895,11.1262930418455));
#47101=CARTESIAN_POINT('Ctrl Pts',(-1.05944758583789,46.8632172518255,11.0250662714878));
#47102=CARTESIAN_POINT('Ctrl Pts',(-0.544166560882871,46.9645676849873,
10.8377624703872));
#47103=CARTESIAN_POINT('Ctrl Pts',(-0.214915533581655,47.0186313783139,
10.7874704793054));
#47104=CARTESIAN_POINT('Ctrl Pts',(0.276761682213298,47.1043207465961,10.8100873388383));
#47105=CARTESIAN_POINT('Ctrl Pts',(0.437519261792401,47.1328212176497,10.8332545201594));
#47106=CARTESIAN_POINT('Ctrl Pts',(0.885760131996727,47.21292858199,10.9430729957404));
#47107=CARTESIAN_POINT('Ctrl Pts',(1.16130971101538,47.2602483499833,11.0658987731741));
#47108=CARTESIAN_POINT('Ctrl Pts',(1.66921185219965,47.3586066748806,11.4124045837215));
#47109=CARTESIAN_POINT('Ctrl Pts',(1.89345795437946,47.410470043977,11.6374877762812));
#47110=CARTESIAN_POINT('Ctrl Pts',(2.24644783535437,47.5111516605348,12.1587326169901));
#47111=CARTESIAN_POINT('Ctrl Pts',(2.37215372753031,47.5573696330684,12.4502498929423));
#47112=CARTESIAN_POINT('Ctrl Pts',(2.4747600485298,47.6288937975688,12.9119953233282));
#47113=CARTESIAN_POINT('Ctrl Pts',(2.4943430314003,47.6527929533407,13.0692291393975));
#47114=CARTESIAN_POINT('Ctrl Pts',(2.50378384770508,47.7012700702939,13.3936681567683));
#47115=CARTESIAN_POINT('Ctrl Pts',(2.49199646048104,47.7258929996258,13.5601290139263));
#47116=CARTESIAN_POINT('Ctrl Pts',(2.43725263891949,47.7739830422757,13.8780890896514));
#47117=CARTESIAN_POINT('Ctrl Pts',(2.39639110721557,47.7973022583608,14.0291817578749));
#47118=CARTESIAN_POINT('Ctrl Pts',(2.2244785699268,47.8695901545692,14.4890030179992));
#47119=CARTESIAN_POINT('Ctrl Pts',(2.04556865224883,47.9148274738864,14.7757189017264));
#47120=CARTESIAN_POINT('Ctrl Pts',(1.61883799436477,48.0030114602919,15.2264157643961));
#47121=CARTESIAN_POINT('Ctrl Pts',(1.38818249737406,48.0448566395512,15.3987030382261));
#47122=CARTESIAN_POINT('Ctrl Pts',(0.839139340630911,48.1340437022763,15.6780182320207));
#47123=CARTESIAN_POINT('Ctrl Pts',(0.517942830195246,48.1784860240865,15.7679950903323));
#47124=CARTESIAN_POINT('Ctrl Pts',(0.0340986027569455,48.2451128817299,
15.8045479509993));
#47125=CARTESIAN_POINT('Ctrl Pts',(-0.120860399820526,48.266421357235,15.8018601577716));
#47126=CARTESIAN_POINT('Ctrl Pts',(-0.43290277621311,48.3101123509077,15.7673820577644));
#47127=CARTESIAN_POINT('Ctrl Pts',(-0.589208928960504,48.3324054043071,
15.7347917179916));
#47128=CARTESIAN_POINT('Ctrl Pts',(-1.06106293249441,48.4011291534717,15.588278470483));
#47129=CARTESIAN_POINT('Ctrl Pts',(-1.35762355331889,48.4457745713593,15.4257913365375));
#47130=CARTESIAN_POINT('Ctrl Pts',(-1.73500600029322,48.5132396489618,15.1069565607301));
#47131=CARTESIAN_POINT('Ctrl Pts',(-1.84652571753528,48.5349543464534,14.9928360831729));
#47132=CARTESIAN_POINT('Ctrl Pts',(-2.12160124238921,48.5941076542015,14.651559193866));
#47133=CARTESIAN_POINT('Ctrl Pts',(-2.25914295898414,48.6312127057787,14.4064310035721));
#47134=CARTESIAN_POINT('Ctrl Pts',(-2.40004964397745,48.6874862202398,14.0133847018049));
#47135=CARTESIAN_POINT('Ctrl Pts',(-2.43586215021993,48.7060956575831,13.8794306460086));
#47136=CARTESIAN_POINT('Ctrl Pts',(-2.48674785730144,48.7443900574573,13.5969335522108));
#47137=CARTESIAN_POINT('Ctrl Pts',(-2.50000000001439,48.7640641411391,13.4486169967807));
#47138=CARTESIAN_POINT('Ctrl Pts',(-2.5,48.7838403868077,13.2999999997579));
#47139=CARTESIAN_POINT('',(-1.95241364042681,45.9847503099714,11.7382273262856));
#47140=CARTESIAN_POINT('Ctrl Pts',(-2.5,47.5828357057113,13.3000000130757));
#47141=CARTESIAN_POINT('Ctrl Pts',(-2.49999999988754,47.580149426164,13.3215013461792));
#47142=CARTESIAN_POINT('Ctrl Pts',(-2.49972261604871,47.5774625853922,13.3430117973173));
#47143=CARTESIAN_POINT('Ctrl Pts',(-2.49064932102071,47.5335626046913,13.694430775638));
#47144=CARTESIAN_POINT('Ctrl Pts',(-2.41689054183271,47.4928768995489,14.0194297820736));
#47145=CARTESIAN_POINT('Ctrl Pts',(-2.21590428308462,47.4319732142735,14.4687935698638));
#47146=CARTESIAN_POINT('Ctrl Pts',(-2.13542073530784,47.4120208351259,14.6100742067107));
#47147=CARTESIAN_POINT('Ctrl Pts',(-1.86622631964636,47.3547396476907,14.9910932697066));
#47148=CARTESIAN_POINT('Ctrl Pts',(-1.64672079606039,47.3180163680394,15.2054990699382));
#47149=CARTESIAN_POINT('Ctrl Pts',(-1.1240201231474,47.2412721013692,15.5566442994732));
#47150=CARTESIAN_POINT('Ctrl Pts',(-0.82107028701758,47.202049173162,15.6836418282125));
#47151=CARTESIAN_POINT('Ctrl Pts',(-0.348087286477959,47.1439686671439,
15.7806469592988));
#47152=CARTESIAN_POINT('Ctrl Pts',(-0.19125206581969,47.1251608335839,15.7976388201433));
#47153=CARTESIAN_POINT('Ctrl Pts',(0.30112414241352,47.0661834403037,15.8043080367654));
#47154=CARTESIAN_POINT('Ctrl Pts',(0.633656549999821,47.0262185349478,15.7414654240893));
#47155=CARTESIAN_POINT('Ctrl Pts',(1.23211609927269,46.9497561628566,15.4974418996739));
#47156=CARTESIAN_POINT('Ctrl Pts',(1.49585027002142,46.9138741700829,15.3271423933475));
#47157=CARTESIAN_POINT('Ctrl Pts',(1.95245580769975,46.8397792533204,14.8935256422817));
#47158=CARTESIAN_POINT('Ctrl Pts',(2.13939672991357,46.8026790523447,14.6320864962856));
#47159=CARTESIAN_POINT('Ctrl Pts',(2.33801366848224,46.7478665454617,14.1992046869808));
#47160=CARTESIAN_POINT('Ctrl Pts',(2.39007607071443,46.7298967541087,14.0499438109266));
#47161=CARTESIAN_POINT('Ctrl Pts',(2.50758575779311,46.6734948504716,13.5719024989991));
#47162=CARTESIAN_POINT('Ctrl Pts',(2.5214364021705,46.6349281579702,13.2342557529887));
#47163=CARTESIAN_POINT('Ctrl Pts',(2.41883814181262,46.5618299390585,12.5949272678783));
#47164=CARTESIAN_POINT('Ctrl Pts',(2.31169697158706,46.5277144725562,12.2980148716835));
#47165=CARTESIAN_POINT('Ctrl Pts',(2.06963958082871,46.4742334299024,11.8882013837772));
#47166=CARTESIAN_POINT('Ctrl Pts',(1.973178442969,46.4559226114626,11.7562514514113));
#47167=CARTESIAN_POINT('Ctrl Pts',(1.66895942718863,46.4052547431179,11.4156482224247));
#47168=CARTESIAN_POINT('Ctrl Pts',(1.43630474427017,46.374001177999,11.2328084599424));
#47169=CARTESIAN_POINT('Ctrl Pts',(0.882482661220567,46.3064936411012,10.9371963448682));
#47170=CARTESIAN_POINT('Ctrl Pts',(0.559159106126154,46.2698835019907,10.8405253564252));
#47171=CARTESIAN_POINT('Ctrl Pts',(-0.07844214110819,46.2024042558339,10.7825577128121));
#47172=CARTESIAN_POINT('Ctrl Pts',(-0.385755012755789,46.1718357764588,
10.8110474174565));
#47173=CARTESIAN_POINT('Ctrl Pts',(-0.949126279226214,46.1109526265218,
10.9703629760132));
#47174=CARTESIAN_POINT('Ctrl Pts',(-1.20341881472457,46.0820057444069,11.090943154281));
#47175=CARTESIAN_POINT('Ctrl Pts',(-1.62814787306659,46.0306164683876,11.3879041868699));
#47176=CARTESIAN_POINT('Ctrl Pts',(-1.80315871885665,46.0080357480293,11.5519756553128));
#47177=CARTESIAN_POINT('Ctrl Pts',(-1.95225418005292,45.9848322558052,11.7383650822084));
#47178=CARTESIAN_POINT('Ctrl Pts',(-1.95219597877177,45.9842543345744,11.73829232554));
#47179=CARTESIAN_POINT('Ctrl Pts',(-2.12796165206232,45.9271257317385,11.9580063259355));
#47180=CARTESIAN_POINT('Ctrl Pts',(-2.26566846203269,45.8714534636839,12.2062796187581));
#47181=CARTESIAN_POINT('Ctrl Pts',(-2.45229591942592,45.7631222498252,12.7381805495956));
#47182=CARTESIAN_POINT('Ctrl Pts',(-2.50000000001646,45.7131063519431,13.0178816481088));
#47183=CARTESIAN_POINT('Ctrl Pts',(-2.5,45.6622749689603,13.3000000001458));
#47184=CARTESIAN_POINT('Origin',(0.,70.2,13.3));
#47185=CARTESIAN_POINT('',(-2.5,43.4016964318852,13.3));
#47186=CARTESIAN_POINT('Ctrl Pts',(-2.49999999728054,45.6622539589675,13.3001166074741));
#47187=CARTESIAN_POINT('Ctrl Pts',(-2.49998664111617,45.6106604689999,13.5864654126283));
#47188=CARTESIAN_POINT('Ctrl Pts',(-2.45078497592242,45.5605981192958,13.8709891497258));
#47189=CARTESIAN_POINT('Ctrl Pts',(-2.24983810586681,45.4604737620495,14.4333224109686));
#47190=CARTESIAN_POINT('Ctrl Pts',(-2.09195269470515,45.4086587772158,14.7035850380949));
#47191=CARTESIAN_POINT('Ctrl Pts',(-1.68198748850155,45.3064765619204,15.1762625889758));
#47192=CARTESIAN_POINT('Ctrl Pts',(-1.43193516873979,45.2562510834677,15.3734451691347));
#47193=CARTESIAN_POINT('Ctrl Pts',(-0.875083021048201,45.1566278827318,
15.662508131224));
#47194=CARTESIAN_POINT('Ctrl Pts',(-0.574044701395826,45.1112015984706,
15.7531198772918));
#47195=CARTESIAN_POINT('Ctrl Pts',(0.0422675366606626,45.0182474319853,
15.8185227476926));
#47196=CARTESIAN_POINT('Ctrl Pts',(0.351594189057949,44.9707018991942,15.7941971063011));
#47197=CARTESIAN_POINT('Ctrl Pts',(0.974006309437163,44.8742410321479,15.6269684377271));
#47198=CARTESIAN_POINT('Ctrl Pts',(1.27837052541315,44.8274949233512,15.4747111513947));
#47199=CARTESIAN_POINT('Ctrl Pts',(1.76609381912382,44.7364782702921,15.0919199708914));
#47200=CARTESIAN_POINT('Ctrl Pts',(1.9574996528276,44.6942642651608,14.8806308671294));
#47201=CARTESIAN_POINT('Ctrl Pts',(2.19626282599974,44.6307703526445,14.5052293408213));
#47202=CARTESIAN_POINT('Ctrl Pts',(2.26961685394048,44.6081147478852,14.3606626821417));
#47203=CARTESIAN_POINT('Ctrl Pts',(2.44389497539902,44.5406851690895,13.9147221371947));
#47204=CARTESIAN_POINT('Ctrl Pts',(2.50207812577016,44.4961668043628,13.6001750912055));
#47205=CARTESIAN_POINT('Ctrl Pts',(2.49767576479121,44.4048307230385,12.9464434015316));
#47206=CARTESIAN_POINT('Ctrl Pts',(2.42740886800472,44.360108503826,12.6136318761029));
#47207=CARTESIAN_POINT('Ctrl Pts',(2.17739961569252,44.272955151226,12.0375697022272));
#47208=CARTESIAN_POINT('Ctrl Pts',(2.01566261751725,44.2319988345987,11.7926948973962));
#47209=CARTESIAN_POINT('Ctrl Pts',(1.59635476843331,44.1486730222525,11.3498389243424));
#47210=CARTESIAN_POINT('Ctrl Pts',(1.33506313530245,44.1062760606926,11.1624410516961));
#47211=CARTESIAN_POINT('Ctrl Pts',(0.75828226891258,44.0209097855453,10.8968640038899));
#47212=CARTESIAN_POINT('Ctrl Pts',(0.448433039469844,43.9781994253374,10.8202922877834));
#47213=CARTESIAN_POINT('Ctrl Pts',(-0.201557863363527,43.8908353903719,
10.7857725748925));
#47214=CARTESIAN_POINT('Ctrl Pts',(-0.535922828130152,43.8472982241007,
10.8352900581576));
#47215=CARTESIAN_POINT('Ctrl Pts',(-1.1613401152287,43.7588818971409,11.0615921907786));
#47216=CARTESIAN_POINT('Ctrl Pts',(-1.44672243022223,43.715966191786,11.2345198571569));
#47217=CARTESIAN_POINT('Ctrl Pts',(-1.80873444394829,43.6512782533907,11.5666939944687));
#47218=CARTESIAN_POINT('Ctrl Pts',(-1.91647670182185,43.6300914126777,11.6866220255007));
#47219=CARTESIAN_POINT('Ctrl Pts',(-2.21038599525522,43.5650433675776,12.0851112037626));
#47220=CARTESIAN_POINT('Ctrl Pts',(-2.3528632622903,43.5220521048097,12.3912576082094));
#47221=CARTESIAN_POINT('Ctrl Pts',(-2.47691254645397,43.4525796362456,12.9079271234051));
#47222=CARTESIAN_POINT('Ctrl Pts',(-2.5,43.4270730771034,13.1038350369808));
#47223=CARTESIAN_POINT('Ctrl Pts',(-2.5,43.4016964318852,13.3));
#47224=CARTESIAN_POINT('',(-2.50002611214299,44.6193946092241,13.2998651846547));
#47225=CARTESIAN_POINT('',(-2.5,70.2,13.3));
#47226=CARTESIAN_POINT('Ctrl Pts',(-2.49999999639604,44.6193990784213,13.2998657621837));
#47227=CARTESIAN_POINT('Ctrl Pts',(-2.49999100145858,44.6409901617092,13.1323470686192));
#47228=CARTESIAN_POINT('Ctrl Pts',(-2.48314441819972,44.6624023350778,12.965242875278));
#47229=CARTESIAN_POINT('Ctrl Pts',(-2.41797240101115,44.7042228684327,12.645248990369));
#47230=CARTESIAN_POINT('Ctrl Pts',(-2.37143889695187,44.7245287023665,12.4928019948569));
#47231=CARTESIAN_POINT('Ctrl Pts',(-2.18409069381321,44.7872598979828,12.0391052509022));
#47232=CARTESIAN_POINT('Ctrl Pts',(-1.99762736346973,44.8289540052538,11.7606413626008));
#47233=CARTESIAN_POINT('Ctrl Pts',(-1.6499239108512,44.8909851826536,11.4151083239769));
#47234=CARTESIAN_POINT('Ctrl Pts',(-1.52727392969976,44.910955647363,11.3144264890428));
#47235=CARTESIAN_POINT('Ctrl Pts',(-1.12680585458803,44.9718631052918,11.0448848129115));
#47236=CARTESIAN_POINT('Ctrl Pts',(-0.824963188572854,45.0121601453836,
10.9178359801667));
#47237=CARTESIAN_POINT('Ctrl Pts',(-0.193166708270342,45.092687514167,10.7869188662199));
#47238=CARTESIAN_POINT('Ctrl Pts',(0.130555871776583,45.1322023431919,10.7828845587215));
#47239=CARTESIAN_POINT('Ctrl Pts',(0.6110651145995,45.1926497638151,10.8700470275991));
#47240=CARTESIAN_POINT('Ctrl Pts',(0.772505911741462,45.2132826631378,10.9164498203768));
#47241=CARTESIAN_POINT('Ctrl Pts',(1.22047443871637,45.2726551871119,11.0955513659098));
#47242=CARTESIAN_POINT('Ctrl Pts',(1.4881722943468,45.3108153377255,11.2666486023629));
#47243=CARTESIAN_POINT('Ctrl Pts',(1.96020347156416,45.3900826946697,11.7127038147139));
#47244=CARTESIAN_POINT('Ctrl Pts',(2.15479685788948,45.4304878677962,11.9889690111091));
#47245=CARTESIAN_POINT('Ctrl Pts',(2.35152892376341,45.4894170845314,12.4372568622078));
#47246=CARTESIAN_POINT('Ctrl Pts',(2.4004766743675,45.5079360915437,12.5846471038827));
#47247=CARTESIAN_POINT('Ctrl Pts',(2.51074327011427,45.5663738945558,13.0604826415139));
#47248=CARTESIAN_POINT('Ctrl Pts',(2.52027469121408,45.606157467725,13.3971634017789));
#47249=CARTESIAN_POINT('Ctrl Pts',(2.43701399373081,45.6641806090174,13.8788750633255));
#47250=CARTESIAN_POINT('Ctrl Pts',(2.39634217504537,45.6824450932429,14.0291676522049));
#47251=CARTESIAN_POINT('Ctrl Pts',(2.2873235497184,45.7189880718122,14.3210540672638));
#47252=CARTESIAN_POINT('Ctrl Pts',(2.21907468010472,45.7371867695919,14.4619410912828));
#47253=CARTESIAN_POINT('Ctrl Pts',(1.96668954146464,45.7943870256208,14.8784732453492));
#47254=CARTESIAN_POINT('Ctrl Pts',(1.74075136704802,45.8330427646287,15.1246358015802));
#47255=CARTESIAN_POINT('Ctrl Pts',(1.20657239910928,45.9092064476877,15.5143347371929));
#47256=CARTESIAN_POINT('Ctrl Pts',(0.903774907157531,45.94648570611,15.6542057950761));
#47257=CARTESIAN_POINT('Ctrl Pts',(0.29484300743038,46.0185762956438,15.8001221323276));
#47258=CARTESIAN_POINT('Ctrl Pts',(-0.00291286656667483,46.0518804236423,
15.817460744914));
#47259=CARTESIAN_POINT('Ctrl Pts',(-0.453161161170635,46.1023490630304,
15.7636226737825));
#47260=CARTESIAN_POINT('Ctrl Pts',(-0.607379572154865,46.1197172591066,
15.7302015365156));
#47261=CARTESIAN_POINT('Ctrl Pts',(-1.06786022589398,46.1737629291231,15.5838090281928));
#47262=CARTESIAN_POINT('Ctrl Pts',(-1.35612248569427,46.2101726162091,15.4253567197509));
#47263=CARTESIAN_POINT('Ctrl Pts',(-1.85627153822428,46.2810207370737,15.0061606385636));
#47264=CARTESIAN_POINT('Ctrl Pts',(-2.06311401634006,46.3155215088971,14.7492349693685));
#47265=CARTESIAN_POINT('Ctrl Pts',(-2.35137090934781,46.3830590275481,14.1988172104408));
#47266=CARTESIAN_POINT('Ctrl Pts',(-2.44089286653981,46.4141758958576,13.9156024449375));
#47267=CARTESIAN_POINT('Ctrl Pts',(-2.49299721967078,46.45566800665,13.5160100875658));
#47268=CARTESIAN_POINT('Ctrl Pts',(-2.5,46.4666961661161,13.4080346065628));
#47269=CARTESIAN_POINT('Ctrl Pts',(-2.5,46.4777801864859,13.3));
#47270=CARTESIAN_POINT('Origin',(0.,70.2,13.3));
#47271=CARTESIAN_POINT('',(-2.5,41.4625301506567,13.3));
#47272=CARTESIAN_POINT('',(-2.5,42.3946776132135,13.2999999999965));
#47273=CARTESIAN_POINT('',(-2.5,70.2,13.3));
#47274=CARTESIAN_POINT('',(-2.49999999975899,42.3946815632985,13.2999652863836));
#47275=CARTESIAN_POINT('Ctrl Pts',(-2.5,42.3946776132135,13.2999999999929));
#47276=CARTESIAN_POINT('Ctrl Pts',(-2.5,42.3946793067792,13.2999851168335));
#47277=CARTESIAN_POINT('Ctrl Pts',(-2.49999999996565,42.3946798697338,13.2999801695507));
#47278=CARTESIAN_POINT('Ctrl Pts',(-2.49999999975899,42.3946815632985,13.2999652863836));
#47279=CARTESIAN_POINT('',(-2.34562647967194,42.4937495273014,12.438593281029));
#47280=CARTESIAN_POINT('Ctrl Pts',(-2.49999999975899,42.3946815632985,13.2999652863836));
#47281=CARTESIAN_POINT('Ctrl Pts',(-2.49999796332142,42.4113700776466,13.1533054315592));
#47282=CARTESIAN_POINT('Ctrl Pts',(-2.48709055897572,42.4279012816079,13.0069169709822));
#47283=CARTESIAN_POINT('Ctrl Pts',(-2.46141993395718,42.4443477685325,12.8624935329413));
#47284=CARTESIAN_POINT('Ctrl Pts',(-2.43572996625103,42.4608066478028,12.7179612725618));
#47285=CARTESIAN_POINT('Ctrl Pts',(-2.39735907207736,42.4771173025678,12.5759685022323));
#47286=CARTESIAN_POINT('Ctrl Pts',(-2.3467496852355,42.4934796045645,12.4381613173876));
#47287=CARTESIAN_POINT('Ctrl Pts',(-2.34568410818789,42.4936477083913,12.4384943467529));
#47288=CARTESIAN_POINT('Ctrl Pts',(-2.32319243510089,42.5044066341044,12.3767211629903));
#47289=CARTESIAN_POINT('Ctrl Pts',(-2.29816641170027,42.5154051459049,12.3160036445523));
#47290=CARTESIAN_POINT('Ctrl Pts',(-2.27084402275472,42.5264576965297,12.2564468004019));
#47291=CARTESIAN_POINT('Ctrl Pts',(-2.26153191904919,42.5302246620698,12.2361484469084));
#47292=CARTESIAN_POINT('Ctrl Pts',(-2.25195285533498,42.5339979531538,12.2159845285737));
#47293=CARTESIAN_POINT('Ctrl Pts',(-2.24211553933993,42.5377703748663,12.1959580269618));
#47294=CARTESIAN_POINT('Ctrl Pts',(-2.20303425107432,42.5527572981777,12.1163975571304));
#47295=CARTESIAN_POINT('Ctrl Pts',(-2.15988069017721,42.5677305682467,12.039004668424));
#47296=CARTESIAN_POINT('Ctrl Pts',(-2.11284707137413,42.5826925682951,11.9641262426941));
#47297=CARTESIAN_POINT('Ctrl Pts',(-2.06625695767561,42.5975134836564,11.8899538856205));
#47298=CARTESIAN_POINT('Ctrl Pts',(-2.01585996950672,42.6123230568688,11.8182484823373));
#47299=CARTESIAN_POINT('Ctrl Pts',(-1.96181183979858,42.6270945088235,11.7493389656302));
#47300=CARTESIAN_POINT('Ctrl Pts',(-1.91893037685003,42.6388140904837,11.6946665670952));
#47301=CARTESIAN_POINT('Ctrl Pts',(-1.87375012255244,42.650509046783,11.641753753135));
#47302=CARTESIAN_POINT('Ctrl Pts',(-1.826332024504,42.6621547426356,11.5907643122431));
#47303=CARTESIAN_POINT('Ctrl Pts',(-1.77150630319007,42.6756197212323,11.5318093353177));
#47304=CARTESIAN_POINT('Ctrl Pts',(-1.71395546762424,42.6889535887934,11.4757108190844));
#47305=CARTESIAN_POINT('Ctrl Pts',(-1.65382295290227,42.7021077324741,11.4226417084105));
#47306=CARTESIAN_POINT('Ctrl Pts',(-1.64790473396646,42.7034023582281,11.4174186669803));
#47307=CARTESIAN_POINT('Ctrl Pts',(-1.64196146632311,42.7046952453212,11.4122249735563));
#47308=CARTESIAN_POINT('Ctrl Pts',(-1.63599325951888,42.7059863488698,11.4070607964659));
#47309=CARTESIAN_POINT('Ctrl Pts',(-1.60759618180394,42.7121294952131,11.3824893392459));
#47310=CARTESIAN_POINT('Ctrl Pts',(-1.578634839558,42.7182320534431,11.3585859512818));
#47311=CARTESIAN_POINT('Ctrl Pts',(-1.54912007543092,42.7242885560419,11.3353687778235));
#47312=CARTESIAN_POINT('Ctrl Pts',(-1.54906789469659,42.7242992636576,11.3353277309375));
#47313=CARTESIAN_POINT('Ctrl Pts',(-1.54901571223328,42.7243099711298,11.3352866861985));
#47314=CARTESIAN_POINT('Ctrl Pts',(-1.54896352804101,42.7243206784584,11.3352456436066));
#47315=CARTESIAN_POINT('Ctrl Pts',(-1.4852389421749,42.7373959040039,11.2851265931339));
#47316=CARTESIAN_POINT('Ctrl Pts',(-1.41893687593455,42.7502574375949,11.2382051472508));
#47317=CARTESIAN_POINT('Ctrl Pts',(-1.35033349917278,42.7630133468244,11.1945851413839));
#47318=CARTESIAN_POINT('Ctrl Pts',(-1.34666103087231,42.7636961947322,11.1922500801031));
#47319=CARTESIAN_POINT('Ctrl Pts',(-1.34298196643404,42.764378739025,11.1899244918653));
#47320=CARTESIAN_POINT('Ctrl Pts',(-1.33929634791449,42.7650609959637,11.1876083967253));
#47321=CARTESIAN_POINT('Ctrl Pts',(-1.26884491142833,42.7781024925612,11.1433357112092));
#47322=CARTESIAN_POINT('Ctrl Pts',(-1.19599798804975,42.7910398549919,11.10252762203));
#47323=CARTESIAN_POINT('Ctrl Pts',(-1.12105332117687,42.8039678222148,11.06533510557));
#47324=CARTESIAN_POINT('Ctrl Pts',(-1.11678133648451,42.8047047402689,11.0632150633092));
#47325=CARTESIAN_POINT('Ctrl Pts',(-1.11250253714567,42.805441626814,11.0611067827626));
#47326=CARTESIAN_POINT('Ctrl Pts',(-1.10821697898267,42.8061784990389,11.0590102969284));
#47327=CARTESIAN_POINT('Ctrl Pts',(-1.07812049158259,42.8113533828664,11.0442871600362));
#47328=CARTESIAN_POINT('Ctrl Pts',(-1.04769071115196,42.8165273203326,11.0301453979786));
#47329=CARTESIAN_POINT('Ctrl Pts',(-1.01694738227775,42.8217052392388,11.0165962399779));
#47330=CARTESIAN_POINT('Ctrl Pts',(-0.93670336909343,42.8352202686189,10.9812312078537));
#47331=CARTESIAN_POINT('Ctrl Pts',(-0.854743063674407,42.8486949837781,
10.9500878614058));
#47332=CARTESIAN_POINT('Ctrl Pts',(-0.771477953212197,42.8621921408794,
10.9232487200998));
#47333=CARTESIAN_POINT('Ctrl Pts',(-0.686960198914593,42.8758923497817,
10.8960058096193));
#47334=CARTESIAN_POINT('Ctrl Pts',(-0.601098315861208,42.889615710475,10.8731980714603));
#47335=CARTESIAN_POINT('Ctrl Pts',(-0.51431293246352,42.9033902912299,10.8549208363218));
#47336=CARTESIAN_POINT('Ctrl Pts',(-0.427674693022967,42.917141517288,10.8366745900964));
#47337=CARTESIAN_POINT('Ctrl Pts',(-0.340116556399769,42.9309436015435,
10.8229435031144));
#47338=CARTESIAN_POINT('Ctrl Pts',(-0.25204183770853,42.9447886797666,10.8138274198997));
#47339=CARTESIAN_POINT('Ctrl Pts',(-0.182662170169835,42.9556949527408,
10.8066463487354));
#47340=CARTESIAN_POINT('Ctrl Pts',(-0.112961714143479,42.9666271453375,
10.8023289442864));
#47341=CARTESIAN_POINT('Ctrl Pts',(-0.0431280667894809,42.9775671581277,
10.8009278439028));
#47342=CARTESIAN_POINT('Ctrl Pts',(0.0381176356362617,42.9902949628087,
10.7992977788962));
#47343=CARTESIAN_POINT('Ctrl Pts',(0.119146921010516,43.0029718850833,10.8016226020268));
#47344=CARTESIAN_POINT('Ctrl Pts',(0.199692924382387,43.0155519372969,10.8078810650787));
#47345=CARTESIAN_POINT('Ctrl Pts',(0.207357072027646,43.0167489597873,10.8084765730227));
#47346=CARTESIAN_POINT('Ctrl Pts',(0.215016870767598,43.017945107523,10.8091077243278));
#47347=CARTESIAN_POINT('Ctrl Pts',(0.222672106946552,43.0191403423437,10.8097745190492));
#47348=CARTESIAN_POINT('Ctrl Pts',(0.300986738960001,43.0313678390491,10.8165959654443));
#47349=CARTESIAN_POINT('Ctrl Pts',(0.378821715553078,43.0434991211718,10.827143874682));
#47350=CARTESIAN_POINT('Ctrl Pts',(0.455967538276286,43.0554802484494,10.8414244650109));
#47351=CARTESIAN_POINT('Ctrl Pts',(0.46504699424431,43.056890332803,10.843105178062));
#47352=CARTESIAN_POINT('Ctrl Pts',(0.474116936893891,43.0582983414146,10.8448376437622));
#47353=CARTESIAN_POINT('Ctrl Pts',(0.483177049511238,43.0597041896624,10.8466219132699));
#47354=CARTESIAN_POINT('Ctrl Pts',(0.499926919556773,43.0623032495691,10.8499205789316));
#47355=CARTESIAN_POINT('Ctrl Pts',(0.516643191327323,43.0648948743572,10.8533962415694));
#47356=CARTESIAN_POINT('Ctrl Pts',(0.533323908054583,43.0674784687919,10.8570492350127));
#47357=CARTESIAN_POINT('Ctrl Pts',(0.533345151962504,43.0674817591566,10.8570538873222));
#47358=CARTESIAN_POINT('Ctrl Pts',(0.53336639581264,43.0674850495084,10.8570585399193));
#47359=CARTESIAN_POINT('Ctrl Pts',(0.53338763960503,43.0674883398472,10.8570631928042));
#47360=CARTESIAN_POINT('Ctrl Pts',(0.610680985342629,43.0794598978972,10.8739922339886));
#47361=CARTESIAN_POINT('Ctrl Pts',(0.687212959521698,43.0912600067255,10.8947268596381));
#47362=CARTESIAN_POINT('Ctrl Pts',(0.762760064942518,43.1029827530012,10.9191678164538));
#47363=CARTESIAN_POINT('Ctrl Pts',(0.770392154344625,43.1041670346109,10.9216369457004));
#47364=CARTESIAN_POINT('Ctrl Pts',(0.778014157187172,43.1053505232405,10.9241439273632));
#47365=CARTESIAN_POINT('Ctrl Pts',(0.785625818862137,43.1065333135789,10.9266886756104));
#47366=CARTESIAN_POINT('Ctrl Pts',(0.834861599878281,43.1141841536418,10.9431492952216));
#47367=CARTESIAN_POINT('Ctrl Pts',(0.88366555061725,43.121805651543,10.9611895958705));
#47368=CARTESIAN_POINT('Ctrl Pts',(0.931966035147949,43.1294206320113,10.9807864459211));
#47369=CARTESIAN_POINT('Ctrl Pts',(1.01245564838017,43.1421105012459,11.0134433208255));
#47370=CARTESIAN_POINT('Ctrl Pts',(1.09113085014283,43.1547180044794,11.0502524528365));
#47371=CARTESIAN_POINT('Ctrl Pts',(1.16768393250191,43.1673282101208,11.0909858831448));
#47372=CARTESIAN_POINT('Ctrl Pts',(1.24565870789114,43.1801726041309,11.1324757876822));
#47373=CARTESIAN_POINT('Ctrl Pts',(1.32143121951073,43.1930199757638,11.1780377923875));
#47374=CARTESIAN_POINT('Ctrl Pts',(1.39465893046395,43.2059273251432,11.2274383518593));
#47375=CARTESIAN_POINT('Ctrl Pts',(1.46841068418584,43.2189270439687,11.2771924387816));
#47376=CARTESIAN_POINT('Ctrl Pts',(1.53958036669501,43.2319875908329,11.3308403079002));
#47377=CARTESIAN_POINT('Ctrl Pts',(1.60781086821449,43.245132980258,11.3881447146781));
#47378=CARTESIAN_POINT('Ctrl Pts',(1.66135999036038,43.2554498334,11.4331187454959));
#47379=CARTESIAN_POINT('Ctrl Pts',(1.7130985314609,43.2658182261341,11.4803449079438));
#47380=CARTESIAN_POINT('Ctrl Pts',(1.76285458740213,43.2762356050361,11.5297102091189));
#47381=CARTESIAN_POINT('Ctrl Pts',(1.82624126810301,43.2895068150972,11.5925990881528));
#47382=CARTESIAN_POINT('Ctrl Pts',(1.88607272173309,43.302787518306,11.6586233216415));
#47383=CARTESIAN_POINT('Ctrl Pts',(1.94211797655693,43.3160456689778,11.7274674702159));
#47384=CARTESIAN_POINT('Ctrl Pts',(1.99379031998758,43.3282693570835,11.7909400781915));
#47385=CARTESIAN_POINT('Ctrl Pts',(2.04224493801208,43.3404734842481,11.8568096895573));
#47386=CARTESIAN_POINT('Ctrl Pts',(2.08731732559338,43.3526168843612,11.9248659069953));
#47387=CARTESIAN_POINT('Ctrl Pts',(2.09085119221849,43.3535689785074,11.9302018035019));
#47388=CARTESIAN_POINT('Ctrl Pts',(2.0943642622003,43.3545207011585,11.9355511675448));
#47389=CARTESIAN_POINT('Ctrl Pts',(2.09785645310077,43.355472033399,11.9409139109309));
#47390=CARTESIAN_POINT('Ctrl Pts',(2.14079863407173,43.367170214397,12.0068575845583));
#47391=CARTESIAN_POINT('Ctrl Pts',(2.18058568411325,43.3788086512971,12.0748201437439));
#47392=CARTESIAN_POINT('Ctrl Pts',(2.21707146100581,43.3903416718601,12.1446554705317));
#47393=CARTESIAN_POINT('Ctrl Pts',(2.22000048808778,43.3912675266025,12.1502617527836));
#47394=CARTESIAN_POINT('Ctrl Pts',(2.22290822948716,43.3921927040942,12.1558801303465));
#47395=CARTESIAN_POINT('Ctrl Pts',(2.22579460380645,43.3931171818214,12.1615105412205));
#47396=CARTESIAN_POINT('Ctrl Pts',(2.2257964153244,43.393117762033,12.1615140749237));
#47397=CARTESIAN_POINT('Ctrl Pts',(2.22579822683392,43.3931183422444,12.1615176086317));
#47398=CARTESIAN_POINT('Ctrl Pts',(2.22580003833503,43.3931189224555,12.1615211423445));
#47399=CARTESIAN_POINT('Ctrl Pts',(2.25801117034599,43.4034359219842,12.2243557090336));
#47400=CARTESIAN_POINT('Ctrl Pts',(2.28756377580288,43.4136658527735,12.2886892862194));
#47401=CARTESIAN_POINT('Ctrl Pts',(2.31437366623366,43.4238602643772,12.3543583619918));
#47402=CARTESIAN_POINT('Ctrl Pts',(2.346991566351,43.4362631609986,12.4342537781954));
#47403=CARTESIAN_POINT('Ctrl Pts',(2.37538129216963,43.4485510705151,12.5157145710211));
#47404=CARTESIAN_POINT('Ctrl Pts',(2.39948963992353,43.4607964735314,12.5983792902655));
#47405=CARTESIAN_POINT('Ctrl Pts',(2.42403098143446,43.4732618079637,12.6825286947204));
#47406=CARTESIAN_POINT('Ctrl Pts',(2.44413497407805,43.4856831727977,12.7679255998961));
#47407=CARTESIAN_POINT('Ctrl Pts',(2.459729330354,43.4981074995305,12.8541844160181));
#47408=CARTESIAN_POINT('Ctrl Pts',(2.47544197671866,43.5106260702761,12.9410975434068));
#47409=CARTESIAN_POINT('Ctrl Pts',(2.48657593222927,43.523147559786,13.028885236833));
#47410=CARTESIAN_POINT('Ctrl Pts',(2.49305021988218,43.5356904189153,13.117152922644));
#47411=CARTESIAN_POINT('Ctrl Pts',(2.49560756544813,43.5406448520357,13.1520186850302));
#47412=CARTESIAN_POINT('Ctrl Pts',(2.49743783559164,43.5456023050079,13.1869593782955));
#47413=CARTESIAN_POINT('Ctrl Pts',(2.49853582421476,43.5505627268715,13.2219509696579));
#47414=CARTESIAN_POINT('Ctrl Pts',(2.49853638756189,43.5505652719246,13.2219689228608));
#47415=CARTESIAN_POINT('Ctrl Pts',(2.49853695071622,43.5505678169786,13.221986876077));
#47416=CARTESIAN_POINT('Ctrl Pts',(2.49853751367776,43.5505703620333,13.2220048293067));
#47417=CARTESIAN_POINT('Ctrl Pts',(2.49967622144808,43.555718268927,13.2583190012753));
#47418=CARTESIAN_POINT('Ctrl Pts',(2.50002624606076,43.5608693880851,13.2946880561884));
#47419=CARTESIAN_POINT('Ctrl Pts',(2.49958353970284,43.5660259951698,13.3310838093336));
#47420=CARTESIAN_POINT('Ctrl Pts',(2.49850970026858,43.5785339881895,13.4193662436561));
#47421=CARTESIAN_POINT('Ctrl Pts',(2.49277750870894,43.5910106166133,13.5073402163106));
#47422=CARTESIAN_POINT('Ctrl Pts',(2.4824727741004,43.603468467095,13.5946136719723));
#47423=CARTESIAN_POINT('Ctrl Pts',(2.47210445202433,43.6160031912849,13.6824256662998));
#47424=CARTESIAN_POINT('Ctrl Pts',(2.45710753280093,43.6285186011674,13.7695279489814));
#47425=CARTESIAN_POINT('Ctrl Pts',(2.43756057094178,43.6410022854227,13.8555491732612));
#47426=CARTESIAN_POINT('Ctrl Pts',(2.41934319006255,43.6526368316245,13.9357192486773));
#47427=CARTESIAN_POINT('Ctrl Pts',(2.39717411513907,43.6642434867231,14.0149504283669));
#47428=CARTESIAN_POINT('Ctrl Pts',(2.37110114656571,43.6757960912124,14.0929682274303));
#47429=CARTESIAN_POINT('Ctrl Pts',(2.36957346353064,43.6764729883535,14.0975394931735));
#47430=CARTESIAN_POINT('Ctrl Pts',(2.36803236379235,43.6771497009232,14.1021065974979));
#47431=CARTESIAN_POINT('Ctrl Pts',(2.3664778515487,43.67782622403,14.1066694866157));
#47432=CARTESIAN_POINT('Ctrl Pts',(2.3445325218236,43.6873768227509,14.1710846152822));
#47433=CARTESIAN_POINT('Ctrl Pts',(2.31991723310749,43.696888999328,14.2346595029851));
#47434=CARTESIAN_POINT('Ctrl Pts',(2.2926420156784,43.7063422882946,14.2972517365443));
#47435=CARTESIAN_POINT('Ctrl Pts',(2.2926368945365,43.7063440632258,14.2972634887406));
#47436=CARTESIAN_POINT('Ctrl Pts',(2.29263177330077,43.7063458381549,14.2972752409023));
#47437=CARTESIAN_POINT('Ctrl Pts',(2.29262665197122,43.706347613082,14.2972869930294));
#47438=CARTESIAN_POINT('Ctrl Pts',(2.29200670382658,43.7065624718801,14.2987096137206));
#47439=CARTESIAN_POINT('Ctrl Pts',(2.29138538081122,43.7067773000871,14.3001317271333));
#47440=CARTESIAN_POINT('Ctrl Pts',(2.2907626834559,43.70699209831,14.3015533316609));
#47441=CARTESIAN_POINT('Ctrl Pts',(2.25906768334438,43.7179252260014,14.3739123280138));
#47442=CARTESIAN_POINT('Ctrl Pts',(2.2239627150649,43.7287303647691,14.4446137883274));
#47443=CARTESIAN_POINT('Ctrl Pts',(2.18561078838783,43.739482210611,14.5134705831952));
#47444=CARTESIAN_POINT('Ctrl Pts',(2.18234908166992,43.7403966201557,14.5193266298102));
#47445=CARTESIAN_POINT('Ctrl Pts',(2.17906387504082,43.7413106412124,14.5251693069775));
#47446=CARTESIAN_POINT('Ctrl Pts',(2.17575526116822,43.7422243180421,14.5309984843913));
#47447=CARTESIAN_POINT('Ctrl Pts',(2.13482840560831,43.7535263076608,14.6031041791731));
#47448=CARTESIAN_POINT('Ctrl Pts',(2.09032113816982,43.7647763544049,14.6731479851909));
#47449=CARTESIAN_POINT('Ctrl Pts',(2.04242125552808,43.7760397844312,14.7408738036126));
#47450=CARTESIAN_POINT('Ctrl Pts',(2.03981864874256,43.7766517750624,14.7445536388201));
#47451=CARTESIAN_POINT('Ctrl Pts',(2.03720602191432,43.7772638040268,14.7482266188967));
#47452=CARTESIAN_POINT('Ctrl Pts',(2.03458340383749,43.7778758813964,14.7518926986234));
#47453=CARTESIAN_POINT('Ctrl Pts',(1.98281974934335,43.7899566955126,14.8242515700877));
#47454=CARTESIAN_POINT('Ctrl Pts',(1.92716488177324,43.8020570141243,14.8939263283273));
#47455=CARTESIAN_POINT('Ctrl Pts',(1.86786532911653,43.8142284487568,14.9605698698303));
#47456=CARTESIAN_POINT('Ctrl Pts',(1.81861304804456,43.8243376467644,15.0159218293423));
#47457=CARTESIAN_POINT('Ctrl Pts',(1.7668468882253,43.8344953552915,15.0691818697345));
#47458=CARTESIAN_POINT('Ctrl Pts',(1.71271910845011,43.8447159041991,15.1201448262752));
#47459=CARTESIAN_POINT('Ctrl Pts',(1.64769299153216,43.8569943056224,15.1813688998334));
#47460=CARTESIAN_POINT('Ctrl Pts',(1.5796070055678,43.8692984228793,15.2389495971852));
#47461=CARTESIAN_POINT('Ctrl Pts',(1.50882929121771,43.8816268677423,15.2926564756774));
#47462=CARTESIAN_POINT('Ctrl Pts',(1.4377895602789,43.8940009520711,15.3465621751292));
#47463=CARTESIAN_POINT('Ctrl Pts',(1.36403937126748,43.906399135297,15.3965654700129));
#47464=CARTESIAN_POINT('Ctrl Pts',(1.28792448754835,43.9187985854612,15.4424636499677));
#47465=CARTESIAN_POINT('Ctrl Pts',(1.21837472863129,43.9301285478482,15.4844029816018));
#47466=CARTESIAN_POINT('Ctrl Pts',(1.14685089075896,43.9414592226689,15.522915452623));
#47467=CARTESIAN_POINT('Ctrl Pts',(1.07358427247098,43.9527617434253,15.5578634725687));
#47468=CARTESIAN_POINT('Ctrl Pts',(1.06805073755035,43.9536153776554,15.56050295687));
#47469=CARTESIAN_POINT('Ctrl Pts',(1.06250723822261,43.9544688533448,15.5631221008957));
#47470=CARTESIAN_POINT('Ctrl Pts',(1.05695386278732,43.955322159067,15.5657208410323));
#47471=CARTESIAN_POINT('Ctrl Pts',(0.994491935694773,43.9649197669421,15.5949503283653));
#47472=CARTESIAN_POINT('Ctrl Pts',(0.930783327332353,43.9744952258414,15.6216005644104));
#47473=CARTESIAN_POINT('Ctrl Pts',(0.865943140492572,43.9840274102256,15.6455878229252));
#47474=CARTESIAN_POINT('Ctrl Pts',(0.806103392321384,43.9928244779219,15.6677251975812));
#47475=CARTESIAN_POINT('Ctrl Pts',(0.745528272931709,44.001550983782,15.6875102987326));
#47476=CARTESIAN_POINT('Ctrl Pts',(0.684304520976044,44.0101912848952,15.7049249939626));
#47477=CARTESIAN_POINT('Ctrl Pts',(0.684249582127082,44.0101990382292,15.7049406209583));
#47478=CARTESIAN_POINT('Ctrl Pts',(0.684194642754202,44.0102067914943,15.7049562460436));
#47479=CARTESIAN_POINT('Ctrl Pts',(0.684139702857418,44.0102145446905,15.7049718692182));
#47480=CARTESIAN_POINT('Ctrl Pts',(0.612191421570442,44.0203679882298,15.7254316922686));
#47481=CARTESIAN_POINT('Ctrl Pts',(0.539342580598442,44.03040372576,15.7426187073691));
#47482=CARTESIAN_POINT('Ctrl Pts',(0.465792504227374,44.0403870832344,15.7565067758889));
#47483=CARTESIAN_POINT('Ctrl Pts',(0.455193062131454,44.0418258039631,15.7585082119902));
#47484=CARTESIAN_POINT('Ctrl Pts',(0.444579102294771,44.0432634277579,15.7604410598144));
#47485=CARTESIAN_POINT('Ctrl Pts',(0.433951270121274,44.044700140944,15.7623051681519));
#47486=CARTESIAN_POINT('Ctrl Pts',(0.356602895948348,44.0551564058984,15.7758719752706));
#47487=CARTESIAN_POINT('Ctrl Pts',(0.278516886314291,44.0655652642482,15.7858001471926));
#47488=CARTESIAN_POINT('Ctrl Pts',(0.19996358876216,44.0759832197129,15.7920378279043));
#47489=CARTESIAN_POINT('Ctrl Pts',(0.186903219592773,44.0777153219747,15.7930749124748));
#47490=CARTESIAN_POINT('Ctrl Pts',(0.173830010431977,44.0794476642253,15.7940098946058));
#47491=CARTESIAN_POINT('Ctrl Pts',(0.160745300561244,44.0811804923826,15.7948424364924));
#47492=CARTESIAN_POINT('Ctrl Pts',(0.0773994813251622,44.0922181068039,
15.8001454876317));
#47493=CARTESIAN_POINT('Ctrl Pts',(-0.00641597124643042,44.1032760357438,
15.8012945090207));
#47494=CARTESIAN_POINT('Ctrl Pts',(-0.0903323110069834,44.1143968109666,
15.7982274792389));
#47495=CARTESIAN_POINT('Ctrl Pts',(-0.0988286635242062,44.1155227660169,
15.7979169489384));
#47496=CARTESIAN_POINT('Ctrl Pts',(-0.107326017400065,44.1166493617228,
15.7975631700255));
#47497=CARTESIAN_POINT('Ctrl Pts',(-0.115823966859831,44.1177766397923,
15.797166059037));
#47498=CARTESIAN_POINT('Ctrl Pts',(-0.204584845519198,44.1295510322401,
15.7930182442686));
#47499=CARTESIAN_POINT('Ctrl Pts',(-0.292943942210145,44.1413382533506,
15.7841678945119));
#47500=CARTESIAN_POINT('Ctrl Pts',(-0.380449539413418,44.1531590749493,
15.770710573128));
#47501=CARTESIAN_POINT('Ctrl Pts',(-0.468800318782251,44.165094069217,15.7571232727669));
#47502=CARTESIAN_POINT('Ctrl Pts',(-0.556279560261329,44.1770629824426,
15.7388399646226));
#47503=CARTESIAN_POINT('Ctrl Pts',(-0.642444892911005,44.189062777786,15.7159833031921));
#47504=CARTESIAN_POINT('Ctrl Pts',(-0.727700913903991,44.2009359380496,
15.6933678504709));
#47505=CARTESIAN_POINT('Ctrl Pts',(-0.811669692603273,44.2128388856667,
15.6662763592815));
#47506=CARTESIAN_POINT('Ctrl Pts',(-0.893962707722052,44.2247508796413,
15.6348383833099));
#47507=CARTESIAN_POINT('Ctrl Pts',(-0.956576084841162,44.2338142268754,
15.6109185179054));
#47508=CARTESIAN_POINT('Ctrl Pts',(-1.01822021388613,44.242882402068,15.5844829630128));
#47509=CARTESIAN_POINT('Ctrl Pts',(-1.07874311180981,44.2519416693289,15.5555843741965));
#47510=CARTESIAN_POINT('Ctrl Pts',(-1.14496652126029,44.2618542079831,15.5239638942563));
#47511=CARTESIAN_POINT('Ctrl Pts',(-1.20955741377997,44.2717127862346,15.4895336024582));
#47512=CARTESIAN_POINT('Ctrl Pts',(-1.27238454152044,44.2814976143977,15.4524181007049));
#47513=CARTESIAN_POINT('Ctrl Pts',(-1.28569633879536,44.2835708215227,15.4445540767894));
#47514=CARTESIAN_POINT('Ctrl Pts',(-1.29892904457969,44.2856407336629,15.4365693429927));
#47515=CARTESIAN_POINT('Ctrl Pts',(-1.3120815432013,44.2877071882353,15.4284648153511));
#47516=CARTESIAN_POINT('Ctrl Pts',(-1.35081614496656,44.2937929744598,15.4045966774614));
#47517=CARTESIAN_POINT('Ctrl Pts',(-1.38885518000683,44.299848553427,15.3796905867644));
#47518=CARTESIAN_POINT('Ctrl Pts',(-1.42617359642233,44.3058694449266,15.3537669118777));
#47519=CARTESIAN_POINT('Ctrl Pts',(-1.42626314939669,44.3058838932552,15.3537047028556));
#47520=CARTESIAN_POINT('Ctrl Pts',(-1.42635269822065,44.3058983413847,15.3536424879691));
#47521=CARTESIAN_POINT('Ctrl Pts',(-1.42644224289338,44.3059127893153,15.3535802672179));
#47522=CARTESIAN_POINT('Ctrl Pts',(-1.48664804685902,44.3156269269582,15.3117458371601));
#47523=CARTESIAN_POINT('Ctrl Pts',(-1.5449815724511,44.3252515595638,15.2672608493679));
#47524=CARTESIAN_POINT('Ctrl Pts',(-1.60132034593166,44.3348359188048,15.2202238907525));
#47525=CARTESIAN_POINT('Ctrl Pts',(-1.61100448833462,44.3364833863302,15.2121386489679));
#47526=CARTESIAN_POINT('Ctrl Pts',(-1.62062956923397,44.3381296519929,15.2039779924162));
#47527=CARTESIAN_POINT('Ctrl Pts',(-1.63019481385692,44.3397749509719,15.1957424125318));
#47528=CARTESIAN_POINT('Ctrl Pts',(-1.68776433825106,44.3496773720222,15.1461756282264));
#47529=CARTESIAN_POINT('Ctrl Pts',(-1.74317011067206,44.3595453660952,15.0938940531257));
#47530=CARTESIAN_POINT('Ctrl Pts',(-1.79622626396811,44.3694216474947,15.039020570549));
#47531=CARTESIAN_POINT('Ctrl Pts',(-1.80469338301604,44.3709977823097,15.0302634277731));
#47532=CARTESIAN_POINT('Ctrl Pts',(-1.8131005545515,44.3725741181431,15.0214402852565));
#47533=CARTESIAN_POINT('Ctrl Pts',(-1.8214469022326,44.3741508171333,15.0125516606569));
#47534=CARTESIAN_POINT('Ctrl Pts',(-1.836280361967,44.3769529890388,14.996754444901));
#47535=CARTESIAN_POINT('Ctrl Pts',(-1.85092185963658,44.3797562606112,14.9807505146924));
#47536=CARTESIAN_POINT('Ctrl Pts',(-1.86536652856784,44.3825614203959,14.9645430656605));
#47537=CARTESIAN_POINT('Ctrl Pts',(-1.92371379910021,44.393892480846,14.899075285277));
#47538=CARTESIAN_POINT('Ctrl Pts',(-1.97854811218913,44.405197219464,14.8306240014923));
#47539=CARTESIAN_POINT('Ctrl Pts',(-2.0296405263341,44.4165150690176,14.7595164795904));
#47540=CARTESIAN_POINT('Ctrl Pts',(-2.081506579579,44.4280042929539,14.6873322507025));
#47541=CARTESIAN_POINT('Ctrl Pts',(-2.12951514617069,44.4395068705651,14.612411143145));
#47542=CARTESIAN_POINT('Ctrl Pts',(-2.17342850391493,44.4510446190335,14.5351199866075));
#47543=CARTESIAN_POINT('Ctrl Pts',(-2.21738895172838,44.4625947398961,14.4577459476376));
#47544=CARTESIAN_POINT('Ctrl Pts',(-2.2572446314795,44.4741798323454,14.377997877658));
#47545=CARTESIAN_POINT('Ctrl Pts',(-2.29277556231768,44.4858057950063,14.2962564099619));
#47546=CARTESIAN_POINT('Ctrl Pts',(-2.31886668641432,44.494342988583,14.236231898158));
#47547=CARTESIAN_POINT('Ctrl Pts',(-2.34262629986971,44.5029018614689,14.1751328954114));
#47548=CARTESIAN_POINT('Ctrl Pts',(-2.36397569414679,44.5114807594104,14.1131078193728));
#47549=CARTESIAN_POINT('Ctrl Pts',(-2.39010827060216,44.5219816993176,14.037186459699));
#47550=CARTESIAN_POINT('Ctrl Pts',(-2.41250514705558,44.5324630052681,13.960239143359));
#47551=CARTESIAN_POINT('Ctrl Pts',(-2.43114099486024,44.5429171624905,13.8825489827748));
#47552=CARTESIAN_POINT('Ctrl Pts',(-2.43324911742662,44.544099756649,13.8737605239706));
#47553=CARTESIAN_POINT('Ctrl Pts',(-2.43530909415252,44.5452820075015,13.8649625075572));
#47554=CARTESIAN_POINT('Ctrl Pts',(-2.43732087366301,44.5464639073091,13.8561553043701));
#47555=CARTESIAN_POINT('Ctrl Pts',(-2.45444088241008,44.5565217366781,13.7812070335404));
#47556=CARTESIAN_POINT('Ctrl Pts',(-2.46807305677235,44.5665536359262,13.705597453051));
#47557=CARTESIAN_POINT('Ctrl Pts',(-2.47819858923538,44.5765524043719,13.6295333731716));
#47558=CARTESIAN_POINT('Ctrl Pts',(-2.47972970810502,44.5780643547899,13.6180314449095));
#47559=CARTESIAN_POINT('Ctrl Pts',(-2.48118060018608,44.5795755559865,13.6065190388408));
#47560=CARTESIAN_POINT('Ctrl Pts',(-2.48255114815379,44.5810859919839,13.5949967802098));
#47561=CARTESIAN_POINT('Ctrl Pts',(-2.48626354567838,44.5851773036271,13.5637864866433));
#47562=CARTESIAN_POINT('Ctrl Pts',(-2.48938680535883,44.589262937982,13.5325040260609));
#47563=CARTESIAN_POINT('Ctrl Pts',(-2.49191879076888,44.5933425241649,13.5011609896512));
#47564=CARTESIAN_POINT('Ctrl Pts',(-2.4919202673538,44.5933449032685,13.5011427112462));
#47565=CARTESIAN_POINT('Ctrl Pts',(-2.49192174373751,44.5933472823699,13.5011244328207));
#47566=CARTESIAN_POINT('Ctrl Pts',(-2.49192321992002,44.5933496614694,13.5011061543745));
#47567=CARTESIAN_POINT('Ctrl Pts',(-2.49732230562144,44.6020511341444,13.434253379173));
#47568=CARTESIAN_POINT('Ctrl Pts',(-2.50003180211327,44.6107255757689,13.36712281549));
#47569=CARTESIAN_POINT('Ctrl Pts',(-2.50002611214299,44.6193946092241,13.2998651846547));
#47570=CARTESIAN_POINT('Ctrl Pts',(-2.5,43.4016964318853,13.3));
#47571=CARTESIAN_POINT('Ctrl Pts',(-2.5,43.3852617716781,13.4270421871792));
#47572=CARTESIAN_POINT('Ctrl Pts',(-2.49031634926891,43.368834406787,13.5541860796652));
#47573=CARTESIAN_POINT('Ctrl Pts',(-2.4462108798017,43.3313307762581,13.8407368121712));
#47574=CARTESIAN_POINT('Ctrl Pts',(-2.40595538844556,43.3103489662895,13.9983720971123));
#47575=CARTESIAN_POINT('Ctrl Pts',(-2.29609289339089,43.2686567057597,14.3018471431555));
#47576=CARTESIAN_POINT('Ctrl Pts',(-2.22708344547497,43.2481001380742,14.4471026079539));
#47577=CARTESIAN_POINT('Ctrl Pts',(-1.98107654260903,43.1866566466313,14.8577616816271));
#47578=CARTESIAN_POINT('Ctrl Pts',(-1.76688211021228,43.146034744725,15.0970604390272));
#47579=CARTESIAN_POINT('Ctrl Pts',(-1.38192588260007,43.0841941276021,15.389889404462));
#47580=CARTESIAN_POINT('Ctrl Pts',(-1.24066763196097,43.063137545343,15.4767184333445));
#47581=CARTESIAN_POINT('Ctrl Pts',(-0.809252614246744,43.0019770630349,
15.6861705819616));
#47582=CARTESIAN_POINT('Ctrl Pts',(-0.503271371124684,42.9623486760914,
15.7688942205564));
#47583=CARTESIAN_POINT('Ctrl Pts',(0.130316300639296,42.881860589194,15.8171817823848));
#47584=CARTESIAN_POINT('Ctrl Pts',(0.452347003458223,42.8415374579058,15.7796331097567));
#47585=CARTESIAN_POINT('Ctrl Pts',(1.07677407195124,42.7588523199414,15.5808241331816));
#47586=CARTESIAN_POINT('Ctrl Pts',(1.3715928254352,42.7173390934895,15.4166850306452));
#47587=CARTESIAN_POINT('Ctrl Pts',(1.87923963864281,42.6335652038256,14.9822738126762));
#47588=CARTESIAN_POINT('Ctrl Pts',(2.08696858621688,42.5922263089786,14.716393108069));
#47589=CARTESIAN_POINT('Ctrl Pts',(2.30808784746728,42.5305927477067,14.2739169922799));
#47590=CARTESIAN_POINT('Ctrl Pts',(2.3658637645178,42.5106600890778,14.1236955877563));
#47591=CARTESIAN_POINT('Ctrl Pts',(2.4972689708802,42.4496258159417,13.6505319233069));
#47592=CARTESIAN_POINT('Ctrl Pts',(2.52169285474868,42.4090602178902,13.3176772921114));
#47593=CARTESIAN_POINT('Ctrl Pts',(2.43922334176455,42.3270557602614,12.6583659515808));
#47594=CARTESIAN_POINT('Ctrl Pts',(2.33180699975093,42.2862597604716,12.3386462133287));
#47595=CARTESIAN_POINT('Ctrl Pts',(2.08504868622191,42.2257498641914,11.9114877736278));
#47596=CARTESIAN_POINT('Ctrl Pts',(1.9923246159707,42.2063050422175,11.7814351912134));
#47597=CARTESIAN_POINT('Ctrl Pts',(1.66953336889731,42.1460936517606,11.4096126348075));
#47598=CARTESIAN_POINT('Ctrl Pts',(1.40313558136579,42.1057789244256,11.2042557730935));
#47599=CARTESIAN_POINT('Ctrl Pts',(0.957230451939393,42.0455123513771,10.9847047047587));
#47600=CARTESIAN_POINT('Ctrl Pts',(0.803366474576863,42.0257016335364,10.9269250852756));
#47601=CARTESIAN_POINT('Ctrl Pts',(0.490212340613467,41.9863894499915,10.8433059540261));
#47602=CARTESIAN_POINT('Ctrl Pts',(0.331845479247272,41.9670348596456,10.8169500191847));
#47603=CARTESIAN_POINT('Ctrl Pts',(0.0153217978071606,41.928800515166,10.7951160967115));
#47604=CARTESIAN_POINT('Ctrl Pts',(-0.142074101189276,41.9100042517287,
10.7991008620169));
#47605=CARTESIAN_POINT('Ctrl Pts',(-0.629403268990953,41.8511612068468,
10.8576190259936));
#47606=CARTESIAN_POINT('Ctrl Pts',(-0.949473633184957,41.8113724229515,
10.9633568070406));
#47607=CARTESIAN_POINT('Ctrl Pts',(-1.5162652735471,41.7338116666724,11.2868898818915));
#47608=CARTESIAN_POINT('Ctrl Pts',(-1.76039885847095,41.6967872741871,11.4964861436722));
#47609=CARTESIAN_POINT('Ctrl Pts',(-2.16616343486832,41.6193772711827,12.0079784770186));
#47610=CARTESIAN_POINT('Ctrl Pts',(-2.31925376322761,41.5793150797788,12.3086842005688));
#47611=CARTESIAN_POINT('Ctrl Pts',(-2.46935912315545,41.5139154476201,12.8488261886895));
#47612=CARTESIAN_POINT('Ctrl Pts',(-2.5,41.4882539293719,13.0740124126314));
#47613=CARTESIAN_POINT('Ctrl Pts',(-2.5,41.4625301506567,13.3));
#47614=CARTESIAN_POINT('Origin',(0.,70.2,13.3));
#47615=CARTESIAN_POINT('',(-2.5,39.6612570972331,13.3));
#47616=CARTESIAN_POINT('',(-2.5,40.3937280662289,13.2999999991311));
#47617=CARTESIAN_POINT('',(-2.5,70.2,13.3));
#47618=CARTESIAN_POINT('Ctrl Pts',(-2.5,40.3937280662289,13.2999999982622));
#47619=CARTESIAN_POINT('Ctrl Pts',(-2.49999999978245,40.4379661198564,12.9870368453108));
#47620=CARTESIAN_POINT('Ctrl Pts',(-2.4412336387843,40.4807379631984,12.6767857341882));
#47621=CARTESIAN_POINT('Ctrl Pts',(-2.22632554663737,40.5630948484494,12.1300634584708));
#47622=CARTESIAN_POINT('Ctrl Pts',(-2.08459119418497,40.6017157099769,11.8929518149928));
#47623=CARTESIAN_POINT('Ctrl Pts',(-1.70481717270669,40.6832438792545,11.4448602899963));
#47624=CARTESIAN_POINT('Ctrl Pts',(-1.4593661341119,40.7257339676381,11.2461567437301));
#47625=CARTESIAN_POINT('Ctrl Pts',(-0.897988983361204,40.8124308533914,
10.9444213644873));
#47626=CARTESIAN_POINT('Ctrl Pts',(-0.585206760151349,40.8548620227273,
10.8479121602653));
#47627=CARTESIAN_POINT('Ctrl Pts',(0.0523483348050161,40.9400703617392,
10.7805569331726));
#47628=CARTESIAN_POINT('Ctrl Pts',(0.37077061627588,40.9823279848828,10.8074510801111));
#47629=CARTESIAN_POINT('Ctrl Pts',(0.932837788469853,41.0612960462026,10.9652248757414));
#47630=CARTESIAN_POINT('Ctrl Pts',(1.17687075883366,41.0972486812662,11.0781972004358));
#47631=CARTESIAN_POINT('Ctrl Pts',(1.53549458939259,41.1540447941993,11.3202010414756));
#47632=CARTESIAN_POINT('Ctrl Pts',(1.66307411447041,41.1753016305061,11.426088176817));
#47633=CARTESIAN_POINT('Ctrl Pts',(1.99958072047131,41.2374130441304,11.7670181048818));
#47634=CARTESIAN_POINT('Ctrl Pts',(2.17594664465665,41.277926458624,12.0297106921224));
#47635=CARTESIAN_POINT('Ctrl Pts',(2.43031359161238,41.3612878253565,12.6253518496065));
#47636=CARTESIAN_POINT('Ctrl Pts',(2.49862527908222,41.4034052564218,12.9557752115897));
#47637=CARTESIAN_POINT('Ctrl Pts',(2.50063792532608,41.4665288918307,13.4523173142111));
#47638=CARTESIAN_POINT('Ctrl Pts',(2.4854606234463,41.487086984546,13.6144541337529));
#47639=CARTESIAN_POINT('Ctrl Pts',(2.42353912827401,41.5283481061993,13.9351374775737));
#47640=CARTESIAN_POINT('Ctrl Pts',(2.37662234536734,41.5489654588928,14.0928509423556));
#47641=CARTESIAN_POINT('Ctrl Pts',(2.19491288165371,41.6093531387659,14.537991146173));
#47642=CARTESIAN_POINT('Ctrl Pts',(2.02061728609311,41.6485874461389,14.805790271673));
#47643=CARTESIAN_POINT('Ctrl Pts',(1.68897440073113,41.7079628689352,15.1502531036789));
#47644=CARTESIAN_POINT('Ctrl Pts',(1.56597429620276,41.7278968398917,15.2554542210286));
#47645=CARTESIAN_POINT('Ctrl Pts',(1.17463083430046,41.7867872521025,15.5294025584051));
#47646=CARTESIAN_POINT('Ctrl Pts',(0.883488052794584,41.825142327897,15.6599732144183));
#47647=CARTESIAN_POINT('Ctrl Pts',(0.418544378133756,41.8833837069086,15.7700017928239));
#47648=CARTESIAN_POINT('Ctrl Pts',(0.25812254959729,41.902963575707,15.7918802302917));
#47649=CARTESIAN_POINT('Ctrl Pts',(-0.22337415050963,41.9612293877349,15.8105196380457));
#47650=CARTESIAN_POINT('Ctrl Pts',(-0.54289773123516,41.9992630877993,15.7612797742278));
#47651=CARTESIAN_POINT('Ctrl Pts',(-1.13728900707918,42.0747361686259,15.5479725788548));
#47652=CARTESIAN_POINT('Ctrl Pts',(-1.40799801326119,42.1112338469496,15.3891135199219));
#47653=CARTESIAN_POINT('Ctrl Pts',(-1.89412243233685,42.1869085569829,14.9654175430183));
#47654=CARTESIAN_POINT('Ctrl Pts',(-2.0992561914926,42.2257196768098,14.6980291423986));
#47655=CARTESIAN_POINT('Ctrl Pts',(-2.32729552311567,42.2857231314088,14.231700131323));
#47656=CARTESIAN_POINT('Ctrl Pts',(-2.38996358047702,42.3069006498049,14.0566049252537));
#47657=CARTESIAN_POINT('Ctrl Pts',(-2.47741115240338,42.3503735727866,13.6873956138112));
#47658=CARTESIAN_POINT('Ctrl Pts',(-2.50000000000055,42.3725986254843,13.4940315075717));
#47659=CARTESIAN_POINT('Ctrl Pts',(-2.5,42.3946776132135,13.2999999999929));
#47660=CARTESIAN_POINT('',(0.29921364472731,40.3086929042607,10.8178945405685));
#47661=CARTESIAN_POINT('Ctrl Pts',(-2.5,41.4625301506567,13.3));
#47662=CARTESIAN_POINT('Ctrl Pts',(-2.5,41.4560785509388,13.3566783547267));
#47663=CARTESIAN_POINT('Ctrl Pts',(-2.49807254879367,41.4496179201224,13.4134065353913));
#47664=CARTESIAN_POINT('Ctrl Pts',(-2.47148213767631,41.4049536465583,13.8033386835103));
#47665=CARTESIAN_POINT('Ctrl Pts',(-2.38219647438595,41.3663719935291,14.1286848321518));
#47666=CARTESIAN_POINT('Ctrl Pts',(-2.09236349753892,41.2928990371905,14.7026692336443));
#47667=CARTESIAN_POINT('Ctrl Pts',(-1.90315733928508,41.2584345053206,14.9502974710062));
#47668=CARTESIAN_POINT('Ctrl Pts',(-1.43371380883422,41.1872437576834,15.3733411230399));
#47669=CARTESIAN_POINT('Ctrl Pts',(-1.15414839789977,41.1510689780122,15.5410470043474));
#47670=CARTESIAN_POINT('Ctrl Pts',(-0.552493634150507,41.080644518305,15.7586776853435));
#47671=CARTESIAN_POINT('Ctrl Pts',(-0.236875365769137,41.0471638778177,
15.8088231800092));
#47672=CARTESIAN_POINT('Ctrl Pts',(0.398445077487314,40.9770276470599,15.7885661577294));
#47673=CARTESIAN_POINT('Ctrl Pts',(0.712541558724279,40.9411190516746,15.7174744657946));
#47674=CARTESIAN_POINT('Ctrl Pts',(1.27025636778447,40.8767556601898,15.4726642950741));
#47675=CARTESIAN_POINT('Ctrl Pts',(1.51333231666157,40.8483665405938,15.310924910557));
#47676=CARTESIAN_POINT('Ctrl Pts',(1.96510748387776,40.7840312890235,14.8810647713995));
#47677=CARTESIAN_POINT('Ctrl Pts',(2.15854110160934,40.7479263175339,14.6047292565089));
#47678=CARTESIAN_POINT('Ctrl Pts',(2.40840350182393,40.68618936217,14.0311557266678));
#47679=CARTESIAN_POINT('Ctrl Pts',(2.47714514170984,40.660214611156,13.7457199251508));
#47680=CARTESIAN_POINT('Ctrl Pts',(2.51593287324437,40.6001147718643,13.1208255095539));
#47681=CARTESIAN_POINT('Ctrl Pts',(2.46937870516111,40.5653455467743,12.7857883898233));
#47682=CARTESIAN_POINT('Ctrl Pts',(2.26356318381571,40.5083103638821,12.2012046620872));
#47683=CARTESIAN_POINT('Ctrl Pts',(2.12391289303238,40.4853118764239,11.9509252325965));
#47684=CARTESIAN_POINT('Ctrl Pts',(1.73613868327223,40.4322867871816,11.4706618591433));
#47685=CARTESIAN_POINT('Ctrl Pts',(1.47750592152716,40.4010497148421,11.2560098035361));
#47686=CARTESIAN_POINT('Ctrl Pts',(0.909078151443106,40.3501549758377,10.9502852158795));
#47687=CARTESIAN_POINT('Ctrl Pts',(0.609047735460097,40.3305173363008,10.8553192285048));
#47688=CARTESIAN_POINT('Ctrl Pts',(0.299195963681299,40.3088185629972,10.817968216296));
#47689=CARTESIAN_POINT('Ctrl Pts',(0.29922011908992,40.3085872692275,10.8179711282236));
#47690=CARTESIAN_POINT('Ctrl Pts',(0.116198641054608,40.2789287682072,10.7959070382057));
#47691=CARTESIAN_POINT('Ctrl Pts',(-0.0686762603413709,40.2491054246701,
10.7941574537077));
#47692=CARTESIAN_POINT('Ctrl Pts',(-0.438507985113607,40.1886677747163,
10.8316316522575));
#47693=CARTESIAN_POINT('Ctrl Pts',(-0.622391748993356,40.1582791495571,
10.8714511195648));
#47694=CARTESIAN_POINT('Ctrl Pts',(-0.939390485172885,40.1059611621546,
10.9785492634775));
#47695=CARTESIAN_POINT('Ctrl Pts',(-1.07421589908956,40.0835661295813,11.0377722117975));
#47696=CARTESIAN_POINT('Ctrl Pts',(-1.48656905412663,40.0115779517093,11.2641483984129));
#47697=CARTESIAN_POINT('Ctrl Pts',(-1.73714292844758,39.9616407800466,11.4732906075798));
#47698=CARTESIAN_POINT('Ctrl Pts',(-2.14142033006415,39.8636098967804,11.9712737432747));
#47699=CARTESIAN_POINT('Ctrl Pts',(-2.29295694249452,39.8182922052658,12.2542172428525));
#47700=CARTESIAN_POINT('Ctrl Pts',(-2.46213065903313,39.7350203443603,12.7986694947532));
#47701=CARTESIAN_POINT('Ctrl Pts',(-2.5,39.6979590514318,13.048786034241));
#47702=CARTESIAN_POINT('Ctrl Pts',(-2.5,39.6612570972331,13.3000000000001));
#47703=CARTESIAN_POINT('Origin',(0.,70.2,13.3));
#47704=CARTESIAN_POINT('',(-2.5,37.5946437602656,13.3));
#47705=CARTESIAN_POINT('',(-2.5,38.6159089611155,13.3000000021922));
#47706=CARTESIAN_POINT('',(-2.5,70.2,13.3));
#47707=CARTESIAN_POINT('',(-2.38728043808747,40.2846522490296,14.040572526374));
#47708=CARTESIAN_POINT('Ctrl Pts',(-2.5,38.6159089611155,13.3000000043844));
#47709=CARTESIAN_POINT('Ctrl Pts',(-2.50000000005366,38.6197079913925,13.2694025310785));
#47710=CARTESIAN_POINT('Ctrl Pts',(-2.49943827756166,38.6235065893519,13.2387964405414));
#47711=CARTESIAN_POINT('Ctrl Pts',(-2.48616875692374,38.6683390855345,12.8776808724054));
#47712=CARTESIAN_POINT('Ctrl Pts',(-2.40855367298769,38.7088102422073,12.5528105212031));
#47713=CARTESIAN_POINT('Ctrl Pts',(-2.20426898953433,38.7686465464089,12.110140157825));
#47714=CARTESIAN_POINT('Ctrl Pts',(-2.12535056754911,38.7877875407426,11.9743093800384));
#47715=CARTESIAN_POINT('Ctrl Pts',(-1.83956379670401,38.8479220297597,11.5742668391486));
#47716=CARTESIAN_POINT('Ctrl Pts',(-1.59209400869922,38.8884943271984,11.3436189247701));
#47717=CARTESIAN_POINT('Ctrl Pts',(-1.03650133667816,38.9672215982648,11.003050754753));
#47718=CARTESIAN_POINT('Ctrl Pts',(-0.737456794249405,39.004744620235,10.8903358409477));
#47719=CARTESIAN_POINT('Ctrl Pts',(-0.264597610750918,39.0624274558073,
10.8086961660701));
#47720=CARTESIAN_POINT('Ctrl Pts',(-0.101519839748652,39.0819694629327,
10.7967407944093));
#47721=CARTESIAN_POINT('Ctrl Pts',(0.357618543640866,39.136733000928,10.808051036079));
#47722=CARTESIAN_POINT('Ctrl Pts',(0.650055821113488,39.1712127316438,10.8678901023741));
#47723=CARTESIAN_POINT('Ctrl Pts',(1.23610977859552,39.2453369040003,11.1013585233494));
#47724=CARTESIAN_POINT('Ctrl Pts',(1.51901982093872,39.2846640132817,11.2863925577538));
#47725=CARTESIAN_POINT('Ctrl Pts',(1.9819103061487,39.360075244422,11.7437561604655));
#47726=CARTESIAN_POINT('Ctrl Pts',(2.16256841943955,39.3956859872853,12.0064890572955));
#47727=CARTESIAN_POINT('Ctrl Pts',(2.35474165464431,39.450929005508,12.4446749399196));
#47728=CARTESIAN_POINT('Ctrl Pts',(2.40533665564667,39.4696436602941,12.5994621647907));
#47729=CARTESIAN_POINT('Ctrl Pts',(2.50465014408154,39.5219387860576,13.0467179202076));
#47730=CARTESIAN_POINT('Ctrl Pts',(2.51703839078177,39.5545358882292,13.3444754963876));
#47731=CARTESIAN_POINT('Ctrl Pts',(2.43198342987368,39.6248445748884,13.9687351236858));
#47732=CARTESIAN_POINT('Ctrl Pts',(2.32087015026554,39.6625696127848,14.2876059817832));
#47733=CARTESIAN_POINT('Ctrl Pts',(1.99069784765935,39.7335660593531,14.8443579787623));
#47734=CARTESIAN_POINT('Ctrl Pts',(1.78195990589462,39.7665295035597,15.0811655365627));
#47735=CARTESIAN_POINT('Ctrl Pts',(1.40684512634722,39.8183912037277,15.372951244866));
#47736=CARTESIAN_POINT('Ctrl Pts',(1.2693272398596,39.8360946785057,15.4598980632706));
#47737=CARTESIAN_POINT('Ctrl Pts',(0.861901378213536,39.8850927100737,15.6650501996874));
#47738=CARTESIAN_POINT('Ctrl Pts',(0.578200738693645,39.9151341009516,15.7499114424441));
#47739=CARTESIAN_POINT('Ctrl Pts',(-0.0453251220284939,39.980052375392,
15.8217714213526));
#47740=CARTESIAN_POINT('Ctrl Pts',(-0.381226569776738,40.0154482219679,
15.7932152220384));
#47741=CARTESIAN_POINT('Ctrl Pts',(-0.995051864017533,40.0799329075217,
15.6137225977727));
#47742=CARTESIAN_POINT('Ctrl Pts',(-1.2702394715904,40.1088324258242,15.4748466918823));
#47743=CARTESIAN_POINT('Ctrl Pts',(-1.73611838947518,40.1668483767574,15.1204622490944));
#47744=CARTESIAN_POINT('Ctrl Pts',(-1.9287966619377,40.1944548137299,14.9149472035747));
#47745=CARTESIAN_POINT('Ctrl Pts',(-2.21484989923174,40.242696624887,14.4836180021855));
#47746=CARTESIAN_POINT('Ctrl Pts',(-2.31729815284615,40.2635916253591,14.2678011957536));
#47747=CARTESIAN_POINT('Ctrl Pts',(-2.38773478971345,40.2851228191638,14.0407581076114));
#47748=CARTESIAN_POINT('',(-2.50017028063955,40.3932053939429,13.3030872967355));
#47749=CARTESIAN_POINT('Ctrl Pts',(-2.38677922580708,40.2852562553959,14.0403593245475));
#47750=CARTESIAN_POINT('Ctrl Pts',(-2.39184533847209,40.2871499823883,14.0260557859757));
#47751=CARTESIAN_POINT('Ctrl Pts',(-2.39633423477753,40.289226676514,14.0118231755317));
#47752=CARTESIAN_POINT('Ctrl Pts',(-2.40062259401216,40.2914645379331,13.997116667899));
#47753=CARTESIAN_POINT('Ctrl Pts',(-2.40187210465684,40.2921165895714,13.9928315936252));
#47754=CARTESIAN_POINT('Ctrl Pts',(-2.4031190599626,40.2927734317743,13.9885118894307));
#47755=CARTESIAN_POINT('Ctrl Pts',(-2.40434046058925,40.2934230064818,13.9842373073297));
#47756=CARTESIAN_POINT('Ctrl Pts',(-2.41558848106818,40.2994050155402,13.9448721834205));
#47757=CARTESIAN_POINT('Ctrl Pts',(-2.42583769655266,40.305368540572,13.9053526778095));
#47758=CARTESIAN_POINT('Ctrl Pts',(-2.43511138146535,40.3113250164977,13.8656194028656));
#47759=CARTESIAN_POINT('Ctrl Pts',(-2.45309587693699,40.3228764348737,13.7885644985822));
#47760=CARTESIAN_POINT('Ctrl Pts',(-2.46737957066467,40.3343853235716,13.7108178911225));
#47761=CARTESIAN_POINT('Ctrl Pts',(-2.47793032286022,40.3458219873893,13.632612756334));
#47762=CARTESIAN_POINT('Ctrl Pts',(-2.4791981035249,40.3471962193861,13.6232156104314));
#47763=CARTESIAN_POINT('Ctrl Pts',(-2.48041195249927,40.348569413132,13.6138117924165));
#47764=CARTESIAN_POINT('Ctrl Pts',(-2.48157178479104,40.3499415208601,13.6044016653308));
#47765=CARTESIAN_POINT('Ctrl Pts',(-2.48817989424502,40.3577590632017,13.5507877504573));
#47766=CARTESIAN_POINT('Ctrl Pts',(-2.49303592985813,40.3655409146392,13.4969698553965));
#47767=CARTESIAN_POINT('Ctrl Pts',(-2.49612472346855,40.3732761501296,13.4430096946578));
#47768=CARTESIAN_POINT('Ctrl Pts',(-2.4961274246664,40.3732829147128,13.4429625056616));
#47769=CARTESIAN_POINT('Ctrl Pts',(-2.49613012451236,40.3732896792603,13.442915316556));
#47770=CARTESIAN_POINT('Ctrl Pts',(-2.49613282300637,40.3732964437722,13.4428681273412));
#47771=CARTESIAN_POINT('Ctrl Pts',(-2.4972156371881,40.3760108130897,13.4239326948875));
#47772=CARTESIAN_POINT('Ctrl Pts',(-2.49808077532599,40.3787194363049,13.4049796606347));
#47773=CARTESIAN_POINT('Ctrl Pts',(-2.49872813109644,40.3814232168861,13.3860127359362));
#47774=CARTESIAN_POINT('Ctrl Pts',(-2.49967173148025,40.3853643084938,13.3583661183537));
#47775=CARTESIAN_POINT('Ctrl Pts',(-2.50015159683804,40.3892908682538,13.3307197832459));
#47776=CARTESIAN_POINT('Ctrl Pts',(-2.50017028063955,40.3932053939429,13.3030872967355));
#47777=CARTESIAN_POINT('Ctrl Pts',(-2.49999807917248,40.3932899595023,13.3030990537122));
#47778=CARTESIAN_POINT('Ctrl Pts',(-2.49999935976079,40.3934360152657,13.3020660066571));
#47779=CARTESIAN_POINT('Ctrl Pts',(-2.50000000000072,40.3935820507829,13.3010329879761));
#47780=CARTESIAN_POINT('Ctrl Pts',(-2.5,40.3937280662289,13.2999999982622));
#47781=CARTESIAN_POINT('Ctrl Pts',(-2.5,39.6612570972331,13.3000000000001));
#47782=CARTESIAN_POINT('Ctrl Pts',(-2.5,39.653123693213,13.3556707326246));
#47783=CARTESIAN_POINT('Ctrl Pts',(-2.49814051750878,39.6450187406706,13.4113969395304));
#47784=CARTESIAN_POINT('Ctrl Pts',(-2.47203053406049,39.5886061827757,13.8011874110541));
#47785=CARTESIAN_POINT('Ctrl Pts',(-2.38274677131432,39.5417764947153,14.1274812070693));
#47786=CARTESIAN_POINT('Ctrl Pts',(-2.11676137747124,39.4571269586374,14.6544383766883));
#47787=CARTESIAN_POINT('Ctrl Pts',(-1.96740882675978,39.4207476870172,14.8635361530646));
#47788=CARTESIAN_POINT('Ctrl Pts',(-1.55539887166156,39.3402050054438,15.285547448765));
#47789=CARTESIAN_POINT('Ctrl Pts',(-1.27641278910592,39.2962232120126,15.4754170763141));
#47790=CARTESIAN_POINT('Ctrl Pts',(-0.683041882390598,39.20670885425,15.7247077964409));
#47791=CARTESIAN_POINT('Ctrl Pts',(-0.37803167167398,39.1625312623935,15.7905412413853));
#47792=CARTESIAN_POINT('Ctrl Pts',(0.24676645044173,39.075250993696,15.8077393947595));
#47793=CARTESIAN_POINT('Ctrl Pts',(0.561122788821101,39.0340312077439,15.7566007588563));
#47794=CARTESIAN_POINT('Ctrl Pts',(1.15912961578192,38.9487172099549,15.538157668776));
#47795=CARTESIAN_POINT('Ctrl Pts',(1.43642055723788,38.9051946996757,15.3711177459246));
#47796=CARTESIAN_POINT('Ctrl Pts',(1.86818525975432,38.8253475582604,14.9816366012639));
#47797=CARTESIAN_POINT('Ctrl Pts',(2.03338676521065,38.7901985060572,14.7776534031731));
#47798=CARTESIAN_POINT('Ctrl Pts',(2.33203173855803,38.7114740038227,14.2613354170784));
#47799=CARTESIAN_POINT('Ctrl Pts',(2.43986117781533,38.6681480807116,13.9400460554133));
#47800=CARTESIAN_POINT('Ctrl Pts',(2.5191469391265,38.5837584416547,13.2993991938612));
#47801=CARTESIAN_POINT('Ctrl Pts',(2.49966976205757,38.5434006298179,12.987311343042));
#47802=CARTESIAN_POINT('Ctrl Pts',(2.3829592714491,38.4816382884601,12.5260638648528));
#47803=CARTESIAN_POINT('Ctrl Pts',(2.3264199951752,38.4602954115601,12.3698131664047));
#47804=CARTESIAN_POINT('Ctrl Pts',(2.11089682384098,38.3958959010657,11.919715190783));
#47805=CARTESIAN_POINT('Ctrl Pts',(1.90829196915177,38.3533731762915,11.650905560836));
#47806=CARTESIAN_POINT('Ctrl Pts',(1.49340588822079,38.2821957701758,11.2828973519894));
#47807=CARTESIAN_POINT('Ctrl Pts',(1.3090878023652,38.2539541001287,11.1586759057338));
#47808=CARTESIAN_POINT('Ctrl Pts',(0.971035791073398,38.2060186696871,10.9910097382391));
#47809=CARTESIAN_POINT('Ctrl Pts',(0.825057175685232,38.1863712699139,10.9349136382988));
#47810=CARTESIAN_POINT('Ctrl Pts',(0.372703141526457,38.1271811573218,10.8081084724525));
#47811=CARTESIAN_POINT('Ctrl Pts',(0.0573506802001572,38.0880693821565,
10.7810431777528));
#47812=CARTESIAN_POINT('Ctrl Pts',(-0.582631752832415,38.0070454280135,
10.8466001293174));
#47813=CARTESIAN_POINT('Ctrl Pts',(-0.9006695475721,37.9659291787871,10.9446979810559));
#47814=CARTESIAN_POINT('Ctrl Pts',(-1.45574598758833,37.8869746020048,11.245303144746));
#47815=CARTESIAN_POINT('Ctrl Pts',(-1.69282980968617,37.8497733454819,11.4357732717793));
#47816=CARTESIAN_POINT('Ctrl Pts',(-2.06678961815314,37.7793227065523,11.8678221581079));
#47817=CARTESIAN_POINT('Ctrl Pts',(-2.20916254837202,37.7465508507352,12.0990102715484));
#47818=CARTESIAN_POINT('Ctrl Pts',(-2.36787119150113,37.6957025312189,12.4846114182324));
#47819=CARTESIAN_POINT('Ctrl Pts',(-2.41176838513802,37.6777969568209,12.6254296680502));
#47820=CARTESIAN_POINT('Ctrl Pts',(-2.48098939879585,37.6379899850485,12.944073891754));
#47821=CARTESIAN_POINT('Ctrl Pts',(-2.5,37.6162662367362,13.1219981617627));
#47822=CARTESIAN_POINT('Ctrl Pts',(-2.5,37.5946437602656,13.3));
#47823=CARTESIAN_POINT('Origin',(0.,70.2,13.3));
#47824=CARTESIAN_POINT('',(-2.5,35.7784429531659,13.3000000000001));
#47825=CARTESIAN_POINT('',(-2.5,36.4895163993155,13.2999999996801));
#47826=CARTESIAN_POINT('',(-2.5,70.2,13.3));
#47827=CARTESIAN_POINT('Ctrl Pts',(-2.5,36.4895163993155,13.2999999993602));
#47828=CARTESIAN_POINT('Ctrl Pts',(-2.49999999995295,36.5164180716991,13.1161283443394));
#47829=CARTESIAN_POINT('Ctrl Pts',(-2.47971719676694,36.5426838350161,12.9328114292078));
#47830=CARTESIAN_POINT('Ctrl Pts',(-2.40581734184516,36.5922050891777,12.6030249444719));
#47831=CARTESIAN_POINT('Ctrl Pts',(-2.35832606702688,36.6151111253982,12.456202198798));
#47832=CARTESIAN_POINT('Ctrl Pts',(-2.19166732682489,36.679208359259,12.0675547917492));
#47833=CARTESIAN_POINT('Ctrl Pts',(-2.04649721218126,36.7210257240423,11.8391132907617));
#47834=CARTESIAN_POINT('Ctrl Pts',(-1.64339674723545,36.8111514981178,11.3860721774674));
#47835=CARTESIAN_POINT('Ctrl Pts',(-1.3703643495528,36.8565045600032,11.1819499306933));
#47836=CARTESIAN_POINT('Ctrl Pts',(-0.930516986354473,36.9255076032598,
10.9748808728237));
#47837=CARTESIAN_POINT('Ctrl Pts',(-0.790869092248727,36.9468256709158,
10.9237542248518));
#47838=CARTESIAN_POINT('Ctrl Pts',(-0.373829622410181,37.0096987915266,
10.8119160537901));
#47839=CARTESIAN_POINT('Ctrl Pts',(-0.089576260525372,37.0517207460895,
10.785572083852));
#47840=CARTESIAN_POINT('Ctrl Pts',(0.352206631553183,37.1146775549043,10.8197933542263));
#47841=CARTESIAN_POINT('Ctrl Pts',(0.509832674521626,37.1366856662043,10.8473337001418));
#47842=CARTESIAN_POINT('Ctrl Pts',(0.821882994016063,37.1816746792334,10.9332730038645));
#47843=CARTESIAN_POINT('Ctrl Pts',(0.975304176411618,37.2045973705891,10.9922595136116));
#47844=CARTESIAN_POINT('Ctrl Pts',(1.26582779450248,37.2498606385876,11.1381392135487));
#47845=CARTESIAN_POINT('Ctrl Pts',(1.40249855676195,37.2719384241438,11.2241943982254));
#47846=CARTESIAN_POINT('Ctrl Pts',(1.73582296806904,37.3298506647626,11.4821223403624));
#47847=CARTESIAN_POINT('Ctrl Pts',(1.9155823494612,37.3660185428071,11.672626415537));
#47848=CARTESIAN_POINT('Ctrl Pts',(2.25181029285251,37.446292962554,12.1636152157564));
#47849=CARTESIAN_POINT('Ctrl Pts',(2.38357327113818,37.4893590535764,12.4749734475991));
#47850=CARTESIAN_POINT('Ctrl Pts',(2.51390957361782,37.5774358033074,13.1176269747578));
#47851=CARTESIAN_POINT('Ctrl Pts',(2.51653062361988,37.6213426693713,13.4414966009373));
#47852=CARTESIAN_POINT('Ctrl Pts',(2.40771056069729,37.7020097291258,14.0268330908957));
#47853=CARTESIAN_POINT('Ctrl Pts',(2.31342928036838,37.7375889165503,14.286650095782));
#47854=CARTESIAN_POINT('Ctrl Pts',(2.02413879705667,37.8143820612513,14.8007484593905));
#47855=CARTESIAN_POINT('Ctrl Pts',(1.81898422348574,37.8553460540575,15.0437380248159));
#47856=CARTESIAN_POINT('Ctrl Pts',(1.36398729756465,37.9330087116023,15.4125147219413));
#47857=CARTESIAN_POINT('Ctrl Pts',(1.12752760846014,37.968797771397,15.5476473510898));
#47858=CARTESIAN_POINT('Ctrl Pts',(0.560752962874162,38.0474284766851,15.7591313971231));
#47859=CARTESIAN_POINT('Ctrl Pts',(0.227197742383383,38.0898486321667,15.8120102985733));
#47860=CARTESIAN_POINT('Ctrl Pts',(-0.428500615184119,38.1742873286512,
15.7839513490688));
#47861=CARTESIAN_POINT('Ctrl Pts',(-0.744476071039354,38.2152359311912,
15.7081968566207));
#47862=CARTESIAN_POINT('Ctrl Pts',(-1.1861135341602,38.2771193234957,15.5067733757899));
#47863=CARTESIAN_POINT('Ctrl Pts',(-1.32781794756963,38.2978322412313,15.4245276218427));
#47864=CARTESIAN_POINT('Ctrl Pts',(-1.72782306550425,38.3603536520828,15.1366077188321));
#47865=CARTESIAN_POINT('Ctrl Pts',(-1.95453124588622,38.4016882989555,14.8932143590788));
#47866=CARTESIAN_POINT('Ctrl Pts',(-2.30134502414229,38.4848482211263,14.3311940669407));
#47867=CARTESIAN_POINT('Ctrl Pts',(-2.41751828882584,38.5258444555845,14.0177667258479));
#47868=CARTESIAN_POINT('Ctrl Pts',(-2.48973048211815,38.5834135228102,13.5614970169554));
#47869=CARTESIAN_POINT('Ctrl Pts',(-2.49999999977056,38.5996652405177,13.4308272869097));
#47870=CARTESIAN_POINT('Ctrl Pts',(-2.5,38.6159089611155,13.3000000043844));
#47871=CARTESIAN_POINT('',(-0.846350554922702,36.2086580169322,10.9476201968673));
#47872=CARTESIAN_POINT('Ctrl Pts',(-2.5,37.5946437602656,13.3));
#47873=CARTESIAN_POINT('Ctrl Pts',(-2.5,37.5758608613471,13.4546256988409));
#47874=CARTESIAN_POINT('Ctrl Pts',(-2.48565439642402,37.5571557154162,13.6093100923753));
#47875=CARTESIAN_POINT('Ctrl Pts',(-2.42722680302701,37.5190899388255,13.9200051148318));
#47876=CARTESIAN_POINT('Ctrl Pts',(-2.38235405824464,37.4998674146584,14.074743695524));
#47877=CARTESIAN_POINT('Ctrl Pts',(-2.19953877727962,37.4405207481708,14.5342901767562));
#47878=CARTESIAN_POINT('Ctrl Pts',(-2.01523932029944,37.4007250256698,14.8166736003359));
#47879=CARTESIAN_POINT('Ctrl Pts',(-1.55195139548261,37.3226156505755,15.2869258589061));
#47880=CARTESIAN_POINT('Ctrl Pts',(-1.27970061915826,37.2848103581954,15.4722797841508));
#47881=CARTESIAN_POINT('Ctrl Pts',(-0.832456925475637,37.227433105574,15.662747169702));
#47882=CARTESIAN_POINT('Ctrl Pts',(-0.679686613721388,37.2086502929714,
15.7111394399072));
#47883=CARTESIAN_POINT('Ctrl Pts',(-0.230815413171425,37.1551129962611,
15.8072317848003));
#47884=CARTESIAN_POINT('Ctrl Pts',(0.0705894370523697,37.1212759056622,
15.8168486334183));
#47885=CARTESIAN_POINT('Ctrl Pts',(0.696802929063635,37.0484863977452,15.7240331077785));
#47886=CARTESIAN_POINT('Ctrl Pts',(1.01399181665485,37.0100092636035,15.6094059933073));
#47887=CARTESIAN_POINT('Ctrl Pts',(1.57564176945598,36.9358143495937,15.267731913643));
#47888=CARTESIAN_POINT('Ctrl Pts',(1.81674497014354,36.9002892620361,15.0475850688783));
#47889=CARTESIAN_POINT('Ctrl Pts',(2.18687825476669,36.8301304928963,14.5476811492629));
#47890=CARTESIAN_POINT('Ctrl Pts',(2.32017373464543,36.7971620961948,14.2777673705857));
#47891=CARTESIAN_POINT('Ctrl Pts',(2.44629623413705,36.747711257298,13.8390132560229));
#47892=CARTESIAN_POINT('Ctrl Pts',(2.47543338932105,36.7308325383625,13.6835728546094));
#47893=CARTESIAN_POINT('Ctrl Pts',(2.51988750766847,36.6776037066035,13.1947716125488));
#47894=CARTESIAN_POINT('Ctrl Pts',(2.48348290504879,36.6411712216394,12.8603075551738));
#47895=CARTESIAN_POINT('Ctrl Pts',(2.28547246478389,36.572464920124,12.2372861160282));
#47896=CARTESIAN_POINT('Ctrl Pts',(2.13052447711007,36.5400411722486,11.9532964471577));
#47897=CARTESIAN_POINT('Ctrl Pts',(1.73688060457641,36.4751983782657,11.4775185956148));
#47898=CARTESIAN_POINT('Ctrl Pts',(1.50824003305037,36.4448691380507,11.2841788113515));
#47899=CARTESIAN_POINT('Ctrl Pts',(1.11149638239736,36.3998183440908,11.0548919430727));
#47900=CARTESIAN_POINT('Ctrl Pts',(0.964611197203937,36.3843195301676,10.9879754236812));
#47901=CARTESIAN_POINT('Ctrl Pts',(0.523767514788698,36.3385852022954,10.8365158384325));
#47902=CARTESIAN_POINT('Ctrl Pts',(0.219386868080082,36.3080353712077,10.7910011058256));
#47903=CARTESIAN_POINT('Ctrl Pts',(-0.34532869839718,36.2549870908647,10.8103777802712));
#47904=CARTESIAN_POINT('Ctrl Pts',(-0.601927411664119,36.2321980347213,
10.8596804591393));
#47905=CARTESIAN_POINT('Ctrl Pts',(-0.846350554899145,36.2086580169353,
10.9476201968598));
#47906=CARTESIAN_POINT('Ctrl Pts',(-0.846422303514195,36.2091836693201,
10.9476460121585));
#47907=CARTESIAN_POINT('Ctrl Pts',(-1.0597631465936,36.1762938847118,11.0244101593771));
#47908=CARTESIAN_POINT('Ctrl Pts',(-1.26174119076661,36.1433776234327,11.1298657021809));
#47909=CARTESIAN_POINT('Ctrl Pts',(-1.66633664079304,36.0731727395765,11.416968366155));
#47910=CARTESIAN_POINT('Ctrl Pts',(-1.85933278671221,36.0362450266669,11.607246829317));
#47911=CARTESIAN_POINT('Ctrl Pts',(-2.20651957219189,35.953839120045,12.082201117234));
#47912=CARTESIAN_POINT('Ctrl Pts',(-2.3437487822392,35.9087830563224,12.3733919715845));
#47913=CARTESIAN_POINT('Ctrl Pts',(-2.4740799188374,35.8352051968173,12.8847061362566));
#47914=CARTESIAN_POINT('Ctrl Pts',(-2.5,35.8068403729879,13.0921698303673));
#47915=CARTESIAN_POINT('Ctrl Pts',(-2.5,35.7784429531659,13.3000000000002));
#47916=CARTESIAN_POINT('Origin',(0.,70.2,13.3));
#47917=CARTESIAN_POINT('',(-2.5,33.7644650054088,13.3000000002187));
#47918=CARTESIAN_POINT('',(-2.5,34.7604761263293,13.3000000000185));
#47919=CARTESIAN_POINT('',(-2.5,70.2,13.3));
#47920=CARTESIAN_POINT('',(-2.49999982102973,34.7605873473017,13.2990540341987));
#47921=CARTESIAN_POINT('Ctrl Pts',(-2.5,34.7604761263292,13.3000000000369));
#47922=CARTESIAN_POINT('Ctrl Pts',(-2.5,34.76051358954,13.2996813693674));
#47923=CARTESIAN_POINT('Ctrl Pts',(-2.49999994159659,34.7605498847325,13.2993726684756));
#47924=CARTESIAN_POINT('Ctrl Pts',(-2.49999982102973,34.7605873473017,13.2990540341987));
#47925=CARTESIAN_POINT('',(-1.81156843952179,36.1875454226321,15.0225226611708));
#47926=CARTESIAN_POINT('Ctrl Pts',(-2.49999982102973,34.7605873473017,13.2990540341987));
#47927=CARTESIAN_POINT('Ctrl Pts',(-2.49988526272856,34.7961829353405,12.9962991861577));
#47928=CARTESIAN_POINT('Ctrl Pts',(-2.44478214320481,34.8310453620436,12.6961179853287));
#47929=CARTESIAN_POINT('Ctrl Pts',(-2.21937139071209,34.9069292536943,12.1020579693682));
#47930=CARTESIAN_POINT('Ctrl Pts',(-2.04040483388747,34.9462712647688,11.8175882391226));
#47931=CARTESIAN_POINT('Ctrl Pts',(-1.61883026837122,35.0167936072861,11.3746355767685));
#47932=CARTESIAN_POINT('Ctrl Pts',(-1.39436054437815,35.0480617144675,11.206345733161));
#47933=CARTESIAN_POINT('Ctrl Pts',(-0.851399687633854,35.1193207762706,
10.9260536485853));
#47934=CARTESIAN_POINT('Ctrl Pts',(-0.528436593682016,35.1578251634748,
10.8339507381643));
#47935=CARTESIAN_POINT('Ctrl Pts',(0.0788819293477749,35.2260961580154,
10.7859847309334));
#47936=CARTESIAN_POINT('Ctrl Pts',(0.356262375455895,35.2560238915552,10.8101080910456));
#47937=CARTESIAN_POINT('Ctrl Pts',(0.948103528783883,35.3255621256351,10.9626771769118));
#47938=CARTESIAN_POINT('Ctrl Pts',(1.25226516906477,35.3637818791458,11.1104808091419));
#47939=CARTESIAN_POINT('Ctrl Pts',(1.74208957173634,35.4308120215263,11.48493736365));
#47940=CARTESIAN_POINT('Ctrl Pts',(1.93530129987065,35.4599097139804,11.6925391593047));
#47941=CARTESIAN_POINT('Ctrl Pts',(2.1802985620806,35.5090599584891,12.0657192359799));
#47942=CARTESIAN_POINT('Ctrl Pts',(2.25688961478123,35.5275353176654,12.2120648221172));
#47943=CARTESIAN_POINT('Ctrl Pts',(2.4195931220143,35.5755168003784,12.6154731181076));
#47944=CARTESIAN_POINT('Ctrl Pts',(2.47940567072807,35.6039391298189,12.8808651027996));
#47945=CARTESIAN_POINT('Ctrl Pts',(2.504627900418,35.6470887925279,13.3027428438554));
#47946=CARTESIAN_POINT('Ctrl Pts',(2.49981578545345,35.6623656760365,13.4551760500165));
#47947=CARTESIAN_POINT('Ctrl Pts',(2.44034072548846,35.7125940126195,13.9370946533036));
#47948=CARTESIAN_POINT('Ctrl Pts',(2.33368952095993,35.7486272092269,14.2566886833866));
#47949=CARTESIAN_POINT('Ctrl Pts',(2.0210274980302,35.8106804137796,14.8005548952924));
#47950=CARTESIAN_POINT('Ctrl Pts',(1.83107790409723,35.8369690342989,15.0272182923819));
#47951=CARTESIAN_POINT('Ctrl Pts',(1.35024119677199,35.8976767669939,15.4303522275185));
#47952=CARTESIAN_POINT('Ctrl Pts',(1.05363837512255,35.9324273498156,15.5916543627122));
#47953=CARTESIAN_POINT('Ctrl Pts',(0.461734683688209,35.9892932414591,15.7734383683323));
#47954=CARTESIAN_POINT('Ctrl Pts',(0.177422069362182,36.0121792761678,15.8098899341102));
#47955=CARTESIAN_POINT('Ctrl Pts',(-0.43915284457503,36.0652002822201,15.7834842281171));
#47956=CARTESIAN_POINT('Ctrl Pts',(-0.765391457556897,36.0963838848401,
15.7031261159702));
#47957=CARTESIAN_POINT('Ctrl Pts',(-1.34626741194371,36.1469262513021,15.4291419512213));
#47958=CARTESIAN_POINT('Ctrl Pts',(-1.59879965261283,36.166409407584,15.2466270173068));
#47959=CARTESIAN_POINT('Ctrl Pts',(-1.81175956334301,36.1879287370222,15.0226512370864));
#47960=CARTESIAN_POINT('',(-2.49999928840966,36.4881581266667,13.3018862532181));
#47961=CARTESIAN_POINT('Ctrl Pts',(-1.81183660638924,36.1881958906855,15.0225702051725));
#47962=CARTESIAN_POINT('Ctrl Pts',(-1.81892097439324,36.189477370912,15.0151187136488));
#47963=CARTESIAN_POINT('Ctrl Pts',(-1.82595923910941,36.1907591156391,15.0076235328133));
#47964=CARTESIAN_POINT('Ctrl Pts',(-1.83293662276303,36.1923838835242,15.0001009784522));
#47965=CARTESIAN_POINT('Ctrl Pts',(-1.84686725918764,36.1956278001275,14.9850818860543));
#47966=CARTESIAN_POINT('Ctrl Pts',(-1.86061157959221,36.1989020602568,14.9698934450896));
#47967=CARTESIAN_POINT('Ctrl Pts',(-1.87416777695279,36.2021760116161,14.9545377432479));
#47968=CARTESIAN_POINT('Ctrl Pts',(-1.90119016409984,36.2087021766444,14.9239282951081));
#47969=CARTESIAN_POINT('Ctrl Pts',(-1.92745885272653,36.215225832546,14.8926611467449));
#47970=CARTESIAN_POINT('Ctrl Pts',(-1.95294978830251,36.2217532634333,14.8607649164333));
#47971=CARTESIAN_POINT('Ctrl Pts',(-2.00440094616609,36.2349282948489,14.7963852479774));
#47972=CARTESIAN_POINT('Ctrl Pts',(-2.05255602129216,36.248114920072,14.7296015234022));
#47973=CARTESIAN_POINT('Ctrl Pts',(-2.09726221388262,36.2613077135368,14.6606951187611));
#47974=CARTESIAN_POINT('Ctrl Pts',(-2.14223936592775,36.2745804671126,14.5913710797668));
#47975=CARTESIAN_POINT('Ctrl Pts',(-2.18372552160831,36.2878594629992,14.5198993718759));
#47976=CARTESIAN_POINT('Ctrl Pts',(-2.22157690179356,36.3011401026881,14.4465583584874));
#47977=CARTESIAN_POINT('Ctrl Pts',(-2.25890395136072,36.3142367742897,14.374233290586));
#47978=CARTESIAN_POINT('Ctrl Pts',(-2.29269662736909,36.3273350454751,14.3000911924193));
#47979=CARTESIAN_POINT('Ctrl Pts',(-2.32282676136498,36.3404313990264,14.224378621933));
#47980=CARTESIAN_POINT('Ctrl Pts',(-2.34756675175684,36.3511848746356,14.1622106851216));
#47981=CARTESIAN_POINT('Ctrl Pts',(-2.36983787706874,36.3619370729079,14.0989837571188));
#47982=CARTESIAN_POINT('Ctrl Pts',(-2.38956957911678,36.3726865049897,14.0348178186188));
#47983=CARTESIAN_POINT('Ctrl Pts',(-2.42230018775947,36.3905174784022,13.9283804613081));
#47984=CARTESIAN_POINT('Ctrl Pts',(-2.44782899532107,36.4080893877882,13.8200452990317));
#47985=CARTESIAN_POINT('Ctrl Pts',(-2.46605367650299,36.4253945284877,13.7105840530343));
#47986=CARTESIAN_POINT('Ctrl Pts',(-2.47192729325118,36.4309717873285,13.6753058826592));
#47987=CARTESIAN_POINT('Ctrl Pts',(-2.4770427155916,36.4365213511696,13.63990910798));
#47988=CARTESIAN_POINT('Ctrl Pts',(-2.4813971292479,36.4420430033563,13.6044146628536));
#47989=CARTESIAN_POINT('Ctrl Pts',(-2.49369610207015,36.4576388230323,13.5041611613707));
#47990=CARTESIAN_POINT('Ctrl Pts',(-2.49992291223824,36.4730118750243,13.4031135817416));
#47991=CARTESIAN_POINT('Ctrl Pts',(-2.49999928840966,36.4881581266667,13.3018862532181));
#47992=CARTESIAN_POINT('Ctrl Pts',(-2.49999916661337,36.489217714823,13.3020413065548));
#47993=CARTESIAN_POINT('Ctrl Pts',(-2.49999972221066,36.4893172865525,13.3013608635544));
#47994=CARTESIAN_POINT('Ctrl Pts',(-2.50000000000017,36.4894168480168,13.3006804277656));
#47995=CARTESIAN_POINT('Ctrl Pts',(-2.5,36.4895163993155,13.2999999993602));
#47996=CARTESIAN_POINT('',(-2.10782919047724,33.9999546381749,11.9560483405783));
#47997=CARTESIAN_POINT('Ctrl Pts',(-2.5,35.7784429531659,13.3000000000002));
#47998=CARTESIAN_POINT('Ctrl Pts',(-2.5,35.7627803554752,13.4146287358281));
#47999=CARTESIAN_POINT('Ctrl Pts',(-2.49211673543698,35.7471213482476,13.5293708036824));
#48000=CARTESIAN_POINT('Ctrl Pts',(-2.43395053540011,35.6894310917777,13.948793271294));
#48001=CARTESIAN_POINT('Ctrl Pts',(-2.33546939726797,35.6477491297446,14.2437533052336));
#48002=CARTESIAN_POINT('Ctrl Pts',(-2.02286969681855,35.5613152085308,14.8068850758757));
#48003=CARTESIAN_POINT('Ctrl Pts',(-1.80244624105573,35.5176163173916,15.0646366521508));
#48004=CARTESIAN_POINT('Ctrl Pts',(-1.29670845882954,35.4324203175144,15.4591561473659));
#48005=CARTESIAN_POINT('Ctrl Pts',(-1.0232670581393,35.3918957264238,15.6013840293111));
#48006=CARTESIAN_POINT('Ctrl Pts',(-0.57538516105805,35.3303880647178,15.7383171466564));
#48007=CARTESIAN_POINT('Ctrl Pts',(-0.415546395330684,35.3092506195382,
15.770584746121));
#48008=CARTESIAN_POINT('Ctrl Pts',(0.0604876803035786,35.247045108235,15.8191427816985));
#48009=CARTESIAN_POINT('Ctrl Pts',(0.377948259338413,35.2064302707169,15.7913710836388));
#48010=CARTESIAN_POINT('Ctrl Pts',(0.842453040063227,35.1443465641293,15.6596908634744));
#48011=CARTESIAN_POINT('Ctrl Pts',(0.998106002767982,35.1230218397156,15.5981857595108));
#48012=CARTESIAN_POINT('Ctrl Pts',(1.2906191205536,35.0809419559713,15.4472343310581));
#48013=CARTESIAN_POINT('Ctrl Pts',(1.42719287203555,35.0602890630069,15.3589893598535));
#48014=CARTESIAN_POINT('Ctrl Pts',(1.81579281967665,34.9971449917828,15.0505408321967));
#48015=CARTESIAN_POINT('Ctrl Pts',(2.03313609359154,34.9554187807748,14.7926160878873));
#48016=CARTESIAN_POINT('Ctrl Pts',(2.34860970661178,34.8729588784015,14.2157888108851));
#48017=CARTESIAN_POINT('Ctrl Pts',(2.44729156605952,34.8329736674971,13.9045136917868));
#48018=CARTESIAN_POINT('Ctrl Pts',(2.50209267416223,34.7729763375332,13.423624155607));
#48019=CARTESIAN_POINT('Ctrl Pts',(2.50486966442622,34.7531962872763,13.2627979850154));
#48020=CARTESIAN_POINT('Ctrl Pts',(2.46646526313834,34.6932587855849,12.7774161968489));
#48021=CARTESIAN_POINT('Ctrl Pts',(2.37723685619148,34.6537100764755,12.4601643297973));
#48022=CARTESIAN_POINT('Ctrl Pts',(2.15774410174524,34.5946730153388,12.0274704339981));
#48023=CARTESIAN_POINT('Ctrl Pts',(2.07262060717391,34.5754789665299,11.8930738701525));
#48024=CARTESIAN_POINT('Ctrl Pts',(1.87717294151182,34.5370104578763,11.6411256027248));
#48025=CARTESIAN_POINT('Ctrl Pts',(1.7670869458932,34.5178261190561,11.5243167589954));
#48026=CARTESIAN_POINT('Ctrl Pts',(1.39551967463749,34.4586456697698,11.1990837780451));
#48027=CARTESIAN_POINT('Ctrl Pts',(1.10295796694357,34.4191313361643,11.031772149259));
#48028=CARTESIAN_POINT('Ctrl Pts',(0.632527884577907,34.3606794892829,10.8759327976478));
#48029=CARTESIAN_POINT('Ctrl Pts',(0.474309764613275,34.3417414496223,10.8400757207167));
#48030=CARTESIAN_POINT('Ctrl Pts',(-0.0132039176921074,34.2841108186178,
10.7784083992674));
#48031=CARTESIAN_POINT('Ctrl Pts',(-0.345159421783913,34.2459202829331,
10.8020965808484));
#48032=CARTESIAN_POINT('Ctrl Pts',(-0.811350338434691,34.1903158765828,
10.9303191753661));
#48033=CARTESIAN_POINT('Ctrl Pts',(-0.955632434546944,34.172761615236,10.9847363963674));
#48034=CARTESIAN_POINT('Ctrl Pts',(-1.30888815416826,34.1277598923389,11.1566550628106));
#48035=CARTESIAN_POINT('Ctrl Pts',(-1.50770133280881,34.1005301349767,11.2915237191095));
#48036=CARTESIAN_POINT('Ctrl Pts',(-1.84710194884547,34.0487412720109,11.6009638960582));
#48037=CARTESIAN_POINT('Ctrl Pts',(-1.98954353185177,34.0243565893973,11.7702174610211));
#48038=CARTESIAN_POINT('Ctrl Pts',(-2.10796460894866,33.9998221304067,11.9559444924335));
#48039=CARTESIAN_POINT('',(-2.49999978507887,33.7646310379939,13.2989633681452));
#48040=CARTESIAN_POINT('Ctrl Pts',(-2.1079929847411,34.0001676959785,11.9559889969638));
#48041=CARTESIAN_POINT('Ctrl Pts',(-2.2350777214743,33.9597552880639,12.1553130597104));
#48042=CARTESIAN_POINT('Ctrl Pts',(-2.33326888345894,33.9189932195931,12.3716816396712));
#48043=CARTESIAN_POINT('Ctrl Pts',(-2.46608509532503,33.8399117586071,12.8261052420337));
#48044=CARTESIAN_POINT('Ctrl Pts',(-2.49990145924373,33.8026104324006,13.0618352444272));
#48045=CARTESIAN_POINT('Ctrl Pts',(-2.49999978507887,33.7646310379939,13.2989633681452));
#48046=CARTESIAN_POINT('Ctrl Pts',(-2.49999978507887,33.7646310379939,13.2989633681452));
#48047=CARTESIAN_POINT('Ctrl Pts',(-2.49999992836101,33.7645756937527,13.2993089154159));
#48048=CARTESIAN_POINT('Ctrl Pts',(-2.50000000000006,33.7645203495589,13.2996544595209));
#48049=CARTESIAN_POINT('Ctrl Pts',(-2.5,33.7644650054088,13.3000000004374));
#48050=CARTESIAN_POINT('Origin',(0.,70.2,13.3));
#48051=CARTESIAN_POINT('',(-2.5,31.5805533683886,13.3));
#48052=CARTESIAN_POINT('',(-2.5,32.7902304403868,13.2999999999969));
#48053=CARTESIAN_POINT('',(-2.5,70.2,13.3));
#48054=CARTESIAN_POINT('',(-2.49999995188264,32.7902949052944,13.2995095035349));
#48055=CARTESIAN_POINT('Ctrl Pts',(-2.5,32.7902304403868,13.2999999999938));
#48056=CARTESIAN_POINT('Ctrl Pts',(-2.5,32.7902519286456,13.2998365014727));
#48057=CARTESIAN_POINT('Ctrl Pts',(-2.49999998396094,32.790273416948,13.2996730026523));
#48058=CARTESIAN_POINT('Ctrl Pts',(-2.49999995188264,32.7902949052944,13.2995095035349));
#48059=CARTESIAN_POINT('Ctrl Pts',(-2.49999995188264,32.7902949052944,13.2995095035349));
#48060=CARTESIAN_POINT('Ctrl Pts',(-2.49995240028355,32.8221483810988,13.0571448711518));
#48061=CARTESIAN_POINT('Ctrl Pts',(-2.46465984246264,32.8540041982013,12.816068610491));
#48062=CARTESIAN_POINT('Ctrl Pts',(-2.32238072864385,32.9193046319804,12.3401911228632));
#48063=CARTESIAN_POINT('Ctrl Pts',(-2.21276418048508,32.9521513730157,12.1090455123802));
#48064=CARTESIAN_POINT('Ctrl Pts',(-1.98020768498113,33.006334104292,11.7655545297637));
#48065=CARTESIAN_POINT('Ctrl Pts',(-1.87766845540534,33.0272937485804,11.6416550501174));
#48066=CARTESIAN_POINT('Ctrl Pts',(-1.52704079262838,33.0917878030711,11.2925311818988));
#48067=CARTESIAN_POINT('Ctrl Pts',(-1.24517172042504,33.1344194555062,11.1065199284851));
#48068=CARTESIAN_POINT('Ctrl Pts',(-0.630070992392071,33.2202889134947,
10.8584509285913));
#48069=CARTESIAN_POINT('Ctrl Pts',(-0.303762911995021,33.2620942606438,
10.7968205077297));
#48070=CARTESIAN_POINT('Ctrl Pts',(0.187332606069724,33.3251398722849,10.8017566523966));
#48071=CARTESIAN_POINT('Ctrl Pts',(0.348996910087456,33.3459397449376,10.8191703724959));
#48072=CARTESIAN_POINT('Ctrl Pts',(0.664335829411573,33.387218306528,10.8845900060884));
#48073=CARTESIAN_POINT('Ctrl Pts',(0.81737129877269,33.4075566807512,10.9319932162142));
#48074=CARTESIAN_POINT('Ctrl Pts',(1.25742166181102,33.4683358412982,11.1160863738191));
#48075=CARTESIAN_POINT('Ctrl Pts',(1.52406886358301,33.5084599627421,11.2930584250303));
#48076=CARTESIAN_POINT('Ctrl Pts',(1.87026155311123,33.5700005219807,11.6325905227454));
#48077=CARTESIAN_POINT('Ctrl Pts',(1.97788978347042,33.5911737889312,11.7617909008723));
#48078=CARTESIAN_POINT('Ctrl Pts',(2.16206369501838,33.6328179738398,12.0344926036629));
#48079=CARTESIAN_POINT('Ctrl Pts',(2.23920647585614,33.6531855465169,12.1766193944784));
#48080=CARTESIAN_POINT('Ctrl Pts',(2.43239537442833,33.7157885259535,12.6328533288876));
#48081=CARTESIAN_POINT('Ctrl Pts',(2.49969166971146,33.7573544465519,12.9635536918305));
#48082=CARTESIAN_POINT('Ctrl Pts',(2.50014741199627,33.8195433266639,13.4591576360897));
#48083=CARTESIAN_POINT('Ctrl Pts',(2.48465459633391,33.8397376209209,13.6202531452103));
#48084=CARTESIAN_POINT('Ctrl Pts',(2.42211976875742,33.8805988150891,13.9407768108108));
#48085=CARTESIAN_POINT('Ctrl Pts',(2.37452790699005,33.9011689958892,14.0992990967107));
#48086=CARTESIAN_POINT('Ctrl Pts',(2.19228714425991,33.9608547969121,14.5418310691081));
#48087=CARTESIAN_POINT('Ctrl Pts',(2.01945451037192,33.9995052285358,14.8066797884993));
#48088=CARTESIAN_POINT('Ctrl Pts',(1.58391383992079,34.0775164844838,15.2596927499158));
#48089=CARTESIAN_POINT('Ctrl Pts',(1.32469161326571,34.1161183192664,15.4434535509518));
#48090=CARTESIAN_POINT('Ctrl Pts',(0.899137327357358,34.1737421130743,15.6377148221355));
#48091=CARTESIAN_POINT('Ctrl Pts',(0.754576004154566,34.1924985381063,15.6882993059959));
#48092=CARTESIAN_POINT('Ctrl Pts',(0.282164411263705,34.2524777834034,15.8063949038974));
#48093=CARTESIAN_POINT('Ctrl Pts',(-0.0549778219401599,34.2933479375769,
15.8216347394788));
#48094=CARTESIAN_POINT('Ctrl Pts',(-0.691583271603203,34.3719565762885,
15.722374142115));
#48095=CARTESIAN_POINT('Ctrl Pts',(-0.986475161246398,34.4091519823723,
15.617986030409));
#48096=CARTESIAN_POINT('Ctrl Pts',(-1.39323446843087,34.4663353644852,15.3819557310794));
#48097=CARTESIAN_POINT('Ctrl Pts',(-1.52370245446907,34.4857341309826,15.2884612938777));
#48098=CARTESIAN_POINT('Ctrl Pts',(-1.87205302472696,34.5415566079259,14.9842837313462));
#48099=CARTESIAN_POINT('Ctrl Pts',(-2.06183036897234,34.5772281284375,14.7457728306188));
#48100=CARTESIAN_POINT('Ctrl Pts',(-2.30778850546009,34.6397836339721,14.2859659798799));
#48101=CARTESIAN_POINT('Ctrl Pts',(-2.38529276680687,34.6662730588992,14.0799959682308));
#48102=CARTESIAN_POINT('Ctrl Pts',(-2.47816977164688,34.7154661110473,13.6808400840174));
#48103=CARTESIAN_POINT('Ctrl Pts',(-2.49999999999718,34.7380489073261,13.490747126747));
#48104=CARTESIAN_POINT('Ctrl Pts',(-2.5,34.7604761263292,13.3000000000369));
#48105=CARTESIAN_POINT('Ctrl Pts',(-2.5,33.7644650054088,13.3000000004374));
#48106=CARTESIAN_POINT('Ctrl Pts',(-2.4999999999464,33.7153957113629,13.6063638855109));
#48107=CARTESIAN_POINT('Ctrl Pts',(-2.44368938266213,33.6656454075914,13.910106766958));
#48108=CARTESIAN_POINT('Ctrl Pts',(-2.21520576547411,33.564932618596,14.5051916857309));
#48109=CARTESIAN_POINT('Ctrl Pts',(-2.03631438537295,33.5165219282223,14.7876816829902));
#48110=CARTESIAN_POINT('Ctrl Pts',(-1.69586182941511,33.4416766566087,15.1439416871495));
#48111=CARTESIAN_POINT('Ctrl Pts',(-1.57326960941569,33.4170237337179,15.2495862741076));
#48112=CARTESIAN_POINT('Ctrl Pts',(-1.17765250647787,33.3433430490473,15.5287443851009));
#48113=CARTESIAN_POINT('Ctrl Pts',(-0.880372849210694,33.296682342617,15.6620372307967));
#48114=CARTESIAN_POINT('Ctrl Pts',(-0.279274251402382,33.2058518380004,
15.8017106718201));
#48115=CARTESIAN_POINT('Ctrl Pts',(0.0168121393118554,33.1620765047058,
15.8171997900144));
#48116=CARTESIAN_POINT('Ctrl Pts',(0.641313157754923,33.0712966323003,15.7394663225526));
#48117=CARTESIAN_POINT('Ctrl Pts',(0.962123178563746,33.0266430018552,15.6316683128468));
#48118=CARTESIAN_POINT('Ctrl Pts',(1.53954873039134,32.932613714711,15.2974942144722));
#48119=CARTESIAN_POINT('Ctrl Pts',(1.79078766198862,32.8842420694693,15.0756968961085));
#48120=CARTESIAN_POINT('Ctrl Pts',(2.15514357154332,32.7969098596996,14.5956735449823));
#48121=CARTESIAN_POINT('Ctrl Pts',(2.28282776823589,32.759670062764,14.354628345475));
#48122=CARTESIAN_POINT('Ctrl Pts',(2.4729474163009,32.6784787274333,13.7898674555445));
#48123=CARTESIAN_POINT('Ctrl Pts',(2.51557744964497,32.6342540481868,13.4649562364397));
#48124=CARTESIAN_POINT('Ctrl Pts',(2.47995562827711,32.5556969889572,12.9058187599586));
#48125=CARTESIAN_POINT('Ctrl Pts',(2.43177343336691,32.5225404605207,12.6738279384654));
#48126=CARTESIAN_POINT('Ctrl Pts',(2.23800089721952,32.4448361464276,12.1364434811551));
#48127=CARTESIAN_POINT('Ctrl Pts',(2.06184068356837,32.402177883595,11.8469117299882));
#48128=CARTESIAN_POINT('Ctrl Pts',(1.73529844227031,32.3388144619718,11.4945361283964));
#48129=CARTESIAN_POINT('Ctrl Pts',(1.62786594145866,32.3196130685598,11.3971066779723));
#48130=CARTESIAN_POINT('Ctrl Pts',(1.31029737764301,32.2662806417064,11.1557759168687));
#48131=CARTESIAN_POINT('Ctrl Pts',(1.08569358158453,32.2320848347257,11.0337551651984));
#48132=CARTESIAN_POINT('Ctrl Pts',(0.531515737620487,32.1542676034036,10.8343171576283));
#48133=CARTESIAN_POINT('Ctrl Pts',(0.196842924385133,32.1120083433719,10.7853584650124));
#48134=CARTESIAN_POINT('Ctrl Pts',(-0.461181655561167,32.0264406794179,
10.821622218201));
#48135=CARTESIAN_POINT('Ctrl Pts',(-0.778228279605227,31.9840742082586,
10.9022175787181));
#48136=CARTESIAN_POINT('Ctrl Pts',(-1.32925164818711,31.9039851167018,11.1634697123731));
#48137=CARTESIAN_POINT('Ctrl Pts',(-1.56462668003421,31.8673414757141,11.3292957303027));
#48138=CARTESIAN_POINT('Ctrl Pts',(-2.00164294062796,31.7881785799826,11.7658744169739));
#48139=CARTESIAN_POINT('Ctrl Pts',(-2.18738722022867,31.7462406606404,12.0448226268867));
#48140=CARTESIAN_POINT('Ctrl Pts',(-2.39981857799535,31.6748115287023,12.5631252680941));
#48141=CARTESIAN_POINT('Ctrl Pts',(-2.45706011617239,31.6458531802989,12.7852356558965));
#48142=CARTESIAN_POINT('Ctrl Pts',(-2.49446628917762,31.6047725711507,13.1078128589546));
#48143=CARTESIAN_POINT('Ctrl Pts',(-2.5,31.592645110597,13.2039632545006));
#48144=CARTESIAN_POINT('Ctrl Pts',(-2.5,31.5805533683886,13.3));
#48145=CARTESIAN_POINT('Origin',(0.,70.2,13.3));
#48146=CARTESIAN_POINT('',(-2.5,29.7319333905705,13.3000000001788));
#48147=CARTESIAN_POINT('',(-2.5,30.448807333626,13.3000000006354));
#48148=CARTESIAN_POINT('',(-2.5,70.2,13.3));
#48149=CARTESIAN_POINT('',(-2.41619328710391,30.5123559175791,12.6571443227054));
#48150=CARTESIAN_POINT('Ctrl Pts',(-2.5,30.448807333626,13.3000000012709));
#48151=CARTESIAN_POINT('Ctrl Pts',(-2.50000000000077,30.4489575841864,13.2984814139764));
#48152=CARTESIAN_POINT('Ctrl Pts',(-2.49999861633713,30.44910781596,13.296962776412));
#48153=CARTESIAN_POINT('Ctrl Pts',(-2.49960317435266,30.4705706394413,13.0799691528022));
#48154=CARTESIAN_POINT('Ctrl Pts',(-2.47135580135003,30.4912362366712,12.8654425703387));
#48155=CARTESIAN_POINT('Ctrl Pts',(-2.41594587876447,30.5121662090965,12.6571893662353));
#48156=CARTESIAN_POINT('Ctrl Pts',(-2.41596675694296,30.5129552114539,12.6572678401181));
#48157=CARTESIAN_POINT('Ctrl Pts',(-2.35883570065213,30.5579490103612,12.4425178378573));
#48158=CARTESIAN_POINT('Ctrl Pts',(-2.27321578263186,30.6017824679034,12.2360288065908));
#48159=CARTESIAN_POINT('Ctrl Pts',(-2.03034648356656,30.6959711890914,11.8182291397699));
#48160=CARTESIAN_POINT('Ctrl Pts',(-1.8649380824931,30.7435817971013,11.6147117438818));
#48161=CARTESIAN_POINT('Ctrl Pts',(-1.45539675357328,30.8428791817054,11.2468160020568));
#48162=CARTESIAN_POINT('Ctrl Pts',(-1.20787754103791,30.8949023392902,11.0920196522197));
#48163=CARTESIAN_POINT('Ctrl Pts',(-0.788006455920246,30.9719008770198,
10.9218486067175));
#48164=CARTESIAN_POINT('Ctrl Pts',(-0.63129322644735,30.9989402025191,10.8755278268355));
#48165=CARTESIAN_POINT('Ctrl Pts',(-0.178217409132333,31.0759719317503,
10.7885867984338));
#48166=CARTESIAN_POINT('Ctrl Pts',(0.12259188344298,31.1253819066478,10.7852127441113));
#48167=CARTESIAN_POINT('Ctrl Pts',(0.723397487068334,31.2229670801232,10.8868619627879));
#48168=CARTESIAN_POINT('Ctrl Pts',(1.0174897166744,31.2727323769274,10.9953785562771));
#48169=CARTESIAN_POINT('Ctrl Pts',(1.56565074144212,31.3730652390623,11.3235365952355));
#48170=CARTESIAN_POINT('Ctrl Pts',(1.81140516656008,31.4219926386856,11.5459640358851));
#48171=CARTESIAN_POINT('Ctrl Pts',(2.19957391636242,31.521484104347,12.0687255044085));
#48172=CARTESIAN_POINT('Ctrl Pts',(2.34002909556593,31.5686955342603,12.3627017477311));
#48173=CARTESIAN_POINT('Ctrl Pts',(2.4602863448112,31.6402516341769,12.8287423804406));
#48174=CARTESIAN_POINT('Ctrl Pts',(2.4851996441707,31.663869639399,12.9855466181158));
#48175=CARTESIAN_POINT('Ctrl Pts',(2.50484045220785,31.7101713974724,13.2990052299316));
#48176=CARTESIAN_POINT('Ctrl Pts',(2.50004895457153,31.7325424902078,13.454913080661));
#48177=CARTESIAN_POINT('Ctrl Pts',(2.44110198011629,31.8009338979227,13.9275255961028));
#48178=CARTESIAN_POINT('Ctrl Pts',(2.3405993722713,31.8470542945225,14.2350953317938));
#48179=CARTESIAN_POINT('Ctrl Pts',(2.10419900918666,31.9162678744218,14.6600701426085));
#48180=CARTESIAN_POINT('Ctrl Pts',(2.00947244171977,31.9396073417861,14.7964860932594));
#48181=CARTESIAN_POINT('Ctrl Pts',(1.80342469173612,31.984661762764,15.0380166791454));
#48182=CARTESIAN_POINT('Ctrl Pts',(1.69458950358715,32.0062405195487,15.1442917715027));
#48183=CARTESIAN_POINT('Ctrl Pts',(1.31558573532985,32.0751809920567,15.4523304182481));
#48184=CARTESIAN_POINT('Ctrl Pts',(1.01421234932664,32.1199351068297,15.6097030337364));
#48185=CARTESIAN_POINT('Ctrl Pts',(0.391317781425657,32.2092432847418,15.7887469780546));
#48186=CARTESIAN_POINT('Ctrl Pts',(0.0785247633640879,32.252953579236,15.8181103920361));
#48187=CARTESIAN_POINT('Ctrl Pts',(-0.546924064232225,32.3381654307809,
15.7599040893123));
#48188=CARTESIAN_POINT('Ctrl Pts',(-0.853786134377966,32.3796765152074,
15.670938715195));
#48189=CARTESIAN_POINT('Ctrl Pts',(-1.27216140957349,32.4435156246173,15.457544710545));
#48190=CARTESIAN_POINT('Ctrl Pts',(-1.40174397850272,32.4644165128666,15.3756941824833));
#48191=CARTESIAN_POINT('Ctrl Pts',(-1.79011033114316,32.5309848591934,15.0773391212701));
#48192=CARTESIAN_POINT('Ctrl Pts',(-2.01300226423329,32.5745482626543,14.8202983121113));
#48193=CARTESIAN_POINT('Ctrl Pts',(-2.27863241584907,32.6466534912303,14.3486333228143));
#48194=CARTESIAN_POINT('Ctrl Pts',(-2.35671875589441,32.674078384212,14.158872179394));
#48195=CARTESIAN_POINT('Ctrl Pts',(-2.43854709728563,32.7155475527714,13.8607628203475));
#48196=CARTESIAN_POINT('Ctrl Pts',(-2.45989829234932,32.7295296661982,13.7581195672206));
#48197=CARTESIAN_POINT('Ctrl Pts',(-2.49156059793428,32.7590875296406,13.5370395037512));
#48198=CARTESIAN_POINT('Ctrl Pts',(-2.50000000000029,32.7746433674768,13.4185979467541));
#48199=CARTESIAN_POINT('Ctrl Pts',(-2.5,32.7902304403868,13.2999999999938));
#48200=CARTESIAN_POINT('',(-2.44274579319255,29.8383352895022,12.7680192277667));
#48201=CARTESIAN_POINT('Ctrl Pts',(-2.5,31.5805533683886,13.3));
#48202=CARTESIAN_POINT('Ctrl Pts',(-2.5,31.5506182064355,13.5377552779758));
#48203=CARTESIAN_POINT('Ctrl Pts',(-2.46608138989822,31.5208908684004,13.7748126054976));
#48204=CARTESIAN_POINT('Ctrl Pts',(-2.3224560244815,31.4570145149412,14.2642743785868));
#48205=CARTESIAN_POINT('Ctrl Pts',(-2.20417068662367,31.4233278057136,14.5104835825318));
#48206=CARTESIAN_POINT('Ctrl Pts',(-1.96504908934518,31.3713635771709,14.8523702419768));
#48207=CARTESIAN_POINT('Ctrl Pts',(-1.87115731336049,31.3532641804217,14.9643449271175));
#48208=CARTESIAN_POINT('Ctrl Pts',(-1.53143566875036,31.2936439297573,15.3041707551186));
#48209=CARTESIAN_POINT('Ctrl Pts',(-1.24967697024499,31.2527810574749,15.4909700005104));
#48210=CARTESIAN_POINT('Ctrl Pts',(-0.791686143764384,31.1923366036486,
15.6766929896363));
#48211=CARTESIAN_POINT('Ctrl Pts',(-0.638487345656817,31.1729425655691,
15.7223486650582));
#48212=CARTESIAN_POINT('Ctrl Pts',(-0.153681305777879,31.1127336090979,
15.8176030120288));
#48213=CARTESIAN_POINT('Ctrl Pts',(0.18427798926919,31.0722886438412,15.8155551435562));
#48214=CARTESIAN_POINT('Ctrl Pts',(0.82724309823683,30.9930546284602,15.6810741364213));
#48215=CARTESIAN_POINT('Ctrl Pts',(1.12696643462638,30.9549073499603,15.5547293621554));
#48216=CARTESIAN_POINT('Ctrl Pts',(1.52834837377316,30.8968574597102,15.284988228244));
#48217=CARTESIAN_POINT('Ctrl Pts',(1.65323449378781,30.8775727856828,15.1822459501393));
#48218=CARTESIAN_POINT('Ctrl Pts',(1.97721053338203,30.8231076043594,14.8584214110551));
#48219=CARTESIAN_POINT('Ctrl Pts',(2.14807252545898,30.7887054516615,14.612955152419));
#48220=CARTESIAN_POINT('Ctrl Pts',(2.41157262967143,30.7146758787045,14.0391347690649));
#48221=CARTESIAN_POINT('Ctrl Pts',(2.4887639286759,30.6754036010154,13.7100013568907));
#48222=CARTESIAN_POINT('Ctrl Pts',(2.50847350276491,30.5998361580507,13.0569670529847));
#48223=CARTESIAN_POINT('Ctrl Pts',(2.45712207088327,30.5639610449962,12.7395873638693));
#48224=CARTESIAN_POINT('Ctrl Pts',(2.29226579615131,30.5086627346294,12.2893613178293));
#48225=CARTESIAN_POINT('Ctrl Pts',(2.22250570281706,30.4901721477675,12.1439936308391));
#48226=CARTESIAN_POINT('Ctrl Pts',(1.98595694320881,30.4381312283265,11.7528292756899));
#48227=CARTESIAN_POINT('Ctrl Pts',(1.78880799060941,30.4055961401458,11.5285710061412));
#48228=CARTESIAN_POINT('Ctrl Pts',(1.29567724061902,30.335366437808,11.1360292397398));
#48229=CARTESIAN_POINT('Ctrl Pts',(0.995280930003226,30.2977913317661,10.9824515185561));
#48230=CARTESIAN_POINT('Ctrl Pts',(0.369242818520919,30.2268328407032,10.8073091330423));
#48231=CARTESIAN_POINT('Ctrl Pts',(0.0515386662844847,30.1936491795691,
10.780635095682));
#48232=CARTESIAN_POINT('Ctrl Pts',(-0.422449236165706,30.1417762105348,
10.8307212083397));
#48233=CARTESIAN_POINT('Ctrl Pts',(-0.580209343291639,30.1243368263708,
10.8629585586074));
#48234=CARTESIAN_POINT('Ctrl Pts',(-1.01411771751827,30.0758692849208,10.9961875778601));
#48235=CARTESIAN_POINT('Ctrl Pts',(-1.27712883285776,30.0461467858501,11.1309054093261));
#48236=CARTESIAN_POINT('Ctrl Pts',(-1.76443951752628,29.9832950364743,11.5005321456237));
#48237=CARTESIAN_POINT('Ctrl Pts',(-1.97903053815114,29.9498157858136,11.7396043951434));
#48238=CARTESIAN_POINT('Ctrl Pts',(-2.28346040715123,29.8906119947612,12.2463451969034));
#48239=CARTESIAN_POINT('Ctrl Pts',(-2.38470555547828,29.8648554638372,12.5015201389497));
#48240=CARTESIAN_POINT('Ctrl Pts',(-2.44274382522039,29.8383396165347,12.7680201090758));
#48241=CARTESIAN_POINT('Ctrl Pts',(-2.44274339219816,29.8383270426146,12.7680181207295));
#48242=CARTESIAN_POINT('Ctrl Pts',(-2.48077087610663,29.8022369430543,12.9426319349569));
#48243=CARTESIAN_POINT('Ctrl Pts',(-2.5000000000256,29.7670454411236,13.1210333618124));
#48244=CARTESIAN_POINT('Ctrl Pts',(-2.5,29.7319333905705,13.3000000003577));
#48245=CARTESIAN_POINT('Origin',(0.,70.2,13.3));
#48246=CARTESIAN_POINT('',(-2.5,27.4053098230045,13.3));
#48247=CARTESIAN_POINT('',(-2.5,28.6199701874195,13.3));
#48248=CARTESIAN_POINT('',(-2.5,70.2,13.3));
#48249=CARTESIAN_POINT('Ctrl Pts',(-2.5,28.6199701874195,13.3));
#48250=CARTESIAN_POINT('Ctrl Pts',(-2.5,28.6327850846717,13.1995694455431));
#48251=CARTESIAN_POINT('Ctrl Pts',(-2.49394822593413,28.6455754439869,13.099168590211));
#48252=CARTESIAN_POINT('Ctrl Pts',(-2.44160871681871,28.7009645375733,12.667115103329));
#48253=CARTESIAN_POINT('Ctrl Pts',(-2.33505473222711,28.74301621687,12.3462931500924));
#48254=CARTESIAN_POINT('Ctrl Pts',(-2.0887767410183,28.8052671422129,11.9170053410973));
#48255=CARTESIAN_POINT('Ctrl Pts',(-1.99588660153722,28.8253117141221,11.7860308127951));
#48256=CARTESIAN_POINT('Ctrl Pts',(-1.69523827910462,28.8828718345511,11.4383228954246));
#48257=CARTESIAN_POINT('Ctrl Pts',(-1.46025075558902,28.9199670416504,11.248815829488));
#48258=CARTESIAN_POINT('Ctrl Pts',(-0.903055295997165,28.9990247628022,
10.9448178848108));
#48259=CARTESIAN_POINT('Ctrl Pts',(-0.579421184943894,29.0402572049479,
10.8450663466309));
#48260=CARTESIAN_POINT('Ctrl Pts',(0.0606219893681992,29.1194799559106,
10.7818460006969));
#48261=CARTESIAN_POINT('Ctrl Pts',(0.369979936040267,29.1567920006692,10.8084305372208));
#48262=CARTESIAN_POINT('Ctrl Pts',(0.822222547126219,29.2139591251509,10.9335724612474));
#48263=CARTESIAN_POINT('Ctrl Pts',(0.97319420288676,29.2335108787594,10.9915528541699));
#48264=CARTESIAN_POINT('Ctrl Pts',(1.39774412380091,29.2908761978435,11.2037082359193));
#48265=CARTESIAN_POINT('Ctrl Pts',(1.64916020085886,29.3279518382367,11.3951634380007));
#48266=CARTESIAN_POINT('Ctrl Pts',(2.08210185327466,29.4059694258053,11.8764558751));
#48267=CARTESIAN_POINT('Ctrl Pts',(2.2535003910037,29.4467100927564,12.1671386423894));
#48268=CARTESIAN_POINT('Ctrl Pts',(2.4334189338219,29.5127017915693,12.6873944491853));
#48269=CARTESIAN_POINT('Ctrl Pts',(2.47730682558507,29.5380696035329,12.9002386381054));
#48270=CARTESIAN_POINT('Ctrl Pts',(2.51603813060199,29.5989771498109,13.4253962642545));
#48271=CARTESIAN_POINT('Ctrl Pts',(2.48110270569015,29.633552990786,13.7361971275792));
#48272=CARTESIAN_POINT('Ctrl Pts',(2.29169115542339,29.7088734894859,14.3541469058951));
#48273=CARTESIAN_POINT('Ctrl Pts',(2.12930782728746,29.7498210900781,14.6524344251759));
#48274=CARTESIAN_POINT('Ctrl Pts',(1.70138660914546,29.8279664515823,15.1609502155387));
#48275=CARTESIAN_POINT('Ctrl Pts',(1.44241546598459,29.8642537873569,15.3682085169965));
#48276=CARTESIAN_POINT('Ctrl Pts',(0.883153410916181,29.9325135829285,15.6581312915006));
#48277=CARTESIAN_POINT('Ctrl Pts',(0.593026387910101,29.9646864238788,15.7472409506213));
#48278=CARTESIAN_POINT('Ctrl Pts',(0.00496183693252068,30.0335247045431,
15.8168814390696));
#48279=CARTESIAN_POINT('Ctrl Pts',(-0.287967281520161,30.0680860885775,
15.8003800463128));
#48280=CARTESIAN_POINT('Ctrl Pts',(-0.79284965984856,30.1264004927931,15.6818239179714));
#48281=CARTESIAN_POINT('Ctrl Pts',(-1.00616018060319,30.1506349362041,15.5998780356437));
#48282=CARTESIAN_POINT('Ctrl Pts',(-1.48968121580609,30.2073677980581,15.3337274573262));
#48283=CARTESIAN_POINT('Ctrl Pts',(-1.74062594994233,30.2388038452988,15.1235751313124));
#48284=CARTESIAN_POINT('Ctrl Pts',(-2.15310079120443,30.3081217889657,14.6131348029968));
#48285=CARTESIAN_POINT('Ctrl Pts',(-2.30830094586534,30.3432598643754,14.3158862160448));
#48286=CARTESIAN_POINT('Ctrl Pts',(-2.46661710644016,30.4015756208221,13.770528762688));
#48287=CARTESIAN_POINT('Ctrl Pts',(-2.49999999988009,30.4254695360297,13.5358758796161));
#48288=CARTESIAN_POINT('Ctrl Pts',(-2.5,30.448807333626,13.3000000012709));
#48289=CARTESIAN_POINT('Ctrl Pts',(-2.5,29.7319333905705,13.3000000003576));
#48290=CARTESIAN_POINT('Ctrl Pts',(-2.49999999999996,29.7318724014283,13.3003108629132));
#48291=CARTESIAN_POINT('Ctrl Pts',(-2.49999994201859,29.7318114131336,13.3006217272935));
#48292=CARTESIAN_POINT('Ctrl Pts',(-2.49992634709586,29.6931068287105,13.4979073586275));
#48293=CARTESIAN_POINT('Ctrl Pts',(-2.47657528164387,29.6551154971477,13.6944516803843));
#48294=CARTESIAN_POINT('Ctrl Pts',(-2.35749764558954,29.5612157236652,14.1878924096993));
#48295=CARTESIAN_POINT('Ctrl Pts',(-2.22913470602397,29.505152474325,14.4736075773388));
#48296=CARTESIAN_POINT('Ctrl Pts',(-1.87105042885647,29.3939564136642,14.9879505733476));
#48297=CARTESIAN_POINT('Ctrl Pts',(-1.64281712267107,29.342397653508,15.2108512677702));
#48298=CARTESIAN_POINT('Ctrl Pts',(-1.1269215969022,29.2390225684145,15.5519316550608));
#48299=CARTESIAN_POINT('Ctrl Pts',(-0.846842233456649,29.1899952735646,
15.6715463120526));
#48300=CARTESIAN_POINT('Ctrl Pts',(-0.263669061310278,29.0946429065696,
15.8035750830613));
#48301=CARTESIAN_POINT('Ctrl Pts',(0.0341682228858632,29.0479609796295,
15.8172273448508));
#48302=CARTESIAN_POINT('Ctrl Pts',(0.491552894477325,28.9772728325731,15.7567720659131));
#48303=CARTESIAN_POINT('Ctrl Pts',(0.652981496791188,28.9523472598469,15.7188807557228));
#48304=CARTESIAN_POINT('Ctrl Pts',(1.09540754359596,28.8812282410761,15.5674649124578));
#48305=CARTESIAN_POINT('Ctrl Pts',(1.36130807796902,28.8353943496751,15.4185541470391));
#48306=CARTESIAN_POINT('Ctrl Pts',(1.83478909242976,28.7442973576672,15.0265806192441));
#48307=CARTESIAN_POINT('Ctrl Pts',(2.0359310493986,28.6978925545718,14.7840879845139));
#48308=CARTESIAN_POINT('Ctrl Pts',(2.34830557372873,28.6033966060118,14.2198427337845));
#48309=CARTESIAN_POINT('Ctrl Pts',(2.44977186980247,28.5566680886389,13.8994781141711));
#48310=CARTESIAN_POINT('Ctrl Pts',(2.52090137313357,28.4614182876343,13.2412808606137));
#48311=CARTESIAN_POINT('Ctrl Pts',(2.4912780919575,28.4158350410216,12.9101392951487));
#48312=CARTESIAN_POINT('Ctrl Pts',(2.35311566499084,28.3467208032282,12.4406601037354));
#48313=CARTESIAN_POINT('Ctrl Pts',(2.2932870118741,28.3240422256198,12.2918060807117));
#48314=CARTESIAN_POINT('Ctrl Pts',(2.06784326620615,28.2551238723809,11.8567887198095));
#48315=CARTESIAN_POINT('Ctrl Pts',(1.85954218222959,28.2102858168898,11.5967688571649));
#48316=CARTESIAN_POINT('Ctrl Pts',(1.35616587493274,28.1193380800673,11.1744937106368));
#48317=CARTESIAN_POINT('Ctrl Pts',(1.06675019950998,28.0754186435454,11.0154737842077));
#48318=CARTESIAN_POINT('Ctrl Pts',(0.60145295222266,28.0088892395113,10.868095770466));
#48319=CARTESIAN_POINT('Ctrl Pts',(0.443683528899947,27.9869020518249,10.8344271189726));
#48320=CARTESIAN_POINT('Ctrl Pts',(-0.0485706254989859,27.9195187716889,
10.7781879926998));
#48321=CARTESIAN_POINT('Ctrl Pts',(-0.385198572893466,27.8754074883351,
10.8073008578459));
#48322=CARTESIAN_POINT('Ctrl Pts',(-1.0166541538013,27.78673226523,10.9932276430615));
#48323=CARTESIAN_POINT('Ctrl Pts',(-1.3065173121412,27.7441862595109,11.1441144621935));
#48324=CARTESIAN_POINT('Ctrl Pts',(-1.80263394475705,27.6598205243732,11.5401044371508));
#48325=CARTESIAN_POINT('Ctrl Pts',(-2.00739589880486,27.6186293346373,11.7777936323127));
#48326=CARTESIAN_POINT('Ctrl Pts',(-2.32165701290964,27.5359838132377,12.3203420891319));
#48327=CARTESIAN_POINT('Ctrl Pts',(-2.42677007441428,27.4946455660611,12.6213064538359));
#48328=CARTESIAN_POINT('Ctrl Pts',(-2.4909986315093,27.4372189377818,13.0551428443414));
#48329=CARTESIAN_POINT('Ctrl Pts',(-2.5,27.4212781500521,13.1775175349232));
#48330=CARTESIAN_POINT('Ctrl Pts',(-2.5,27.4053098230045,13.3));
#48331=CARTESIAN_POINT('Origin',(0.,70.2,13.3));
#48332=CARTESIAN_POINT('',(-2.5,25.4505462844759,13.3));
#48333=CARTESIAN_POINT('',(-2.49999999999832,26.3929871638855,13.3));
#48334=CARTESIAN_POINT('',(-2.5,70.2,13.3));
#48335=CARTESIAN_POINT('',(-2.49999988262115,26.3931137665368,13.2992339097816));
#48336=CARTESIAN_POINT('Ctrl Pts',(-2.49999999999832,26.3929871638855,13.3));
#48337=CARTESIAN_POINT('Ctrl Pts',(-2.49999999999943,26.3930293663056,13.2997446371823));
#48338=CARTESIAN_POINT('Ctrl Pts',(-2.4999999608739,26.3930715671874,13.2994892737731));
#48339=CARTESIAN_POINT('Ctrl Pts',(-2.49999988262115,26.3931137665368,13.2992339097816));
#48340=CARTESIAN_POINT('Ctrl Pts',(-2.49999988262115,26.3931137665368,13.2992339097816));
#48341=CARTESIAN_POINT('Ctrl Pts',(-2.49990861043225,26.4423341093278,13.0013832701664));
#48342=CARTESIAN_POINT('Ctrl Pts',(-2.44659790091214,26.4898005592029,12.7058762675489));
#48343=CARTESIAN_POINT('Ctrl Pts',(-2.23996167708881,26.5875207226236,12.1516598654052));
#48344=CARTESIAN_POINT('Ctrl Pts',(-2.08974477813341,26.6360141905069,11.8966669489459));
#48345=CARTESIAN_POINT('Ctrl Pts',(-1.6917835838025,26.7326629013295,11.4321538623161));
#48346=CARTESIAN_POINT('Ctrl Pts',(-1.44078604149619,26.7819002676501,11.2323362820651));
#48347=CARTESIAN_POINT('Ctrl Pts',(-1.015987975505,26.8558398436871,11.0100557996151));
#48348=CARTESIAN_POINT('Ctrl Pts',(-0.865990378075362,26.8802140053644,
10.9492231009399));
#48349=CARTESIAN_POINT('Ctrl Pts',(-0.418968433668596,26.9508198986062,
10.8165866801885));
#48350=CARTESIAN_POINT('Ctrl Pts',(-0.113339936063998,26.9971554395426,
10.7840304409995));
#48351=CARTESIAN_POINT('Ctrl Pts',(0.351552396105956,27.0663728142287,10.819586160685));
#48352=CARTESIAN_POINT('Ctrl Pts',(0.510927143312623,27.0898813569698,10.8474471574717));
#48353=CARTESIAN_POINT('Ctrl Pts',(0.985496692595052,27.1618019364457,10.978722957087));
#48354=CARTESIAN_POINT('Ctrl Pts',(1.28382526795159,27.2097588689324,11.1294336485431));
#48355=CARTESIAN_POINT('Ctrl Pts',(1.77152336191823,27.2996259194926,11.5124608521681));
#48356=CARTESIAN_POINT('Ctrl Pts',(1.9662366539096,27.3416973668749,11.7291580730582));
#48357=CARTESIAN_POINT('Ctrl Pts',(2.29722266389161,27.4300086449687,12.2583692666568));
#48358=CARTESIAN_POINT('Ctrl Pts',(2.41596305661392,27.4732030838945,12.5751265719609));
#48359=CARTESIAN_POINT('Ctrl Pts',(2.51589625545696,27.5588168204824,13.2014270989334));
#48360=CARTESIAN_POINT('Ctrl Pts',(2.50961776146324,27.6002749760034,13.5026508389486));
#48361=CARTESIAN_POINT('Ctrl Pts',(2.39653289185163,27.6820069025001,14.0619263683701));
#48362=CARTESIAN_POINT('Ctrl Pts',(2.29953697319745,27.7213531424566,14.3179062002621));
#48363=CARTESIAN_POINT('Ctrl Pts',(1.99999732415954,27.8040697449607,14.8349079818321));
#48364=CARTESIAN_POINT('Ctrl Pts',(1.78331977387523,27.8466332134415,15.0821014183643));
#48365=CARTESIAN_POINT('Ctrl Pts',(1.39631904103432,27.9120465077539,15.3800858519101));
#48366=CARTESIAN_POINT('Ctrl Pts',(1.2580409952468,27.9337803836223,15.4665177116332));
#48367=CARTESIAN_POINT('Ctrl Pts',(0.820833682891556,27.9990181836344,15.6837341729523));
#48368=CARTESIAN_POINT('Ctrl Pts',(0.503813621442931,28.042340383823,15.7702504394689));
#48369=CARTESIAN_POINT('Ctrl Pts',(0.0177717747247502,28.1072010320218,
15.8051654697502));
#48370=CARTESIAN_POINT('Ctrl Pts',(-0.144337122208285,28.128478756645,15.8010687342534));
#48371=CARTESIAN_POINT('Ctrl Pts',(-0.620476810429327,28.1916648307116,
15.7425570502418));
#48372=CARTESIAN_POINT('Ctrl Pts',(-0.925775051887367,28.2332994033375,
15.6439372786663));
#48373=CARTESIAN_POINT('Ctrl Pts',(-1.34993803306391,28.2965893237324,15.4107457519792));
#48374=CARTESIAN_POINT('Ctrl Pts',(-1.48714088271485,28.3181478216139,15.3164316668437));
#48375=CARTESIAN_POINT('Ctrl Pts',(-1.73994854041058,28.3612382589392,15.1027168173146));
#48376=CARTESIAN_POINT('Ctrl Pts',(-1.85507293998218,28.3826618023661,14.9840175525638));
#48377=CARTESIAN_POINT('Ctrl Pts',(-2.16547247099176,28.4474831044656,14.5932015067003));
#48378=CARTESIAN_POINT('Ctrl Pts',(-2.31874752319724,28.4900088363419,14.2925147860756));
#48379=CARTESIAN_POINT('Ctrl Pts',(-2.45168825657745,28.5537149303618,13.8150600852883));
#48380=CARTESIAN_POINT('Ctrl Pts',(-2.47982687888544,28.5744064397878,13.6557030345326));
#48381=CARTESIAN_POINT('Ctrl Pts',(-2.49746876000698,28.6033840922305,13.4299158608522));
#48382=CARTESIAN_POINT('Ctrl Pts',(-2.5,28.6116823732052,13.3649517323781));
#48383=CARTESIAN_POINT('Ctrl Pts',(-2.5,28.6199701874195,13.3));
#48384=CARTESIAN_POINT('Ctrl Pts',(-2.5,27.4053098230045,13.3));
#48385=CARTESIAN_POINT('Ctrl Pts',(-2.5,27.3996223211976,13.3436250609951));
#48386=CARTESIAN_POINT('Ctrl Pts',(-2.49885811801832,27.3939321052226,13.3872638958897));
#48387=CARTESIAN_POINT('Ctrl Pts',(-2.48810867827697,27.3671441573085,13.5923251578246));
#48388=CARTESIAN_POINT('Ctrl Pts',(-2.46400345374254,27.3460475310011,13.7525747338723));
#48389=CARTESIAN_POINT('Ctrl Pts',(-2.34310063192789,27.2812148409896,14.2336317514487));
#48390=CARTESIAN_POINT('Ctrl Pts',(-2.19737174054802,27.2384858740639,14.5382961866477));
#48391=CARTESIAN_POINT('Ctrl Pts',(-1.90040500245466,27.1746169454776,14.9320791795483));
#48392=CARTESIAN_POINT('Ctrl Pts',(-1.79291441677868,27.1540661780335,15.0494804302878));
#48393=CARTESIAN_POINT('Ctrl Pts',(-1.42695493726365,27.0904234463954,15.3797729942216));
#48394=CARTESIAN_POINT('Ctrl Pts',(-1.13649652588632,27.048062452115,15.5516773622605));
#48395=CARTESIAN_POINT('Ctrl Pts',(-0.504581222342047,26.962137241801,15.7713369552786));
#48396=CARTESIAN_POINT('Ctrl Pts',(-0.169414111429522,26.9199158989573,
15.816631373289));
#48397=CARTESIAN_POINT('Ctrl Pts',(0.324975605872016,26.8567752480209,15.7839854355352));
#48398=CARTESIAN_POINT('Ctrl Pts',(0.483838868790364,26.8363454752803,15.757985874583));
#48399=CARTESIAN_POINT('Ctrl Pts',(0.797157813576045,26.7951411273092,15.6751348315224));
#48400=CARTESIAN_POINT('Ctrl Pts',(0.950731445552928,26.7744856242565,15.6179385623772));
#48401=CARTESIAN_POINT('Ctrl Pts',(1.37226598561706,26.7150874730926,15.4119486729574));
#48402=CARTESIAN_POINT('Ctrl Pts',(1.61999029041852,26.6766916919098,15.2284933504146));
#48403=CARTESIAN_POINT('Ctrl Pts',(1.94066653337549,26.6174474021038,14.8845758973231));
#48404=CARTESIAN_POINT('Ctrl Pts',(2.04071530886955,26.59681630124,14.753461742974));
#48405=CARTESIAN_POINT('Ctrl Pts',(2.20962028042095,26.556438896401,14.4799210111295));
#48406=CARTESIAN_POINT('Ctrl Pts',(2.27932506639292,26.5367862509454,14.3389005299839));
#48407=CARTESIAN_POINT('Ctrl Pts',(2.45445007565042,26.4752981207319,13.8805474580364));
#48408=CARTESIAN_POINT('Ctrl Pts',(2.50994679852911,26.4340547773478,13.5480890627087));
#48409=CARTESIAN_POINT('Ctrl Pts',(2.49323279542962,26.373164809232,13.0593982211623));
#48410=CARTESIAN_POINT('Ctrl Pts',(2.47348700883369,26.3538962325488,12.9050796679274));
#48411=CARTESIAN_POINT('Ctrl Pts',(2.37643390160687,26.2986820783243,12.4717657912131));
#48412=CARTESIAN_POINT('Ctrl Pts',(2.26494625460606,26.2630987162367,12.2029826667315));
#48413=CARTESIAN_POINT('Ctrl Pts',(1.94239856320779,26.1888780297846,11.6953858638462));
#48414=CARTESIAN_POINT('Ctrl Pts',(1.72676095872817,26.1508557958496,11.4653333277888));
#48415=CARTESIAN_POINT('Ctrl Pts',(1.34324621327224,26.0923901785833,11.1852820823339));
#48416=CARTESIAN_POINT('Ctrl Pts',(1.20315502230001,26.0724675564974,11.1025550276125));
#48417=CARTESIAN_POINT('Ctrl Pts',(0.793578013645412,26.0171259806383,10.9116792885689));
#48418=CARTESIAN_POINT('Ctrl Pts',(0.511845809783451,25.9822894612031,10.8358824036639));
#48419=CARTESIAN_POINT('Ctrl Pts',(-0.11131845983581,25.9063581622406,10.7799688051623));
#48420=CARTESIAN_POINT('Ctrl Pts',(-0.448711406021424,25.8656000665261,
10.8177372412971));
#48421=CARTESIAN_POINT('Ctrl Pts',(-1.0651316616425,25.7874832580424,11.0168796619845));
#48422=CARTESIAN_POINT('Ctrl Pts',(-1.34119636797327,25.7507366285312,11.1673172008032));
#48423=CARTESIAN_POINT('Ctrl Pts',(-1.8118219336404,25.6773856466678,11.5521269243203));
#48424=CARTESIAN_POINT('Ctrl Pts',(-2.00605564565092,25.6418943480628,11.7789606147578));
#48425=CARTESIAN_POINT('Ctrl Pts',(-2.31304622677275,25.5703443722778,12.3020020390374));
#48426=CARTESIAN_POINT('Ctrl Pts',(-2.41889024678534,25.5349304284088,12.5963374116816));
#48427=CARTESIAN_POINT('Ctrl Pts',(-2.48939769060973,25.4823025486937,13.0341472013468));
#48428=CARTESIAN_POINT('Ctrl Pts',(-2.5,25.4663859015973,13.1670681074021));
#48429=CARTESIAN_POINT('Ctrl Pts',(-2.5,25.4505462844759,13.3));
#48430=CARTESIAN_POINT('Origin',(0.,70.2,13.3));
#48431=CARTESIAN_POINT('',(-2.5,20.4,13.3));
#48432=CARTESIAN_POINT('Origin',(0.,20.4,13.3));
#48433=CARTESIAN_POINT('',(-2.5,22.6116296396575,13.3));
#48434=CARTESIAN_POINT('',(-2.5,70.2,13.3));
#48435=CARTESIAN_POINT('',(-1.80813900541952,24.1372606373433,15.0222732043098));
#48436=CARTESIAN_POINT('Ctrl Pts',(-1.81028567158556,24.1386394120584,15.0242000427015));
#48437=CARTESIAN_POINT('Ctrl Pts',(-1.62817173955969,24.114723319155,15.2154065347429));
#48438=CARTESIAN_POINT('Ctrl Pts',(-1.41694756494607,24.0913164310824,15.3765297752926));
#48439=CARTESIAN_POINT('Ctrl Pts',(-0.924156731153752,24.0383425219184,
15.6416398587418));
#48440=CARTESIAN_POINT('Ctrl Pts',(-0.641172790021728,24.0088848798015,
15.7343752869735));
#48441=CARTESIAN_POINT('Ctrl Pts',(-0.191166389328545,23.964562234863,15.797746599409));
#48442=CARTESIAN_POINT('Ctrl Pts',(-0.0319733094634541,23.9491491640395,
15.804846138491));
#48443=CARTESIAN_POINT('Ctrl Pts',(0.455698514788413,23.9006726261604,15.7800780211352));
#48444=CARTESIAN_POINT('Ctrl Pts',(0.777988740413514,23.8663730008719,15.6985549214629));
#48445=CARTESIAN_POINT('Ctrl Pts',(1.35382716141607,23.800742079636,15.4242516057205));
#48446=CARTESIAN_POINT('Ctrl Pts',(1.60549250967171,23.7697041807392,15.2410467794464));
#48447=CARTESIAN_POINT('Ctrl Pts',(1.92940593611467,23.7197133936811,14.8981184132296));
#48448=CARTESIAN_POINT('Ctrl Pts',(2.02949951422288,23.702179261639,14.7689149942455));
#48449=CARTESIAN_POINT('Ctrl Pts',(2.20391056801833,23.6669594708688,14.4915814794044));
#48450=CARTESIAN_POINT('Ctrl Pts',(2.27755631464174,23.6495142844082,14.343947630229));
#48451=CARTESIAN_POINT('Ctrl Pts',(2.44621775174173,23.5988439045661,13.9013008857712));
#48452=CARTESIAN_POINT('Ctrl Pts',(2.50172957006313,23.565231912974,13.5946162156367));
#48453=CARTESIAN_POINT('Ctrl Pts',(2.49900670227979,23.5122570362497,13.1195226833282));
#48454=CARTESIAN_POINT('Ctrl Pts',(2.48149275392758,23.4938356230605,12.9538755101879));
#48455=CARTESIAN_POINT('Ctrl Pts',(2.38193024416109,23.4394766726213,12.474916242549));
#48456=CARTESIAN_POINT('Ctrl Pts',(2.25550934280905,23.4034286357378,12.174398566632));
#48457=CARTESIAN_POINT('Ctrl Pts',(1.98432892060312,23.3482906657723,11.7705675284845));
#48458=CARTESIAN_POINT('Ctrl Pts',(1.88010313594603,23.3297164904084,11.6441219062015));
#48459=CARTESIAN_POINT('Ctrl Pts',(1.53501053736421,23.2741269355648,11.3003825521099));
#48460=CARTESIAN_POINT('Ctrl Pts',(1.2635768739027,23.2371912876301,11.1187029053315));
#48461=CARTESIAN_POINT('Ctrl Pts',(0.813131910942001,23.1805658665522,10.930198570904));
#48462=CARTESIAN_POINT('Ctrl Pts',(0.655243673772007,23.1614154088171,10.8817787103818));
#48463=CARTESIAN_POINT('Ctrl Pts',(0.335914808662987,23.1234496792875,10.8174439251418));
#48464=CARTESIAN_POINT('Ctrl Pts',(0.175384440319663,23.1046854656622,10.8009685465805));
#48465=CARTESIAN_POINT('Ctrl Pts',(-0.149484151903419,23.066510887471,10.7990976992974));
#48466=CARTESIAN_POINT('Ctrl Pts',(-0.313053856599623,23.0471883356712,
10.8142706837244));
#48467=CARTESIAN_POINT('Ctrl Pts',(-0.632630036280473,23.0086964515106,
10.875975037635));
#48468=CARTESIAN_POINT('Ctrl Pts',(-0.787958017962882,22.9896045334834,
10.9219260723622));
#48469=CARTESIAN_POINT('Ctrl Pts',(-1.09086661666943,22.9507192196918,11.0444974717313));
#48470=CARTESIAN_POINT('Ctrl Pts',(-1.23745477480971,22.9310151443303,11.1214723932316));
#48471=CARTESIAN_POINT('Ctrl Pts',(-1.51078846884569,22.8918249036477,11.3015468741404));
#48472=CARTESIAN_POINT('Ctrl Pts',(-1.63719969881383,22.8724470716651,11.4037218918722));
#48473=CARTESIAN_POINT('Ctrl Pts',(-1.8708194044265,22.8330444106825,11.633440320949));
#48474=CARTESIAN_POINT('Ctrl Pts',(-1.97700117694386,22.8131109911634,11.7608938065539));
#48475=CARTESIAN_POINT('Ctrl Pts',(-2.16077650210772,22.7734586871545,12.0321850023688));
#48476=CARTESIAN_POINT('Ctrl Pts',(-2.23845920549876,22.7538585391541,12.1750079222615));
#48477=CARTESIAN_POINT('Ctrl Pts',(-2.36644648432654,22.7140011223799,12.4769529908112));
#48478=CARTESIAN_POINT('Ctrl Pts',(-2.41579438734412,22.693833981374,12.6356146637894));
#48479=CARTESIAN_POINT('Ctrl Pts',(-2.48301959290936,22.6528949202455,12.963569463533));
#48480=CARTESIAN_POINT('Ctrl Pts',(-2.5,22.6322916274191,13.1317725807118));
#48481=CARTESIAN_POINT('Ctrl Pts',(-2.5,22.6116296396575,13.3));
#48482=CARTESIAN_POINT('',(-2.49962956580465,24.4076684122549,13.3002239646526));
#48483=CARTESIAN_POINT('Ctrl Pts',(-1.80833658952121,24.1386090163582,15.0220712193704));
#48484=CARTESIAN_POINT('Ctrl Pts',(-1.81020050232586,24.1389337537035,15.0202577426898));
#48485=CARTESIAN_POINT('Ctrl Pts',(-1.81198682056181,24.1392454317471,15.0185145328336));
#48486=CARTESIAN_POINT('Ctrl Pts',(-1.81382907906759,24.1395965832126,15.0166507577355));
#48487=CARTESIAN_POINT('Ctrl Pts',(-1.84511374165097,24.1455597284942,14.9850007070546));
#48488=CARTESIAN_POINT('Ctrl Pts',(-1.87518987859362,24.1517791058518,14.9522286304461));
#48489=CARTESIAN_POINT('Ctrl Pts',(-1.90416092244935,24.1581166532201,14.9185705131251));
#48490=CARTESIAN_POINT('Ctrl Pts',(-1.93313196630509,24.1644542005884,14.8849123958042));
#48491=CARTESIAN_POINT('Ctrl Pts',(-1.96099824777268,24.170909918477,14.8503685507711));
#48492=CARTESIAN_POINT('Ctrl Pts',(-1.98790086801484,24.1773521102019,14.8151392463294));
#48493=CARTESIAN_POINT('Ctrl Pts',(-2.03641945626578,24.1889705341666,14.7516035720648));
#48494=CARTESIAN_POINT('Ctrl Pts',(-2.08181417555863,24.200546145274,14.6858324035231));
#48495=CARTESIAN_POINT('Ctrl Pts',(-2.12395119533515,24.2120525428482,14.6180120824061));
#48496=CARTESIAN_POINT('Ctrl Pts',(-2.12856658903148,24.2133128729597,14.6105835199632));
#48497=CARTESIAN_POINT('Ctrl Pts',(-2.13314288835672,24.2145723763142,14.6031303224517));
#48498=CARTESIAN_POINT('Ctrl Pts',(-2.13767990859671,24.215831020905,14.5956526976106));
#48499=CARTESIAN_POINT('Ctrl Pts',(-2.15006608266115,24.2192671508235,14.5752386024621));
#48500=CARTESIAN_POINT('Ctrl Pts',(-2.16215964544334,24.2226968046935,14.5546425496117));
#48501=CARTESIAN_POINT('Ctrl Pts',(-2.17395700753042,24.2261192080105,14.5338686059686));
#48502=CARTESIAN_POINT('Ctrl Pts',(-2.17398855418554,24.2261283596646,14.5338130555472));
#48503=CARTESIAN_POINT('Ctrl Pts',(-2.17402009872259,24.2261375112669,14.5337575038535));
#48504=CARTESIAN_POINT('Ctrl Pts',(-2.1740516411416,24.2261466628173,14.5337019508877));
#48505=CARTESIAN_POINT('Ctrl Pts',(-2.21384369734985,24.2376917193109,14.4636196044073));
#48506=CARTESIAN_POINT('Ctrl Pts',(-2.2502669318921,24.2491559865257,14.3915106216839));
#48507=CARTESIAN_POINT('Ctrl Pts',(-2.28317904319985,24.2605980621657,14.3176173417912));
#48508=CARTESIAN_POINT('Ctrl Pts',(-2.28618364083904,24.2616426269805,14.3108715097708));
#48509=CARTESIAN_POINT('Ctrl Pts',(-2.2891589413337,24.2626870039974,14.304110814845));
#48510=CARTESIAN_POINT('Ctrl Pts',(-2.29210481557446,24.2637312360772,14.2973354467699));
#48511=CARTESIAN_POINT('Ctrl Pts',(-2.3042995770904,24.2680539464643,14.2692880859167));
#48512=CARTESIAN_POINT('Ctrl Pts',(-2.31599047958798,24.2723740128452,14.2409893710612));
#48513=CARTESIAN_POINT('Ctrl Pts',(-2.32716887971432,24.2766938806141,14.2124532790457));
#48514=CARTESIAN_POINT('Ctrl Pts',(-2.35879787736297,24.2889168361322,14.1317111355313));
#48515=CARTESIAN_POINT('Ctrl Pts',(-2.38616662427351,24.3010794544928,14.0494696349969));
#48516=CARTESIAN_POINT('Ctrl Pts',(-2.4091989526512,24.3132214044725,13.9661006403656));
#48517=CARTESIAN_POINT('Ctrl Pts',(-2.43274903125694,24.3256362967821,13.8808575705093));
#48518=CARTESIAN_POINT('Ctrl Pts',(-2.45176516544558,24.3380294312079,13.794436431863));
#48519=CARTESIAN_POINT('Ctrl Pts',(-2.46616766170601,24.350418449224,13.7072287381561));
#48520=CARTESIAN_POINT('Ctrl Pts',(-2.46874290237542,24.3526336695908,13.6916355524016));
#48521=CARTESIAN_POINT('Ctrl Pts',(-2.47117064890133,24.354848699713,13.6760171874997));
#48522=CARTESIAN_POINT('Ctrl Pts',(-2.47345045763519,24.3570635663588,13.6603758326943));
#48523=CARTESIAN_POINT('Ctrl Pts',(-2.47346714033298,24.3570797738372,13.6602613757263));
#48524=CARTESIAN_POINT('Ctrl Pts',(-2.47348381510892,24.3570959813069,13.6601469175272));
#48525=CARTESIAN_POINT('Ctrl Pts',(-2.47350048196299,24.3571121887678,13.6600324580979));
#48526=CARTESIAN_POINT('Ctrl Pts',(-2.4862662866267,24.3695261260101,13.5723634409001));
#48527=CARTESIAN_POINT('Ctrl Pts',(-2.49438449435988,24.3819369045509,13.4839724022708));
#48528=CARTESIAN_POINT('Ctrl Pts',(-2.49778878735398,24.3943638978535,13.3952617518356));
#48529=CARTESIAN_POINT('Ctrl Pts',(-2.49900315849596,24.3987968247709,13.3636171037218));
#48530=CARTESIAN_POINT('Ctrl Pts',(-2.49961772539878,24.40323159877,13.3319317884665));
#48531=CARTESIAN_POINT('Ctrl Pts',(-2.49962956580465,24.4076684122549,13.3002239646526));
#48532=CARTESIAN_POINT('',(-2.5,23.6803207434639,13.2999999993226));
#48533=CARTESIAN_POINT('',(-2.5,70.2,13.3));
#48534=CARTESIAN_POINT('',(2.5,22.5894736842105,13.3));
#48535=CARTESIAN_POINT('Ctrl Pts',(-2.5,23.6803207434639,13.2999999986451));
#48536=CARTESIAN_POINT('Ctrl Pts',(-2.50000000012045,23.6459460095297,13.5222442475586));
#48537=CARTESIAN_POINT('Ctrl Pts',(-2.4704272669999,23.6147118780889,13.7432791390963));
#48538=CARTESIAN_POINT('Ctrl Pts',(-2.3411668218586,23.5475698736697,14.2171224251415));
#48539=CARTESIAN_POINT('Ctrl Pts',(-2.22919616600022,23.5115414052313,14.4631000178917));
#48540=CARTESIAN_POINT('Ctrl Pts',(-1.8996327770728,23.4265535877506,14.9575442480085));
#48541=CARTESIAN_POINT('Ctrl Pts',(-1.66787132558335,23.3772637209859,15.1904998765396));
#48542=CARTESIAN_POINT('Ctrl Pts',(-1.26623858292357,23.3051655955838,15.4614813800414));
#48543=CARTESIAN_POINT('Ctrl Pts',(-1.12590945121923,23.28207350758,15.5378087959533));
#48544=CARTESIAN_POINT('Ctrl Pts',(-0.670759057692837,23.2135390652347,
15.7315376323321));
#48545=CARTESIAN_POINT('Ctrl Pts',(-0.339085465467693,23.1703807948407,
15.7994976518128));
#48546=CARTESIAN_POINT('Ctrl Pts',(0.260693413184836,23.0884249977271,15.8003911170477));
#48547=CARTESIAN_POINT('Ctrl Pts',(0.523401695645916,23.0513739468048,15.7588333700899));
#48548=CARTESIAN_POINT('Ctrl Pts',(1.07592400691972,22.9690407659882,15.5787750078992));
#48549=CARTESIAN_POINT('Ctrl Pts',(1.35601979032557,22.9254268943002,15.4241211559787));
#48550=CARTESIAN_POINT('Ctrl Pts',(1.71964076389121,22.8625629124352,15.1213018488941));
#48551=CARTESIAN_POINT('Ctrl Pts',(1.82983196068492,22.8419598691273,15.0105592143298));
#48552=CARTESIAN_POINT('Ctrl Pts',(2.09969541621544,22.7849831730603,14.683219524228));
#48553=CARTESIAN_POINT('Ctrl Pts',(2.23591951817411,22.7480601948783,14.4500491783475));
#48554=CARTESIAN_POINT('Ctrl Pts',(2.4431562272875,22.6693975947776,13.9128451862319));
#48555=CARTESIAN_POINT('Ctrl Pts',(2.5,22.6291961383663,13.6078280522502));
#48556=CARTESIAN_POINT('Ctrl Pts',(2.5,22.5894736842105,13.3));
#48557=CARTESIAN_POINT('',(2.5,21.6105263157895,13.3));
#48558=CARTESIAN_POINT('',(2.5,70.2,13.3));
#48559=CARTESIAN_POINT('Ctrl Pts',(-2.5,22.6116296396575,13.3));
#48560=CARTESIAN_POINT('Ctrl Pts',(-2.5,22.5924668561326,13.4560210787061));
#48561=CARTESIAN_POINT('Ctrl Pts',(-2.48539461222184,22.573251129917,13.6120627591118));
#48562=CARTESIAN_POINT('Ctrl Pts',(-2.39559058063777,22.5137915737753,14.08533547675));
#48563=CARTESIAN_POINT('Ctrl Pts',(-2.27333684123802,22.4739041219184,14.3897338451193));
#48564=CARTESIAN_POINT('Ctrl Pts',(-2.00865809026983,22.4134356942506,14.7970497810158));
#48565=CARTESIAN_POINT('Ctrl Pts',(-1.90822223056209,22.3934222341015,14.9231293121602));
#48566=CARTESIAN_POINT('Ctrl Pts',(-1.56687450718985,22.3319591699888,15.2758048587272));
#48567=CARTESIAN_POINT('Ctrl Pts',(-1.29268689868116,22.2908032340347,15.4651410527906));
#48568=CARTESIAN_POINT('Ctrl Pts',(-0.685592003802375,22.207364289261,15.7268534999989));
#48569=CARTESIAN_POINT('Ctrl Pts',(-0.358483890929012,22.1657797807692,
15.7962212509069));
#48570=CARTESIAN_POINT('Ctrl Pts',(0.285301823842494,22.0839647725545,15.8032769734437));
#48571=CARTESIAN_POINT('Ctrl Pts',(0.595840871907412,22.0445506619614,15.7480029313275));
#48572=CARTESIAN_POINT('Ctrl Pts',(1.18942160917842,21.9625008959697,15.5224287666394));
#48573=CARTESIAN_POINT('Ctrl Pts',(1.46579069100765,21.9209040823827,15.3507018085121));
#48574=CARTESIAN_POINT('Ctrl Pts',(1.94023559772861,21.8372435214935,14.9097617920686));
#48575=CARTESIAN_POINT('Ctrl Pts',(2.13296587506391,21.7954326514263,14.6439509026954));
#48576=CARTESIAN_POINT('Ctrl Pts',(2.34055789893654,21.7293522534676,14.1947481054972));
#48577=CARTESIAN_POINT('Ctrl Pts',(2.39587212153975,21.7065664559455,14.0338850769603));
#48578=CARTESIAN_POINT('Ctrl Pts',(2.47798344621124,21.65870920032,13.6823585884458));
#48579=CARTESIAN_POINT('Ctrl Pts',(2.5,21.6338674213799,13.4915574323461));
#48580=CARTESIAN_POINT('Ctrl Pts',(2.5,21.6105263157895,13.3));
#48581=CARTESIAN_POINT('Origin',(0.,70.2,13.3));
#48582=CARTESIAN_POINT('',(-2.48616900737713,26.3471379964276,13.5677880585459));
#48583=CARTESIAN_POINT('Ctrl Pts',(-2.49999999183544,24.407511587746,13.3002020465273));
#48584=CARTESIAN_POINT('Ctrl Pts',(-2.50001929365448,24.4409600114742,13.0613731584544));
#48585=CARTESIAN_POINT('Ctrl Pts',(-2.4658149491821,24.4741969076914,12.8237123231116));
#48586=CARTESIAN_POINT('Ctrl Pts',(-2.32581088600144,24.5421763645029,12.3477731262211));
#48587=CARTESIAN_POINT('Ctrl Pts',(-2.21560394886077,24.5768594070736,12.1137297679167));
#48588=CARTESIAN_POINT('Ctrl Pts',(-1.89787935016659,24.6546455782246,11.6433680242041));
#48589=CARTESIAN_POINT('Ctrl Pts',(-1.67769222506848,24.6973385022906,11.4207048187397));
#48590=CARTESIAN_POINT('Ctrl Pts',(-1.15201874668985,24.7840059525177,11.057030208371));
#48591=CARTESIAN_POINT('Ctrl Pts',(-0.847361079951804,24.827088526998,10.9251047770606));
#48592=CARTESIAN_POINT('Ctrl Pts',(-0.230843896234704,24.9107769898447,
10.7924564888713));
#48593=CARTESIAN_POINT('Ctrl Pts',(0.0732732684954316,24.950611137483,10.7829118544294));
#48594=CARTESIAN_POINT('Ctrl Pts',(0.532590161893144,25.0114370647908,10.8519798196951));
#48595=CARTESIAN_POINT('Ctrl Pts',(0.690703404405739,25.0324978888,10.8918071137798));
#48596=CARTESIAN_POINT('Ctrl Pts',(1.15528571238928,25.0964821783083,11.0583958715576));
#48597=CARTESIAN_POINT('Ctrl Pts',(1.4414980794328,25.1389826087854,11.2308055265104));
#48598=CARTESIAN_POINT('Ctrl Pts',(1.92198551185649,25.223124277075,11.6695862848393));
#48599=CARTESIAN_POINT('Ctrl Pts',(2.11460790562612,25.2636010545971,11.9285915123811));
#48600=CARTESIAN_POINT('Ctrl Pts',(2.32321013274833,25.3248334163836,12.3625507451866));
#48601=CARTESIAN_POINT('Ctrl Pts',(2.37894021841261,25.345293614433,12.514656051798));
#48602=CARTESIAN_POINT('Ctrl Pts',(2.46120545611504,25.3866200083521,12.8311493730713));
#48603=CARTESIAN_POINT('Ctrl Pts',(2.48682722270015,25.4074006379551,12.9949608230336));
#48604=CARTESIAN_POINT('Ctrl Pts',(2.5146917357811,25.4699403728579,13.4921372592396));
#48605=CARTESIAN_POINT('Ctrl Pts',(2.46686591915056,25.511042430498,13.8246000050189));
#48606=CARTESIAN_POINT('Ctrl Pts',(2.24500666145808,25.5931180216562,14.4482024106216));
#48607=CARTESIAN_POINT('Ctrl Pts',(2.07441443456947,25.6333128364487,14.7336211164078));
#48608=CARTESIAN_POINT('Ctrl Pts',(1.62923400751575,25.7144980886799,15.22539808679));
#48609=CARTESIAN_POINT('Ctrl Pts',(1.35768468883391,25.7547972660912,15.4256294544487));
#48610=CARTESIAN_POINT('Ctrl Pts',(0.908665683530526,25.8145327190637,15.6345890718155));
#48611=CARTESIAN_POINT('Ctrl Pts',(0.756292207196053,25.8338400953433,15.6883061057311));
#48612=CARTESIAN_POINT('Ctrl Pts',(0.275664118819158,25.8931857081566,15.8070887356835));
#48613=CARTESIAN_POINT('Ctrl Pts',(-0.0613030305722818,25.9326969470317,
15.821463648482));
#48614=CARTESIAN_POINT('Ctrl Pts',(-0.552179682928576,25.9912737049207,
15.7437011244677));
#48615=CARTESIAN_POINT('Ctrl Pts',(-0.710322241437892,26.0103394186011,
15.7025035173479));
#48616=CARTESIAN_POINT('Ctrl Pts',(-1.16853457910079,26.0676155842894,15.5338957579576));
#48617=CARTESIAN_POINT('Ctrl Pts',(-1.44895659615568,26.1052630866398,15.3630913338774));
#48618=CARTESIAN_POINT('Ctrl Pts',(-1.80006889063422,26.1600137487588,15.0414130139519));
#48619=CARTESIAN_POINT('Ctrl Pts',(-1.90187043698653,26.1772366660204,14.9296189547623));
#48620=CARTESIAN_POINT('Ctrl Pts',(-2.1337701667803,26.2212635145788,14.6234103165689));
#48621=CARTESIAN_POINT('Ctrl Pts',(-2.24788012884225,26.247838143168,14.4186815080764));
#48622=CARTESIAN_POINT('Ctrl Pts',(-2.41059213792532,26.2987657420784,13.9975960829663));
#48623=CARTESIAN_POINT('Ctrl Pts',(-2.46225581692207,26.3229414940952,13.7846677762047));
#48624=CARTESIAN_POINT('Ctrl Pts',(-2.48562243203351,26.3472602063278,13.5677333101648));
#48625=CARTESIAN_POINT('Ctrl Pts',(-2.48561657000623,26.3478373019899,13.5677877273336));
#48626=CARTESIAN_POINT('Ctrl Pts',(-2.49040728835277,26.355511883304,13.5233200849104));
#48627=CARTESIAN_POINT('Ctrl Pts',(-2.49400562263312,26.3631210348639,13.4787161189908));
#48628=CARTESIAN_POINT('Ctrl Pts',(-2.49880070726847,26.3781627629798,13.3893975884711));
#48629=CARTESIAN_POINT('Ctrl Pts',(-2.49999999980375,26.3855985398547,13.3447078590484));
#48630=CARTESIAN_POINT('Ctrl Pts',(-2.49999999999832,26.3929871638855,13.3));
#48631=CARTESIAN_POINT('',(-0.790532179204624,24.1655288633479,10.9282793432527));
#48632=CARTESIAN_POINT('Ctrl Pts',(-2.5,25.4505462844759,13.3));
#48633=CARTESIAN_POINT('Ctrl Pts',(-2.5,25.4346615266009,13.4333107304046));
#48634=CARTESIAN_POINT('Ctrl Pts',(-2.48933645207011,25.4188567362605,13.5666328076926));
#48635=CARTESIAN_POINT('Ctrl Pts',(-2.42324395792347,25.3702827392235,13.9757840738102));
#48636=CARTESIAN_POINT('Ctrl Pts',(-2.33212866227708,25.3385997000097,14.2433969388235));
#48637=CARTESIAN_POINT('Ctrl Pts',(-2.03959957204297,25.2680868661861,14.7836982679379));
#48638=CARTESIAN_POINT('Ctrl Pts',(-1.82362150819777,25.2286776131871,15.0423330092833));
#48639=CARTESIAN_POINT('Ctrl Pts',(-1.34493833058986,25.158314656507,15.4258879748345));
#48640=CARTESIAN_POINT('Ctrl Pts',(-1.09880443934562,25.1276257097723,15.562945456558));
#48641=CARTESIAN_POINT('Ctrl Pts',(-0.520730508196071,25.0593035631249,
15.7678037619262));
#48642=CARTESIAN_POINT('Ctrl Pts',(-0.187326421714155,25.0206568083071,
15.8151734986127));
#48643=CARTESIAN_POINT('Ctrl Pts',(0.420421962637397,24.9526566181903,15.7797283299768));
#48644=CARTESIAN_POINT('Ctrl Pts',(0.690769551352685,24.923533803137,15.7184075514967));
#48645=CARTESIAN_POINT('Ctrl Pts',(1.25685316725015,24.8582398111244,15.4870726759433));
#48646=CARTESIAN_POINT('Ctrl Pts',(1.53911953807666,24.8204500228646,15.2985012375989));
#48647=CARTESIAN_POINT('Ctrl Pts',(1.87845471199616,24.7683199088682,14.9561215064622));
#48648=CARTESIAN_POINT('Ctrl Pts',(1.971999279987,24.7529354255617,14.8435579696091));
#48649=CARTESIAN_POINT('Ctrl Pts',(2.243464174008,24.7037507866139,14.4516079119598));
#48650=CARTESIAN_POINT('Ctrl Pts',(2.37593068207173,24.6709951528344,14.1451326843892));
#48651=CARTESIAN_POINT('Ctrl Pts',(2.50416688031434,24.6057570862472,13.5442892572167));
#48652=CARTESIAN_POINT('Ctrl Pts',(2.51574993528651,24.576384292556,13.2585326566879));
#48653=CARTESIAN_POINT('Ctrl Pts',(2.43724795843491,24.5175853955505,12.6563871696382));
#48654=CARTESIAN_POINT('Ctrl Pts',(2.3337649705917,24.4882695828866,12.3471343843325));
#48655=CARTESIAN_POINT('Ctrl Pts',(2.09644986008896,24.4402255726524,11.9289542677213));
#48656=CARTESIAN_POINT('Ctrl Pts',(2.00579234730328,24.424462288069,11.7994361632438));
#48657=CARTESIAN_POINT('Ctrl Pts',(1.72843745579795,24.3834881852855,11.4736835393712));
#48658=CARTESIAN_POINT('Ctrl Pts',(1.52123163852952,24.3602284421505,11.297780355606));
#48659=CARTESIAN_POINT('Ctrl Pts',(1.00429900121169,24.3097657542319,10.9864742600211));
#48660=CARTESIAN_POINT('Ctrl Pts',(0.687370774496695,24.279429585749,10.8733916016535));
#48661=CARTESIAN_POINT('Ctrl Pts',(0.149164509496832,24.2330693451276,10.7955685681763));
#48662=CARTESIAN_POINT('Ctrl Pts',(-0.0624686035915402,24.2167113037373,
10.7918886621725));
#48663=CARTESIAN_POINT('Ctrl Pts',(-0.448560379140616,24.189229973862,10.834181355582));
#48664=CARTESIAN_POINT('Ctrl Pts',(-0.622284832998793,24.1777142215037,
10.8721998294773));
#48665=CARTESIAN_POINT('Ctrl Pts',(-0.790532179204627,24.1655288633479,
10.9282793432527));
#48666=CARTESIAN_POINT('',(-0.830840037653311,24.1597523284343,10.9410233051414));
#48667=CARTESIAN_POINT('Ctrl Pts',(-0.831036541944574,24.1603152340113,
10.940719093145));
#48668=CARTESIAN_POINT('Ctrl Pts',(-0.817567384401107,24.1620535629164,
10.9364517239282));
#48669=CARTESIAN_POINT('Ctrl Pts',(-0.804065260568294,24.1637914392606,
10.9323052309739));
#48670=CARTESIAN_POINT('Ctrl Pts',(-0.790532179204624,24.1655288633479,
10.9282793432527));
#48671=CARTESIAN_POINT('',(-2.49999972384016,23.6805025116397,13.2988249259027));
#48672=CARTESIAN_POINT('Ctrl Pts',(-0.830274846070968,24.1581332823986,
10.9418982888811));
#48673=CARTESIAN_POINT('Ctrl Pts',(-1.02912308992684,24.1232364201349,11.0119116790078));
#48674=CARTESIAN_POINT('Ctrl Pts',(-1.21842442783496,24.0883981669736,11.1068342240936));
#48675=CARTESIAN_POINT('Ctrl Pts',(-1.64597028965375,24.0073058843925,11.3939124963739));
#48676=CARTESIAN_POINT('Ctrl Pts',(-1.86507159543317,23.9652828488002,11.6076765519296));
#48677=CARTESIAN_POINT('Ctrl Pts',(-2.19064207469752,23.8826599052698,12.0677436289267));
#48678=CARTESIAN_POINT('Ctrl Pts',(-2.30650255866757,23.8431942411814,12.3014188211821));
#48679=CARTESIAN_POINT('Ctrl Pts',(-2.46088053508975,23.7614727519614,12.791239366162));
#48680=CARTESIAN_POINT('Ctrl Pts',(-2.49988005997949,23.7198878942854,13.0442370498513));
#48681=CARTESIAN_POINT('Ctrl Pts',(-2.49999972384016,23.6805025116397,13.2988249259027));
#48682=CARTESIAN_POINT('Ctrl Pts',(-2.49999972384016,23.6805025116397,13.2988249259027));
#48683=CARTESIAN_POINT('Ctrl Pts',(-2.49999990949688,23.6804414057986,13.2992199152432));
#48684=CARTESIAN_POINT('Ctrl Pts',(-2.49999999999979,23.6803818355265,13.2996050178555));
#48685=CARTESIAN_POINT('Ctrl Pts',(-2.5,23.6803207434639,13.2999999986451));
#48686=CARTESIAN_POINT('Origin',(1.6,144.5,10.3));
#48687=CARTESIAN_POINT('',(1.6,144.5,14.5));
#48688=CARTESIAN_POINT('',(1.6,144.5,12.1));
#48689=CARTESIAN_POINT('Origin',(0.,144.5,13.3));
#48690=CARTESIAN_POINT('',(1.6,144.5,10.3));
#48691=CARTESIAN_POINT('Origin',(1.6,136.,16.3));
#48692=CARTESIAN_POINT('',(1.6,136.,12.1));
#48693=CARTESIAN_POINT('',(1.6,136.,14.5));
#48694=CARTESIAN_POINT('Origin',(0.,136.,13.3));
#48695=CARTESIAN_POINT('',(1.6,136.,16.3));
#48696=CARTESIAN_POINT('Origin',(1.6,140.25,13.3));
#48697=CARTESIAN_POINT('',(1.6,132.35,14.5));
#48698=CARTESIAN_POINT('',(1.6,132.35,12.1));
#48699=CARTESIAN_POINT('Origin',(2.26918997026575,118.064918569113,12.5575400117452));
#48700=CARTESIAN_POINT('',(1.73940833428499,117.962536543046,12.7139827773687));
#48701=CARTESIAN_POINT('',(1.73940833428499,117.962536543046,12.7139827773687));
#48702=CARTESIAN_POINT('',(1.95209195497481,118.519715684653,12.6482782748721));
#48703=CARTESIAN_POINT('',(1.95209195497481,118.519715684653,12.6482782748721));
#48704=CARTESIAN_POINT('',(2.90531341659142,118.445890165984,12.3682449948735));
#48705=CARTESIAN_POINT('Ctrl Pts',(2.95532532744321,114.524755006807,12.5175939454839));
#48706=CARTESIAN_POINT('Ctrl Pts',(3.06876373495539,114.584537551976,12.9831594433255));
#48707=CARTESIAN_POINT('Ctrl Pts',(3.06785527722985,114.700312831601,13.9338767019519));
#48708=CARTESIAN_POINT('Ctrl Pts',(2.25534968607699,114.926403080468,15.609150838537));
#48709=CARTESIAN_POINT('Ctrl Pts',(0.0662652269878777,115.200811352631,
16.6410423398491));
#48710=CARTESIAN_POINT('Ctrl Pts',(-2.50595963339538,115.52278944504,15.4068000621842));
#48711=CARTESIAN_POINT('Ctrl Pts',(-2.937218093367,115.738804616394,13.546395210328));
#48712=CARTESIAN_POINT('Ctrl Pts',(-2.71348433299149,115.85500608334,12.6424604110653));
#48713=CARTESIAN_POINT('Ctrl Pts',(-2.65350431190029,115.880786019828,12.4447186453377));
#48714=CARTESIAN_POINT('Ctrl Pts',(-2.51956517014225,115.925788602732,12.1093992582891));
#48715=CARTESIAN_POINT('Ctrl Pts',(-2.14456329762995,116.015344903557,11.4921752961234));
#48716=CARTESIAN_POINT('Ctrl Pts',(-1.50208232786518,116.116660442079,10.9634323628369));
#48717=CARTESIAN_POINT('Ctrl Pts',(-0.743705841514237,116.216924112424,
10.6832072795712));
#48718=CARTESIAN_POINT('Ctrl Pts',(0.0519424989325072,116.316482211687,
10.5766342196015));
#48719=CARTESIAN_POINT('Ctrl Pts',(1.04279822899032,116.439601730527,10.7807965086205));
#48720=CARTESIAN_POINT('Ctrl Pts',(1.9954829094094,116.58519875718,11.5039772484606));
#48721=CARTESIAN_POINT('Ctrl Pts',(2.53561723147412,116.728640862891,12.5517410043371));
#48722=CARTESIAN_POINT('Ctrl Pts',(2.5694900167613,116.869918400196,13.7111768527204));
#48723=CARTESIAN_POINT('Ctrl Pts',(2.05742503005493,117.024497486579,14.8738134954349));
#48724=CARTESIAN_POINT('Ctrl Pts',(0.930701672170671,117.191464070288,15.7005591366327));
#48725=CARTESIAN_POINT('Ctrl Pts',(-0.562095627157725,117.369822261529,
15.7584322387535));
#48726=CARTESIAN_POINT('Ctrl Pts',(-1.59617390811852,117.515351376341,15.1152935972272));
#48727=CARTESIAN_POINT('Ctrl Pts',(-2.03359602972292,117.615626970315,14.4308327626405));
#48728=CARTESIAN_POINT('Ctrl Pts',(-2.17011759536166,117.665364077208,14.0554925009457));
#48729=CARTESIAN_POINT('Ctrl Pts',(-2.21671921699844,117.690134597954,13.8624602176105));
#48730=CARTESIAN_POINT('Ctrl Pts',(-2.23459322200071,117.702496092692,13.7650534213741));
#48731=CARTESIAN_POINT('Ctrl Pts',(-2.24324088520118,117.709552710981,13.7091809472188));
#48732=CARTESIAN_POINT('Ctrl Pts',(-2.30787845616854,117.769500502143,13.233386793593));
#48733=CARTESIAN_POINT('Ctrl Pts',(-2.14259558128388,117.882889231505,12.2973265421649));
#48734=CARTESIAN_POINT('Ctrl Pts',(-1.26569931155285,118.03312163484,11.395784096862));
#48735=CARTESIAN_POINT('Ctrl Pts',(-0.207382758034273,118.167589041999,
11.0848752646015));
#48736=CARTESIAN_POINT('Ctrl Pts',(0.756408994557853,118.286006106533,11.2469230615091));
#48737=CARTESIAN_POINT('Ctrl Pts',(1.56745847087833,118.40662964019,11.8126008815501));
#48738=CARTESIAN_POINT('Ctrl Pts',(1.86831064635946,118.484468543414,12.35991743902));
#48739=CARTESIAN_POINT('Ctrl Pts',(1.96892768266466,118.526537502283,12.703608403237));
#48740=CARTESIAN_POINT('Ctrl Pts',(2.7669220611078,114.591352155898,12.5327846010662));
#48741=CARTESIAN_POINT('Ctrl Pts',(2.87674269859879,114.647538874759,12.9695240152525));
#48742=CARTESIAN_POINT('Ctrl Pts',(2.88232355626827,114.756241528531,13.8620584078666));
#48743=CARTESIAN_POINT('Ctrl Pts',(2.13221229569936,114.968135572939,15.4375130757603));
#48744=CARTESIAN_POINT('Ctrl Pts',(0.0926580189939055,115.224683159866,
16.4162364195046));
#48745=CARTESIAN_POINT('Ctrl Pts',(-2.31360202512171,115.524901307596,15.2827271366528));
#48746=CARTESIAN_POINT('Ctrl Pts',(-2.72779167000299,115.725916081504,13.5548349021305));
#48747=CARTESIAN_POINT('Ctrl Pts',(-2.52648386507752,115.833973569872,12.712701434762));
#48748=CARTESIAN_POINT('Ctrl Pts',(-2.4721874848677,115.85794478792,12.5284078779757));
#48749=CARTESIAN_POINT('Ctrl Pts',(-2.35016956426982,115.899786125458,12.2156840563554));
#48750=CARTESIAN_POINT('Ctrl Pts',(-2.00623455037881,115.98303414384,11.6392046808839));
#48751=CARTESIAN_POINT('Ctrl Pts',(-1.41325953841494,116.077182179787,11.1431032941946));
#48752=CARTESIAN_POINT('Ctrl Pts',(-0.71088717098477,116.170336542424,10.8769908864139));
#48753=CARTESIAN_POINT('Ctrl Pts',(0.0273902380339246,116.262830174928,
10.7718808932291));
#48754=CARTESIAN_POINT('Ctrl Pts',(0.949387253166724,116.377212890765,10.9538151649334));
#48755=CARTESIAN_POINT('Ctrl Pts',(1.84025305635243,116.512506445318,11.6181657831876));
#48756=CARTESIAN_POINT('Ctrl Pts',(2.35077936414752,116.645857799176,12.5876989105077));
#48757=CARTESIAN_POINT('Ctrl Pts',(2.39183470744452,116.777286985799,13.6658663168934));
#48758=CARTESIAN_POINT('Ctrl Pts',(1.92487206745958,116.921229337443,14.7525882984064));
#48759=CARTESIAN_POINT('Ctrl Pts',(0.881632553648049,117.076924480568,15.5331978841402));
#48760=CARTESIAN_POINT('Ctrl Pts',(-0.512501371025649,117.24359289046,15.6006921262506));
#48761=CARTESIAN_POINT('Ctrl Pts',(-1.48703573917562,117.379936763826,15.0078964255291));
#48762=CARTESIAN_POINT('Ctrl Pts',(-1.90403082779443,117.474103647466,14.3692654859918));
#48763=CARTESIAN_POINT('Ctrl Pts',(-2.03581316980885,117.520865644744,14.0176944890301));
#48764=CARTESIAN_POINT('Ctrl Pts',(-2.08143067211384,117.544169556656,13.8365532081328));
#48765=CARTESIAN_POINT('Ctrl Pts',(-2.09914966879132,117.555803332789,13.7450628668842));
#48766=CARTESIAN_POINT('Ctrl Pts',(-2.10780582026366,117.562445575008,13.6925603576404));
#48767=CARTESIAN_POINT('Ctrl Pts',(-2.17304406469775,117.618882305616,13.2453208704162));
#48768=CARTESIAN_POINT('Ctrl Pts',(-2.02647430250429,117.725837543343,12.360927019113));
#48769=CARTESIAN_POINT('Ctrl Pts',(-1.20558819876245,117.868088734324,11.4984595098835));
#48770=CARTESIAN_POINT('Ctrl Pts',(-0.202110281410913,117.996018243275,
11.1919879778851));
#48771=CARTESIAN_POINT('Ctrl Pts',(0.717727730873791,118.108870229896,11.3359284262728));
#48772=CARTESIAN_POINT('Ctrl Pts',(1.50313989498709,118.224745568758,11.8710949030945));
#48773=CARTESIAN_POINT('Ctrl Pts',(1.79734640115767,118.299357347357,12.3917842530883));
#48774=CARTESIAN_POINT('Ctrl Pts',(1.8978404554453,118.340237099782,12.7236097563076));
#48775=CARTESIAN_POINT('Ctrl Pts',(2.57851879477238,114.657949304988,12.5479752566485));
#48776=CARTESIAN_POINT('Ctrl Pts',(2.68472166224218,114.710540197541,12.9558885871796));
#48777=CARTESIAN_POINT('Ctrl Pts',(2.69679183530668,114.812170225459,13.7902401137812));
#48778=CARTESIAN_POINT('Ctrl Pts',(2.00907490532175,115.009868065408,15.2658753129837));
#48779=CARTESIAN_POINT('Ctrl Pts',(0.119050810999923,115.2485549671,16.1914304991601));
#48780=CARTESIAN_POINT('Ctrl Pts',(-2.12124441684804,115.527013170151,15.1586542111214));
#48781=CARTESIAN_POINT('Ctrl Pts',(-2.51836524663899,115.713027546611,13.5632745939329));
#48782=CARTESIAN_POINT('Ctrl Pts',(-2.33948339716357,115.812941056406,12.7829424584588));
#48783=CARTESIAN_POINT('Ctrl Pts',(-2.29087065783513,115.835103556013,12.6120971106138));
#48784=CARTESIAN_POINT('Ctrl Pts',(-2.1807739583974,115.873783648183,12.3219688544218));
#48785=CARTESIAN_POINT('Ctrl Pts',(-1.86790580312768,115.950723384123,11.7862340656444));
#48786=CARTESIAN_POINT('Ctrl Pts',(-1.32443674896469,116.037703917496,11.3227742255522));
#48787=CARTESIAN_POINT('Ctrl Pts',(-0.678068500455315,116.123748972425,
11.0707744932568));
#48788=CARTESIAN_POINT('Ctrl Pts',(0.0028379771353343,116.209178138168,
10.9671275668568));
#48789=CARTESIAN_POINT('Ctrl Pts',(0.855976277343122,116.314824051003,11.1268338212465));
#48790=CARTESIAN_POINT('Ctrl Pts',(1.68502320329546,116.439814133456,11.7323543179146));
#48791=CARTESIAN_POINT('Ctrl Pts',(2.16594149682093,116.56307473546,12.6236568166783));
#48792=CARTESIAN_POINT('Ctrl Pts',(2.21417939812775,116.684655571401,13.6205557810665));
#48793=CARTESIAN_POINT('Ctrl Pts',(1.79231910486424,116.817961188309,14.631363101378));
#48794=CARTESIAN_POINT('Ctrl Pts',(0.832563435125419,116.962384890849,15.3658366316477));
#48795=CARTESIAN_POINT('Ctrl Pts',(-0.46290711489358,117.117363519388,15.4429520137478));
#48796=CARTESIAN_POINT('Ctrl Pts',(-1.37789757023272,117.244522151312,14.9004992538312));
#48797=CARTESIAN_POINT('Ctrl Pts',(-1.77446562586595,117.332580324617,14.3076982093431));
#48798=CARTESIAN_POINT('Ctrl Pts',(-1.90150874425604,117.37636721228,13.9798964771144));
#48799=CARTESIAN_POINT('Ctrl Pts',(-1.94614212722925,117.398204515359,13.8106461986552));
#48800=CARTESIAN_POINT('Ctrl Pts',(-1.96370611558196,117.409110572885,13.7250723123942));
#48801=CARTESIAN_POINT('Ctrl Pts',(-1.97237075532615,117.415338439035,13.6759397680619));
#48802=CARTESIAN_POINT('Ctrl Pts',(-2.03820967322699,117.468264109088,13.2572549472395));
#48803=CARTESIAN_POINT('Ctrl Pts',(-1.91035302372471,117.568785855181,12.424527496061));
#48804=CARTESIAN_POINT('Ctrl Pts',(-1.14547708597207,117.703055833809,11.601134922905));
#48805=CARTESIAN_POINT('Ctrl Pts',(-0.196837804787558,117.82444744455,11.2991006911685));
#48806=CARTESIAN_POINT('Ctrl Pts',(0.679046467189727,117.931734353258,11.4249337910364));
#48807=CARTESIAN_POINT('Ctrl Pts',(1.43882131909583,118.042861497326,11.9295889246391));
#48808=CARTESIAN_POINT('Ctrl Pts',(1.72638215595589,118.1142461513,12.4236510671564));
#48809=CARTESIAN_POINT('Ctrl Pts',(1.82675322822595,118.153936697284,12.7436111093781));
#48810=CARTESIAN_POINT('Ctrl Pts',(2.39011552843695,114.72454645408,12.5631659122308));
#48811=CARTESIAN_POINT('Ctrl Pts',(2.49270062588558,114.773541520323,12.9422531591066));
#48812=CARTESIAN_POINT('Ctrl Pts',(2.51126011434509,114.868098922389,13.7184218196959));
#48813=CARTESIAN_POINT('Ctrl Pts',(1.88593751494413,115.051600557879,15.094237550207));
#48814=CARTESIAN_POINT('Ctrl Pts',(0.14544360300595,115.272426774335,15.9666245788156));
#48815=CARTESIAN_POINT('Ctrl Pts',(-1.92888680857437,115.529125032708,15.03458128559));
#48816=CARTESIAN_POINT('Ctrl Pts',(-2.30893882327498,115.70013901172,13.5717142857354));
#48817=CARTESIAN_POINT('Ctrl Pts',(-2.1524829292496,115.791908542938,12.8531834821556));
#48818=CARTESIAN_POINT('Ctrl Pts',(-2.10955383080254,115.812262324106,12.6957863432518));
#48819=CARTESIAN_POINT('Ctrl Pts',(-2.01137835252497,115.847781170908,12.428253652488));
#48820=CARTESIAN_POINT('Ctrl Pts',(-1.72957705587654,115.918412624405,11.9332634504048));
#48821=CARTESIAN_POINT('Ctrl Pts',(-1.23561395951444,115.998225655204,11.5024451569099));
#48822=CARTESIAN_POINT('Ctrl Pts',(-0.645249829925848,116.077161402425,
11.2645581000994));
#48823=CARTESIAN_POINT('Ctrl Pts',(-0.0217142837632479,116.155526101408,
11.1623742404844));
#48824=CARTESIAN_POINT('Ctrl Pts',(0.762565301519525,116.252435211241,11.2998524775594));
#48825=CARTESIAN_POINT('Ctrl Pts',(1.5297933502385,116.367121821593,11.8465428526414));
#48826=CARTESIAN_POINT('Ctrl Pts',(1.98110362949434,116.480291671746,12.6596147228489));
#48827=CARTESIAN_POINT('Ctrl Pts',(2.03652408881097,116.592024157004,13.5752452452394));
#48828=CARTESIAN_POINT('Ctrl Pts',(1.65976614226889,116.714693039174,14.5101379043495));
#48829=CARTESIAN_POINT('Ctrl Pts',(0.783494316602796,116.847845301129,15.1984753791552));
#48830=CARTESIAN_POINT('Ctrl Pts',(-0.413312858761503,116.991134148319,
15.2852119012451));
#48831=CARTESIAN_POINT('Ctrl Pts',(-1.26875940128983,117.109107538797,14.7931020821331));
#48832=CARTESIAN_POINT('Ctrl Pts',(-1.64490042393746,117.191057001769,14.2461309326945));
#48833=CARTESIAN_POINT('Ctrl Pts',(-1.76720431870323,117.231868779816,13.9420984651988));
#48834=CARTESIAN_POINT('Ctrl Pts',(-1.81085358234464,117.252239474061,13.7847391891774));
#48835=CARTESIAN_POINT('Ctrl Pts',(-1.82826256237257,117.262417812982,13.7050817579043));
#48836=CARTESIAN_POINT('Ctrl Pts',(-1.83693569038863,117.268231303062,13.6593191784835));
#48837=CARTESIAN_POINT('Ctrl Pts',(-1.9033752817562,117.317645912561,13.2691890240628));
#48838=CARTESIAN_POINT('Ctrl Pts',(-1.79423174494513,117.411734167019,12.488127973009));
#48839=CARTESIAN_POINT('Ctrl Pts',(-1.08536597318167,117.538022933295,11.7038103359265));
#48840=CARTESIAN_POINT('Ctrl Pts',(-0.191565328164199,117.652876645827,
11.406213404452));
#48841=CARTESIAN_POINT('Ctrl Pts',(0.640365203505663,117.754598476621,11.5139391558001));
#48842=CARTESIAN_POINT('Ctrl Pts',(1.37450274320459,117.860977425892,11.9880829461835));
#48843=CARTESIAN_POINT('Ctrl Pts',(1.6554179107541,117.929134955243,12.4555178812246));
#48844=CARTESIAN_POINT('Ctrl Pts',(1.75566600100659,117.967636294783,12.7636124624487));
#48845=CARTESIAN_POINT('Ctrl Pts',(2.31548671935009,116.940942573699,14.2367878010894));
#48846=CARTESIAN_POINT('Ctrl Pts',(2.25782459523788,116.958633659998,14.3663197206516));
#48847=CARTESIAN_POINT('Ctrl Pts',(2.18932717831191,116.976291415496,14.4907161059409));
#48848=CARTESIAN_POINT('Ctrl Pts',(2.11090464171477,116.993906320744,14.607987749139));
#48849=CARTESIAN_POINT('Ctrl Pts',(2.08896395990088,116.998834534596,14.6407974479941));
#48850=CARTESIAN_POINT('Ctrl Pts',(2.06624670924219,117.003759395706,14.673049517398));
#48851=CARTESIAN_POINT('Ctrl Pts',(2.0427735176532,117.008680698696,14.7047005845127));
#48852=CARTESIAN_POINT('Ctrl Pts',(1.95793393600213,117.026467853258,14.8190976098446));
#48853=CARTESIAN_POINT('Ctrl Pts',(1.8632159759054,117.044208509281,14.9256409238034));
#48854=CARTESIAN_POINT('Ctrl Pts',(1.7604463664943,117.061893253579,15.0231276638096));
#48855=CARTESIAN_POINT('Ctrl Pts',(1.65765638941339,117.079581502774,15.120633724486));
#48856=CARTESIAN_POINT('Ctrl Pts',(1.54681285063823,117.097213818201,15.2090788045913));
#48857=CARTESIAN_POINT('Ctrl Pts',(1.4297753456656,117.114781010957,15.2873000870842));
#48858=CARTESIAN_POINT('Ctrl Pts',(1.31725506068872,117.13167017427,15.362502313921));
#48859=CARTESIAN_POINT('Ctrl Pts',(1.19901090213151,117.14849914637,15.4282543220876));
#48860=CARTESIAN_POINT('Ctrl Pts',(1.07670649422147,117.165259960218,15.4835687990835));
#48861=CARTESIAN_POINT('Ctrl Pts',(1.02706604615356,117.172062775617,15.506019628695));
#48862=CARTESIAN_POINT('Ctrl Pts',(0.976756765588284,117.17885436515,15.5267516003765));
#48863=CARTESIAN_POINT('Ctrl Pts',(0.925889782910585,117.185634205178,15.5457012048358));
#48864=CARTESIAN_POINT('Ctrl Pts',(0.912886479342423,117.187367359248,15.5505453580824));
#48865=CARTESIAN_POINT('Ctrl Pts',(0.899842705489527,117.189099753323,15.5552737754267));
#48866=CARTESIAN_POINT('Ctrl Pts',(0.886760298193248,117.190831399141,15.5598852350733));
#48867=CARTESIAN_POINT('Ctrl Pts',(0.761178174160384,117.207454009562,15.6041520801728));
#48868=CARTESIAN_POINT('Ctrl Pts',(0.632034792388793,117.224007429506,15.6376370989038));
#48869=CARTESIAN_POINT('Ctrl Pts',(0.501236200781654,117.240503740859,15.6603315069497));
#48870=CARTESIAN_POINT('Ctrl Pts',(0.363479587821818,117.257877597492,15.684233177045));
#48871=CARTESIAN_POINT('Ctrl Pts',(0.223888496440542,117.27518808512,15.6961659209278));
#48872=CARTESIAN_POINT('Ctrl Pts',(0.0846939106435335,117.292452770346,
15.6961783519871));
#48873=CARTESIAN_POINT('Ctrl Pts',(-0.0540836526485132,117.309665731131,
15.6961907458034));
#48874=CARTESIAN_POINT('Ctrl Pts',(-0.192465693473643,117.326833173632,
15.6843549295801));
#48875=CARTESIAN_POINT('Ctrl Pts',(-0.32825944952498,117.343975900692,15.6607672364423));
#48876=CARTESIAN_POINT('Ctrl Pts',(-0.392775511795997,117.352120466972,
15.6495606454799));
#48877=CARTESIAN_POINT('Ctrl Pts',(-0.456707734830717,117.360259502979,
15.6357020129467));
#48878=CARTESIAN_POINT('Ctrl Pts',(-0.519823689133548,117.36839549867,15.6192047402386));
#48879=CARTESIAN_POINT('Ctrl Pts',(-0.653936963993893,117.385683441766,
15.5841501602424));
#48880=CARTESIAN_POINT('Ctrl Pts',(-0.784361510700284,117.402957449876,
15.5371810040624));
#48881=CARTESIAN_POINT('Ctrl Pts',(-0.909380986500572,117.420243878384,
15.4796350958842));
#48882=CARTESIAN_POINT('Ctrl Pts',(-0.916037991934534,117.421164341758,
15.4765709059171));
#48883=CARTESIAN_POINT('Ctrl Pts',(-0.922679684067035,117.422084841101,
15.4734767309246));
#48884=CARTESIAN_POINT('Ctrl Pts',(-0.929305807850316,117.423005380643,
15.470352773874));
#48885=CARTESIAN_POINT('Ctrl Pts',(-1.04223429111457,117.438694060435,15.4171114305111));
#48886=CARTESIAN_POINT('Ctrl Pts',(-1.15084607653313,117.454344584733,15.3550070389703));
#48887=CARTESIAN_POINT('Ctrl Pts',(-1.25375654870144,117.469949685013,15.2849692667603));
#48888=CARTESIAN_POINT('Ctrl Pts',(-1.35637815267582,117.485510982004,15.2151280895551));
#48889=CARTESIAN_POINT('Ctrl Pts',(-1.45332936855855,117.501027110519,15.1373988742834));
#48890=CARTESIAN_POINT('Ctrl Pts',(-1.54325869101494,117.516491423543,15.0527504127095));
#48891=CARTESIAN_POINT('Ctrl Pts',(-1.59588298748066,117.525540736614,15.0032163384436));
#48892=CARTESIAN_POINT('Ctrl Pts',(-1.64610327006513,117.534572317048,14.9513137316402));
#48893=CARTESIAN_POINT('Ctrl Pts',(-1.69365429344754,117.543584920282,14.8972424084114));
#48894=CARTESIAN_POINT('Ctrl Pts',(-1.77565544949361,117.559127043912,14.803997075329));
#48895=CARTESIAN_POINT('Ctrl Pts',(-1.84971583932375,117.574612701386,14.7043016672338));
#48896=CARTESIAN_POINT('Ctrl Pts',(-1.91519240285048,117.590035579994,14.5997566402122));
#48897=CARTESIAN_POINT('Ctrl Pts',(-1.97148366797609,117.603294879229,14.5098775824752));
#48898=CARTESIAN_POINT('Ctrl Pts',(-2.02143108836489,117.616507787263,14.4164150045289));
#48899=CARTESIAN_POINT('Ctrl Pts',(-2.06465665364232,117.629670617629,14.3203898888529));
#48900=CARTESIAN_POINT('Ctrl Pts',(-2.09269581380972,117.638208960772,14.2581012043382));
#48901=CARTESIAN_POINT('Ctrl Pts',(-2.1179071968939,117.646726238826,14.1947342920141));
#48902=CARTESIAN_POINT('Ctrl Pts',(-2.140211784327,117.655221705677,14.13054504922));
#48903=CARTESIAN_POINT('Ctrl Pts',(-2.15521750441253,117.660937148652,14.0873608471916));
#48904=CARTESIAN_POINT('Ctrl Pts',(-2.16892218130902,117.666647211072,14.0437582790948));
#48905=CARTESIAN_POINT('Ctrl Pts',(-2.18129520696717,117.67235188627,13.9998107137466));
#48906=CARTESIAN_POINT('Ctrl Pts',(-2.19667226087415,117.67944159096,13.9451931852527));
#48907=CARTESIAN_POINT('Ctrl Pts',(-2.20999250553756,117.686522974354,13.8900427740209));
#48908=CARTESIAN_POINT('Ctrl Pts',(-2.22124632398131,117.693596222074,13.8345336184934));
#48909=CARTESIAN_POINT('Ctrl Pts',(-2.22687030744894,117.697131007039,13.8067934719335));
#48910=CARTESIAN_POINT('Ctrl Pts',(-2.23197823813659,117.70066376053,13.7789637472521));
#48911=CARTESIAN_POINT('Ctrl Pts',(-2.23656440171793,117.70419437115,13.7510591660253));
#48912=CARTESIAN_POINT('Ctrl Pts',(-2.2388569471652,117.705959263561,13.7371101388014));
#48913=CARTESIAN_POINT('Ctrl Pts',(-2.24101911263932,117.707723620513,13.7231424064524));
#48914=CARTESIAN_POINT('Ctrl Pts',(-2.24305093600475,117.709487539801,13.7091607254232));
#48915=CARTESIAN_POINT('Ctrl Pts',(-2.24508246270506,117.711251201541,13.6951810858495));
#48916=CARTESIAN_POINT('Ctrl Pts',(-2.24698368566634,117.713014425758,13.6811875019834));
#48917=CARTESIAN_POINT('Ctrl Pts',(-2.2487502882931,117.714777135929,13.6671806052955));
#48918=CARTESIAN_POINT('Ctrl Pts',(-2.26747755359704,117.733463138388,13.5186973717788));
#48919=CARTESIAN_POINT('Ctrl Pts',(-2.27107227506438,117.752091302631,13.368716862753));
#48920=CARTESIAN_POINT('Ctrl Pts',(-2.26019055608962,117.770660224938,13.220185355213));
#48921=CARTESIAN_POINT('Ctrl Pts',(-2.2490170609104,117.789727043733,13.0676712085682));
#48922=CARTESIAN_POINT('Ctrl Pts',(-2.22258075160084,117.808731399743,12.9166864938122));
#48923=CARTESIAN_POINT('Ctrl Pts',(-2.181646239744,117.827672698453,12.7704218019344));
#48924=CARTESIAN_POINT('Ctrl Pts',(-2.14379302181703,117.845188214709,12.6351670008991));
#48925=CARTESIAN_POINT('Ctrl Pts',(-2.09354304189675,117.862649821055,12.5039494152616));
#48926=CARTESIAN_POINT('Ctrl Pts',(-2.03153612752338,117.880057728102,12.3792736542313));
#48927=CARTESIAN_POINT('Ctrl Pts',(-2.02897425696137,117.880776951193,12.3741225647889));
#48928=CARTESIAN_POINT('Ctrl Pts',(-2.02639218492681,117.881496084643,12.3689824178837));
#48929=CARTESIAN_POINT('Ctrl Pts',(-2.02378995298469,117.882215127807,12.3638533940535));
#48930=CARTESIAN_POINT('Ctrl Pts',(-1.96229123084959,117.899208323168,12.2426388296426));
#48931=CARTESIAN_POINT('Ctrl Pts',(-1.88952855036872,117.916151065869,12.1276385950614));
#48932=CARTESIAN_POINT('Ctrl Pts',(-1.80723705440563,117.93303877345,12.020372574875));
#48933=CARTESIAN_POINT('Ctrl Pts',(-1.72431704050033,117.950055464312,11.9122872887671));
#48934=CARTESIAN_POINT('Ctrl Pts',(-1.6317232596914,117.967016278302,11.8120558463563));
#48935=CARTESIAN_POINT('Ctrl Pts',(-1.53127193155889,117.983916829116,11.7212014158956));
#48936=CARTESIAN_POINT('Ctrl Pts',(-1.43231274007286,118.00056633366,11.6316965666471));
#48937=CARTESIAN_POINT('Ctrl Pts',(-1.32572892005661,118.017157355224,11.5512930528403));
#48938=CARTESIAN_POINT('Ctrl Pts',(-1.21327869517553,118.033685950845,11.4814027134611));
#48939=CARTESIAN_POINT('Ctrl Pts',(-1.1846536335545,118.037893430809,11.4636115950035));
#48940=CARTESIAN_POINT('Ctrl Pts',(-1.15564849141823,118.042096866747,11.4465014632854));
#48941=CARTESIAN_POINT('Ctrl Pts',(-1.12629235719603,118.046296195893,11.4300950390516));
#48942=CARTESIAN_POINT('Ctrl Pts',(-1.01286248312528,118.062522084922,11.3667018613019));
#48943=CARTESIAN_POINT('Ctrl Pts',(-0.894193424257419,118.078686628009,
11.3138187460284));
#48944=CARTESIAN_POINT('Ctrl Pts',(-0.772389826872618,118.094772953157,
11.2719115286261));
#48945=CARTESIAN_POINT('Ctrl Pts',(-0.762313123950836,118.096103760482,
11.2684445819258));
#48946=CARTESIAN_POINT('Ctrl Pts',(-0.75221495837161,118.09743403271,11.2650527271387));
#48947=CARTESIAN_POINT('Ctrl Pts',(-0.742096515874733,118.098763760418,
11.2617362125407));
#48948=CARTESIAN_POINT('Ctrl Pts',(-0.64585072143041,118.111412021222,11.2301897979245));
#48949=CARTESIAN_POINT('Ctrl Pts',(-0.547391584981575,118.124036862978,
11.2053559596369));
#48950=CARTESIAN_POINT('Ctrl Pts',(-0.44777739688656,118.136631687336,11.1875956852635));
#48951=CARTESIAN_POINT('Ctrl Pts',(-0.367575533423394,118.146772094068,
11.1732964460928));
#48952=CARTESIAN_POINT('Ctrl Pts',(-0.286625952168628,118.156893052899,
11.1635817152682));
#48953=CARTESIAN_POINT('Ctrl Pts',(-0.205492391651079,118.166991426656,
11.1586182595621));
#48954=CARTESIAN_POINT('Ctrl Pts',(-0.103949228820018,118.179630102985,
11.1524062187277));
#48955=CARTESIAN_POINT('Ctrl Pts',(-0.0021185408589806,118.19223336774,
11.1536384272072));
#48956=CARTESIAN_POINT('Ctrl Pts',(0.0989456394163543,118.204814703464,
11.1620680830616));
#48957=CARTESIAN_POINT('Ctrl Pts',(0.200471484960796,118.21745351124,11.1705362459254));
#48958=CARTESIAN_POINT('Ctrl Pts',(0.301222672823428,118.230070208414,11.1862674062512));
#48959=CARTESIAN_POINT('Ctrl Pts',(0.400139050405618,118.242679170451,11.2089598970625));
#48960=CARTESIAN_POINT('Ctrl Pts',(0.498254479478169,118.255186034841,11.231468641591));
#48961=CARTESIAN_POINT('Ctrl Pts',(0.594563670688071,118.267685310577,11.2608260073517));
#48962=CARTESIAN_POINT('Ctrl Pts',(0.688056301876717,118.280191412531,11.2966931214302));
#48963=CARTESIAN_POINT('Ctrl Pts',(0.701543645072954,118.28199555567,11.3018673482209));
#48964=CARTESIAN_POINT('Ctrl Pts',(0.714972428772829,118.283799841202,11.3071769812151));
#48965=CARTESIAN_POINT('Ctrl Pts',(0.728339680957676,118.285604312653,11.3126209338532));
#48966=CARTESIAN_POINT('Ctrl Pts',(0.792100320495337,118.294211485774,11.3385881182095));
#48967=CARTESIAN_POINT('Ctrl Pts',(0.854460161502878,118.302822870294,11.3676117165583));
#48968=CARTESIAN_POINT('Ctrl Pts',(0.915102614013134,118.311430933557,11.3993855441404));
#48969=CARTESIAN_POINT('Ctrl Pts',(1.02395133490683,118.326881770994,11.4564172166247));
#48970=CARTESIAN_POINT('Ctrl Pts',(1.12769715551922,118.34222108742,11.5226262102829));
#48971=CARTESIAN_POINT('Ctrl Pts',(1.22457620944338,118.357466037869,11.5965368760917));
#48972=CARTESIAN_POINT('Ctrl Pts',(1.31633407816222,118.37190511531,11.6665405032484));
#48973=CARTESIAN_POINT('Ctrl Pts',(1.40193313080892,118.386259593316,11.7434537970661));
#48974=CARTESIAN_POINT('Ctrl Pts',(1.47983283887281,118.400545038101,11.8260342518042));
#48975=CARTESIAN_POINT('Ctrl Pts',(1.48467388906669,118.401432802086,11.8311661853679));
#48976=CARTESIAN_POINT('Ctrl Pts',(1.48948518746606,118.402320299667,11.8363200070697));
#48977=CARTESIAN_POINT('Ctrl Pts',(1.49426635716349,118.403207534653,11.8414954192839));
#48978=CARTESIAN_POINT('Ctrl Pts',(1.51684664234933,118.407397726654,11.8659376146352));
#48979=CARTESIAN_POINT('Ctrl Pts',(1.53875493098091,118.411582058567,11.8908613378136));
#48980=CARTESIAN_POINT('Ctrl Pts',(1.56000169303648,118.415765174845,11.916289301571));
#48981=CARTESIAN_POINT('Ctrl Pts',(1.60829237522143,118.425272766552,11.9740832239207));
#48982=CARTESIAN_POINT('Ctrl Pts',(1.65295011389502,118.434771772457,12.0341865167866));
#48983=CARTESIAN_POINT('Ctrl Pts',(1.69422527970214,118.44428774061,12.0968985325894));
#48984=CARTESIAN_POINT('Ctrl Pts',(1.73580640222509,118.453874246925,12.1600754081213));
#48985=CARTESIAN_POINT('Ctrl Pts',(1.77395426723288,118.463477888898,12.2258993614165));
#48986=CARTESIAN_POINT('Ctrl Pts',(1.80887719598704,118.47312326642,12.2947000711838));
#48987=CARTESIAN_POINT('Ctrl Pts',(1.84374351978064,118.482753010196,12.3633892650616));
#48988=CARTESIAN_POINT('Ctrl Pts',(1.87539495059614,118.492424267128,12.4350450843965));
#48989=CARTESIAN_POINT('Ctrl Pts',(1.90399723373718,118.502161258426,12.5100261594205));
#48990=CARTESIAN_POINT('Ctrl Pts',(1.92111149427981,118.507987415909,12.5548913069824));
#48991=CARTESIAN_POINT('Ctrl Pts',(1.93713331225682,118.513837108712,12.6009475989391));
#48992=CARTESIAN_POINT('Ctrl Pts',(1.95209195497482,118.519715684653,12.6482782748721));
#48993=CARTESIAN_POINT('Ctrl Pts',(2.40669191446941,114.731988374668,12.6249749337064));
#48994=CARTESIAN_POINT('Ctrl Pts',(2.43475306965379,114.74686978407,12.740863873503));
#48995=CARTESIAN_POINT('Ctrl Pts',(2.45447945011169,114.761614334258,12.8584224961112));
#48996=CARTESIAN_POINT('Ctrl Pts',(2.4658540228946,114.776289540321,12.9764721284355));
#48997=CARTESIAN_POINT('Ctrl Pts',(2.47720853484785,114.790938864373,13.0943135618579));
#48998=CARTESIAN_POINT('Ctrl Pts',(2.48024135459445,114.805519102271,13.2126454127005));
#48999=CARTESIAN_POINT('Ctrl Pts',(2.47489421501086,114.820100419095,13.3303250218578));
#49000=CARTESIAN_POINT('Ctrl Pts',(2.47094722867391,114.830863605166,13.4171901208925));
#49001=CARTESIAN_POINT('Ctrl Pts',(2.46243349325285,114.841627441902,13.5037005683707));
#49002=CARTESIAN_POINT('Ctrl Pts',(2.44931187061213,114.852421139954,13.5894013795713));
#49003=CARTESIAN_POINT('Ctrl Pts',(2.44260496807706,114.857938161957,13.6332059457928));
#49004=CARTESIAN_POINT('Ctrl Pts',(2.43469394423745,114.863462998683,13.6767990142332));
#49005=CARTESIAN_POINT('Ctrl Pts',(2.42560683986979,114.868999635026,13.7201269729547));
#49006=CARTESIAN_POINT('Ctrl Pts',(2.39853149953261,114.885496233639,13.8492241177696));
#49007=CARTESIAN_POINT('Ctrl Pts',(2.36102101525659,114.902033972754,13.9757830595316));
#49008=CARTESIAN_POINT('Ctrl Pts',(2.31383592171913,114.918519364437,14.0981944290528));
#49009=CARTESIAN_POINT('Ctrl Pts',(2.28825187124149,114.927457846092,14.1645666331131));
#49010=CARTESIAN_POINT('Ctrl Pts',(2.25982442869193,114.936380857678,14.2297190613628));
#49011=CARTESIAN_POINT('Ctrl Pts',(2.22868099465303,114.945272946841,14.2933935594758));
#49012=CARTESIAN_POINT('Ctrl Pts',(2.17167369366009,114.961549700482,14.4099481846006));
#49013=CARTESIAN_POINT('Ctrl Pts',(2.10556322161123,114.977723070201,14.5215497325451));
#49014=CARTESIAN_POINT('Ctrl Pts',(2.03135185048887,114.993695124257,14.6267674579025));
#49015=CARTESIAN_POINT('Ctrl Pts',(2.0135346205562,114.997529816371,14.6520289289861));
#49016=CARTESIAN_POINT('Ctrl Pts',(1.9952506603965,115.001352886589,14.6769224977211));
#49017=CARTESIAN_POINT('Ctrl Pts',(1.9765142564639,115.005162946815,14.7014285489423));
#49018=CARTESIAN_POINT('Ctrl Pts',(1.92537243181487,115.01556267094,14.7683188753307));
#49019=CARTESIAN_POINT('Ctrl Pts',(1.87079136938365,115.025943804624,14.8324693624242));
#49020=CARTESIAN_POINT('Ctrl Pts',(1.8130406021481,115.036309680939,14.8934653663168));
#49021=CARTESIAN_POINT('Ctrl Pts',(1.72389292042246,115.052311093331,14.9876225974991));
#49022=CARTESIAN_POINT('Ctrl Pts',(1.62719019971625,115.068276086599,15.0742607310478));
#49023=CARTESIAN_POINT('Ctrl Pts',(1.5243971463275,115.084218127803,15.1525367046183));
#49024=CARTESIAN_POINT('Ctrl Pts',(1.4350458707153,115.098075501142,15.2205768868849));
#49025=CARTESIAN_POINT('Ctrl Pts',(1.34109422436839,115.111915556258,15.2822992339472));
#49026=CARTESIAN_POINT('Ctrl Pts',(1.24352480822076,115.125747922801,15.3371743252976));
#49027=CARTESIAN_POINT('Ctrl Pts',(1.13138273130218,115.141646248055,15.4002453875024));
#49028=CARTESIAN_POINT('Ctrl Pts',(1.01446221224332,115.157534398343,15.454269788355));
#49029=CARTESIAN_POINT('Ctrl Pts',(0.894468315725866,115.173428041082,15.4983384961725));
#49030=CARTESIAN_POINT('Ctrl Pts',(0.790037839342134,115.18726025031,15.5366914148171));
#49031=CARTESIAN_POINT('Ctrl Pts',(0.68328027521778,115.201096640735,15.567504184207));
#49032=CARTESIAN_POINT('Ctrl Pts',(0.575318498023721,115.214948205653,15.5902098339972));
#49033=CARTESIAN_POINT('Ctrl Pts',(0.447210181395969,115.231384584439,15.6171525413901));
#49034=CARTESIAN_POINT('Ctrl Pts',(0.317407831723781,115.247842310195,15.6326803318094));
#49035=CARTESIAN_POINT('Ctrl Pts',(0.187703615051371,115.264340942193,15.637441971482));
#49036=CARTESIAN_POINT('Ctrl Pts',(0.174318219487164,115.26604359089,15.6379333697741));
#49037=CARTESIAN_POINT('Ctrl Pts',(0.16093384073973,115.267746676144,15.6383101435246));
#49038=CARTESIAN_POINT('Ctrl Pts',(0.147552427361176,115.269450220062,15.6385730299968));
#49039=CARTESIAN_POINT('Ctrl Pts',(0.0311432612617477,115.284269889801,
15.6408599629343));
#49040=CARTESIAN_POINT('Ctrl Pts',(-0.0854558591225894,115.298990932322,
15.63444536016));
#49041=CARTESIAN_POINT('Ctrl Pts',(-0.200909700546528,115.313627679424,
15.6196714832657));
#49042=CARTESIAN_POINT('Ctrl Pts',(-0.322521225697206,115.329045071486,
15.6041096476494));
#49043=CARTESIAN_POINT('Ctrl Pts',(-0.442860879206709,115.344368930949,
15.5792732160875));
#49044=CARTESIAN_POINT('Ctrl Pts',(-0.560365328594014,115.359617383775,
15.54562000471));
#49045=CARTESIAN_POINT('Ctrl Pts',(-0.677869777981319,115.3748658366,15.5119667933325));
#49046=CARTESIAN_POINT('Ctrl Pts',(-0.792537782828811,115.390038890025,
15.4694974322853));
#49047=CARTESIAN_POINT('Ctrl Pts',(-0.90282176453482,115.405155981277,15.4187194369708));
#49048=CARTESIAN_POINT('Ctrl Pts',(-1.00985159669809,115.419827012504,15.3694397480076));
#49049=CARTESIAN_POINT('Ctrl Pts',(-1.1127513980594,115.434445347986,15.3123352244253));
#49050=CARTESIAN_POINT('Ctrl Pts',(-1.21013698639887,115.449029833971,15.2479064194388));
#49051=CARTESIAN_POINT('Ctrl Pts',(-1.27702484761514,115.459046973992,15.2036544408889));
#49052=CARTESIAN_POINT('Ctrl Pts',(-1.34131205064833,115.469048167882,15.1559480279997));
#49053=CARTESIAN_POINT('Ctrl Pts',(-1.40256201138118,115.479039786204,15.1049574357649));
#49054=CARTESIAN_POINT('Ctrl Pts',(-1.49548743629538,115.494198577607,15.0275970196381));
#49055=CARTESIAN_POINT('Ctrl Pts',(-1.58141977934296,115.509335285618,14.9426779610095));
#49056=CARTESIAN_POINT('Ctrl Pts',(-1.65982151015904,115.524473068663,14.8517915593901));
#49057=CARTESIAN_POINT('Ctrl Pts',(-1.66477676469785,115.525429827747,14.8460472314339));
#49058=CARTESIAN_POINT('Ctrl Pts',(-1.66970195431248,115.526386591441,14.8402790662085));
#49059=CARTESIAN_POINT('Ctrl Pts',(-1.67459695039572,115.527343365718,14.8344874652654));
#49060=CARTESIAN_POINT('Ctrl Pts',(-1.7819615100526,115.548328806199,14.7074571930475));
#49061=CARTESIAN_POINT('Ctrl Pts',(-1.87516835190207,115.569125875581,14.5685630766246));
#49062=CARTESIAN_POINT('Ctrl Pts',(-1.9526207174621,115.58979491357,14.4216976039055));
#49063=CARTESIAN_POINT('Ctrl Pts',(-2.03666670163025,115.61222353311,14.2623292862853));
#49064=CARTESIAN_POINT('Ctrl Pts',(-2.10216154528806,115.634501390266,14.0935759022937));
#49065=CARTESIAN_POINT('Ctrl Pts',(-2.14710204093268,115.656709229068,13.9204632370897));
#49066=CARTESIAN_POINT('Ctrl Pts',(-2.19922267580225,115.682465212415,13.719692375866));
#49067=CARTESIAN_POINT('Ctrl Pts',(-2.22369540787726,115.708126986251,13.5130596298197));
#49068=CARTESIAN_POINT('Ctrl Pts',(-2.21745183639977,115.733825600408,13.3084479348659));
#49069=CARTESIAN_POINT('Ctrl Pts',(-2.21400458772954,115.748014516767,13.1954761532685));
#49070=CARTESIAN_POINT('Ctrl Pts',(-2.20119446652922,115.762214752214,13.0831210539546));
#49071=CARTESIAN_POINT('Ctrl Pts',(-2.17975849413663,115.776448986664,12.9725597778872));
#49072=CARTESIAN_POINT('Ctrl Pts',(-2.17197188526608,115.781619566948,12.9323984361389));
#49073=CARTESIAN_POINT('Ctrl Pts',(-2.16304771225363,115.786772238818,12.8924989800121));
#49074=CARTESIAN_POINT('Ctrl Pts',(-2.15303250877005,115.791934561425,12.8529191255056));
#49075=CARTESIAN_POINT('Ctrl Pts',(-2.14301730528641,115.797096884031,12.8133392709989));
#49076=CARTESIAN_POINT('Ctrl Pts',(-2.13191205941212,115.802268315464,12.7740833838265));
#49077=CARTESIAN_POINT('Ctrl Pts',(-2.11975235485977,115.807417983291,12.7352107449596));
#49078=CARTESIAN_POINT('Ctrl Pts',(-2.09543294575521,115.817717318945,12.6574654672262));
#49079=CARTESIAN_POINT('Ctrl Pts',(-2.06687614682154,115.827839259825,12.5812427758128));
#49080=CARTESIAN_POINT('Ctrl Pts',(-2.0344006165645,115.837933723714,12.5069067743895));
#49081=CARTESIAN_POINT('Ctrl Pts',(-1.99645086165813,115.849729756835,12.4200403548913));
#49082=CARTESIAN_POINT('Ctrl Pts',(-1.95315339155439,115.861487218842,12.3357571733488));
#49083=CARTESIAN_POINT('Ctrl Pts',(-1.90492117136718,115.873219467641,12.2546565754633));
#49084=CARTESIAN_POINT('Ctrl Pts',(-1.87060387681194,115.881566979663,12.196953382547));
#49085=CARTESIAN_POINT('Ctrl Pts',(-1.8337873100898,115.889901722998,12.1408615641731));
#49086=CARTESIAN_POINT('Ctrl Pts',(-1.79460654855197,115.898228438316,12.0866054254144));
#49087=CARTESIAN_POINT('Ctrl Pts',(-1.73617001600234,115.910647399857,12.0056845730842));
#49088=CARTESIAN_POINT('Ctrl Pts',(-1.67236145606815,115.923062979607,11.9287040403723));
#49089=CARTESIAN_POINT('Ctrl Pts',(-1.60371240566613,115.935469871571,11.8566413562907));
#49090=CARTESIAN_POINT('Ctrl Pts',(-1.53440342756294,115.947996031778,11.7838859290296));
#49091=CARTESIAN_POINT('Ctrl Pts',(-1.46016104345744,115.960513337421,11.7161444856533));
#49092=CARTESIAN_POINT('Ctrl Pts',(-1.38157990701867,115.973016628262,11.6544018915107));
#49093=CARTESIAN_POINT('Ctrl Pts',(-1.36418582545402,115.975784255082,11.6407350527857));
#49094=CARTESIAN_POINT('Ctrl Pts',(-1.34657932263432,115.978551196342,11.6273620180571));
#49095=CARTESIAN_POINT('Ctrl Pts',(-1.32876711287241,115.981317397953,11.6142932435803));
#49096=CARTESIAN_POINT('Ctrl Pts',(-1.24965483992903,115.993603380421,11.556248763571));
#49097=CARTESIAN_POINT('Ctrl Pts',(-1.166482404834,116.005874752867,11.5042098614192));
#49098=CARTESIAN_POINT('Ctrl Pts',(-1.08024451964533,116.018126996144,11.4583191342909));
#49099=CARTESIAN_POINT('Ctrl Pts',(-0.964456029554463,116.034577640152,
11.3967033143792));
#49100=CARTESIAN_POINT('Ctrl Pts',(-0.843308660808071,116.050928154555,
11.3462556953615));
#49101=CARTESIAN_POINT('Ctrl Pts',(-0.7190845582525,116.067193672212,11.3070695193659));
#49102=CARTESIAN_POINT('Ctrl Pts',(-0.692972217249571,116.070612740935,
11.2988324480638));
#49103=CARTESIAN_POINT('Ctrl Pts',(-0.666723753635358,116.074028054686,
11.2910929172646));
#49104=CARTESIAN_POINT('Ctrl Pts',(-0.64036007948357,116.077439754974,11.2838517103464));
#49105=CARTESIAN_POINT('Ctrl Pts',(-0.547244823989042,116.089489719715,
11.2582761085393));
#49106=CARTESIAN_POINT('Ctrl Pts',(-0.452690304569924,116.101495114013,
11.2389114682594));
#49107=CARTESIAN_POINT('Ctrl Pts',(-0.357495819040103,116.113469518491,
11.2257905671347));
#49108=CARTESIAN_POINT('Ctrl Pts',(-0.309101221454461,116.119557019073,
11.2191202151037));
#49109=CARTESIAN_POINT('Ctrl Pts',(-0.26054087605447,116.125636506673,11.2140643790259));
#49110=CARTESIAN_POINT('Ctrl Pts',(-0.211918517964794,116.131709742554,
11.2106326906361));
#49111=CARTESIAN_POINT('Ctrl Pts',(-0.182192770128042,116.135422673918,
11.2085346948223));
#49112=CARTESIAN_POINT('Ctrl Pts',(-0.152444447246134,116.139133192433,
11.2070436537523));
#49113=CARTESIAN_POINT('Ctrl Pts',(-0.12268249260673,116.142843534232,11.2061625355098));
#49114=CARTESIAN_POINT('Ctrl Pts',(-0.0153736119534298,116.156221440021,
11.2029855999399));
#49115=CARTESIAN_POINT('Ctrl Pts',(0.092054654109126,116.169589640168,11.2077469018766));
#49116=CARTESIAN_POINT('Ctrl Pts',(0.198244015014826,116.182937381495,11.2206306431426));
#49117=CARTESIAN_POINT('Ctrl Pts',(0.298709414128022,116.195565634912,11.2328199076539));
#49118=CARTESIAN_POINT('Ctrl Pts',(0.398064683415244,116.208175577783,11.2522792791066));
#49119=CARTESIAN_POINT('Ctrl Pts',(0.495155236231196,116.220758284055,11.2791220046775));
#49120=CARTESIAN_POINT('Ctrl Pts',(0.574891207390632,116.231091877544,11.3011666911056));
#49121=CARTESIAN_POINT('Ctrl Pts',(0.653099413496132,116.24140710442,11.328190295651));
#49122=CARTESIAN_POINT('Ctrl Pts',(0.729256505323708,116.251699113371,11.3597901748801));
#49123=CARTESIAN_POINT('Ctrl Pts',(0.787017445332149,116.259505032653,11.3837569347002));
#49124=CARTESIAN_POINT('Ctrl Pts',(0.843590323984023,116.267296436205,11.4103514048508));
#49125=CARTESIAN_POINT('Ctrl Pts',(0.898774149368019,116.275074539465,11.4394037618789));
#49126=CARTESIAN_POINT('Ctrl Pts',(1.00545542585605,116.290111155334,11.4955677286062));
#49127=CARTESIAN_POINT('Ctrl Pts',(1.10694903466504,116.305098342093,11.5609155026284));
#49128=CARTESIAN_POINT('Ctrl Pts',(1.20180118240028,116.320046286155,11.6342646596012));
#49129=CARTESIAN_POINT('Ctrl Pts',(1.23959813028786,116.326002784518,11.6634930358678));
#49130=CARTESIAN_POINT('Ctrl Pts',(1.27634022257083,116.331953049336,11.6939924640879));
#49131=CARTESIAN_POINT('Ctrl Pts',(1.31193413354399,116.33789771633,11.7256899934454));
#49132=CARTESIAN_POINT('Ctrl Pts',(1.37533506352807,116.348486533506,11.7821505729243));
#49133=CARTESIAN_POINT('Ctrl Pts',(1.43509262147617,116.35905738331,11.8424108497414));
#49134=CARTESIAN_POINT('Ctrl Pts',(1.49087120655567,116.369614516537,11.9059855018094));
#49135=CARTESIAN_POINT('Ctrl Pts',(1.56552512652914,116.383744157474,11.9910736585108));
#49136=CARTESIAN_POINT('Ctrl Pts',(1.63305359548156,116.397850559611,12.0821114610562));
#49137=CARTESIAN_POINT('Ctrl Pts',(1.69254649560885,116.411924456967,12.1778104866814));
#49138=CARTESIAN_POINT('Ctrl Pts',(1.75119310963197,116.425798153227,12.2721481943107));
#49139=CARTESIAN_POINT('Ctrl Pts',(1.80203048836647,116.439640264006,12.371014285989));
#49140=CARTESIAN_POINT('Ctrl Pts',(1.84422852407979,116.453442098142,12.4731477436492));
#49141=CARTESIAN_POINT('Ctrl Pts',(1.86792589212045,116.461192865153,12.5305033549833));
#49142=CARTESIAN_POINT('Ctrl Pts',(1.888899560676,116.468930933507,12.5888889728115));
#49143=CARTESIAN_POINT('Ctrl Pts',(1.90712464981553,116.476654791649,12.6480236031063));
#49144=CARTESIAN_POINT('Ctrl Pts',(1.91877508216826,116.481592286665,12.6858255586786));
#49145=CARTESIAN_POINT('Ctrl Pts',(1.92930298789426,116.486524097902,12.7239344528093));
#49146=CARTESIAN_POINT('Ctrl Pts',(1.93870540361382,116.491451661224,12.7622914012232));
#49147=CARTESIAN_POINT('Ctrl Pts',(1.97129883535493,116.508533037283,12.895255590131));
#49148=CARTESIAN_POINT('Ctrl Pts',(1.99036184829165,116.525559397266,13.0311693385362));
#49149=CARTESIAN_POINT('Ctrl Pts',(1.99561611600238,116.542540264114,13.1672079630254));
#49150=CARTESIAN_POINT('Ctrl Pts',(1.99819202915474,116.550865161256,13.2339011163522));
#49151=CARTESIAN_POINT('Ctrl Pts',(1.99744827903915,116.559179121435,13.3006244608754));
#49152=CARTESIAN_POINT('Ctrl Pts',(1.99334747419319,116.567483250863,13.3670451432938));
#49153=CARTESIAN_POINT('Ctrl Pts',(1.98912186126324,116.57604011665,13.4354873406152));
#49154=CARTESIAN_POINT('Ctrl Pts',(1.98133161838024,116.584586620847,13.5036088311572));
#49155=CARTESIAN_POINT('Ctrl Pts',(1.97009180727589,116.593123729406,13.5710791606626));
#49156=CARTESIAN_POINT('Ctrl Pts',(1.94788382248079,116.6099916265,13.7043892348148));
#49157=CARTESIAN_POINT('Ctrl Pts',(1.91220864772609,116.626819254494,13.8351278076438));
#49158=CARTESIAN_POINT('Ctrl Pts',(1.8640076007052,116.643599947005,13.9606342202399));
#49159=CARTESIAN_POINT('Ctrl Pts',(1.82897034182154,116.655797803775,14.0518646175336));
#49160=CARTESIAN_POINT('Ctrl Pts',(1.78731583833951,116.667970864599,14.1403303265684));
#49161=CARTESIAN_POINT('Ctrl Pts',(1.73942138132993,116.680116625926,14.2250166520074));
#49162=CARTESIAN_POINT('Ctrl Pts',(1.71068616549277,116.687403712888,14.2758258686033));
#49163=CARTESIAN_POINT('Ctrl Pts',(1.67970505922128,116.694680973931,14.3252748102773));
#49164=CARTESIAN_POINT('Ctrl Pts',(1.64664640176096,116.701947885141,14.3731997781275));
#49165=CARTESIAN_POINT('Ctrl Pts',(1.62704784448877,116.706256014583,14.4016117070846));
#49166=CARTESIAN_POINT('Ctrl Pts',(1.60671407341517,116.710561626033,14.4294954714279));
#49167=CARTESIAN_POINT('Ctrl Pts',(1.58567712235569,116.714865011729,14.4568188234608));
#49168=CARTESIAN_POINT('Ctrl Pts',(1.49913879255966,116.732567568032,14.5692171098222));
#49169=CARTESIAN_POINT('Ctrl Pts',(1.40070708779234,116.750230374466,14.672116242543));
#49170=CARTESIAN_POINT('Ctrl Pts',(1.29276196358478,116.767847645003,14.7631129897568));
#49171=CARTESIAN_POINT('Ctrl Pts',(1.24452040517771,116.775720947218,14.8037801799407));
#49172=CARTESIAN_POINT('Ctrl Pts',(1.19437936245796,116.783585156946,14.842070520652));
#49173=CARTESIAN_POINT('Ctrl Pts',(1.14255369257811,116.791439768281,14.8777718213301));
#49174=CARTESIAN_POINT('Ctrl Pts',(1.02080713973,116.809891471003,14.9616397250123));
#49175=CARTESIAN_POINT('Ctrl Pts',(0.88976316004629,116.82829019289,15.0312156933588));
#49176=CARTESIAN_POINT('Ctrl Pts',(0.753093529829106,116.846629914899,15.0852770787824));
#49177=CARTESIAN_POINT('Ctrl Pts',(0.723803194010996,116.850560390277,15.0968632382777));
#49178=CARTESIAN_POINT('Ctrl Pts',(0.694247095485108,116.854489153646,15.1077400735973));
#49179=CARTESIAN_POINT('Ctrl Pts',(0.664454578271815,116.858416983078,15.1178967007645));
#49180=CARTESIAN_POINT('Ctrl Pts',(0.555234271048197,116.872816529589,15.1551312161166));
#49181=CARTESIAN_POINT('Ctrl Pts',(0.442864032700579,116.887199572224,15.1826711409601));
#49182=CARTESIAN_POINT('Ctrl Pts',(0.329150962525186,116.901558454711,15.1998707026059));
#49183=CARTESIAN_POINT('Ctrl Pts',(0.214068667916537,116.916090233179,15.2172773649835));
#49184=CARTESIAN_POINT('Ctrl Pts',(0.0976124776931342,116.930597266838,
15.2240926615264));
#49185=CARTESIAN_POINT('Ctrl Pts',(-0.0182859125916594,116.945071164092,
15.2205350884505));
#49186=CARTESIAN_POINT('Ctrl Pts',(-0.10604441062489,116.956030828679,15.2178412868452));
#49187=CARTESIAN_POINT('Ctrl Pts',(-0.193482669233001,116.966971497382,
15.2092012674747));
#49188=CARTESIAN_POINT('Ctrl Pts',(-0.279765449072471,116.977889579526,
15.194729438234));
#49189=CARTESIAN_POINT('Ctrl Pts',(-0.312106818934253,116.981982003686,
15.1893049632354));
#49190=CARTESIAN_POINT('Ctrl Pts',(-0.344285911746652,116.986071254933,
15.1830612987958));
#49191=CARTESIAN_POINT('Ctrl Pts',(-0.376259037902826,116.990157145737,
15.1760050562577));
#49192=CARTESIAN_POINT('Ctrl Pts',(-0.410203973017803,116.994495016783,
15.168513649445));
#49193=CARTESIAN_POINT('Ctrl Pts',(-0.443924325172075,116.998830061935,
15.1601048276074));
#49194=CARTESIAN_POINT('Ctrl Pts',(-0.477375487000464,117.003163074823,
15.1507830465092));
#49195=CARTESIAN_POINT('Ctrl Pts',(-0.49647583620284,117.00563719096,15.1454603831268));
#49196=CARTESIAN_POINT('Ctrl Pts',(-0.515487839346988,117.008110570362,
15.1398401905004));
#49197=CARTESIAN_POINT('Ctrl Pts',(-0.53440213830564,117.010583227121,15.1339235123191));
#49198=CARTESIAN_POINT('Ctrl Pts',(-0.686067213261841,117.030410325846,
15.0864803878435));
#49199=CARTESIAN_POINT('Ctrl Pts',(-0.831453110605257,117.050190967813,
15.019976503841));
#49200=CARTESIAN_POINT('Ctrl Pts',(-0.966310415421474,117.06993608109,14.9370403466912));
#49201=CARTESIAN_POINT('Ctrl Pts',(-1.07727880405652,117.086183502073,14.8687956807383));
#49202=CARTESIAN_POINT('Ctrl Pts',(-1.1811182709215,117.102406864446,14.7894239141178));
#49203=CARTESIAN_POINT('Ctrl Pts',(-1.27543669211679,117.118612221601,14.7003788828808));
#49204=CARTESIAN_POINT('Ctrl Pts',(-1.31684386356554,117.125726611278,14.6612868070343));
#49205=CARTESIAN_POINT('Ctrl Pts',(-1.35641786923958,117.132837965838,14.6203275917402));
#49206=CARTESIAN_POINT('Ctrl Pts',(-1.39404208976212,117.139944780179,14.577698052834));
#49207=CARTESIAN_POINT('Ctrl Pts',(-1.46607112697874,117.153550297783,14.4960866705447));
#49208=CARTESIAN_POINT('Ctrl Pts',(-1.53094642551177,117.167138236835,14.4083575652026));
#49209=CARTESIAN_POINT('Ctrl Pts',(-1.58788514907687,117.180698432732,14.3159193029345));
#49210=CARTESIAN_POINT('Ctrl Pts',(-1.62663012303909,117.189925710832,14.2530180322273));
#49211=CARTESIAN_POINT('Ctrl Pts',(-1.66170150186151,117.199140305292,14.1879358397825));
#49212=CARTESIAN_POINT('Ctrl Pts',(-1.69286357661844,117.208338477689,14.1211260289112));
#49213=CARTESIAN_POINT('Ctrl Pts',(-1.71258060781417,117.214158393517,14.0788537753657));
#49214=CARTESIAN_POINT('Ctrl Pts',(-1.73073361608754,117.219971866751,14.0358891527244));
#49215=CARTESIAN_POINT('Ctrl Pts',(-1.7472697287625,117.225779773835,13.9923333288776));
#49216=CARTESIAN_POINT('Ctrl Pts',(-1.77386070669752,117.235119207604,13.9222931704911));
#49217=CARTESIAN_POINT('Ctrl Pts',(-1.79627143159348,117.244444051522,13.8507261726921));
#49218=CARTESIAN_POINT('Ctrl Pts',(-1.81438776136439,117.253761733308,13.7781403018514));
#49219=CARTESIAN_POINT('Ctrl Pts',(-1.8233312033563,117.258361569346,13.7423070214075));
#49220=CARTESIAN_POINT('Ctrl Pts',(-1.8312276588904,117.262959563972,13.7062260685609));
#49221=CARTESIAN_POINT('Ctrl Pts',(-1.83806222368246,117.267557219643,13.6699532356282));
#49222=CARTESIAN_POINT('Ctrl Pts',(-1.84085659153172,117.269437008859,13.6551227904965));
#49223=CARTESIAN_POINT('Ctrl Pts',(-1.84347304444535,117.271316482654,13.6402623089836));
#49224=CARTESIAN_POINT('Ctrl Pts',(-1.84591075327413,117.273195889375,13.6253744577075));
#49225=CARTESIAN_POINT('Ctrl Pts',(-1.85971572148554,117.283839141649,13.5410631933034));
#49226=CARTESIAN_POINT('Ctrl Pts',(-1.8678047482461,117.294492742878,13.4557528112906));
#49227=CARTESIAN_POINT('Ctrl Pts',(-1.86992137198423,117.305136545796,13.3703636749658));
#49228=CARTESIAN_POINT('Ctrl Pts',(-1.87170907388779,117.314126309256,13.2982439501414));
#49229=CARTESIAN_POINT('Ctrl Pts',(-1.86923710776832,117.323109093235,13.2260688838612));
#49230=CARTESIAN_POINT('Ctrl Pts',(-1.86237967622628,117.332073054458,13.1543969176522));
#49231=CARTESIAN_POINT('Ctrl Pts',(-1.85423887153773,117.342714627341,13.0693114924497));
#49232=CARTESIAN_POINT('Ctrl Pts',(-1.83991647495421,117.353329659416,12.9849362386533));
#49233=CARTESIAN_POINT('Ctrl Pts',(-1.81989415050543,117.363895185557,12.9020346284525));
#49234=CARTESIAN_POINT('Ctrl Pts',(-1.79972072205488,117.374540447359,12.8185073783523));
#49235=CARTESIAN_POINT('Ctrl Pts',(-1.77376174147136,117.385135449304,12.7364771470377));
#49236=CARTESIAN_POINT('Ctrl Pts',(-1.74255499710192,117.395657275435,12.6566988894436));
#49237=CARTESIAN_POINT('Ctrl Pts',(-1.7268372303829,117.400956758349,12.6165173175606));
#49238=CARTESIAN_POINT('Ctrl Pts',(-1.70978885588439,117.406237687464,12.5769065173321));
#49239=CARTESIAN_POINT('Ctrl Pts',(-1.69148196311947,117.411497193792,12.5379592168163));
#49240=CARTESIAN_POINT('Ctrl Pts',(-1.64422641244845,117.425073548391,12.4374246172718));
#49241=CARTESIAN_POINT('Ctrl Pts',(-1.58820047488711,117.438900237672,12.3410139841719));
#49242=CARTESIAN_POINT('Ctrl Pts',(-1.52439771598195,117.452848649161,12.2501830196273));
#49243=CARTESIAN_POINT('Ctrl Pts',(-1.46217654483511,117.466451297593,12.161603637053));
#49244=CARTESIAN_POINT('Ctrl Pts',(-1.39255982919765,117.480169700269,12.0783289541421));
#49245=CARTESIAN_POINT('Ctrl Pts',(-1.3164220316241,117.493891230108,12.001703326054));
#49246=CARTESIAN_POINT('Ctrl Pts',(-1.24771768854726,117.506273105126,11.9325587801331));
#49247=CARTESIAN_POINT('Ctrl Pts',(-1.17370317273219,117.518657587153,11.8688270140121));
#49248=CARTESIAN_POINT('Ctrl Pts',(-1.09498183832174,117.530966906991,11.811512383697));
#49249=CARTESIAN_POINT('Ctrl Pts',(-1.06858713662752,117.535094134097,11.7922951971337));
#49250=CARTESIAN_POINT('Ctrl Pts',(-1.04166295250224,117.539212952506,11.7737996665922));
#49251=CARTESIAN_POINT('Ctrl Pts',(-1.01423097499657,117.543320558148,11.7560645295145));
#49252=CARTESIAN_POINT('Ctrl Pts',(-0.998041927346321,117.545744671519,
11.7455980956172));
#49253=CARTESIAN_POINT('Ctrl Pts',(-0.981676013135029,117.548164880914,
11.7353965049393));
#49254=CARTESIAN_POINT('Ctrl Pts',(-0.965141588692916,117.550580691203,
11.7254609363924));
#49255=CARTESIAN_POINT('Ctrl Pts',(-0.885330420180348,117.562241734668,
11.6775022464278));
#49256=CARTESIAN_POINT('Ctrl Pts',(-0.801863080831363,117.573695835655,
11.6358450243134));
#49257=CARTESIAN_POINT('Ctrl Pts',(-0.715805975492523,117.585061449866,
11.6006923062261));
#49258=CARTESIAN_POINT('Ctrl Pts',(-0.631194966603208,117.59623607724,11.5661302914936));
#49259=CARTESIAN_POINT('Ctrl Pts',(-0.544080928567308,117.607325181313,
11.5378571908184));
#49260=CARTESIAN_POINT('Ctrl Pts',(-0.455522731807488,117.618434684624,
11.516046342729));
#49261=CARTESIAN_POINT('Ctrl Pts',(-0.366964535047849,117.629544187936,
11.4942354946396));
#49262=CARTESIAN_POINT('Ctrl Pts',(-0.276962930050188,117.64067411174,11.4788882325044));
#49263=CARTESIAN_POINT('Ctrl Pts',(-0.186613838556208,117.651923366021,
11.470139291332));
#49264=CARTESIAN_POINT('Ctrl Pts',(-0.108075132966351,117.661702123676,
11.4625340071659));
#49265=CARTESIAN_POINT('Ctrl Pts',(-0.0291274892094371,117.671636391611,
11.4599362158693));
#49266=CARTESIAN_POINT('Ctrl Pts',(0.0496472966318842,117.681644743467,
11.4623331568941));
#49267=CARTESIAN_POINT('Ctrl Pts',(0.127204302154861,117.691498376097,11.46469304358));
#49268=CARTESIAN_POINT('Ctrl Pts',(0.204594489606238,117.701423817813,11.4718936477988));
#49269=CARTESIAN_POINT('Ctrl Pts',(0.281300662862718,117.711348164116,11.4839540427299));
#49270=CARTESIAN_POINT('Ctrl Pts',(0.356745070184129,117.72110926147,11.4958160521226));
#49271=CARTESIAN_POINT('Ctrl Pts',(0.431528619424435,117.730869298819,11.5123785167616));
#49272=CARTESIAN_POINT('Ctrl Pts',(0.505184687685248,117.740563609283,11.5337014305304));
#49273=CARTESIAN_POINT('Ctrl Pts',(0.535928413375962,117.744609972722,11.54260152291));
#49274=CARTESIAN_POINT('Ctrl Pts',(0.566475946798625,117.748644942287,11.5523315502387));
#49275=CARTESIAN_POINT('Ctrl Pts',(0.59679413335784,117.752664064104,11.5628985939744));
#49276=CARTESIAN_POINT('Ctrl Pts',(0.60532443654273,117.75379488133,11.5658717298068));
#49277=CARTESIAN_POINT('Ctrl Pts',(0.613836585694016,117.754924444915,11.5689111375289));
#49278=CARTESIAN_POINT('Ctrl Pts',(0.622329766038321,117.756052622435,11.572015885102));
#49279=CARTESIAN_POINT('Ctrl Pts',(0.718273749250566,117.768797182265,11.6070889480715));
#49280=CARTESIAN_POINT('Ctrl Pts',(0.811526709167048,117.781580106972,11.6506547523446));
#49281=CARTESIAN_POINT('Ctrl Pts',(0.900544082088829,117.794340444296,11.7012952481804));
#49282=CARTESIAN_POINT('Ctrl Pts',(0.99543471658107,117.807942693669,11.7552769443722));
#49283=CARTESIAN_POINT('Ctrl Pts',(1.08551068967412,117.821519213535,11.8172964829959));
#49284=CARTESIAN_POINT('Ctrl Pts',(1.16892107576438,117.834996948096,11.8855815030142));
#49285=CARTESIAN_POINT('Ctrl Pts',(1.21514949032297,117.842466692931,11.9234270083705));
#49286=CARTESIAN_POINT('Ctrl Pts',(1.25933094458218,117.849906112872,11.9631962343358));
#49287=CARTESIAN_POINT('Ctrl Pts',(1.30115581020482,117.85730298323,12.0045832583054));
#49288=CARTESIAN_POINT('Ctrl Pts',(1.30433811149824,117.857865784084,12.0077322458263));
#49289=CARTESIAN_POINT('Ctrl Pts',(1.30750677256674,117.858428338708,12.0108905981791));
#49290=CARTESIAN_POINT('Ctrl Pts',(1.31066183021349,117.858990661359,12.0140584282958));
#49291=CARTESIAN_POINT('Ctrl Pts',(1.39218015888058,117.873519588495,12.0959067637396));
#49292=CARTESIAN_POINT('Ctrl Pts',(1.46448549790502,117.888027757926,12.1841610834581));
#49293=CARTESIAN_POINT('Ctrl Pts',(1.52832261184637,117.902711711588,12.2807762477784));
#49294=CARTESIAN_POINT('Ctrl Pts',(1.58626948775732,117.916040779715,12.3684767497641));
#49295=CARTESIAN_POINT('Ctrl Pts',(1.63723974859756,117.929514685645,12.4630655608177));
#49296=CARTESIAN_POINT('Ctrl Pts',(1.68180326677914,117.943285624186,12.5660476116433));
#49297=CARTESIAN_POINT('Ctrl Pts',(1.70234791144629,117.94963429347,12.613524330889));
#49298=CARTESIAN_POINT('Ctrl Pts',(1.72153097871086,117.956046170297,12.6627856374267));
#49299=CARTESIAN_POINT('Ctrl Pts',(1.73940833428493,117.962536543046,12.7139827773687));
#49300=CARTESIAN_POINT('Ctrl Pts',(1.89901808267227,22.3854922851854,13.1430245619172));
#49301=CARTESIAN_POINT('Ctrl Pts',(1.91613969489008,22.4388279619656,13.5964108599035));
#49302=CARTESIAN_POINT('Ctrl Pts',(1.71821761744411,22.5298182997524,14.3052845584749));
#49303=CARTESIAN_POINT('Ctrl Pts',(0.851232992570897,22.6680906574048,15.079778475839));
#49304=CARTESIAN_POINT('Ctrl Pts',(-0.20609293949006,22.7963599803505,15.2366541763624));
#49305=CARTESIAN_POINT('Ctrl Pts',(-1.31284734837634,22.9401313869705,14.7857986719247));
#49306=CARTESIAN_POINT('Ctrl Pts',(-1.98673499945204,23.0964011152393,13.6207000133225));
#49307=CARTESIAN_POINT('Ctrl Pts',(-1.72784747405538,23.2386153490056,12.4321198834099));
#49308=CARTESIAN_POINT('Ctrl Pts',(-1.16168516194224,23.3380220181386,11.849943041944));
#49309=CARTESIAN_POINT('Ctrl Pts',(-0.815536846787828,23.3878154581211,
11.6489769798242));
#49310=CARTESIAN_POINT('Ctrl Pts',(-0.603916967857474,23.4162803789959,
11.5630510794694));
#49311=CARTESIAN_POINT('Ctrl Pts',(-0.0574765629675266,23.4874854098496,
11.3968778460358));
#49312=CARTESIAN_POINT('Ctrl Pts',(0.97493037193895,23.6087644299663,11.523756852127));
#49313=CARTESIAN_POINT('Ctrl Pts',(1.94094774955337,23.7812659840327,12.6445967993243));
#49314=CARTESIAN_POINT('Ctrl Pts',(1.89788000011945,23.9555004545731,14.1415343184278));
#49315=CARTESIAN_POINT('Ctrl Pts',(1.01652133303839,24.1026054592893,15.0447532345077));
#49316=CARTESIAN_POINT('Ctrl Pts',(0.0737468811550872,24.2216732044994,
15.2763220602092));
#49317=CARTESIAN_POINT('Ctrl Pts',(-0.898370169248287,24.3417518600375,
15.156344869436));
#49318=CARTESIAN_POINT('Ctrl Pts',(-1.70997761919059,24.4634436928123,14.5022214873614));
#49319=CARTESIAN_POINT('Ctrl Pts',(-2.03808699269719,24.5869882902184,13.5494030506149));
#49320=CARTESIAN_POINT('Ctrl Pts',(-2.00577746566736,24.7118373079241,12.5318452734765));
#49321=CARTESIAN_POINT('Ctrl Pts',(-1.45608643562398,24.8281603678822,11.7018449784035));
#49322=CARTESIAN_POINT('Ctrl Pts',(-0.534872821177135,24.9570582485252,
11.2162952702369));
#49323=CARTESIAN_POINT('Ctrl Pts',(0.534301246424838,25.0874961960025,11.0852460992961));
#49324=CARTESIAN_POINT('Ctrl Pts',(1.49649042191416,25.2150609213097,11.604772215406));
#49325=CARTESIAN_POINT('Ctrl Pts',(1.96187327074999,25.3165078617568,12.2763104036369));
#49326=CARTESIAN_POINT('Ctrl Pts',(2.18730068378442,25.3845718318905,12.7752090509047));
#49327=CARTESIAN_POINT('Ctrl Pts',(2.28997050485051,25.4704763225682,13.4681040828783));
#49328=CARTESIAN_POINT('Ctrl Pts',(2.13265524663939,25.5575042190843,14.1597458020817));
#49329=CARTESIAN_POINT('Ctrl Pts',(1.89449930397993,25.6190258395685,14.5938340517913));
#49330=CARTESIAN_POINT('Ctrl Pts',(1.725122197418,25.654354604935,14.8209950885772));
#49331=CARTESIAN_POINT('Ctrl Pts',(1.34494084944462,25.7252462124837,15.2438421767498));
#49332=CARTESIAN_POINT('Ctrl Pts',(0.501632786354249,25.841769628763,15.7232686865407));
#49333=CARTESIAN_POINT('Ctrl Pts',(-0.867995626280332,26.0063411933124,
15.6711561235961));
#49334=CARTESIAN_POINT('Ctrl Pts',(-2.07840568160389,26.181656386924,14.8548222868116));
#49335=CARTESIAN_POINT('Ctrl Pts',(-2.46671766690266,26.3035423891514,13.90616329438));
#49336=CARTESIAN_POINT('Ctrl Pts',(-2.50116807429277,26.3690142660915,13.3823003528019));
#49337=CARTESIAN_POINT('Ctrl Pts',(1.89745606312038,22.1838751864406,13.1425059908936));
#49338=CARTESIAN_POINT('Ctrl Pts',(1.91889546766375,22.2371618336946,13.5972022198302));
#49339=CARTESIAN_POINT('Ctrl Pts',(1.73104184020844,22.3284542101753,14.3110046545806));
#49340=CARTESIAN_POINT('Ctrl Pts',(0.86568005728612,22.4681490366909,15.1044063130677));
#49341=CARTESIAN_POINT('Ctrl Pts',(-0.208364405618377,22.5987783158082,
15.2797778720042));
#49342=CARTESIAN_POINT('Ctrl Pts',(-1.34875877659589,22.7461331969493,14.8331662634924));
#49343=CARTESIAN_POINT('Ctrl Pts',(-2.06307172611114,22.907673614335,13.6398788074659));
#49344=CARTESIAN_POINT('Ctrl Pts',(-1.81136828346712,23.0559625763966,12.3966281499362));
#49345=CARTESIAN_POINT('Ctrl Pts',(-1.22573074374783,23.1602868256609,11.7777180850658));
#49346=CARTESIAN_POINT('Ctrl Pts',(-0.864316318410229,23.2126975916322,
11.5613857654943));
#49347=CARTESIAN_POINT('Ctrl Pts',(-0.642511578839508,23.2427032710701,
11.4678676191461));
#49348=CARTESIAN_POINT('Ctrl Pts',(-0.0684751251893176,23.3178339145423,
11.2849180188622));
#49349=CARTESIAN_POINT('Ctrl Pts',(1.02727112385617,23.4463590679339,11.4033876706341));
#49350=CARTESIAN_POINT('Ctrl Pts',(2.07500014479947,23.6304250145684,12.5840481667664));
#49351=CARTESIAN_POINT('Ctrl Pts',(2.05172154059502,23.8174703500441,14.1912761391829));
#49352=CARTESIAN_POINT('Ctrl Pts',(1.11445288131786,23.976195483412,15.1788657585492));
#49353=CARTESIAN_POINT('Ctrl Pts',(0.0975471875992922,24.1050695693536,
15.442820271682));
#49354=CARTESIAN_POINT('Ctrl Pts',(-0.957915377985352,24.2352719613535,
15.3264954005426));
#49355=CARTESIAN_POINT('Ctrl Pts',(-1.84913680784375,24.3675342639,14.6273375566598));
#49356=CARTESIAN_POINT('Ctrl Pts',(-2.21930990799663,24.5020294856332,13.5947971624621));
#49357=CARTESIAN_POINT('Ctrl Pts',(-2.19793297618546,24.6380579027441,12.4859601647338));
#49358=CARTESIAN_POINT('Ctrl Pts',(-1.60976628295625,24.7649137460929,11.5736243555951));
#49359=CARTESIAN_POINT('Ctrl Pts',(-0.611501641164774,24.9055128600071,
11.0320566514164));
#49360=CARTESIAN_POINT('Ctrl Pts',(0.552802652311208,25.047791884706,10.8753244014993));
#49361=CARTESIAN_POINT('Ctrl Pts',(1.60824932137011,25.186880522897,11.4296603515728));
#49362=CARTESIAN_POINT('Ctrl Pts',(2.12347369309861,25.2973992201485,12.1553207266224));
#49363=CARTESIAN_POINT('Ctrl Pts',(2.3750851755453,25.3715225705239,12.6957361107479));
#49364=CARTESIAN_POINT('Ctrl Pts',(2.49521255144033,25.4650159651105,13.4484599298977));
#49365=CARTESIAN_POINT('Ctrl Pts',(2.33247101541913,25.5596369978143,14.2021831444921));
#49366=CARTESIAN_POINT('Ctrl Pts',(2.07897058752978,25.6264683921513,14.6764770325329));
#49367=CARTESIAN_POINT('Ctrl Pts',(1.89778840277349,25.6648284026719,14.9250865509826));
#49368=CARTESIAN_POINT('Ctrl Pts',(1.49019255835625,25.7417767105877,15.3884618689839));
#49369=CARTESIAN_POINT('Ctrl Pts',(0.581448415540573,25.8681129363819,15.9177505457125));
#49370=CARTESIAN_POINT('Ctrl Pts',(-0.900453073796818,26.0461313544131,
15.8764698702819));
#49371=CARTESIAN_POINT('Ctrl Pts',(-2.21491668089787,26.2352800753748,15.0088027917896));
#49372=CARTESIAN_POINT('Ctrl Pts',(-2.64230284098423,26.3663838566027,13.9924904480118));
#49373=CARTESIAN_POINT('Ctrl Pts',(-2.68486387351535,26.4366806810332,13.4305008334684));
#49374=CARTESIAN_POINT('Ctrl Pts',(1.89589404356848,21.9822580876958,13.14198741987));
#49375=CARTESIAN_POINT('Ctrl Pts',(1.92165124043742,22.0354957054235,13.5979935797571));
#49376=CARTESIAN_POINT('Ctrl Pts',(1.74386606297277,22.1270901205983,14.316724750686));
#49377=CARTESIAN_POINT('Ctrl Pts',(0.880127122001338,22.2682074159771,15.1290341502964));
#49378=CARTESIAN_POINT('Ctrl Pts',(-0.210635871746706,22.4011966512656,
15.322901567646));
#49379=CARTESIAN_POINT('Ctrl Pts',(-1.38467020481544,22.552135006928,14.8805338550601));
#49380=CARTESIAN_POINT('Ctrl Pts',(-2.13940845277027,22.7189461134307,13.6590576016092));
#49381=CARTESIAN_POINT('Ctrl Pts',(-1.89488909287888,22.8733098037875,12.3611364164627));
#49382=CARTESIAN_POINT('Ctrl Pts',(-1.28977632555346,22.9825516331833,11.7054931281874));
#49383=CARTESIAN_POINT('Ctrl Pts',(-0.913095790032648,23.0375797251433,
11.4737945511643));
#49384=CARTESIAN_POINT('Ctrl Pts',(-0.681106189821558,23.0691261631444,
11.372684158823));
#49385=CARTESIAN_POINT('Ctrl Pts',(-0.0794736874111196,23.1481824192349,
11.1729581916887));
#49386=CARTESIAN_POINT('Ctrl Pts',(1.07961187577341,23.2839537059015,11.2830184891413));
#49387=CARTESIAN_POINT('Ctrl Pts',(2.20905254004556,23.4795840451043,12.5234995342084));
#49388=CARTESIAN_POINT('Ctrl Pts',(2.20556308107057,23.6794402455151,14.241017959938));
#49389=CARTESIAN_POINT('Ctrl Pts',(1.21238442959733,23.849785507535,15.3129782825907));
#49390=CARTESIAN_POINT('Ctrl Pts',(0.12134749404349,23.9884659342077,15.6093184831547));
#49391=CARTESIAN_POINT('Ctrl Pts',(-1.01746058672243,24.1287920626696,15.4966459316494));
#49392=CARTESIAN_POINT('Ctrl Pts',(-1.98829599649688,24.2716248349878,14.7524536259582));
#49393=CARTESIAN_POINT('Ctrl Pts',(-2.40053282329608,24.4170706810479,13.6401912743091));
#49394=CARTESIAN_POINT('Ctrl Pts',(-2.39008848670359,24.5642784975641,12.4400750559912));
#49395=CARTESIAN_POINT('Ctrl Pts',(-1.76344613028854,24.7016671243036,11.4454037327865));
#49396=CARTESIAN_POINT('Ctrl Pts',(-0.68813046115242,24.8539674714891,10.847818032596));
#49397=CARTESIAN_POINT('Ctrl Pts',(0.571304058197572,25.0080875734096,10.6654027037025));
#49398=CARTESIAN_POINT('Ctrl Pts',(1.72000822082606,25.1587001244841,11.2545484877396));
#49399=CARTESIAN_POINT('Ctrl Pts',(2.28507411544722,25.2782905785403,12.0343310496079));
#49400=CARTESIAN_POINT('Ctrl Pts',(2.56286966730619,25.3584733091573,12.6162631705913));
#49401=CARTESIAN_POINT('Ctrl Pts',(2.70045459803015,25.4595556076531,13.428815776917));
#49402=CARTESIAN_POINT('Ctrl Pts',(2.53228678419889,25.5617697765442,14.2446204869025));
#49403=CARTESIAN_POINT('Ctrl Pts',(2.26344187107965,25.6339109447338,14.7591200132746));
#49404=CARTESIAN_POINT('Ctrl Pts',(2.070454608129,25.6753022004089,15.0291780133881));
#49405=CARTESIAN_POINT('Ctrl Pts',(1.63544426726789,25.758307208692,15.533081561218));
#49406=CARTESIAN_POINT('Ctrl Pts',(0.661264044726898,25.8944562440005,16.1122324048843));
#49407=CARTESIAN_POINT('Ctrl Pts',(-0.932910521313303,26.0859215155139,
16.0817836169678));
#49408=CARTESIAN_POINT('Ctrl Pts',(-2.35142768019183,26.2889037638257,15.1627832967678));
#49409=CARTESIAN_POINT('Ctrl Pts',(-2.8178880150658,26.4292253240541,14.0788176016433));
#49410=CARTESIAN_POINT('Ctrl Pts',(-2.86855967273795,26.5043470959747,13.4787013141351));
#49411=CARTESIAN_POINT('Ctrl Pts',(1.89433202401659,21.780640988951,13.1414688488465));
#49412=CARTESIAN_POINT('Ctrl Pts',(1.9244070132111,21.8338295771525,13.5987849396839));
#49413=CARTESIAN_POINT('Ctrl Pts',(1.75669028573709,21.9257260310212,14.3224448467915));
#49414=CARTESIAN_POINT('Ctrl Pts',(0.894574186716559,22.0682657952632,15.1536619875252));
#49415=CARTESIAN_POINT('Ctrl Pts',(-0.212907337875024,22.2036149867232,
15.3660252632878));
#49416=CARTESIAN_POINT('Ctrl Pts',(-1.42058163303499,22.3581368169068,14.9279014466279));
#49417=CARTESIAN_POINT('Ctrl Pts',(-2.21574517942938,22.5302186125265,13.6782363957527));
#49418=CARTESIAN_POINT('Ctrl Pts',(-1.97840990229062,22.6906570311784,12.3256446829891));
#49419=CARTESIAN_POINT('Ctrl Pts',(-1.35382190735905,22.8048164407056,11.6332681713093));
#49420=CARTESIAN_POINT('Ctrl Pts',(-0.961875261655053,22.8624618586543,
11.3862033368344));
#49421=CARTESIAN_POINT('Ctrl Pts',(-0.719700800803596,22.8955490552187,
11.2775006984997));
#49422=CARTESIAN_POINT('Ctrl Pts',(-0.0904722496329132,22.9785309239276,
11.0609983645151));
#49423=CARTESIAN_POINT('Ctrl Pts',(1.13195262769064,23.1215483438691,11.1626493076482));
#49424=CARTESIAN_POINT('Ctrl Pts',(2.34310493529166,23.3287430756401,12.4629509016504));
#49425=CARTESIAN_POINT('Ctrl Pts',(2.35940462154613,23.5414101409862,14.290759780693));
#49426=CARTESIAN_POINT('Ctrl Pts',(1.31031597787682,23.7233755316578,15.4470908066323));
#49427=CARTESIAN_POINT('Ctrl Pts',(0.145147800487696,23.8718622990619,15.7758166946274));
#49428=CARTESIAN_POINT('Ctrl Pts',(-1.07700579545949,24.0223121639856,15.666796462756));
#49429=CARTESIAN_POINT('Ctrl Pts',(-2.12745518515003,24.1757154060755,14.8775696952566));
#49430=CARTESIAN_POINT('Ctrl Pts',(-2.58175573859553,24.3321118764628,13.6855853861563));
#49431=CARTESIAN_POINT('Ctrl Pts',(-2.58224399722169,24.4904990923843,12.3941899472485));
#49432=CARTESIAN_POINT('Ctrl Pts',(-1.91712597762081,24.6384205025145,11.317183109978));
#49433=CARTESIAN_POINT('Ctrl Pts',(-0.764759281140061,24.8024220829711,
10.6635794137756));
#49434=CARTESIAN_POINT('Ctrl Pts',(0.589805464083942,24.9683832621133,10.4554810059057));
#49435=CARTESIAN_POINT('Ctrl Pts',(1.831767120282,25.1305197260712,11.0794366239064));
#49436=CARTESIAN_POINT('Ctrl Pts',(2.44667453779583,25.259181936932,11.9133413725934));
#49437=CARTESIAN_POINT('Ctrl Pts',(2.75065415906708,25.3454240477907,12.5367902304347));
#49438=CARTESIAN_POINT('Ctrl Pts',(2.90569664461998,25.4540952501954,13.4091716239364));
#49439=CARTESIAN_POINT('Ctrl Pts',(2.73210255297864,25.5639025552742,14.287057829313));
#49440=CARTESIAN_POINT('Ctrl Pts',(2.44791315462951,25.6413534973164,14.8417629940163));
#49441=CARTESIAN_POINT('Ctrl Pts',(2.2431208134845,25.6857759981459,15.1332694757937));
#49442=CARTESIAN_POINT('Ctrl Pts',(1.78069597617953,25.7748377067961,15.677701253452));
#49443=CARTESIAN_POINT('Ctrl Pts',(0.74107967391322,25.9207995516194,16.3067142640562));
#49444=CARTESIAN_POINT('Ctrl Pts',(-0.96536796882979,26.1257116766147,16.2870973636537));
#49445=CARTESIAN_POINT('Ctrl Pts',(-2.48793867948582,26.3425274522765,15.3167638017459));
#49446=CARTESIAN_POINT('Ctrl Pts',(-2.99347318914736,26.4920667915054,14.165144755275));
#49447=CARTESIAN_POINT('Ctrl Pts',(-3.05225547196054,26.5720135109164,13.5269017948015));
#49448=CARTESIAN_POINT('',(1.9,21.8,13.3));
#49449=CARTESIAN_POINT('Ctrl Pts',(1.90000000000001,21.8,13.3));
#49450=CARTESIAN_POINT('Ctrl Pts',(1.90034617523604,21.8090010354302,13.3759055909997));
#49451=CARTESIAN_POINT('Ctrl Pts',(1.89706050239537,21.8178848211233,13.4497039057687));
#49452=CARTESIAN_POINT('Ctrl Pts',(1.89024211642034,21.8266870935422,13.5215832394767));
#49453=CARTESIAN_POINT('Ctrl Pts',(1.88321809876848,21.8357548284979,13.5956303395703));
#49454=CARTESIAN_POINT('Ctrl Pts',(1.87244522789137,21.8447360075938,13.6676409355473));
#49455=CARTESIAN_POINT('Ctrl Pts',(1.8579806294168,21.8536683860142,13.7377960259859));
#49456=CARTESIAN_POINT('Ctrl Pts',(1.84367989488745,21.8624995729102,13.8071563560364));
#49457=CARTESIAN_POINT('Ctrl Pts',(1.82577044097264,21.8712830015836,13.874702816309));
#49458=CARTESIAN_POINT('Ctrl Pts',(1.80425871233331,21.8800547258861,13.9405881368359));
#49459=CARTESIAN_POINT('Ctrl Pts',(1.78237724778465,21.8889772154532,14.0076058707222));
#49460=CARTESIAN_POINT('Ctrl Pts',(1.75676871234439,21.897887536015,14.0729048292138));
#49461=CARTESIAN_POINT('Ctrl Pts',(1.72738931112095,21.9068240537372,14.1366241000423));
#49462=CARTESIAN_POINT('Ctrl Pts',(1.69800990989751,21.9157605714594,14.2003433708709));
#49463=CARTESIAN_POINT('Ctrl Pts',(1.66485962352026,21.9247232267287,14.2624828718383));
#49464=CARTESIAN_POINT('Ctrl Pts',(1.62784413803072,21.9337516952225,14.323161258052));
#49465=CARTESIAN_POINT('Ctrl Pts',(1.60707419358073,21.9388177043969,14.3572088112396));
#49466=CARTESIAN_POINT('Ctrl Pts',(1.58518200176035,21.9438793654298,14.3907313388816));
#49467=CARTESIAN_POINT('Ctrl Pts',(1.56216457238228,21.9489444761508,14.4237311549527));
#49468=CARTESIAN_POINT('Ctrl Pts',(1.51717383901757,21.9588449321126,14.4882338368792));
#49469=CARTESIAN_POINT('Ctrl Pts',(1.4678811340779,21.9687589700013,14.5507411453126));
#49470=CARTESIAN_POINT('Ctrl Pts',(1.41473793359226,21.9786978113935,14.6105568327851));
#49471=CARTESIAN_POINT('Ctrl Pts',(1.36146953824052,21.9886600667297,14.6705134341828));
#49472=CARTESIAN_POINT('Ctrl Pts',(1.30433212071809,21.9986472232976,14.7277644362177));
#49473=CARTESIAN_POINT('Ctrl Pts',(1.24382892666125,22.0086641846916,14.7815892869782));
#49474=CARTESIAN_POINT('Ctrl Pts',(1.18369020234143,22.0186208041592,14.8350898981757));
#49475=CARTESIAN_POINT('Ctrl Pts',(1.12022606881676,22.0286068499976,14.885204124714));
#49476=CARTESIAN_POINT('Ctrl Pts',(1.05398172255351,22.0386211344547,14.9312252524384));
#49477=CARTESIAN_POINT('Ctrl Pts',(0.987737376290259,22.0486354189118,14.9772463801628));
#49478=CARTESIAN_POINT('Ctrl Pts',(0.918712930155135,22.0586779344765,15.0191729398781));
#49479=CARTESIAN_POINT('Ctrl Pts',(0.847504407217753,22.068741671468,15.0563205105648));
#49480=CARTESIAN_POINT('Ctrl Pts',(0.776019618274311,22.0788444524997,15.0936122017944));
#49481=CARTESIAN_POINT('Ctrl Pts',(0.7022810315133,22.0889425867954,15.1264768539342));
#49482=CARTESIAN_POINT('Ctrl Pts',(0.626749433413019,22.0990327790289,15.1543406173158));
#49483=CARTESIAN_POINT('Ctrl Pts',(0.521406870438683,22.1131053888706,15.1932017075423));
#49484=CARTESIAN_POINT('Ctrl Pts',(0.412576666681248,22.127162529881,15.2223376131965));
#49485=CARTESIAN_POINT('Ctrl Pts',(0.301790749552458,22.1412276519157,15.2418700938868));
#49486=CARTESIAN_POINT('Ctrl Pts',(0.191666938041238,22.1552087145631,15.2612858398376));
#49487=CARTESIAN_POINT('Ctrl Pts',(0.079609407275202,22.1691976620542,15.2712125593463));
#49488=CARTESIAN_POINT('Ctrl Pts',(-0.0328784186612369,22.1832177494457,
15.2717194946849));
#49489=CARTESIAN_POINT('Ctrl Pts',(-0.0916837471965429,22.190547038978,
15.2719845055773));
#49490=CARTESIAN_POINT('Ctrl Pts',(-0.150606570501646,22.1978848425051,
15.2696743612906));
#49491=CARTESIAN_POINT('Ctrl Pts',(-0.209430405166893,22.2052345084796,
15.2647934813694));
#49492=CARTESIAN_POINT('Ctrl Pts',(-0.293235601605187,22.2157054375554,
15.2578397847442));
#49493=CARTESIAN_POINT('Ctrl Pts',(-0.376827517946635,22.2261880737978,
15.2457661402555));
#49494=CARTESIAN_POINT('Ctrl Pts',(-0.459536375158249,22.2366976635983,
15.2284990899665));
#49495=CARTESIAN_POINT('Ctrl Pts',(-0.497767673881477,22.2415556108686,
15.2205175777086));
#49496=CARTESIAN_POINT('Ctrl Pts',(-0.535809564887223,22.2464192336659,
15.2114265062888));
#49497=CARTESIAN_POINT('Ctrl Pts',(-0.573592271050726,22.2512896053801,
15.2012195186864));
#49498=CARTESIAN_POINT('Ctrl Pts',(-0.655205552149098,22.2618099480483,
15.1791717134083));
#49499=CARTESIAN_POINT('Ctrl Pts',(-0.735612228619729,22.2723621681961,
15.1519150840058));
#49500=CARTESIAN_POINT('Ctrl Pts',(-0.814123694366391,22.2829457456128,
15.1196337113446));
#49501=CARTESIAN_POINT('Ctrl Pts',(-0.892191040472025,22.2934694543906,
15.0875349462999));
#49502=CARTESIAN_POINT('Ctrl Pts',(-0.968383848101112,22.3040241596809,
15.0504673884392));
#49503=CARTESIAN_POINT('Ctrl Pts',(-1.04198865827739,22.3146035515234,15.0086475436306));
#49504=CARTESIAN_POINT('Ctrl Pts',(-1.1094759609872,22.3243036596829,14.9703034664009));
#49505=CARTESIAN_POINT('Ctrl Pts',(-1.17478665200284,22.3340244571065,14.9279642837113));
#49506=CARTESIAN_POINT('Ctrl Pts',(-1.23735227846962,22.3437568153301,14.8818304976722));
#49507=CARTESIAN_POINT('Ctrl Pts',(-1.33686420100706,22.3592363323164,14.808453757089));
#49508=CARTESIAN_POINT('Ctrl Pts',(-1.43002938158697,22.3747533541792,14.7258857054826));
#49509=CARTESIAN_POINT('Ctrl Pts',(-1.5148938053479,22.3902984772833,14.634910568396));
#49510=CARTESIAN_POINT('Ctrl Pts',(-1.5439567183862,22.3956221045575,14.6037549630125));
#49511=CARTESIAN_POINT('Ctrl Pts',(-1.5720460240266,22.4009489972205,14.5716138111196));
#49512=CARTESIAN_POINT('Ctrl Pts',(-1.59908316744238,22.4062786834821,14.5385200116539));
#49513=CARTESIAN_POINT('Ctrl Pts',(-1.61008158302221,22.4084467418274,14.5250578143337));
#49514=CARTESIAN_POINT('Ctrl Pts',(-1.62090589004253,22.4106152617884,14.5114379829887));
#49515=CARTESIAN_POINT('Ctrl Pts',(-1.63156723422555,22.4127856975921,14.497686110411));
#49516=CARTESIAN_POINT('Ctrl Pts',(-1.64222799992902,22.4149560156289,14.4839349840034));
#49517=CARTESIAN_POINT('Ctrl Pts',(-1.65272582151843,22.4171282495049,14.4700518318093));
#49518=CARTESIAN_POINT('Ctrl Pts',(-1.6630471897459,22.4193010708845,14.4560281669034));
#49519=CARTESIAN_POINT('Ctrl Pts',(-1.68368930085215,22.4236465819973,14.4279816867541));
#49520=CARTESIAN_POINT('Ctrl Pts',(-1.70362563026762,22.4279944438579,14.3993731698481));
#49521=CARTESIAN_POINT('Ctrl Pts',(-1.72283016099311,22.432345792295,14.3702521569207));
#49522=CARTESIAN_POINT('Ctrl Pts',(-1.76124376446553,22.4410495182971,14.3120032437189));
#49523=CARTESIAN_POINT('Ctrl Pts',(-1.79672928601972,22.4497672159115,14.2517036122225));
#49524=CARTESIAN_POINT('Ctrl Pts',(-1.82908634094825,22.4584952742547,14.1896720330967));
#49525=CARTESIAN_POINT('Ctrl Pts',(-1.88554175016769,22.473723672097,14.0814415964326));
#49526=CARTESIAN_POINT('Ctrl Pts',(-1.93247076419735,22.4889837873255,13.9679375033174));
#49527=CARTESIAN_POINT('Ctrl Pts',(-1.96889307972031,22.5042661215331,13.8509879908307));
#49528=CARTESIAN_POINT('Ctrl Pts',(-1.97426102130403,22.5065184406433,13.8337519051436));
#49529=CARTESIAN_POINT('Ctrl Pts',(-1.979400828438,22.5087712367606,13.8164410243084));
#49530=CARTESIAN_POINT('Ctrl Pts',(-1.98430945388527,22.5110244736619,13.7990612406476));
#49531=CARTESIAN_POINT('Ctrl Pts',(-1.99959210052039,22.5180397621002,13.7449505542374));
#49532=CARTESIAN_POINT('Ctrl Pts',(-2.01263363809429,22.5250593338859,13.6901719394164));
#49533=CARTESIAN_POINT('Ctrl Pts',(-2.02341162482424,22.5320823127815,13.6349209726575));
#49534=CARTESIAN_POINT('Ctrl Pts',(-2.04842010727672,22.548377939124,13.5067205148826));
#49535=CARTESIAN_POINT('Ctrl Pts',(-2.06129275235582,22.5647344926122,13.3756303213226));
#49536=CARTESIAN_POINT('Ctrl Pts',(-2.06166334293173,22.5811476373884,13.2440592448445));
#49537=CARTESIAN_POINT('Ctrl Pts',(-2.06193254000901,22.5930701494268,13.1484859854469));
#49538=CARTESIAN_POINT('Ctrl Pts',(-2.05560612922728,22.6050225678144,13.0526595946214));
#49539=CARTESIAN_POINT('Ctrl Pts',(-2.04256085155299,22.6170039430696,12.9575039464542));
#49540=CARTESIAN_POINT('Ctrl Pts',(-2.02449774749023,22.6335939178829,12.8257469675751));
#49541=CARTESIAN_POINT('Ctrl Pts',(-1.993551370792,22.6502393264052,12.6952777357297));
#49542=CARTESIAN_POINT('Ctrl Pts',(-1.95044799723897,22.6669360972741,12.5685500336052));
#49543=CARTESIAN_POINT('Ctrl Pts',(-1.90837297422408,22.6832345203597,12.4448457723378));
#49544=CARTESIAN_POINT('Ctrl Pts',(-1.854715159545,22.6995818941742,12.3247077201271));
#49545=CARTESIAN_POINT('Ctrl Pts',(-1.79018285086913,22.7159763850598,12.2103819720975));
#49546=CARTESIAN_POINT('Ctrl Pts',(-1.77914030747185,22.7187817531118,12.1908189491723));
#49547=CARTESIAN_POINT('Ctrl Pts',(-1.76777940798862,22.7215885053195,12.1714260067366));
#49548=CARTESIAN_POINT('Ctrl Pts',(-1.75610376767816,22.7243966380861,12.1522142564495));
#49549=CARTESIAN_POINT('Ctrl Pts',(-1.75609312576069,22.724399197596,12.1521967456445));
#49550=CARTESIAN_POINT('Ctrl Pts',(-1.75608248357209,22.7244017571067,12.1521792349886));
#49551=CARTESIAN_POINT('Ctrl Pts',(-1.75607184111235,22.7244043166181,12.1521617244818));
#49552=CARTESIAN_POINT('Ctrl Pts',(-1.70602464861915,22.73644066582,12.0698168789036));
#49553=CARTESIAN_POINT('Ctrl Pts',(-1.64998124464433,22.7484933761121,11.990774269108));
#49554=CARTESIAN_POINT('Ctrl Pts',(-1.5886224448513,22.7605683218413,11.9157699396956));
#49555=CARTESIAN_POINT('Ctrl Pts',(-1.52697928682789,22.7726992271104,11.8404180138757));
#49556=CARTESIAN_POINT('Ctrl Pts',(-1.45997258035869,22.784852571806,11.7691416615236));
#49557=CARTESIAN_POINT('Ctrl Pts',(-1.3882850840447,22.7970403334136,11.7026357684154));
#49558=CARTESIAN_POINT('Ctrl Pts',(-1.33900586419685,22.8054184106878,11.6569184718689));
#49559=CARTESIAN_POINT('Ctrl Pts',(-1.28751458748217,22.8138128771267,11.6134543165319));
#49560=CARTESIAN_POINT('Ctrl Pts',(-1.23402673793582,22.8222292653591,11.5724562683856));
#49561=CARTESIAN_POINT('Ctrl Pts',(-1.21085154590683,22.8258759143669,11.5546926520379));
#49562=CARTESIAN_POINT('Ctrl Pts',(-1.18730732101797,22.8295269549272,11.5373913333772));
#49563=CARTESIAN_POINT('Ctrl Pts',(-1.16340403922038,22.8331818264926,11.520572756893));
#49564=CARTESIAN_POINT('Ctrl Pts',(-1.09738320232914,22.8432765775616,11.4741198679464));
#49565=CARTESIAN_POINT('Ctrl Pts',(-1.02862130032526,22.853400982747,11.431346416387));
#49566=CARTESIAN_POINT('Ctrl Pts',(-0.957487322430239,22.8635387970186,
11.3925497814004));
#49567=CARTESIAN_POINT('Ctrl Pts',(-0.938375761414071,22.8662625228914,
11.3821262921101));
#49568=CARTESIAN_POINT('Ctrl Pts',(-0.919093132063599,22.8689871836512,
11.3719901073133));
#49569=CARTESIAN_POINT('Ctrl Pts',(-0.89964696783731,22.8717123915825,11.3621475069002));
#49570=CARTESIAN_POINT('Ctrl Pts',(-0.840631475660235,22.8799828908688,
11.3322770449972));
#49571=CARTESIAN_POINT('Ctrl Pts',(-0.7800995080275,22.8882586795186,11.3051108697579));
#49572=CARTESIAN_POINT('Ctrl Pts',(-0.718378889207034,22.8965571443992,
11.2807095405642));
#49573=CARTESIAN_POINT('Ctrl Pts',(-0.66015096252314,22.9043860095967,11.2576890518777));
#49574=CARTESIAN_POINT('Ctrl Pts',(-0.600865963332381,22.9122346929815,
11.23712959669));
#49575=CARTESIAN_POINT('Ctrl Pts',(-0.540681088327972,22.9200672254062,
11.219278553958));
#49576=CARTESIAN_POINT('Ctrl Pts',(-0.53707101234487,22.9205370450609,11.2182077928966));
#49577=CARTESIAN_POINT('Ctrl Pts',(-0.533457713020527,22.9210068046686,
11.2171467822687));
#49578=CARTESIAN_POINT('Ctrl Pts',(-0.529841229840762,22.921476495726,11.2160955774765));
#49579=CARTESIAN_POINT('Ctrl Pts',(-0.47293739841567,22.9288668856218,11.199555315207));
#49580=CARTESIAN_POINT('Ctrl Pts',(-0.415260096998153,22.9362722510411,
11.1853241913507));
#49581=CARTESIAN_POINT('Ctrl Pts',(-0.356992449122508,22.9436918706304,
11.1734995547958));
#49582=CARTESIAN_POINT('Ctrl Pts',(-0.224657608253982,22.9605429743466,
11.1466439762051));
#49583=CARTESIAN_POINT('Ctrl Pts',(-0.0892760184599879,22.9774676839623,
11.1322046530843));
#49584=CARTESIAN_POINT('Ctrl Pts',(0.0467160701239138,22.9944573160433,
11.1303758754179));
#49585=CARTESIAN_POINT('Ctrl Pts',(0.182822450839455,23.0114612267584,11.1285455607879));
#49586=CARTESIAN_POINT('Ctrl Pts',(0.319538748472705,23.0285301696247,11.139347356567));
#49587=CARTESIAN_POINT('Ctrl Pts',(0.454409559166268,23.045654228185,11.1629271179154));
#49588=CARTESIAN_POINT('Ctrl Pts',(0.480790119540459,23.04900367243,11.1675392894792));
#49589=CARTESIAN_POINT('Ctrl Pts',(0.507100077358982,23.0523552216179,11.1726401720616));
#49590=CARTESIAN_POINT('Ctrl Pts',(0.533321083292172,23.0557087961119,11.1782306203905));
#49591=CARTESIAN_POINT('Ctrl Pts',(0.66435187770533,23.0724671741541,11.2061670347114));
#49592=CARTESIAN_POINT('Ctrl Pts',(0.793159418990842,23.0892762164664,11.2463321881611));
#49593=CARTESIAN_POINT('Ctrl Pts',(0.917520791015336,23.1061258989711,11.2979488789536));
#49594=CARTESIAN_POINT('Ctrl Pts',(0.960851012678654,23.1119966968403,11.3159332628274));
#49595=CARTESIAN_POINT('Ctrl Pts',(1.00364171995528,23.1178724184597,11.3353074568489));
#49596=CARTESIAN_POINT('Ctrl Pts',(1.04579984609325,23.1237526081734,11.3560373996693));
#49597=CARTESIAN_POINT('Ctrl Pts',(1.08675652479358,23.1294652207314,11.3761765682081));
#49598=CARTESIAN_POINT('Ctrl Pts',(1.12715108040483,23.1351882832585,11.3976071882125));
#49599=CARTESIAN_POINT('Ctrl Pts',(1.16689591677254,23.1409213493446,11.4203041172429));
#49600=CARTESIAN_POINT('Ctrl Pts',(1.28051631826157,23.1573107304568,11.4851888777472));
#49601=CARTESIAN_POINT('Ctrl Pts',(1.38882683471882,23.1737819846396,11.5604265113867));
#49602=CARTESIAN_POINT('Ctrl Pts',(1.49004567469032,23.1903219342844,11.6448777959143));
#49603=CARTESIAN_POINT('Ctrl Pts',(1.56519864906441,23.2026025177425,11.7075811940539));
#49604=CARTESIAN_POINT('Ctrl Pts',(1.63644184944928,23.214920937324,11.7753626167078));
#49605=CARTESIAN_POINT('Ctrl Pts',(1.70304958895036,23.2272712204125,11.8477376096129));
#49606=CARTESIAN_POINT('Ctrl Pts',(1.79220005105934,23.2438013331708,11.9446071943031));
#49607=CARTESIAN_POINT('Ctrl Pts',(1.87304455589512,23.2603885847949,12.0497067849583));
#49608=CARTESIAN_POINT('Ctrl Pts',(1.94426242074266,23.2770195316268,12.161347316853));
#49609=CARTESIAN_POINT('Ctrl Pts',(1.99795342908258,23.2895575697577,12.2455128944347));
#49610=CARTESIAN_POINT('Ctrl Pts',(2.04617345407436,23.3021204101728,12.3333951026968));
#49611=CARTESIAN_POINT('Ctrl Pts',(2.08837296977119,23.3147017053923,12.424259253471));
#49612=CARTESIAN_POINT('Ctrl Pts',(2.10773883103045,23.320475411883,12.4659578964122));
#49613=CARTESIAN_POINT('Ctrl Pts',(2.12583700996293,23.3262529979351,12.5082844297924));
#49614=CARTESIAN_POINT('Ctrl Pts',(2.14264366952361,23.3320336869479,12.5511537969633));
#49615=CARTESIAN_POINT('Ctrl Pts',(2.16850476118605,23.3409286686004,12.6171186384545));
#49616=CARTESIAN_POINT('Ctrl Pts',(2.19136299542564,23.3498537327965,12.68443503575));
#49617=CARTESIAN_POINT('Ctrl Pts',(2.21110758798156,23.3588032190322,12.7528101322129));
#49618=CARTESIAN_POINT('Ctrl Pts',(2.24365216241923,23.3735544589048,12.8655112887556));
#49619=CARTESIAN_POINT('Ctrl Pts',(2.26773655635913,23.3883722400078,12.9810908979152));
#49620=CARTESIAN_POINT('Ctrl Pts',(2.28254142021421,23.4032287350915,13.0982132722858));
#49621=CARTESIAN_POINT('Ctrl Pts',(2.2978253267114,23.4185659434548,13.2191253884749));
#49622=CARTESIAN_POINT('Ctrl Pts',(2.30321800020739,23.4339444271894,13.3416811846617));
#49623=CARTESIAN_POINT('Ctrl Pts',(2.29882885160258,23.4493306956133,13.464252681421));
#49624=CARTESIAN_POINT('Ctrl Pts',(2.29425118527407,23.465377817556,13.5920887298371));
#49625=CARTESIAN_POINT('Ctrl Pts',(2.27903224885156,23.4814334301426,13.7199407845635));
#49626=CARTESIAN_POINT('Ctrl Pts',(2.25334613239327,23.4974549071042,13.8459290279421));
#49627=CARTESIAN_POINT('Ctrl Pts',(2.22930897513146,23.5124478610573,13.9638292649883));
#49628=CARTESIAN_POINT('Ctrl Pts',(2.19610540563927,23.527410870655,14.0800958534789));
#49629=CARTESIAN_POINT('Ctrl Pts',(2.15392753614281,23.5423053741867,14.1931793929172));
#49630=CARTESIAN_POINT('Ctrl Pts',(2.15103411638287,23.5433271434545,14.200936971748));
#49631=CARTESIAN_POINT('Ctrl Pts',(2.14809848387044,23.5443485889938,14.2086795723589));
#49632=CARTESIAN_POINT('Ctrl Pts',(2.14512070981644,23.5453696977673,14.2164066955463));
#49633=CARTESIAN_POINT('Ctrl Pts',(2.10996949583209,23.5574234037735,14.3076217292327));
#49634=CARTESIAN_POINT('Ctrl Pts',(2.06897791375395,23.569504711142,14.3968612204971));
#49635=CARTESIAN_POINT('Ctrl Pts',(2.02223032330238,23.5816177990558,14.483331947589));
#49636=CARTESIAN_POINT('Ctrl Pts',(1.95119959217953,23.6000230576446,14.6147200877418));
#49637=CARTESIAN_POINT('Ctrl Pts',(1.86687763322092,23.6185015297287,14.7397136812518));
#49638=CARTESIAN_POINT('Ctrl Pts',(1.77116245925139,23.6370695232595,14.856132200404));
#49639=CARTESIAN_POINT('Ctrl Pts',(1.67390402864993,23.6559368964808,14.9744277850653));
#49640=CARTESIAN_POINT('Ctrl Pts',(1.56488382774509,23.674896701891,15.0838687275083));
#49641=CARTESIAN_POINT('Ctrl Pts',(1.44612313093434,23.6939696171635,15.1822113192552));
#49642=CARTESIAN_POINT('Ctrl Pts',(1.3302949809633,23.7125715667133,15.2781255465315));
#49643=CARTESIAN_POINT('Ctrl Pts',(1.20520292293797,23.7312811333672,15.363482535802));
#49644=CARTESIAN_POINT('Ctrl Pts',(1.07272586484995,23.750120643866,15.4362494088806));
#49645=CARTESIAN_POINT('Ctrl Pts',(1.04594961399663,23.7539284840034,15.4509570426059));
#49646=CARTESIAN_POINT('Ctrl Pts',(1.01887164069649,23.7577416424881,15.4651505066664));
#49647=CARTESIAN_POINT('Ctrl Pts',(0.991507402002442,23.7615603184461,15.4788132733641));
#49648=CARTESIAN_POINT('Ctrl Pts',(0.989372951962116,23.7618581806721,15.4798789888498));
#49649=CARTESIAN_POINT('Ctrl Pts',(0.987236734171534,23.7621560594999,15.4809414585348));
#49650=CARTESIAN_POINT('Ctrl Pts',(0.985098755439263,23.7624539548253,15.4820006743314));
#49651=CARTESIAN_POINT('Ctrl Pts',(0.853241280819933,23.7808263196765,15.547326637546));
#49652=CARTESIAN_POINT('Ctrl Pts',(0.714684835416255,23.7992617702816,15.6002802227186));
#49653=CARTESIAN_POINT('Ctrl Pts',(0.571892893158105,23.8177343014512,15.6402853378414));
#49654=CARTESIAN_POINT('Ctrl Pts',(0.430589480859245,23.8360142663203,15.6798734209423));
#49655=CARTESIAN_POINT('Ctrl Pts',(0.285137078569464,23.8543305250424,15.7067808395966));
#49656=CARTESIAN_POINT('Ctrl Pts',(0.137946779997347,23.872654112305,15.7204051672449));
#49657=CARTESIAN_POINT('Ctrl Pts',(0.0166372293009362,23.8877558286513,
15.7316339036602));
#49658=CARTESIAN_POINT('Ctrl Pts',(-0.105853298504911,23.9029507858283,
15.7339466020836));
#49659=CARTESIAN_POINT('Ctrl Pts',(-0.228084068191911,23.9182050932659,
15.7269919643805));
#49660=CARTESIAN_POINT('Ctrl Pts',(-0.308748575019462,23.9282719625951,
15.7224023473641));
#49661=CARTESIAN_POINT('Ctrl Pts',(-0.389299231225943,23.9383646229679,
15.7137774593658));
#49662=CARTESIAN_POINT('Ctrl Pts',(-0.469317257680067,23.948472685808,15.7010278929291));
#49663=CARTESIAN_POINT('Ctrl Pts',(-0.566247339062064,23.960717118683,15.6855836665833));
#49664=CARTESIAN_POINT('Ctrl Pts',(-0.662395564656194,23.9729841799441,
15.664086476296));
#49665=CARTESIAN_POINT('Ctrl Pts',(-0.75705030671739,23.9852545166603,15.6368308527521));
#49666=CARTESIAN_POINT('Ctrl Pts',(-0.879291061645446,24.001100898899,15.6016318978399));
#49667=CARTESIAN_POINT('Ctrl Pts',(-0.999240921484818,24.0168963352913,
15.5566670380693));
#49668=CARTESIAN_POINT('Ctrl Pts',(-1.11539944299005,24.0327012286101,15.5026136497645));
#49669=CARTESIAN_POINT('Ctrl Pts',(-1.23256398476096,24.0486430042064,15.4480921184137));
#49670=CARTESIAN_POINT('Ctrl Pts',(-1.34587113347849,24.0645944091951,15.3843253628821));
#49671=CARTESIAN_POINT('Ctrl Pts',(-1.45383298371875,24.0806237318463,15.3120172562257));
#49672=CARTESIAN_POINT('Ctrl Pts',(-1.56239279217184,24.0967418346092,15.2393086634149));
#49673=CARTESIAN_POINT('Ctrl Pts',(-1.66554821936208,24.1129387350077,15.1579650704219));
#49674=CARTESIAN_POINT('Ctrl Pts',(-1.76183724711987,24.1292900331302,15.06869090456));
#49675=CARTESIAN_POINT('Ctrl Pts',(-1.77787018829626,24.1320126631854,15.0538259974863));
#49676=CARTESIAN_POINT('Ctrl Pts',(-1.79371286406918,24.1347395874191,15.0387411663101));
#49677=CARTESIAN_POINT('Ctrl Pts',(-1.80935864822686,24.1374711708594,15.0234395982253));
#49678=CARTESIAN_POINT('',(1.9,22.4,13.3));
#49679=CARTESIAN_POINT('',(1.9,22.4,13.3));
#49680=CARTESIAN_POINT('Ctrl Pts',(1.9,22.4,13.3));
#49681=CARTESIAN_POINT('Ctrl Pts',(1.89077819837431,22.4422021414379,13.6519691914269));
#49682=CARTESIAN_POINT('Ctrl Pts',(1.71537787585695,22.5206083204434,14.2515774145128));
#49683=CARTESIAN_POINT('Ctrl Pts',(0.776895987153429,22.6819257904964,15.2190094254541));
#49684=CARTESIAN_POINT('Ctrl Pts',(-1.01219784483332,22.8782378453878,15.2495646232149));
#49685=CARTESIAN_POINT('Ctrl Pts',(-2.18535724516091,23.1134574970354,13.4517991919584));
#49686=CARTESIAN_POINT('Ctrl Pts',(-1.37199074496505,23.3213768149546,11.7396096714547));
#49687=CARTESIAN_POINT('Ctrl Pts',(0.123403026550972,23.504121058761,11.3105725465261));
#49688=CARTESIAN_POINT('Ctrl Pts',(1.35501251051576,23.661466918215,11.8220255257895));
#49689=CARTESIAN_POINT('Ctrl Pts',(1.94832765695265,23.8068375246815,12.9042814161785));
#49690=CARTESIAN_POINT('Ctrl Pts',(1.84336678935325,23.9401410891422,14.0034773628334));
#49691=CARTESIAN_POINT('Ctrl Pts',(1.27754402361024,24.0611907458831,14.8296511355055));
#49692=CARTESIAN_POINT('Ctrl Pts',(0.371246325431991,24.1834651264945,15.2797269167144));
#49693=CARTESIAN_POINT('Ctrl Pts',(-0.765145428848119,24.3208689298072,
15.2281627669602));
#49694=CARTESIAN_POINT('Ctrl Pts',(-1.81032562534546,24.4742008762416,14.4542829226342));
#49695=CARTESIAN_POINT('Ctrl Pts',(-2.17704469672661,24.6445536494329,13.0553638368446));
#49696=CARTESIAN_POINT('Ctrl Pts',(-1.57203155460298,24.8182979987203,11.709895265911));
#49697=CARTESIAN_POINT('Ctrl Pts',(-0.23180116439731,24.99574025007,11.0244995821736));
#49698=CARTESIAN_POINT('Ctrl Pts',(1.27630691611381,25.1771408957878,11.3398317849377));
#49699=CARTESIAN_POINT('Ctrl Pts',(2.27577079055389,25.3627495865527,12.5571271706314));
#49700=CARTESIAN_POINT('Ctrl Pts',(2.29218789520766,25.5527742410498,14.1699219694977));
#49701=CARTESIAN_POINT('Ctrl Pts',(1.26950162628108,25.74739985761,15.4673025113756));
#49702=CARTESIAN_POINT('Ctrl Pts',(-0.379485062712953,25.9467742695935,
15.8456532640155));
#49703=CARTESIAN_POINT('Ctrl Pts',(-1.90561289077789,26.1465422559426,15.107782139803));
#49704=CARTESIAN_POINT('Ctrl Pts',(-2.41085879002264,26.2813144727143,14.08936731534));
#49705=CARTESIAN_POINT('Ctrl Pts',(-2.48616900737713,26.3471379964276,13.5677880585459));
#49706=CARTESIAN_POINT('Ctrl Pts',(-2.53714261746217,33.794702538555,11.5837945911968));
#49707=CARTESIAN_POINT('Ctrl Pts',(-2.20302045656255,33.8670105940936,11.110489816432));
#49708=CARTESIAN_POINT('Ctrl Pts',(-1.27342212310457,34.00910827188,10.375303523525));
#49709=CARTESIAN_POINT('Ctrl Pts',(0.463317385363586,34.2188326311658,10.1881891863586));
#49710=CARTESIAN_POINT('Ctrl Pts',(2.00461530565732,34.4242135651314,10.9298496609176));
#49711=CARTESIAN_POINT('Ctrl Pts',(2.9101807189669,34.626789103856,12.3532946652702));
#49712=CARTESIAN_POINT('Ctrl Pts',(2.9285690247221,34.8264375311958,14.0157823092848));
#49713=CARTESIAN_POINT('Ctrl Pts',(2.07948629363936,35.0230507318404,15.4164655904329));
#49714=CARTESIAN_POINT('Ctrl Pts',(0.644202929896784,35.2165344443341,16.1458951292022));
#49715=CARTESIAN_POINT('Ctrl Pts',(-1.11292611387905,35.4279525102656,15.997334529376));
#49716=CARTESIAN_POINT('Ctrl Pts',(-2.16612159687256,35.5936923565744,15.0466138670219));
#49717=CARTESIAN_POINT('Ctrl Pts',(-2.52608715609147,35.7161456129446,14.1285591261768));
#49718=CARTESIAN_POINT('Ctrl Pts',(-2.65004752744008,35.7972859707521,13.488171032948));
#49719=CARTESIAN_POINT('Ctrl Pts',(-2.55248073601967,35.9379787039982,12.3436775763336));
#49720=CARTESIAN_POINT('Ctrl Pts',(-1.53423707359805,36.1352271943492,10.9940745150984));
#49721=CARTESIAN_POINT('Ctrl Pts',(0.414031698965699,36.3659328772203,10.6302615404033));
#49722=CARTESIAN_POINT('Ctrl Pts',(2.04980546711222,36.590686252149,11.6566868060208));
#49723=CARTESIAN_POINT('Ctrl Pts',(2.51010674367927,36.7913391087015,13.3133883571633));
#49724=CARTESIAN_POINT('Ctrl Pts',(1.96182694676073,36.9695819315518,14.6953200830345));
#49725=CARTESIAN_POINT('Ctrl Pts',(0.913154495044754,37.1268632725084,15.4780580828442));
#49726=CARTESIAN_POINT('Ctrl Pts',(-0.367392365969926,37.281098280273,15.5856567059268));
#49727=CARTESIAN_POINT('Ctrl Pts',(-1.48957786961239,37.4323952581935,15.0136248643657));
#49728=CARTESIAN_POINT('Ctrl Pts',(-2.12989204619479,37.580873057395,13.9555713790989));
#49729=CARTESIAN_POINT('Ctrl Pts',(-2.11563312293493,37.7266668431562,12.7413002907563));
#49730=CARTESIAN_POINT('Ctrl Pts',(-1.4734213597753,37.8699258077578,11.7360649626158));
#49731=CARTESIAN_POINT('Ctrl Pts',(-0.416200202780098,38.0108006676585,
11.2271354294049));
#49732=CARTESIAN_POINT('Ctrl Pts',(0.731872469631232,38.1494725717998,11.3527537042491));
#49733=CARTESIAN_POINT('Ctrl Pts',(1.62909612187799,38.2861087083245,12.0527247864151));
#49734=CARTESIAN_POINT('Ctrl Pts',(2.01607881421587,38.420910106321,13.1070091406949));
#49735=CARTESIAN_POINT('Ctrl Pts',(1.79172084866822,38.5540703969794,14.1931449414799));
#49736=CARTESIAN_POINT('Ctrl Pts',(1.03692345394962,38.6857972959208,14.9894180523881));
#49737=CARTESIAN_POINT('Ctrl Pts',(-0.015088982985104,38.8163035818771,
15.2648321582235));
#49738=CARTESIAN_POINT('Ctrl Pts',(-1.04426227167881,38.9458044926218,14.9462196494202));
#49739=CARTESIAN_POINT('Ctrl Pts',(-1.82985905407118,39.0888382556108,14.0491931927851));
#49740=CARTESIAN_POINT('Ctrl Pts',(-1.92248310902473,39.2453849714331,12.7108350899886));
#49741=CARTESIAN_POINT('Ctrl Pts',(-1.01321098977672,39.4157297322394,11.5639384682371));
#49742=CARTESIAN_POINT('Ctrl Pts',(0.431328930297244,39.5861937286102,11.3330209300884));
#49743=CARTESIAN_POINT('Ctrl Pts',(1.45502419956615,39.728797825825,12.00370853134));
#49744=CARTESIAN_POINT('Ctrl Pts',(1.84542351138279,39.8434880354635,12.8539190362301));
#49745=CARTESIAN_POINT('Ctrl Pts',(1.90901377452895,39.9586677453586,13.7914090498871));
#49746=CARTESIAN_POINT('Ctrl Pts',(1.44201319640107,40.0747166553859,14.6691796791337));
#49747=CARTESIAN_POINT('Ctrl Pts',(0.612739553103985,40.1918981421937,15.1463780893102));
#49748=CARTESIAN_POINT('Ctrl Pts',(0.0790120767017547,40.25828434609,15.230428162705));
#49749=CARTESIAN_POINT('Ctrl Pts',(-0.276763612704706,40.3027552942086,
15.202780730348));
#49750=CARTESIAN_POINT('Ctrl Pts',(-0.5115856699662,40.3324632619737,15.1625337767236));
#49751=CARTESIAN_POINT('Ctrl Pts',(-0.79725179899804,40.3697101209255,15.0717252071008));
#49752=CARTESIAN_POINT('Ctrl Pts',(-1.11514470712696,40.4145899651528,14.9003327976856));
#49753=CARTESIAN_POINT('Ctrl Pts',(-1.68066644673384,40.5047478080795,14.4466263558439));
#49754=CARTESIAN_POINT('Ctrl Pts',(-2.17634554015148,40.6414894617506,13.3813510245936));
#49755=CARTESIAN_POINT('Ctrl Pts',(-1.74732493907859,40.8068384562209,12.0329549479021));
#49756=CARTESIAN_POINT('Ctrl Pts',(-0.493115687221394,40.9962690026588,
11.0836019300558));
#49757=CARTESIAN_POINT('Ctrl Pts',(0.766873073701429,41.1375762814092,11.1873998032218));
#49758=CARTESIAN_POINT('Ctrl Pts',(1.63769882242631,41.2747095576386,11.8683492876489));
#49759=CARTESIAN_POINT('Ctrl Pts',(2.12293894185963,41.3743602909584,12.5220924979612));
#49760=CARTESIAN_POINT('Ctrl Pts',(2.29726804509882,41.5136636354595,13.6710807665245));
#49761=CARTESIAN_POINT('Ctrl Pts',(1.79017023846489,41.6685969694184,14.8567246269234));
#49762=CARTESIAN_POINT('Ctrl Pts',(0.71282329412476,41.8265976614803,15.6134221495628));
#49763=CARTESIAN_POINT('Ctrl Pts',(-0.626664005515929,41.9877563906676,
15.6898056909252));
#49764=CARTESIAN_POINT('Ctrl Pts',(-1.82898756958588,42.1521456502828,15.0362175564882));
#49765=CARTESIAN_POINT('Ctrl Pts',(-2.5759705941618,42.3335725612856,13.7232903735765));
#49766=CARTESIAN_POINT('Ctrl Pts',(-2.46701467117438,42.4619079332118,12.6396216068561));
#49767=CARTESIAN_POINT('Ctrl Pts',(-2.20984257971657,42.5339741612212,12.1210770352365));
#49768=CARTESIAN_POINT('Ctrl Pts',(-2.40023872834448,33.8617379370758,11.7171990219698));
#49769=CARTESIAN_POINT('Ctrl Pts',(-2.08972378175159,33.9296563314948,11.2703464575275));
#49770=CARTESIAN_POINT('Ctrl Pts',(-1.22264220293187,34.062963020044,10.574517277758));
#49771=CARTESIAN_POINT('Ctrl Pts',(0.401620283615534,34.2592803421303,10.3876332565902));
#49772=CARTESIAN_POINT('Ctrl Pts',(1.84648101894249,34.4511554191802,11.0698597282399));
#49773=CARTESIAN_POINT('Ctrl Pts',(2.70086130924968,34.6400836730942,12.3909315353159));
#49774=CARTESIAN_POINT('Ctrl Pts',(2.72977180381108,34.8260078761717,13.9388082726507));
#49775=CARTESIAN_POINT('Ctrl Pts',(1.95023745713216,35.0088847893345,15.2475926736166));
#49776=CARTESIAN_POINT('Ctrl Pts',(0.622012464087979,35.1886854204671,15.9359219413486));
#49777=CARTESIAN_POINT('Ctrl Pts',(-1.01071028039656,35.3850305540958,15.8111919221846));
#49778=CARTESIAN_POINT('Ctrl Pts',(-1.99566752188188,35.5389014813403,14.9368171104688));
#49779=CARTESIAN_POINT('Ctrl Pts',(-2.33707413395951,35.6526009429733,14.08734522877));
#49780=CARTESIAN_POINT('Ctrl Pts',(-2.45723222087079,35.72794749456,13.4937395625812));
#49781=CARTESIAN_POINT('Ctrl Pts',(-2.37578369332297,35.8586209988653,12.4301500330078));
#49782=CARTESIAN_POINT('Ctrl Pts',(-1.44087298808843,36.0419421060423,11.167583556436));
#49783=CARTESIAN_POINT('Ctrl Pts',(0.36908873702616,36.2566957249332,10.8120654899176));
#49784=CARTESIAN_POINT('Ctrl Pts',(1.90430675260224,36.4663895638823,11.7545860581376));
#49785=CARTESIAN_POINT('Ctrl Pts',(2.35071958929505,36.6541730382628,13.3003264205421));
#49786=CARTESIAN_POINT('Ctrl Pts',(1.84928551059103,36.8215462219214,14.6030222361114));
#49787=CARTESIAN_POINT('Ctrl Pts',(0.86921171423766,36.9697311952702,15.3506845341415));
#49788=CARTESIAN_POINT('Ctrl Pts',(-0.340491125387667,37.1155991148782,
15.4655045756358));
#49789=CARTESIAN_POINT('Ctrl Pts',(-1.41209004722825,37.2592980591129,14.9341478868308));
#49790=CARTESIAN_POINT('Ctrl Pts',(-2.03444167603858,37.4009824323719,13.9317371260455));
#49791=CARTESIAN_POINT('Ctrl Pts',(-2.03438454184915,37.5408199942793,12.767224166747));
#49792=CARTESIAN_POINT('Ctrl Pts',(-1.42675985213229,37.6789883174979,11.7905291103843));
#49793=CARTESIAN_POINT('Ctrl Pts',(-0.407448290021044,37.8156610740227,
11.2843509198806));
#49794=CARTESIAN_POINT('Ctrl Pts',(0.714623696940499,37.9510407034962,11.3928816172433));
#49795=CARTESIAN_POINT('Ctrl Pts',(1.60483188112312,38.08530868396,12.0691957199895));
#49796=CARTESIAN_POINT('Ctrl Pts',(2.00125500268751,38.2186781833416,13.1069546625132));
#49797=CARTESIAN_POINT('Ctrl Pts',(1.79220751461922,38.3513491921946,14.1917552318724));
#49798=CARTESIAN_POINT('Ctrl Pts',(1.04587569520604,38.4835318537754,15.0007847356739));
#49799=CARTESIAN_POINT('Ctrl Pts',(-0.013271108315001,38.6154367303176,
15.2936923811263));
#49800=CARTESIAN_POINT('Ctrl Pts',(-1.06519193510901,38.7472727137213,14.9839418685836));
#49801=CARTESIAN_POINT('Ctrl Pts',(-1.88328876777746,38.8939284090276,14.0759218299553));
#49802=CARTESIAN_POINT('Ctrl Pts',(-1.99949277300357,39.0557570565816,12.6943472018712));
#49803=CARTESIAN_POINT('Ctrl Pts',(-1.06936178982378,39.2334335463509,11.4843618678959));
#49804=CARTESIAN_POINT('Ctrl Pts',(0.446044403009374,39.412736616575,11.2189550970895));
#49805=CARTESIAN_POINT('Ctrl Pts',(1.54131410052628,39.5639017725726,11.9136852163027));
#49806=CARTESIAN_POINT('Ctrl Pts',(1.96963148607505,39.6861138284552,12.8137954486716));
#49807=CARTESIAN_POINT('Ctrl Pts',(2.05127330681957,39.8092486198186,13.8147372274146));
#49808=CARTESIAN_POINT('Ctrl Pts',(1.56333544279269,39.933877636358,14.7642723274395));
#49809=CARTESIAN_POINT('Ctrl Pts',(0.676407604025829,40.0602090961192,15.2906307544418));
#49810=CARTESIAN_POINT('Ctrl Pts',(0.101053978248039,40.1319449413606,15.389076917094));
#49811=CARTESIAN_POINT('Ctrl Pts',(-0.284182044219036,40.1800626930222,
15.3642008365041));
#49812=CARTESIAN_POINT('Ctrl Pts',(-0.538878969923101,40.2122223538578,
15.3239558518647));
#49813=CARTESIAN_POINT('Ctrl Pts',(-0.849543410497253,40.252572700832,15.2296458276861));
#49814=CARTESIAN_POINT('Ctrl Pts',(-1.19656882044088,40.3012377839666,15.0483186351474));
#49815=CARTESIAN_POINT('Ctrl Pts',(-1.8164799946024,40.3990797829461,14.5640427909459));
#49816=CARTESIAN_POINT('Ctrl Pts',(-2.37071699481453,40.5477712211053,13.4130859800096));
#49817=CARTESIAN_POINT('Ctrl Pts',(-1.92218168690635,40.7279584153765,11.9380100336219));
#49818=CARTESIAN_POINT('Ctrl Pts',(-0.567095654611867,40.9346017873572,
10.8855790573643));
#49819=CARTESIAN_POINT('Ctrl Pts',(0.809297734590367,41.0888438713821,10.9822321946955));
#49820=CARTESIAN_POINT('Ctrl Pts',(1.768006429168,41.2384680537974,11.7138499166356));
#49821=CARTESIAN_POINT('Ctrl Pts',(2.30552670588767,41.3471689506707,12.4206370433311));
#49822=CARTESIAN_POINT('Ctrl Pts',(2.50974914981252,41.4990127984438,13.6706870932952));
#49823=CARTESIAN_POINT('Ctrl Pts',(1.97209080071686,41.6676811835294,14.9673314840827));
#49824=CARTESIAN_POINT('Ctrl Pts',(0.810223789912052,41.8394078589309,15.8022801288837));
#49825=CARTESIAN_POINT('Ctrl Pts',(-0.641625837636128,42.0142173167945,
15.9004073151369));
#49826=CARTESIAN_POINT('Ctrl Pts',(-1.94982840906498,42.1921184914192,15.2065402529954));
#49827=CARTESIAN_POINT('Ctrl Pts',(-2.7701221386624,42.3879448295554,13.797659693616));
#49828=CARTESIAN_POINT('Ctrl Pts',(-2.66398655743805,42.5260201441487,12.6306928713517));
#49829=CARTESIAN_POINT('Ctrl Pts',(-2.39344664640429,42.6034004278108,12.0713137073846));
#49830=CARTESIAN_POINT('Ctrl Pts',(-2.26333483922681,33.9287733355967,11.8506034527428));
#49831=CARTESIAN_POINT('Ctrl Pts',(-1.97642710694064,33.9923020688959,11.430203098623));
#49832=CARTESIAN_POINT('Ctrl Pts',(-1.17186228275916,34.1168177682079,10.7737310319911));
#49833=CARTESIAN_POINT('Ctrl Pts',(0.339923181867489,34.2997280530948,10.5870773268218));
#49834=CARTESIAN_POINT('Ctrl Pts',(1.6883467322277,34.4780972732292,11.209869795562));
#49835=CARTESIAN_POINT('Ctrl Pts',(2.49154189953247,34.6533782423325,12.4285684053618));
#49836=CARTESIAN_POINT('Ctrl Pts',(2.53097458290008,34.8255782211476,13.8618342360166));
#49837=CARTESIAN_POINT('Ctrl Pts',(1.82098862062497,34.9947188468287,15.0787197568002));
#49838=CARTESIAN_POINT('Ctrl Pts',(0.599821998279183,35.1608363966002,15.725948753495));
#49839=CARTESIAN_POINT('Ctrl Pts',(-0.908494446914065,35.342108597926,15.6250493149932));
#49840=CARTESIAN_POINT('Ctrl Pts',(-1.8252134468912,35.4841106061063,14.8270203539157));
#49841=CARTESIAN_POINT('Ctrl Pts',(-2.14806111182756,35.5890562730018,14.0461313313633));
#49842=CARTESIAN_POINT('Ctrl Pts',(-2.26441691430149,35.6586090183679,13.4993080922143));
#49843=CARTESIAN_POINT('Ctrl Pts',(-2.19908665062627,35.7792632937322,12.5166224896819));
#49844=CARTESIAN_POINT('Ctrl Pts',(-1.3475089025788,35.9486570177353,11.3410925977736));
#49845=CARTESIAN_POINT('Ctrl Pts',(0.324145775086629,36.1474585726462,10.9938694394317));
#49846=CARTESIAN_POINT('Ctrl Pts',(1.75880803809227,36.3420928756156,11.8524853102545));
#49847=CARTESIAN_POINT('Ctrl Pts',(2.19133243491085,36.517006967824,13.2872644839208));
#49848=CARTESIAN_POINT('Ctrl Pts',(1.73674407442132,36.673510512291,14.5107243891885));
#49849=CARTESIAN_POINT('Ctrl Pts',(0.825268933430571,36.8125991180322,15.223310985439));
#49850=CARTESIAN_POINT('Ctrl Pts',(-0.313589884805409,36.9500999494832,
15.3453524453448));
#49851=CARTESIAN_POINT('Ctrl Pts',(-1.33460222484412,37.0862008600325,14.8546709092959));
#49852=CARTESIAN_POINT('Ctrl Pts',(-1.9389913058824,37.2210918073491,13.9079028729921));
#49853=CARTESIAN_POINT('Ctrl Pts',(-1.95313596076338,37.3549731454022,12.7931480427377));
#49854=CARTESIAN_POINT('Ctrl Pts',(-1.38009834448925,37.4880508272381,11.8449932581528));
#49855=CARTESIAN_POINT('Ctrl Pts',(-0.398696377261994,37.6205214803867,
11.3415664103564));
#49856=CARTESIAN_POINT('Ctrl Pts',(0.697374924249768,37.7526088351928,11.4330095302377));
#49857=CARTESIAN_POINT('Ctrl Pts',(1.58056764036826,37.8845086595957,12.0856666535639));
#49858=CARTESIAN_POINT('Ctrl Pts',(1.98643119115913,38.0164462603624,13.1069001843313));
#49859=CARTESIAN_POINT('Ctrl Pts',(1.79269418057024,38.1486279874099,14.1903655222649));
#49860=CARTESIAN_POINT('Ctrl Pts',(1.05482793646247,38.2812664116301,15.0121514189598));
#49861=CARTESIAN_POINT('Ctrl Pts',(-0.0114532336448994,38.4145698787582,
15.3225526040293));
#49862=CARTESIAN_POINT('Ctrl Pts',(-1.0861215985392,38.5487409348208,15.021664087747));
#49863=CARTESIAN_POINT('Ctrl Pts',(-1.93671848148375,38.6990185624443,14.1026504671256));
#49864=CARTESIAN_POINT('Ctrl Pts',(-2.07650243698238,38.86612914173,12.6778593137538));
#49865=CARTESIAN_POINT('Ctrl Pts',(-1.12551258987084,39.0511373604624,11.4047852675546));
#49866=CARTESIAN_POINT('Ctrl Pts',(0.4607598757215,39.2392795045397,11.1048892640904));
#49867=CARTESIAN_POINT('Ctrl Pts',(1.62760400148641,39.3990057193203,11.8236619012656));
#49868=CARTESIAN_POINT('Ctrl Pts',(2.0938394607673,39.5287396214468,12.7736718611132));
#49869=CARTESIAN_POINT('Ctrl Pts',(2.19353283911017,39.6598294942784,13.8380654049421));
#49870=CARTESIAN_POINT('Ctrl Pts',(1.6846576891843,39.79303861733,14.8593649757452));
#49871=CARTESIAN_POINT('Ctrl Pts',(0.740075654947661,39.9285200500448,15.4348834195735));
#49872=CARTESIAN_POINT('Ctrl Pts',(0.123095879794312,40.0056055366311,15.5477256714831));
#49873=CARTESIAN_POINT('Ctrl Pts',(-0.291600475733375,40.0573700918359,
15.5256209426602));
#49874=CARTESIAN_POINT('Ctrl Pts',(-0.566172269880012,40.0919814457418,
15.4853779270059));
#49875=CARTESIAN_POINT('Ctrl Pts',(-0.901835021996476,40.1354352807384,
15.3875664482714));
#49876=CARTESIAN_POINT('Ctrl Pts',(-1.27799293375482,40.18788560278,15.1963044726091));
#49877=CARTESIAN_POINT('Ctrl Pts',(-1.95229354247097,40.2934117578129,14.6814592260479));
#49878=CARTESIAN_POINT('Ctrl Pts',(-2.56508844947758,40.45405298046,13.4448209354256));
#49879=CARTESIAN_POINT('Ctrl Pts',(-2.09703843473412,40.6490783745322,11.8430651193419));
#49880=CARTESIAN_POINT('Ctrl Pts',(-0.641075622002351,40.8729345720558,
10.6875561846728));
#49881=CARTESIAN_POINT('Ctrl Pts',(0.851722395479298,41.0401114613552,10.7770645861692));
#49882=CARTESIAN_POINT('Ctrl Pts',(1.89831403590967,41.2022265499563,11.5593505456222));
#49883=CARTESIAN_POINT('Ctrl Pts',(2.48811446991572,41.319977610383,12.319181588701));
#49884=CARTESIAN_POINT('Ctrl Pts',(2.72223025452621,41.4843619614282,13.6702934200658));
#49885=CARTESIAN_POINT('Ctrl Pts',(2.15401136296883,41.6667653976404,15.0779383412421));
#49886=CARTESIAN_POINT('Ctrl Pts',(0.907624285699337,41.8522180563816,15.9911381082045));
#49887=CARTESIAN_POINT('Ctrl Pts',(-0.656587669756328,42.0406782429216,
16.1110089393486));
#49888=CARTESIAN_POINT('Ctrl Pts',(-2.07066924854409,42.2320913325556,15.3768629495027));
#49889=CARTESIAN_POINT('Ctrl Pts',(-2.964273683163,42.4423170978249,13.8720290136556));
#49890=CARTESIAN_POINT('Ctrl Pts',(-2.86095844370172,42.5901323550855,12.6217641358473));
#49891=CARTESIAN_POINT('Ctrl Pts',(-2.57705071309201,42.6728266944004,12.0215503795327));
#49892=CARTESIAN_POINT('Ctrl Pts',(-2.12643095010913,33.9958087341176,11.9840078835159));
#49893=CARTESIAN_POINT('Ctrl Pts',(-1.86313043212967,34.0549478062971,11.5900597397185));
#49894=CARTESIAN_POINT('Ctrl Pts',(-1.12108236258647,34.1706725163719,10.9729447862239));
#49895=CARTESIAN_POINT('Ctrl Pts',(0.278226080119438,34.3401757640595,10.7865213970534));
#49896=CARTESIAN_POINT('Ctrl Pts',(1.53021244551289,34.5050391272781,11.3498798628842));
#49897=CARTESIAN_POINT('Ctrl Pts',(2.28222248981525,34.6666728115709,12.4662052754075));
#49898=CARTESIAN_POINT('Ctrl Pts',(2.33217736198906,34.8251485661237,13.7848601993824));
#49899=CARTESIAN_POINT('Ctrl Pts',(1.69173978411777,34.9805529043229,14.9098468399839));
#49900=CARTESIAN_POINT('Ctrl Pts',(0.577631532470381,35.1329873727333,15.5159755656414));
#49901=CARTESIAN_POINT('Ctrl Pts',(-0.806278613431565,35.2991866417561,
15.4389067078018));
#49902=CARTESIAN_POINT('Ctrl Pts',(-1.65475937190052,35.4293197308722,14.7172235973626));
#49903=CARTESIAN_POINT('Ctrl Pts',(-1.95904808969561,35.5255116030304,14.0049174339565));
#49904=CARTESIAN_POINT('Ctrl Pts',(-2.0716016077322,35.5892705421757,13.5048766218472));
#49905=CARTESIAN_POINT('Ctrl Pts',(-2.02238960792956,35.6999055885991,12.603094946356));
#49906=CARTESIAN_POINT('Ctrl Pts',(-1.25414481706918,35.8553719294284,11.5146016391112));
#49907=CARTESIAN_POINT('Ctrl Pts',(0.27920281314709,36.0382214203591,11.175673388946));
#49908=CARTESIAN_POINT('Ctrl Pts',(1.61330932358228,36.2177961873488,11.9503845623713));
#49909=CARTESIAN_POINT('Ctrl Pts',(2.03194528052665,36.3798408973854,13.2742025472996));
#49910=CARTESIAN_POINT('Ctrl Pts',(1.62420263825162,36.5254748026605,14.4184265422655));
#49911=CARTESIAN_POINT('Ctrl Pts',(0.781326152623479,36.6554670407941,15.0959374367363));
#49912=CARTESIAN_POINT('Ctrl Pts',(-0.286688644223147,36.7846007840884,
15.2252003150539));
#49913=CARTESIAN_POINT('Ctrl Pts',(-1.25711440246,36.913103660952,14.7751939317609));
#49914=CARTESIAN_POINT('Ctrl Pts',(-1.84354093572621,37.0412011823262,13.8840686199387));
#49915=CARTESIAN_POINT('Ctrl Pts',(-1.87188737967761,37.1691262965253,12.8190719187284));
#49916=CARTESIAN_POINT('Ctrl Pts',(-1.33343683684623,37.2971133369783,11.8994574059213));
#49917=CARTESIAN_POINT('Ctrl Pts',(-0.38994446450294,37.4253818867507,11.3987819008321));
#49918=CARTESIAN_POINT('Ctrl Pts',(0.680126151559037,37.5541769668892,11.4731374432319));
#49919=CARTESIAN_POINT('Ctrl Pts',(1.5563033996134,37.6837086352313,12.1021375871384));
#49920=CARTESIAN_POINT('Ctrl Pts',(1.97160737963077,37.8142143373832,13.1068457061496));
#49921=CARTESIAN_POINT('Ctrl Pts',(1.79318084652126,37.9459067826252,14.1889758126573));
#49922=CARTESIAN_POINT('Ctrl Pts',(1.06378017771889,38.0790009694848,15.0235181022458));
#49923=CARTESIAN_POINT('Ctrl Pts',(-0.00963535897479482,38.2137030271988,
15.3514128269322));
#49924=CARTESIAN_POINT('Ctrl Pts',(-1.10705126196939,38.3502091559204,15.0593863069105));
#49925=CARTESIAN_POINT('Ctrl Pts',(-1.99014819519003,38.5041087158611,14.1293791042958));
#49926=CARTESIAN_POINT('Ctrl Pts',(-2.1535121009612,38.6765012268785,12.6613714256366));
#49927=CARTESIAN_POINT('Ctrl Pts',(-1.18166338991789,38.8688411745739,11.3252086672135));
#49928=CARTESIAN_POINT('Ctrl Pts',(0.47547534843363,39.0658223925045,10.9908234310914));
#49929=CARTESIAN_POINT('Ctrl Pts',(1.71389390244653,39.2341096660681,11.7336385862284));
#49930=CARTESIAN_POINT('Ctrl Pts',(2.21804743545955,39.3713654144385,12.7335482735547));
#49931=CARTESIAN_POINT('Ctrl Pts',(2.33579237140079,39.5104103687383,13.8613935824697));
#49932=CARTESIAN_POINT('Ctrl Pts',(1.80597993557594,39.6521995983019,14.954457624051));
#49933=CARTESIAN_POINT('Ctrl Pts',(0.803743705869504,39.7968310039704,15.579136084705));
#49934=CARTESIAN_POINT('Ctrl Pts',(0.145137781340595,39.8792661319018,15.7063744258721));
#49935=CARTESIAN_POINT('Ctrl Pts',(-0.299018907247705,39.9346774906494,
15.6870410488163));
#49936=CARTESIAN_POINT('Ctrl Pts',(-0.593465569836916,39.971740537626,15.6468000021472));
#49937=CARTESIAN_POINT('Ctrl Pts',(-0.954126633495691,40.0182978606449,
15.5454870688567));
#49938=CARTESIAN_POINT('Ctrl Pts',(-1.35941704706874,40.0745334215935,15.3442903100708));
#49939=CARTESIAN_POINT('Ctrl Pts',(-2.08810709033953,40.1877437326795,14.7988756611499));
#49940=CARTESIAN_POINT('Ctrl Pts',(-2.75945990414063,40.3603347398146,13.4765558908418));
#49941=CARTESIAN_POINT('Ctrl Pts',(-2.27189518256189,40.5701983336878,11.7481202050619));
#49942=CARTESIAN_POINT('Ctrl Pts',(-0.71505558939283,40.8112673567543,10.4895333119812));
#49943=CARTESIAN_POINT('Ctrl Pts',(0.894147056368231,40.9913790513282,10.5718969776429));
#49944=CARTESIAN_POINT('Ctrl Pts',(2.02862164265135,41.165985046115,11.4048511746087));
#49945=CARTESIAN_POINT('Ctrl Pts',(2.67070223394375,41.2927862700951,12.217726134071));
#49946=CARTESIAN_POINT('Ctrl Pts',(2.9347113592399,41.4697111244126,13.6698997468364));
#49947=CARTESIAN_POINT('Ctrl Pts',(2.33593192522078,41.6658496117512,15.1885451984014));
#49948=CARTESIAN_POINT('Ctrl Pts',(1.00502478148663,41.8650282538322,16.1799960875252));
#49949=CARTESIAN_POINT('Ctrl Pts',(-0.671549501876531,42.0671391690486,
16.3216105635603));
#49950=CARTESIAN_POINT('Ctrl Pts',(-2.1915100880232,42.272064173692,15.54718564601));
#49951=CARTESIAN_POINT('Ctrl Pts',(-3.15842522766362,42.4966893660946,13.9463983336952));
#49952=CARTESIAN_POINT('Ctrl Pts',(-3.05793032996539,42.6542445660225,12.6128354003429));
#49953=CARTESIAN_POINT('Ctrl Pts',(-2.76065477977972,42.7422529609897,11.9717870516811));
#49954=CARTESIAN_POINT('Ctrl Pts',(-2.10782919047724,33.9999546381749,11.9560483405783));
#49955=CARTESIAN_POINT('Ctrl Pts',(-2.03273535221384,34.0164964355435,11.847021833405));
#49956=CARTESIAN_POINT('Ctrl Pts',(-1.9492165505024,34.0329315510199,11.7440383142592));
#49957=CARTESIAN_POINT('Ctrl Pts',(-1.85841109175917,34.0493013566143,11.6484909358993));
#49958=CARTESIAN_POINT('Ctrl Pts',(-1.76710699104391,34.065761054075,11.552418876162));
#49959=CARTESIAN_POINT('Ctrl Pts',(-1.66843721253304,34.0821547324428,11.4638653656978));
#49960=CARTESIAN_POINT('Ctrl Pts',(-1.56358057298744,34.0985279043319,11.3841998154946));
#49961=CARTESIAN_POINT('Ctrl Pts',(-1.54652083475084,34.1011917511587,11.3712385625035));
#49962=CARTESIAN_POINT('Ctrl Pts',(-1.52929735445489,34.1038550623631,11.358512463993));
#49963=CARTESIAN_POINT('Ctrl Pts',(-1.51191522969689,34.1065180422329,11.3460272877833));
#49964=CARTESIAN_POINT('Ctrl Pts',(-1.40365743100421,34.1231033758838,11.2682682271638));
#49965=CARTESIAN_POINT('Ctrl Pts',(-1.28924662839032,34.1396755903245,11.1998585707924));
#49966=CARTESIAN_POINT('Ctrl Pts',(-1.17049154474186,34.1562860535771,11.1411548406653));
#49967=CARTESIAN_POINT('Ctrl Pts',(-1.1348996732179,34.1612643455026,11.1235608517895));
#49968=CARTESIAN_POINT('Ctrl Pts',(-1.09891749700162,34.1662460952939,11.1068383518619));
#49969=CARTESIAN_POINT('Ctrl Pts',(-1.06259342015375,34.1712327416556,11.0909960745263));
#49970=CARTESIAN_POINT('Ctrl Pts',(-0.93062390262081,34.189349797107,11.0334392725913));
#49971=CARTESIAN_POINT('Ctrl Pts',(-0.79383698357811,34.2072493013734,10.9875977444433));
#49972=CARTESIAN_POINT('Ctrl Pts',(-0.654538430841714,34.225032705138,10.9539518906291));
#49973=CARTESIAN_POINT('Ctrl Pts',(-0.51123900890397,34.2433268756767,10.9193396760192));
#49974=CARTESIAN_POINT('Ctrl Pts',(-0.365282556606137,34.2614981852811,
10.8976324138633));
#49975=CARTESIAN_POINT('Ctrl Pts',(-0.219137538585945,34.2796641606059,
10.8893180979243));
#49976=CARTESIAN_POINT('Ctrl Pts',(-0.143501639810857,34.2890657802398,
10.8850151065034));
#49977=CARTESIAN_POINT('Ctrl Pts',(-0.0678144599389599,34.2984660849497,
10.8842989483639));
#49978=CARTESIAN_POINT('Ctrl Pts',(0.0075869599259221,34.3078820684392,
10.8872355795483));
#49979=CARTESIAN_POINT('Ctrl Pts',(0.0908171073773173,34.3182756882892,
10.8904771132877));
#49980=CARTESIAN_POINT('Ctrl Pts',(0.173699009113757,34.328688403995,10.8981692516035));
#49981=CARTESIAN_POINT('Ctrl Pts',(0.255827425286371,34.3391437244705,10.9101052218915));
#49982=CARTESIAN_POINT('Ctrl Pts',(0.404667353738437,34.3580917235193,10.9317365773525));
#49983=CARTESIAN_POINT('Ctrl Pts',(0.550960479222043,34.3768611210909,10.9674728990995));
#49984=CARTESIAN_POINT('Ctrl Pts',(0.692327527943376,34.3955106167962,11.0161108799022));
#49985=CARTESIAN_POINT('Ctrl Pts',(0.835342138318517,34.4143774629681,11.0653157118404));
#49986=CARTESIAN_POINT('Ctrl Pts',(0.973316893376609,34.4331216111008,11.1277245401747));
#49987=CARTESIAN_POINT('Ctrl Pts',(1.10380084494927,34.4518066391112,11.2021423942935));
#49988=CARTESIAN_POINT('Ctrl Pts',(1.22566726657539,34.4692576549195,11.2716454824299));
#49989=CARTESIAN_POINT('Ctrl Pts',(1.34100105104289,34.4866571411023,11.3516243731409));
#49990=CARTESIAN_POINT('Ctrl Pts',(1.44779387776708,34.5040588762033,11.4411450268477));
#49991=CARTESIAN_POINT('Ctrl Pts',(1.44978479354124,34.5043832930202,11.4428139412031));
#49992=CARTESIAN_POINT('Ctrl Pts',(1.45177270423769,34.5047077106641,11.4444861388728));
#49993=CARTESIAN_POINT('Ctrl Pts',(1.45375759680208,34.5050321288439,11.4461616137071));
#49994=CARTESIAN_POINT('Ctrl Pts',(1.58859138980106,34.5270698625166,11.5599766538967));
#49995=CARTESIAN_POINT('Ctrl Pts',(1.70950255399661,34.5491105540052,11.6889128162493));
#49996=CARTESIAN_POINT('Ctrl Pts',(1.8145138197773,34.5710601364776,11.8290114666171));
#49997=CARTESIAN_POINT('Ctrl Pts',(1.92639920057061,34.5944465548293,11.978281078106));
#49998=CARTESIAN_POINT('Ctrl Pts',(2.02023435097168,34.6177295466144,12.1402246339982));
#49999=CARTESIAN_POINT('Ctrl Pts',(2.09357098283322,34.640788687189,12.3100512487185));
#50000=CARTESIAN_POINT('Ctrl Pts',(2.12046074090695,34.6492435984073,12.3723202194688));
#50001=CARTESIAN_POINT('Ctrl Pts',(2.14459417887735,34.6576683536396,12.4356488050096));
#50002=CARTESIAN_POINT('Ctrl Pts',(2.16584912590779,34.6660568151005,12.4997999582565));
#50003=CARTESIAN_POINT('Ctrl Pts',(2.1925649769702,34.6766004728527,12.5804330764277));
#50004=CARTESIAN_POINT('Ctrl Pts',(2.21476956359949,34.6871683815634,12.6623760906023));
#50005=CARTESIAN_POINT('Ctrl Pts',(2.23220764994495,34.6977437180901,12.7451481318184));
#50006=CARTESIAN_POINT('Ctrl Pts',(2.26060785934909,34.7149670398428,12.8799532507274));
#50007=CARTESIAN_POINT('Ctrl Pts',(2.27636242604132,34.7322101696369,13.0169582802029));
#50008=CARTESIAN_POINT('Ctrl Pts',(2.27987051823402,34.7493987123355,13.1539104307647));
#50009=CARTESIAN_POINT('Ctrl Pts',(2.28339206483647,34.7666531773884,13.2913878270299));
#50010=CARTESIAN_POINT('Ctrl Pts',(2.27457274402304,34.783852614774,13.4288102577253));
#50011=CARTESIAN_POINT('Ctrl Pts',(2.25386591578396,34.8009197707479,13.5638866209621));
#50012=CARTESIAN_POINT('Ctrl Pts',(2.24413352999502,34.8089414795457,13.6273736631499));
#50013=CARTESIAN_POINT('Ctrl Pts',(2.23177583441848,34.8169339396777,13.6903424211484));
#50014=CARTESIAN_POINT('Ctrl Pts',(2.21684385546882,34.8248889990484,13.7525557655596));
#50015=CARTESIAN_POINT('Ctrl Pts',(2.19007127872373,34.8391521746284,13.8641023692237));
#50016=CARTESIAN_POINT('Ctrl Pts',(2.1549944411202,34.8534168700116,13.9734539700032));
#50017=CARTESIAN_POINT('Ctrl Pts',(2.11185539310998,34.8676662265314,14.0791836053381));
#50018=CARTESIAN_POINT('Ctrl Pts',(2.0933089549537,34.873792342467,14.1246391319079));
#50019=CARTESIAN_POINT('Ctrl Pts',(2.07327301275871,34.8799156238577,14.1694252158986));
#50020=CARTESIAN_POINT('Ctrl Pts',(2.05176971917693,34.886034734027,14.2134289597084));
#50021=CARTESIAN_POINT('Ctrl Pts',(2.00178921632222,34.9002574949319,14.3157076750474));
#50022=CARTESIAN_POINT('Ctrl Pts',(1.94387841983718,34.9144577161843,14.4137577970048));
#50023=CARTESIAN_POINT('Ctrl Pts',(1.87908721990913,34.9286187143673,14.5066422832625));
#50024=CARTESIAN_POINT('Ctrl Pts',(1.81413095811237,34.9428157890673,14.5997634017618));
#50025=CARTESIAN_POINT('Ctrl Pts',(1.74226018673928,34.9569734394458,14.6876916058643));
#50026=CARTESIAN_POINT('Ctrl Pts',(1.66456928421305,34.9710749335319,14.7695187972507));
#50027=CARTESIAN_POINT('Ctrl Pts',(1.64740712450417,34.9741899970177,14.7875946759114));
#50028=CARTESIAN_POINT('Ctrl Pts',(1.62996106027555,34.9773023205237,14.8053730065465));
#50029=CARTESIAN_POINT('Ctrl Pts',(1.6122430516455,34.9804117242923,14.8228443067699));
#50030=CARTESIAN_POINT('Ctrl Pts',(1.52088799773868,34.9964439858645,14.912927318188));
#50031=CARTESIAN_POINT('Ctrl Pts',(1.42202916652567,35.0124052328162,14.995098404239));
#50032=CARTESIAN_POINT('Ctrl Pts',(1.31718349483541,35.0283135985736,15.0679803984461));
#50033=CARTESIAN_POINT('Ctrl Pts',(1.2258607493309,35.0421701137166,15.1314621206911));
#50034=CARTESIAN_POINT('Ctrl Pts',(1.12999721080024,35.0559865271651,15.1878964571));
#50035=CARTESIAN_POINT('Ctrl Pts',(1.03061700120121,35.0697753328408,15.2363970979685));
#50036=CARTESIAN_POINT('Ctrl Pts',(0.915725435099798,35.0857163082637,15.2924677644401));
#50037=CARTESIAN_POINT('Ctrl Pts',(0.796134489436802,35.1016203778816,15.3379334682777));
#50038=CARTESIAN_POINT('Ctrl Pts',(0.673885991351223,35.117507612992,15.3726835629812));
#50039=CARTESIAN_POINT('Ctrl Pts',(0.634695361371716,35.1226007696554,15.38382380703));
#50040=CARTESIAN_POINT('Ctrl Pts',(0.595231663506183,35.1276922011631,15.3938631791469));
#50041=CARTESIAN_POINT('Ctrl Pts',(0.555562200299993,35.1327825820645,15.4027991621468));
#50042=CARTESIAN_POINT('Ctrl Pts',(0.427915219441533,35.1491622277912,15.4315530488584));
#50043=CARTESIAN_POINT('Ctrl Pts',(0.29792052998284,35.1654493899942,15.4489072536342));
#50044=CARTESIAN_POINT('Ctrl Pts',(0.167804766505765,35.1816687993293,15.4547071197683));
#50045=CARTESIAN_POINT('Ctrl Pts',(0.0376874216217125,35.1978884057927,
15.460507056393));
#50046=CARTESIAN_POINT('Ctrl Pts',(-0.0925495030302005,35.2140402692686,
15.4547524213929));
#50047=CARTESIAN_POINT('Ctrl Pts',(-0.220677358214982,35.2301498780449,
15.437339170878));
#50048=CARTESIAN_POINT('Ctrl Pts',(-0.271299343155901,35.2365146171697,
15.4304593764409));
#50049=CARTESIAN_POINT('Ctrl Pts',(-0.321592212096991,35.2428727678739,
15.4217602732624));
#50050=CARTESIAN_POINT('Ctrl Pts',(-0.371419217300234,35.2492259284662,
15.4112376094421));
#50051=CARTESIAN_POINT('Ctrl Pts',(-0.457972173071773,35.2602618080162,
15.3929590142803));
#50052=CARTESIAN_POINT('Ctrl Pts',(-0.543119017933009,35.2712826251268,
15.3691775932306));
#50053=CARTESIAN_POINT('Ctrl Pts',(-0.626284090550383,35.2822968674306,
15.3403038136358));
#50054=CARTESIAN_POINT('Ctrl Pts',(-0.773088044699655,35.301739336141,15.2893354818309));
#50055=CARTESIAN_POINT('Ctrl Pts',(-0.913980015554586,35.321099528776,15.2223949186247));
#50056=CARTESIAN_POINT('Ctrl Pts',(-1.04581618355905,35.340384350165,15.1415968138546));
#50057=CARTESIAN_POINT('Ctrl Pts',(-1.18127774119407,35.3601994887845,15.0585768255479));
#50058=CARTESIAN_POINT('Ctrl Pts',(-1.30717699825575,35.3799350595191,14.9609275733912));
#50059=CARTESIAN_POINT('Ctrl Pts',(-1.42012179785065,35.3995989528989,14.8509929840464));
#50060=CARTESIAN_POINT('Ctrl Pts',(-1.46858614366081,35.4080366829419,14.80382031232));
#50061=CARTESIAN_POINT('Ctrl Pts',(-1.51466562117316,35.4164612198121,14.7543861378517));
#50062=CARTESIAN_POINT('Ctrl Pts',(-1.55809436667318,35.4248732044062,14.7028777079071));
#50063=CARTESIAN_POINT('Ctrl Pts',(-1.64900693489217,35.4424826267938,14.5950513454996));
#50064=CARTESIAN_POINT('Ctrl Pts',(-1.72830137475248,35.4600370350596,14.4781348494354));
#50065=CARTESIAN_POINT('Ctrl Pts',(-1.79511211395845,35.4775425369219,14.3549260254373));
#50066=CARTESIAN_POINT('Ctrl Pts',(-1.85648490514971,35.4936232078328,14.2417455769341));
#50067=CARTESIAN_POINT('Ctrl Pts',(-1.9073467947352,35.5096393678861,14.123213423905));
#50068=CARTESIAN_POINT('Ctrl Pts',(-1.94703030634917,35.5256205098076,14.0014818662496));
#50069=CARTESIAN_POINT('Ctrl Pts',(-1.9746954648963,35.5367616817212,13.9166173291721));
#50070=CARTESIAN_POINT('Ctrl Pts',(-1.99692889193797,35.547884525986,13.8302101887822));
#50071=CARTESIAN_POINT('Ctrl Pts',(-2.01352118408605,35.5589884385217,13.742879251034));
#50072=CARTESIAN_POINT('Ctrl Pts',(-2.02072924056195,35.5638122222368,13.7049407717833));
#50073=CARTESIAN_POINT('Ctrl Pts',(-2.02687204406997,35.5686324306605,13.6668278286596));
#50074=CARTESIAN_POINT('Ctrl Pts',(-2.03192934439831,35.5734490038586,13.6285909314804));
#50075=CARTESIAN_POINT('Ctrl Pts',(-2.04014579325388,35.5812743503423,13.5664685559697));
#50076=CARTESIAN_POINT('Ctrl Pts',(-2.04549409264654,35.589082667069,13.5040325687331));
#50077=CARTESIAN_POINT('Ctrl Pts',(-2.04788332093059,35.5968769086578,13.4415650199189));
#50078=CARTESIAN_POINT('Ctrl Pts',(-2.05154446858571,35.6088204594296,13.3458425134561));
#50079=CARTESIAN_POINT('Ctrl Pts',(-2.0482546344716,35.6207309551597,13.2500464480908));
#50080=CARTESIAN_POINT('Ctrl Pts',(-2.03835097321585,35.6326192116472,13.1551583079904));
#50081=CARTESIAN_POINT('Ctrl Pts',(-2.0284473119601,35.6445074681347,13.06027016789));
#50082=CARTESIAN_POINT('Ctrl Pts',(-2.0119302656843,35.6563734905405,12.966291131447));
#50083=CARTESIAN_POINT('Ctrl Pts',(-1.98918917550094,35.6682281905391,12.8741894258666));
#50084=CARTESIAN_POINT('Ctrl Pts',(-1.96162155315965,35.6825989128702,12.7625402034258));
#50085=CARTESIAN_POINT('Ctrl Pts',(-1.92481653315395,35.69693732528,12.6532517716315));
#50086=CARTESIAN_POINT('Ctrl Pts',(-1.87932281509479,35.7112429296544,12.54797575677));
#50087=CARTESIAN_POINT('Ctrl Pts',(-1.83301509,35.7258045004151,12.4408160660861));
#50088=CARTESIAN_POINT('Ctrl Pts',(-1.77770530153866,35.7403320813291,12.3378150814881));
#50089=CARTESIAN_POINT('Ctrl Pts',(-1.71402428391801,35.754825300147,12.2407074433751));
#50090=CARTESIAN_POINT('Ctrl Pts',(-1.69861786353295,35.7583316609148,12.2172140830101));
#50091=CARTESIAN_POINT('Ctrl Pts',(-1.68272169122856,35.7618360110277,12.1940655747937));
#50092=CARTESIAN_POINT('Ctrl Pts',(-1.66634511075174,35.7653383462395,12.1712862720119));
#50093=CARTESIAN_POINT('Ctrl Pts',(-1.59611327140501,35.7803582977047,12.0735960163649));
#50094=CARTESIAN_POINT('Ctrl Pts',(-1.51704280174011,35.7953411852278,11.9826996171978));
#50095=CARTESIAN_POINT('Ctrl Pts',(-1.43083543098776,35.8102867488178,11.8996820965413));
#50096=CARTESIAN_POINT('Ctrl Pts',(-1.34462806023541,35.8252323124077,11.8166645758849));
#50097=CARTESIAN_POINT('Ctrl Pts',(-1.25128529133472,35.8401405559852,11.7415269159067));
#50098=CARTESIAN_POINT('Ctrl Pts',(-1.15253542916576,35.855011268336,11.6753007627733));
#50099=CARTESIAN_POINT('Ctrl Pts',(-1.06327096491324,35.868453577438,11.6154359493029));
#50100=CARTESIAN_POINT('Ctrl Pts',(-0.969313042202289,35.8818470131201,
11.5626566717203));
#50101=CARTESIAN_POINT('Ctrl Pts',(-0.871894961021909,35.8952019643656,
11.5178284930221));
#50102=CARTESIAN_POINT('Ctrl Pts',(-0.785413590500806,35.907057612444,11.4780329819136));
#50103=CARTESIAN_POINT('Ctrl Pts',(-0.696206613574874,35.9188829352861,
11.4445035168071));
#50104=CARTESIAN_POINT('Ctrl Pts',(-0.605160422711497,35.9306851646132,
11.4178206318541));
#50105=CARTESIAN_POINT('Ctrl Pts',(-0.502376287738908,35.9440089722392,
11.3876977104835));
#50106=CARTESIAN_POINT('Ctrl Pts',(-0.397248796987259,35.9573033556558,
11.3663019080391));
#50107=CARTESIAN_POINT('Ctrl Pts',(-0.2912851877516,35.9705786660213,11.3535055397407));
#50108=CARTESIAN_POINT('Ctrl Pts',(-0.186014828194546,35.983767124828,11.3407928896007));
#50109=CARTESIAN_POINT('Ctrl Pts',(-0.0799206249175964,35.9969367649317,
11.3365673951363));
#50110=CARTESIAN_POINT('Ctrl Pts',(0.0255194181043174,36.0100975095415,
11.3406537309221));
#50111=CARTESIAN_POINT('Ctrl Pts',(0.0995112658213549,36.0193329743905,
11.3435212898353));
#50112=CARTESIAN_POINT('Ctrl Pts',(0.173180945864884,36.0285640540735,11.3504809179512));
#50113=CARTESIAN_POINT('Ctrl Pts',(0.246023155369535,36.0377940886885,11.361457586701));
#50114=CARTESIAN_POINT('Ctrl Pts',(0.349173102021139,36.0508644991635,11.3770013600661));
#50115=CARTESIAN_POINT('Ctrl Pts',(0.451060390357706,36.0638869807897,11.4006369620851));
#50116=CARTESIAN_POINT('Ctrl Pts',(0.550226705112536,36.0768748402712,11.4322888224452));
#50117=CARTESIAN_POINT('Ctrl Pts',(0.591720584632716,36.0823093134376,11.4455328205066));
#50118=CARTESIAN_POINT('Ctrl Pts',(0.632737888490082,36.0877377222362,11.4601797002687));
#50119=CARTESIAN_POINT('Ctrl Pts',(0.673171354865221,36.0931610280814,11.4762212759687));
#50120=CARTESIAN_POINT('Ctrl Pts',(0.769601574921968,36.1060951300264,11.514479006841));
#50121=CARTESIAN_POINT('Ctrl Pts',(0.862709909997599,36.1190002327184,11.5606731839098));
#50122=CARTESIAN_POINT('Ctrl Pts',(0.951463450775792,36.1318891699932,11.6138795055761));
#50123=CARTESIAN_POINT('Ctrl Pts',(1.04120770432058,36.1449219802289,11.667679743628));
#50124=CARTESIAN_POINT('Ctrl Pts',(1.12649832144998,36.1579382696876,11.7286487883445));
#50125=CARTESIAN_POINT('Ctrl Pts',(1.20629091800974,36.1709508742725,11.7957833557257));
#50126=CARTESIAN_POINT('Ctrl Pts',(1.28445287897005,36.1836975542329,11.8615459660551));
#50127=CARTESIAN_POINT('Ctrl Pts',(1.35733834381253,36.1964407026541,11.9332237535062));
#50128=CARTESIAN_POINT('Ctrl Pts',(1.4240025218212,36.2091918877558,12.0098410593243));
#50129=CARTESIAN_POINT('Ctrl Pts',(1.4388154544048,36.2120252302032,12.0268655996355));
#50130=CARTESIAN_POINT('Ctrl Pts',(1.4533213947603,36.2148589673348,12.0441339234977));
#50131=CARTESIAN_POINT('Ctrl Pts',(1.46751030002944,36.2176932223302,12.0616351716412));
#50132=CARTESIAN_POINT('Ctrl Pts',(1.52735459729779,36.229647209989,12.1354498794426));
#50133=CARTESIAN_POINT('Ctrl Pts',(1.58173333528113,36.2415626030895,12.2135799447662));
#50134=CARTESIAN_POINT('Ctrl Pts',(1.62985222800578,36.2534408955121,12.2952946960849));
#50135=CARTESIAN_POINT('Ctrl Pts',(1.69177523284277,36.2687267742489,12.4004513747749));
#50136=CARTESIAN_POINT('Ctrl Pts',(1.74332943193823,36.2839512176407,12.5115451983607));
#50137=CARTESIAN_POINT('Ctrl Pts',(1.78392093449125,36.2991174457196,12.6263368155275));
#50138=CARTESIAN_POINT('Ctrl Pts',(1.82514202908956,36.314518908662,12.7429089011296));
#50139=CARTESIAN_POINT('Ctrl Pts',(1.85505715911335,36.3298603418756,12.8632928281798));
#50140=CARTESIAN_POINT('Ctrl Pts',(1.87309126705035,36.3451449889762,12.9851207938013));
#50141=CARTESIAN_POINT('Ctrl Pts',(1.87843564658592,36.3496745701153,13.0212243198866));
#50142=CARTESIAN_POINT('Ctrl Pts',(1.88273694666996,36.3541991630102,13.0574546029022));
#50143=CARTESIAN_POINT('Ctrl Pts',(1.88598108934285,36.3587188488552,13.0937499627023));
#50144=CARTESIAN_POINT('Ctrl Pts',(1.89453315073255,36.3706334391511,13.1894301397075));
#50145=CARTESIAN_POINT('Ctrl Pts',(1.89573743070339,36.3825139356724,13.2855620769068));
#50146=CARTESIAN_POINT('Ctrl Pts',(1.88981146057019,36.394361687848,13.3810517445343));
#50147=CARTESIAN_POINT('Ctrl Pts',(1.88326688185853,36.4074462199883,13.4865095230737));
#50148=CARTESIAN_POINT('Ctrl Pts',(1.86796407409775,36.4206150563038,13.5914000038421));
#50149=CARTESIAN_POINT('Ctrl Pts',(1.8441512360903,36.4338077285074,13.6942046335211));
#50150=CARTESIAN_POINT('Ctrl Pts',(1.8265451487186,36.4435617670394,13.770213519643));
#50151=CARTESIAN_POINT('Ctrl Pts',(1.8042883809506,36.4533288725361,13.8450820123745));
#50152=CARTESIAN_POINT('Ctrl Pts',(1.77749860781857,36.4630853279683,13.9182020409971));
#50153=CARTESIAN_POINT('Ctrl Pts',(1.74141677072747,36.4762258213109,14.0166838365633));
#50154=CARTESIAN_POINT('Ctrl Pts',(1.69711118751256,36.4893469045138,14.111991885435));
#50155=CARTESIAN_POINT('Ctrl Pts',(1.64527973583635,36.502392924998,14.2028247163159));
#50156=CARTESIAN_POINT('Ctrl Pts',(1.62833313638777,36.506658398497,14.232523047193));
#50157=CARTESIAN_POINT('Ctrl Pts',(1.61058227251594,36.5109158659881,14.2617433029065));
#50158=CARTESIAN_POINT('Ctrl Pts',(1.5920521732993,36.5151634364617,14.290441034415));
#50159=CARTESIAN_POINT('Ctrl Pts',(1.57688560628607,36.5186399997266,14.3139296333135));
#50160=CARTESIAN_POINT('Ctrl Pts',(1.56119702690944,36.5221099333285,14.3370681966813));
#50161=CARTESIAN_POINT('Ctrl Pts',(1.54500959542846,36.5255722087906,14.3598383941216));
#50162=CARTESIAN_POINT('Ctrl Pts',(1.48382006123124,36.5386598331634,14.4459112078718));
#50163=CARTESIAN_POINT('Ctrl Pts',(1.41543631336881,36.5518084567257,14.5266569385406));
#50164=CARTESIAN_POINT('Ctrl Pts',(1.34101407134697,36.5649854886612,14.6011690475079));
#50165=CARTESIAN_POINT('Ctrl Pts',(1.26616099598456,36.5782388029625,14.676112510059));
#50166=CARTESIAN_POINT('Ctrl Pts',(1.1851985792311,36.5915208413091,14.74475116306));
#50167=CARTESIAN_POINT('Ctrl Pts',(1.09925484292431,36.6048002565126,14.8061412973413));
#50168=CARTESIAN_POINT('Ctrl Pts',(1.01654823758621,36.61757949325,14.8652191292561));
#50169=CARTESIAN_POINT('Ctrl Pts',(0.929227554730378,36.6303563005821,14.9175851595059));
#50170=CARTESIAN_POINT('Ctrl Pts',(0.838266607600032,36.6431044985123,14.9623631944754));
#50171=CARTESIAN_POINT('Ctrl Pts',(0.807317111196533,36.6474420776431,14.9775989376813));
#50172=CARTESIAN_POINT('Ctrl Pts',(0.775945965359559,36.6517763601189,14.9919558429113));
#50173=CARTESIAN_POINT('Ctrl Pts',(0.744190943597326,36.6561063637833,15.0053981067694));
#50174=CARTESIAN_POINT('Ctrl Pts',(0.708189246510862,36.6610154292369,15.0206380368567));
#50175=CARTESIAN_POINT('Ctrl Pts',(0.671721621828844,36.6658870487025,15.0347110946733));
#50176=CARTESIAN_POINT('Ctrl Pts',(0.634846570587766,36.6707297013909,15.0475611518812));
#50177=CARTESIAN_POINT('Ctrl Pts',(0.540748903266454,36.6830871709072,15.0803518970467));
#50178=CARTESIAN_POINT('Ctrl Pts',(0.443994601445002,36.6952565152842,15.1051789905932));
#50179=CARTESIAN_POINT('Ctrl Pts',(0.345878901046004,36.7073738930339,15.1221280130944));
#50180=CARTESIAN_POINT('Ctrl Pts',(0.244089875378566,36.719944929777,15.1397115851363));
#50181=CARTESIAN_POINT('Ctrl Pts',(0.140835280574491,36.732460125289,15.1488145233718));
#50182=CARTESIAN_POINT('Ctrl Pts',(0.0376199817696723,36.7450631920612,
15.14954271623));
#50183=CARTESIAN_POINT('Ctrl Pts',(-0.0583978346931932,36.7567874128522,
15.1502201302279));
#50184=CARTESIAN_POINT('Ctrl Pts',(-0.154380541120703,36.7685876183003,
15.1436489919699));
#50185=CARTESIAN_POINT('Ctrl Pts',(-0.249074603876776,36.7805724777801,
15.1299423721303));
#50186=CARTESIAN_POINT('Ctrl Pts',(-0.256172857822581,36.7814708612016,
15.1289149257886));
#50187=CARTESIAN_POINT('Ctrl Pts',(-0.26326385474469,36.7823702789282,15.1278474033987));
#50188=CARTESIAN_POINT('Ctrl Pts',(-0.270347059162533,36.7832707751351,
15.1267398619482));
#50189=CARTESIAN_POINT('Ctrl Pts',(-0.359741935093517,36.7946356520945,
15.1127619326497));
#50190=CARTESIAN_POINT('Ctrl Pts',(-0.448245687484448,36.8061249358034,
15.0924190560047));
#50191=CARTESIAN_POINT('Ctrl Pts',(-0.534788423534536,36.8176479233723,
15.0658468746533));
#50192=CARTESIAN_POINT('Ctrl Pts',(-0.620971637574773,36.8291230413241,
15.0393850813539));
#50193=CARTESIAN_POINT('Ctrl Pts',(-0.705209039686781,36.8406315682017,
15.0067466198686));
#50194=CARTESIAN_POINT('Ctrl Pts',(-0.786477085132356,36.8520882771613,
14.9681038614056));
#50195=CARTESIAN_POINT('Ctrl Pts',(-0.841873113264734,36.8598976955907,
14.9417631844127));
#50196=CARTESIAN_POINT('Ctrl Pts',(-0.895890180580959,36.86768312773,14.9126334644819));
#50197=CARTESIAN_POINT('Ctrl Pts',(-0.948216350538084,36.8754187988796,
14.880775906438));
#50198=CARTESIAN_POINT('Ctrl Pts',(-1.02405932632251,36.8866310913166,14.8346006942018));
#50199=CARTESIAN_POINT('Ctrl Pts',(-1.0963476335419,36.8977386382427,14.7826952561138));
#50200=CARTESIAN_POINT('Ctrl Pts',(-1.16459156201923,36.9086668288595,14.7259270744155));
#50201=CARTESIAN_POINT('Ctrl Pts',(-1.17419518179789,36.9102046973541,14.7179383779158));
#50202=CARTESIAN_POINT('Ctrl Pts',(-1.1837187927073,36.911739021452,14.7098533772982));
#50203=CARTESIAN_POINT('Ctrl Pts',(-1.193161112349,36.913269600617,14.7016744800817));
#50204=CARTESIAN_POINT('Ctrl Pts',(-1.26635192657766,36.9251336699959,14.6382769072937));
#50205=CARTESIAN_POINT('Ctrl Pts',(-1.3344343809947,36.9370717143419,14.5690871425987));
#50206=CARTESIAN_POINT('Ctrl Pts',(-1.3968207555326,36.9490735856253,14.4951213528827));
#50207=CARTESIAN_POINT('Ctrl Pts',(-1.46021206049806,36.961268785111,14.4199641095324));
#50208=CARTESIAN_POINT('Ctrl Pts',(-1.51772331354799,36.9735298768924,14.3398747979504));
#50209=CARTESIAN_POINT('Ctrl Pts',(-1.56871064427456,36.9858473584534,14.2558725847206));
#50210=CARTESIAN_POINT('Ctrl Pts',(-1.6184835382327,36.9978714572801,14.1738711700211));
#50211=CARTESIAN_POINT('Ctrl Pts',(-1.6620403903747,37.0099492915742,14.0881398681812));
#50212=CARTESIAN_POINT('Ctrl Pts',(-1.69874329383057,37.0220731469179,13.9995984580638));
#50213=CARTESIAN_POINT('Ctrl Pts',(-1.71835034527889,37.0285498294986,13.9522987673032));
#50214=CARTESIAN_POINT('Ctrl Pts',(-1.736000678138,37.0350396648645,13.9041967447192));
#50215=CARTESIAN_POINT('Ctrl Pts',(-1.75159108002485,37.0415416140855,13.8554309174612));
#50216=CARTESIAN_POINT('Ctrl Pts',(-1.77850249502875,37.0527649715775,13.7712536509049));
#50217=CARTESIAN_POINT('Ctrl Pts',(-1.79941306612529,37.0638700466476,13.6851522039074));
#50218=CARTESIAN_POINT('Ctrl Pts',(-1.81371393571048,37.0748991615949,13.5979485978916));
#50219=CARTESIAN_POINT('Ctrl Pts',(-1.81575584668309,37.0764739239333,13.5854974669367));
#50220=CARTESIAN_POINT('Ctrl Pts',(-1.81766306122867,37.0780471322918,13.5730239342238));
#50221=CARTESIAN_POINT('Ctrl Pts',(-1.81943386595458,37.0796189044161,13.5605304574353));
#50222=CARTESIAN_POINT('Ctrl Pts',(-1.83173154207434,37.0905343623632,13.4737672311418));
#50223=CARTESIAN_POINT('Ctrl Pts',(-1.837446673463,37.1013808239721,13.3860398430746));
#50224=CARTESIAN_POINT('Ctrl Pts',(-1.83681903068068,37.1121958285686,13.2983067064745));
#50225=CARTESIAN_POINT('Ctrl Pts',(-1.83618756062209,37.1230767815225,13.2100385857045));
#50226=CARTESIAN_POINT('Ctrl Pts',(-1.82913541383387,37.1339259064831,13.1217657421755));
#50227=CARTESIAN_POINT('Ctrl Pts',(-1.81595528194813,37.1447779413162,13.0344833715383));
#50228=CARTESIAN_POINT('Ctrl Pts',(-1.8062316911794,37.1527839875864,12.970091143846));
#50229=CARTESIAN_POINT('Ctrl Pts',(-1.79317382057122,37.1607915453244,12.9062385215738));
#50230=CARTESIAN_POINT('Ctrl Pts',(-1.77691737143006,37.1688132973504,12.8433259136689));
#50231=CARTESIAN_POINT('Ctrl Pts',(-1.75273331561296,37.1807469304006,12.7497333949117));
#50232=CARTESIAN_POINT('Ctrl Pts',(-1.72125565569971,37.1928665653301,12.6578643564013));
#50233=CARTESIAN_POINT('Ctrl Pts',(-1.68292786097389,37.2050732623165,12.5689297780961));
#50234=CARTESIAN_POINT('Ctrl Pts',(-1.64473503304942,37.2172369748615,12.4803083724023));
#50235=CARTESIAN_POINT('Ctrl Pts',(-1.59974186674591,37.2294871164617,12.3946005856137));
#50236=CARTESIAN_POINT('Ctrl Pts',(-1.54838160112248,37.2417338157826,12.3129542055393));
#50237=CARTESIAN_POINT('Ctrl Pts',(-1.49815382222756,37.2537104770832,12.2331081168134));
#50238=CARTESIAN_POINT('Ctrl Pts',(-1.44183803035782,37.2656838525028,12.1571454414428));
#50239=CARTESIAN_POINT('Ctrl Pts',(-1.37981186334457,37.2775776440079,12.086099646022));
#50240=CARTESIAN_POINT('Ctrl Pts',(-1.3695906542137,37.2795376060076,12.0743921043855));
#50241=CARTESIAN_POINT('Ctrl Pts',(-1.35921428973727,37.2814954242028,12.0628180105673));
#50242=CARTESIAN_POINT('Ctrl Pts',(-1.34868434603657,37.2834507778102,12.0513819113163));
#50243=CARTESIAN_POINT('Ctrl Pts',(-1.32238196798846,37.2883349871907,12.0228160790149));
#50244=CARTESIAN_POINT('Ctrl Pts',(-1.2951214512437,37.2932038028834,11.9951112983189));
#50245=CARTESIAN_POINT('Ctrl Pts',(-1.26697452896051,37.2980523861965,11.9682910254143));
#50246=CARTESIAN_POINT('Ctrl Pts',(-1.20317523033163,37.3090424408677,11.9074987802398));
#50247=CARTESIAN_POINT('Ctrl Pts',(-1.13496692031192,37.3199204173598,11.8514198724786));
#50248=CARTESIAN_POINT('Ctrl Pts',(-1.06311008949083,37.3307657155399,11.8003937600291));
#50249=CARTESIAN_POINT('Ctrl Pts',(-0.990911241118183,37.3416626341754,
11.7491247781704));
#50250=CARTESIAN_POINT('Ctrl Pts',(-0.915027598556622,37.3525265792606,
11.7029574649945));
#50251=CARTESIAN_POINT('Ctrl Pts',(-0.836246103777801,37.3634314369721,
11.6622863877922));
#50252=CARTESIAN_POINT('Ctrl Pts',(-0.758385854858158,37.3742087767299,
11.6220909052909));
#50253=CARTESIAN_POINT('Ctrl Pts',(-0.677694116748348,37.3850260769621,
11.5872648057675));
#50254=CARTESIAN_POINT('Ctrl Pts',(-0.594963973008873,37.3959480907742,
11.5582258127621));
#50255=CARTESIAN_POINT('Ctrl Pts',(-0.521009688641192,37.4057115177287,
11.5322672219825));
#50256=CARTESIAN_POINT('Ctrl Pts',(-0.445426620962867,37.4155585399473,
11.5109340972001));
#50257=CARTESIAN_POINT('Ctrl Pts',(-0.368812822755948,37.4255308710731,
11.4945403116791));
#50258=CARTESIAN_POINT('Ctrl Pts',(-0.269224375159485,37.4384936662743,
11.4732304211831));
#50259=CARTESIAN_POINT('Ctrl Pts',(-0.167801264918345,37.4514022987213,
11.4598028010033));
#50260=CARTESIAN_POINT('Ctrl Pts',(-0.0658556672410014,37.4642758852663,
11.4548878867486));
#50261=CARTESIAN_POINT('Ctrl Pts',(-0.00409324698879404,37.4720751809737,
11.4519102495909));
#50262=CARTESIAN_POINT('Ctrl Pts',(0.0578599822949168,37.4798615625061,
11.4520566539944));
#50263=CARTESIAN_POINT('Ctrl Pts',(0.119705201033959,37.4876387920326,11.4554612490146));
#50264=CARTESIAN_POINT('Ctrl Pts',(0.22093662297219,37.5003689596958,11.4610340645377));
#50265=CARTESIAN_POINT('Ctrl Pts',(0.321879291848365,37.5130747556518,11.4753394587183));
#50266=CARTESIAN_POINT('Ctrl Pts',(0.421078028215027,37.5257702555449,11.4976990787541));
#50267=CARTESIAN_POINT('Ctrl Pts',(0.455550372083947,37.5301820419641,11.5054692232024));
#50268=CARTESIAN_POINT('Ctrl Pts',(0.489811969198873,37.5345925600645,11.5142115624586));
#50269=CARTESIAN_POINT('Ctrl Pts',(0.523801452546336,37.5390023199556,11.5238962113574));
#50270=CARTESIAN_POINT('Ctrl Pts',(0.565740826890602,37.5444434903597,11.5358460286407));
#50271=CARTESIAN_POINT('Ctrl Pts',(0.607265893251684,37.5498835092932,11.5492305637103));
#50272=CARTESIAN_POINT('Ctrl Pts',(0.648266270211475,37.5553232976998,11.5640317540731));
#50273=CARTESIAN_POINT('Ctrl Pts',(0.736204072212425,37.566990581547,11.595777417016));
#50274=CARTESIAN_POINT('Ctrl Pts',(0.821827069603859,37.5786698796599,11.6340755837756));
#50275=CARTESIAN_POINT('Ctrl Pts',(0.904090269375511,37.59036064197,11.6787707765648));
#50276=CARTESIAN_POINT('Ctrl Pts',(1.02468526577214,37.6074988938562,11.7442923783056));
#50277=CARTESIAN_POINT('Ctrl Pts',(1.13805853563312,37.6246617858551,11.8235628872294));
#50278=CARTESIAN_POINT('Ctrl Pts',(1.24183702425236,37.6418456265658,11.914126941895));
#50279=CARTESIAN_POINT('Ctrl Pts',(1.32864768216617,37.6562199014029,11.9898837318951));
#50280=CARTESIAN_POINT('Ctrl Pts',(1.40874436015618,37.6706088341558,12.0735421237424));
#50281=CARTESIAN_POINT('Ctrl Pts',(1.48013748955479,37.6850107467071,12.1641253724113));
#50282=CARTESIAN_POINT('Ctrl Pts',(1.49411662122227,37.6878307131873,12.1818620253733));
#50283=CARTESIAN_POINT('Ctrl Pts',(1.5077749468182,37.6906422060092,12.1998510629921));
#50284=CARTESIAN_POINT('Ctrl Pts',(1.52109707091888,37.6934467053931,12.2180881367112));
#50285=CARTESIAN_POINT('Ctrl Pts',(1.5689807848348,37.7035269182152,12.2836376552436));
#50286=CARTESIAN_POINT('Ctrl Pts',(1.61252495621774,37.7135173702108,12.3523942733967));
#50287=CARTESIAN_POINT('Ctrl Pts',(1.65151456542215,37.7234819098149,12.4237792308908));
#50288=CARTESIAN_POINT('Ctrl Pts',(1.68902135207338,37.7330674857833,12.4924493310911));
#50289=CARTESIAN_POINT('Ctrl Pts',(1.7223122370472,37.742629045399,12.5635522396304));
#50290=CARTESIAN_POINT('Ctrl Pts',(1.75116010543387,37.7522166977056,12.6365343098017));
#50291=CARTESIAN_POINT('Ctrl Pts',(1.77986975086396,37.7617584113096,12.7091666904438));
#50292=CARTESIAN_POINT('Ctrl Pts',(1.80417787447923,37.7713259690187,12.7836607272367));
#50293=CARTESIAN_POINT('Ctrl Pts',(1.82384013888311,37.78096218026,12.8594239654089));
#50294=CARTESIAN_POINT('Ctrl Pts',(1.84333888420058,37.7905182529971,12.9345571268395));
#50295=CARTESIAN_POINT('Ctrl Pts',(1.85826770420485,37.8001418387852,13.0109386128204));
#50296=CARTESIAN_POINT('Ctrl Pts',(1.86838300661926,37.8098682229002,13.0879401454036));
#50297=CARTESIAN_POINT('Ctrl Pts',(1.8697816564832,37.8112130967617,13.0985872005937));
#50298=CARTESIAN_POINT('Ctrl Pts',(1.87108828362893,37.8125599258635,13.1092460295507));
#50299=CARTESIAN_POINT('Ctrl Pts',(1.87230225335561,37.8139087937046,13.1199148935139));
#50300=CARTESIAN_POINT('Ctrl Pts',(1.88155220003328,37.8241866081605,13.2012072195101));
#50301=CARTESIAN_POINT('Ctrl Pts',(1.88565818101676,37.8345296782578,13.2833068905848));
#50302=CARTESIAN_POINT('Ctrl Pts',(1.88447514247342,37.8448953804118,13.3654266858299));
#50303=CARTESIAN_POINT('Ctrl Pts',(1.88330137449124,37.8551798545482,13.446902971539));
#50304=CARTESIAN_POINT('Ctrl Pts',(1.87692181961835,37.8654866069461,13.5283980941142));
#50305=CARTESIAN_POINT('Ctrl Pts',(1.86523687322021,37.8757788587898,13.6091711708453));
#50306=CARTESIAN_POINT('Ctrl Pts',(1.85565474609755,37.8842189202315,13.6754083501145));
#50307=CARTESIAN_POINT('Ctrl Pts',(1.84250587208248,37.8926493189246,13.7411603284638));
#50308=CARTESIAN_POINT('Ctrl Pts',(1.82575174022672,37.9010522336897,13.8060388875534));
#50309=CARTESIAN_POINT('Ctrl Pts',(1.80541874857518,37.9112500999378,13.8847761931739));
#50310=CARTESIAN_POINT('Ctrl Pts',(1.77977617891474,37.9214073576267,13.962225480692));
#50311=CARTESIAN_POINT('Ctrl Pts',(1.74934969868926,37.931496497684,14.0378577509446));
#50312=CARTESIAN_POINT('Ctrl Pts',(1.73443711073289,37.936441374232,14.0749265434609));
#50313=CARTESIAN_POINT('Ctrl Pts',(1.71837553799444,37.9413699612472,14.1115596261691));
#50314=CARTESIAN_POINT('Ctrl Pts',(1.7012272587251,37.9462794415417,14.1476992722481));
#50315=CARTESIAN_POINT('Ctrl Pts',(1.65536953948287,37.9594083138579,14.2443434729503));
#50316=CARTESIAN_POINT('Ctrl Pts',(1.60109742222298,37.9726277492245,14.3371931665222));
#50317=CARTESIAN_POINT('Ctrl Pts',(1.53941338370294,37.9859333601115,14.4250707321891));
#50318=CARTESIAN_POINT('Ctrl Pts',(1.47592002794693,37.9996292513967,14.5155259240626));
#50319=CARTESIAN_POINT('Ctrl Pts',(1.40457296024107,38.013416443659,14.6007146775164));
#50320=CARTESIAN_POINT('Ctrl Pts',(1.32641016648189,38.0272918876079,14.6793479109264));
#50321=CARTESIAN_POINT('Ctrl Pts',(1.25019104527154,38.040822291184,14.7560257733748));
#50322=CARTESIAN_POINT('Ctrl Pts',(1.16748988153653,38.0544366217045,14.8264716092764));
#50323=CARTESIAN_POINT('Ctrl Pts',(1.07923056703853,38.0681336113904,14.8894621550906));
#50324=CARTESIAN_POINT('Ctrl Pts',(1.05532560088906,38.0718434303104,14.906523095049));
#50325=CARTESIAN_POINT('Ctrl Pts',(1.03101271994426,38.0755593216332,14.923036887145));
#50326=CARTESIAN_POINT('Ctrl Pts',(1.00630993556873,38.0792812792025,14.9389786380786));
#50327=CARTESIAN_POINT('Ctrl Pts',(0.931813705546694,38.09050559315,14.9870542042356));
#50328=CARTESIAN_POINT('Ctrl Pts',(0.854050897258177,38.1016783441784,15.0302224781016));
#50329=CARTESIAN_POINT('Ctrl Pts',(0.773446603681667,38.1128295662079,15.0677543178446));
#50330=CARTESIAN_POINT('Ctrl Pts',(0.692845204371131,38.1239803878293,15.1052848099284));
#50331=CARTESIAN_POINT('Ctrl Pts',(0.609401976885697,38.135109688761,15.1371780828391));
#50332=CARTESIAN_POINT('Ctrl Pts',(0.523968011596957,38.1462410762626,15.1632326981605));
#50333=CARTESIAN_POINT('Ctrl Pts',(0.437199628779924,38.157546328088,15.1896942679673));
#50334=CARTESIAN_POINT('Ctrl Pts',(0.348377553615163,38.1688537548445,15.2101321372207));
#50335=CARTESIAN_POINT('Ctrl Pts',(0.25844726538386,38.1801811519831,15.2243277362019));
#50336=CARTESIAN_POINT('Ctrl Pts',(0.168516977152557,38.1915085491216,15.2385233351831));
#50337=CARTESIAN_POINT('Ctrl Pts',(0.0774787389347745,38.2028559191199,
15.2464753286676));
#50338=CARTESIAN_POINT('Ctrl Pts',(-0.0136685470148311,38.214234012426,
15.247977050252));
#50339=CARTESIAN_POINT('Ctrl Pts',(-0.0294357107357523,38.2162022581957,
15.2482368263917));
#50340=CARTESIAN_POINT('Ctrl Pts',(-0.0452102629264591,38.2181716841655,
15.2483052034339));
#50341=CARTESIAN_POINT('Ctrl Pts',(-0.0609870846454569,38.2201422176861,
15.2481816691172));
#50342=CARTESIAN_POINT('Ctrl Pts',(-0.167861317030268,38.2334908668084,
15.2473448316664));
#50343=CARTESIAN_POINT('Ctrl Pts',(-0.274836074129024,38.2468898222752,
15.2376990938252));
#50344=CARTESIAN_POINT('Ctrl Pts',(-0.380578198734069,38.2603198260231,
15.2193486574701));
#50345=CARTESIAN_POINT('Ctrl Pts',(-0.417366157078181,38.2649921590246,
15.2129644932522));
#50346=CARTESIAN_POINT('Ctrl Pts',(-0.454005326035501,38.2696683063962,
15.2055269746925));
#50347=CARTESIAN_POINT('Ctrl Pts',(-0.490440916802775,38.2743476382891,
15.1970410556936));
#50348=CARTESIAN_POINT('Ctrl Pts',(-0.595332394070263,38.2878185886577,
15.172611629382));
#50349=CARTESIAN_POINT('Ctrl Pts',(-0.698532919360637,38.3013154565255,
15.1394935750653));
#50350=CARTESIAN_POINT('Ctrl Pts',(-0.798523269889506,38.3148278959151,
15.0980935250948));
#50351=CARTESIAN_POINT('Ctrl Pts',(-0.832977639475209,38.319483971009,15.0838280223238));
#50352=CARTESIAN_POINT('Ctrl Pts',(-0.86705130550624,38.324141951439,15.0685791480927));
#50353=CARTESIAN_POINT('Ctrl Pts',(-0.900683525930329,38.3288015922403,
15.0523633011244));
#50354=CARTESIAN_POINT('Ctrl Pts',(-0.953802916976569,38.3361611206551,
15.0267516731856));
#50355=CARTESIAN_POINT('Ctrl Pts',(-1.00582088986153,38.3435247625456,14.9987280011649));
#50356=CARTESIAN_POINT('Ctrl Pts',(-1.05656606986707,38.3508919848372,14.9684465575659));
#50357=CARTESIAN_POINT('Ctrl Pts',(-1.1512670174672,38.3646407375684,14.9119351528727));
#50358=CARTESIAN_POINT('Ctrl Pts',(-1.24147956422147,38.3784414699224,14.8472740887571));
#50359=CARTESIAN_POINT('Ctrl Pts',(-1.32593793858643,38.3922798854461,14.7754679152784));
#50360=CARTESIAN_POINT('Ctrl Pts',(-1.41011964597831,38.4060729693782,14.7038969629582));
#50361=CARTESIAN_POINT('Ctrl Pts',(-1.4885842459314,38.4199034898599,14.6252288770287));
#50362=CARTESIAN_POINT('Ctrl Pts',(-1.56012293710475,38.4337598646462,14.5404830745007));
#50363=CARTESIAN_POINT('Ctrl Pts',(-1.63166162827809,38.4476162394325,14.4557372719726));
#50364=CARTESIAN_POINT('Ctrl Pts',(-1.69627398786503,38.4614984682388,14.3649148501332));
#50365=CARTESIAN_POINT('Ctrl Pts',(-1.75280334582966,38.475397552503,14.2690424737355));
#50366=CARTESIAN_POINT('Ctrl Pts',(-1.77188593180274,38.4800894591506,14.2366788854882));
#50367=CARTESIAN_POINT('Ctrl Pts',(-1.79004790890814,38.4847833082817,14.2037398383331));
#50368=CARTESIAN_POINT('Ctrl Pts',(-1.80727197431892,38.489478839319,14.1702942128208));
#50369=CARTESIAN_POINT('Ctrl Pts',(-1.83527483310092,38.4971128263836,14.1159183668308));
#50370=CARTESIAN_POINT('Ctrl Pts',(-1.86084066759219,38.5047597895004,14.0601450907728));
#50371=CARTESIAN_POINT('Ctrl Pts',(-1.88387488847079,38.5124193040841,14.0032558925948));
#50372=CARTESIAN_POINT('Ctrl Pts',(-1.92103627323572,38.5247764908133,13.9114758669711));
#50373=CARTESIAN_POINT('Ctrl Pts',(-1.95160763534726,38.5371663818236,13.8167906890215));
#50374=CARTESIAN_POINT('Ctrl Pts',(-1.97513569698453,38.5495856892822,13.7201224936645));
#50375=CARTESIAN_POINT('Ctrl Pts',(-2.00432522563287,38.5649934069449,13.6001934021287));
#50376=CARTESIAN_POINT('Ctrl Pts',(-2.02267215165502,38.5804464493681,13.4772121624051));
#50377=CARTESIAN_POINT('Ctrl Pts',(-2.02968898387652,38.5959385938295,13.3532907829735));
#50378=CARTESIAN_POINT('Ctrl Pts',(-2.03397888163678,38.6054100638217,13.2775286682056));
#50379=CARTESIAN_POINT('Ctrl Pts',(-2.03403471424584,38.6148961174031,13.201415701224));
#50380=CARTESIAN_POINT('Ctrl Pts',(-2.02975445317098,38.6243950291442,13.1254368311003));
#50381=CARTESIAN_POINT('Ctrl Pts',(-2.02280967740017,38.6398071292369,13.0021601881341));
#50382=CARTESIAN_POINT('Ctrl Pts',(-2.00444757115455,38.6552531620673,12.879237787665));
#50383=CARTESIAN_POINT('Ctrl Pts',(-1.97526544816996,38.6707239507206,12.7587251172616));
#50384=CARTESIAN_POINT('Ctrl Pts',(-1.97096571892869,38.6730034354035,12.7409686348717));
#50385=CARTESIAN_POINT('Ctrl Pts',(-1.96643117940809,38.6752834546776,12.723264432834));
#50386=CARTESIAN_POINT('Ctrl Pts',(-1.96166382899896,38.6775639762411,12.7056190442356));
#50387=CARTESIAN_POINT('Ctrl Pts',(-1.93445889617108,38.6905777953698,12.6049254575796));
#50388=CARTESIAN_POINT('Ctrl Pts',(-1.89963150194229,38.7036474933163,12.5058494960527));
#50389=CARTESIAN_POINT('Ctrl Pts',(-1.85744175271546,38.7167644025515,12.4096604907267));
#50390=CARTESIAN_POINT('Ctrl Pts',(-1.81471393547527,38.7300485986139,12.3122447365351));
#50391=CARTESIAN_POINT('Ctrl Pts',(-1.76443465003305,38.7433812228378,12.2177913129304));
#50392=CARTESIAN_POINT('Ctrl Pts',(-1.70692567539847,38.7567514050638,12.1276292830182));
#50393=CARTESIAN_POINT('Ctrl Pts',(-1.67917225935526,38.7632037584964,12.0841177381966));
#50394=CARTESIAN_POINT('Ctrl Pts',(-1.64973585385529,38.7696648309556,12.0416056773222));
#50395=CARTESIAN_POINT('Ctrl Pts',(-1.61865694793425,38.7761332434927,12.000241932981));
#50396=CARTESIAN_POINT('Ctrl Pts',(-1.55453211870822,38.7894794613539,11.9148964884287));
#50397=CARTESIAN_POINT('Ctrl Pts',(-1.48341208340305,38.8028570449867,11.8344414834723));
#50398=CARTESIAN_POINT('Ctrl Pts',(-1.40637875111882,38.8162525285523,11.7597475756211));
#50399=CARTESIAN_POINT('Ctrl Pts',(-1.3303324971104,38.8294763670595,11.6860107694763));
#50400=CARTESIAN_POINT('Ctrl Pts',(-1.24852441498115,38.8427176444261,11.6178893151297));
#50401=CARTESIAN_POINT('Ctrl Pts',(-1.16203176929779,38.8559616492614,11.5561868610373));
#50402=CARTESIAN_POINT('Ctrl Pts',(-1.13104879439214,38.8607058522653,11.5340841080037));
#50403=CARTESIAN_POINT('Ctrl Pts',(-1.09946498277994,38.8654503891011,11.5128046402907));
#50404=CARTESIAN_POINT('Ctrl Pts',(-1.06733066340167,38.8701945297612,11.4923839582497));
#50405=CARTESIAN_POINT('Ctrl Pts',(-0.972607256998674,38.8841789916224,
11.4321892318196));
#50406=CARTESIAN_POINT('Ctrl Pts',(-0.872839454613605,38.8982274412983,
11.3791452675653));
#50407=CARTESIAN_POINT('Ctrl Pts',(-0.769176366339235,38.9123291835519,
11.3342590985451));
#50408=CARTESIAN_POINT('Ctrl Pts',(-0.676647765071094,38.9249162529503,
11.2941941679623));
#50409=CARTESIAN_POINT('Ctrl Pts',(-0.581016842324058,38.9375457468101,
11.2606292273347));
#50410=CARTESIAN_POINT('Ctrl Pts',(-0.483133214779234,38.9502083200589,
11.2342672004245));
#50411=CARTESIAN_POINT('Ctrl Pts',(-0.374104051159969,38.964312719387,11.2049034567891));
#50412=CARTESIAN_POINT('Ctrl Pts',(-0.26228009898579,38.9784582001722,11.1844779374543));
#50413=CARTESIAN_POINT('Ctrl Pts',(-0.149211834206222,38.9926293412044,
11.1730342926814));
#50414=CARTESIAN_POINT('Ctrl Pts',(-0.0367979066216767,39.0067184724464,
11.161656873409));
#50415=CARTESIAN_POINT('Ctrl Pts',(0.0768447085266355,39.0208329632453,
11.1591580928637));
#50416=CARTESIAN_POINT('Ctrl Pts',(0.190172257764394,39.0349552099529,11.1655346303781));
#50417=CARTESIAN_POINT('Ctrl Pts',(0.27616395271878,39.0456710150605,11.1703730767442));
#50418=CARTESIAN_POINT('Ctrl Pts',(0.361973669224714,39.056391235503,11.1803206866011));
#50419=CARTESIAN_POINT('Ctrl Pts',(0.446926283662682,39.0671072570587,11.1953559052037));
#50420=CARTESIAN_POINT('Ctrl Pts',(0.557762231489612,39.0810882323814,11.2149720490461));
#50421=CARTESIAN_POINT('Ctrl Pts',(0.667456695819849,39.0951569273598,11.2430588959332));
#50422=CARTESIAN_POINT('Ctrl Pts',(0.774587654394998,39.1092997002696,11.279716904837));
#50423=CARTESIAN_POINT('Ctrl Pts',(0.821213735347596,39.1154549898643,11.2956713900152));
#50424=CARTESIAN_POINT('Ctrl Pts',(0.867353625063725,39.1216242526135,11.3132491260835));
#50425=CARTESIAN_POINT('Ctrl Pts',(0.912887566933807,39.1278060923235,11.3324566821536));
#50426=CARTESIAN_POINT('Ctrl Pts',(1.01816490605173,39.1420988947647,11.3768657605458));
#50427=CARTESIAN_POINT('Ctrl Pts',(1.12020465598396,39.1564592462259,11.429990595082));
#50428=CARTESIAN_POINT('Ctrl Pts',(1.21778291735022,39.1708665109701,11.4909839652763));
#50429=CARTESIAN_POINT('Ctrl Pts',(1.31590359196629,39.1853538621105,11.5523163824232));
#50430=CARTESIAN_POINT('Ctrl Pts',(1.4095117775228,39.1998886500518,11.621605329692));
#50431=CARTESIAN_POINT('Ctrl Pts',(1.49734755732802,39.2144451458915,11.6979392701371));
#50432=CARTESIAN_POINT('Ctrl Pts',(1.58390229667661,39.2287893425961,11.7731599186396));
#50433=CARTESIAN_POINT('Ctrl Pts',(1.66485035258449,39.2431546018885,11.8552214353057));
#50434=CARTESIAN_POINT('Ctrl Pts',(1.73899121814928,39.2575118529509,11.9432022807421));
#50435=CARTESIAN_POINT('Ctrl Pts',(1.75952788815997,39.2614887437665,11.9675725598888));
#50436=CARTESIAN_POINT('Ctrl Pts',(1.77954236860206,39.2654649943525,11.992396721077));
#50437=CARTESIAN_POINT('Ctrl Pts',(1.79900945011226,39.2694399279205,12.0176545279864));
#50438=CARTESIAN_POINT('Ctrl Pts',(1.8648746565806,39.2828887759161,12.1031121589189));
#50439=CARTESIAN_POINT('Ctrl Pts',(1.92466113418795,39.2963712277619,12.1936984375978));
#50440=CARTESIAN_POINT('Ctrl Pts',(1.97742211730071,39.3099037258777,12.2885951626925));
#50441=CARTESIAN_POINT('Ctrl Pts',(2.02834600704809,39.3229650337117,12.3801876630783));
#50442=CARTESIAN_POINT('Ctrl Pts',(2.07272547499223,39.3360729971241,12.4757945953722));
#50443=CARTESIAN_POINT('Ctrl Pts',(2.11032929023137,39.34924701252,12.5742859751103));
#50444=CARTESIAN_POINT('Ctrl Pts',(2.13229742930302,39.3569432688841,12.6318246135086));
#50445=CARTESIAN_POINT('Ctrl Pts',(2.15195409073792,39.3646621538228,12.6903478973526));
#50446=CARTESIAN_POINT('Ctrl Pts',(2.16926057692105,39.3724082463288,12.7496340491348));
#50447=CARTESIAN_POINT('Ctrl Pts',(2.20499938889948,39.3884043382394,12.8720630973567));
#50448=CARTESIAN_POINT('Ctrl Pts',(2.23050054750311,39.4044245201669,12.997856234636));
#50449=CARTESIAN_POINT('Ctrl Pts',(2.24524477699743,39.4204386971286,13.125211320992));
#50450=CARTESIAN_POINT('Ctrl Pts',(2.25984430316941,39.436295707206,13.2513165146955));
#50451=CARTESIAN_POINT('Ctrl Pts',(2.26389576834546,39.4521468097985,13.3789539579255));
#50452=CARTESIAN_POINT('Ctrl Pts',(2.25686901755235,39.4679566252646,13.5063310262745));
#50453=CARTESIAN_POINT('Ctrl Pts',(2.25557898741884,39.4708591244363,13.5297159820424));
#50454=CARTESIAN_POINT('Ctrl Pts',(2.25391552734149,39.4737602156173,13.553092027494));
#50455=CARTESIAN_POINT('Ctrl Pts',(2.25187531184562,39.4766596578138,13.5764478840497));
#50456=CARTESIAN_POINT('Ctrl Pts',(2.24737834603513,39.4830504986117,13.6279279794702));
#50457=CARTESIAN_POINT('Ctrl Pts',(2.24110742310709,39.4894581531109,13.67930762029));
#50458=CARTESIAN_POINT('Ctrl Pts',(2.23303044536404,39.4958822443291,13.7304716656013));
#50459=CARTESIAN_POINT('Ctrl Pts',(2.20765171897598,39.5160674247897,13.8912345583772));
#50460=CARTESIAN_POINT('Ctrl Pts',(2.16444241364464,39.5364153426137,14.0498730313516));
#50461=CARTESIAN_POINT('Ctrl Pts',(2.10488708145267,39.5569100664321,14.2029025809024));
#50462=CARTESIAN_POINT('Ctrl Pts',(2.04252350325459,39.578371189466,14.3631480186957));
#50463=CARTESIAN_POINT('Ctrl Pts',(1.96223410268545,39.5999933319345,14.5172425693329));
#50464=CARTESIAN_POINT('Ctrl Pts',(1.86573413249446,39.6217510677722,14.6611277667625));
#50465=CARTESIAN_POINT('Ctrl Pts',(1.76992981325946,39.6433519559994,14.8039757216422));
#50466=CARTESIAN_POINT('Ctrl Pts',(1.65814643351817,39.6650864667814,14.9367591694373));
#50467=CARTESIAN_POINT('Ctrl Pts',(1.53209748668832,39.6869228001303,15.0554700291448));
#50468=CARTESIAN_POINT('Ctrl Pts',(1.52660601812724,39.6878741253186,15.0606418054296));
#50469=CARTESIAN_POINT('Ctrl Pts',(1.52108748071761,39.6888256427,15.0657868687584));
#50470=CARTESIAN_POINT('Ctrl Pts',(1.51554219727787,39.689777349341,15.070905040698));
#50471=CARTESIAN_POINT('Ctrl Pts',(1.40993244337401,39.7079025732794,15.168380469115));
#50472=CARTESIAN_POINT('Ctrl Pts',(1.29452495950882,39.7260673948832,15.2560975042179));
#50473=CARTESIAN_POINT('Ctrl Pts',(1.17156908372708,39.7442254101507,15.3327459533929));
#50474=CARTESIAN_POINT('Ctrl Pts',(1.04861320794535,39.7623834254181,15.4093944025679));
#50475=CARTESIAN_POINT('Ctrl Pts',(0.918109393126689,39.7805346191256,15.474972521862));
#50476=CARTESIAN_POINT('Ctrl Pts',(0.78236694783971,39.7986269225969,15.5281863917256));
#50477=CARTESIAN_POINT('Ctrl Pts',(0.674184584539994,39.8130459065993,15.570596134603));
#50478=CARTESIAN_POINT('Ctrl Pts',(0.562639589759075,39.8274689786143,15.6052257702722));
#50479=CARTESIAN_POINT('Ctrl Pts',(0.448917494117073,39.8419532158612,15.631536517183));
#50480=CARTESIAN_POINT('Ctrl Pts',(0.344470930111066,39.8552560731831,15.655701276861));
#50481=CARTESIAN_POINT('Ctrl Pts',(0.23818767329683,39.8686106077482,15.6728499352464));
#50482=CARTESIAN_POINT('Ctrl Pts',(0.130950146145734,39.8820659530989,15.6825787805095));
#50483=CARTESIAN_POINT('Ctrl Pts',(0.0619357240280919,39.8907253553478,
15.6888399341516));
#50484=CARTESIAN_POINT('Ctrl Pts',(-0.00747466447897276,39.8994266059004,
15.6920281986405));
#50485=CARTESIAN_POINT('Ctrl Pts',(-0.0770187597906271,39.9081837908669,
15.6922092589488));
#50486=CARTESIAN_POINT('Ctrl Pts',(-0.15083418087625,39.917478832997,15.6924014397923));
#50487=CARTESIAN_POINT('Ctrl Pts',(-0.224814304867329,39.9267837732083,
15.689126374746));
#50488=CARTESIAN_POINT('Ctrl Pts',(-0.298585723235663,39.9360898120054,
15.6824440425789));
#50489=CARTESIAN_POINT('Ctrl Pts',(-0.372357141603997,39.9453958508025,
15.6757617104117));
#50490=CARTESIAN_POINT('Ctrl Pts',(-0.445920003627971,39.9547015994929,
15.6656731457466));
#50491=CARTESIAN_POINT('Ctrl Pts',(-0.518996000608588,39.963993101745,15.6522066196876));
#50492=CARTESIAN_POINT('Ctrl Pts',(-0.649050855860098,39.9805293794613,
15.6282399662074));
#50493=CARTESIAN_POINT('Ctrl Pts',(-0.777562113765256,39.9970209905262,
15.5935741587819));
#50494=CARTESIAN_POINT('Ctrl Pts',(-0.902740062950962,40.0134430802308,
15.5484535570547));
#50495=CARTESIAN_POINT('Ctrl Pts',(-0.918233577649619,40.0154756737497,
15.5428688936964));
#50496=CARTESIAN_POINT('Ctrl Pts',(-0.933675976443711,40.0175071990136,
15.5371240271856));
#50497=CARTESIAN_POINT('Ctrl Pts',(-0.949063819652945,40.0195376061761,
15.5312193878286));
#50498=CARTESIAN_POINT('Ctrl Pts',(-1.03061029609617,40.030297564384,15.4999282882454));
#50499=CARTESIAN_POINT('Ctrl Pts',(-1.11064181727098,40.0410300409155,15.4641445833943));
#50500=CARTESIAN_POINT('Ctrl Pts',(-1.1886437811041,40.0518269270513,15.4240795684269));
#50501=CARTESIAN_POINT('Ctrl Pts',(-1.24428110356763,40.0595281413031,15.3955019525862));
#50502=CARTESIAN_POINT('Ctrl Pts',(-1.29888698283431,40.0672622641483,15.3647461915998));
#50503=CARTESIAN_POINT('Ctrl Pts',(-1.35229042157928,40.0750646633413,15.3318856940637));
#50504=CARTESIAN_POINT('Ctrl Pts',(-1.36651191821623,40.0771424657542,15.3231348445645));
#50505=CARTESIAN_POINT('Ctrl Pts',(-1.38064702607825,40.0792256896704,15.3142366233478));
#50506=CARTESIAN_POINT('Ctrl Pts',(-1.39469212530709,40.0813134338249,15.3051904271304));
#50507=CARTESIAN_POINT('Ctrl Pts',(-1.46302294019609,40.091470518302,15.2611797762189));
#50508=CARTESIAN_POINT('Ctrl Pts',(-1.52922710773669,40.1017351285523,15.2136648644734));
#50509=CARTESIAN_POINT('Ctrl Pts',(-1.59298260229315,40.1119994019961,15.1628259031572));
#50510=CARTESIAN_POINT('Ctrl Pts',(-1.63432250007387,40.118654891345,15.1298612547186));
#50511=CARTESIAN_POINT('Ctrl Pts',(-1.67463186284525,40.1253101017758,15.0954994458754));
#50512=CARTESIAN_POINT('Ctrl Pts',(-1.71381313588905,40.131934140182,15.0597958761118));
#50513=CARTESIAN_POINT('Ctrl Pts',(-1.79641772214658,40.1458993819772,14.9845232170294));
#50514=CARTESIAN_POINT('Ctrl Pts',(-1.87416648810312,40.1598005498757,14.9032238652839));
#50515=CARTESIAN_POINT('Ctrl Pts',(-1.94629403927576,40.1736911961933,14.8167859073364));
#50516=CARTESIAN_POINT('Ctrl Pts',(-2.01881835699388,40.1876582535863,14.729872462707));
#50517=CARTESIAN_POINT('Ctrl Pts',(-2.08565956552004,40.201614679656,14.6377649500271));
#50518=CARTESIAN_POINT('Ctrl Pts',(-2.14609222190778,40.2156200980235,14.5413667041427));
#50519=CARTESIAN_POINT('Ctrl Pts',(-2.20645007732472,40.2296081810802,14.4450877759055));
#50520=CARTESIAN_POINT('Ctrl Pts',(-2.26041556080545,40.2436451498221,14.3445297159776));
#50521=CARTESIAN_POINT('Ctrl Pts',(-2.30731486398802,40.2577953963599,14.24057637183));
#50522=CARTESIAN_POINT('Ctrl Pts',(-2.33681844803083,40.2666970848632,14.1751810244055));
#50523=CARTESIAN_POINT('Ctrl Pts',(-2.36352658682643,40.2756437014626,14.1084416141264));
#50524=CARTESIAN_POINT('Ctrl Pts',(-2.38728043808747,40.2846522490296,14.040572526374));
#50525=CARTESIAN_POINT('Ctrl Pts',(-0.846350554922702,36.2086580169322,
10.9476201968673));
#50526=CARTESIAN_POINT('Ctrl Pts',(-0.320239388270522,36.2776098215264,
10.7790676939286));
#50527=CARTESIAN_POINT('Ctrl Pts',(0.832775930125362,36.4139226702905,10.808549500351));
#50528=CARTESIAN_POINT('Ctrl Pts',(2.13906229672172,36.6136666354338,11.8831979032289));
#50529=CARTESIAN_POINT('Ctrl Pts',(2.49776983260815,36.808758111583,13.495739293786));
#50530=CARTESIAN_POINT('Ctrl Pts',(1.80437349953285,36.9993052263523,14.952542053131));
#50531=CARTESIAN_POINT('Ctrl Pts',(0.394900147917386,37.185448210336,15.6574645158721));
#50532=CARTESIAN_POINT('Ctrl Pts',(-1.11565382654404,37.3673476166458,15.3516804870708));
#50533=CARTESIAN_POINT('Ctrl Pts',(-2.09311765211965,37.5452064656626,14.2088709500021));
#50534=CARTESIAN_POINT('Ctrl Pts',(-2.1720579761826,37.7385796988706,12.5707062008505));
#50535=CARTESIAN_POINT('Ctrl Pts',(-0.949636867934553,37.9462055979747,
11.2027877013928));
#50536=CARTESIAN_POINT('Ctrl Pts',(0.673815046857492,38.1301938802853,11.2772200756772));
#50537=CARTESIAN_POINT('Ctrl Pts',(1.57727284316267,38.2749046007684,12.0503331491926));
#50538=CARTESIAN_POINT('Ctrl Pts',(1.94325033553157,38.3822910046209,12.8523955445105));
#50539=CARTESIAN_POINT('Ctrl Pts',(1.92810669679268,38.4886294217223,13.7248605615257));
#50540=CARTESIAN_POINT('Ctrl Pts',(1.42241170095239,38.6291577761382,14.7650632826532));
#50541=CARTESIAN_POINT('Ctrl Pts',(0.0401515959749049,38.8027238580628,
15.4262990840038));
#50542=CARTESIAN_POINT('Ctrl Pts',(-1.46965088290585,38.9913613874058,14.7220128335763));
#50543=CARTESIAN_POINT('Ctrl Pts',(-1.97854444794942,39.1617067135922,13.370700241503));
#50544=CARTESIAN_POINT('Ctrl Pts',(-1.59936214624478,39.3145198762853,12.1352956525774));
#50545=CARTESIAN_POINT('Ctrl Pts',(-0.537697718828742,39.467221677783,11.3957752654928));
#50546=CARTESIAN_POINT('Ctrl Pts',(0.431453487286904,39.581964807185,11.4476593843084));
#50547=CARTESIAN_POINT('Ctrl Pts',(0.981899433556111,39.6586655307137,11.7263662420974));
#50548=CARTESIAN_POINT('Ctrl Pts',(1.31369659088836,39.7098688329335,11.9697816194113));
#50549=CARTESIAN_POINT('Ctrl Pts',(1.77927598222622,39.7996585507031,12.5319575286557));
#50550=CARTESIAN_POINT('Ctrl Pts',(1.99002909214103,39.9285999970237,13.6022652497978));
#50551=CARTESIAN_POINT('Ctrl Pts',(1.39274427027988,40.0847604456334,14.7825804722783));
#50552=CARTESIAN_POINT('Ctrl Pts',(0.182808632813018,40.2427406148847,15.3521158945863));
#50553=CARTESIAN_POINT('Ctrl Pts',(-1.13947383359755,40.4028817003577,15.0538629730217));
#50554=CARTESIAN_POINT('Ctrl Pts',(-2.01284312485354,40.5655300227019,13.9883677995854));
#50555=CARTESIAN_POINT('Ctrl Pts',(-2.04026673680089,40.703437009905,12.8220937324209));
#50556=CARTESIAN_POINT('Ctrl Pts',(-1.67504874026637,40.8013405748775,12.11478228846));
#50557=CARTESIAN_POINT('Ctrl Pts',(-1.37512744085228,40.8577000030924,11.7753778421044));
#50558=CARTESIAN_POINT('Ctrl Pts',(-0.84520156220626,40.942653269374,11.3441539863298));
#50559=CARTESIAN_POINT('Ctrl Pts',(0.20619225565922,41.07169276057,11.0515151341635));
#50560=CARTESIAN_POINT('Ctrl Pts',(1.58303660030943,41.2474326928145,11.6176574340441));
#50561=CARTESIAN_POINT('Ctrl Pts',(2.33325522018996,41.4270957461375,12.9390680613749));
#50562=CARTESIAN_POINT('Ctrl Pts',(2.08870142664571,41.6313181674013,14.6528956012928));
#50563=CARTESIAN_POINT('Ctrl Pts',(0.478042449382701,41.8621181773002,15.897365670719));
#50564=CARTESIAN_POINT('Ctrl Pts',(-1.761592798532,42.1219415711064,15.3873242298046));
#50565=CARTESIAN_POINT('Ctrl Pts',(-2.59367583188875,42.3340558257298,13.7054240007776));
#50566=CARTESIAN_POINT('Ctrl Pts',(-2.43193369746059,42.4594565353203,12.6998858182967));
#50567=CARTESIAN_POINT('Ctrl Pts',(-2.34562647967194,42.4937495273014,12.438593281029));
#50568=CARTESIAN_POINT('Ctrl Pts',(-1.50589870835376,49.9431019076281,10.6371826091256));
#50569=CARTESIAN_POINT('Ctrl Pts',(-0.997967678553802,50.0151271970462,
10.363255806184));
#50570=CARTESIAN_POINT('Ctrl Pts',(0.158195592874908,50.1568524066829,10.118721243365));
#50571=CARTESIAN_POINT('Ctrl Pts',(1.79381557388335,50.3661150852637,10.7207619811602));
#50572=CARTESIAN_POINT('Ctrl Pts',(2.84419434848047,50.5712195350034,12.067783810989));
#50573=CARTESIAN_POINT('Ctrl Pts',(3.02341717505406,50.7735159459258,13.7431013283951));
#50574=CARTESIAN_POINT('Ctrl Pts',(2.30286206288198,50.9728836506257,15.2388199884596));
#50575=CARTESIAN_POINT('Ctrl Pts',(0.92205760400918,51.1692158544984,16.1161415454293));
#50576=CARTESIAN_POINT('Ctrl Pts',(-0.685453262226371,51.3624197803939,
16.1320659429518));
#50577=CARTESIAN_POINT('Ctrl Pts',(-2.19238056120144,51.5735293389412,15.2219934660806));
#50578=CARTESIAN_POINT('Ctrl Pts',(-2.90735272931905,51.8010880510178,13.4061487489255));
#50579=CARTESIAN_POINT('Ctrl Pts',(-2.16425376166143,52.0434177919142,11.4615023835655));
#50580=CARTESIAN_POINT('Ctrl Pts',(-0.502081140238918,52.2600779708778,
10.630409517392));
#50581=CARTESIAN_POINT('Ctrl Pts',(1.07593746233167,52.4526832569537,10.9256670839091));
#50582=CARTESIAN_POINT('Ctrl Pts',(2.12276587212965,52.6226828382186,11.8771254661021));
#50583=CARTESIAN_POINT('Ctrl Pts',(2.50200021911292,52.7893692149562,13.2132811311121));
#50584=CARTESIAN_POINT('Ctrl Pts',(2.12706423374028,52.9527900207895,14.5212359218611));
#50585=CARTESIAN_POINT('Ctrl Pts',(1.13781104018586,53.1130091141584,15.4174536119083));
#50586=CARTESIAN_POINT('Ctrl Pts',(0.0654657851665619,53.2439207055765,
15.6121783318573));
#50587=CARTESIAN_POINT('Ctrl Pts',(-0.746623315045519,53.3471366675035,
15.4169819595003));
#50588=CARTESIAN_POINT('Ctrl Pts',(-1.24224768410671,53.4174127398507,15.1386872585679));
#50589=CARTESIAN_POINT('Ctrl Pts',(-1.53955280475257,53.4680994158948,14.8585927685747));
#50590=CARTESIAN_POINT('Ctrl Pts',(-1.72953687809877,53.5059325452741,14.6222034008512));
#50591=CARTESIAN_POINT('Ctrl Pts',(-1.83900671316259,53.5310650918408,14.4524985484517));
#50592=CARTESIAN_POINT('Ctrl Pts',(-1.92953388679311,53.5561097283772,14.2734012151605));
#50593=CARTESIAN_POINT('Ctrl Pts',(-2.16406279700829,53.6310687712466,13.719290031839));
#50594=CARTESIAN_POINT('Ctrl Pts',(-2.17177819037875,53.7358927560662,12.832395135736));
#50595=CARTESIAN_POINT('Ctrl Pts',(-1.45710175821801,53.9054769110698,11.6357747936092));
#50596=CARTESIAN_POINT('Ctrl Pts',(-0.413266964323039,54.0361204336834,
11.1919935846092));
#50597=CARTESIAN_POINT('Ctrl Pts',(0.711216260265478,54.1763643967519,11.3652778255788));
#50598=CARTESIAN_POINT('Ctrl Pts',(1.52066824573736,54.2918677043501,11.880340058231));
#50599=CARTESIAN_POINT('Ctrl Pts',(2.01443006791509,54.428455762762,12.9067219771098));
#50600=CARTESIAN_POINT('Ctrl Pts',(1.89256617764797,54.5632269584251,14.0220272624448));
#50601=CARTESIAN_POINT('Ctrl Pts',(1.38063078199914,54.6630909695851,14.6774342504526));
#50602=CARTESIAN_POINT('Ctrl Pts',(0.930736007320949,54.7292209179053,14.9598721955184));
#50603=CARTESIAN_POINT('Ctrl Pts',(0.608667091714335,54.773198599464,15.1048739140154));
#50604=CARTESIAN_POINT('Ctrl Pts',(0.175602575225595,54.8279616001322,15.1990651595965));
#50605=CARTESIAN_POINT('Ctrl Pts',(-0.352406871985372,54.893380841766,15.1649979748017));
#50606=CARTESIAN_POINT('Ctrl Pts',(-1.01514487004226,54.9802401150033,14.930429326385));
#50607=CARTESIAN_POINT('Ctrl Pts',(-1.66780664136042,55.088200471646,14.3122806208394));
#50608=CARTESIAN_POINT('Ctrl Pts',(-1.94015073865359,55.2169934028641,13.2743783173256));
#50609=CARTESIAN_POINT('Ctrl Pts',(-1.62596701268505,55.3452548126108,12.253428093674));
#50610=CARTESIAN_POINT('Ctrl Pts',(-0.822759016554036,55.4732131481038,
11.552987892603));
#50611=CARTESIAN_POINT('Ctrl Pts',(0.22864918135393,55.6011019347585,11.3811964479907));
#50612=CARTESIAN_POINT('Ctrl Pts',(0.994467824367534,55.7006917801432,11.6991450082289));
#50613=CARTESIAN_POINT('Ctrl Pts',(1.36698632717851,55.7648487863085,12.0567353290565));
#50614=CARTESIAN_POINT('Ctrl Pts',(1.50893253971056,55.7933864622217,12.2363773760104));
#50615=CARTESIAN_POINT('Ctrl Pts',(1.69571438886681,55.8362209424235,12.5244913797639));
#50616=CARTESIAN_POINT('Ctrl Pts',(1.95466728844487,55.929201785116,13.2382690435808));
#50617=CARTESIAN_POINT('Ctrl Pts',(1.74920409027378,56.0442438038412,14.2008603846282));
#50618=CARTESIAN_POINT('Ctrl Pts',(1.17286032909157,56.1456895858431,14.7965620237573));
#50619=CARTESIAN_POINT('Ctrl Pts',(0.768526008089416,56.2039055636691,15.0317400892323));
#50620=CARTESIAN_POINT('Ctrl Pts',(0.104606995860322,56.2915081081481,15.2699416184091));
#50621=CARTESIAN_POINT('Ctrl Pts',(-1.02326211770975,56.4239720744945,15.1364144040356));
#50622=CARTESIAN_POINT('Ctrl Pts',(-2.02993586215422,56.6033780628028,13.9721301674421));
#50623=CARTESIAN_POINT('Ctrl Pts',(-1.99001292699949,56.7860310929108,12.4035952810077));
#50624=CARTESIAN_POINT('Ctrl Pts',(-1.0032412314103,56.9516808788094,11.3821713282861));
#50625=CARTESIAN_POINT('Ctrl Pts',(0.197329230236401,57.0992917294341,11.1593006877948));
#50626=CARTESIAN_POINT('Ctrl Pts',(1.20762964212908,57.2277551469465,11.4805246362353));
#50627=CARTESIAN_POINT('Ctrl Pts',(1.99047227458886,57.3637094919575,12.2871144386262));
#50628=CARTESIAN_POINT('Ctrl Pts',(2.28235856496914,57.5075737399963,13.4485263777013));
#50629=CARTESIAN_POINT('Ctrl Pts',(1.89658779363131,57.6598213116464,14.6569347041676));
#50630=CARTESIAN_POINT('Ctrl Pts',(0.914041736627156,57.8150355469431,15.4962660713587));
#50631=CARTESIAN_POINT('Ctrl Pts',(-0.38890798366212,57.9733172811768,15.6958293398159));
#50632=CARTESIAN_POINT('Ctrl Pts',(-1.62534529857286,58.1347548824581,15.1683265160832));
#50633=CARTESIAN_POINT('Ctrl Pts',(-2.41372763907556,58.2994204314994,14.0465052931711));
#50634=CARTESIAN_POINT('Ctrl Pts',(-2.49386038142991,58.4673719419849,12.6500189571622));
#50635=CARTESIAN_POINT('Ctrl Pts',(-2.04000962209625,58.5815575858371,11.8147420052546));
#50636=CARTESIAN_POINT('Ctrl Pts',(-1.71585603698212,58.6392095497043,11.4856667176634));
#50637=CARTESIAN_POINT('Ctrl Pts',(-1.44314689269042,50.0096600245596,10.8164178498533));
#50638=CARTESIAN_POINT('Ctrl Pts',(-0.967833206190739,50.0773357805971,
10.5555388260198));
#50639=CARTESIAN_POINT('Ctrl Pts',(0.115434306511918,50.2103396991322,10.3183871031536));
#50640=CARTESIAN_POINT('Ctrl Pts',(1.65093114637839,50.4062957717865,10.8710554596649));
#50641=CARTESIAN_POINT('Ctrl Pts',(2.64169322568085,50.5979836964062,12.1226297867223));
#50642=CARTESIAN_POINT('Ctrl Pts',(2.82051984598436,50.7867229952345,13.6842352127829));
#50643=CARTESIAN_POINT('Ctrl Pts',(2.15988775952974,50.9724571312247,15.082582164639));
#50644=CARTESIAN_POINT('Ctrl Pts',(0.881537136075658,51.1551438493973,15.9087514070269));
#50645=CARTESIAN_POINT('Ctrl Pts',(-0.612562908279529,51.33475498818,15.9353575960212));
#50646=CARTESIAN_POINT('Ctrl Pts',(-2.0192227121573,51.530891439638,15.1012354462255));
#50647=CARTESIAN_POINT('Ctrl Pts',(-2.69711124774285,51.7422379283989,13.4205467389996));
#50648=CARTESIAN_POINT('Ctrl Pts',(-2.02247298214849,51.9673511700767,11.6084678588967));
#50649=CARTESIAN_POINT('Ctrl Pts',(-0.484267511851704,52.1687924756556,
10.8220839616332));
#50650=CARTESIAN_POINT('Ctrl Pts',(0.987164463079186,52.3481129585181,11.0834955949316));
#50651=CARTESIAN_POINT('Ctrl Pts',(1.97144859362409,52.5066367477731,11.9614279805005));
#50652=CARTESIAN_POINT('Ctrl Pts',(2.33773697406492,52.6623825463245,13.2062234102142));
#50653=CARTESIAN_POINT('Ctrl Pts',(1.99873683538971,52.8154495056158,14.4345354278471));
#50654=CARTESIAN_POINT('Ctrl Pts',(1.07824398048702,52.9659507012417,15.2856626082588));
#50655=CARTESIAN_POINT('Ctrl Pts',(0.0697049573621546,53.0893317916579,
15.4797027775451));
#50656=CARTESIAN_POINT('Ctrl Pts',(-0.699607585085375,53.1868862908566,
15.3031285416865));
#50657=CARTESIAN_POINT('Ctrl Pts',(-1.17161314368012,53.2534397586931,15.044498237106));
#50658=CARTESIAN_POINT('Ctrl Pts',(-1.45641635268664,53.3015314616841,14.7817377808518));
#50659=CARTESIAN_POINT('Ctrl Pts',(-1.6391690146498,53.337466301464,14.5591301402832));
#50660=CARTESIAN_POINT('Ctrl Pts',(-1.74490480360317,53.3613577519319,14.3989309299869));
#50661=CARTESIAN_POINT('Ctrl Pts',(-1.83280603061363,53.3851861785151,14.2294653625524));
#50662=CARTESIAN_POINT('Ctrl Pts',(-2.06159148754384,53.4565465193291,13.7044345680607));
#50663=CARTESIAN_POINT('Ctrl Pts',(-2.07877019877502,53.5566611884873,12.8575983361216));
#50664=CARTESIAN_POINT('Ctrl Pts',(-1.40603614418218,53.7194678026363,11.7012894016199));
#50665=CARTESIAN_POINT('Ctrl Pts',(-0.403405186271102,53.8456725193569,
11.2598606725744));
#50666=CARTESIAN_POINT('Ctrl Pts',(0.691219352687192,53.9819685221532,11.4153747691577));
#50667=CARTESIAN_POINT('Ctrl Pts',(1.48757896395445,54.0947462754909,11.9083621144659));
#50668=CARTESIAN_POINT('Ctrl Pts',(1.98557800160514,54.2289819014901,12.9105081365746));
#50669=CARTESIAN_POINT('Ctrl Pts',(1.87938366711896,54.3623306653876,14.0153323317459));
#50670=CARTESIAN_POINT('Ctrl Pts',(1.37812277860126,54.4618301452917,14.6748860962729));
#50671=CARTESIAN_POINT('Ctrl Pts',(0.93151130558792,54.5280104671103,14.9630837165789));
#50672=CARTESIAN_POINT('Ctrl Pts',(0.610531160974068,54.5720998812823,15.1124430650131));
#50673=CARTESIAN_POINT('Ctrl Pts',(0.176535664765444,54.6271491611219,15.2126589477959));
#50674=CARTESIAN_POINT('Ctrl Pts',(-0.356437580665123,54.6931459505594,
15.185131838619));
#50675=CARTESIAN_POINT('Ctrl Pts',(-1.03027121446636,54.7810865292972,14.9564103073955));
#50676=CARTESIAN_POINT('Ctrl Pts',(-1.70305637580998,54.890979739731,14.3365617953708));
#50677=CARTESIAN_POINT('Ctrl Pts',(-1.99697946426401,55.0230112459747,13.276794154045));
#50678=CARTESIAN_POINT('Ctrl Pts',(-1.68750568280781,55.1554149288954,12.218662248392));
#50679=CARTESIAN_POINT('Ctrl Pts',(-0.863245869663355,55.2883998181656,
11.4792032203492));
#50680=CARTESIAN_POINT('Ctrl Pts',(0.23369382995798,55.4221752650644,11.2840552404368));
#50681=CARTESIAN_POINT('Ctrl Pts',(1.04417672785527,55.5269917049279,11.6072605812333));
#50682=CARTESIAN_POINT('Ctrl Pts',(1.44269341168101,55.5947748560472,11.9797147371851));
#50683=CARTESIAN_POINT('Ctrl Pts',(1.59535621613771,55.6249683503327,12.1677271002977));
#50684=CARTESIAN_POINT('Ctrl Pts',(1.79714499201008,55.6703301088737,12.4701299601362));
#50685=CARTESIAN_POINT('Ctrl Pts',(2.08224613391108,55.7690189750693,13.2236988047189));
#50686=CARTESIAN_POINT('Ctrl Pts',(1.87781477739677,55.8917577693071,14.2535363827309));
#50687=CARTESIAN_POINT('Ctrl Pts',(1.26887003484619,56.0004790852983,14.9001774851111));
#50688=CARTESIAN_POINT('Ctrl Pts',(0.838066930964846,56.063002212917,15.1583893894994));
#50689=CARTESIAN_POINT('Ctrl Pts',(0.127712822964686,56.1572085860953,15.4238835554972));
#50690=CARTESIAN_POINT('Ctrl Pts',(-1.0907223837963,56.3001117619415,15.2967205489644));
#50691=CARTESIAN_POINT('Ctrl Pts',(-2.19800052179846,56.4944516616297,14.0505820561347));
#50692=CARTESIAN_POINT('Ctrl Pts',(-2.17705412607774,56.6929311041823,12.345920491215));
#50693=CARTESIAN_POINT('Ctrl Pts',(-1.11681994234011,56.8733219428292,11.2201611370152));
#50694=CARTESIAN_POINT('Ctrl Pts',(0.188678422475607,57.0342316102921,10.9612004285832));
#50695=CARTESIAN_POINT('Ctrl Pts',(1.29443431864757,57.1743272227455,11.2981696268465));
#50696=CARTESIAN_POINT('Ctrl Pts',(2.15840176208839,57.3225935604102,12.1675464585855));
#50697=CARTESIAN_POINT('Ctrl Pts',(2.49115674000038,57.4794296539054,13.4297720046328));
#50698=CARTESIAN_POINT('Ctrl Pts',(2.08583932942016,57.6452671332937,14.7505474672967));
#50699=CARTESIAN_POINT('Ctrl Pts',(1.0271187815923,57.8141257639239,15.675240097315));
#50700=CARTESIAN_POINT('Ctrl Pts',(-0.385530753414024,57.9860425989135,
15.9070961282611));
#50701=CARTESIAN_POINT('Ctrl Pts',(-1.73158520520778,58.1610409781782,15.3493347285684));
#50702=CARTESIAN_POINT('Ctrl Pts',(-2.59642604963151,58.3391292245915,14.1448963194587));
#50703=CARTESIAN_POINT('Ctrl Pts',(-2.6977480214632,58.5203013328294,12.6395458443079));
#50704=CARTESIAN_POINT('Ctrl Pts',(-2.21829017326044,58.6431246926601,11.7364920572358));
#50705=CARTESIAN_POINT('Ctrl Pts',(-1.87373118021481,58.7050409812207,11.3796721415008));
#50706=CARTESIAN_POINT('Ctrl Pts',(-1.38039507702709,50.076218141491,10.9956530905807));
#50707=CARTESIAN_POINT('Ctrl Pts',(-0.937698733827671,50.139544364148,10.7478218458557));
#50708=CARTESIAN_POINT('Ctrl Pts',(0.0726730201489353,50.2638269915814,
10.5180529629421));
#50709=CARTESIAN_POINT('Ctrl Pts',(1.50804671887345,50.4464764583093,11.0213489381696));
#50710=CARTESIAN_POINT('Ctrl Pts',(2.43919210288125,50.6247478578092,12.1774757624556));
#50711=CARTESIAN_POINT('Ctrl Pts',(2.61762251691468,50.7999300445433,13.6253690971706));
#50712=CARTESIAN_POINT('Ctrl Pts',(2.01691345617751,50.9720306118236,14.9263443408183));
#50713=CARTESIAN_POINT('Ctrl Pts',(0.84101666814214,51.141071844296,15.7013612686244));
#50714=CARTESIAN_POINT('Ctrl Pts',(-0.539672554332687,51.3070901959662,
15.7386492490906));
#50715=CARTESIAN_POINT('Ctrl Pts',(-1.84606486311318,51.488253540335,14.9804774263704));
#50716=CARTESIAN_POINT('Ctrl Pts',(-2.48686976616666,51.6833878057799,13.4349447290737));
#50717=CARTESIAN_POINT('Ctrl Pts',(-1.88069220263553,51.8912845482392,11.7554333342278));
#50718=CARTESIAN_POINT('Ctrl Pts',(-0.466453883464498,52.0775069804336,
11.0137584058744));
#50719=CARTESIAN_POINT('Ctrl Pts',(0.898391463826697,52.2435426600827,11.2413241059542));
#50720=CARTESIAN_POINT('Ctrl Pts',(1.82013131511852,52.3905906573276,12.0457304948989));
#50721=CARTESIAN_POINT('Ctrl Pts',(2.17347372901692,52.535395877693,13.1991656893163));
#50722=CARTESIAN_POINT('Ctrl Pts',(1.87040943703913,52.6781089904421,14.3478349338331));
#50723=CARTESIAN_POINT('Ctrl Pts',(1.01867692078817,52.818892288325,15.1538716046093));
#50724=CARTESIAN_POINT('Ctrl Pts',(0.0739441295577446,52.9347428777394,
15.3472272232332));
#50725=CARTESIAN_POINT('Ctrl Pts',(-0.652591855125238,53.0266359142099,
15.1892751238726));
#50726=CARTESIAN_POINT('Ctrl Pts',(-1.10097860325353,53.0894667775354,14.9503092156441));
#50727=CARTESIAN_POINT('Ctrl Pts',(-1.37327990062071,53.1349635074734,14.7048827931288));
#50728=CARTESIAN_POINT('Ctrl Pts',(-1.54880115120083,53.169000057654,14.4960568797151));
#50729=CARTESIAN_POINT('Ctrl Pts',(-1.65080289404375,53.1916504120229,14.3453633115221));
#50730=CARTESIAN_POINT('Ctrl Pts',(-1.73607817443418,53.2142626286529,14.1855295099443));
#50731=CARTESIAN_POINT('Ctrl Pts',(-1.95912017807941,53.2820242674115,13.6895791042823));
#50732=CARTESIAN_POINT('Ctrl Pts',(-1.9857622071713,53.3774296209084,12.8828015365073));
#50733=CARTESIAN_POINT('Ctrl Pts',(-1.35497053014638,53.5334586942027,11.7668040096305));
#50734=CARTESIAN_POINT('Ctrl Pts',(-0.393543408219166,53.6552246050305,
11.3277277605396));
#50735=CARTESIAN_POINT('Ctrl Pts',(0.671222445108904,53.7875726475542,11.4654717127364));
#50736=CARTESIAN_POINT('Ctrl Pts',(1.45448968217153,53.8976248466317,11.9363841707008));
#50737=CARTESIAN_POINT('Ctrl Pts',(1.95672593529519,54.029508040218,12.9142942960394));
#50738=CARTESIAN_POINT('Ctrl Pts',(1.86620115658996,54.1614343723501,14.0086374010468));
#50739=CARTESIAN_POINT('Ctrl Pts',(1.37561477520337,54.2605693209982,14.6723379420933));
#50740=CARTESIAN_POINT('Ctrl Pts',(0.932286603854889,54.3268000163154,14.9662952376396));
#50741=CARTESIAN_POINT('Ctrl Pts',(0.612395230233797,54.3710011631004,15.1200122160106));
#50742=CARTESIAN_POINT('Ctrl Pts',(0.177468754305291,54.4263367221115,15.2262527359952));
#50743=CARTESIAN_POINT('Ctrl Pts',(-0.360468289344878,54.492911059353,15.2052657024364));
#50744=CARTESIAN_POINT('Ctrl Pts',(-1.04539755889047,54.5819329435911,14.9823912884061));
#50745=CARTESIAN_POINT('Ctrl Pts',(-1.73830611025955,54.6937590078159,14.360842969902));
#50746=CARTESIAN_POINT('Ctrl Pts',(-2.05380818987441,54.829029089085,13.2792099907643));
#50747=CARTESIAN_POINT('Ctrl Pts',(-1.74904435293057,54.96557504518,12.1838964031099));
#50748=CARTESIAN_POINT('Ctrl Pts',(-0.903732722772673,55.1035864882273,
11.4054185480954));
#50749=CARTESIAN_POINT('Ctrl Pts',(0.238738478562035,55.2432485953703,11.1869140328831));
#50750=CARTESIAN_POINT('Ctrl Pts',(1.09388563134303,55.3532916297124,11.5153761542378));
#50751=CARTESIAN_POINT('Ctrl Pts',(1.51840049618351,55.4247009257859,11.9026941453137));
#50752=CARTESIAN_POINT('Ctrl Pts',(1.68177989256486,55.4565502384435,12.0990768245851));
#50753=CARTESIAN_POINT('Ctrl Pts',(1.89857559515335,55.504439275324,12.4157685405086));
#50754=CARTESIAN_POINT('Ctrl Pts',(2.20982497937729,55.6088361650228,13.2091285658572));
#50755=CARTESIAN_POINT('Ctrl Pts',(2.00642546451976,55.7392717347732,14.3062123808336));
#50756=CARTESIAN_POINT('Ctrl Pts',(1.36487974060081,55.8552685847536,15.0037929464649));
#50757=CARTESIAN_POINT('Ctrl Pts',(0.907607853840278,55.9220988621651,15.2850386897666));
#50758=CARTESIAN_POINT('Ctrl Pts',(0.150818650069051,56.0229090640423,15.5778254925855));
#50759=CARTESIAN_POINT('Ctrl Pts',(-1.15818264988283,56.1762514493885,15.4570266938932));
#50760=CARTESIAN_POINT('Ctrl Pts',(-2.36606518144271,56.3855252604566,14.1290339448272));
#50761=CARTESIAN_POINT('Ctrl Pts',(-2.36409532515597,56.5998311154537,12.2882457014221));
#50762=CARTESIAN_POINT('Ctrl Pts',(-1.23039865326991,56.7949630068492,11.0581509457444));
#50763=CARTESIAN_POINT('Ctrl Pts',(0.180027614714824,56.9691714911501,10.7631001693718));
#50764=CARTESIAN_POINT('Ctrl Pts',(1.38123899516607,57.1208992985444,11.1158146174577));
#50765=CARTESIAN_POINT('Ctrl Pts',(2.32633124958793,57.2814776288627,12.047978478545));
#50766=CARTESIAN_POINT('Ctrl Pts',(2.69995491503163,57.4512855678146,13.4110176315643));
#50767=CARTESIAN_POINT('Ctrl Pts',(2.27509086520902,57.630712954941,14.8441602304258));
#50768=CARTESIAN_POINT('Ctrl Pts',(1.14019582655745,57.8132159809048,15.8542141232712));
#50769=CARTESIAN_POINT('Ctrl Pts',(-0.382153523165924,57.9987679166501,
16.1183629167064));
#50770=CARTESIAN_POINT('Ctrl Pts',(-1.83782511184269,58.1873270738983,15.5303429410537));
#50771=CARTESIAN_POINT('Ctrl Pts',(-2.77912446018748,58.3788380176838,14.2432873457464));
#50772=CARTESIAN_POINT('Ctrl Pts',(-2.9016356614965,58.573230723674,12.6290727314537));
#50773=CARTESIAN_POINT('Ctrl Pts',(-2.39657072442463,58.704691799483,11.6582421092171));
#50774=CARTESIAN_POINT('Ctrl Pts',(-2.0316063234475,58.770872412737,11.2736775653382));
#50775=CARTESIAN_POINT('Ctrl Pts',(-1.31764326136376,50.1427762584224,11.1748883313082));
#50776=CARTESIAN_POINT('Ctrl Pts',(-0.907564261464606,50.2017529476989,
10.9401048656914));
#50777=CARTESIAN_POINT('Ctrl Pts',(0.0299117337859448,50.3173142840308,
10.7177188227307));
#50778=CARTESIAN_POINT('Ctrl Pts',(1.36516229136849,50.4866571448322,11.1716424166742));
#50779=CARTESIAN_POINT('Ctrl Pts',(2.23669098008163,50.6515120192122,12.2323217381889));
#50780=CARTESIAN_POINT('Ctrl Pts',(2.41472518784499,50.8131370938521,13.5665029815585));
#50781=CARTESIAN_POINT('Ctrl Pts',(1.87393915282527,50.9716040924225,14.7701065169977));
#50782=CARTESIAN_POINT('Ctrl Pts',(0.800496200208616,51.1269998391949,15.4939711302219));
#50783=CARTESIAN_POINT('Ctrl Pts',(-0.466782200385848,51.2794254037523,
15.5419409021598));
#50784=CARTESIAN_POINT('Ctrl Pts',(-1.67290701406904,51.4456156410318,14.8597194065153));
#50785=CARTESIAN_POINT('Ctrl Pts',(-2.27662828459044,51.624537683161,13.4493427191478));
#50786=CARTESIAN_POINT('Ctrl Pts',(-1.73891142312258,51.8152179264018,11.902398809559));
#50787=CARTESIAN_POINT('Ctrl Pts',(-0.448640255077288,51.9862214852115,
11.2054328501155));
#50788=CARTESIAN_POINT('Ctrl Pts',(0.809618464574202,52.138972361647,11.3991526169767));
#50789=CARTESIAN_POINT('Ctrl Pts',(1.66881403661296,52.2745445668821,12.1300330092972));
#50790=CARTESIAN_POINT('Ctrl Pts',(2.00921048396892,52.4084092090614,13.1921079684185));
#50791=CARTESIAN_POINT('Ctrl Pts',(1.74208203868856,52.5407684752683,14.2611344398192));
#50792=CARTESIAN_POINT('Ctrl Pts',(0.95910986108932,52.6718338754084,15.0220806009597));
#50793=CARTESIAN_POINT('Ctrl Pts',(0.0781833017533357,52.7801539638208,
15.2147516689212));
#50794=CARTESIAN_POINT('Ctrl Pts',(-0.605576125165097,52.866385537563,15.0754217060589));
#50795=CARTESIAN_POINT('Ctrl Pts',(-1.03034406282696,52.9254937963779,14.8561201941823));
#50796=CARTESIAN_POINT('Ctrl Pts',(-1.29014344855479,52.9683955532627,14.6280278054059));
#50797=CARTESIAN_POINT('Ctrl Pts',(-1.45843328775186,53.0005338138439,14.4329836191468));
#50798=CARTESIAN_POINT('Ctrl Pts',(-1.55670098448433,53.021943072114,14.2917956930573));
#50799=CARTESIAN_POINT('Ctrl Pts',(-1.63935031825471,53.0433390787907,14.1415936573363));
#50800=CARTESIAN_POINT('Ctrl Pts',(-1.85664886861498,53.1075020154939,13.674723640504));
#50801=CARTESIAN_POINT('Ctrl Pts',(-1.89275421556756,53.1981980533294,12.9080047368929));
#50802=CARTESIAN_POINT('Ctrl Pts',(-1.30390491611055,53.3474495857692,11.8323186176413));
#50803=CARTESIAN_POINT('Ctrl Pts',(-0.383681630167233,53.4647766907041,
11.3955948485047));
#50804=CARTESIAN_POINT('Ctrl Pts',(0.651225537530613,53.5931767729554,11.5155686563152));
#50805=CARTESIAN_POINT('Ctrl Pts',(1.42140040038861,53.7005034177724,11.9644062269358));
#50806=CARTESIAN_POINT('Ctrl Pts',(1.92787386898523,53.830034178946,12.9180804555043));
#50807=CARTESIAN_POINT('Ctrl Pts',(1.85301864606095,53.9605380793125,14.0019424703478));
#50808=CARTESIAN_POINT('Ctrl Pts',(1.3731067718055,54.059308496705,14.6697897879136));
#50809=CARTESIAN_POINT('Ctrl Pts',(0.933061902121851,54.1255895655204,14.9695067587001));
#50810=CARTESIAN_POINT('Ctrl Pts',(0.614259299493522,54.1699024449187,15.1275813670082));
#50811=CARTESIAN_POINT('Ctrl Pts',(0.178401843845132,54.2255242831011,15.2398465241946));
#50812=CARTESIAN_POINT('Ctrl Pts',(-0.364498998024635,54.2926761681464,
15.2253995662538));
#50813=CARTESIAN_POINT('Ctrl Pts',(-1.06052390331458,54.3827793578848,15.0083722694167));
#50814=CARTESIAN_POINT('Ctrl Pts',(-1.77355584470913,54.4965382759009,14.3851241444334));
#50815=CARTESIAN_POINT('Ctrl Pts',(-2.11063691548484,54.6350469321954,13.2816258274837));
#50816=CARTESIAN_POINT('Ctrl Pts',(-1.81058302305334,54.7757351614645,12.1491305578278));
#50817=CARTESIAN_POINT('Ctrl Pts',(-0.944219575881998,54.918773158289,11.3316338758417));
#50818=CARTESIAN_POINT('Ctrl Pts',(0.24378312716608,55.0643219256763,11.0897728253293));
#50819=CARTESIAN_POINT('Ctrl Pts',(1.14359453483077,55.179591554497,11.4234917272422));
#50820=CARTESIAN_POINT('Ctrl Pts',(1.594107580686,55.2546269955245,11.8256735534423));
#50821=CARTESIAN_POINT('Ctrl Pts',(1.76820356899201,55.2881321265545,12.0304265488723));
#50822=CARTESIAN_POINT('Ctrl Pts',(2.00000619829663,55.3385484417741,12.3614071208809));
#50823=CARTESIAN_POINT('Ctrl Pts',(2.3374038248435,55.4486533549761,13.1945583269953));
#50824=CARTESIAN_POINT('Ctrl Pts',(2.13503615164275,55.586785700239,14.3588883789362));
#50825=CARTESIAN_POINT('Ctrl Pts',(1.46088944635544,55.710058084209,15.1074084078187));
#50826=CARTESIAN_POINT('Ctrl Pts',(0.977148776715703,55.781195511413,15.4116879900337));
#50827=CARTESIAN_POINT('Ctrl Pts',(0.173924477173412,55.8886095419895,15.7317674296736));
#50828=CARTESIAN_POINT('Ctrl Pts',(-1.22564291596938,56.0523911368355,15.6173328388221));
#50829=CARTESIAN_POINT('Ctrl Pts',(-2.53412984108696,56.2765988592834,14.2074858335199));
#50830=CARTESIAN_POINT('Ctrl Pts',(-2.55113652423423,56.5067311267252,12.2305709116292));
#50831=CARTESIAN_POINT('Ctrl Pts',(-1.34397736419971,56.7166040708691,10.8961407544736));
#50832=CARTESIAN_POINT('Ctrl Pts',(0.171376806954028,56.9041113720079,10.5649999101602));
#50833=CARTESIAN_POINT('Ctrl Pts',(1.46804367168455,57.0674713743434,10.9334596080689));
#50834=CARTESIAN_POINT('Ctrl Pts',(2.49426073708746,57.2403616973154,11.9284104985044));
#50835=CARTESIAN_POINT('Ctrl Pts',(2.90875309006288,57.4231414817237,13.3922632584958));
#50836=CARTESIAN_POINT('Ctrl Pts',(2.46434240099787,57.6161587765882,14.937772993555));
#50837=CARTESIAN_POINT('Ctrl Pts',(1.25327287152259,57.8123061978857,16.0331881492274));
#50838=CARTESIAN_POINT('Ctrl Pts',(-0.378776292917826,58.0114932343869,
16.3296297051516));
#50839=CARTESIAN_POINT('Ctrl Pts',(-1.94406501847761,58.2136131696184,15.7113511535389));
#50840=CARTESIAN_POINT('Ctrl Pts',(-2.96182287074345,58.4185468107759,14.3416783720341));
#50841=CARTESIAN_POINT('Ctrl Pts',(-3.10552330152979,58.6261601145185,12.6185996185993));
#50842=CARTESIAN_POINT('Ctrl Pts',(-2.57485127558882,58.766258906306,11.5799921611984));
#50843=CARTESIAN_POINT('Ctrl Pts',(-2.1894814666802,58.8367038442533,11.1676829891756));
#50844=CARTESIAN_POINT('Ctrl Pts',(-1.29179640210147,50.1461249705794,11.1593417706458));
#50845=CARTESIAN_POINT('Ctrl Pts',(-1.17586424793724,50.1627439522706,11.0949541057819));
#50846=CARTESIAN_POINT('Ctrl Pts',(-1.05506647233865,50.1792583497506,11.0397640939357));
#50847=CARTESIAN_POINT('Ctrl Pts',(-0.806845719013178,50.2121678519162,
10.9492055679426));
#50848=CARTESIAN_POINT('Ctrl Pts',(-0.679414851388805,50.2285627637462,
10.9138653769205));
#50849=CARTESIAN_POINT('Ctrl Pts',(-0.529965369448136,50.2475136893414,
10.8852859534053));
#50850=CARTESIAN_POINT('Ctrl Pts',(-0.509490630910326,50.2501040671278,
10.8816456967675));
#50851=CARTESIAN_POINT('Ctrl Pts',(-0.35763717065511,50.2692794071308,10.8566918042585));
#50852=CARTESIAN_POINT('Ctrl Pts',(-0.224930869811676,50.2858350211732,
10.8461950652809));
#50853=CARTESIAN_POINT('Ctrl Pts',(-0.0521410480261596,50.3074751348745,
10.8463357374599));
#50854=CARTESIAN_POINT('Ctrl Pts',(-0.0116722601119271,50.3125494626139,
10.8473628673328));
#50855=CARTESIAN_POINT('Ctrl Pts',(0.193236338609998,50.3383118287223,10.8575462627135));
#50856=CARTESIAN_POINT('Ctrl Pts',(0.356593166603047,50.3587994429838,10.8821914828471));
#50857=CARTESIAN_POINT('Ctrl Pts',(0.680754099283437,50.4004080786556,10.9644180392955));
#50858=CARTESIAN_POINT('Ctrl Pts',(0.841169971214191,50.4215200682444,11.0233226785241));
#50859=CARTESIAN_POINT('Ctrl Pts',(1.02106458037202,50.4465567330081,11.1121586059517));
#50860=CARTESIAN_POINT('Ctrl Pts',(1.04899253268544,50.450485635207,11.1266537702159));
#50861=CARTESIAN_POINT('Ctrl Pts',(1.15005120124451,50.4648734370134,11.1817332145071));
#50862=CARTESIAN_POINT('Ctrl Pts',(1.2211901834219,50.4753360438438,11.2256500811951));
#50863=CARTESIAN_POINT('Ctrl Pts',(1.418399848808,50.5054907842792,11.3621121143303));
#50864=CARTESIAN_POINT('Ctrl Pts',(1.53778885079935,50.5250399263045,11.4635464474702));
#50865=CARTESIAN_POINT('Ctrl Pts',(1.75695410848228,50.5643650866753,11.6889686450017));
#50866=CARTESIAN_POINT('Ctrl Pts',(1.85622983574385,50.5841363126383,11.8134137692257));
#50867=CARTESIAN_POINT('Ctrl Pts',(2.01079050490025,50.6195700815444,12.051823621597));
#50868=CARTESIAN_POINT('Ctrl Pts',(2.07090096760105,50.6352647387523,12.1629203938869));
#50869=CARTESIAN_POINT('Ctrl Pts',(2.1224071124382,50.6512188039548,12.2801085395122));
#50870=CARTESIAN_POINT('Ctrl Pts',(2.12339031658304,50.6515244779251,12.2823553349035));
#50871=CARTESIAN_POINT('Ctrl Pts',(2.19638114822366,50.6743013862446,12.4498845871826));
#50872=CARTESIAN_POINT('Ctrl Pts',(2.24857224748294,50.6967310898809,12.6229960356089));
#50873=CARTESIAN_POINT('Ctrl Pts',(2.29457780293144,50.7289582945877,12.8768626019824));
#50874=CARTESIAN_POINT('Ctrl Pts',(2.3047165576568,50.7388180282312,12.9552293374338));
#50875=CARTESIAN_POINT('Ctrl Pts',(2.32423796476578,50.7700886808865,13.2047365765726));
#50876=CARTESIAN_POINT('Ctrl Pts',(2.31867125305314,50.7914312158333,13.376466475896));
#50877=CARTESIAN_POINT('Ctrl Pts',(2.28267958031064,50.8232467749868,13.6287825259408));
#50878=CARTESIAN_POINT('Ctrl Pts',(2.26609809947773,50.833822646406,13.7119840627583));
#50879=CARTESIAN_POINT('Ctrl Pts',(2.20724046855379,50.8632383604427,13.9400923928012));
#50880=CARTESIAN_POINT('Ctrl Pts',(2.15500951480601,50.8820368501375,14.0820711253277));
#50881=CARTESIAN_POINT('Ctrl Pts',(2.04534812313239,50.9135193781906,14.3092231015875));
#50882=CARTESIAN_POINT('Ctrl Pts',(1.99489994162873,50.9262398524308,14.3980630649955));
#50883=CARTESIAN_POINT('Ctrl Pts',(1.89729738157964,50.9483522867086,14.5459858768816));
#50884=CARTESIAN_POINT('Ctrl Pts',(1.85262945323311,50.9577594047374,14.6068481547701));
#50885=CARTESIAN_POINT('Ctrl Pts',(1.78652888145326,50.9708331892289,14.6881566921951));
#50886=CARTESIAN_POINT('Ctrl Pts',(1.7674606261628,50.9745163949834,14.7106999398698));
#50887=CARTESIAN_POINT('Ctrl Pts',(1.66758140032378,50.9933823288577,14.8242170465195));
#50888=CARTESIAN_POINT('Ctrl Pts',(1.58001302620175,51.0085365102027,14.9089121159274));
#50889=CARTESIAN_POINT('Ctrl Pts',(1.46837758706177,51.026560523629,15.0004222798649));
#50890=CARTESIAN_POINT('Ctrl Pts',(1.45013318498345,51.0294685360955,15.0148993419957));
#50891=CARTESIAN_POINT('Ctrl Pts',(1.3332453445594,51.0478721224418,15.1046435322073));
#50892=CARTESIAN_POINT('Ctrl Pts',(1.2286840050754,51.063325503062,15.171574111418));
#50893=CARTESIAN_POINT('Ctrl Pts',(1.03797613055253,51.0902744474102,15.2727381849875));
#50894=CARTESIAN_POINT('Ctrl Pts',(0.953761854894311,51.1017936342927,15.3109637342375));
#50895=CARTESIAN_POINT('Ctrl Pts',(0.83654647437363,51.1174529760332,15.3558387378948));
#50896=CARTESIAN_POINT('Ctrl Pts',(0.805065623226275,51.121623155736,15.3671002953147));
#50897=CARTESIAN_POINT('Ctrl Pts',(0.751497073195426,51.1286671720629,15.3849433348014));
#50898=CARTESIAN_POINT('Ctrl Pts',(0.729504660089768,51.1315444632091,15.3918983640672));
#50899=CARTESIAN_POINT('Ctrl Pts',(0.59077613133458,51.1496119923445,15.4334553885158));
#50900=CARTESIAN_POINT('Ctrl Pts',(0.471527395855336,51.1647775623704,15.4589347154352));
#50901=CARTESIAN_POINT('Ctrl Pts',(0.255444467995113,51.1919823954698,15.4868218740711));
#50902=CARTESIAN_POINT('Ctrl Pts',(0.158948751454997,51.2040344282913,15.4928509746133));
#50903=CARTESIAN_POINT('Ctrl Pts',(-0.0606144237304076,51.2314718057864,
15.4915853832341));
#50904=CARTESIAN_POINT('Ctrl Pts',(-0.183507513308038,51.2468396234302,
15.4800566095026));
#50905=CARTESIAN_POINT('Ctrl Pts',(-0.346682219876221,51.2675349729358,
15.4508484975454));
#50906=CARTESIAN_POINT('Ctrl Pts',(-0.388853073455517,51.2729104729639,
15.4420071485642));
#50907=CARTESIAN_POINT('Ctrl Pts',(-0.460714312994654,51.2821326748638,
15.4247369920905));
#50908=CARTESIAN_POINT('Ctrl Pts',(-0.4905775182599,51.2859838954058,15.4168935616789));
#50909=CARTESIAN_POINT('Ctrl Pts',(-0.662388445407937,51.3082698972205,
15.3679111806786));
#50910=CARTESIAN_POINT('Ctrl Pts',(-0.800135864393537,51.326651692665,15.3132516977476));
#50911=CARTESIAN_POINT('Ctrl Pts',(-1.05111869021365,51.3619071966508,15.1832536191353));
#50912=CARTESIAN_POINT('Ctrl Pts',(-1.16541856053576,51.378789975927,15.1097891701591));
#50913=CARTESIAN_POINT('Ctrl Pts',(-1.34032287189366,51.4066220560649,14.9717203670751));
#50914=CARTESIAN_POINT('Ctrl Pts',(-1.40583084792222,51.4176049990611,14.9128329597658));
#50915=CARTESIAN_POINT('Ctrl Pts',(-1.55710172033224,51.4445494309785,14.7589776593018));
#50916=CARTESIAN_POINT('Ctrl Pts',(-1.63849547777328,51.4605055280583,14.6597068329473));
#50917=CARTESIAN_POINT('Ctrl Pts',(-1.78396947503599,51.492695415786,14.446550254468));
#50918=CARTESIAN_POINT('Ctrl Pts',(-1.84762121195314,51.5089274427981,14.3323886904574));
#50919=CARTESIAN_POINT('Ctrl Pts',(-1.95039781399511,51.5405318486693,14.1008765240707));
#50920=CARTESIAN_POINT('Ctrl Pts',(-1.99053792233632,51.5559086533289,13.9839319099237));
#50921=CARTESIAN_POINT('Ctrl Pts',(-2.05051883101226,51.5873985547467,13.7390920925521));
#50922=CARTESIAN_POINT('Ctrl Pts',(-2.06913373203656,51.6035060902381,13.6109490311358));
#50923=CARTESIAN_POINT('Ctrl Pts',(-2.07658307411553,51.6209979176689,13.4710355237018));
#50924=CARTESIAN_POINT('Ctrl Pts',(-2.07710333853888,51.6224437457318,13.4594649641365));
#50925=CARTESIAN_POINT('Ctrl Pts',(-2.08161127178146,51.6377785645872,13.3367015492881));
#50926=CARTESIAN_POINT('Ctrl Pts',(-2.0768906847889,51.6516451125443,13.225232731368));
#50927=CARTESIAN_POINT('Ctrl Pts',(-2.04996245357585,51.6795430946767,13.002999483218));
#50928=CARTESIAN_POINT('Ctrl Pts',(-2.02747647562859,51.6935736212083,12.8922761942963));
#50929=CARTESIAN_POINT('Ctrl Pts',(-1.96986329330764,51.7194408597748,12.6929337032827));
#50930=CARTESIAN_POINT('Ctrl Pts',(-1.93717477217231,51.7312872218979,12.603511469113));
#50931=CARTESIAN_POINT('Ctrl Pts',(-1.85250536853668,51.7570978496006,12.414821694989));
#50932=CARTESIAN_POINT('Ctrl Pts',(-1.79808195042894,51.7710509339456,12.3167695391442));
#50933=CARTESIAN_POINT('Ctrl Pts',(-1.69222557680776,51.7948861173685,12.1578491771332));
#50934=CARTESIAN_POINT('Ctrl Pts',(-1.64440025423007,51.8047897740442,12.0943729990204));
#50935=CARTESIAN_POINT('Ctrl Pts',(-1.51889540976364,51.8290393881842,11.9461348902174));
#50936=CARTESIAN_POINT('Ctrl Pts',(-1.43727839884043,51.8433817647499,11.864518711087));
#50937=CARTESIAN_POINT('Ctrl Pts',(-1.26018468176299,51.8723019326257,11.7146941756349));
#50938=CARTESIAN_POINT('Ctrl Pts',(-1.16445722035746,51.8868784620027,11.646799062312));
#50939=CARTESIAN_POINT('Ctrl Pts',(-1.0403118987082,51.9048138851257,11.5742565394263));
#50940=CARTESIAN_POINT('Ctrl Pts',(-1.0165580949766,51.9082050026956,11.5610270483265));
#50941=CARTESIAN_POINT('Ctrl Pts',(-0.886230181033722,51.9266059286065,
11.4919699006493));
#50942=CARTESIAN_POINT('Ctrl Pts',(-0.774980714599116,51.9415806150534,
11.4456417155808));
#50943=CARTESIAN_POINT('Ctrl Pts',(-0.546665599177198,51.9714506849704,
11.3734376767949));
#50944=CARTESIAN_POINT('Ctrl Pts',(-0.429601728614386,51.9863460715534,
11.3475620219376));
#50945=CARTESIAN_POINT('Ctrl Pts',(-0.20907029431664,52.0141170173263,11.3185983547831));
#50946=CARTESIAN_POINT('Ctrl Pts',(-0.105507065200747,52.0270354059357,
11.3129390984546));
#50947=CARTESIAN_POINT('Ctrl Pts',(0.0968600497403189,52.0523391978825,
11.3175607270828));
#50948=CARTESIAN_POINT('Ctrl Pts',(0.195690778708763,52.0647257440447,11.3272285239059));
#50949=CARTESIAN_POINT('Ctrl Pts',(0.394666389716627,52.0900046130345,11.3624215846142));
#50950=CARTESIAN_POINT('Ctrl Pts',(0.494666261615732,52.1028943938056,11.388646349898));
#50951=CARTESIAN_POINT('Ctrl Pts',(0.650436010770195,52.1234862819425,11.4427582385991));
#50952=CARTESIAN_POINT('Ctrl Pts',(0.708009702836697,52.1312170896882,11.465854397369));
#50953=CARTESIAN_POINT('Ctrl Pts',(0.908378342693344,52.1586620965296,11.557219078334));
#50954=CARTESIAN_POINT('Ctrl Pts',(1.04433397233415,52.1783760941834,11.6399044718939));
#50955=CARTESIAN_POINT('Ctrl Pts',(1.25596480420899,52.2119564581144,11.8058424032475));
#50956=CARTESIAN_POINT('Ctrl Pts',(1.33764786615372,52.2258487508522,11.8818722370674));
#50957=CARTESIAN_POINT('Ctrl Pts',(1.47438965523274,52.2513576139545,12.0335455604943));
#50958=CARTESIAN_POINT('Ctrl Pts',(1.5316168485671,52.262985037636,12.1073305051343));
#50959=CARTESIAN_POINT('Ctrl Pts',(1.67651718649737,52.2955324176947,12.3244608194884));
#50960=CARTESIAN_POINT('Ctrl Pts',(1.751625979797,52.3164404623527,12.4761088530483));
#50961=CARTESIAN_POINT('Ctrl Pts',(1.85747547577759,52.3568550308588,12.7825292048041));
#50962=CARTESIAN_POINT('Ctrl Pts',(1.89071205140988,52.3763669053139,12.9365034058105));
#50963=CARTESIAN_POINT('Ctrl Pts',(1.90496519311471,52.3971496326665,13.1022334456341));
#50964=CARTESIAN_POINT('Ctrl Pts',(1.9057728968132,52.3984581090635,13.1126750815767));
#50965=CARTESIAN_POINT('Ctrl Pts',(1.90809346985574,52.4026904974495,13.1464687856724));
#50966=CARTESIAN_POINT('Ctrl Pts',(1.90924527016826,52.4056137288121,13.1698392143514));
#50967=CARTESIAN_POINT('Ctrl Pts',(1.91309537134773,52.4215488005786,13.2973190082068));
#50968=CARTESIAN_POINT('Ctrl Pts',(1.90743589505222,52.4344232528633,13.4013571204969));
#50969=CARTESIAN_POINT('Ctrl Pts',(1.87915170135077,52.460524475602,13.6106265793392));
#50970=CARTESIAN_POINT('Ctrl Pts',(1.85591940311975,52.4737471623773,13.7157662255528));
#50971=CARTESIAN_POINT('Ctrl Pts',(1.7926210353516,52.5003841586456,13.9216751125366));
#50972=CARTESIAN_POINT('Ctrl Pts',(1.7523861734177,52.5137990825969,14.0223908190224));
#50973=CARTESIAN_POINT('Ctrl Pts',(1.68896709292507,52.5316406160847,14.1496679706925));
#50974=CARTESIAN_POINT('Ctrl Pts',(1.67285356038215,52.5359612550644,14.1799816478008));
#50975=CARTESIAN_POINT('Ctrl Pts',(1.61463063172757,52.5509024881449,14.2828327404829));
#50976=CARTESIAN_POINT('Ctrl Pts',(1.5685788779595,52.5614898243686,14.3532338477688));
#50977=CARTESIAN_POINT('Ctrl Pts',(1.467961958202,52.5825407647531,14.4867185085709));
#50978=CARTESIAN_POINT('Ctrl Pts',(1.4134602066283,52.5930047153806,14.5498495048677));
#50979=CARTESIAN_POINT('Ctrl Pts',(1.34293420300396,52.6055738417265,14.620898234876));
#50980=CARTESIAN_POINT('Ctrl Pts',(1.33078705314162,52.6077073105751,14.6327913976951));
#50981=CARTESIAN_POINT('Ctrl Pts',(1.25778486523938,52.6203483968795,14.7022350773085));
#50982=CARTESIAN_POINT('Ctrl Pts',(1.19305604375341,52.6308261052914,14.7555888359258));
#50983=CARTESIAN_POINT('Ctrl Pts',(1.05770518068061,52.6516236232434,14.8526032457158));
#50984=CARTESIAN_POINT('Ctrl Pts',(0.987135813715497,52.6619440270014,14.8963380206378));
#50985=CARTESIAN_POINT('Ctrl Pts',(0.828435187824385,52.6843151760371,14.9810847293576));
#50986=CARTESIAN_POINT('Ctrl Pts',(0.739230858262599,52.6964132353955,15.0203306293797));
#50987=CARTESIAN_POINT('Ctrl Pts',(0.55667191136831,52.7205449514636,15.0849210004443));
#50988=CARTESIAN_POINT('Ctrl Pts',(0.463342791847309,52.7325785749457,15.1103445647152));
#50989=CARTESIAN_POINT('Ctrl Pts',(0.278547995135265,52.7560859638772,15.1461123668855));
#50990=CARTESIAN_POINT('Ctrl Pts',(0.187197112947158,52.767559680129,15.1571043406759));
#50991=CARTESIAN_POINT('Ctrl Pts',(0.0333489091256805,52.7868272388106,
15.1641428131738));
#50992=CARTESIAN_POINT('Ctrl Pts',(-0.0290093074805301,52.7946215233249,
15.1638501338707));
#50993=CARTESIAN_POINT('Ctrl Pts',(-0.130161023150543,52.8072974862492,
15.1580738250435));
#50994=CARTESIAN_POINT('Ctrl Pts',(-0.16903749864418,52.812180450813,15.154568420337));
#50995=CARTESIAN_POINT('Ctrl Pts',(-0.282951798217108,52.8265496495956,
15.1404086688194));
#50996=CARTESIAN_POINT('Ctrl Pts',(-0.357502667492476,52.836032692471,15.1261265810317));
#50997=CARTESIAN_POINT('Ctrl Pts',(-0.487431559665585,52.8528096790146,
15.0927052855356));
#50998=CARTESIAN_POINT('Ctrl Pts',(-0.543311667052286,52.8601106545406,
15.0754124712946));
#50999=CARTESIAN_POINT('Ctrl Pts',(-0.672468927188591,52.8772555493765,
15.0287275110183));
#51000=CARTESIAN_POINT('Ctrl Pts',(-0.744968824082721,52.8869749370748,
14.9972904130696));
#51001=CARTESIAN_POINT('Ctrl Pts',(-0.88625594940133,52.9064666469949,14.9254612112881));
#51002=CARTESIAN_POINT('Ctrl Pts',(-0.954992927424705,52.9162383603264,
14.8849712410689));
#51003=CARTESIAN_POINT('Ctrl Pts',(-1.03237681943862,52.927810179237,14.8326387508207));
#51004=CARTESIAN_POINT('Ctrl Pts',(-1.04377042911234,52.9295293459953,14.8247515713228));
#51005=CARTESIAN_POINT('Ctrl Pts',(-1.12772375223892,52.9423197256733,14.7652693977536));
#51006=CARTESIAN_POINT('Ctrl Pts',(-1.19671876868382,52.9535337352294,14.7087197105301));
#51007=CARTESIAN_POINT('Ctrl Pts',(-1.29040020935121,52.9698180030159,14.6202129638619));
#51008=CARTESIAN_POINT('Ctrl Pts',(-1.31856185527217,52.9748705118411,14.5918639537878));
#51009=CARTESIAN_POINT('Ctrl Pts',(-1.37505353547673,52.9853433031168,14.5312336301288));
#51010=CARTESIAN_POINT('Ctrl Pts',(-1.40327439448105,52.9907017870527,14.4988476507206));
#51011=CARTESIAN_POINT('Ctrl Pts',(-1.47406010616561,53.0047365927575,14.4115649842979));
#51012=CARTESIAN_POINT('Ctrl Pts',(-1.51472285237196,53.0134194689159,14.3551075209223));
#51013=CARTESIAN_POINT('Ctrl Pts',(-1.56993877475166,53.0263273541817,14.267892303756));
#51014=CARTESIAN_POINT('Ctrl Pts',(-1.5871878131941,53.0305548494566,14.2388040871341));
#51015=CARTESIAN_POINT('Ctrl Pts',(-1.61596633367774,53.03796972398,14.1869558536698));
#51016=CARTESIAN_POINT('Ctrl Pts',(-1.62786167879273,53.0411579930626,14.1643930901733));
#51017=CARTESIAN_POINT('Ctrl Pts',(-1.65847188291452,53.0497088701303,14.1032180448185));
#51018=CARTESIAN_POINT('Ctrl Pts',(-1.67633651634066,53.0550296808571,14.064167328875));
#51019=CARTESIAN_POINT('Ctrl Pts',(-1.72761725199409,53.0712352593059,13.941490778788));
#51020=CARTESIAN_POINT('Ctrl Pts',(-1.75613310696713,53.0823149282675,13.8558862008896));
#51021=CARTESIAN_POINT('Ctrl Pts',(-1.80125458925947,53.1049138539715,13.6792179862168));
#51022=CARTESIAN_POINT('Ctrl Pts',(-1.81751391322657,53.1164368270852,13.5880682666396));
#51023=CARTESIAN_POINT('Ctrl Pts',(-1.83659901735704,53.1394540437642,13.4053349580862));
#51024=CARTESIAN_POINT('Ctrl Pts',(-1.8395484580033,53.1509475590332,13.3137620309028));
#51025=CARTESIAN_POINT('Ctrl Pts',(-1.83232956546884,53.1733429593277,13.1360677270543));
#51026=CARTESIAN_POINT('Ctrl Pts',(-1.8228506889041,53.184243814313,13.0499143095028));
#51027=CARTESIAN_POINT('Ctrl Pts',(-1.79514578072454,53.2036006190261,12.8986188081948));
#51028=CARTESIAN_POINT('Ctrl Pts',(-1.77933056012774,53.2120616708149,12.8330613116409));
#51029=CARTESIAN_POINT('Ctrl Pts',(-1.75553580489027,53.2223153072095,12.7546790551827));
#51030=CARTESIAN_POINT('Ctrl Pts',(-1.75116778966746,53.2241201943003,12.740898178659));
#51031=CARTESIAN_POINT('Ctrl Pts',(-1.72018614796545,53.2364149462963,12.6471902915767));
#51032=CARTESIAN_POINT('Ctrl Pts',(-1.68798199364942,53.246766229533,12.5691261348581));
#51033=CARTESIAN_POINT('Ctrl Pts',(-1.61338950991954,53.2672915820224,12.4187346356801));
#51034=CARTESIAN_POINT('Ctrl Pts',(-1.57108010244899,53.2774664081388,12.3463690886902));
#51035=CARTESIAN_POINT('Ctrl Pts',(-1.48230345323922,53.296791016633,12.2154954163202));
#51036=CARTESIAN_POINT('Ctrl Pts',(-1.43677168397069,53.3059333969882,12.1563347568848));
#51037=CARTESIAN_POINT('Ctrl Pts',(-1.32189492162835,53.3276685152984,12.0241407949197));
#51038=CARTESIAN_POINT('Ctrl Pts',(-1.24956792870111,53.3402656824691,11.9531049964235));
#51039=CARTESIAN_POINT('Ctrl Pts',(-1.09319962842738,53.3657518310656,11.8222453555277));
#51040=CARTESIAN_POINT('Ctrl Pts',(-1.0089838251504,53.3786421421447,11.7626301584854));
#51041=CARTESIAN_POINT('Ctrl Pts',(-0.835660084156748,53.4038730474459,
11.6605321070325));
#51042=CARTESIAN_POINT('Ctrl Pts',(-0.746904437412114,53.4162141446784,
11.6174379818867));
#51043=CARTESIAN_POINT('Ctrl Pts',(-0.55687120493277,53.4416891463299,11.5443386851595));
#51044=CARTESIAN_POINT('Ctrl Pts',(-0.455153850915069,53.4548165153692,
11.5154912212315));
#51045=CARTESIAN_POINT('Ctrl Pts',(-0.253404567611201,53.4802178240072,
11.4763900477341));
#51046=CARTESIAN_POINT('Ctrl Pts',(-0.153553967050764,53.4925010753352,
11.4652586462183));
#51047=CARTESIAN_POINT('Ctrl Pts',(-0.0480126903616401,53.5053244641644,
11.4616570030259));
#51048=CARTESIAN_POINT('Ctrl Pts',(-0.0426079119451699,53.5059807100768,
11.4614950504468));
#51049=CARTESIAN_POINT('Ctrl Pts',(0.0513733894600363,53.5173845659481,
11.4590691863365));
#51050=CARTESIAN_POINT('Ctrl Pts',(0.140254137527553,53.5283771592707,11.4632546135913));
#51051=CARTESIAN_POINT('Ctrl Pts',(0.310685215532395,53.5499414985786,11.4835636241241));
#51052=CARTESIAN_POINT('Ctrl Pts',(0.392326816791214,53.5604918787679,11.4988643053244));
#51053=CARTESIAN_POINT('Ctrl Pts',(0.582550331029838,53.5856968951546,11.5478513516785));
#51054=CARTESIAN_POINT('Ctrl Pts',(0.690080426533256,53.6001540354735,11.5858565329136));
#51055=CARTESIAN_POINT('Ctrl Pts',(0.838421464801602,53.6208203533813,11.6543071758409));
#51056=CARTESIAN_POINT('Ctrl Pts',(0.882775666748859,53.6271001355276,11.6770034415749));
#51057=CARTESIAN_POINT('Ctrl Pts',(1.02543888640962,53.6477191786957,11.7577221125681));
#51058=CARTESIAN_POINT('Ctrl Pts',(1.11946751763241,53.6619956713904,11.823522325871));
#51059=CARTESIAN_POINT('Ctrl Pts',(1.25746426902585,53.6844652997591,11.9401938591112));
#51060=CARTESIAN_POINT('Ctrl Pts',(1.30587427989571,53.6926955982797,11.9857312680104));
#51061=CARTESIAN_POINT('Ctrl Pts',(1.41651485955325,53.7125031119117,12.1012932274944));
#51062=CARTESIAN_POINT('Ctrl Pts',(1.4763566033618,53.7241420850694,12.1739261982714));
#51063=CARTESIAN_POINT('Ctrl Pts',(1.58916731369618,53.7484867988033,12.333991562844));
#51064=CARTESIAN_POINT('Ctrl Pts',(1.64111509444718,53.7611989419891,12.4221570457005));
#51065=CARTESIAN_POINT('Ctrl Pts',(1.7009760206621,53.7783822065853,12.5461529278465));
#51066=CARTESIAN_POINT('Ctrl Pts',(1.71552967964692,53.7828269823785,12.5786597637478));
#51067=CARTESIAN_POINT('Ctrl Pts',(1.75544958828922,53.7958795401923,12.6752638704256));
#51068=CARTESIAN_POINT('Ctrl Pts',(1.77820933196254,53.8044958945969,12.7404933543574));
#51069=CARTESIAN_POINT('Ctrl Pts',(1.81016291687527,53.818835618921,12.8507253527809));
#51070=CARTESIAN_POINT('Ctrl Pts',(1.82134356595601,53.8245549610328,12.8951328802289));
#51071=CARTESIAN_POINT('Ctrl Pts',(1.83566011474081,53.8331932585586,12.9626944877087));
#51072=CARTESIAN_POINT('Ctrl Pts',(1.84007397545403,53.8361016976207,12.985597685492));
#51073=CARTESIAN_POINT('Ctrl Pts',(1.85783388420497,53.8490750701629,13.0883439639632));
#51074=CARTESIAN_POINT('Ctrl Pts',(1.86630207219487,53.8590657291333,13.1690460907899));
#51075=CARTESIAN_POINT('Ctrl Pts',(1.87260437825337,53.8786337609155,13.3281044480159));
#51076=CARTESIAN_POINT('Ctrl Pts',(1.87081981580395,53.8882126943262,13.4064365546596));
#51077=CARTESIAN_POINT('Ctrl Pts',(1.8576294032269,53.9073808205236,13.5621825064978));
#51078=CARTESIAN_POINT('Ctrl Pts',(1.846264239738,53.9169697910096,13.6395986515081));
#51079=CARTESIAN_POINT('Ctrl Pts',(1.81420647608039,53.9362077923623,13.7920280038178));
#51080=CARTESIAN_POINT('Ctrl Pts',(1.7935810874306,53.9458558834466,13.867054064916));
#51081=CARTESIAN_POINT('Ctrl Pts',(1.76504038369673,53.95689471959,13.950259512124));
#51082=CARTESIAN_POINT('Ctrl Pts',(1.76161259861716,53.9581910207318,13.959989761124));
#51083=CARTESIAN_POINT('Ctrl Pts',(1.72936900531379,53.9701216179985,14.0491502227609));
#51084=CARTESIAN_POINT('Ctrl Pts',(1.69532154673149,53.9808329901845,14.1269135916044));
#51085=CARTESIAN_POINT('Ctrl Pts',(1.61731520646525,54.0022769951949,14.2770750666882));
#51086=CARTESIAN_POINT('Ctrl Pts',(1.57340457294557,54.0130092894204,14.3494961122909));
#51087=CARTESIAN_POINT('Ctrl Pts',(1.48890474205988,54.0316556374554,14.469719730799));
#51088=CARTESIAN_POINT('Ctrl Pts',(1.45046576971118,54.0395706510287,14.5189981605161));
#51089=CARTESIAN_POINT('Ctrl Pts',(1.35457793571589,54.0580987293182,14.6297651066965));
#51090=CARTESIAN_POINT('Ctrl Pts',(1.29514743632753,54.0687001937351,14.6895977819501));
#51091=CARTESIAN_POINT('Ctrl Pts',(1.20499617301088,54.0837609105672,14.7692549802991));
#51092=CARTESIAN_POINT('Ctrl Pts',(1.17730528186333,54.0882638247712,14.7923831782251));
#51093=CARTESIAN_POINT('Ctrl Pts',(1.07963596307844,54.1037564082215,14.8695287126092));
#51094=CARTESIAN_POINT('Ctrl Pts',(1.00629893197122,54.1148030853843,14.9194748670905));
#51095=CARTESIAN_POINT('Ctrl Pts',(0.867063621703206,54.1349395177051,15.0008702222197));
#51096=CARTESIAN_POINT('Ctrl Pts',(0.802214373268047,54.1440219150142,15.0340303763525));
#51097=CARTESIAN_POINT('Ctrl Pts',(0.720984782991892,54.1551055669021,15.0699821747632));
#51098=CARTESIAN_POINT('Ctrl Pts',(0.706253100245556,54.1571043616304,15.0762865178801));
#51099=CARTESIAN_POINT('Ctrl Pts',(0.605461147890766,54.1707071055754,15.1179645308399));
#51100=CARTESIAN_POINT('Ctrl Pts',(0.516785170310873,54.1823182943499,15.1474599833267));
#51101=CARTESIAN_POINT('Ctrl Pts',(0.343916787107568,54.2045478640552,15.1914614216871));
#51102=CARTESIAN_POINT('Ctrl Pts',(0.260032551484708,54.2151620925175,15.2070720870098));
#51103=CARTESIAN_POINT('Ctrl Pts',(0.0938161801991205,54.2360529814985,
15.2265141889014));
#51104=CARTESIAN_POINT('Ctrl Pts',(0.0115174049717453,54.2463306464609,
15.2307636250779));
#51105=CARTESIAN_POINT('Ctrl Pts',(-0.0783049134808558,54.2575614895967,
15.2293221490236));
#51106=CARTESIAN_POINT('Ctrl Pts',(-0.0858120862299798,54.25850024603,15.22915538111));
#51107=CARTESIAN_POINT('Ctrl Pts',(-0.17502821521666,54.269658490363,15.2266208581259));
#51108=CARTESIAN_POINT('Ctrl Pts',(-0.256683691118636,54.2798906327115,
15.2187874177528));
#51109=CARTESIAN_POINT('Ctrl Pts',(-0.345476748668277,54.29111444431,15.2044954604915));
#51110=CARTESIAN_POINT('Ctrl Pts',(-0.353343031094722,54.2921096211492,
15.2031790943686));
#51111=CARTESIAN_POINT('Ctrl Pts',(-0.423608049976724,54.3010071105924,
15.1909732193392));
#51112=CARTESIAN_POINT('Ctrl Pts',(-0.485548963003283,54.3088688662889,
15.1772294827954));
#51113=CARTESIAN_POINT('Ctrl Pts',(-0.608046839776311,54.324586298138,15.1439180214162));
#51114=CARTESIAN_POINT('Ctrl Pts',(-0.668602551159439,54.3324419655529,
15.1243446958));
#51115=CARTESIAN_POINT('Ctrl Pts',(-0.778230478913236,54.3469472519682,
15.0829453712371));
#51116=CARTESIAN_POINT('Ctrl Pts',(-0.827599995327668,54.3535904692277,
15.0619685912211));
#51117=CARTESIAN_POINT('Ctrl Pts',(-0.950976246159398,54.3705827952107,
15.0033180862864));
#51118=CARTESIAN_POINT('Ctrl Pts',(-1.02383873525204,54.3809722959893,14.9628079756871));
#51119=CARTESIAN_POINT('Ctrl Pts',(-1.16412019588339,54.4018334782146,14.8728024421635));
#51120=CARTESIAN_POINT('Ctrl Pts',(-1.23153866919633,54.4123051632831,14.8233071516301));
#51121=CARTESIAN_POINT('Ctrl Pts',(-1.35968369748512,54.4332789078702,14.7161609033528));
#51122=CARTESIAN_POINT('Ctrl Pts',(-1.42041521979204,54.4437809388632,14.6585166132706));
#51123=CARTESIAN_POINT('Ctrl Pts',(-1.51506550555719,54.4612668319717,14.5563869130981));
#51124=CARTESIAN_POINT('Ctrl Pts',(-1.55114464821752,54.4682489634417,14.5139754319317));
#51125=CARTESIAN_POINT('Ctrl Pts',(-1.62147125016784,54.482594105633,14.4236617534963));
#51126=CARTESIAN_POINT('Ctrl Pts',(-1.65550906414146,54.4899569418111,14.3755861175269));
#51127=CARTESIAN_POINT('Ctrl Pts',(-1.76160584561978,54.514421556358,14.2108807721874));
#51128=CARTESIAN_POINT('Ctrl Pts',(-1.82389696878703,54.5315630777004,14.087480370682));
#51129=CARTESIAN_POINT('Ctrl Pts',(-1.92267203028798,54.5660298041196,13.8291421681136));
#51130=CARTESIAN_POINT('Ctrl Pts',(-1.95901400714649,54.5833555000449,13.6941433984061));
#51131=CARTESIAN_POINT('Ctrl Pts',(-1.98984229918007,54.6077633743642,13.5008599846904));
#51132=CARTESIAN_POINT('Ctrl Pts',(-1.99636526435242,54.6147998337516,13.4447789288554));
#51133=CARTESIAN_POINT('Ctrl Pts',(-2.00694691888882,54.6330408434406,13.2989647806689));
#51134=CARTESIAN_POINT('Ctrl Pts',(-2.00729272169291,54.6442604477564,13.20885705357));
#51135=CARTESIAN_POINT('Ctrl Pts',(-1.99196859307335,54.674595210111,12.966254759167));
#51136=CARTESIAN_POINT('Ctrl Pts',(-1.96495212694323,54.6937563833621,12.8141054799532));
#51137=CARTESIAN_POINT('Ctrl Pts',(-1.87744779962502,54.7322103694805,12.5187919464199));
#51138=CARTESIAN_POINT('Ctrl Pts',(-1.81696027218507,54.7515031833634,12.3756296837104));
#51139=CARTESIAN_POINT('Ctrl Pts',(-1.69954010945417,54.7811954145858,12.1689580027143));
#51140=CARTESIAN_POINT('Ctrl Pts',(-1.65407764507147,54.791551087009,12.0994101835497));
#51141=CARTESIAN_POINT('Ctrl Pts',(-1.50902585055616,54.8218798868502,11.9044555190775));
#51142=CARTESIAN_POINT('Ctrl Pts',(-1.3982346508918,54.8418997417864,11.7867995231772));
#51143=CARTESIAN_POINT('Ctrl Pts',(-1.18973149493884,54.8759202504295,11.6110120890975));
#51144=CARTESIAN_POINT('Ctrl Pts',(-1.09843392202422,54.8898832191871,11.5456933353741));
#51145=CARTESIAN_POINT('Ctrl Pts',(-0.959593076632585,54.9100805965764,
11.4626167398557));
#51146=CARTESIAN_POINT('Ctrl Pts',(-0.916028734927509,54.9162844128338,
11.4386436928017));
#51147=CARTESIAN_POINT('Ctrl Pts',(-0.768957068956217,54.9368373000166,
11.3646436217929));
#51148=CARTESIAN_POINT('Ctrl Pts',(-0.661605311957139,54.9512219289493,
11.3215767122849));
#51149=CARTESIAN_POINT('Ctrl Pts',(-0.495999003212708,54.9728560242593,
11.2703959610723));
#51150=CARTESIAN_POINT('Ctrl Pts',(-0.440040968124541,54.9800760518959,
11.2555729359028));
#51151=CARTESIAN_POINT('Ctrl Pts',(-0.326923092939371,54.9945349639386,
11.2306037560387));
#51152=CARTESIAN_POINT('Ctrl Pts',(-0.269763200048498,55.001773849506,11.2204578986548));
#51153=CARTESIAN_POINT('Ctrl Pts',(-0.0970750496432848,55.0235230128508,
11.1971594092239));
#51154=CARTESIAN_POINT('Ctrl Pts',(0.0196137485806436,55.0380596792661,
11.191162174232));
#51155=CARTESIAN_POINT('Ctrl Pts',(0.168443546981575,55.0566436786176,11.1958270484659));
#51156=CARTESIAN_POINT('Ctrl Pts',(0.200602780793859,55.0606618969659,11.1975685142009));
#51157=CARTESIAN_POINT('Ctrl Pts',(0.264575114192646,55.0686690219848,11.2024978272794));
#51158=CARTESIAN_POINT('Ctrl Pts',(0.296397193709932,55.072658933182,11.2056739484811));
#51159=CARTESIAN_POINT('Ctrl Pts',(0.380623964693239,55.0832492211649,11.2160156172632));
#51160=CARTESIAN_POINT('Ctrl Pts',(0.432920832162374,55.0898554904921,11.2244319236168));
#51161=CARTESIAN_POINT('Ctrl Pts',(0.618413676359414,55.1134677494716,11.261540930968));
#51162=CARTESIAN_POINT('Ctrl Pts',(0.749768860398253,55.130524332922,11.3013299973599));
#51163=CARTESIAN_POINT('Ctrl Pts',(0.968347650589545,55.1600202312374,11.3910724311691));
#51164=CARTESIAN_POINT('Ctrl Pts',(1.05774505411059,55.1724345570082,11.4351879672249));
#51165=CARTESIAN_POINT('Ctrl Pts',(1.18549892263016,55.1908918000413,11.5097053571938));
#51166=CARTESIAN_POINT('Ctrl Pts',(1.22638227727023,55.1969157625829,11.5354312678751));
#51167=CARTESIAN_POINT('Ctrl Pts',(1.29171644184769,55.206760855601,11.5796700588564));
#51168=CARTESIAN_POINT('Ctrl Pts',(1.31668857015409,55.2105785964763,11.5973627140674));
#51169=CARTESIAN_POINT('Ctrl Pts',(1.40526456338941,55.2243333496964,11.6629867641403));
#51170=CARTESIAN_POINT('Ctrl Pts',(1.4667630061718,55.2342899411088,11.7140195135995));
#51171=CARTESIAN_POINT('Ctrl Pts',(1.56724222383337,55.2514051041058,11.8073478064762));
#51172=CARTESIAN_POINT('Ctrl Pts',(1.60765111814264,55.2585536663766,11.8479970395813));
#51173=CARTESIAN_POINT('Ctrl Pts',(1.66181615272736,55.2685602592642,11.9070945871655));
#51174=CARTESIAN_POINT('Ctrl Pts',(1.67696921794576,55.271409807239,11.9241720121809));
#51175=CARTESIAN_POINT('Ctrl Pts',(1.71727003150136,55.279131600391,11.9711047855904));
#51176=CARTESIAN_POINT('Ctrl Pts',(1.74188994587628,55.2840060844735,12.0014384181443));
#51177=CARTESIAN_POINT('Ctrl Pts',(1.8065848918423,55.2972694829167,12.0857520585659));
#51178=CARTESIAN_POINT('Ctrl Pts',(1.84511050502288,55.3056915931741,12.1409711044007));
#51179=CARTESIAN_POINT('Ctrl Pts',(1.93595186696758,55.3270212045074,12.2843722563573));
#51180=CARTESIAN_POINT('Ctrl Pts',(1.98486260872712,55.3399222266209,12.3749086425223));
#51181=CARTESIAN_POINT('Ctrl Pts',(2.06981939645706,55.3657345378285,12.5622729693026));
#51182=CARTESIAN_POINT('Ctrl Pts',(2.10587792485611,55.37864579455,12.6590943828494));
#51183=CARTESIAN_POINT('Ctrl Pts',(2.15349014491728,55.3997321409488,12.8212008163602));
#51184=CARTESIAN_POINT('Ctrl Pts',(2.16918594921391,55.4079207826309,12.8851389193291));
#51185=CARTESIAN_POINT('Ctrl Pts',(2.20276718436149,55.4294576717754,13.055456523819));
#51186=CARTESIAN_POINT('Ctrl Pts',(2.21599272358748,55.4428802470817,13.1628683822018));
#51187=CARTESIAN_POINT('Ctrl Pts',(2.22817911102804,55.4751762881486,13.4220030672915));
#51188=CARTESIAN_POINT('Ctrl Pts',(2.2193936360582,55.4940986489574,13.574391865939));
#51189=CARTESIAN_POINT('Ctrl Pts',(2.17101642313604,55.5323481640879,13.8774680825458));
#51190=CARTESIAN_POINT('Ctrl Pts',(2.13104402819563,55.5516774345543,14.0281115650887));
#51191=CARTESIAN_POINT('Ctrl Pts',(2.02727527647819,55.5882953250669,14.3028298501184));
#51192=CARTESIAN_POINT('Ctrl Pts',(1.96664700474721,55.6055699943675,14.4279898314726));
#51193=CARTESIAN_POINT('Ctrl Pts',(1.8678683021456,55.6293181129264,14.5909387234281));
#51194=CARTESIAN_POINT('Ctrl Pts',(1.83951777143476,55.635779799292,14.6342803451875));
#51195=CARTESIAN_POINT('Ctrl Pts',(1.75150366139421,55.6548565937528,14.759004427163));
#51196=CARTESIAN_POINT('Ctrl Pts',(1.6875562492725,55.6675184735274,14.8376445410234));
#51197=CARTESIAN_POINT('Ctrl Pts',(1.54892405178738,55.6929987854296,14.9866582924729));
#51198=CARTESIAN_POINT('Ctrl Pts',(1.47416437906414,55.7058176847556,15.0569660321525));
#51199=CARTESIAN_POINT('Ctrl Pts',(1.37408466664728,55.722016130923,15.1393251494684));
#51200=CARTESIAN_POINT('Ctrl Pts',(1.35287448981891,55.7253990507332,15.1561677880244));
#51201=CARTESIAN_POINT('Ctrl Pts',(1.26256883969667,55.7396021042372,15.2253432039206));
#51202=CARTESIAN_POINT('Ctrl Pts',(1.19071055364304,55.7503933195221,15.2742371749297));
#51203=CARTESIAN_POINT('Ctrl Pts',(1.06865975664079,55.7680903490432,15.3476607002243));
#51204=CARTESIAN_POINT('Ctrl Pts',(1.02004049247093,55.7749885396146,15.3746024109667));
#51205=CARTESIAN_POINT('Ctrl Pts',(0.883799957013692,55.7939812750692,15.4438491266533));
#51206=CARTESIAN_POINT('Ctrl Pts',(0.794172374943345,55.8061191550956,15.4826152506759));
#51207=CARTESIAN_POINT('Ctrl Pts',(0.666120248972946,55.823082662627,15.5284752501652));
#51208=CARTESIAN_POINT('Ctrl Pts',(0.629658995114581,55.8278720505244,15.5405059382731));
#51209=CARTESIAN_POINT('Ctrl Pts',(0.585625974941044,55.833612963806,15.5537945321524));
#51210=CARTESIAN_POINT('Ctrl Pts',(0.578357476081339,55.834559224075,15.5559480889085));
#51211=CARTESIAN_POINT('Ctrl Pts',(0.407324793040697,55.8567938866377,15.6056873667656));
#51212=CARTESIAN_POINT('Ctrl Pts',(0.237401599318956,55.8781731093593,15.6349311711548));
#51213=CARTESIAN_POINT('Ctrl Pts',(-0.103907242058289,55.9208364668511,
15.6562180332499));
#51214=CARTESIAN_POINT('Ctrl Pts',(-0.275242125909403,55.9421181369697,
15.648747758641));
#51215=CARTESIAN_POINT('Ctrl Pts',(-0.603645192470279,55.9836529641875,
15.5989882287064));
#51216=CARTESIAN_POINT('Ctrl Pts',(-0.760968353342703,56.0038954620483,
15.5587124997302));
#51217=CARTESIAN_POINT('Ctrl Pts',(-0.922015525945914,56.0254597460298,
15.4988425221125));
#51218=CARTESIAN_POINT('Ctrl Pts',(-0.931193005698925,56.0266916328361,
15.4953639618438));
#51219=CARTESIAN_POINT('Ctrl Pts',(-1.00552057873781,56.0366939590796,15.466645674492));
#51220=CARTESIAN_POINT('Ctrl Pts',(-1.06963654225242,56.045480904963,15.4384593514847));
#51221=CARTESIAN_POINT('Ctrl Pts',(-1.25098158552824,56.070889733718,15.34893816718));
#51222=CARTESIAN_POINT('Ctrl Pts',(-1.36511778035346,56.0874951412478,15.2801181361817));
#51223=CARTESIAN_POINT('Ctrl Pts',(-1.58345993447679,56.1210626324979,15.1226711204873));
#51224=CARTESIAN_POINT('Ctrl Pts',(-1.68743798665633,56.1380255455942,15.033697291398));
#51225=CARTESIAN_POINT('Ctrl Pts',(-1.87912994352279,56.1719567677729,14.8397418486595));
#51226=CARTESIAN_POINT('Ctrl Pts',(-1.96692908706153,56.1889245573967,14.7348514382924));
#51227=CARTESIAN_POINT('Ctrl Pts',(-2.07860482722401,56.2131959329734,14.5756209362927));
#51228=CARTESIAN_POINT('Ctrl Pts',(-2.11016737775064,56.2204354673342,14.5269723536886));
#51229=CARTESIAN_POINT('Ctrl Pts',(-2.20918486750619,56.2445761630928,14.3612863809782));
#51230=CARTESIAN_POINT('Ctrl Pts',(-2.26868842527496,56.261550098513,14.2391634980653));
#51231=CARTESIAN_POINT('Ctrl Pts',(-2.36017442714328,56.2932809676468,14.00443926774));
#51232=CARTESIAN_POINT('Ctrl Pts',(-2.39475962923237,56.3078402829316,13.8926888555084));
#51233=CARTESIAN_POINT('Ctrl Pts',(-2.44824801252212,56.3370191898033,13.6638749836948));
#51234=CARTESIAN_POINT('Ctrl Pts',(-2.46703334575657,56.3516384295017,13.5467792574595));
#51235=CARTESIAN_POINT('Ctrl Pts',(-2.4879153038017,56.3809581310081,13.3104745764312));
#51236=CARTESIAN_POINT('Ctrl Pts',(-2.48999639793424,56.3956586714332,13.1912644177639));
#51237=CARTESIAN_POINT('Ctrl Pts',(-2.48034706819867,56.4174897145385,13.0157293520969));
#51238=CARTESIAN_POINT('Ctrl Pts',(-2.47529036441297,56.4245455467382,12.9592240236162));
#51239=CARTESIAN_POINT('Ctrl Pts',(-2.46826046448302,56.4316304354619,12.9028993853228));
#51240=CARTESIAN_POINT('Ctrl Pts',(0.286897399705336,52.3546462541016,10.8159730008272));
#51241=CARTESIAN_POINT('Ctrl Pts',(0.378604545572326,52.366273264052,10.8299117351835));
#51242=CARTESIAN_POINT('Ctrl Pts',(0.46941326367117,52.3777703139944,10.8490035483265));
#51243=CARTESIAN_POINT('Ctrl Pts',(0.558740568487378,52.389208221275,10.8730280161214));
#51244=CARTESIAN_POINT('Ctrl Pts',(0.619668574418693,52.3970097427031,10.8894145277184));
#51245=CARTESIAN_POINT('Ctrl Pts',(0.679906668173053,52.4047836614174,10.9080949961699));
#51246=CARTESIAN_POINT('Ctrl Pts',(0.739263037046509,52.4125512777111,10.9289874100517));
#51247=CARTESIAN_POINT('Ctrl Pts',(0.832526775312518,52.4247561505278,10.9618146307359));
#51248=CARTESIAN_POINT('Ctrl Pts',(0.923624974476453,52.4369502239068,11.0001090003664));
#51249=CARTESIAN_POINT('Ctrl Pts',(1.0118830480884,52.4492374792539,11.0435763649142));
#51250=CARTESIAN_POINT('Ctrl Pts',(1.10141442806073,52.4617020038269,11.087670836643));
#51251=CARTESIAN_POINT('Ctrl Pts',(1.1880363424801,52.4742672637596,11.1370966569693));
#51252=CARTESIAN_POINT('Ctrl Pts',(1.2712048670289,52.4868467571487,11.19139013783));
#51253=CARTESIAN_POINT('Ctrl Pts',(1.31745190903785,52.4938417635213,11.2215808007496));
#51254=CARTESIAN_POINT('Ctrl Pts',(1.36263174845131,52.5008412749167,11.2532772805539));
#51255=CARTESIAN_POINT('Ctrl Pts',(1.40665451137732,52.5078312137426,11.2864057567896));
#51256=CARTESIAN_POINT('Ctrl Pts',(1.48277798855463,52.5199181072795,11.3436910028085));
#51257=CARTESIAN_POINT('Ctrl Pts',(1.55543851145377,52.531973226489,11.4052548403952));
#51258=CARTESIAN_POINT('Ctrl Pts',(1.62411723972848,52.5439090053706,11.4706603829727));
#51259=CARTESIAN_POINT('Ctrl Pts',(1.65458644294996,52.5492042937588,11.4996774428204));
#51260=CARTESIAN_POINT('Ctrl Pts',(1.68427259471252,52.5544761708037,11.5294507960024));
#51261=CARTESIAN_POINT('Ctrl Pts',(1.71313348876987,52.5597173654126,11.5599433789351));
#51262=CARTESIAN_POINT('Ctrl Pts',(1.7131342012995,52.5597174948094,11.5599441317485));
#51263=CARTESIAN_POINT('Ctrl Pts',(1.71313491382864,52.5597176242061,11.5599448845624));
#51264=CARTESIAN_POINT('Ctrl Pts',(1.71313562635727,52.5597177536029,11.5599456373767));
#51265=CARTESIAN_POINT('Ctrl Pts',(1.77093737997985,52.5702146764983,11.6210154470465));
#51266=CARTESIAN_POINT('Ctrl Pts',(1.82547359849269,52.5805903254852,11.6850091277299));
#51267=CARTESIAN_POINT('Ctrl Pts',(1.87646608175138,52.5909392249462,11.7515532965285));
#51268=CARTESIAN_POINT('Ctrl Pts',(1.91162048389922,52.5980737936157,11.7974290868616));
#51269=CARTESIAN_POINT('Ctrl Pts',(1.94509008894011,52.6051955239253,11.8445161270279));
#51270=CARTESIAN_POINT('Ctrl Pts',(1.97677937323057,52.6123336839022,11.8926783920446));
#51271=CARTESIAN_POINT('Ctrl Pts',(1.98769496610871,52.6147924724155,11.9092682169265));
#51272=CARTESIAN_POINT('Ctrl Pts',(1.99839982660474,52.617253371613,11.9259864059183));
#51273=CARTESIAN_POINT('Ctrl Pts',(2.00889043434765,52.6197176754979,11.9428279934674));
#51274=CARTESIAN_POINT('Ctrl Pts',(2.06611700706165,52.6331605254181,12.034699347169));
#51275=CARTESIAN_POINT('Ctrl Pts',(2.11697020498068,52.6467081567378,12.1302489683145));
#51276=CARTESIAN_POINT('Ctrl Pts',(2.1612007237327,52.6602925392306,12.228530179788));
#51277=CARTESIAN_POINT('Ctrl Pts',(2.17484117486492,52.6644818888196,12.2588395702302));
#51278=CARTESIAN_POINT('Ctrl Pts',(2.18785176832704,52.6686747752264,12.2894091277353));
#51279=CARTESIAN_POINT('Ctrl Pts',(2.2002251301063,52.6728693150193,12.3202120767204));
#51280=CARTESIAN_POINT('Ctrl Pts',(2.25218578100817,52.6904838503222,12.4495658697733));
#51281=CARTESIAN_POINT('Ctrl Pts',(2.29312496909258,52.7079624405621,12.5829731053493));
#51282=CARTESIAN_POINT('Ctrl Pts',(2.32233770635006,52.7252560733271,12.718421779341));
#51283=CARTESIAN_POINT('Ctrl Pts',(2.33286794707285,52.7314898649223,12.7672466166078));
#51284=CARTESIAN_POINT('Ctrl Pts',(2.34184912297622,52.7377170578108,12.8163384484872));
#51285=CARTESIAN_POINT('Ctrl Pts',(2.3492445571228,52.7439361194972,12.8655905848478));
#51286=CARTESIAN_POINT('Ctrl Pts',(2.35424968762134,52.7481450969152,12.898923769206));
#51287=CARTESIAN_POINT('Ctrl Pts',(2.358528548211,52.7523503502017,12.9323303676679));
#51288=CARTESIAN_POINT('Ctrl Pts',(2.36207060378534,52.7565514078527,12.9657772649005));
#51289=CARTESIAN_POINT('Ctrl Pts',(2.3629356126977,52.7575773523172,12.9739453649175));
#51290=CARTESIAN_POINT('Ctrl Pts',(2.36375668195591,52.7586030458296,12.9821158624631));
#51291=CARTESIAN_POINT('Ctrl Pts',(2.36453366611607,52.7596284837788,12.9902882932491));
#51292=CARTESIAN_POINT('Ctrl Pts',(2.37188172323651,52.7693262060883,13.067576211469));
#51293=CARTESIAN_POINT('Ctrl Pts',(2.3752920055037,52.7790097070089,13.1451059550479));
#51294=CARTESIAN_POINT('Ctrl Pts',(2.37487726394704,52.7886735986088,13.2224778137936));
#51295=CARTESIAN_POINT('Ctrl Pts',(2.37413425718948,52.8059863965374,13.3610889873552));
#51296=CARTESIAN_POINT('Ctrl Pts',(2.36112302584554,52.8232395554245,13.4992196296424));
#51297=CARTESIAN_POINT('Ctrl Pts',(2.33650449061312,52.8404407532392,13.6348826289493));
#51298=CARTESIAN_POINT('Ctrl Pts',(2.30880269869488,52.8597962509611,13.787536234955));
#51299=CARTESIAN_POINT('Ctrl Pts',(2.26639959314252,52.879086427903,13.9370694808791));
#51300=CARTESIAN_POINT('Ctrl Pts',(2.21021589336869,52.8983129681719,14.080571485906));
#51301=CARTESIAN_POINT('Ctrl Pts',(2.17849703195257,52.9091674325228,14.1615864462719));
#51302=CARTESIAN_POINT('Ctrl Pts',(2.1423853790687,52.9200015916103,14.2406785161887));
#51303=CARTESIAN_POINT('Ctrl Pts',(2.10205519678664,52.930813691901,14.317308941313));
#51304=CARTESIAN_POINT('Ctrl Pts',(2.07500136436392,52.9380665415746,14.3687132881939));
#51305=CARTESIAN_POINT('Ctrl Pts',(2.04604966208516,52.9453094014196,14.4190095405316));
#51306=CARTESIAN_POINT('Ctrl Pts',(2.01525326350672,52.9525419488395,14.4680373158271));
#51307=CARTESIAN_POINT('Ctrl Pts',(2.01218499602166,52.9532625327748,14.4729219885728));
#51308=CARTESIAN_POINT('Ctrl Pts',(2.0090983916613,52.9539830205944,14.4777941129881));
#51309=CARTESIAN_POINT('Ctrl Pts',(2.00599346816136,52.9547034198318,14.4826535828735));
#51310=CARTESIAN_POINT('Ctrl Pts',(1.98586676221557,52.9593731850012,14.514153592918));
#51311=CARTESIAN_POINT('Ctrl Pts',(1.96496839544559,52.9640396745915,14.5451249036443));
#51312=CARTESIAN_POINT('Ctrl Pts',(1.94333277185748,52.9687031081194,14.5755436631792));
#51313=CARTESIAN_POINT('Ctrl Pts',(1.87430998326427,52.9835805709854,14.6725867458569));
#51314=CARTESIAN_POINT('Ctrl Pts',(1.79779191505982,52.9984243439752,14.7639865514538));
#51315=CARTESIAN_POINT('Ctrl Pts',(1.71500292316759,53.0132242563846,14.8488720449154));
#51316=CARTESIAN_POINT('Ctrl Pts',(1.64583799177366,53.0255886408642,14.9197884698823));
#51317=CARTESIAN_POINT('Ctrl Pts',(1.57230333098493,53.0379215660797,14.9861549462414));
#51318=CARTESIAN_POINT('Ctrl Pts',(1.49509560112678,53.0502225028627,15.0475082024516));
#51319=CARTESIAN_POINT('Ctrl Pts',(1.41657636869863,53.0627323916538,15.1099036464497));
#51320=CARTESIAN_POINT('Ctrl Pts',(1.33425890477864,53.0752091530701,15.1671144271994));
#51321=CARTESIAN_POINT('Ctrl Pts',(1.24886044937028,53.0876542281749,15.2186643420193));
#51322=CARTESIAN_POINT('Ctrl Pts',(1.15388791611956,53.1014945289572,15.275993552201));
#51323=CARTESIAN_POINT('Ctrl Pts',(1.05510126433165,53.1152963125072,15.3263271268123));
#51324=CARTESIAN_POINT('Ctrl Pts',(0.953422201694293,53.1290688673279,15.3690181733183));
#51325=CARTESIAN_POINT('Ctrl Pts',(0.913600253053039,53.1344627995348,15.3857378461527));
#51326=CARTESIAN_POINT('Ctrl Pts',(0.873335769951871,53.1398520704015,15.4012842727042));
#51327=CARTESIAN_POINT('Ctrl Pts',(0.832685060509524,53.1452370532317,15.4156166726461));
#51328=CARTESIAN_POINT('Ctrl Pts',(0.791075003150014,53.1507491204876,15.4302873141149));
#51329=CARTESIAN_POINT('Ctrl Pts',(0.749052457409756,53.1562577204812,15.4436884918247));
#51330=CARTESIAN_POINT('Ctrl Pts',(0.706698280387312,53.161762047546,15.4558206545638));
#51331=CARTESIAN_POINT('Ctrl Pts',(0.608132708228648,53.1745715786153,15.4840543175924));
#51332=CARTESIAN_POINT('Ctrl Pts',(0.507777250054708,53.1873570674503,15.505409762825));
#51333=CARTESIAN_POINT('Ctrl Pts',(0.406676257051895,53.2001067683875,15.5199270150308));
#51334=CARTESIAN_POINT('Ctrl Pts',(0.335339323040758,53.2091029666186,15.5301703987195));
#51335=CARTESIAN_POINT('Ctrl Pts',(0.263638041361633,53.2180805540776,15.5370104696948));
#51336=CARTESIAN_POINT('Ctrl Pts',(0.191906243718386,53.2270396901202,15.5404768058473));
#51337=CARTESIAN_POINT('Ctrl Pts',(0.106801154506927,53.2376691194279,15.5445893871179));
#51338=CARTESIAN_POINT('Ctrl Pts',(0.0216491506267357,53.2482730711808,
15.5439538001737));
#51339=CARTESIAN_POINT('Ctrl Pts',(-0.0630107385862956,53.2588537959295,
15.5386149146513));
#51340=CARTESIAN_POINT('Ctrl Pts',(-0.114508583652721,53.2652899551174,
15.5353673188653));
#51341=CARTESIAN_POINT('Ctrl Pts',(-0.165824675143732,53.2717175497265,
15.5303795993431));
#51342=CARTESIAN_POINT('Ctrl Pts',(-0.216852813418056,53.278138981017,15.5236574306784));
#51343=CARTESIAN_POINT('Ctrl Pts',(-0.287558469935319,53.2870366506269,
15.5143430530678));
#51344=CARTESIAN_POINT('Ctrl Pts',(-0.357702850727178,53.2959214332314,
15.5016988676326));
#51345=CARTESIAN_POINT('Ctrl Pts',(-0.426950888544439,53.3047932471048,
15.4857425202606));
#51346=CARTESIAN_POINT('Ctrl Pts',(-0.471181986881598,53.3104599791052,
15.4755506535744));
#51347=CARTESIAN_POINT('Ctrl Pts',(-0.515047377913757,53.3161214201456,
15.4640074957561));
#51348=CARTESIAN_POINT('Ctrl Pts',(-0.558459593907759,53.3217775493788,
15.4511177477559));
#51349=CARTESIAN_POINT('Ctrl Pts',(-0.583013376677091,53.3249766343673,
15.4438273557522));
#51350=CARTESIAN_POINT('Ctrl Pts',(-0.607420694881155,53.3281738270904,
15.4361066036092));
#51351=CARTESIAN_POINT('Ctrl Pts',(-0.63166339466273,53.3313688080905,15.4279574015993));
#51352=CARTESIAN_POINT('Ctrl Pts',(-0.666425076872119,53.33595010123,15.4162722356285));
#51353=CARTESIAN_POINT('Ctrl Pts',(-0.700865438636589,53.3405291103146,
15.4037002662725));
#51354=CARTESIAN_POINT('Ctrl Pts',(-0.734940871487638,53.3451046241908,
15.3902736918485));
#51355=CARTESIAN_POINT('Ctrl Pts',(-0.815017811682377,53.3558570378908,
15.3587213708003));
#51356=CARTESIAN_POINT('Ctrl Pts',(-0.893067261237862,53.3665885123108,
15.3224546218366));
#51357=CARTESIAN_POINT('Ctrl Pts',(-0.968688727694473,53.3772595662987,
15.281965743812));
#51358=CARTESIAN_POINT('Ctrl Pts',(-1.00974331905814,53.3830528387837,15.2599844940432));
#51359=CARTESIAN_POINT('Ctrl Pts',(-1.05008317632462,53.3888284125057,15.2367586482058));
#51360=CARTESIAN_POINT('Ctrl Pts',(-1.08965021009618,53.3945807528981,15.2123647107976));
#51361=CARTESIAN_POINT('Ctrl Pts',(-1.15120498421712,53.4035297182302,15.1744148529499));
#51362=CARTESIAN_POINT('Ctrl Pts',(-1.21082688378749,53.4124647514594,15.1335317623874));
#51363=CARTESIAN_POINT('Ctrl Pts',(-1.26819795552164,53.421416990598,15.0898744137285));
#51364=CARTESIAN_POINT('Ctrl Pts',(-1.34233226310685,53.4329849817443,15.0334608377572));
#51365=CARTESIAN_POINT('Ctrl Pts',(-1.41271035693283,53.4445822067216,14.9724115105954));
#51366=CARTESIAN_POINT('Ctrl Pts',(-1.47880049445705,53.4561712566132,14.907331404647));
#51367=CARTESIAN_POINT('Ctrl Pts',(-1.50721428041528,53.4611536760092,14.8793518562632));
#51368=CARTESIAN_POINT('Ctrl Pts',(-1.53483606346469,53.4661346659615,14.8506269439165));
#51369=CARTESIAN_POINT('Ctrl Pts',(-1.56162593402063,53.4711116247684,14.8212029673402));
#51370=CARTESIAN_POINT('Ctrl Pts',(-1.57469113672623,53.4735388472342,14.8068531324811));
#51371=CARTESIAN_POINT('Ctrl Pts',(-1.58755822840402,53.4759650578836,14.7923373233404));
#51372=CARTESIAN_POINT('Ctrl Pts',(-1.60022243656977,53.478389924412,14.7776611398467));
#51373=CARTESIAN_POINT('Ctrl Pts',(-1.63324791992227,53.4847134456395,14.7393888651568));
#51374=CARTESIAN_POINT('Ctrl Pts',(-1.66489365639477,53.4910279397085,14.7000259269526));
#51375=CARTESIAN_POINT('Ctrl Pts',(-1.69510025535646,53.4973261597594,14.6596621725213));
#51376=CARTESIAN_POINT('Ctrl Pts',(-1.72025473141081,53.5025709880718,14.626049348529));
#51377=CARTESIAN_POINT('Ctrl Pts',(-1.74441120426201,53.5078044085106,14.5917424672605));
#51378=CARTESIAN_POINT('Ctrl Pts',(-1.76752626686844,53.5130197475694,14.5568082706509));
#51379=CARTESIAN_POINT('Ctrl Pts',(-1.76753172518083,53.5130209791019,14.5568000214083));
#51380=CARTESIAN_POINT('Ctrl Pts',(-1.76753718343626,53.5130222106335,14.5567917721293));
#51381=CARTESIAN_POINT('Ctrl Pts',(-1.76754264163471,53.5130234421644,14.5567835228138));
#51382=CARTESIAN_POINT('Ctrl Pts',(-1.79994554156808,53.5203344938398,14.5078110007303));
#51383=CARTESIAN_POINT('Ctrl Pts',(-1.83034051010383,53.527617509957,14.4575510638308));
#51384=CARTESIAN_POINT('Ctrl Pts',(-1.8585993480451,53.5348876682701,14.4061925809449));
#51385=CARTESIAN_POINT('Ctrl Pts',(-1.88277887985237,53.5411083424727,14.3622479547331));
#51386=CARTESIAN_POINT('Ctrl Pts',(-1.90539461130247,53.5473201288166,14.3174991724067));
#51387=CARTESIAN_POINT('Ctrl Pts',(-1.92647365191702,53.5535208525157,14.2720316941406));
#51388=CARTESIAN_POINT('Ctrl Pts',(-1.94753705207156,53.5597169753331,14.2265979523375));
#51389=CARTESIAN_POINT('Ctrl Pts',(-1.96706590250326,53.5659011887381,14.1804465192646));
#51390=CARTESIAN_POINT('Ctrl Pts',(-1.98486750734344,53.5720962182315,14.1337424961699));
#51391=CARTESIAN_POINT('Ctrl Pts',(-2.01310453648316,53.5819228170071,14.0596602506135));
#51392=CARTESIAN_POINT('Ctrl Pts',(-2.03699332425505,53.5917802249531,13.9841826632899));
#51393=CARTESIAN_POINT('Ctrl Pts',(-2.05656808333809,53.6016504734671,13.9077925559741));
#51394=CARTESIAN_POINT('Ctrl Pts',(-2.06538702068936,53.606097276767,13.8733768286685));
#51395=CARTESIAN_POINT('Ctrl Pts',(-2.07333014721432,53.6105467503804,13.8387751935792));
#51396=CARTESIAN_POINT('Ctrl Pts',(-2.08039942415651,53.6149975654674,13.8040285817165));
#51397=CARTESIAN_POINT('Ctrl Pts',(-2.09572783431339,53.6246483288685,13.7286870266254));
#51398=CARTESIAN_POINT('Ctrl Pts',(-2.10695004179422,53.6343045627027,13.6526660854498));
#51399=CARTESIAN_POINT('Ctrl Pts',(-2.11410726864506,53.6439395872891,13.5764221390983));
#51400=CARTESIAN_POINT('Ctrl Pts',(-2.11770578382013,53.6487838912226,13.5380881581207));
#51401=CARTESIAN_POINT('Ctrl Pts',(-2.12027678461537,53.6536229360829,13.4996969874888));
#51402=CARTESIAN_POINT('Ctrl Pts',(-2.12182529008515,53.6584539546973,13.4613016906794));
#51403=CARTESIAN_POINT('Ctrl Pts',(-2.12479825068366,53.6677289803731,13.3875869335736));
#51404=CARTESIAN_POINT('Ctrl Pts',(-2.12400355021684,53.6769730620142,13.3138636726511));
#51405=CARTESIAN_POINT('Ctrl Pts',(-2.11948894684724,53.6861613022635,13.2405350020391));
#51406=CARTESIAN_POINT('Ctrl Pts',(-2.11867825173027,53.6878112504193,13.2273672461296));
#51407=CARTESIAN_POINT('Ctrl Pts',(-2.11774762931345,53.6894594143941,13.2142120817822));
#51408=CARTESIAN_POINT('Ctrl Pts',(-2.11669738116017,53.6911056716687,13.201071667521));
#51409=CARTESIAN_POINT('Ctrl Pts',(-2.11669666944272,53.6911067872812,13.2010627627093));
#51410=CARTESIAN_POINT('Ctrl Pts',(-2.11669595767028,53.691107902893,13.201053857904));
#51411=CARTESIAN_POINT('Ctrl Pts',(-2.11669524584283,53.6911090185039,13.201044953105));
#51412=CARTESIAN_POINT('Ctrl Pts',(-2.11084161280211,53.7002831194977,13.1278173393418));
#51413=CARTESIAN_POINT('Ctrl Pts',(-2.10126801495813,53.7094026193869,13.0550147556555));
#51414=CARTESIAN_POINT('Ctrl Pts',(-2.08801392842047,53.7184963324333,12.9829836038374));
#51415=CARTESIAN_POINT('Ctrl Pts',(-2.07475984188281,53.7275900454798,12.9109524520193));
#51416=CARTESIAN_POINT('Ctrl Pts',(-2.05782432908718,53.7366579745326,12.8396929553331));
#51417=CARTESIAN_POINT('Ctrl Pts',(-2.03726016858693,53.7457218987084,12.769606170018));
#51418=CARTESIAN_POINT('Ctrl Pts',(-2.02874434142801,53.7494753615187,12.7405825223052));
#51419=CARTESIAN_POINT('Ctrl Pts',(-2.01960546756002,53.7532284872154,12.7117575053214));
#51420=CARTESIAN_POINT('Ctrl Pts',(-2.00984647418317,53.7569830676624,12.6831574839871));
#51421=CARTESIAN_POINT('Ctrl Pts',(-1.97716131346694,53.7695580393416,12.5873692958306));
#51422=CARTESIAN_POINT('Ctrl Pts',(-1.93752131365257,53.7821490605221,12.494099342539));
#51423=CARTESIAN_POINT('Ctrl Pts',(-1.89151142633677,53.7947329481063,12.404322229798));
#51424=CARTESIAN_POINT('Ctrl Pts',(-1.87157864015484,53.8001846445826,12.3654282420772));
#51425=CARTESIAN_POINT('Ctrl Pts',(-1.85045034272277,53.8056350850442,12.3271891462092));
#51426=CARTESIAN_POINT('Ctrl Pts',(-1.82817385043466,53.8110827658278,12.2896811929973));
#51427=CARTESIAN_POINT('Ctrl Pts',(-1.77544770939433,53.8239768598184,12.2009037676465));
#51428=CARTESIAN_POINT('Ctrl Pts',(-1.71629124316072,53.8368545379083,12.1162262276396));
#51429=CARTESIAN_POINT('Ctrl Pts',(-1.65131768918288,53.8497001526603,12.0367107283857));
#51430=CARTESIAN_POINT('Ctrl Pts',(-1.62547657818727,53.8548090767732,12.0050860331629));
#51431=CARTESIAN_POINT('Ctrl Pts',(-1.59871560076123,53.8599129587562,11.974277362838));
#51432=CARTESIAN_POINT('Ctrl Pts',(-1.57107423804931,53.8650109319293,11.9443494144863));
#51433=CARTESIAN_POINT('Ctrl Pts',(-1.57107126173674,53.8650114808588,11.9443461919633));
#51434=CARTESIAN_POINT('Ctrl Pts',(-1.57106828541389,53.8650120297884,11.9443429694505));
#51435=CARTESIAN_POINT('Ctrl Pts',(-1.57106530908085,53.8650125787178,11.944339746948));
#51436=CARTESIAN_POINT('Ctrl Pts',(-1.56919139572923,53.8653581872944,11.9423108441458));
#51437=CARTESIAN_POINT('Ctrl Pts',(-1.56731342907328,53.8657037692991,11.9402860230933));
#51438=CARTESIAN_POINT('Ctrl Pts',(-1.56543142240293,53.8660493257425,11.9382653056425));
#51439=CARTESIAN_POINT('Ctrl Pts',(-1.514776842156,53.8753500454827,11.8838772974168));
#51440=CARTESIAN_POINT('Ctrl Pts',(-1.46119442488989,53.8846325486842,11.8324655478395));
#51441=CARTESIAN_POINT('Ctrl Pts',(-1.4051361512904,53.8938900984857,11.7841100430016));
#51442=CARTESIAN_POINT('Ctrl Pts',(-1.36898430674358,53.8998602698773,11.7529256953286));
#51443=CARTESIAN_POINT('Ctrl Pts',(-1.33180186061339,53.9058201818434,11.7230118660596));
#51444=CARTESIAN_POINT('Ctrl Pts',(-1.29369935058448,53.9117693222334,11.6943859268918));
#51445=CARTESIAN_POINT('Ctrl Pts',(-1.21962533799752,53.923334877883,11.6387350478125));
#51446=CARTESIAN_POINT('Ctrl Pts',(-1.14201854121693,53.9348676699908,11.5880125932902));
#51447=CARTESIAN_POINT('Ctrl Pts',(-1.06155834882649,53.9463802354961,11.5426610760724));
#51448=CARTESIAN_POINT('Ctrl Pts',(-1.03502675166717,53.9501764823255,11.5277064985398));
#51449=CARTESIAN_POINT('Ctrl Pts',(-1.00818516350613,53.953970483159,11.5133362450871));
#51450=CARTESIAN_POINT('Ctrl Pts',(-0.98105881327435,53.9577625495424,11.4995670617175));
#51451=CARTESIAN_POINT('Ctrl Pts',(-0.899330135635023,53.9691876239953,
11.4580820429312));
#51452=CARTESIAN_POINT('Ctrl Pts',(-0.815015032667117,53.9805951916943,
11.422055145314));
#51453=CARTESIAN_POINT('Ctrl Pts',(-0.728915015204727,53.9919791178223,
11.3918916048773));
#51454=CARTESIAN_POINT('Ctrl Pts',(-0.666116891336237,54.0002821266273,
11.3698914496568));
#51455=CARTESIAN_POINT('Ctrl Pts',(-0.602366337967937,54.0085729746407,
11.3510094364104));
#51456=CARTESIAN_POINT('Ctrl Pts',(-0.537994295480503,54.0168471244047,
11.3353972583123));
#51457=CARTESIAN_POINT('Ctrl Pts',(-0.537978733718646,54.0168491246574,
11.3353934841118));
#51458=CARTESIAN_POINT('Ctrl Pts',(-0.537963171919938,54.0168511249091,
11.3353897100994));
#51459=CARTESIAN_POINT('Ctrl Pts',(-0.537947610084269,54.0168531251599,
11.3353859362753));
#51460=CARTESIAN_POINT('Ctrl Pts',(-0.418471797387094,54.0322100276408,
11.3064124448631));
#51461=CARTESIAN_POINT('Ctrl Pts',(-0.296820149650447,54.0475135210664,
11.2885263070439));
#51462=CARTESIAN_POINT('Ctrl Pts',(-0.174817987250954,54.0627784164899,
11.2814679421645));
#51463=CARTESIAN_POINT('Ctrl Pts',(-0.12956541297104,54.0684404129697,11.2788498805275));
#51464=CARTESIAN_POINT('Ctrl Pts',(-0.0842647042719535,54.0740970713534,
11.2777220117312));
#51465=CARTESIAN_POINT('Ctrl Pts',(-0.0390095089471808,54.0797490490657,
11.2780728087121));
#51466=CARTESIAN_POINT('Ctrl Pts',(0.0320295530716223,54.0886212060049,
11.2786234700958));
#51467=CARTESIAN_POINT('Ctrl Pts',(0.103004028875918,54.097489027784,11.2830798353659));
#51468=CARTESIAN_POINT('Ctrl Pts',(0.173464121690939,54.1063436422542,11.291277655428));
#51469=CARTESIAN_POINT('Ctrl Pts',(0.244046248390177,54.1152135925401,11.2994896737657));
#51470=CARTESIAN_POINT('Ctrl Pts',(0.314112023364961,54.1240702865772,11.3114552314023));
#51471=CARTESIAN_POINT('Ctrl Pts',(0.383259896863854,54.1329111150333,11.3269979817466));
#51472=CARTESIAN_POINT('Ctrl Pts',(0.427669540820878,54.1385890632355,11.3369801832804));
#51473=CARTESIAN_POINT('Ctrl Pts',(0.471701620791059,54.1442605950328,11.3484376963137));
#51474=CARTESIAN_POINT('Ctrl Pts',(0.51526103274021,54.14992639429,11.3613239412686));
#51475=CARTESIAN_POINT('Ctrl Pts',(0.556277498627599,54.1552614310033,11.3734579027468));
#51476=CARTESIAN_POINT('Ctrl Pts',(0.596880229991585,54.1605918796447,11.3868250567179));
#51477=CARTESIAN_POINT('Ctrl Pts',(0.636970441946457,54.165916285565,11.401479821767));
#51478=CARTESIAN_POINT('Ctrl Pts',(0.636982682653804,54.165917911261,11.4014842962929));
#51479=CARTESIAN_POINT('Ctrl Pts',(0.636994923314774,54.1659195369565,11.4014887709393));
#51480=CARTESIAN_POINT('Ctrl Pts',(0.637007163929467,54.1659211626517,11.4014932457064));
#51481=CARTESIAN_POINT('Ctrl Pts',(0.738398353557972,54.1793870852429,11.4385585372037));
#51482=CARTESIAN_POINT('Ctrl Pts',(0.83660966707235,54.1928275875312,11.4838997993307));
#51483=CARTESIAN_POINT('Ctrl Pts',(0.930414541120341,54.2062363306581,11.5366246031919));
#51484=CARTESIAN_POINT('Ctrl Pts',(1.03306360519614,54.2209092881817,11.594320451354));
#51485=CARTESIAN_POINT('Ctrl Pts',(1.13043985693448,54.2355445307112,11.6608551719195));
#51486=CARTESIAN_POINT('Ctrl Pts',(1.22101709910568,54.2501438905498,11.7350820030085));
#51487=CARTESIAN_POINT('Ctrl Pts',(1.28576061236064,54.2605793357518,11.7881384408873));
#51488=CARTESIAN_POINT('Ctrl Pts',(1.34703310260344,54.2709968101427,11.8451265234236));
#51489=CARTESIAN_POINT('Ctrl Pts',(1.40428453585257,54.2813987634094,11.9056414349209));
#51490=CARTESIAN_POINT('Ctrl Pts',(1.44154360268005,54.2881683244475,11.9450243639338));
#51491=CARTESIAN_POINT('Ctrl Pts',(1.47710198632334,54.2949318149268,11.9859043278642));
#51492=CARTESIAN_POINT('Ctrl Pts',(1.51079846717546,54.3016883029445,12.0281608435957));
#51493=CARTESIAN_POINT('Ctrl Pts',(1.52887923112574,54.3053136804882,12.0508347272472));
#51494=CARTESIAN_POINT('Ctrl Pts',(1.54642332042148,54.3089369194602,12.0739041582257));
#51495=CARTESIAN_POINT('Ctrl Pts',(1.56340511917397,54.3125576318131,12.0973485954084));
#51496=CARTESIAN_POINT('Ctrl Pts',(1.56341365864612,54.3125594525255,12.0973603846847));
#51497=CARTESIAN_POINT('Ctrl Pts',(1.56342219797969,54.3125612732381,12.0973721740608));
#51498=CARTESIAN_POINT('Ctrl Pts',(1.56343073717471,54.3125630939508,12.0973839635368));
#51499=CARTESIAN_POINT('Ctrl Pts',(1.60414875847956,54.3212449215193,12.1536005193228));
#51500=CARTESIAN_POINT('Ctrl Pts',(1.64171168012391,54.3299293102567,12.2120857444096));
#51501=CARTESIAN_POINT('Ctrl Pts',(1.67607898341393,54.3386175999711,12.2723487961211));
#51502=CARTESIAN_POINT('Ctrl Pts',(1.6971750047835,54.3439508186974,12.3093406606258));
#51503=CARTESIAN_POINT('Ctrl Pts',(1.71706799479513,54.3492856053713,12.347002490196));
#51504=CARTESIAN_POINT('Ctrl Pts',(1.73575785935933,54.3546231997247,12.3852233581526));
#51505=CARTESIAN_POINT('Ctrl Pts',(1.76142165479252,54.3619524625515,12.4377059501558));
#51506=CARTESIAN_POINT('Ctrl Pts',(1.78490977422095,54.3693010491427,12.4911998775491));
#51507=CARTESIAN_POINT('Ctrl Pts',(1.80606354150889,54.3766506970259,12.54555450817));
#51508=CARTESIAN_POINT('Ctrl Pts',(1.82704768297592,54.3839414102503,12.599473285039));
#51509=CARTESIAN_POINT('Ctrl Pts',(1.84573402483613,54.3912331563084,12.6542391567784));
#51510=CARTESIAN_POINT('Ctrl Pts',(1.86195192454017,54.3985016771668,12.7096572714523));
#51511=CARTESIAN_POINT('Ctrl Pts',(1.88236246291403,54.407649250318,12.7794020335238));
#51512=CARTESIAN_POINT('Ctrl Pts',(1.89886396325648,54.4167604367007,12.8501851518565));
#51513=CARTESIAN_POINT('Ctrl Pts',(1.91126977912049,54.4258110530799,12.921567490084));
#51514=CARTESIAN_POINT('Ctrl Pts',(1.92317449250243,54.434496092025,12.990066513965));
#51515=CARTESIAN_POINT('Ctrl Pts',(1.93130616693919,54.44312573541,13.0591253496143));
#51516=CARTESIAN_POINT('Ctrl Pts',(1.93572931569931,54.4517206464745,13.1283203272785));
#51517=CARTESIAN_POINT('Ctrl Pts',(1.9386919849011,54.4574776037202,13.1746678141848));
#51518=CARTESIAN_POINT('Ctrl Pts',(1.9399909490566,54.4632191137398,13.2210774921035));
#51519=CARTESIAN_POINT('Ctrl Pts',(1.93964393421203,54.4689530231657,13.2674349060169));
#51520=CARTESIAN_POINT('Ctrl Pts',(1.93913709339929,54.4773278214175,13.3351433332291));
#51521=CARTESIAN_POINT('Ctrl Pts',(1.93512117200686,54.4856868461961,13.4027379628502));
#51522=CARTESIAN_POINT('Ctrl Pts',(1.92766189460317,54.4940511799848,13.4698207365016));
#51523=CARTESIAN_POINT('Ctrl Pts',(1.9226554375866,54.49966508537,13.5148448058131));
#51524=CARTESIAN_POINT('Ctrl Pts',(1.91609819964657,54.5052815165365,13.5596393322053));
#51525=CARTESIAN_POINT('Ctrl Pts',(1.90801160717522,54.510908482447,13.6040969579081));
#51526=CARTESIAN_POINT('Ctrl Pts',(1.89950815886185,54.5168255128836,13.6508463302349));
#51527=CARTESIAN_POINT('Ctrl Pts',(1.88931363287462,54.5227535003215,13.6972182478163));
#51528=CARTESIAN_POINT('Ctrl Pts',(1.87745482154452,54.5286995303713,13.7430796443201));
#51529=CARTESIAN_POINT('Ctrl Pts',(1.87745390524781,54.5286999898042,13.7430831879001));
#51530=CARTESIAN_POINT('Ctrl Pts',(1.87745298894106,54.5287004492373,13.7430867314775));
#51531=CARTESIAN_POINT('Ctrl Pts',(1.87745207262426,54.5287009086705,13.7430902750522));
#51532=CARTESIAN_POINT('Ctrl Pts',(1.8628892767985,54.5360025666133,13.7994074304433));
#51533=CARTESIAN_POINT('Ctrl Pts',(1.84578665227882,54.543345664524,13.8550660333931));
#51534=CARTESIAN_POINT('Ctrl Pts',(1.82617215597624,54.5506964228564,13.9098241588855));
#51535=CARTESIAN_POINT('Ctrl Pts',(1.81753531532175,54.553933178337,13.9339357749638));
#51536=CARTESIAN_POINT('Ctrl Pts',(1.80841181690004,54.5571713405063,13.9578722294145));
#51537=CARTESIAN_POINT('Ctrl Pts',(1.79880597984343,54.5604076548173,13.9816103365177));
#51538=CARTESIAN_POINT('Ctrl Pts',(1.76115590409911,54.5730923878837,14.0746518408859));
#51539=CARTESIAN_POINT('Ctrl Pts',(1.71607964918136,54.5857501826966,14.1646657427447));
#51540=CARTESIAN_POINT('Ctrl Pts',(1.66435797001852,54.598350653071,14.2506283426667));
#51541=CARTESIAN_POINT('Ctrl Pts',(1.61168717432495,54.6111823478549,14.3381683957173));
#51542=CARTESIAN_POINT('Ctrl Pts',(1.55212566300802,54.6239543178497,14.4215061875728));
#51543=CARTESIAN_POINT('Ctrl Pts',(1.48654463182221,54.6366428235215,14.4995805360594));
#51544=CARTESIAN_POINT('Ctrl Pts',(1.42169839649399,54.6491891621484,14.5767801086113));
#51545=CARTESIAN_POINT('Ctrl Pts',(1.35096774966186,54.6616535771729,14.6488328300364));
#51546=CARTESIAN_POINT('Ctrl Pts',(1.27522614131539,54.6740255661475,14.7147439947356));
#51547=CARTESIAN_POINT('Ctrl Pts',(1.235482709428,54.6805174444143,14.7493291579244));
#51548=CARTESIAN_POINT('Ctrl Pts',(1.19436001237438,54.6869841095851,14.7822239216797));
#51549=CARTESIAN_POINT('Ctrl Pts',(1.15198645237769,54.6934259532847,14.8132889771581));
#51550=CARTESIAN_POINT('Ctrl Pts',(1.1045291109289,54.7006406592484,14.8480810726317));
#51551=CARTESIAN_POINT('Ctrl Pts',(1.05549789251919,54.7078251990735,14.8805815184628));
#51552=CARTESIAN_POINT('Ctrl Pts',(1.00517136700043,54.715021033663,14.9106936329748));
#51553=CARTESIAN_POINT('Ctrl Pts',(0.979758885777928,54.7186545849463,14.9258988063246));
#51554=CARTESIAN_POINT('Ctrl Pts',(0.954015563949888,54.7222911175633,14.9404956120231));
#51555=CARTESIAN_POINT('Ctrl Pts',(0.927973476651595,54.7259365878508,14.9544748801754));
#51556=CARTESIAN_POINT('Ctrl Pts',(0.893796745032809,54.7307207765456,14.9728207865691));
#51557=CARTESIAN_POINT('Ctrl Pts',(0.859108679011762,54.735519788836,14.9901008160229));
#51558=CARTESIAN_POINT('Ctrl Pts',(0.823979210983868,54.7403413047258,15.0062811231433));
#51559=CARTESIAN_POINT('Ctrl Pts',(0.779141519510945,54.7464952732894,15.0269329479312));
#51560=CARTESIAN_POINT('Ctrl Pts',(0.733494641480898,54.7526971847942,15.0458314250729));
#51561=CARTESIAN_POINT('Ctrl Pts',(0.68717595580574,54.7589200776843,15.0629043571269));
#51562=CARTESIAN_POINT('Ctrl Pts',(0.621138160611772,54.7677922233465,15.0872456952696));
#51563=CARTESIAN_POINT('Ctrl Pts',(0.553739777889215,54.7767067860648,15.1078753309841));
#51564=CARTESIAN_POINT('Ctrl Pts',(0.485420860759286,54.7856209161682,15.1247012912355));
#51565=CARTESIAN_POINT('Ctrl Pts',(0.452329342757525,54.7899386382455,15.1328512530608));
#51566=CARTESIAN_POINT('Ctrl Pts',(0.41902263846378,54.7942561695393,15.1401088905563));
#51567=CARTESIAN_POINT('Ctrl Pts',(0.385555037498852,54.7985681399962,15.1464645876144));
#51568=CARTESIAN_POINT('Ctrl Pts',(0.315694081238318,54.8075690355132,15.1597315999303));
#51569=CARTESIAN_POINT('Ctrl Pts',(0.245123721470782,54.8165460827816,15.1690684576352));
#51570=CARTESIAN_POINT('Ctrl Pts',(0.174308308039462,54.825453119872,15.1743969078876));
#51571=CARTESIAN_POINT('Ctrl Pts',(0.0811955562954068,54.8371646766248,
15.1814031038764));
#51572=CARTESIAN_POINT('Ctrl Pts',(-0.0123431206148276,54.8487535530874,
15.1814778415116));
#51573=CARTESIAN_POINT('Ctrl Pts',(-0.105269596113297,54.8602467086059,
15.1747487460213));
#51574=CARTESIAN_POINT('Ctrl Pts',(-0.117388982246299,54.8617456354604,
15.1738711435282));
#51575=CARTESIAN_POINT('Ctrl Pts',(-0.129498009966489,54.8632429406556,
15.1728777664557));
#51576=CARTESIAN_POINT('Ctrl Pts',(-0.141594422119124,54.8647386897927,
15.1717688530728));
#51577=CARTESIAN_POINT('Ctrl Pts',(-0.210698118429061,54.8732835205096,
15.1654339156816));
#51578=CARTESIAN_POINT('Ctrl Pts',(-0.279387638366443,54.8817780342576,
15.1553310248002));
#51579=CARTESIAN_POINT('Ctrl Pts',(-0.347233554303374,54.8902407042179,
15.1415196819552));
#51580=CARTESIAN_POINT('Ctrl Pts',(-0.404438769885582,54.8973761205918,
15.1298744585984));
#51581=CARTESIAN_POINT('Ctrl Pts',(-0.461046174909015,54.9044895283375,
15.1155926501386));
#51582=CARTESIAN_POINT('Ctrl Pts',(-0.516811919155424,54.9116423589655,
15.0988271178759));
#51583=CARTESIAN_POINT('Ctrl Pts',(-0.558034649440151,54.9169298201433,
15.0864338283416));
#51584=CARTESIAN_POINT('Ctrl Pts',(-0.598798584235844,54.9222389603687,
15.0726833773101));
#51585=CARTESIAN_POINT('Ctrl Pts',(-0.639022928620526,54.9275968903586,
15.0576333803174));
#51586=CARTESIAN_POINT('Ctrl Pts',(-0.691423284760062,54.9345766794376,
15.038027710806));
#51587=CARTESIAN_POINT('Ctrl Pts',(-0.742858689603912,54.94156918436,15.0160690950034));
#51588=CARTESIAN_POINT('Ctrl Pts',(-0.79304668132035,54.9485513112826,14.9917571192118));
#51589=CARTESIAN_POINT('Ctrl Pts',(-0.793050137497275,54.9485517921041,
14.9917554449768));
#51590=CARTESIAN_POINT('Ctrl Pts',(-0.793053593668232,54.9485522729256,
14.9917537707307));
#51591=CARTESIAN_POINT('Ctrl Pts',(-0.793057049833323,54.948552753747,14.9917520964735));
#51592=CARTESIAN_POINT('Ctrl Pts',(-0.843325930740229,54.9555461564257,
14.967400528705));
#51593=CARTESIAN_POINT('Ctrl Pts',(-0.892436597767239,54.9625420879354,
14.9406429966578));
#51594=CARTESIAN_POINT('Ctrl Pts',(-0.940209835462784,54.9695356076179,
14.9116696924882));
#51595=CARTESIAN_POINT('Ctrl Pts',(-0.99948060200036,54.9782122494444,14.875723417333));
#51596=CARTESIAN_POINT('Ctrl Pts',(-1.05669633444349,54.986885757279,14.8363641429508));
#51597=CARTESIAN_POINT('Ctrl Pts',(-1.11154495611551,54.9955493130894,14.7939676217205));
#51598=CARTESIAN_POINT('Ctrl Pts',(-1.18011836431855,55.0063807529865,14.7409622066692));
#51599=CARTESIAN_POINT('Ctrl Pts',(-1.24507317015746,55.0172647628307,14.6833216989991));
#51600=CARTESIAN_POINT('Ctrl Pts',(-1.30585067138259,55.0281499189929,14.6216377858003));
#51601=CARTESIAN_POINT('Ctrl Pts',(-1.32326904095905,55.0312695219563,14.6039596454464));
#51602=CARTESIAN_POINT('Ctrl Pts',(-1.34034407033215,55.0343891732573,14.5859496246742));
#51603=CARTESIAN_POINT('Ctrl Pts',(-1.35706209430618,55.0375075526115,14.5676222358385));
#51604=CARTESIAN_POINT('Ctrl Pts',(-1.4148722599396,55.0482907664203,14.5042469597972));
#51605=CARTESIAN_POINT('Ctrl Pts',(-1.46834378222509,55.0590039229693,14.436999571369));
#51606=CARTESIAN_POINT('Ctrl Pts',(-1.51691811043868,55.0695959792902,14.3664663840971));
#51607=CARTESIAN_POINT('Ctrl Pts',(-1.53174347091961,55.0728287785684,14.344938964869));
#51608=CARTESIAN_POINT('Ctrl Pts',(-1.54611232790725,55.0760502512918,14.323105646365));
#51609=CARTESIAN_POINT('Ctrl Pts',(-1.56000801185874,55.0792588263726,14.3009836527408));
#51610=CARTESIAN_POINT('Ctrl Pts',(-1.56785142348161,55.0810699049182,14.2884969048758));
#51611=CARTESIAN_POINT('Ctrl Pts',(-1.57554417590168,55.08287693321,14.275918244921));
#51612=CARTESIAN_POINT('Ctrl Pts',(-1.58311073051578,55.0846979624443,14.2632682439016));
#51613=CARTESIAN_POINT('Ctrl Pts',(-1.62534322423445,55.0948619815549,14.1926626491703));
#51614=CARTESIAN_POINT('Ctrl Pts',(-1.66310508793709,55.1050900365467,14.1194240766291));
#51615=CARTESIAN_POINT('Ctrl Pts',(-1.69586650256542,55.1153377196764,14.0440500537282));
#51616=CARTESIAN_POINT('Ctrl Pts',(-1.70752168791717,55.1189834305731,14.0172350270395));
#51617=CARTESIAN_POINT('Ctrl Pts',(-1.71854371166593,55.1226315743923,13.9901501189781));
#51618=CARTESIAN_POINT('Ctrl Pts',(-1.72890790254973,55.1262799825131,13.9628190815204));
#51619=CARTESIAN_POINT('Ctrl Pts',(-1.75333580604556,55.1348791064089,13.8984011300426));
#51620=CARTESIAN_POINT('Ctrl Pts',(-1.77410160560406,55.1434784421197,13.832624048792));
#51621=CARTESIAN_POINT('Ctrl Pts',(-1.79091349418602,55.1520644111161,13.7659367660082));
#51622=CARTESIAN_POINT('Ctrl Pts',(-1.79246644812194,55.1528575173922,13.759776703873));
#51623=CARTESIAN_POINT('Ctrl Pts',(-1.79398570053851,55.1536505096524,13.7536088842887));
#51624=CARTESIAN_POINT('Ctrl Pts',(-1.7954710437966,55.154443377217,13.7474336659534));
#51625=CARTESIAN_POINT('Ctrl Pts',(-1.80135087869247,55.1575819987772,13.7229886334265));
#51626=CARTESIAN_POINT('Ctrl Pts',(-1.80670183139332,55.1607199865764,13.6984173801498));
#51627=CARTESIAN_POINT('Ctrl Pts',(-1.81155592987185,55.1638573620779,13.6737506746323));
#51628=CARTESIAN_POINT('Ctrl Pts',(-1.81330583161973,55.1649883854591,13.6648583311229));
#51629=CARTESIAN_POINT('Ctrl Pts',(-1.81499116133037,55.1661193291232,13.6559535835665));
#51630=CARTESIAN_POINT('Ctrl Pts',(-1.81661341753146,55.1672501939202,13.6470378741801));
#51631=CARTESIAN_POINT('Ctrl Pts',(-1.82273579646637,55.1715180665328,13.6133900747136));
#51632=CARTESIAN_POINT('Ctrl Pts',(-1.82795995185744,55.175784914625,13.5795853653127));
#51633=CARTESIAN_POINT('Ctrl Pts',(-1.83223365124789,55.1800507599276,13.5456737987172));
#51634=CARTESIAN_POINT('Ctrl Pts',(-1.84078126599194,55.188582666099,13.4778489518705));
#51635=CARTESIAN_POINT('Ctrl Pts',(-1.8455267573646,55.1971103793718,13.4095981151255));
#51636=CARTESIAN_POINT('Ctrl Pts',(-1.84652897031419,55.2056346992264,13.3412881479247));
#51637=CARTESIAN_POINT('Ctrl Pts',(-1.84753119218581,55.2141590949674,13.2729775726064));
#51638=CARTESIAN_POINT('Ctrl Pts',(-1.8447901515034,55.2226801902056,13.2046070996695));
#51639=CARTESIAN_POINT('Ctrl Pts',(-1.83824820549194,55.2311986099251,13.1366853948064));
#51640=CARTESIAN_POINT('Ctrl Pts',(-1.83170648471668,55.2397167363594,13.0687660284565));
#51641=CARTESIAN_POINT('Ctrl Pts',(-1.82136420101102,55.2482319227119,13.0012975276562));
#51642=CARTESIAN_POINT('Ctrl Pts',(-1.80738596135678,55.2567441298735,12.9345246763386));
#51643=CARTESIAN_POINT('Ctrl Pts',(-1.7958763752515,55.2637530225307,12.8795443711826));
#51644=CARTESIAN_POINT('Ctrl Pts',(-1.78190396256387,55.27075866633,12.8250453163076));
#51645=CARTESIAN_POINT('Ctrl Pts',(-1.76553466932195,55.2777622567396,12.7712659931012));
#51646=CARTESIAN_POINT('Ctrl Pts',(-1.73900282001386,55.2891138894959,12.6840988272306));
#51647=CARTESIAN_POINT('Ctrl Pts',(-1.70617317211776,55.3004606173606,12.5988184176065));
#51648=CARTESIAN_POINT('Ctrl Pts',(-1.66731880928453,55.3118054938855,12.5164595315625));
#51649=CARTESIAN_POINT('Ctrl Pts',(-1.63622777574238,55.320883597626,12.4505564333834));
#51650=CARTESIAN_POINT('Ctrl Pts',(-1.60127815679782,55.3299605556722,12.3865240861352));
#51651=CARTESIAN_POINT('Ctrl Pts',(-1.56261594941289,55.3390359058805,12.3249085851209));
#51652=CARTESIAN_POINT('Ctrl Pts',(-1.53459200795931,55.3456140890757,12.2802471622522));
#51653=CARTESIAN_POINT('Ctrl Pts',(-1.50461590022783,55.352191706902,12.2368539906714));
#51654=CARTESIAN_POINT('Ctrl Pts',(-1.4727569997285,55.3587661371559,12.1949514660604));
#51655=CARTESIAN_POINT('Ctrl Pts',(-1.46117279727529,55.3611566631905,12.1797153053396));
#51656=CARTESIAN_POINT('Ctrl Pts',(-1.44933381467607,55.3635479861347,12.1646684157009));
#51657=CARTESIAN_POINT('Ctrl Pts',(-1.43724904690904,55.3659398809156,12.1498168760294));
#51658=CARTESIAN_POINT('Ctrl Pts',(-1.39109517265427,55.375074951864,12.093096208516));
#51659=CARTESIAN_POINT('Ctrl Pts',(-1.34135318348424,55.3842183341153,12.0392277203063));
#51660=CARTESIAN_POINT('Ctrl Pts',(-1.28855352533096,55.3933571845613,11.9885318653594));
#51661=CARTESIAN_POINT('Ctrl Pts',(-1.27681760630921,55.3953885009095,11.977263564215));
#51662=CARTESIAN_POINT('Ctrl Pts',(-1.26493077684308,55.3974195934414,11.966151872421));
#51663=CARTESIAN_POINT('Ctrl Pts',(-1.25289910879172,55.3994503212419,11.9552000687445));
#51664=CARTESIAN_POINT('Ctrl Pts',(-1.18633035288021,55.4106859223814,11.8946059813228));
#51665=CARTESIAN_POINT('Ctrl Pts',(-1.11533190320657,55.4219097733954,11.8389101339942));
#51666=CARTESIAN_POINT('Ctrl Pts',(-1.04084807000666,55.4331806272757,11.7884745408066));
#51667=CARTESIAN_POINT('Ctrl Pts',(-1.02245212373735,55.4359642920454,11.7760180059791));
#51668=CARTESIAN_POINT('Ctrl Pts',(-1.00384339555138,55.4387508482516,11.7638821670127));
#51669=CARTESIAN_POINT('Ctrl Pts',(-0.985035741393843,55.4415412284531,
11.752072159837));
#51670=CARTESIAN_POINT('Ctrl Pts',(-0.936512183150477,55.4487403812605,
11.721602460307));
#51671=CARTESIAN_POINT('Ctrl Pts',(-0.886691372514162,55.4560121312427,
11.693252979208));
#51672=CARTESIAN_POINT('Ctrl Pts',(-0.835685478204693,55.4632411084962,
11.6672298356327));
#51673=CARTESIAN_POINT('Ctrl Pts',(-0.817858458691767,55.4657677011636,
11.6581345125414));
#51674=CARTESIAN_POINT('Ctrl Pts',(-0.799887020170616,55.4682890112393,
11.6493236758217));
#51675=CARTESIAN_POINT('Ctrl Pts',(-0.781777121593457,55.4707999286012,
11.6408070442452));
#51676=CARTESIAN_POINT('Ctrl Pts',(-0.716426553116967,55.4798607124755,
11.6100743091801));
#51677=CARTESIAN_POINT('Ctrl Pts',(-0.649259766796169,55.4887874631735,
11.5831662722903));
#51678=CARTESIAN_POINT('Ctrl Pts',(-0.580774250314715,55.4976838882126,
11.5602168129255));
#51679=CARTESIAN_POINT('Ctrl Pts',(-0.542986589613307,55.5025925916597,
11.5475541883545));
#51680=CARTESIAN_POINT('Ctrl Pts',(-0.504796551051388,55.5074921845024,
11.53609645761));
#51681=CARTESIAN_POINT('Ctrl Pts',(-0.466281015117716,55.5124009729648,
11.5258653905635));
#51682=CARTESIAN_POINT('Ctrl Pts',(-0.393893962647231,55.521626671618,11.5066368696778));
#51683=CARTESIAN_POINT('Ctrl Pts',(-0.320375910066749,55.5309460030142,
11.491681157064));
#51684=CARTESIAN_POINT('Ctrl Pts',(-0.246275569710484,55.5402915980726,
11.481338529198));
#51685=CARTESIAN_POINT('Ctrl Pts',(-0.212808585785349,55.5445124812438,
11.4766673420095));
#51686=CARTESIAN_POINT('Ctrl Pts',(-0.179223385183204,55.5487386688748,
11.4729367241748));
#51687=CARTESIAN_POINT('Ctrl Pts',(-0.145572996244575,55.5529636959111,
11.4701755549305));
#51688=CARTESIAN_POINT('Ctrl Pts',(-0.120424406205636,55.5561212663342,
11.4681119974043));
#51689=CARTESIAN_POINT('Ctrl Pts',(-0.0952411304475411,55.5592779727016,
11.4665900555687));
#51690=CARTESIAN_POINT('Ctrl Pts',(-0.0700489944315699,55.5624330172247,
11.4656184500148));
#51691=CARTESIAN_POINT('Ctrl Pts',(-0.0700341519148885,55.5624348760905,
11.4656178775714));
#51692=CARTESIAN_POINT('Ctrl Pts',(-0.0700193093888145,55.562436734963,
11.4656173053121));
#51693=CARTESIAN_POINT('Ctrl Pts',(-0.0700044668533595,55.5624385938423,
11.465616733237));
#51694=CARTESIAN_POINT('Ctrl Pts',(0.00238493529662621,55.5715046429639,
11.462826632086));
#51695=CARTESIAN_POINT('Ctrl Pts',(0.075001165013121,55.5807303128564,11.4644191143735));
#51696=CARTESIAN_POINT('Ctrl Pts',(0.147334995159917,55.5900284904859,11.4702925062558));
#51697=CARTESIAN_POINT('Ctrl Pts',(0.17072954618932,55.5930357512738,11.4721921065649));
#51698=CARTESIAN_POINT('Ctrl Pts',(0.194094231384653,55.5960505570346,11.4745392584708));
#51699=CARTESIAN_POINT('Ctrl Pts',(0.21741095317351,55.5990698478536,11.4773297641015));
#51700=CARTESIAN_POINT('Ctrl Pts',(0.315510529343815,55.6117727977951,11.4890701546313));
#51701=CARTESIAN_POINT('Ctrl Pts',(0.412796477800318,55.6243902239284,11.5088324041391));
#51702=CARTESIAN_POINT('Ctrl Pts',(0.508054631261452,55.6368958253134,11.5361404005733));
#51703=CARTESIAN_POINT('Ctrl Pts',(0.604937458395263,55.6496147157513,11.5639141480351));
#51704=CARTESIAN_POINT('Ctrl Pts',(0.699722509577989,55.6622180924772,11.5994929288359));
#51705=CARTESIAN_POINT('Ctrl Pts',(0.791131408574685,55.6747007094324,11.6423601989366));
#51706=CARTESIAN_POINT('Ctrl Pts',(0.881175096093966,55.6869968958308,11.6845872371804));
#51707=CARTESIAN_POINT('Ctrl Pts',(0.967942559080783,55.6991759410771,11.7338864645313));
#51708=CARTESIAN_POINT('Ctrl Pts',(1.05021417244992,55.7112528001152,11.7897532406534));
#51709=CARTESIAN_POINT('Ctrl Pts',(1.08566836928764,55.7164572116976,11.8138285151766));
#51710=CARTESIAN_POINT('Ctrl Pts',(1.12028768546031,55.7216428988617,11.839123331228));
#51711=CARTESIAN_POINT('Ctrl Pts',(1.15397469145896,55.7268122444113,11.8655966986872));
#51712=CARTESIAN_POINT('Ctrl Pts',(1.2108410677276,55.7355385155766,11.910285872759));
#51713=CARTESIAN_POINT('Ctrl Pts',(1.26516494342727,55.7444350125964,11.9581902961626));
#51714=CARTESIAN_POINT('Ctrl Pts',(1.31639363809883,55.7534138154864,12.0091358894873));
#51715=CARTESIAN_POINT('Ctrl Pts',(1.33567634726397,55.7567934769415,12.0283120380428));
#51716=CARTESIAN_POINT('Ctrl Pts',(1.35452053906315,55.7601847572048,12.0479185383536));
#51717=CARTESIAN_POINT('Ctrl Pts',(1.37289698704502,55.7635828157681,12.0679441978291));
#51718=CARTESIAN_POINT('Ctrl Pts',(1.37795301575926,55.7645177451781,12.0734539845643));
#51719=CARTESIAN_POINT('Ctrl Pts',(1.38297317089069,55.7654525783454,12.0789957082114));
#51720=CARTESIAN_POINT('Ctrl Pts',(1.38795682403215,55.7663872885772,12.0845689660414));
#51721=CARTESIAN_POINT('Ctrl Pts',(1.39949629048309,55.7685515759092,12.0974736405694));
#51722=CARTESIAN_POINT('Ctrl Pts',(1.41084700069948,55.7707165090372,12.1105551753011));
#51723=CARTESIAN_POINT('Ctrl Pts',(1.42200470289133,55.7728817995221,12.1238052629277));
#51724=CARTESIAN_POINT('Ctrl Pts',(1.45566265210831,55.7794135419839,12.1637750316837));
#51725=CARTESIAN_POINT('Ctrl Pts',(1.48756365211122,55.7859485648259,12.2052793343133));
#51726=CARTESIAN_POINT('Ctrl Pts',(1.51761462390527,55.7924819067513,12.2481011209081));
#51727=CARTESIAN_POINT('Ctrl Pts',(1.54766559569933,55.7990152486767,12.2909229075029));
#51728=CARTESIAN_POINT('Ctrl Pts',(1.57587332813735,55.8055479803492,12.3350678823099));
#51729=CARTESIAN_POINT('Ctrl Pts',(1.60218878834419,55.8120850137067,12.3803850023654));
#51730=CARTESIAN_POINT('Ctrl Pts',(1.64845076863821,55.8235769696136,12.4600514683331));
#51731=CARTESIAN_POINT('Ctrl Pts',(1.68885348102637,55.8350806624248,12.5433328066042));
#51732=CARTESIAN_POINT('Ctrl Pts',(1.72305341899742,55.8466891972649,12.6291521935411));
#51733=CARTESIAN_POINT('Ctrl Pts',(1.73239851669919,55.8498612174115,12.6526022523193));
#51734=CARTESIAN_POINT('Ctrl Pts',(1.74128074819349,55.8530410970104,12.6762419566786));
#51735=CARTESIAN_POINT('Ctrl Pts',(1.74969366836096,55.8562308054419,12.7000497027787));
#51736=CARTESIAN_POINT('Ctrl Pts',(1.78454516205636,55.8694445411099,12.7986760413855));
#51737=CARTESIAN_POINT('Ctrl Pts',(1.8111965418513,55.8826079458639,12.9002677257654));
#51738=CARTESIAN_POINT('Ctrl Pts',(1.82902797094738,55.8956085399769,13.0034160787279));
#51739=CARTESIAN_POINT('Ctrl Pts',(1.83028611148198,55.8965258290142,13.0106939656118));
#51740=CARTESIAN_POINT('Ctrl Pts',(1.83150033296328,55.8974423047915,13.0179795834037));
#51741=CARTESIAN_POINT('Ctrl Pts',(1.83267041346338,55.8983579265671,13.0252724285714));
#51742=CARTESIAN_POINT('Ctrl Pts',(1.84206444066225,55.9057090240887,13.083823259781));
#51743=CARTESIAN_POINT('Ctrl Pts',(1.84861496845924,55.9130059892496,13.1428471078161));
#51744=CARTESIAN_POINT('Ctrl Pts',(1.85226648614548,55.920319285591,13.2020811701997));
#51745=CARTESIAN_POINT('Ctrl Pts',(1.85226753774617,55.9203213917474,13.2020982290191));
#51746=CARTESIAN_POINT('Ctrl Pts',(1.85226858910766,55.920323497907,13.2021152878546));
#51747=CARTESIAN_POINT('Ctrl Pts',(1.85226964022996,55.9203256040698,13.2021323467061));
#51748=CARTESIAN_POINT('Ctrl Pts',(1.85902336759589,55.9338582340013,13.3117397944665));
#51749=CARTESIAN_POINT('Ctrl Pts',(1.85589972572324,55.9475221773674,13.4220160755468));
#51750=CARTESIAN_POINT('Ctrl Pts',(1.84323309485339,55.9612356686241,13.5312848453473));
#51751=CARTESIAN_POINT('Ctrl Pts',(1.84011107204006,55.9646157175884,13.55821699452));
#51752=CARTESIAN_POINT('Ctrl Pts',(1.83640946560615,55.9679987528036,13.5850877443923));
#51753=CARTESIAN_POINT('Ctrl Pts',(1.83213361865251,55.9713835039069,13.6118716542082));
#51754=CARTESIAN_POINT('Ctrl Pts',(1.81019802534562,55.9887476716263,13.7492762337592));
#51755=CARTESIAN_POINT('Ctrl Pts',(1.77316380370024,56.0061759019501,13.8843946461673));
#51756=CARTESIAN_POINT('Ctrl Pts',(1.721841056594,56.0236692220895,14.0139129323168));
#51757=CARTESIAN_POINT('Ctrl Pts',(1.67792950830242,56.0386364406309,14.1247282880327));
#51758=CARTESIAN_POINT('Ctrl Pts',(1.62354173049666,56.0536231692044,14.2314457018421));
#51759=CARTESIAN_POINT('Ctrl Pts',(1.55912072822312,56.0686012394853,14.3320167736881));
#51760=CARTESIAN_POINT('Ctrl Pts',(1.55558827495383,56.0694225451382,14.3375314754003));
#51761=CARTESIAN_POINT('Ctrl Pts',(1.55202564578714,56.0702438242641,14.3430276865584));
#51762=CARTESIAN_POINT('Ctrl Pts',(1.54843291093098,56.0710650720493,14.3485050657812));
#51763=CARTESIAN_POINT('Ctrl Pts',(1.54236165712056,56.0724528738062,14.3577611230214));
#51764=CARTESIAN_POINT('Ctrl Pts',(1.53620441579189,56.0738406055688,14.3669634397666));
#51765=CARTESIAN_POINT('Ctrl Pts',(1.52996196036076,56.0752287214057,14.3761102651033));
#51766=CARTESIAN_POINT('Ctrl Pts',(1.5299561689752,56.0752300092185,14.3761187509936));
#51767=CARTESIAN_POINT('Ctrl Pts',(1.52995037751575,56.0752312970319,14.3761272368371));
#51768=CARTESIAN_POINT('Ctrl Pts',(1.52994458598239,56.0752325848458,14.3761357226337));
#51769=CARTESIAN_POINT('Ctrl Pts',(1.48073277321199,56.0861753961918,14.448241227112));
#51770=CARTESIAN_POINT('Ctrl Pts',(1.42618104474603,56.0971582812265,14.5169620994692));
#51771=CARTESIAN_POINT('Ctrl Pts',(1.36700329858654,56.1081536370437,14.5816650405516));
#51772=CARTESIAN_POINT('Ctrl Pts',(1.34777982439549,56.1117254009666,14.6026833354125));
#51773=CARTESIAN_POINT('Ctrl Pts',(1.32806857343291,56.1152984746277,14.623277826765));
#51774=CARTESIAN_POINT('Ctrl Pts',(1.30789502252752,56.1188718941239,14.6434274028874));
#51775=CARTESIAN_POINT('Ctrl Pts',(1.23332838239186,56.1320801729677,14.7179054260498));
#51776=CARTESIAN_POINT('Ctrl Pts',(1.1524419907,56.1452918989564,14.78630148597));
#51777=CARTESIAN_POINT('Ctrl Pts',(1.06649397803563,56.1584436465506,14.8476206408121));
#51778=CARTESIAN_POINT('Ctrl Pts',(1.00092954881442,56.1684763023101,14.8943972359063));
#51779=CARTESIAN_POINT('Ctrl Pts',(0.932411137742052,56.1784705523755,14.937067035271));
#51780=CARTESIAN_POINT('Ctrl Pts',(0.861396890224984,56.1884804284716,14.9752810838156));
#51781=CARTESIAN_POINT('Ctrl Pts',(0.829645719418002,56.1929559428478,14.9923669620019));
#51782=CARTESIAN_POINT('Ctrl Pts',(0.797395108893155,56.1974346009196,15.0085616334312));
#51783=CARTESIAN_POINT('Ctrl Pts',(0.764683860406484,56.2019213265822,15.0238312852542));
#51784=CARTESIAN_POINT('Ctrl Pts',(0.697830046211415,56.2110910996011,15.0550387295744));
#51785=CARTESIAN_POINT('Ctrl Pts',(0.629059785282966,56.22029826175,15.0823759652349));
#51786=CARTESIAN_POINT('Ctrl Pts',(0.558876386431781,56.2295436592919,15.1054854320513));
#51787=CARTESIAN_POINT('Ctrl Pts',(0.553821518874132,56.2302095469641,15.1071498611898));
#51788=CARTESIAN_POINT('Ctrl Pts',(0.548759327893151,56.2308756330845,15.1087923805333));
#51789=CARTESIAN_POINT('Ctrl Pts',(0.543690004547129,56.2315419180171,15.1104128666647));
#51790=CARTESIAN_POINT('Ctrl Pts',(0.543678051144725,56.2315434891088,15.1104166877511));
#51791=CARTESIAN_POINT('Ctrl Pts',(0.543666097701438,56.2315450602015,15.1104205087153));
#51792=CARTESIAN_POINT('Ctrl Pts',(0.54365414421728,56.231546631295,15.1104243295572));
#51793=CARTESIAN_POINT('Ctrl Pts',(0.507541019102652,56.2362931216487,15.1219676201155));
#51794=CARTESIAN_POINT('Ctrl Pts',(0.471054633796932,56.2410479110577,15.1323946376915));
#51795=CARTESIAN_POINT('Ctrl Pts',(0.434265931366752,56.2457936695816,15.14169693376));
#51796=CARTESIAN_POINT('Ctrl Pts',(0.335571148175681,56.2585253392966,15.1666526411651));
#51797=CARTESIAN_POINT('Ctrl Pts',(0.234687921336243,56.2711916404696,15.1835209071129));
#51798=CARTESIAN_POINT('Ctrl Pts',(0.132892379707592,56.2838529014418,15.192323894123));
#51799=CARTESIAN_POINT('Ctrl Pts',(0.108514262031127,56.286885035315,15.1944320439477));
#51800=CARTESIAN_POINT('Ctrl Pts',(0.0840837083974954,56.2899168895166,
15.1960774334646));
#51801=CARTESIAN_POINT('Ctrl Pts',(0.0596180681824553,56.292949310042,15.1972599649554));
#51802=CARTESIAN_POINT('Ctrl Pts',(-0.0685561533320207,56.308836004064,
15.2034551861683));
#51803=CARTESIAN_POINT('Ctrl Pts',(-0.197691698140074,56.3247402671585,
15.1969458271626));
#51804=CARTESIAN_POINT('Ctrl Pts',(-0.325118024785957,56.3407799463547,
15.1777131839381));
#51805=CARTESIAN_POINT('Ctrl Pts',(-0.419898235242895,56.3527103237726,
15.1634078671292));
#51806=CARTESIAN_POINT('Ctrl Pts',(-0.513732117860426,56.364704380367,15.1420555001306));
#51807=CARTESIAN_POINT('Ctrl Pts',(-0.605457643405961,56.3768028412959,
15.1136862713413));
#51808=CARTESIAN_POINT('Ctrl Pts',(-0.637051603263352,56.380970037795,15.1039147680414));
#51809=CARTESIAN_POINT('Ctrl Pts',(-0.66839563189717,56.385149631178,15.0933111903414));
#51810=CARTESIAN_POINT('Ctrl Pts',(-0.699443003129483,56.3893433170818,
15.0818780096305));
#51811=CARTESIAN_POINT('Ctrl Pts',(-0.69947526575327,56.3893476749164,15.0818661289336));
#51812=CARTESIAN_POINT('Ctrl Pts',(-0.699507528056461,56.3893520327582,
15.0818542473376));
#51813=CARTESIAN_POINT('Ctrl Pts',(-0.699539790038952,56.389356390607,15.0818423648428));
#51814=CARTESIAN_POINT('Ctrl Pts',(-0.78224520260987,56.4005279820027,15.0513809187576));
#51815=CARTESIAN_POINT('Ctrl Pts',(-0.862845916453469,56.4117464350318,
15.0150127704698));
#51816=CARTESIAN_POINT('Ctrl Pts',(-0.940695421505603,56.422863422228,14.9731872027529));
#51817=CARTESIAN_POINT('Ctrl Pts',(-1.02619563775041,56.4350729386357,14.9272511999232));
#51818=CARTESIAN_POINT('Ctrl Pts',(-1.10840993016031,56.4471642416883,14.8747167149216));
#51819=CARTESIAN_POINT('Ctrl Pts',(-1.18649340540652,56.4592287353092,14.8162241243345));
#51820=CARTESIAN_POINT('Ctrl Pts',(-1.19648353546117,56.4607722867448,14.8087404847378));
#51821=CARTESIAN_POINT('Ctrl Pts',(-1.20640602416328,56.4623154026554,14.8011592507069));
#51822=CARTESIAN_POINT('Ctrl Pts',(-1.2162590773069,56.4638582773433,14.7934817067346));
#51823=CARTESIAN_POINT('Ctrl Pts',(-1.30651622245473,56.4779915071776,14.7231529273614));
#51824=CARTESIAN_POINT('Ctrl Pts',(-1.39094420748223,56.4921062989355,14.6447395298765));
#51825=CARTESIAN_POINT('Ctrl Pts',(-1.46799871801572,56.5063320712309,14.5593892863486));
#51826=CARTESIAN_POINT('Ctrl Pts',(-1.52148336091198,56.51620638418,14.5001464559861));
#51827=CARTESIAN_POINT('Ctrl Pts',(-1.57141296562096,56.5261347541126,14.4375617369057));
#51828=CARTESIAN_POINT('Ctrl Pts',(-1.61724853091761,56.5361453034843,14.372092803771));
#51829=CARTESIAN_POINT('Ctrl Pts',(-1.63329747805945,56.5396504152177,14.3491693939578));
#51830=CARTESIAN_POINT('Ctrl Pts',(-1.64884489548224,56.5431656067566,14.3258926168765));
#51831=CARTESIAN_POINT('Ctrl Pts',(-1.66386901373267,56.5466920994784,14.3022828030678));
#51832=CARTESIAN_POINT('Ctrl Pts',(-1.66775409226985,56.5476040133064,14.2961775542029));
#51833=CARTESIAN_POINT('Ctrl Pts',(-1.67160414596099,56.5485166645035,14.2900500889728));
#51834=CARTESIAN_POINT('Ctrl Pts',(-1.67541879375985,56.5494300660031,14.2839007854373));
#51835=CARTESIAN_POINT('Ctrl Pts',(-1.67542857316578,56.5494324076411,14.2838850208009));
#51836=CARTESIAN_POINT('Ctrl Pts',(-1.67543835234168,56.5494347492824,14.2838692560154));
#51837=CARTESIAN_POINT('Ctrl Pts',(-1.67544813128754,56.549437090927,14.2838534910808));
#51838=CARTESIAN_POINT('Ctrl Pts',(-1.73166717470118,56.5628991780055,14.1932210695618));
#51839=CARTESIAN_POINT('Ctrl Pts',(-1.7802821448428,56.5764719208028,14.0976574064469));
#51840=CARTESIAN_POINT('Ctrl Pts',(-1.82086816109241,56.5899673755073,13.9985909126802));
#51841=CARTESIAN_POINT('Ctrl Pts',(-1.83346210570417,56.594155049607,13.9678503263732));
#51842=CARTESIAN_POINT('Ctrl Pts',(-1.84528453972575,56.5983357505854,13.9367695762817));
#51843=CARTESIAN_POINT('Ctrl Pts',(-1.85632531934735,56.6025053100698,13.905383230766));
#51844=CARTESIAN_POINT('Ctrl Pts',(-1.89151540826478,56.6157948760269,13.8053460660597));
#51845=CARTESIAN_POINT('Ctrl Pts',(-1.91877554968822,56.6289730326751,13.7021842607744));
#51846=CARTESIAN_POINT('Ctrl Pts',(-1.93772504824362,56.6421593605133,13.5971903439077));
#51847=CARTESIAN_POINT('Ctrl Pts',(-1.95452879666546,56.6538525319685,13.5040854335222));
#51848=CARTESIAN_POINT('Ctrl Pts',(-1.96478960842525,56.6655532679108,13.4095385159904));
#51849=CARTESIAN_POINT('Ctrl Pts',(-1.96821851392384,56.6773260564793,13.3146094627546));
#51850=CARTESIAN_POINT('Ctrl Pts',(-1.96864668786567,56.6787961469468,13.3027554915867));
#51851=CARTESIAN_POINT('Ctrl Pts',(-1.96896839853184,56.6802673622679,13.2908955655712));
#51852=CARTESIAN_POINT('Ctrl Pts',(-1.96918314058438,56.6817398291142,13.2790317489242));
#51853=CARTESIAN_POINT('Ctrl Pts',(-1.9705243099076,56.6909361059507,13.2049364017167));
#51854=CARTESIAN_POINT('Ctrl Pts',(-1.96768877568565,56.700180753234,13.1306939107237));
#51855=CARTESIAN_POINT('Ctrl Pts',(-1.96057944937995,56.7094914055201,13.056870603467));
#51856=CARTESIAN_POINT('Ctrl Pts',(-1.95988008122185,56.7104073254624,13.0496083583258));
#51857=CARTESIAN_POINT('Ctrl Pts',(-1.95913939547865,56.7113238842644,13.0423501628215));
#51858=CARTESIAN_POINT('Ctrl Pts',(-1.95835732692828,56.7122410987799,13.0350965506566));
#51859=CARTESIAN_POINT('Ctrl Pts',(-1.9583549776439,56.7122438540342,13.0350747612652));
#51860=CARTESIAN_POINT('Ctrl Pts',(-1.95835262798405,56.712246609294,13.0350529719006));
#51861=CARTESIAN_POINT('Ctrl Pts',(-1.95835027794874,56.7122493645591,13.0350311825627));
#51862=CARTESIAN_POINT('Ctrl Pts',(-1.94942210937261,56.7227170675724,12.9522499239088));
#51863=CARTESIAN_POINT('Ctrl Pts',(-1.93507012850912,56.7332631872279,12.8698553643149));
#51864=CARTESIAN_POINT('Ctrl Pts',(-1.91555053220342,56.7438198278824,12.7885681907034));
#51865=CARTESIAN_POINT('Ctrl Pts',(-1.91187738352266,56.7458063500464,12.7732717742284));
#51866=CARTESIAN_POINT('Ctrl Pts',(-1.90802139393833,56.7477932422511,12.7580145634693));
#51867=CARTESIAN_POINT('Ctrl Pts',(-1.90398447376313,56.7497800486625,12.7428013385255));
#51868=CARTESIAN_POINT('Ctrl Pts',(-1.87969668306578,56.7617335023307,12.6512722502031));
#51869=CARTESIAN_POINT('Ctrl Pts',(-1.84886272379624,56.773683397275,12.5613300144799));
#51870=CARTESIAN_POINT('Ctrl Pts',(-1.81181807371057,56.7855656036989,12.4737890131985));
#51871=CARTESIAN_POINT('Ctrl Pts',(-1.77337490374494,56.7978963904674,12.3829431398149));
#51872=CARTESIAN_POINT('Ctrl Pts',(-1.72822716320002,56.8101594420461,12.2946479662481));
#51873=CARTESIAN_POINT('Ctrl Pts',(-1.67673317282235,56.8224286711405,12.2098773844661));
#51874=CARTESIAN_POINT('Ctrl Pts',(-1.63200254411193,56.833086426097,12.1362408029651));
#51875=CARTESIAN_POINT('Ctrl Pts',(-1.5824772617458,56.8437495532281,12.0652671014348));
#51876=CARTESIAN_POINT('Ctrl Pts',(-1.52848077798596,56.8544481068479,11.9977181194456));
#51877=CARTESIAN_POINT('Ctrl Pts',(-1.52027105502172,56.8560747342729,11.9874478501608));
#51878=CARTESIAN_POINT('Ctrl Pts',(-1.51195805342695,56.8577021810085,11.9772566934403));
#51879=CARTESIAN_POINT('Ctrl Pts',(-1.50354299493526,56.859330553044,11.9671472623586));
#51880=CARTESIAN_POINT('Ctrl Pts',(-1.47174310670255,56.8654840514161,11.928944464504));
#51881=CARTESIAN_POINT('Ctrl Pts',(-1.43848741615714,56.8716502280323,11.8919122782969));
#51882=CARTESIAN_POINT('Ctrl Pts',(-1.40386139808873,56.877831231114,11.8562029393545));
#51883=CARTESIAN_POINT('Ctrl Pts',(-1.40386046433392,56.8778313977962,11.8562019763859));
#51884=CARTESIAN_POINT('Ctrl Pts',(-1.40385953057813,56.8778315644784,11.8562010134183));
#51885=CARTESIAN_POINT('Ctrl Pts',(-1.40385859682132,56.8778317311607,11.8562000504517));
#51886=CARTESIAN_POINT('Ctrl Pts',(-1.34522097650263,56.888298963774,11.7957281242066));
#51887=CARTESIAN_POINT('Ctrl Pts',(-1.28249847102813,56.8988525226504,11.7388890411541));
#51888=CARTESIAN_POINT('Ctrl Pts',(-1.21634219263946,56.9094485475929,11.6861013943469));
#51889=CARTESIAN_POINT('Ctrl Pts',(-1.19953584886059,56.9121403622204,11.6726912183042));
#51890=CARTESIAN_POINT('Ctrl Pts',(-1.18250809592946,56.9148349151284,11.6595423287713));
#51891=CARTESIAN_POINT('Ctrl Pts',(-1.16526997419257,56.9175314826331,11.6466612036137));
#51892=CARTESIAN_POINT('Ctrl Pts',(-1.08024870125905,56.9308314004145,11.5831293598069));
#51893=CARTESIAN_POINT('Ctrl Pts',(-0.990110409353869,56.944179928467,11.5261072649819));
#51894=CARTESIAN_POINT('Ctrl Pts',(-0.895963198840052,56.9575258852969,
11.4762188380546));
#51895=CARTESIAN_POINT('Ctrl Pts',(-0.86252406533658,56.9622660919343,11.4584995051164));
#51896=CARTESIAN_POINT('Ctrl Pts',(-0.828577042689153,56.9670063253804,
11.4416791736747));
#51897=CARTESIAN_POINT('Ctrl Pts',(-0.794164262756547,56.9717454508399,
11.425784319842));
#51898=CARTESIAN_POINT('Ctrl Pts',(-0.698103620334191,56.984974356992,11.3814150514084));
#51899=CARTESIAN_POINT('Ctrl Pts',(-0.598389926248981,56.9981979151434,
11.3442478963313));
#51900=CARTESIAN_POINT('Ctrl Pts',(-0.496141424071205,57.0114391775981,
11.3149825420423));
#51901=CARTESIAN_POINT('Ctrl Pts',(-0.419989513947958,57.0213009106005,
11.2931865002219));
#51902=CARTESIAN_POINT('Ctrl Pts',(-0.342433433999361,57.0311722124074,
11.2757784038796));
#51903=CARTESIAN_POINT('Ctrl Pts',(-0.264046529588669,57.0410477488817,
11.2630516991051));
#51904=CARTESIAN_POINT('Ctrl Pts',(-0.249205642273958,57.0429174709366,
11.260642169186));
#51905=CARTESIAN_POINT('Ctrl Pts',(-0.234335003176676,57.0447873443258,
11.2584002982776));
#51906=CARTESIAN_POINT('Ctrl Pts',(-0.21943853560129,57.0466573321898,11.2563278666349));
#51907=CARTESIAN_POINT('Ctrl Pts',(-0.11879000273389,57.0592919741976,11.2423254057661));
#51908=CARTESIAN_POINT('Ctrl Pts',(-0.0167823939950706,57.0719792727903,
11.2360362300478));
#51909=CARTESIAN_POINT('Ctrl Pts',(0.0853667345546593,57.0847009503705,
11.2373113037582));
#51910=CARTESIAN_POINT('Ctrl Pts',(0.110531223645454,57.0878349420279,11.2376254188067));
#51911=CARTESIAN_POINT('Ctrl Pts',(0.13570428321117,57.0909710189366,11.2383983493524));
#51912=CARTESIAN_POINT('Ctrl Pts',(0.160867712219528,57.0941089055934,11.2396273856827));
#51913=CARTESIAN_POINT('Ctrl Pts',(0.17190683574445,57.0954854873939,11.240166560366));
#51914=CARTESIAN_POINT('Ctrl Pts',(0.182944465887215,57.0968624637778,11.240793529023));
#51915=CARTESIAN_POINT('Ctrl Pts',(0.193979268323433,57.0982398378226,11.241508084893));
#51916=CARTESIAN_POINT('Ctrl Pts',(0.310199306268968,57.1127465283301,11.2490338843623));
#51917=CARTESIAN_POINT('Ctrl Pts',(0.426117937433488,57.1272987039844,11.2662718750778));
#51918=CARTESIAN_POINT('Ctrl Pts',(0.540146549680601,57.1419037653696,11.2930139483905));
#51919=CARTESIAN_POINT('Ctrl Pts',(0.551276280104599,57.1433292882523,11.2956241008872));
#51920=CARTESIAN_POINT('Ctrl Pts',(0.562387996858273,57.1447553151042,11.298324835973));
#51921=CARTESIAN_POINT('Ctrl Pts',(0.573480216019194,57.1461818529016,11.3011159860358));
#51922=CARTESIAN_POINT('Ctrl Pts',(0.697527491616906,57.1621352094609,11.3323301692442));
#51923=CARTESIAN_POINT('Ctrl Pts',(0.819136344563904,57.1781526813702,11.3748562817526));
#51924=CARTESIAN_POINT('Ctrl Pts',(0.93606778237377,57.1942216481512,11.4283982508154));
#51925=CARTESIAN_POINT('Ctrl Pts',(0.99511780650718,57.2023364280084,11.4554367840321));
#51926=CARTESIAN_POINT('Ctrl Pts',(1.05297228500711,57.2104639569118,11.4852831934948));
#51927=CARTESIAN_POINT('Ctrl Pts',(1.10933041666177,57.2186004187615,11.5178839589184));
#51928=CARTESIAN_POINT('Ctrl Pts',(1.10933175267172,57.2186006116422,11.5178847317429));
#51929=CARTESIAN_POINT('Ctrl Pts',(1.10933308868084,57.2186008045229,11.517885504569));
#51930=CARTESIAN_POINT('Ctrl Pts',(1.10933442468911,57.2186009974035,11.5178862773967));
#51931=CARTESIAN_POINT('Ctrl Pts',(1.12852030193005,57.2213708791972,11.5289845440871));
#51932=CARTESIAN_POINT('Ctrl Pts',(1.14753692501207,57.2241416825675,11.5404042732587));
#51933=CARTESIAN_POINT('Ctrl Pts',(1.16637602644111,57.2269135946435,11.552137425452));
#51934=CARTESIAN_POINT('Ctrl Pts',(1.27525068865178,57.2429329887787,11.6199454887253));
#51935=CARTESIAN_POINT('Ctrl Pts',(1.37818710760162,57.258988265738,11.6982209598812));
#51936=CARTESIAN_POINT('Ctrl Pts',(1.47356521081465,57.2750817193222,11.7853567463418));
#51937=CARTESIAN_POINT('Ctrl Pts',(1.48314108575922,57.2766974874467,11.7941051001697));
#51938=CARTESIAN_POINT('Ctrl Pts',(1.49264079909951,57.2783136401906,11.8029427313062));
#51939=CARTESIAN_POINT('Ctrl Pts',(1.50206273000616,57.2799301797367,11.8118679915361));
#51940=CARTESIAN_POINT('Ctrl Pts',(1.60475210073033,57.2975488006307,11.9091441619562));
#51941=CARTESIAN_POINT('Ctrl Pts',(1.69820428117194,57.3152139186673,12.0168279148488));
#51942=CARTESIAN_POINT('Ctrl Pts',(1.78041366025471,57.3329448589268,12.1328930198129));
#51943=CARTESIAN_POINT('Ctrl Pts',(1.81839841676897,57.34113742109,12.1865207786046));
#51944=CARTESIAN_POINT('Ctrl Pts',(1.85398400347341,57.3493442200302,12.2419396266027));
#51945=CARTESIAN_POINT('Ctrl Pts',(1.88697436285143,57.3575676858942,12.2989601069398));
#51946=CARTESIAN_POINT('Ctrl Pts',(1.93596769315265,57.3697801924232,12.3836400946622));
#51947=CARTESIAN_POINT('Ctrl Pts',(1.97924341638224,57.3820318062515,12.4718732311336));
#51948=CARTESIAN_POINT('Ctrl Pts',(2.01610593080336,57.3942624585106,12.5629186579116));
#51949=CARTESIAN_POINT('Ctrl Pts',(2.01610697815278,57.3942628060118,12.5629212447231));
#51950=CARTESIAN_POINT('Ctrl Pts',(2.01610802549702,57.3942631535129,12.5629238315368));
#51951=CARTESIAN_POINT('Ctrl Pts',(2.01610907283609,57.3942635010141,12.5629264183528));
#51952=CARTESIAN_POINT('Ctrl Pts',(2.05154606796938,57.4060212937583,12.6504520235051));
#51953=CARTESIAN_POINT('Ctrl Pts',(2.08109335709301,57.4177969516692,12.74067767571));
#51954=CARTESIAN_POINT('Ctrl Pts',(2.10461089161464,57.4296087684235,12.8326815628148));
#51955=CARTESIAN_POINT('Ctrl Pts',(2.11116188035192,57.4328990401335,12.8583099477824));
#51956=CARTESIAN_POINT('Ctrl Pts',(2.11724527915549,57.4361921147007,12.8840761843313));
#51957=CARTESIAN_POINT('Ctrl Pts',(2.12285872882916,57.4394883806281,12.9099600987078));
#51958=CARTESIAN_POINT('Ctrl Pts',(2.14887168309908,57.4547634111023,13.0299072114719));
#51959=CARTESIAN_POINT('Ctrl Pts',(2.164793939548,57.4701168724529,13.1523804142498));
#51960=CARTESIAN_POINT('Ctrl Pts',(2.17046447447609,57.4855089821036,13.2756306015249));
#51961=CARTESIAN_POINT('Ctrl Pts',(2.17310856134027,57.4926860959836,13.3331003473805));
#51962=CARTESIAN_POINT('Ctrl Pts',(2.17352397983032,57.4998720476228,13.3907427526979));
#51963=CARTESIAN_POINT('Ctrl Pts',(2.17168907884137,57.507069560088,13.4483984305321));
#51964=CARTESIAN_POINT('Ctrl Pts',(2.16778234790218,57.5223939535036,13.5711544929962));
#51965=CARTESIAN_POINT('Ctrl Pts',(2.15365044376428,57.5378670458362,13.6940004938917));
#51966=CARTESIAN_POINT('Ctrl Pts',(2.12908713899266,57.5533516912026,13.8151280705915));
#51967=CARTESIAN_POINT('Ctrl Pts',(2.11820072091225,57.5602144616992,13.8688116222668));
#51968=CARTESIAN_POINT('Ctrl Pts',(2.10526733362143,57.5670735780649,13.9221527172546));
#51969=CARTESIAN_POINT('Ctrl Pts',(2.09028234147873,57.5739147073408,13.9749698748476));
#51970=CARTESIAN_POINT('Ctrl Pts',(2.09028139064532,57.5739151414267,13.9749732262219));
#51971=CARTESIAN_POINT('Ctrl Pts',(2.09028043980363,57.5739155755126,13.9749765775942));
#51972=CARTESIAN_POINT('Ctrl Pts',(2.09027948895371,57.5739160095984,13.9749799289644));
#51973=CARTESIAN_POINT('Ctrl Pts',(2.06838335284136,57.5839121206977,14.0521551533744));
#51974=CARTESIAN_POINT('Ctrl Pts',(2.04207605996703,57.5939491656667,14.128270426977));
#51975=CARTESIAN_POINT('Ctrl Pts',(2.01160877246451,57.6040107056676,14.2028291736451));
#51976=CARTESIAN_POINT('Ctrl Pts',(1.99599643373423,57.6091665361836,14.2410352793968));
#51977=CARTESIAN_POINT('Ctrl Pts',(1.97929160389414,57.6143288730566,14.2788335405652));
#51978=CARTESIAN_POINT('Ctrl Pts',(1.96152606695844,57.6194957795549,14.3161619667831));
#51979=CARTESIAN_POINT('Ctrl Pts',(1.96152459443129,57.6194962078229,14.316165060814));
#51980=CARTESIAN_POINT('Ctrl Pts',(1.96152312189686,57.6194966360909,14.3161681548417));
#51981=CARTESIAN_POINT('Ctrl Pts',(1.96152164935513,57.6194970643589,14.3161712488662));
#51982=CARTESIAN_POINT('Ctrl Pts',(1.92897574505878,57.628962582074,14.3845549307998));
#51983=CARTESIAN_POINT('Ctrl Pts',(1.89286971516756,57.6384435260741,14.4513607768799));
#51984=CARTESIAN_POINT('Ctrl Pts',(1.85339670738357,57.6479368122006,14.516286924724));
#51985=CARTESIAN_POINT('Ctrl Pts',(1.83670686721662,57.6519507304958,14.5437387732404));
#51986=CARTESIAN_POINT('Ctrl Pts',(1.81941486125606,57.6559669850194,14.5708551735042));
#51987=CARTESIAN_POINT('Ctrl Pts',(1.80153377049652,57.6599858781018,14.5976157278655));
#51988=CARTESIAN_POINT('Ctrl Pts',(1.793570187723,57.6617757458537,14.6095338984395));
#51989=CARTESIAN_POINT('Ctrl Pts',(1.78548973929216,57.663566141785,14.6213815115252));
#51990=CARTESIAN_POINT('Ctrl Pts',(1.77729365128469,57.6653567549875,14.6331567786028));
#51991=CARTESIAN_POINT('Ctrl Pts',(1.77729193427258,57.6653571301061,14.6331592454231));
#51992=CARTESIAN_POINT('Ctrl Pts',(1.77729021725538,57.6653575052246,14.6331617122403));
#51993=CARTESIAN_POINT('Ctrl Pts',(1.77728850023312,57.6653578803432,14.6331641790542));
#51994=CARTESIAN_POINT('Ctrl Pts',(1.73393580426888,57.6748291616104,14.6954481907934));
#51995=CARTESIAN_POINT('Ctrl Pts',(1.68737652870182,57.6843072213637,14.7556671002019));
#51996=CARTESIAN_POINT('Ctrl Pts',(1.63778729106415,57.6938025052366,14.8134821898953));
#51997=CARTESIAN_POINT('Ctrl Pts',(1.58822204723924,57.7032931948048,14.8712693056874));
#51998=CARTESIAN_POINT('Ctrl Pts',(1.53562822159541,57.7128009278753,14.9266541483628));
#51999=CARTESIAN_POINT('Ctrl Pts',(1.48020683297272,57.7223264388571,14.9792508401895));
#52000=CARTESIAN_POINT('Ctrl Pts',(1.42489588709152,57.7318329675727,15.0317427182794));
#52001=CARTESIAN_POINT('Ctrl Pts',(1.3667674610436,57.7413569461082,15.0814561529771));
#52002=CARTESIAN_POINT('Ctrl Pts',(1.30606647115989,57.7508925704664,15.1279763795914));
#52003=CARTESIAN_POINT('Ctrl Pts',(1.2915763606101,57.7531688472022,15.1390813587315));
#52004=CARTESIAN_POINT('Ctrl Pts',(1.27693989936916,57.7554457689097,15.1500042944493));
#52005=CARTESIAN_POINT('Ctrl Pts',(1.26216089829315,57.7577232302763,15.1607394370694));
#52006=CARTESIAN_POINT('Ctrl Pts',(1.26215807027415,57.7577236660773,15.1607414912804));
#52007=CARTESIAN_POINT('Ctrl Pts',(1.2621552422499,57.7577241018783,15.1607435454846));
#52008=CARTESIAN_POINT('Ctrl Pts',(1.26215241422026,57.7577245376793,15.1607455996821));
#52009=CARTESIAN_POINT('Ctrl Pts',(1.1821024916842,57.7700602766915,15.2188915071568));
#52010=CARTESIAN_POINT('Ctrl Pts',(1.09777583633315,57.7823787703683,15.2716098900839));
#52011=CARTESIAN_POINT('Ctrl Pts',(1.01010282620475,57.7947581127681,15.3185931659071));
#52012=CARTESIAN_POINT('Ctrl Pts',(0.98372483612274,57.7984826589035,15.3327289231016));
#52013=CARTESIAN_POINT('Ctrl Pts',(0.957044199268231,57.802212699256,15.3463457681613));
#52014=CARTESIAN_POINT('Ctrl Pts',(0.930086900172838,57.8059503238116,15.3594359711277));
#52015=CARTESIAN_POINT('Ctrl Pts',(0.850978071322352,57.8169187483645,15.3978504510958));
#52016=CARTESIAN_POINT('Ctrl Pts',(0.769463204092305,57.8279050259332,15.4317615894296));
#52017=CARTESIAN_POINT('Ctrl Pts',(0.686093571267212,57.8389144685452,15.461031010559));
#52018=CARTESIAN_POINT('Ctrl Pts',(0.598922955959961,57.8504258528964,15.491634881094));
#52019=CARTESIAN_POINT('Ctrl Pts',(0.509725733949969,57.8619623442583,15.5171631613577));
#52020=CARTESIAN_POINT('Ctrl Pts',(0.419141906685512,57.8735279509147,15.5374357709995));
#52021=CARTESIAN_POINT('Ctrl Pts',(0.316167620052189,57.8866755527648,15.5604813584857));
#52022=CARTESIAN_POINT('Ctrl Pts',(0.211405608724186,57.8998601824428,15.576733339609));
#52023=CARTESIAN_POINT('Ctrl Pts',(0.105826024951418,57.9130840446135,15.5859073055695));
#52024=CARTESIAN_POINT('Ctrl Pts',(-0.0197282419384677,57.9288097394967,
15.5968169012459));
#52025=CARTESIAN_POINT('Ctrl Pts',(-0.146439200881165,57.9445909373644,
15.5977142886005));
#52026=CARTESIAN_POINT('Ctrl Pts',(-0.27260456530094,57.9604427243888,15.5881099353691));
#52027=CARTESIAN_POINT('Ctrl Pts',(-0.307697137477017,57.9648518582492,
15.5854385091775));
#52028=CARTESIAN_POINT('Ctrl Pts',(-0.342741440753223,57.969310802562,15.5819373104183));
#52029=CARTESIAN_POINT('Ctrl Pts',(-0.377704756191395,57.9737727477083,
15.5776147022987));
#52030=CARTESIAN_POINT('Ctrl Pts',(-0.457793389572851,57.983993491494,15.5677131305339));
#52031=CARTESIAN_POINT('Ctrl Pts',(-0.537469825606877,57.9942304878195,
15.5534967718189));
#52032=CARTESIAN_POINT('Ctrl Pts',(-0.616216254675355,58.0043814023485,
15.5349138487034));
#52033=CARTESIAN_POINT('Ctrl Pts',(-0.63028710889917,58.006195224769,15.5315933476305));
#52034=CARTESIAN_POINT('Ctrl Pts',(-0.644328335635221,58.0080063032693,
15.528133545172));
#52035=CARTESIAN_POINT('Ctrl Pts',(-0.658337074143732,58.0098140600242,
15.5245342972585));
#52036=CARTESIAN_POINT('Ctrl Pts',(-0.658338275441633,58.0098142150456,
15.5245339886105));
#52037=CARTESIAN_POINT('Ctrl Pts',(-0.658339476739311,58.009814370067,15.5245336799615));
#52038=CARTESIAN_POINT('Ctrl Pts',(-0.658340678036733,58.0098145250883,
15.5245333713115));
#52039=CARTESIAN_POINT('Ctrl Pts',(-0.739222618996494,58.0202519307906,
15.5037523275969));
#52040=CARTESIAN_POINT('Ctrl Pts',(-0.819204934486232,58.0306008708064,
15.4782729641146));
#52041=CARTESIAN_POINT('Ctrl Pts',(-0.897738436735581,58.0410160411495,
15.4483462602352));
#52042=CARTESIAN_POINT('Ctrl Pts',(-0.92649322773712,58.0448295225032,15.4373886931999));
#52043=CARTESIAN_POINT('Ctrl Pts',(-0.9550535891957,58.0486518445508,15.4258353655298));
#52044=CARTESIAN_POINT('Ctrl Pts',(-0.983391973449421,58.052490464911,15.4137002333862));
#52045=CARTESIAN_POINT('Ctrl Pts',(-1.09169238759642,58.0671604676548,15.3673235654325));
#52046=CARTESIAN_POINT('Ctrl Pts',(-1.19679237425643,58.0819014253187,15.3125136141435));
#52047=CARTESIAN_POINT('Ctrl Pts',(-1.29755132669116,58.0966671351421,15.2501467519184));
#52048=CARTESIAN_POINT('Ctrl Pts',(-1.36875778954245,58.1071020785649,15.2060720215756));
#52049=CARTESIAN_POINT('Ctrl Pts',(-1.4378010898869,58.1175498179365,15.1582232951837));
#52050=CARTESIAN_POINT('Ctrl Pts',(-1.50433297279242,58.1280191132008,15.1068504820689));
#52051=CARTESIAN_POINT('Ctrl Pts',(-1.54974714864477,58.1351653774492,15.0717837761989));
#52052=CARTESIAN_POINT('Ctrl Pts',(-1.59399216625096,58.1423218737279,15.0350736355508));
#52053=CARTESIAN_POINT('Ctrl Pts',(-1.63695408575892,58.1494917037906,14.9967914350999));
#52054=CARTESIAN_POINT('Ctrl Pts',(-1.69734190352785,58.1595697076652,14.9429814896622));
#52055=CARTESIAN_POINT('Ctrl Pts',(-1.75518989077996,58.1696732263718,14.886069715756));
#52056=CARTESIAN_POINT('Ctrl Pts',(-1.81014253459797,58.1798063669947,14.8262699726838));
#52057=CARTESIAN_POINT('Ctrl Pts',(-1.87387451074958,58.1915583962265,14.7569165160608));
#52058=CARTESIAN_POINT('Ctrl Pts',(-1.93370658902649,58.2033612615372,14.6836703597443));
#52059=CARTESIAN_POINT('Ctrl Pts',(-1.98893194374559,58.2153383669724,14.6069358635697));
#52060=CARTESIAN_POINT('Ctrl Pts',(-2.00335825377246,58.2184671008142,14.5868908020721));
#52061=CARTESIAN_POINT('Ctrl Pts',(-2.01747019945016,58.221607701593,14.5666079736676));
#52062=CARTESIAN_POINT('Ctrl Pts',(-2.03125520687666,58.2247623194602,14.5460951747106));
#52063=CARTESIAN_POINT('Ctrl Pts',(-2.07642243173065,58.235098573198,14.4788840246394));
#52064=CARTESIAN_POINT('Ctrl Pts',(-2.11816673589426,58.2454008500489,14.4092448347116));
#52065=CARTESIAN_POINT('Ctrl Pts',(-2.15610926884306,58.255610553224,14.337534168832));
#52066=CARTESIAN_POINT('Ctrl Pts',(-2.17407630646753,58.260445183567,14.3035768093253));
#52067=CARTESIAN_POINT('Ctrl Pts',(-2.1911915558923,58.2652590716473,14.2691551915749));
#52068=CARTESIAN_POINT('Ctrl Pts',(-2.20741879394274,58.2700460825528,14.2343081529327));
#52069=CARTESIAN_POINT('Ctrl Pts',(-2.20742037612162,58.2700465492932,14.2343047552967));
#52070=CARTESIAN_POINT('Ctrl Pts',(-2.20742195829227,58.2700470160334,14.2343013576562));
#52071=CARTESIAN_POINT('Ctrl Pts',(-2.20742354045467,58.2700474827733,14.2342979600113));
#52072=CARTESIAN_POINT('Ctrl Pts',(-2.2423675324464,58.2803560050086,14.1592568166455));
#52073=CARTESIAN_POINT('Ctrl Pts',(-2.27329381777304,58.2905507441748,14.0820463417982));
#52074=CARTESIAN_POINT('Ctrl Pts',(-2.30006406188348,58.3007721133346,14.0031713102078));
#52075=CARTESIAN_POINT('Ctrl Pts',(-2.3323740168309,58.3131086454816,13.9079742433956));
#52076=CARTESIAN_POINT('Ctrl Pts',(-2.35852831113392,58.3256652461448,13.8103298458482));
#52077=CARTESIAN_POINT('Ctrl Pts',(-2.37856484609779,58.3382746346422,13.7111382426403));
#52078=CARTESIAN_POINT('Ctrl Pts',(-2.38226392232532,58.3406025366132,13.6928258297376));
#52079=CARTESIAN_POINT('Ctrl Pts',(-2.38575457854688,58.3429322532296,13.6744605754864));
#52080=CARTESIAN_POINT('Ctrl Pts',(-2.38903717202239,58.3452627531585,13.6560479890038));
#52081=CARTESIAN_POINT('Ctrl Pts',(-2.40987265671179,58.3600550495393,13.5391784568449));
#52082=CARTESIAN_POINT('Ctrl Pts',(-2.42232664060288,58.3748790286422,13.4204016788481));
#52083=CARTESIAN_POINT('Ctrl Pts',(-2.42634547880896,58.3897364539911,13.3010464102513));
#52084=CARTESIAN_POINT('Ctrl Pts',(-2.43027591694206,58.4042670690985,13.1843165308619));
#52085=CARTESIAN_POINT('Ctrl Pts',(-2.42614041294498,58.4188295468759,13.0670338935525));
#52086=CARTESIAN_POINT('Ctrl Pts',(-2.41387033313529,58.433431651294,12.9503879038096));
#52087=CARTESIAN_POINT('Ctrl Pts',(-2.40412122003183,58.4450336595717,12.8577075818632));
#52088=CARTESIAN_POINT('Ctrl Pts',(-2.38923682936086,58.4566606239254,12.765429212999));
#52089=CARTESIAN_POINT('Ctrl Pts',(-2.36916153037971,58.4683187763596,12.6741341540109));
#52090=CARTESIAN_POINT('Ctrl Pts',(-2.34908729832197,58.4799763092087,12.5828439469971));
#52091=CARTESIAN_POINT('Ctrl Pts',(-2.32369861772447,58.4918483155166,12.492561724561));
#52092=CARTESIAN_POINT('Ctrl Pts',(-2.29305561911638,58.5037818778372,12.4039662773282));
#52093=CARTESIAN_POINT('Ctrl Pts',(-2.28370438907306,58.507423606505,12.3769298760131));
#52094=CARTESIAN_POINT('Ctrl Pts',(-2.27386400194058,58.5110711045075,12.3500502322717));
#52095=CARTESIAN_POINT('Ctrl Pts',(-2.26353653476627,58.5147201244505,12.3233457404454));
#52096=CARTESIAN_POINT('Ctrl Pts',(-2.24107844936941,58.5226552744839,12.2652742164413));
#52097=CARTESIAN_POINT('Ctrl Pts',(-2.21634898676585,58.5305477092106,12.2080222560835));
#52098=CARTESIAN_POINT('Ctrl Pts',(-2.18939070437801,58.5383506903398,12.1518002682921));
#52099=CARTESIAN_POINT('Ctrl Pts',(-2.18938782706648,58.5383515231677,12.1517942676066));
#52100=CARTESIAN_POINT('Ctrl Pts',(-2.18938494972885,58.538352355995,12.1517882669321));
#52101=CARTESIAN_POINT('Ctrl Pts',(-2.18938207236512,58.538353188822,12.1517822662684));
#52102=CARTESIAN_POINT('Ctrl Pts',(-2.15380875524676,58.548649563825,12.077595083127));
#52103=CARTESIAN_POINT('Ctrl Pts',(-2.1142433990334,58.5588769501379,12.0050782113557));
#52104=CARTESIAN_POINT('Ctrl Pts',(-2.07099563869339,58.5690748660087,11.9346041460495));
#52105=CARTESIAN_POINT('Ctrl Pts',(-2.02764045632519,58.5792981122273,11.8639550319785));
#52106=CARTESIAN_POINT('Ctrl Pts',(-1.98058610030465,58.5894923299576,11.7953580761275));
#52107=CARTESIAN_POINT('Ctrl Pts',(-1.93012306899672,58.5997142606411,11.7291406106755));
#52108=CARTESIAN_POINT('Ctrl Pts',(-1.87972234867691,58.6099235694391,11.6630049095488));
#52109=CARTESIAN_POINT('Ctrl Pts',(-1.8258426072529,58.6203100199353,11.599323431948));
#52110=CARTESIAN_POINT('Ctrl Pts',(-1.76885646971354,58.6307171702467,11.5382756463943));
#52111=CARTESIAN_POINT('Ctrl Pts',(-1.75227196569756,58.6337459318646,11.5205090931868));
#52112=CARTESIAN_POINT('Ctrl Pts',(-1.73542377387291,58.6367765420156,11.5029650986599));
#52113=CARTESIAN_POINT('Ctrl Pts',(-1.71831766398917,58.6398093087261,11.4856494580447));
#52114=CARTESIAN_POINT('Ctrl Pts',(-0.211978292710951,66.0826669143831,
10.2439166213909));
#52115=CARTESIAN_POINT('Ctrl Pts',(0.380426698411577,66.1566886141943,10.2144267143116));
#52116=CARTESIAN_POINT('Ctrl Pts',(1.54604714045993,66.3004784630863,10.5056263688969));
#52117=CARTESIAN_POINT('Ctrl Pts',(2.75615769215105,66.5118442591118,11.7841923780606));
#52118=CARTESIAN_POINT('Ctrl Pts',(3.09938745941552,66.7171914208913,13.4595450858029));
#52119=CARTESIAN_POINT('Ctrl Pts',(2.51521498728355,66.919733558191,15.0420371329737));
#52120=CARTESIAN_POINT('Ctrl Pts',(1.20364263133209,67.1193482064331,16.0633151491819));
#52121=CARTESIAN_POINT('Ctrl Pts',(-0.425010768267335,67.3159276396824,
16.2362178374675));
#52122=CARTESIAN_POINT('Ctrl Pts',(-1.874476613348,67.5093778719358,15.5355630093087));
#52123=CARTESIAN_POINT('Ctrl Pts',(-2.82066310998034,67.7207586572874,14.0488554654566));
#52124=CARTESIAN_POINT('Ctrl Pts',(-2.65718161004858,67.9486110389564,12.101625506873));
#52125=CARTESIAN_POINT('Ctrl Pts',(-1.12386966785095,68.1912532325112,10.6893961684456));
#52126=CARTESIAN_POINT('Ctrl Pts',(0.90652387195178,68.4279099084122,10.683338398873));
#52127=CARTESIAN_POINT('Ctrl Pts',(2.37479267666757,68.6585764425755,12.0118831411098));
#52128=CARTESIAN_POINT('Ctrl Pts',(2.54915169405804,68.8832926157084,13.935283018162));
#52129=CARTESIAN_POINT('Ctrl Pts',(1.50934916221757,69.0839138557608,15.3042900857091));
#52130=CARTESIAN_POINT('Ctrl Pts',(0.0788806318954479,69.2621301783978,
15.7062194542042));
#52131=CARTESIAN_POINT('Ctrl Pts',(-1.1790274152294,69.4193887352863,15.3450857446561));
#52132=CARTESIAN_POINT('Ctrl Pts',(-2.04074624188028,69.5736038028972,14.3920281022972));
#52133=CARTESIAN_POINT('Ctrl Pts',(-2.26609286242154,69.7248824507778,13.1524725423401));
#52134=CARTESIAN_POINT('Ctrl Pts',(-1.81045081861987,69.8733436066605,12.0031498816977));
#52135=CARTESIAN_POINT('Ctrl Pts',(-0.836645778823911,70.0191227628882,
11.2782840667528));
#52136=CARTESIAN_POINT('Ctrl Pts',(0.352571010602829,70.1623683591737,11.1804871759654));
#52137=CARTESIAN_POINT('Ctrl Pts',(1.13590843302084,70.2680173733739,11.5801035007707));
#52138=CARTESIAN_POINT('Ctrl Pts',(1.51874801489704,70.3377610718551,11.9891882143963));
#52139=CARTESIAN_POINT('Ctrl Pts',(1.73313352509794,70.3840751496341,12.2931037723312));
#52140=CARTESIAN_POINT('Ctrl Pts',(1.99094615982158,70.464668067495,12.892271037609));
#52141=CARTESIAN_POINT('Ctrl Pts',(1.98017460809902,70.5785246349932,13.8401174532572));
#52142=CARTESIAN_POINT('Ctrl Pts',(1.37511235343592,70.7133250089865,14.7866139544086));
#52143=CARTESIAN_POINT('Ctrl Pts',(0.375128048534321,70.8464820657692,15.2661514257348));
#52144=CARTESIAN_POINT('Ctrl Pts',(-0.442862949154468,70.9452798994256,
15.1768702880818));
#52145=CARTESIAN_POINT('Ctrl Pts',(-1.07271986066901,71.0325888573339,14.8687929172157));
#52146=CARTESIAN_POINT('Ctrl Pts',(-1.60325302953884,71.1195156735062,14.3937214166867));
#52147=CARTESIAN_POINT('Ctrl Pts',(-1.94329386684104,71.238230764045,13.465985211871));
#52148=CARTESIAN_POINT('Ctrl Pts',(-1.70419247526824,71.3812704329662,12.297859121067));
#52149=CARTESIAN_POINT('Ctrl Pts',(-0.695068394539133,71.537828646783,11.4125559681135));
#52150=CARTESIAN_POINT('Ctrl Pts',(0.767455142864972,71.7081887803066,11.4411332113733));
#52151=CARTESIAN_POINT('Ctrl Pts',(1.82687444435982,71.8786768812991,12.451469255393));
#52152=CARTESIAN_POINT('Ctrl Pts',(1.93180306940232,72.0498248057693,13.9160723142885));
#52153=CARTESIAN_POINT('Ctrl Pts',(1.01274800143708,72.2221959240743,15.0763853677582));
#52154=CARTESIAN_POINT('Ctrl Pts',(-0.463802623258719,72.3962970524919,
15.3172652274182));
#52155=CARTESIAN_POINT('Ctrl Pts',(-1.41174851696204,72.5285808476124,14.6949935892069));
#52156=CARTESIAN_POINT('Ctrl Pts',(-1.77120197887337,72.6176272164111,14.0747773357718));
#52157=CARTESIAN_POINT('Ctrl Pts',(-1.89237232728703,72.6623344317626,13.7360097561691));
#52158=CARTESIAN_POINT('Ctrl Pts',(-1.94839182416811,72.7072228438111,13.3793116458357));
#52159=CARTESIAN_POINT('Ctrl Pts',(-1.93017702510986,72.7973993946095,12.6532690816778));
#52160=CARTESIAN_POINT('Ctrl Pts',(-1.50263901342807,72.9037786179062,11.8496624808967));
#52161=CARTESIAN_POINT('Ctrl Pts',(-0.630581690926918,73.0272027788306,
11.3457210074282));
#52162=CARTESIAN_POINT('Ctrl Pts',(0.205537810305626,73.1311361320603,11.2132845890605));
#52163=CARTESIAN_POINT('Ctrl Pts',(1.12633452278661,73.246925337271,11.4727990344487));
#52164=CARTESIAN_POINT('Ctrl Pts',(1.88802696495275,73.3751787428074,12.2092415047944));
#52165=CARTESIAN_POINT('Ctrl Pts',(2.16788213476735,73.4864771984917,13.0849137392193));
#52166=CARTESIAN_POINT('Ctrl Pts',(2.10875605441894,73.5799628212917,13.839064603789));
#52167=CARTESIAN_POINT('Ctrl Pts',(1.89824583651733,73.6548938780849,14.407528971708));
#52168=CARTESIAN_POINT('Ctrl Pts',(1.53626458253903,73.7305404812233,14.9009329211788));
#52169=CARTESIAN_POINT('Ctrl Pts',(0.886359411788144,73.8323674503564,15.4073073512682));
#52170=CARTESIAN_POINT('Ctrl Pts',(-0.155974258659698,73.9615073445991,
15.6703330193617));
#52171=CARTESIAN_POINT('Ctrl Pts',(-1.4103108874569,74.11954167518,15.2705985126791));
#52172=CARTESIAN_POINT('Ctrl Pts',(-2.28241883663609,74.2807336983208,14.250391442501));
#52173=CARTESIAN_POINT('Ctrl Pts',(-2.49025969304922,74.4451559691366,12.8970113274614));
#52174=CARTESIAN_POINT('Ctrl Pts',(-1.89750274873868,74.6266654271034,11.5063938234114));
#52175=CARTESIAN_POINT('Ctrl Pts',(-0.968179087375076,74.7550741614314,
10.9360195678874));
#52176=CARTESIAN_POINT('Ctrl Pts',(-0.399335820024005,74.8272038040824,
10.8269364066545));
#52177=CARTESIAN_POINT('Ctrl Pts',(-0.232712102076973,66.1500001422474,
10.4337952405977));
#52178=CARTESIAN_POINT('Ctrl Pts',(0.323505159358684,66.2195320956462,10.4019766084206));
#52179=CARTESIAN_POINT('Ctrl Pts',(1.41885650546918,66.3544304567715,10.6673707794366));
#52180=CARTESIAN_POINT('Ctrl Pts',(2.5601329833614,66.5522844135896,11.8558770664517));
#52181=CARTESIAN_POINT('Ctrl Pts',(2.89225673664195,66.7441284736519,13.4185171662456));
#52182=CARTESIAN_POINT('Ctrl Pts',(2.35854209488697,66.9330258398754,14.8982921253924));
#52183=CARTESIAN_POINT('Ctrl Pts',(1.14452779598673,67.1189188109853,15.858546537134));
#52184=CARTESIAN_POINT('Ctrl Pts',(-0.368886136917636,67.3017645672808,
16.0311146214169));
#52185=CARTESIAN_POINT('Ctrl Pts',(-1.7208292711234,67.4815341043535,15.3907835204228));
#52186=CARTESIAN_POINT('Ctrl Pts',(-2.61060558070679,67.6778450412109,14.0173879819278));
#52187=CARTESIAN_POINT('Ctrl Pts',(-2.47388624749099,67.8893805174368,12.2086454666814));
#52188=CARTESIAN_POINT('Ctrl Pts',(-1.06167646901042,68.1146940198439,10.8852381073462));
#52189=CARTESIAN_POINT('Ctrl Pts',(0.824939146135245,68.3346416449378,10.8626410058012));
#52190=CARTESIAN_POINT('Ctrl Pts',(2.20292293912136,68.5493585943811,12.0862717801252));
#52191=CARTESIAN_POINT('Ctrl Pts',(2.38312259731573,68.7590181212548,13.8788181919177));
#52192=CARTESIAN_POINT('Ctrl Pts',(1.42321675441193,68.9467723674098,15.1696260261314));
#52193=CARTESIAN_POINT('Ctrl Pts',(0.0841122076395244,69.114121213424,15.5607304375997));
#52194=CARTESIAN_POINT('Ctrl Pts',(-1.10435554946171,69.2622850508236,15.2329820656295));
#52195=CARTESIAN_POINT('Ctrl Pts',(-1.92886454480659,69.4081347580794,14.3406387637774));
#52196=CARTESIAN_POINT('Ctrl Pts',(-2.15589492821219,69.5518169497582,13.1659981100321));
#52197=CARTESIAN_POINT('Ctrl Pts',(-1.73368924628502,69.6934860371802,12.0645543898351));
#52198=CARTESIAN_POINT('Ctrl Pts',(-0.808056908338198,69.8333100483188,
11.3585939430159));
#52199=CARTESIAN_POINT('Ctrl Pts',(0.337496169984268,69.9714658525598,11.2505370053794));
#52200=CARTESIAN_POINT('Ctrl Pts',(1.10199168624709,70.0739639583279,11.6288124504944));
#52201=CARTESIAN_POINT('Ctrl Pts',(1.4794208139859,70.1418912017691,12.0228157110452));
#52202=CARTESIAN_POINT('Ctrl Pts',(1.69196418541103,70.1870702500522,12.31676674533));
#52203=CARTESIAN_POINT('Ctrl Pts',(1.95099988179501,70.265877979775,12.8994774417758));
#52204=CARTESIAN_POINT('Ctrl Pts',(1.95234057170264,70.3777613097285,13.8307171871858));
#52205=CARTESIAN_POINT('Ctrl Pts',(1.36616071463902,70.5111302178427,14.7747372260413));
#52206=CARTESIAN_POINT('Ctrl Pts',(0.376518429062347,70.6437980414608,15.2656471251188));
#52207=CARTESIAN_POINT('Ctrl Pts',(-0.445266890827574,70.7429376681528,
15.1871923622793));
#52208=CARTESIAN_POINT('Ctrl Pts',(-1.08393108388633,70.8309432285604,14.8848086793263));
#52209=CARTESIAN_POINT('Ctrl Pts',(-1.6268240779312,70.9188802310522,14.4115488637459));
#52210=CARTESIAN_POINT('Ctrl Pts',(-1.98597374383122,71.0397352815001,13.4721919911164));
#52211=CARTESIAN_POINT('Ctrl Pts',(-1.75776001616476,71.1863965767199,12.2715025036978));
#52212=CARTESIAN_POINT('Ctrl Pts',(-0.72856317221135,71.3482357693688,11.341204564793));
#52213=CARTESIAN_POINT('Ctrl Pts',(0.796736434165317,71.525926773327,11.3482292755109));
#52214=CARTESIAN_POINT('Ctrl Pts',(1.92658702317335,71.7052519183896,12.3940355331555));
#52215=CARTESIAN_POINT('Ctrl Pts',(2.06063201142701,71.8866716744668,13.9443662779092));
#52216=CARTESIAN_POINT('Ctrl Pts',(1.09800003567519,72.0706593400645,15.1968247724198));
#52217=CARTESIAN_POINT('Ctrl Pts',(-0.483584678898562,72.2576289765107,
15.4781733998579));
#52218=CARTESIAN_POINT('Ctrl Pts',(-1.51594107605642,72.400417605289,14.8209080799252));
#52219=CARTESIAN_POINT('Ctrl Pts',(-1.91364046970523,72.4967881402075,14.1549274787836));
#52220=CARTESIAN_POINT('Ctrl Pts',(-2.04964515460577,72.5452183807088,13.7897650560395));
#52221=CARTESIAN_POINT('Ctrl Pts',(-2.11538726758662,72.593891541241,13.403882027485));
#52222=CARTESIAN_POINT('Ctrl Pts',(-2.10583383941686,72.6917508546746,12.6159577385697));
#52223=CARTESIAN_POINT('Ctrl Pts',(-1.65259506466878,72.8074223333838,11.7362211740724));
#52224=CARTESIAN_POINT('Ctrl Pts',(-0.709990601959533,72.9418458825809,
11.1754511852134));
#52225=CARTESIAN_POINT('Ctrl Pts',(0.199383467279647,73.055138674421,11.0197089552784));
#52226=CARTESIAN_POINT('Ctrl Pts',(1.20709847264826,73.1814449840387,11.2902860435783));
#52227=CARTESIAN_POINT('Ctrl Pts',(2.04790744246493,73.3214054143136,12.0836804919538));
#52228=CARTESIAN_POINT('Ctrl Pts',(2.36463705500525,73.4428655296851,13.0354647113357));
#52229=CARTESIAN_POINT('Ctrl Pts',(2.30982205012451,73.5448575784662,13.8588149816474));
#52230=CARTESIAN_POINT('Ctrl Pts',(2.08749320339945,73.6265834298673,14.4813690786832));
#52231=CARTESIAN_POINT('Ctrl Pts',(1.69914608640829,73.7090528163163,15.0237069822103));
#52232=CARTESIAN_POINT('Ctrl Pts',(0.997414939924506,73.8200083024837,15.5834484621141));
#52233=CARTESIAN_POINT('Ctrl Pts',(-0.133920474939632,73.9605915715644,
15.8823022870827));
#52234=CARTESIAN_POINT('Ctrl Pts',(-1.50164951944074,74.1323493045711,15.4626328954726));
#52235=CARTESIAN_POINT('Ctrl Pts',(-2.45908764564237,74.3071896509351,14.3661585846542));
#52236=CARTESIAN_POINT('Ctrl Pts',(-2.6989717800723,74.4851213923391,12.9040951113791));
#52237=CARTESIAN_POINT('Ctrl Pts',(-2.07424714095716,74.681031593353,11.3969787136035));
#52238=CARTESIAN_POINT('Ctrl Pts',(-1.08029539867703,74.8191821549513,10.7738526892301));
#52239=CARTESIAN_POINT('Ctrl Pts',(-0.470844590569356,74.8966283641617,
10.6507068346715));
#52240=CARTESIAN_POINT('Ctrl Pts',(-0.253445911442996,66.2173333701116,
10.6236738598046));
#52241=CARTESIAN_POINT('Ctrl Pts',(0.266583620305798,66.2823755770983,10.5895265025299));
#52242=CARTESIAN_POINT('Ctrl Pts',(1.29166587047844,66.4083824504568,10.8291151899761));
#52243=CARTESIAN_POINT('Ctrl Pts',(2.36410827457176,66.5927245680674,11.9275617548428));
#52244=CARTESIAN_POINT('Ctrl Pts',(2.68512601386841,66.7710655264124,13.3774892466885));
#52245=CARTESIAN_POINT('Ctrl Pts',(2.2018692024904,66.9463181215596,14.7545471178109));
#52246=CARTESIAN_POINT('Ctrl Pts',(1.08541296064137,67.1184894155377,15.6537779250861));
#52247=CARTESIAN_POINT('Ctrl Pts',(-0.312761505567944,67.2876014948792,
15.8260114053663));
#52248=CARTESIAN_POINT('Ctrl Pts',(-1.56718192889881,67.4536903367711,15.246004031537));
#52249=CARTESIAN_POINT('Ctrl Pts',(-2.40054805143325,67.6349314251346,13.985920498399));
#52250=CARTESIAN_POINT('Ctrl Pts',(-2.2905908849334,67.8301499959172,12.31566542649));
#52251=CARTESIAN_POINT('Ctrl Pts',(-0.999483270169913,68.0381348071765,
11.0810800462465));
#52252=CARTESIAN_POINT('Ctrl Pts',(0.74335442031871,68.2413733814635,11.0419436127296));
#52253=CARTESIAN_POINT('Ctrl Pts',(2.03105320157515,68.4401407461865,12.1606604191405));
#52254=CARTESIAN_POINT('Ctrl Pts',(2.21709350057343,68.6347436268011,13.8223533656732));
#52255=CARTESIAN_POINT('Ctrl Pts',(1.3370843466063,68.8096308790588,15.0349619665538));
#52256=CARTESIAN_POINT('Ctrl Pts',(0.0893437833835981,68.9661122484503,
15.4152414209954));
#52257=CARTESIAN_POINT('Ctrl Pts',(-1.02968368369404,69.1051813663608,15.1208783866031));
#52258=CARTESIAN_POINT('Ctrl Pts',(-1.81698284773289,69.2426657132616,14.2892494252577));
#52259=CARTESIAN_POINT('Ctrl Pts',(-2.04569699400286,69.3787514487384,13.1795236777241));
#52260=CARTESIAN_POINT('Ctrl Pts',(-1.65692767395016,69.5136284676997,12.1259588979727));
#52261=CARTESIAN_POINT('Ctrl Pts',(-0.779468037852491,69.6474973337496,
11.4389038192792));
#52262=CARTESIAN_POINT('Ctrl Pts',(0.322421329365702,69.7805633459459,11.3205868347935));
#52263=CARTESIAN_POINT('Ctrl Pts',(1.06807493947333,69.8799105432819,11.677521400218));
#52264=CARTESIAN_POINT('Ctrl Pts',(1.44009361307476,69.9460213316832,12.0564432076942));
#52265=CARTESIAN_POINT('Ctrl Pts',(1.65079484572412,69.9900653504704,12.3404297183289));
#52266=CARTESIAN_POINT('Ctrl Pts',(1.91105360376844,70.0670878920549,12.9066838459426));
#52267=CARTESIAN_POINT('Ctrl Pts',(1.92450653530627,70.1769979844637,13.8213169211144));
#52268=CARTESIAN_POINT('Ctrl Pts',(1.35720907584211,70.3089354266989,14.7628604976741));
#52269=CARTESIAN_POINT('Ctrl Pts',(0.377908809590368,70.4411140171526,15.2651428245026));
#52270=CARTESIAN_POINT('Ctrl Pts',(-0.447670832500686,70.54059543688,15.1975144364766));
#52271=CARTESIAN_POINT('Ctrl Pts',(-1.09514230710363,70.6292975997868,14.9008244414368));
#52272=CARTESIAN_POINT('Ctrl Pts',(-1.65039512632356,70.7182447885983,14.4293763108051));
#52273=CARTESIAN_POINT('Ctrl Pts',(-2.0286536208214,70.8412397989554,13.4783987703618));
#52274=CARTESIAN_POINT('Ctrl Pts',(-1.81132755706128,70.9915227204736,12.2451458863287));
#52275=CARTESIAN_POINT('Ctrl Pts',(-0.762057949883573,71.1586428919545,
11.2698531614724));
#52276=CARTESIAN_POINT('Ctrl Pts',(0.826017725465654,71.3436647663474,11.2553253396486));
#52277=CARTESIAN_POINT('Ctrl Pts',(2.0262996019869,71.5318269554803,12.3366018109182));
#52278=CARTESIAN_POINT('Ctrl Pts',(2.1894609534517,71.7235185431642,13.9726602415297));
#52279=CARTESIAN_POINT('Ctrl Pts',(1.18325206991327,71.9191227560546,15.3172641770814));
#52280=CARTESIAN_POINT('Ctrl Pts',(-0.503366734538406,72.1189609005295,
15.6390815722975));
#52281=CARTESIAN_POINT('Ctrl Pts',(-1.6201336351508,72.2722543629655,14.9468225706433));
#52282=CARTESIAN_POINT('Ctrl Pts',(-2.0560789605371,72.3759490640039,14.2350776217954));
#52283=CARTESIAN_POINT('Ctrl Pts',(-2.20691798192451,72.4281023296549,13.84352035591));
#52284=CARTESIAN_POINT('Ctrl Pts',(-2.28238271100513,72.4805602386708,13.4284524091344));
#52285=CARTESIAN_POINT('Ctrl Pts',(-2.28149065372387,72.5861023147396,12.5786463954616));
#52286=CARTESIAN_POINT('Ctrl Pts',(-1.80255111590949,72.7110660488616,11.6227798672479));
#52287=CARTESIAN_POINT('Ctrl Pts',(-0.789399512992146,72.8564889863311,
11.0051813629984));
#52288=CARTESIAN_POINT('Ctrl Pts',(0.193229124253671,72.9791412167817,10.8261333214963));
#52289=CARTESIAN_POINT('Ctrl Pts',(1.28786242250991,73.1159646308063,11.1077730527079));
#52290=CARTESIAN_POINT('Ctrl Pts',(2.20778791997711,73.2676320858199,11.9581194791132));
#52291=CARTESIAN_POINT('Ctrl Pts',(2.56139197524314,73.3992538608785,12.9860156834522));
#52292=CARTESIAN_POINT('Ctrl Pts',(2.51088804583008,73.5097523356408,13.8785653595058));
#52293=CARTESIAN_POINT('Ctrl Pts',(2.27674057028156,73.5982729816497,14.5552091856582));
#52294=CARTESIAN_POINT('Ctrl Pts',(1.86202759027756,73.6875651514094,15.1464810432419));
#52295=CARTESIAN_POINT('Ctrl Pts',(1.10847046806087,73.8076491546109,15.7595895729601));
#52296=CARTESIAN_POINT('Ctrl Pts',(-0.111866691219567,73.9596757985298,
16.0942715548037));
#52297=CARTESIAN_POINT('Ctrl Pts',(-1.59298815142457,74.1451569339621,15.6546672782663));
#52298=CARTESIAN_POINT('Ctrl Pts',(-2.63575645464866,74.3336456035494,14.4819257268073));
#52299=CARTESIAN_POINT('Ctrl Pts',(-2.90768386709537,74.5250868155417,12.911178895297));
#52300=CARTESIAN_POINT('Ctrl Pts',(-2.25099153317564,74.7353977596027,11.2875636037955));
#52301=CARTESIAN_POINT('Ctrl Pts',(-1.19241170997896,74.8832901484711,10.6116858105728));
#52302=CARTESIAN_POINT('Ctrl Pts',(-0.542353361114717,74.9660529242413,
10.4744772626884));
#52303=CARTESIAN_POINT('Ctrl Pts',(-0.274179720809018,66.2846665979758,
10.8135524790114));
#52304=CARTESIAN_POINT('Ctrl Pts',(0.209662081252906,66.3452190585503,10.7770763966391));
#52305=CARTESIAN_POINT('Ctrl Pts',(1.1644752354877,66.462334444142,10.9908596005156));
#52306=CARTESIAN_POINT('Ctrl Pts',(2.1680835657821,66.6331647225451,11.9992464432339));
#52307=CARTESIAN_POINT('Ctrl Pts',(2.47799529109485,66.7980025791729,13.3364613271311));
#52308=CARTESIAN_POINT('Ctrl Pts',(2.04519631009381,66.9596104032439,14.6108021102295));
#52309=CARTESIAN_POINT('Ctrl Pts',(1.026298125296,67.11806002009,15.4490093130383));
#52310=CARTESIAN_POINT('Ctrl Pts',(-0.256636874218245,67.2734384224776,
15.6209081893157));
#52311=CARTESIAN_POINT('Ctrl Pts',(-1.41353458667422,67.4258465691887,15.101224542651));
#52312=CARTESIAN_POINT('Ctrl Pts',(-2.1904905221597,67.5920178090584,13.9544530148703));
#52313=CARTESIAN_POINT('Ctrl Pts',(-2.10729552237581,67.7709194743977,12.4226853862984));
#52314=CARTESIAN_POINT('Ctrl Pts',(-0.937290071329389,67.9615755945092,
11.276921985147));
#52315=CARTESIAN_POINT('Ctrl Pts',(0.661769694502177,68.1481051179891,11.2212462196578));
#52316=CARTESIAN_POINT('Ctrl Pts',(1.85918346402893,68.330922897992,12.2350490581559));
#52317=CARTESIAN_POINT('Ctrl Pts',(2.05106440383111,68.5104691323476,13.765888539429));
#52318=CARTESIAN_POINT('Ctrl Pts',(1.25095193880067,68.6724893907078,14.9002979069763));
#52319=CARTESIAN_POINT('Ctrl Pts',(0.094575359127677,68.8181032834765,15.2697524043909));
#52320=CARTESIAN_POINT('Ctrl Pts',(-0.95501181792635,68.9480776818981,15.0087747075765));
#52321=CARTESIAN_POINT('Ctrl Pts',(-1.70510115065919,69.0771966684437,14.237860086738));
#52322=CARTESIAN_POINT('Ctrl Pts',(-1.93549905979351,69.2056859477188,13.1930492454163));
#52323=CARTESIAN_POINT('Ctrl Pts',(-1.58016610161529,69.3337708982194,12.1873634061102));
#52324=CARTESIAN_POINT('Ctrl Pts',(-0.750879167366774,69.4616846191802,
11.5192136955424));
#52325=CARTESIAN_POINT('Ctrl Pts',(0.307346488747144,69.589660839332,11.3906366642075));
#52326=CARTESIAN_POINT('Ctrl Pts',(1.03415819269958,69.6858571282358,11.7262303499418));
#52327=CARTESIAN_POINT('Ctrl Pts',(1.40076641216363,69.7501514615973,12.0900707043431));
#52328=CARTESIAN_POINT('Ctrl Pts',(1.60962550603721,69.7930604508885,12.3640926913277));
#52329=CARTESIAN_POINT('Ctrl Pts',(1.87110732574187,69.8682978043347,12.9138902501093));
#52330=CARTESIAN_POINT('Ctrl Pts',(1.89667249890989,69.9762346591989,13.8119166550429));
#52331=CARTESIAN_POINT('Ctrl Pts',(1.34825743704521,70.1067406355551,14.7509837693068));
#52332=CARTESIAN_POINT('Ctrl Pts',(0.379299190118395,70.2384299928442,15.2646385238866));
#52333=CARTESIAN_POINT('Ctrl Pts',(-0.450074774173788,70.3382532056071,
15.2078365106741));
#52334=CARTESIAN_POINT('Ctrl Pts',(-1.10635353032094,70.4276519710131,14.9168402035474));
#52335=CARTESIAN_POINT('Ctrl Pts',(-1.67396617471592,70.5176093461441,14.4472037578643));
#52336=CARTESIAN_POINT('Ctrl Pts',(-2.07133349781158,70.6427443164105,13.4846055496071));
#52337=CARTESIAN_POINT('Ctrl Pts',(-1.8648950979578,70.7966488642273,12.2187892689594));
#52338=CARTESIAN_POINT('Ctrl Pts',(-0.79555272755579,70.9690500145402,11.1985017581518));
#52339=CARTESIAN_POINT('Ctrl Pts',(0.855299016765999,71.1614027593676,11.1624214037862));
#52340=CARTESIAN_POINT('Ctrl Pts',(2.12601218080043,71.3584019925708,12.2791680886806));
#52341=CARTESIAN_POINT('Ctrl Pts',(2.31828989547639,71.5603654118617,14.0009542051504));
#52342=CARTESIAN_POINT('Ctrl Pts',(1.26850410415137,71.7675861720447,15.4377035817429));
#52343=CARTESIAN_POINT('Ctrl Pts',(-0.523148790178248,71.9802928245481,
15.7999897447371));
#52344=CARTESIAN_POINT('Ctrl Pts',(-1.72432619424518,72.1440911206419,15.0727370613615));
#52345=CARTESIAN_POINT('Ctrl Pts',(-2.19851745136895,72.2551099878002,14.3152277648071));
#52346=CARTESIAN_POINT('Ctrl Pts',(-2.36419080924325,72.3109862786011,13.8972756557804));
#52347=CARTESIAN_POINT('Ctrl Pts',(-2.44937815442366,72.3672289361006,13.4530227907838));
#52348=CARTESIAN_POINT('Ctrl Pts',(-2.45714746803088,72.4804537748047,12.5413350523533));
#52349=CARTESIAN_POINT('Ctrl Pts',(-1.9525071671502,72.6147097643392,11.5093385604234));
#52350=CARTESIAN_POINT('Ctrl Pts',(-0.868808424024757,72.7711320900814,
10.8349115407836));
#52351=CARTESIAN_POINT('Ctrl Pts',(0.187074781227695,72.9031437591424,10.6325576877142));
#52352=CARTESIAN_POINT('Ctrl Pts',(1.36862637237156,73.0504842775738,10.9252600618375));
#52353=CARTESIAN_POINT('Ctrl Pts',(2.36766839748931,73.2138587573261,11.8325584662726));
#52354=CARTESIAN_POINT('Ctrl Pts',(2.75814689548104,73.355642192072,12.9365666555686));
#52355=CARTESIAN_POINT('Ctrl Pts',(2.71195404153565,73.4746470928152,13.8983157373642));
#52356=CARTESIAN_POINT('Ctrl Pts',(2.46598793716368,73.5699625334321,14.6290492926334));
#52357=CARTESIAN_POINT('Ctrl Pts',(2.02490909414682,73.6660774865024,15.2692551042736));
#52358=CARTESIAN_POINT('Ctrl Pts',(1.21952599619723,73.795290006738,15.935730683806));
#52359=CARTESIAN_POINT('Ctrl Pts',(-0.0898129074995017,73.9587600254952,
16.3062408225249));
#52360=CARTESIAN_POINT('Ctrl Pts',(-1.68432678340842,74.1579645633531,15.8467016610598));
#52361=CARTESIAN_POINT('Ctrl Pts',(-2.81242526365495,74.3601015561637,14.5976928689606));
#52362=CARTESIAN_POINT('Ctrl Pts',(-3.11639595411845,74.5650522387442,12.9182626792148));
#52363=CARTESIAN_POINT('Ctrl Pts',(-2.42773592539411,74.7897639258524,11.1781484939875));
#52364=CARTESIAN_POINT('Ctrl Pts',(-1.30452802128091,74.947398141991,10.4495189319157));
#52365=CARTESIAN_POINT('Ctrl Pts',(-0.613862131660059,75.0354774843205,
10.2982476907052));
#52366=CARTESIAN_POINT('Ctrl Pts',(-0.20632980674377,66.2927243572952,10.8082436938974));
#52367=CARTESIAN_POINT('Ctrl Pts',(-0.128574527433418,66.3024089395535,
10.8044812541815));
#52368=CARTESIAN_POINT('Ctrl Pts',(-0.0506754578630011,66.3120240875613,
10.804265682262));
#52369=CARTESIAN_POINT('Ctrl Pts',(0.0269800873958463,66.3216036971303,
10.8076269268464));
#52370=CARTESIAN_POINT('Ctrl Pts',(0.0605881294274984,66.3257495945027,
10.8090816181875));
#52371=CARTESIAN_POINT('Ctrl Pts',(0.0941500065403234,66.329888771884,10.811205889199));
#52372=CARTESIAN_POINT('Ctrl Pts',(0.127631933618099,66.3340236840922,10.8140003326875));
#52373=CARTESIAN_POINT('Ctrl Pts',(0.207592087260993,66.3438985104337,10.8206739070658));
#52374=CARTESIAN_POINT('Ctrl Pts',(0.28709887183089,66.353750182809,10.8311726784691));
#52375=CARTESIAN_POINT('Ctrl Pts',(0.365733082267086,66.3636214504582,10.8455067276754));
#52376=CARTESIAN_POINT('Ctrl Pts',(0.395837834971989,66.3674006207432,10.8509944537456));
#52377=CARTESIAN_POINT('Ctrl Pts',(0.425814190594611,66.371182595206,10.8570441252314));
#52378=CARTESIAN_POINT('Ctrl Pts',(0.455636808229107,66.3749695193208,10.8636554465057));
#52379=CARTESIAN_POINT('Ctrl Pts',(0.517293924456777,66.3827988394413,10.8773240992452));
#52380=CARTESIAN_POINT('Ctrl Pts',(0.578298801727241,66.3906500383086,10.8933946452472));
#52381=CARTESIAN_POINT('Ctrl Pts',(0.63844465679772,66.3985429049582,10.9118645401074));
#52382=CARTESIAN_POINT('Ctrl Pts',(0.708879361742415,66.4077859647333,10.9334939872791));
#52383=CARTESIAN_POINT('Ctrl Pts',(0.778141127474599,66.4170876831115,10.9584175255254));
#52384=CARTESIAN_POINT('Ctrl Pts',(0.845994629726718,66.4264002712149,10.9864050187958));
#52385=CARTESIAN_POINT('Ctrl Pts',(0.880948989604227,66.4311975999475,11.0008226225948));
#52386=CARTESIAN_POINT('Ctrl Pts',(0.91553040598333,66.4359979173664,11.0160536611649));
#52387=CARTESIAN_POINT('Ctrl Pts',(0.949711354512664,66.4407953576399,11.0320693502863));
#52388=CARTESIAN_POINT('Ctrl Pts',(1.00559245745332,66.4486385060986,11.0582527773404));
#52389=CARTESIAN_POINT('Ctrl Pts',(1.0603979421282,66.4564726611815,11.0865296427796));
#52390=CARTESIAN_POINT('Ctrl Pts',(1.11399609828178,66.4642684761698,11.1167611542193));
#52391=CARTESIAN_POINT('Ctrl Pts',(1.11400306933225,66.4642694901043,11.1167650861716));
#52392=CARTESIAN_POINT('Ctrl Pts',(1.11401004036335,66.4642705040378,11.1167690181557));
#52393=CARTESIAN_POINT('Ctrl Pts',(1.11401701137518,66.4642715179701,11.1167729501718));
#52394=CARTESIAN_POINT('Ctrl Pts',(1.17827799662113,66.4736182663468,11.1530195143464));
#52395=CARTESIAN_POINT('Ctrl Pts',(1.24090219464405,66.4828754714546,11.1919803961549));
#52396=CARTESIAN_POINT('Ctrl Pts',(1.30162376134801,66.492087325675,11.2335589286607));
#52397=CARTESIAN_POINT('Ctrl Pts',(1.33696003876224,66.4974480673998,11.2577551185624));
#52398=CARTESIAN_POINT('Ctrl Pts',(1.37165114866207,66.5027933319895,11.2828372815448));
#52399=CARTESIAN_POINT('Ctrl Pts',(1.40563841799055,66.5081308304738,11.3087812985492));
#52400=CARTESIAN_POINT('Ctrl Pts',(1.49914029805756,66.5228147445684,11.3801555046663));
#52401=CARTESIAN_POINT('Ctrl Pts',(1.58726120625653,66.5374568742704,11.4580964528296));
#52402=CARTESIAN_POINT('Ctrl Pts',(1.6691858726033,66.552055734798,11.5416423539517));
#52403=CARTESIAN_POINT('Ctrl Pts',(1.72792555617097,66.5625230639442,11.6015444568728));
#52404=CARTESIAN_POINT('Ctrl Pts',(1.783478182354,66.5729676196947,11.6643239448273));
#52405=CARTESIAN_POINT('Ctrl Pts',(1.83566700012392,66.5833648758533,11.7295897058178));
#52406=CARTESIAN_POINT('Ctrl Pts',(1.85446199222063,66.5871092861634,11.7530941558977));
#52407=CARTESIAN_POINT('Ctrl Pts',(1.87282091500671,66.5908476195423,11.776921509298));
#52408=CARTESIAN_POINT('Ctrl Pts',(1.89073609827162,66.5945789255838,11.8010550384089));
#52409=CARTESIAN_POINT('Ctrl Pts',(1.94243923882681,66.6053474585016,11.8707042978814));
#52410=CARTESIAN_POINT('Ctrl Pts',(1.99041327308698,66.6160671105291,11.9429260565201));
#52411=CARTESIAN_POINT('Ctrl Pts',(2.03423646585349,66.6267693105913,12.01742935282));
#52412=CARTESIAN_POINT('Ctrl Pts',(2.04177936952561,66.6286113868768,12.0302529549304));
#52413=CARTESIAN_POINT('Ctrl Pts',(2.04919921354728,66.6304529315439,12.0431440616382));
#52414=CARTESIAN_POINT('Ctrl Pts',(2.05649374231333,66.6322940866312,12.0561010755627));
#52415=CARTESIAN_POINT('Ctrl Pts',(2.05651131612243,66.6322985222993,12.0561322912994));
#52416=CARTESIAN_POINT('Ctrl Pts',(2.0565288892047,66.6323029579623,12.0561635074063));
#52417=CARTESIAN_POINT('Ctrl Pts',(2.05654646156012,66.6323073936202,12.0561947238834));
#52418=CARTESIAN_POINT('Ctrl Pts',(2.08973882214424,66.640685892394,12.1151594180502));
#52419=CARTESIAN_POINT('Ctrl Pts',(2.12033951567111,66.6490469766174,12.1754488244082));
#52420=CARTESIAN_POINT('Ctrl Pts',(2.14816376735373,66.6574225110525,12.2368725263844));
#52421=CARTESIAN_POINT('Ctrl Pts',(2.1588245023618,66.6606315588351,12.2604067373832));
#52422=CARTESIAN_POINT('Ctrl Pts',(2.16907744849476,66.6638426595896,12.2841069643975));
#52423=CARTESIAN_POINT('Ctrl Pts',(2.17891157135012,66.6670573505497,12.3079605868637));
#52424=CARTESIAN_POINT('Ctrl Pts',(2.21103541485258,66.6775583612481,12.3858800969552));
#52425=CARTESIAN_POINT('Ctrl Pts',(2.23869378441463,66.6881003976164,12.4654516961015));
#52426=CARTESIAN_POINT('Ctrl Pts',(2.26192857755125,66.6986571054894,12.5461589481352));
#52427=CARTESIAN_POINT('Ctrl Pts',(2.26945233491085,66.7020755180436,12.5722931072771));
#52428=CARTESIAN_POINT('Ctrl Pts',(2.2765122979034,66.7054955185458,12.5985467504864));
#52429=CARTESIAN_POINT('Ctrl Pts',(2.28310993093245,66.708916354768,12.6249035025459));
#52430=CARTESIAN_POINT('Ctrl Pts',(2.29772380927258,66.7164935698316,12.6832841924605));
#52431=CARTESIAN_POINT('Ctrl Pts',(2.31006995575646,66.7240742115067,12.7421670091656));
#52432=CARTESIAN_POINT('Ctrl Pts',(2.32029033489198,66.7316277682419,12.8013610671194));
#52433=CARTESIAN_POINT('Ctrl Pts',(2.32913573241391,66.7381651198549,12.8525915514874));
#52434=CARTESIAN_POINT('Ctrl Pts',(2.33638929861048,66.7446822853669,12.9040559349618));
#52435=CARTESIAN_POINT('Ctrl Pts',(2.34214460101437,66.7511634606035,12.9556617412829));
#52436=CARTESIAN_POINT('Ctrl Pts',(2.35154000132738,66.7617438318113,13.0399070467136));
#52437=CARTESIAN_POINT('Ctrl Pts',(2.35643489871645,66.7723064011337,13.1245139713782));
#52438=CARTESIAN_POINT('Ctrl Pts',(2.35674260359262,66.7828379873103,13.2088734477217));
#52439=CARTESIAN_POINT('Ctrl Pts',(2.35683598286597,66.7860340103197,13.234474038453));
#52440=CARTESIAN_POINT('Ctrl Pts',(2.35650726928768,66.7892271781399,13.2600518228344));
#52441=CARTESIAN_POINT('Ctrl Pts',(2.35575499732339,66.7924171175958,13.2855897940599));
#52442=CARTESIAN_POINT('Ctrl Pts',(2.3553580237854,66.7941004470457,13.299066168658));
#52443=CARTESIAN_POINT('Ctrl Pts',(2.35484311653384,66.7957828491342,13.312531230463));
#52444=CARTESIAN_POINT('Ctrl Pts',(2.35421017337586,66.7974642404135,13.3259823103315));
#52445=CARTESIAN_POINT('Ctrl Pts',(2.35420420852186,66.7974800858387,13.3261090732589));
#52446=CARTESIAN_POINT('Ctrl Pts',(2.35419823318525,66.7974959311742,13.3262358349446));
#52447=CARTESIAN_POINT('Ctrl Pts',(2.35419224736687,66.7975117764198,13.3263625953865));
#52448=CARTESIAN_POINT('Ctrl Pts',(2.3498557505447,66.8089910517747,13.4181956947107));
#52449=CARTESIAN_POINT('Ctrl Pts',(2.34000021559603,66.8204583206326,13.5096570933105));
#52450=CARTESIAN_POINT('Ctrl Pts',(2.32488075766611,66.8318982230755,13.6000526938134));
#52451=CARTESIAN_POINT('Ctrl Pts',(2.31622785363271,66.8384453081924,13.6517863247291));
#52452=CARTESIAN_POINT('Ctrl Pts',(2.30585184672865,66.8449834475544,13.7031710052325));
#52453=CARTESIAN_POINT('Ctrl Pts',(2.29380786495925,66.8515099027997,13.7540788498824));
#52454=CARTESIAN_POINT('Ctrl Pts',(2.27850022461253,66.859804886265,13.818781619419));
#52455=CARTESIAN_POINT('Ctrl Pts',(2.26070184706353,66.8680569366806,13.8827974598016));
#52456=CARTESIAN_POINT('Ctrl Pts',(2.240352918434,66.8762889633602,13.9458858798222));
#52457=CARTESIAN_POINT('Ctrl Pts',(2.21999116305402,66.8845261790181,14.0090140670184));
#52458=CARTESIAN_POINT('Ctrl Pts',(2.19707493853215,66.8927433465053,14.0712134292098));
#52459=CARTESIAN_POINT('Ctrl Pts',(2.171560354261,66.9009568640359,14.1321939171343));
#52460=CARTESIAN_POINT('Ctrl Pts',(2.162848206583,66.9037614316872,14.1530161657208));
#52461=CARTESIAN_POINT('Ctrl Pts',(2.15383329251866,66.906565517488,14.1736958976251));
#52462=CARTESIAN_POINT('Ctrl Pts',(2.14451451176516,66.9093695990993,14.1942203440636));
#52463=CARTESIAN_POINT('Ctrl Pts',(2.12491521274497,66.9152671553818,14.2373874464574));
#52464=CARTESIAN_POINT('Ctrl Pts',(2.10396974110037,66.9211653741846,14.2798728753076));
#52465=CARTESIAN_POINT('Ctrl Pts',(2.08168992125604,66.9270668759013,14.3215809602485));
#52466=CARTESIAN_POINT('Ctrl Pts',(2.05028777690612,66.9353847083651,14.3803661440168));
#52467=CARTESIAN_POINT('Ctrl Pts',(2.01623275577107,66.9437095392524,14.4376089298039));
#52468=CARTESIAN_POINT('Ctrl Pts',(1.97974060707564,66.9520291918567,14.4931656805495));
#52469=CARTESIAN_POINT('Ctrl Pts',(1.96959382145095,66.9543425040201,14.5086134538369));
#52470=CARTESIAN_POINT('Ctrl Pts',(1.95925840028277,66.9566554544955,14.5239310965515));
#52471=CARTESIAN_POINT('Ctrl Pts',(1.94873846627286,66.9589678709832,14.5391160110685));
#52472=CARTESIAN_POINT('Ctrl Pts',(1.94872104198101,66.9589717010661,14.5391411620231));
#52473=CARTESIAN_POINT('Ctrl Pts',(1.94870361719158,66.9589755311455,14.5391663125967));
#52474=CARTESIAN_POINT('Ctrl Pts',(1.94868619190455,66.9589793612212,14.5391914627893));
#52475=CARTESIAN_POINT('Ctrl Pts',(1.89403693194997,66.970991261193,14.6180676049373));
#52476=CARTESIAN_POINT('Ctrl Pts',(1.83449757953572,66.9829673125227,14.6931949198015));
#52477=CARTESIAN_POINT('Ctrl Pts',(1.77072151982188,66.9949079017398,14.7642457570623));
#52478=CARTESIAN_POINT('Ctrl Pts',(1.75846157446336,66.9972032923928,14.7779041640947));
#52479=CARTESIAN_POINT('Ctrl Pts',(1.74604492160895,66.9994973882052,14.7914119831457));
#52480=CARTESIAN_POINT('Ctrl Pts',(1.73347599386595,67.0017902142481,14.8047669541893));
#52481=CARTESIAN_POINT('Ctrl Pts',(1.67720405971062,67.0120553505235,14.8645580570246));
#52482=CARTESIAN_POINT('Ctrl Pts',(1.61794709446245,67.0222902773526,14.9213753155833));
#52483=CARTESIAN_POINT('Ctrl Pts',(1.5559915757977,67.0325046651358,14.9748663003062));
#52484=CARTESIAN_POINT('Ctrl Pts',(1.52958317353144,67.0368585252485,14.9976667137742));
#52485=CARTESIAN_POINT('Ctrl Pts',(1.50268493007333,67.0412085746359,15.0198623253546));
#52486=CARTESIAN_POINT('Ctrl Pts',(1.47532121336855,67.0455552096023,15.0414239960638));
#52487=CARTESIAN_POINT('Ctrl Pts',(1.40606940945473,67.0565556272586,15.0959920435303));
#52488=CARTESIAN_POINT('Ctrl Pts',(1.33384075616785,67.0675334930611,15.1464966187475));
#52489=CARTESIAN_POINT('Ctrl Pts',(1.25917508646185,67.078486108812,15.19268924909));
#52490=CARTESIAN_POINT('Ctrl Pts',(1.23426236182438,67.0821405259134,15.2081017443443));
#52491=CARTESIAN_POINT('Ctrl Pts',(1.20907797401137,67.0857921854888,15.2230344376171));
#52492=CARTESIAN_POINT('Ctrl Pts',(1.18364085068563,67.089441147962,15.2374787195179));
#52493=CARTESIAN_POINT('Ctrl Pts',(1.11822926315564,67.0988244585334,15.2746222045638));
#52494=CARTESIAN_POINT('Ctrl Pts',(1.05119792189493,67.1081888260333,15.3086733309431));
#52495=CARTESIAN_POINT('Ctrl Pts',(0.982784239981919,67.1175391347301,15.339316920084));
#52496=CARTESIAN_POINT('Ctrl Pts',(0.982754689870178,67.117543173435,15.3393301560546));
#52497=CARTESIAN_POINT('Ctrl Pts',(0.982725139490667,67.1175472121386,15.3393433913963));
#52498=CARTESIAN_POINT('Ctrl Pts',(0.982695588843454,67.117551250841,15.3393566261091));
#52499=CARTESIAN_POINT('Ctrl Pts',(0.922109324786144,67.1258316073113,15.3664911182148));
#52500=CARTESIAN_POINT('Ctrl Pts',(0.860393446777788,67.1341074761172,15.3909823791377));
#52501=CARTESIAN_POINT('Ctrl Pts',(0.797780896354277,67.1423763150738,15.4126612129705));
#52502=CARTESIAN_POINT('Ctrl Pts',(0.766596055873062,67.1464946974442,15.4234585845888));
#52503=CARTESIAN_POINT('Ctrl Pts',(0.735189585599855,67.1506112410446,15.4335581944996));
#52504=CARTESIAN_POINT('Ctrl Pts',(0.703595057907955,67.1547250667235,15.4429389996781));
#52505=CARTESIAN_POINT('Ctrl Pts',(0.641949281710978,67.1627517724741,15.4612423913991));
#52506=CARTESIAN_POINT('Ctrl Pts',(0.579580168885443,67.1707690573066,15.4768103078731));
#52507=CARTESIAN_POINT('Ctrl Pts',(0.516718838837556,67.1787729109142,15.4894972302361));
#52508=CARTESIAN_POINT('Ctrl Pts',(0.441872852807582,67.1883027174716,15.5046029432908));
#52509=CARTESIAN_POINT('Ctrl Pts',(0.366326326676958,67.1978137420768,15.5156230006873));
#52510=CARTESIAN_POINT('Ctrl Pts',(0.290532214727299,67.2073042918928,15.522654148052));
#52511=CARTESIAN_POINT('Ctrl Pts',(0.269175928660516,67.2099784164598,15.5246352939568));
#52512=CARTESIAN_POINT('Ctrl Pts',(0.247799672064465,67.212650955634,15.5262997854447));
#52513=CARTESIAN_POINT('Ctrl Pts',(0.226412839104641,67.2153219660869,15.5276498267794));
#52514=CARTESIAN_POINT('Ctrl Pts',(0.153760445636115,67.2243955536886,15.5322360006383));
#52515=CARTESIAN_POINT('Ctrl Pts',(0.0809892877114056,67.2334511436151,
15.5331939577042));
#52516=CARTESIAN_POINT('Ctrl Pts',(0.0084977608233186,67.2424878466249,
15.5306280363472));
#52517=CARTESIAN_POINT('Ctrl Pts',(-0.0171323136797231,67.2456828596333,
15.529720830245));
#52518=CARTESIAN_POINT('Ctrl Pts',(-0.0427278879719226,67.2488755695627,
15.528373252418));
#52519=CARTESIAN_POINT('Ctrl Pts',(-0.0682728697896764,67.2520661270457,
15.5265902350381));
#52520=CARTESIAN_POINT('Ctrl Pts',(-0.124540879855816,67.2590939778326,
15.522662777168));
#52521=CARTESIAN_POINT('Ctrl Pts',(-0.18055920935557,67.2661108894267,15.5166226061125));
#52522=CARTESIAN_POINT('Ctrl Pts',(-0.236146700513096,67.2731171545432,
15.50852728233));
#52523=CARTESIAN_POINT('Ctrl Pts',(-0.236233284555977,67.2731280676236,
15.5085146729129));
#52524=CARTESIAN_POINT('Ctrl Pts',(-0.236319867735188,67.2731389807008,
15.5085020584813));
#52525=CARTESIAN_POINT('Ctrl Pts',(-0.236406450050159,67.273149893775,15.5084894390349));
#52526=CARTESIAN_POINT('Ctrl Pts',(-0.316070580862892,67.2831909808522,
15.4968783239268));
#52527=CARTESIAN_POINT('Ctrl Pts',(-0.395006978126522,67.2932299245716,
15.4810193120499));
#52528=CARTESIAN_POINT('Ctrl Pts',(-0.472747734688077,67.3032562003277,
15.4610162228001));
#52529=CARTESIAN_POINT('Ctrl Pts',(-0.550488491249631,67.3132824760838,
15.4410131335504));
#52530=CARTESIAN_POINT('Ctrl Pts',(-0.627032943894451,67.3232960838948,
15.4168652821069));
#52531=CARTESIAN_POINT('Ctrl Pts',(-0.701871333130362,67.333280333127,15.3887132297439));
#52532=CARTESIAN_POINT('Ctrl Pts',(-0.774821849382517,67.3430127197179,
15.3612713409699));
#52533=CARTESIAN_POINT('Ctrl Pts',(-0.846161267725897,67.3527182757035,
15.3300166603921));
#52534=CARTESIAN_POINT('Ctrl Pts',(-0.915438489116591,67.3623829279607,
15.2950659221268));
#52535=CARTESIAN_POINT('Ctrl Pts',(-0.980872828743778,67.3715114715928,
15.2620539387943));
#52536=CARTESIAN_POINT('Ctrl Pts',(-1.0444799377276,67.3806050676091,15.2257336576489));
#52537=CARTESIAN_POINT('Ctrl Pts',(-1.10599348298211,67.3896757278653,15.1864015641231));
#52538=CARTESIAN_POINT('Ctrl Pts',(-1.16757719813956,67.3987567352304,15.1470246035818));
#52539=CARTESIAN_POINT('Ctrl Pts',(-1.22706311989344,67.4078147542586,15.1046296196428));
#52540=CARTESIAN_POINT('Ctrl Pts',(-1.28422412356873,67.4168682564532,15.0594815636921));
#52541=CARTESIAN_POINT('Ctrl Pts',(-1.2955747325846,67.4186660339069,15.050516396918));
#52542=CARTESIAN_POINT('Ctrl Pts',(-1.30683377813668,67.420463653499,15.0414425531802));
#52543=CARTESIAN_POINT('Ctrl Pts',(-1.31799963780015,67.4222612899385,15.0322619206413));
#52544=CARTESIAN_POINT('Ctrl Pts',(-1.32453057563323,67.4233127317609,15.0268921468678));
#52545=CARTESIAN_POINT('Ctrl Pts',(-1.33102942544951,67.4243641463121,15.0214860540425));
#52546=CARTESIAN_POINT('Ctrl Pts',(-1.33749952549552,67.4254162679058,15.0160475134865));
#52547=CARTESIAN_POINT('Ctrl Pts',(-1.33751806149286,67.4254192820977,15.0160319327733));
#52548=CARTESIAN_POINT('Ctrl Pts',(-1.33753659725431,67.4254222962954,15.0160163517937));
#52549=CARTESIAN_POINT('Ctrl Pts',(-1.33755513278003,67.425425310499,15.0160007705477));
#52550=CARTESIAN_POINT('Ctrl Pts',(-1.40298136426129,67.4360647702156,14.9610024812003));
#52551=CARTESIAN_POINT('Ctrl Pts',(-1.46511058522356,67.4467073549907,14.9022625456091));
#52552=CARTESIAN_POINT('Ctrl Pts',(-1.52353124202221,67.4573366947174,14.8402373390394));
#52553=CARTESIAN_POINT('Ctrl Pts',(-1.54897547923987,67.4619661435509,14.8132231944557));
#52554=CARTESIAN_POINT('Ctrl Pts',(-1.57371600557726,67.4665930088666,14.785586495174));
#52555=CARTESIAN_POINT('Ctrl Pts',(-1.59771806237704,67.4712156094635,14.7573679195037));
#52556=CARTESIAN_POINT('Ctrl Pts',(-1.65325135088431,67.4819108684051,14.692078918772));
#52557=CARTESIAN_POINT('Ctrl Pts',(-1.70487583412141,67.4925918169658,14.6237000370156));
#52558=CARTESIAN_POINT('Ctrl Pts',(-1.75218278013087,67.5032409785434,14.552690583972));
#52559=CARTESIAN_POINT('Ctrl Pts',(-1.77189075024948,67.5076773959379,14.5231082013248));
#52560=CARTESIAN_POINT('Ctrl Pts',(-1.79084902985319,67.512108215328,14.4930697761375));
#52561=CARTESIAN_POINT('Ctrl Pts',(-1.8090267429479,67.5165318258867,14.4626108117319));
#52562=CARTESIAN_POINT('Ctrl Pts',(-1.84335536439334,67.5248858169252,14.4050890402497));
#52563=CARTESIAN_POINT('Ctrl Pts',(-1.87490195828364,67.5332142608485,14.346067564168));
#52564=CARTESIAN_POINT('Ctrl Pts',(-1.9035877123574,67.5415337881176,14.2858085576063));
#52565=CARTESIAN_POINT('Ctrl Pts',(-1.94202078541709,67.5526802616784,14.2050737512026));
#52566=CARTESIAN_POINT('Ctrl Pts',(-1.97537637401675,67.5638241508068,14.1221106450092));
#52567=CARTESIAN_POINT('Ctrl Pts',(-2.00317650316492,67.5749463956344,14.0375344464522));
#52568=CARTESIAN_POINT('Ctrl Pts',(-2.00320023983893,67.5749558921765,14.0374622324835));
#52569=CARTESIAN_POINT('Ctrl Pts',(-2.00322397246332,67.5749653887027,14.0373900173417));
#52570=CARTESIAN_POINT('Ctrl Pts',(-2.00324770103807,67.5749748852127,14.0373178010271));
#52571=CARTESIAN_POINT('Ctrl Pts',(-2.03196544584963,67.5864681314573,13.9499172843105));
#52572=CARTESIAN_POINT('Ctrl Pts',(-2.0547759415268,67.5979492797131,13.8607102695829));
#52573=CARTESIAN_POINT('Ctrl Pts',(-2.07171504811789,67.6094062229046,13.7705530614861));
#52574=CARTESIAN_POINT('Ctrl Pts',(-2.08118435698114,67.6158108897106,13.7201533284704));
#52575=CARTESIAN_POINT('Ctrl Pts',(-2.08881975601745,67.6222079961578,13.6694570053028));
#52576=CARTESIAN_POINT('Ctrl Pts',(-2.09463440220168,67.6285954557751,13.6186151067743));
#52577=CARTESIAN_POINT('Ctrl Pts',(-2.11079879530123,67.6463522383703,13.4772774556597));
#52578=CARTESIAN_POINT('Ctrl Pts',(-2.11295458015199,67.6640480070286,13.3348199791513));
#52579=CARTESIAN_POINT('Ctrl Pts',(-2.10146517596219,67.6816853824547,13.1940825068232));
#52580=CARTESIAN_POINT('Ctrl Pts',(-2.09503340637605,67.6915587869386,13.1152976560862));
#52581=CARTESIAN_POINT('Ctrl Pts',(-2.08420569210718,67.7013817774878,13.0370725157586));
#52582=CARTESIAN_POINT('Ctrl Pts',(-2.06913454676473,67.7111860523834,12.959848535269));
#52583=CARTESIAN_POINT('Ctrl Pts',(-2.06599239843656,67.7132301230411,12.9437482857076));
#52584=CARTESIAN_POINT('Ctrl Pts',(-2.0626656890284,67.7152733992467,12.9276914124349));
#52585=CARTESIAN_POINT('Ctrl Pts',(-2.05915561342543,67.7173161983369,12.9116817033688));
#52586=CARTESIAN_POINT('Ctrl Pts',(-2.03713566130002,67.7301314032656,12.8112471067808));
#52587=CARTESIAN_POINT('Ctrl Pts',(-2.00790429751469,67.7429423660994,12.7125993664872));
#52588=CARTESIAN_POINT('Ctrl Pts',(-1.97153595331814,67.755730975715,12.6169478106865));
#52589=CARTESIAN_POINT('Ctrl Pts',(-1.95784057497515,67.7605468355249,12.5809279072587));
#52590=CARTESIAN_POINT('Ctrl Pts',(-1.94313362391793,67.7653595013681,12.5453330264051));
#52591=CARTESIAN_POINT('Ctrl Pts',(-1.92742097746522,67.7701679189001,12.5102280246347));
#52592=CARTESIAN_POINT('Ctrl Pts',(-1.9273624926875,67.7701858165363,12.5100973586625));
#52593=CARTESIAN_POINT('Ctrl Pts',(-1.92730399397775,67.7702037141136,12.5099666994772));
#52594=CARTESIAN_POINT('Ctrl Pts',(-1.92724548133832,67.770221611632,12.5098360470811));
#52595=CARTESIAN_POINT('Ctrl Pts',(-1.89388268805193,67.78042643594,12.4353405376545));
#52596=CARTESIAN_POINT('Ctrl Pts',(-1.85594606712321,67.7906246373749,12.3629623359507));
#52597=CARTESIAN_POINT('Ctrl Pts',(-1.81390514066782,67.8008029960214,12.2931814052689));
#52598=CARTESIAN_POINT('Ctrl Pts',(-1.78587564941085,67.8075891027689,12.2466571216396));
#52599=CARTESIAN_POINT('Ctrl Pts',(-1.75602455769745,67.8143660326299,12.2012893012407));
#52600=CARTESIAN_POINT('Ctrl Pts',(-1.72449539874654,67.8211312655222,12.15720489228));
#52601=CARTESIAN_POINT('Ctrl Pts',(-1.67186591855563,67.8324240085683,12.0836177873484));
#52602=CARTESIAN_POINT('Ctrl Pts',(-1.61455546875788,67.8436855174882,12.0135978166629));
#52603=CARTESIAN_POINT('Ctrl Pts',(-1.55319430343768,67.854913951671,11.9476584511344));
#52604=CARTESIAN_POINT('Ctrl Pts',(-1.490176702463,67.866445495787,11.8799390621086));
#52605=CARTESIAN_POINT('Ctrl Pts',(-1.42290462552336,67.8779542420573,11.8164900235485));
#52606=CARTESIAN_POINT('Ctrl Pts',(-1.3519086775529,67.8894258700583,11.7578511951201));
#52607=CARTESIAN_POINT('Ctrl Pts',(-1.26422403677566,67.9035940811907,11.6854284054634));
#52608=CARTESIAN_POINT('Ctrl Pts',(-1.17086690995426,67.9177431912997,11.6202438185883));
#52609=CARTESIAN_POINT('Ctrl Pts',(-1.07297991040925,67.9318726891546,11.5633852818377));
#52610=CARTESIAN_POINT('Ctrl Pts',(-1.00587196812349,67.9415593843335,11.5244050350178));
#52611=CARTESIAN_POINT('Ctrl Pts',(-0.936641483811394,67.9512356360637,
11.4893481233654));
#52612=CARTESIAN_POINT('Ctrl Pts',(-0.865781018865037,67.960887828404,11.4586032577573));
#52613=CARTESIAN_POINT('Ctrl Pts',(-0.847384567092266,67.9633936839755,
11.450621424194));
#52614=CARTESIAN_POINT('Ctrl Pts',(-0.828869449365365,67.9658991326647,
11.4429260972646));
#52615=CARTESIAN_POINT('Ctrl Pts',(-0.810245547536746,67.9684040062905,
11.4355179994328));
#52616=CARTESIAN_POINT('Ctrl Pts',(-0.736597453735771,67.9783095120996,
11.4062227266687));
#52617=CARTESIAN_POINT('Ctrl Pts',(-0.661248837710498,67.9882057440261,
11.38142390213));
#52618=CARTESIAN_POINT('Ctrl Pts',(-0.584846569699776,67.998079249931,11.3611449005179));
#52619=CARTESIAN_POINT('Ctrl Pts',(-0.573442856976445,67.9995529578175,
11.3581180805724));
#52620=CARTESIAN_POINT('Ctrl Pts',(-0.562015697016959,68.001026159749,11.3551918633376));
#52621=CARTESIAN_POINT('Ctrl Pts',(-0.550567263942966,68.0024988113496,
11.3523662310898));
#52622=CARTESIAN_POINT('Ctrl Pts',(-0.472904306267075,68.0124888665996,
11.3331979347609));
#52623=CARTESIAN_POINT('Ctrl Pts',(-0.39428703663205,68.0225320115889,11.3184783768812));
#52624=CARTESIAN_POINT('Ctrl Pts',(-0.315215629184613,68.0325840335563,
11.3082877865524));
#52625=CARTESIAN_POINT('Ctrl Pts',(-0.282660584676796,68.0367226221196,
11.3040921470358));
#52626=CARTESIAN_POINT('Ctrl Pts',(-0.25002913617594,68.0408626348629,11.3006644275602));
#52627=CARTESIAN_POINT('Ctrl Pts',(-0.217358653533609,68.0450006500746,
11.298010839096));
#52628=CARTESIAN_POINT('Ctrl Pts',(-0.181681488236276,68.0495194891235,
11.2951130394122));
#52629=CARTESIAN_POINT('Ctrl Pts',(-0.145955374805118,68.0540179908222,
11.2931782964597));
#52630=CARTESIAN_POINT('Ctrl Pts',(-0.110230287715655,68.0584894806757,
11.2922190932064));
#52631=CARTESIAN_POINT('Ctrl Pts',(-0.0423475323296861,68.0669859484711,
11.2903964703632));
#52632=CARTESIAN_POINT('Ctrl Pts',(0.0255381246184789,68.0753844205154,
11.2920980014165));
#52633=CARTESIAN_POINT('Ctrl Pts',(0.0930775806306368,68.0837449761361,
11.2971864971469));
#52634=CARTESIAN_POINT('Ctrl Pts',(0.137346259163022,68.0892248951491,11.3005217473102));
#52635=CARTESIAN_POINT('Ctrl Pts',(0.181467291853591,68.0946886578296,11.3053121976461));
#52636=CARTESIAN_POINT('Ctrl Pts',(0.225353864231717,68.1001546860651,11.3115228668994));
#52637=CARTESIAN_POINT('Ctrl Pts',(0.297516569778419,68.1091424781092,11.3217350724168));
#52638=CARTESIAN_POINT('Ctrl Pts',(0.369075997083405,68.1181922182479,11.335681354184));
#52639=CARTESIAN_POINT('Ctrl Pts',(0.439522592928712,68.127252151519,11.3534441897224));
#52640=CARTESIAN_POINT('Ctrl Pts',(0.476542392403333,68.1320131610317,11.3627785883806));
#52641=CARTESIAN_POINT('Ctrl Pts',(0.513254263083907,68.1367769028364,11.3731663224128));
#52642=CARTESIAN_POINT('Ctrl Pts',(0.549580840090984,68.1415353209377,11.3846147330983));
#52643=CARTESIAN_POINT('Ctrl Pts',(0.564733045808992,68.1435201082725,11.389389988246));
#52644=CARTESIAN_POINT('Ctrl Pts',(0.579817609193851,68.1455038884702,11.3943495590984));
#52645=CARTESIAN_POINT('Ctrl Pts',(0.594828695117815,68.1474864940762,11.3994926536556));
#52646=CARTESIAN_POINT('Ctrl Pts',(0.594906076925064,68.1474967143631,11.3995191661913));
#52647=CARTESIAN_POINT('Ctrl Pts',(0.594983456779897,68.1475069346188,11.3995456836037));
#52648=CARTESIAN_POINT('Ctrl Pts',(0.595060834681638,68.1475171548433,11.3995722058921));
#52649=CARTESIAN_POINT('Ctrl Pts',(0.665877287827978,68.1568707303468,11.423845471988));
#52650=CARTESIAN_POINT('Ctrl Pts',(0.73518618280262,68.1662151610773,11.4522488590251));
#52651=CARTESIAN_POINT('Ctrl Pts',(0.802629491157741,68.1756010542221,11.4843469818994));
#52652=CARTESIAN_POINT('Ctrl Pts',(0.835024812134113,68.1801094187803,11.4997648049364));
#52653=CARTESIAN_POINT('Ctrl Pts',(0.866990480367676,68.1846274397819,11.5160350135853));
#52654=CARTESIAN_POINT('Ctrl Pts',(0.898491049337421,68.189161220833,11.533109553695));
#52655=CARTESIAN_POINT('Ctrl Pts',(0.954629245752853,68.1972410206422,11.563538651255));
#52656=CARTESIAN_POINT('Ctrl Pts',(1.00926548907983,68.2053397654749,11.596575708451));
#52657=CARTESIAN_POINT('Ctrl Pts',(1.06211801029435,68.2133825614083,11.6321386704489));
#52658=CARTESIAN_POINT('Ctrl Pts',(1.0856187251249,68.2169587664658,11.6479516346981));
#52659=CARTESIAN_POINT('Ctrl Pts',(1.1087661791076,68.2205238214085,11.6642636601206));
#52660=CARTESIAN_POINT('Ctrl Pts',(1.13153290330004,68.2240707202695,11.6810656650742));
#52661=CARTESIAN_POINT('Ctrl Pts',(1.19303899423634,68.233652945716,11.7264575991906));
#52662=CARTESIAN_POINT('Ctrl Pts',(1.2517793554944,68.243103398153,11.7754365697995));
#52663=CARTESIAN_POINT('Ctrl Pts',(1.30743930758822,68.2524853875863,11.8275669677571));
#52664=CARTESIAN_POINT('Ctrl Pts',(1.33212184564187,68.2566458531005,11.8506843166397));
#52665=CARTESIAN_POINT('Ctrl Pts',(1.35619901603249,68.2607929394217,11.8744219613097));
#52666=CARTESIAN_POINT('Ctrl Pts',(1.37964491300665,68.2649325665086,11.898744776689));
#52667=CARTESIAN_POINT('Ctrl Pts',(1.43951542026191,68.2755033531079,11.9608545478032));
#52668=CARTESIAN_POINT('Ctrl Pts',(1.49544913426984,68.2861632631523,12.0266391247986));
#52669=CARTESIAN_POINT('Ctrl Pts',(1.54679585661343,68.2968697758467,12.0956172984592));
#52670=CARTESIAN_POINT('Ctrl Pts',(1.56054512482113,68.2997366913553,12.114087794079));
#52671=CARTESIAN_POINT('Ctrl Pts',(1.57396550254669,68.3026069255889,12.1327869891534));
#52672=CARTESIAN_POINT('Ctrl Pts',(1.58704457420983,68.3054796122426,12.1517050167623));
#52673=CARTESIAN_POINT('Ctrl Pts',(1.62490231172075,68.3137946838385,12.2064637750206));
#52674=CARTESIAN_POINT('Ctrl Pts',(1.6598499050247,68.3220977869915,12.2630779089639));
#52675=CARTESIAN_POINT('Ctrl Pts',(1.69159465907481,68.3303776403841,12.3212218319517));
#52676=CARTESIAN_POINT('Ctrl Pts',(1.69162866258708,68.3303865093801,12.3212841130327));
#52677=CARTESIAN_POINT('Ctrl Pts',(1.69166266242805,68.3303953783495,12.3213463958674));
#52678=CARTESIAN_POINT('Ctrl Pts',(1.69169665859768,68.3304042472921,12.3214086804553));
#52679=CARTESIAN_POINT('Ctrl Pts',(1.73837666322693,68.3425821569951,12.4069313990927));
#52680=CARTESIAN_POINT('Ctrl Pts',(1.7784439712871,68.354873351144,12.4959070786658));
#52681=CARTESIAN_POINT('Ctrl Pts',(1.81184444214334,68.3673094571146,12.5871853379815));
#52682=CARTESIAN_POINT('Ctrl Pts',(1.81511395909518,68.3685268069975,12.5961204160962));
#52683=CARTESIAN_POINT('Ctrl Pts',(1.81831963390605,68.3697455484385,12.6050775647659));
#52684=CARTESIAN_POINT('Ctrl Pts',(1.82146144150065,68.3709657130339,12.6140557110386));
#52685=CARTESIAN_POINT('Ctrl Pts',(1.83518482791304,68.3762953806616,12.6532721706269));
#52686=CARTESIAN_POINT('Ctrl Pts',(1.84763132521184,68.3816113175297,12.6929107899243));
#52687=CARTESIAN_POINT('Ctrl Pts',(1.85876621911123,68.3868926362954,12.7328949381302));
#52688=CARTESIAN_POINT('Ctrl Pts',(1.88213228354135,68.3979752416324,12.8167998402876));
#52689=CARTESIAN_POINT('Ctrl Pts',(1.89972274998347,68.4089036487107,12.9022325279816));
#52690=CARTESIAN_POINT('Ctrl Pts',(1.91156292015285,68.4197387381173,12.9883869853891));
#52691=CARTESIAN_POINT('Ctrl Pts',(1.91418807307555,68.4221410487443,13.0074887907206));
#52692=CARTESIAN_POINT('Ctrl Pts',(1.91653048657638,68.4245387945221,13.0266262679722));
#52693=CARTESIAN_POINT('Ctrl Pts',(1.91859030038067,68.4269326771513,13.0457909463844));
#52694=CARTESIAN_POINT('Ctrl Pts',(1.92780694550799,68.4376441145752,13.1315433767914));
#52695=CARTESIAN_POINT('Ctrl Pts',(1.93136651984106,68.4482792579377,13.2178383265643));
#52696=CARTESIAN_POINT('Ctrl Pts',(1.92929849046949,68.4589098962436,13.303852590471));
#52697=CARTESIAN_POINT('Ctrl Pts',(1.92865281765568,68.4622289565248,13.3307076596339));
#52698=CARTESIAN_POINT('Ctrl Pts',(1.92745865079619,68.465547629321,13.3575357406677));
#52699=CARTESIAN_POINT('Ctrl Pts',(1.9257170153009,68.4688682392933,13.3843128006366));
#52700=CARTESIAN_POINT('Ctrl Pts',(1.92063311035048,68.4785612350564,13.4624761293595));
#52701=CARTESIAN_POINT('Ctrl Pts',(1.91088369555087,68.4882716339163,13.540200727461));
#52702=CARTESIAN_POINT('Ctrl Pts',(1.89651268966639,68.4980493886105,13.6168404080137));
#52703=CARTESIAN_POINT('Ctrl Pts',(1.89163960444516,68.5013649416261,13.6428282684088));
#52704=CARTESIAN_POINT('Ctrl Pts',(1.88623536412119,68.5046882787922,13.6686917434138));
#52705=CARTESIAN_POINT('Ctrl Pts',(1.88030238419093,68.5080214676176,13.6944068048617));
#52706=CARTESIAN_POINT('Ctrl Pts',(1.87853989043799,68.5090116486988,13.7020459062393));
#52707=CARTESIAN_POINT('Ctrl Pts',(1.8767307406184,68.5100026769951,13.7096718313121));
#52708=CARTESIAN_POINT('Ctrl Pts',(1.87487500718747,68.5109945955062,13.7172839207466));
#52709=CARTESIAN_POINT('Ctrl Pts',(1.87486545951162,68.5109996988882,13.7173230846487));
#52710=CARTESIAN_POINT('Ctrl Pts',(1.87485591059547,68.5110048022975,13.7173622482144));
#52711=CARTESIAN_POINT('Ctrl Pts',(1.87484636043896,68.5110099057344,13.7174014114436));
#52712=CARTESIAN_POINT('Ctrl Pts',(1.85917391303867,68.5193849879302,13.781670897485));
#52713=CARTESIAN_POINT('Ctrl Pts',(1.84015899201398,68.5278345730983,13.8450380564246));
#52714=CARTESIAN_POINT('Ctrl Pts',(1.81789758862606,68.5362602246994,13.9071800405893));
#52715=CARTESIAN_POINT('Ctrl Pts',(1.80795815696797,68.5400221702877,13.9349256410774));
#52716=CARTESIAN_POINT('Ctrl Pts',(1.79737187952954,68.5437792600655,13.9624263961141));
#52717=CARTESIAN_POINT('Ctrl Pts',(1.78614921560244,68.5475223268054,13.9896508523836));
#52718=CARTESIAN_POINT('Ctrl Pts',(1.74796944304481,68.5602563298663,14.0822691072939));
#52719=CARTESIAN_POINT('Ctrl Pts',(1.70240793878841,68.5728284818333,14.1717234680048));
#52720=CARTESIAN_POINT('Ctrl Pts',(1.65027068966862,68.5852971810842,14.2570857062341));
#52721=CARTESIAN_POINT('Ctrl Pts',(1.6353432564385,68.5888670985363,14.2815257972065));
#52722=CARTESIAN_POINT('Ctrl Pts',(1.61987649583512,68.5924285700032,14.3056305968578));
#52723=CARTESIAN_POINT('Ctrl Pts',(1.60388860643214,68.5959830481571,14.3293786131698));
#52724=CARTESIAN_POINT('Ctrl Pts',(1.54680696873879,68.6086736184419,14.4141662689318));
#52725=CARTESIAN_POINT('Ctrl Pts',(1.48308517939347,68.621276833383,14.4944038412733));
#52726=CARTESIAN_POINT('Ctrl Pts',(1.41360953097037,68.6338621081308,14.5690594159253));
#52727=CARTESIAN_POINT('Ctrl Pts',(1.39411697807346,68.6373931170428,14.5900052835924));
#52728=CARTESIAN_POINT('Ctrl Pts',(1.3741713902224,68.6409227560878,14.6105120462728));
#52729=CARTESIAN_POINT('Ctrl Pts',(1.35379203710025,68.6444526565273,14.6305575735054));
#52730=CARTESIAN_POINT('Ctrl Pts',(1.29005185512864,68.6554930705682,14.6932536534969));
#52731=CARTESIAN_POINT('Ctrl Pts',(1.222070258675,68.6665368844859,14.7514333519707));
#52732=CARTESIAN_POINT('Ctrl Pts',(1.15048022755247,68.6776191296774,14.8043943858278));
#52733=CARTESIAN_POINT('Ctrl Pts',(1.12769732473153,68.6811459575231,14.8212487727968));
#52734=CARTESIAN_POINT('Ctrl Pts',(1.10454900298406,68.6846767030892,14.8375750169322));
#52735=CARTESIAN_POINT('Ctrl Pts',(1.08105568853527,68.688212565933,14.8533515989667));
#52736=CARTESIAN_POINT('Ctrl Pts',(1.08100793061116,68.6882197537425,14.8533836700825));
#52737=CARTESIAN_POINT('Ctrl Pts',(1.08096017123722,68.6882269415754,14.8534157389415));
#52738=CARTESIAN_POINT('Ctrl Pts',(1.08091241041353,68.6882341294314,14.8534478055435));
#52739=CARTESIAN_POINT('Ctrl Pts',(1.04397323247013,68.6937933613285,14.8782487579797));
#52740=CARTESIAN_POINT('Ctrl Pts',(1.00616614155911,68.6993665948157,14.9016999595785));
#52741=CARTESIAN_POINT('Ctrl Pts',(0.967582305246923,68.7049215413284,14.9237450951548));
#52742=CARTESIAN_POINT('Ctrl Pts',(0.876599878534621,68.7180203558135,14.9757285193976));
#52743=CARTESIAN_POINT('Ctrl Pts',(0.781288567449834,68.7310154485496,15.0198988992346));
#52744=CARTESIAN_POINT('Ctrl Pts',(0.68307542716729,68.7439719937914,15.0559590573212));
#52745=CARTESIAN_POINT('Ctrl Pts',(0.6597944733637,68.7470432806921,15.0645069448253));
#52746=CARTESIAN_POINT('Ctrl Pts',(0.636350240894378,68.750112424547,15.0725990593959));
#52747=CARTESIAN_POINT('Ctrl Pts',(0.612761336926078,68.7531803358453,15.080231302944));
#52748=CARTESIAN_POINT('Ctrl Pts',(0.514135265683734,68.7660073853207,15.1121419926873));
#52749=CARTESIAN_POINT('Ctrl Pts',(0.412982668221154,68.7788149252882,15.1360130738438));
#52750=CARTESIAN_POINT('Ctrl Pts',(0.310748511205798,68.791674532808,15.1515415805569));
#52751=CARTESIAN_POINT('Ctrl Pts',(0.284690919064263,68.7949522084659,15.1554995091622));
#52752=CARTESIAN_POINT('Ctrl Pts',(0.258562866953896,68.7982332972666,15.158915640518));
#52753=CARTESIAN_POINT('Ctrl Pts',(0.23238785137156,68.8015190464572,15.1617852813338));
#52754=CARTESIAN_POINT('Ctrl Pts',(0.186079891383616,68.8073320837625,15.1668621536536));
#52755=CARTESIAN_POINT('Ctrl Pts',(0.139627173158232,68.8131594362542,15.1702280817056));
#52756=CARTESIAN_POINT('Ctrl Pts',(0.0931656021664205,68.819006769892,15.1718581172147));
#52757=CARTESIAN_POINT('Ctrl Pts',(0.0931363051828622,68.8190104570087,
15.1718591450561));
#52758=CARTESIAN_POINT('Ctrl Pts',(0.0931070081897869,68.8190141441331,
15.1718601722065));
#52759=CARTESIAN_POINT('Ctrl Pts',(0.0930777111871997,68.819017831265,15.171861198666));
#52760=CARTESIAN_POINT('Ctrl Pts',(0.0168424844714795,68.8286123056233,
15.1745322012442));
#52761=CARTESIAN_POINT('Ctrl Pts',(-0.0594613922952572,68.8382587090525,
15.172524000833));
#52762=CARTESIAN_POINT('Ctrl Pts',(-0.135291198925329,68.8478383066952,
15.1658754378252));
#52763=CARTESIAN_POINT('Ctrl Pts',(-0.169829887171067,68.8522015874578,
15.1628471742015));
#52764=CARTESIAN_POINT('Ctrl Pts',(-0.20426951442597,68.8565509183454,15.1588563460492));
#52765=CARTESIAN_POINT('Ctrl Pts',(-0.238555396103396,68.8608746332391,
15.1539076293075));
#52766=CARTESIAN_POINT('Ctrl Pts',(-0.324231610074392,68.8716790665585,
15.1415413930115));
#52767=CARTESIAN_POINT('Ctrl Pts',(-0.408985156019361,68.8823265393815,
15.1231883931297));
#52768=CARTESIAN_POINT('Ctrl Pts',(-0.492035858729042,68.8929252685954,
15.0991508658813));
#52769=CARTESIAN_POINT('Ctrl Pts',(-0.522655954429459,68.8968329309299,
15.0902884317209));
#52770=CARTESIAN_POINT('Ctrl Pts',(-0.553045033027673,68.9007340325433,
15.0806530445927));
#52771=CARTESIAN_POINT('Ctrl Pts',(-0.58316546096429,68.9046342223475,15.0702588694412));
#52772=CARTESIAN_POINT('Ctrl Pts',(-0.657939331423372,68.9143164316374,
15.044455361339));
#52773=CARTESIAN_POINT('Ctrl Pts',(-0.731054767225249,68.923995341976,15.0139754646491));
#52774=CARTESIAN_POINT('Ctrl Pts',(-0.801855521623986,68.9337441827855,
14.9790783821898));
#52775=CARTESIAN_POINT('Ctrl Pts',(-0.836912412580603,68.9385713071871,
14.9617991423728));
#52776=CARTESIAN_POINT('Ctrl Pts',(-0.871402523768628,68.9434156445553,
14.9434372900059));
#52777=CARTESIAN_POINT('Ctrl Pts',(-0.905250619902248,68.9482864747851,
14.9240259389021));
#52778=CARTESIAN_POINT('Ctrl Pts',(-0.905266930137861,68.948288821871,14.9240165852383));
#52779=CARTESIAN_POINT('Ctrl Pts',(-0.905283240224452,68.948291168963,14.9240072313309));
#52780=CARTESIAN_POINT('Ctrl Pts',(-0.905299550162034,68.9482935160612,
14.9239978771798));
#52781=CARTESIAN_POINT('Ctrl Pts',(-0.970253699103387,68.9576408090992,
14.886745072231));
#52782=CARTESIAN_POINT('Ctrl Pts',(-1.03295147104993,68.9670915532174,14.8455528180476));
#52783=CARTESIAN_POINT('Ctrl Pts',(-1.09292850686405,68.9765452662854,14.8007804210796));
#52784=CARTESIAN_POINT('Ctrl Pts',(-1.11214782069943,68.9795746570497,14.7864333507917));
#52785=CARTESIAN_POINT('Ctrl Pts',(-1.13108766917462,68.9826043180204,14.7717190471577));
#52786=CARTESIAN_POINT('Ctrl Pts',(-1.14973261369638,68.9856308458847,14.7566504437348));
#52787=CARTESIAN_POINT('Ctrl Pts',(-1.21031410155768,68.9954646944571,14.7076892674604));
#52788=CARTESIAN_POINT('Ctrl Pts',(-1.26778845896674,69.0052650179686,14.6549820159269));
#52789=CARTESIAN_POINT('Ctrl Pts',(-1.32169867323303,69.0149270081729,14.5989165098566));
#52790=CARTESIAN_POINT('Ctrl Pts',(-1.37953165188915,69.0252920508809,14.5387714100822));
#52791=CARTESIAN_POINT('Ctrl Pts',(-1.43327523568867,69.0354990150761,14.4747485045646));
#52792=CARTESIAN_POINT('Ctrl Pts',(-1.48247885284466,69.0456765259749,14.4074637756967));
#52793=CARTESIAN_POINT('Ctrl Pts',(-1.49158732613464,69.0475605660422,14.395008163871));
#52794=CARTESIAN_POINT('Ctrl Pts',(-1.50054027425752,69.0494436145655,14.3824406410803));
#52795=CARTESIAN_POINT('Ctrl Pts',(-1.50933489930898,69.0513265115291,14.3697649315476));
#52796=CARTESIAN_POINT('Ctrl Pts',(-1.5489866824539,69.0598158128522,14.3126147423519));
#52797=CARTESIAN_POINT('Ctrl Pts',(-1.58549035758771,69.0684227163165,14.2533140301097));
#52798=CARTESIAN_POINT('Ctrl Pts',(-1.61848591346177,69.0770917173401,14.1922107166905));
#52799=CARTESIAN_POINT('Ctrl Pts',(-1.61850931052721,69.0770978645069,14.1921673884851));
#52800=CARTESIAN_POINT('Ctrl Pts',(-1.6185327058295,69.0771040117048,14.1921240593746));
#52801=CARTESIAN_POINT('Ctrl Pts',(-1.61855609936858,69.0771101589338,14.192080729359));
#52802=CARTESIAN_POINT('Ctrl Pts',(-1.66070022745041,69.0881845673918,14.1140204701822));
#52803=CARTESIAN_POINT('Ctrl Pts',(-1.69710444854914,69.099259015454,14.0328720507928));
#52804=CARTESIAN_POINT('Ctrl Pts',(-1.7275382889765,69.1103228311945,13.9496120546416));
#52805=CARTESIAN_POINT('Ctrl Pts',(-1.73599710152014,69.1133979193875,13.9264706866795));
#52806=CARTESIAN_POINT('Ctrl Pts',(-1.74399497917996,69.1164721865456,13.9031663243045));
#52807=CARTESIAN_POINT('Ctrl Pts',(-1.75152764174066,69.1195454042379,13.8797201735005));
#52808=CARTESIAN_POINT('Ctrl Pts',(-1.78195104824263,69.131957715339,13.7850243377229));
#52809=CARTESIAN_POINT('Ctrl Pts',(-1.80484100416277,69.1444324335709,13.6880260368187));
#52810=CARTESIAN_POINT('Ctrl Pts',(-1.81988876386058,69.1568625540882,13.5899141816979));
#52811=CARTESIAN_POINT('Ctrl Pts',(-1.82183488333921,69.1584701355585,13.577225422961));
#52812=CARTESIAN_POINT('Ctrl Pts',(-1.82364978265495,69.1600769627076,13.5645180883504));
#52813=CARTESIAN_POINT('Ctrl Pts',(-1.82533275185528,69.1616827966858,13.5517947958796));
#52814=CARTESIAN_POINT('Ctrl Pts',(-1.82750250595369,69.1637531048381,13.5353913964719));
#52815=CARTESIAN_POINT('Ctrl Pts',(-1.82945186819067,69.1658199909594,13.5189609076884));
#52816=CARTESIAN_POINT('Ctrl Pts',(-1.83117927532594,69.1678829316276,13.5025085813656));
#52817=CARTESIAN_POINT('Ctrl Pts',(-1.84019634134475,69.1786514828382,13.4166274306009));
#52818=CARTESIAN_POINT('Ctrl Pts',(-1.84317880715676,69.1893342220889,13.3301344567272));
#52819=CARTESIAN_POINT('Ctrl Pts',(-1.84003546593005,69.2000820374621,13.2439078475955));
#52820=CARTESIAN_POINT('Ctrl Pts',(-1.83949636341294,69.2019253544624,13.2291194493048));
#52821=CARTESIAN_POINT('Ctrl Pts',(-1.838777102145,69.2037706015976,13.2143387659784));
#52822=CARTESIAN_POINT('Ctrl Pts',(-1.83787724861594,69.2056185596576,13.1995700790813));
#52823=CARTESIAN_POINT('Ctrl Pts',(-1.83787470789756,69.2056237773301,13.1995283799904));
#52824=CARTESIAN_POINT('Ctrl Pts',(-1.8378721657395,69.2056289950242,13.199486680995));
#52825=CARTESIAN_POINT('Ctrl Pts',(-1.8378696221418,69.2056342127399,13.1994449820954));
#52826=CARTESIAN_POINT('Ctrl Pts',(-1.83209449120491,69.2174808154877,13.1047693951828));
#52827=CARTESIAN_POINT('Ctrl Pts',(-1.81881982165952,69.2293288211434,13.0105424621769));
#52828=CARTESIAN_POINT('Ctrl Pts',(-1.79847145921251,69.2412080594862,12.9179033354241));
#52829=CARTESIAN_POINT('Ctrl Pts',(-1.79176339780701,69.245124181015,12.8873638287473));
#52830=CARTESIAN_POINT('Ctrl Pts',(-1.78428698650568,69.2490437111564,12.8569967182915));
#52831=CARTESIAN_POINT('Ctrl Pts',(-1.77605856810413,69.2529677599195,12.8268422391248));
#52832=CARTESIAN_POINT('Ctrl Pts',(-1.76412320153114,69.2586596144353,12.7831029996854));
#52833=CARTESIAN_POINT('Ctrl Pts',(-1.75060234828232,69.264357284898,12.7398079525592));
#52834=CARTESIAN_POINT('Ctrl Pts',(-1.73552925179681,69.2700398628983,12.6970738834494));
#52835=CARTESIAN_POINT('Ctrl Pts',(-1.72421277786779,69.2743061890544,12.6649902980078));
#52836=CARTESIAN_POINT('Ctrl Pts',(-1.7120214176308,69.2785639695877,12.6332225871527));
#52837=CARTESIAN_POINT('Ctrl Pts',(-1.69897118040291,69.2828169025217,12.6018098352524));
#52838=CARTESIAN_POINT('Ctrl Pts',(-1.68592135101795,69.2870697025441,12.5703980650559));
#52839=CARTESIAN_POINT('Ctrl Pts',(-1.67201256779544,69.2913177462213,12.5393414325066));
#52840=CARTESIAN_POINT('Ctrl Pts',(-1.65726440129855,69.2955608417011,12.5086925894493));
#52841=CARTESIAN_POINT('Ctrl Pts',(-1.62776592614726,69.3040476489664,12.4473904516187));
#52842=CARTESIAN_POINT('Ctrl Pts',(-1.59490854670523,69.3125146766274,12.3877174264648));
#52843=CARTESIAN_POINT('Ctrl Pts',(-1.55885295601687,69.3209949076823,12.3300602016484));
#52844=CARTESIAN_POINT('Ctrl Pts',(-1.54048039462877,69.3253161117638,12.3006802668815));
#52845=CARTESIAN_POINT('Ctrl Pts',(-1.52127756550842,69.3296407416996,12.2718241534475));
#52846=CARTESIAN_POINT('Ctrl Pts',(-1.501269486861,69.3339738588297,12.243546551302));
#52847=CARTESIAN_POINT('Ctrl Pts',(-1.50125417910618,69.3339771740053,12.2435249167109));
#52848=CARTESIAN_POINT('Ctrl Pts',(-1.50123887088004,69.3339804891859,12.2435032824584));
#52849=CARTESIAN_POINT('Ctrl Pts',(-1.5012235621826,69.3339838043714,12.2434816485444));
#52850=CARTESIAN_POINT('Ctrl Pts',(-1.44270312331132,69.3466567385215,12.1607818535739));
#52851=CARTESIAN_POINT('Ctrl Pts',(-1.37727059666993,69.3594023695588,12.0830028973156));
#52852=CARTESIAN_POINT('Ctrl Pts',(-1.30595300121857,69.3720704918851,12.0110840954185));
#52853=CARTESIAN_POINT('Ctrl Pts',(-1.22373895563992,69.3866741472626,11.9281769864546));
#52854=CARTESIAN_POINT('Ctrl Pts',(-1.13368135921862,69.4011774147825,11.8530272603493));
#52855=CARTESIAN_POINT('Ctrl Pts',(-1.03741168707502,69.4156969169235,11.7869269111661));
#52856=CARTESIAN_POINT('Ctrl Pts',(-1.02836624472683,69.4170611608917,11.7807161608393));
#52857=CARTESIAN_POINT('Ctrl Pts',(-1.01926592256557,69.4184255518865,11.774585308269));
#52858=CARTESIAN_POINT('Ctrl Pts',(-1.01011205113707,69.4197901889151,11.7685354310156));
#52859=CARTESIAN_POINT('Ctrl Pts',(-0.927728839566411,69.4320716789841,
11.714087613867));
#52860=CARTESIAN_POINT('Ctrl Pts',(-0.841010321457216,69.4443741814331,
11.666203708608));
#52861=CARTESIAN_POINT('Ctrl Pts',(-0.751025060748099,69.4567556143385,
11.6257067166657));
#52862=CARTESIAN_POINT('Ctrl Pts',(-0.738337487655072,69.4585013484036,
11.6199967977161));
#52863=CARTESIAN_POINT('Ctrl Pts',(-0.725584981363605,69.4602486552138,
11.6144336457452));
#52864=CARTESIAN_POINT('Ctrl Pts',(-0.712770542514273,69.4619977006017,
11.6090194833255));
#52865=CARTESIAN_POINT('Ctrl Pts',(-0.712748839065249,69.4620006629099,
11.6090103135133));
#52866=CARTESIAN_POINT('Ctrl Pts',(-0.712727135438581,69.4620036252231,
11.6090011441285));
#52867=CARTESIAN_POINT('Ctrl Pts',(-0.712705431634265,69.4620065875413,
11.608991975171));
#52868=CARTESIAN_POINT('Ctrl Pts',(-0.68373789530444,69.4659603211094,11.5967543920721));
#52869=CARTESIAN_POINT('Ctrl Pts',(-0.654446042270547,69.4699210624971,
11.5852762013665));
#52870=CARTESIAN_POINT('Ctrl Pts',(-0.624871340462196,69.4738815372614,
11.5745657079349));
#52871=CARTESIAN_POINT('Ctrl Pts',(-0.5038218893111,69.4900917868059,11.5307275871027));
#52872=CARTESIAN_POINT('Ctrl Pts',(-0.378032318714275,69.5062965304003,
11.4997508387732));
#52873=CARTESIAN_POINT('Ctrl Pts',(-0.250354183834203,69.5224717181252,
11.4819724632507));
#52874=CARTESIAN_POINT('Ctrl Pts',(-0.12071941207351,69.5388947867334,11.4639216383754));
#52875=CARTESIAN_POINT('Ctrl Pts',(0.0108627437138111,69.5552872739215,
11.459474420351));
#52876=CARTESIAN_POINT('Ctrl Pts',(0.141436553988745,69.5716444458873,11.4689754951994));
#52877=CARTESIAN_POINT('Ctrl Pts',(0.153514045885899,69.573157410941,11.4698543020157));
#52878=CARTESIAN_POINT('Ctrl Pts',(0.165582926188795,69.5746700887724,11.4708524507153));
#52879=CARTESIAN_POINT('Ctrl Pts',(0.177640863840469,69.5761824848123,11.4719702206754));
#52880=CARTESIAN_POINT('Ctrl Pts',(0.216070703669195,69.581002640568,11.4755326640861));
#52881=CARTESIAN_POINT('Ctrl Pts',(0.254389918738245,69.5858200152393,11.4803103128853));
#52882=CARTESIAN_POINT('Ctrl Pts',(0.29251715287334,69.5906438953241,11.4863076060511));
#52883=CARTESIAN_POINT('Ctrl Pts',(0.292527528266156,69.590645208025,11.4863092380675));
#52884=CARTESIAN_POINT('Ctrl Pts',(0.292537903645354,69.5906465207263,11.4863108701744));
#52885=CARTESIAN_POINT('Ctrl Pts',(0.292548279010891,69.5906478334283,11.4863125023716));
#52886=CARTESIAN_POINT('Ctrl Pts',(0.388751094272645,69.6028195128875,11.5014466165791));
#52887=CARTESIAN_POINT('Ctrl Pts',(0.483781469591908,69.6150409052945,11.5243562069561));
#52888=CARTESIAN_POINT('Ctrl Pts',(0.576463822122927,69.6272495061805,11.5545531893843));
#52889=CARTESIAN_POINT('Ctrl Pts',(0.682512323524433,69.6412187656222,11.5891050177087));
#52890=CARTESIAN_POINT('Ctrl Pts',(0.785493577277762,69.6551694244689,11.633191059219));
#52891=CARTESIAN_POINT('Ctrl Pts',(0.883813285938799,69.6690842139963,11.6861095460118));
#52892=CARTESIAN_POINT('Ctrl Pts',(0.905440101635131,69.6721449694914,11.6977497184287));
#52893=CARTESIAN_POINT('Ctrl Pts',(0.926841273950825,69.6752039869934,11.7098174162052));
#52894=CARTESIAN_POINT('Ctrl Pts',(0.947999644255617,69.6782610787044,11.7223054517188));
#52895=CARTESIAN_POINT('Ctrl Pts',(0.977334911426482,69.6824996188573,11.7396196329603));
#52896=CARTESIAN_POINT('Ctrl Pts',(1.0062044211962,69.6867347405138,11.7577423413469));
#52897=CARTESIAN_POINT('Ctrl Pts',(1.03456180279423,69.690973810479,11.776651724978));
#52898=CARTESIAN_POINT('Ctrl Pts',(1.06292010858455,69.6952130185992,11.7955617248828));
#52899=CARTESIAN_POINT('Ctrl Pts',(1.09076538640764,69.6994561467566,11.8152581911504));
#52900=CARTESIAN_POINT('Ctrl Pts',(1.11803848669445,69.7036964996888,11.8357132175244));
#52901=CARTESIAN_POINT('Ctrl Pts',(1.15077513339974,69.7087863110557,11.8602659440098));
#52902=CARTESIAN_POINT('Ctrl Pts',(1.18269098424645,69.7138745411377,11.8859129245652));
#52903=CARTESIAN_POINT('Ctrl Pts',(1.21371105698516,69.7189734331952,11.912617539152));
#52904=CARTESIAN_POINT('Ctrl Pts',(1.23438455871875,69.7223716184503,11.9304149795578));
#52905=CARTESIAN_POINT('Ctrl Pts',(1.2546601880194,69.7257745416328,11.9486822204782));
#52906=CARTESIAN_POINT('Ctrl Pts',(1.27452332141809,69.7291858428091,11.967395862835));
#52907=CARTESIAN_POINT('Ctrl Pts',(1.31715055371471,69.7365066579474,12.007556232493));
#52908=CARTESIAN_POINT('Ctrl Pts',(1.35787582192742,69.7438593168303,12.0497730907761));
#52909=CARTESIAN_POINT('Ctrl Pts',(1.39653348139712,69.7512108225702,12.0938224692718));
#52910=CARTESIAN_POINT('Ctrl Pts',(1.40333686633492,69.7525046185244,12.1015747461113));
#52911=CARTESIAN_POINT('Ctrl Pts',(1.41007620558189,69.7537983776909,12.1093837751367));
#52912=CARTESIAN_POINT('Ctrl Pts',(1.41675059216139,69.7550919204249,12.1172485883696));
#52913=CARTESIAN_POINT('Ctrl Pts',(1.46052910805424,69.7635765025607,12.1688353292648));
#52914=CARTESIAN_POINT('Ctrl Pts',(1.50151284102932,69.7720536819369,12.2228206859292));
#52915=CARTESIAN_POINT('Ctrl Pts',(1.53944830035807,69.7804859331021,12.2789293798705));
#52916=CARTESIAN_POINT('Ctrl Pts',(1.54389162139629,69.7814735894971,12.2855013034646));
#52917=CARTESIAN_POINT('Ctrl Pts',(1.54829317003369,69.7824606371911,12.2921024302378));
#52918=CARTESIAN_POINT('Ctrl Pts',(1.55265261989843,69.7834471680316,12.298732390422));
#52919=CARTESIAN_POINT('Ctrl Pts',(1.55266401720386,69.7834497472087,12.2987497237287));
#52920=CARTESIAN_POINT('Ctrl Pts',(1.55267541421877,69.7834523263782,12.2987670572298));
#52921=CARTESIAN_POINT('Ctrl Pts',(1.55268681094315,69.7834549055402,12.2987843909253));
#52922=CARTESIAN_POINT('Ctrl Pts',(1.59993576317875,69.794147688385,12.3706470530331));
#52923=CARTESIAN_POINT('Ctrl Pts',(1.64219334337782,69.8047098714146,12.4458491507882));
#52924=CARTESIAN_POINT('Ctrl Pts',(1.67908667743357,69.8152487412729,12.5236951541159));
#52925=CARTESIAN_POINT('Ctrl Pts',(1.71597474371204,69.8257861063493,12.601530042281));
#52926=CARTESIAN_POINT('Ctrl Pts',(1.74749420336776,69.8363010435062,12.682011004518));
#52927=CARTESIAN_POINT('Ctrl Pts',(1.77322308422684,69.8469495522407,12.7643046379956));
#52928=CARTESIAN_POINT('Ctrl Pts',(1.77323296526681,69.8469536417439,12.7643362424282));
#52929=CARTESIAN_POINT('Ctrl Pts',(1.7732428454533,69.8469577312668,12.7643678471283));
#52930=CARTESIAN_POINT('Ctrl Pts',(1.77325272478628,69.8469618208095,12.7643994520956));
#52931=CARTESIAN_POINT('Ctrl Pts',(1.79992357399828,69.8580021993299,12.8497221475336));
#52932=CARTESIAN_POINT('Ctrl Pts',(1.82039847299613,69.8691749690202,12.937104973935));
#52933=CARTESIAN_POINT('Ctrl Pts',(1.83456353934237,69.880353384387,13.0255553584996));
#52934=CARTESIAN_POINT('Ctrl Pts',(1.84872059399211,69.8915254772934,13.1139557159326));
#52935=CARTESIAN_POINT('Ctrl Pts',(1.85658086837671,69.9027139196788,13.2034183259347));
#52936=CARTESIAN_POINT('Ctrl Pts',(1.85811281102288,69.914042475166,13.2930013745112));
#52937=CARTESIAN_POINT('Ctrl Pts',(1.85961737215055,69.9251685471905,13.3809832404928));
#52938=CARTESIAN_POINT('Ctrl Pts',(1.85500143945498,69.9363253476092,13.4690832168717));
#52939=CARTESIAN_POINT('Ctrl Pts',(1.84420378027491,69.9474653598375,13.5564675180094));
#52940=CARTESIAN_POINT('Ctrl Pts',(1.8345395353106,69.95743602156,13.6346792190963));
#52941=CARTESIAN_POINT('Ctrl Pts',(1.81992454299468,69.9673932662656,13.7123189970479));
#52942=CARTESIAN_POINT('Ctrl Pts',(1.80028811406486,69.9773093570152,13.7888228408032));
#52943=CARTESIAN_POINT('Ctrl Pts',(1.80028560513862,69.9773106239838,13.7888326156203));
#52944=CARTESIAN_POINT('Ctrl Pts',(1.80028309613099,69.9773118909515,13.7888423904164));
#52945=CARTESIAN_POINT('Ctrl Pts',(1.80028058704198,69.9773131579182,13.7888521651914));
#52946=CARTESIAN_POINT('Ctrl Pts',(1.79446016413059,69.9802521855423,13.8115270580995));
#52947=CARTESIAN_POINT('Ctrl Pts',(1.78820186104656,69.9831858509615,13.8340887284314));
#52948=CARTESIAN_POINT('Ctrl Pts',(1.78151353793073,69.9861135095289,13.8565259325416));
#52949=CARTESIAN_POINT('Ctrl Pts',(1.75782960471734,69.9964806028617,13.935978021569));
#52950=CARTESIAN_POINT('Ctrl Pts',(1.7287544737392,70.0067732359488,14.0138794677029));
#52951=CARTESIAN_POINT('Ctrl Pts',(1.69462535931963,70.0170483962411,14.0896684836126));
#52952=CARTESIAN_POINT('Ctrl Pts',(1.69183469961894,70.0178885726193,14.0958655782648));
#52953=CARTESIAN_POINT('Ctrl Pts',(1.68901022154927,70.0187286324704,14.1020485413191));
#52954=CARTESIAN_POINT('Ctrl Pts',(1.68615209497705,70.0195686071028,14.1082170607523));
#52955=CARTESIAN_POINT('Ctrl Pts',(1.64842455736105,70.030656350678,14.1896420932248));
#52956=CARTESIAN_POINT('Ctrl Pts',(1.60483464544317,70.0417295703943,14.2685507960509));
#52957=CARTESIAN_POINT('Ctrl Pts',(1.55581371265823,70.0528476944124,14.3441219594759));
#52958=CARTESIAN_POINT('Ctrl Pts',(1.50732926037688,70.0638441427212,14.4188660791564));
#52959=CARTESIAN_POINT('Ctrl Pts',(1.45352846295804,70.0748846241759,14.4903420632944));
#52960=CARTESIAN_POINT('Ctrl Pts',(1.39490150108386,70.0860110902979,14.557678414196));
#52961=CARTESIAN_POINT('Ctrl Pts',(1.35786942450768,70.0930391902076,14.6002118292534));
#52962=CARTESIAN_POINT('Ctrl Pts',(1.3189135161113,70.1001012649247,14.6410920456838));
#52963=CARTESIAN_POINT('Ctrl Pts',(1.27818060303822,70.1072045904037,14.6800943415359));
#52964=CARTESIAN_POINT('Ctrl Pts',(1.27816250885692,70.1072077458092,14.6801116669507));
#52965=CARTESIAN_POINT('Ctrl Pts',(1.27814441432512,70.1072109012229,14.680128991995));
#52966=CARTESIAN_POINT('Ctrl Pts',(1.27812631944288,70.1072140566447,14.680146316669));
#52967=CARTESIAN_POINT('Ctrl Pts',(1.22493024275396,70.116490495039,14.7310781035215));
#52968=CARTESIAN_POINT('Ctrl Pts',(1.16856508890574,70.1257915775979,14.7789302298088));
#52969=CARTESIAN_POINT('Ctrl Pts',(1.10954585560057,70.1350925529722,14.8233679525907));
#52970=CARTESIAN_POINT('Ctrl Pts',(1.09646681096988,70.137153709399,14.8332156399801));
#52971=CARTESIAN_POINT('Ctrl Pts',(1.08325756611831,70.1392148600082,14.8428957953405));
#52972=CARTESIAN_POINT('Ctrl Pts',(1.06992394830663,70.1412757345038,14.8524050373711));
#52973=CARTESIAN_POINT('Ctrl Pts',(0.996965772678296,70.1525523171633,14.904437198482));
#52974=CARTESIAN_POINT('Ctrl Pts',(0.920283437593562,70.1638204440748,14.951352796264));
#52975=CARTESIAN_POINT('Ctrl Pts',(0.840676818107517,70.175061902439,14.9927205550713));
#52976=CARTESIAN_POINT('Ctrl Pts',(0.795391524750961,70.181456756825,15.0162531595856));
#52977=CARTESIAN_POINT('Ctrl Pts',(0.749157050823362,70.1878434907123,15.0379927628673));
#52978=CARTESIAN_POINT('Ctrl Pts',(0.702094673609501,70.1942225345618,15.0578681942149));
#52979=CARTESIAN_POINT('Ctrl Pts',(0.618921025038079,70.2054962606836,15.0929941746686));
#52980=CARTESIAN_POINT('Ctrl Pts',(0.533133877493328,70.2167497624942,15.1223069293621));
#52981=CARTESIAN_POINT('Ctrl Pts',(0.445527765571953,70.2279938296179,15.1453246978411));
#52982=CARTESIAN_POINT('Ctrl Pts',(0.41604327251346,70.2317781046164,15.1530715002052));
#52983=CARTESIAN_POINT('Ctrl Pts',(0.386355096314788,70.235560989632,15.1601045217764));
#52984=CARTESIAN_POINT('Ctrl Pts',(0.356501118187787,70.2393419128353,15.1664045404908));
#52985=CARTESIAN_POINT('Ctrl Pts',(0.356497694570308,70.2393423464269,15.1664052629692));
#52986=CARTESIAN_POINT('Ctrl Pts',(0.356494270950439,70.2393427800186,15.166405985438));
#52987=CARTESIAN_POINT('Ctrl Pts',(0.356490847328433,70.2393432136104,15.1664067078971));
#52988=CARTESIAN_POINT('Ctrl Pts',(0.26518298974908,70.2509070882866,15.185674663696));
#52989=CARTESIAN_POINT('Ctrl Pts',(0.172264435215834,70.2625249530684,15.198098086844));
#52990=CARTESIAN_POINT('Ctrl Pts',(0.0787817346057373,70.2741829872538,
15.2037064118793));
#52991=CARTESIAN_POINT('Ctrl Pts',(-0.0156222507291631,70.2859559129512,
15.2093700077205));
#52992=CARTESIAN_POINT('Ctrl Pts',(-0.110600567102631,70.2977695714574,
15.2080845097316));
#52993=CARTESIAN_POINT('Ctrl Pts',(-0.205096011477666,70.3096120876114,
15.1998951032177));
#52994=CARTESIAN_POINT('Ctrl Pts',(-0.297223970214025,70.3211579017698,
15.191910873815));
#52995=CARTESIAN_POINT('Ctrl Pts',(-0.388892914324814,70.3327309933088,
15.177365559377));
#52996=CARTESIAN_POINT('Ctrl Pts',(-0.479149317467216,70.3443253752098,
15.1562983448823));
#52997=CARTESIAN_POINT('Ctrl Pts',(-0.551891956122537,70.3536699303183,
15.1393191088603));
#52998=CARTESIAN_POINT('Ctrl Pts',(-0.62371763751532,70.3630283842836,15.118103776966));
#52999=CARTESIAN_POINT('Ctrl Pts',(-0.694139123852421,70.3724009765456,
15.0926628341088));
#53000=CARTESIAN_POINT('Ctrl Pts',(-0.764864088097802,70.3818139595299,
15.0671122547682));
#53001=CARTESIAN_POINT('Ctrl Pts',(-0.834160445598943,70.391216549276,15.0373047095698));
#53002=CARTESIAN_POINT('Ctrl Pts',(-0.901575673922172,70.4006539779655,
15.0034955940613));
#53003=CARTESIAN_POINT('Ctrl Pts',(-0.913682702578334,70.4023488356768,
14.997423851215));
#53004=CARTESIAN_POINT('Ctrl Pts',(-0.92572935864844,70.4040448559331,14.9912229041927));
#53005=CARTESIAN_POINT('Ctrl Pts',(-0.937713386497447,70.4057423488503,
14.9848940070625));
#53006=CARTESIAN_POINT('Ctrl Pts',(-0.938294742236985,70.4058246957259,
14.9845869866918));
#53007=CARTESIAN_POINT('Ctrl Pts',(-0.938875950619259,70.4059070460711,
14.9842796651939));
#53008=CARTESIAN_POINT('Ctrl Pts',(-0.939457011373071,70.4059893998935,
14.9839720427189));
#53009=CARTESIAN_POINT('Ctrl Pts',(-0.939465540023992,70.4059906086604,
14.9839675275203));
#53010=CARTESIAN_POINT('Ctrl Pts',(-0.939474068641808,70.4059918174268,
14.9839630122576));
#53011=CARTESIAN_POINT('Ctrl Pts',(-0.939482597226596,70.4059930261928,
14.9839584969309));
#53012=CARTESIAN_POINT('Ctrl Pts',(-1.00939412915963,70.4159016668488,14.9469449221697));
#53013=CARTESIAN_POINT('Ctrl Pts',(-1.07708576410025,70.4257798249436,14.9056298077126));
#53014=CARTESIAN_POINT('Ctrl Pts',(-1.14215186022346,70.4356567711562,14.8602973421181));
#53015=CARTESIAN_POINT('Ctrl Pts',(-1.20733991421339,70.4455522304097,14.8148799067602));
#53016=CARTESIAN_POINT('Ctrl Pts',(-1.26989112231966,70.4554464180391,14.7654263960899));
#53017=CARTESIAN_POINT('Ctrl Pts',(-1.32930124400838,70.4653537079032,14.7122515857891));
#53018=CARTESIAN_POINT('Ctrl Pts',(-1.38859276529357,70.4752412198483,14.659182928342));
#53019=CARTESIAN_POINT('Ctrl Pts',(-1.44475293254124,70.4851415401354,14.6024050340269));
#53020=CARTESIAN_POINT('Ctrl Pts',(-1.49721656075818,70.4950561567261,14.5423079518511));
#53021=CARTESIAN_POINT('Ctrl Pts',(-1.51814295636831,70.4990108429754,14.518336767254));
#53022=CARTESIAN_POINT('Ctrl Pts',(-1.53848075620142,70.5029676821934,14.4938385830972));
#53023=CARTESIAN_POINT('Ctrl Pts',(-1.55819304826531,70.5069263743563,14.4688428834298));
#53024=CARTESIAN_POINT('Ctrl Pts',(-1.55820491784598,70.5069287580475,14.4688278324924));
#53025=CARTESIAN_POINT('Ctrl Pts',(-1.55821678719993,70.5069311417393,14.4688127813746));
#53026=CARTESIAN_POINT('Ctrl Pts',(-1.5582286563271,70.5069335254318,14.4687977300765));
#53027=CARTESIAN_POINT('Ctrl Pts',(-1.60608790998573,70.5165451625486,14.4081071769877));
#53028=CARTESIAN_POINT('Ctrl Pts',(-1.65037144160631,70.5261963929361,14.3443353252483));
#53029=CARTESIAN_POINT('Ctrl Pts',(-1.69077538048006,70.5358717255455,14.2780585430121));
#53030=CARTESIAN_POINT('Ctrl Pts',(-1.69503801462446,70.5368924775882,14.2710663119867));
#53031=CARTESIAN_POINT('Ctrl Pts',(-1.69925750474247,70.5379134977626,14.2640462300519));
#53032=CARTESIAN_POINT('Ctrl Pts',(-1.7034335209034,70.5389347677829,14.2569989939056));
#53033=CARTESIAN_POINT('Ctrl Pts',(-1.74721911509653,70.5496427997798,14.1831086136498));
#53034=CARTESIAN_POINT('Ctrl Pts',(-1.78622351033457,70.5603785454426,14.1062323600374));
#53035=CARTESIAN_POINT('Ctrl Pts',(-1.82013061855966,70.5711368687535,14.027094074813));
#53036=CARTESIAN_POINT('Ctrl Pts',(-1.85399094680987,70.5818803493332,13.9480649728009));
#53037=CARTESIAN_POINT('Ctrl Pts',(-1.88277186781581,70.592646729472,13.8667814792335));
#53038=CARTESIAN_POINT('Ctrl Pts',(-1.90619754185183,70.6034421128268,13.7838715555113));
#53039=CARTESIAN_POINT('Ctrl Pts',(-1.91915314766995,70.6094125165465,13.7380180919779));
#53040=CARTESIAN_POINT('Ctrl Pts',(-1.93047113420154,70.6153919626634,13.6916653440043));
#53041=CARTESIAN_POINT('Ctrl Pts',(-1.94010317057641,70.6213821810444,13.6449060603244));
#53042=CARTESIAN_POINT('Ctrl Pts',(-1.95201614892721,70.6287909302551,13.5870738104761));
#53043=CARTESIAN_POINT('Ctrl Pts',(-1.9613503006164,70.6362166060507,13.5286148927615));
#53044=CARTESIAN_POINT('Ctrl Pts',(-1.96800620138842,70.6436261756634,13.4697421946718));
#53045=CARTESIAN_POINT('Ctrl Pts',(-1.98416216515208,70.661611530654,13.3268396470551));
#53046=CARTESIAN_POINT('Ctrl Pts',(-1.98448596022075,70.6796484252118,13.1816590285085));
#53047=CARTESIAN_POINT('Ctrl Pts',(-1.96926429907825,70.6977348846467,13.0377052164726));
#53048=CARTESIAN_POINT('Ctrl Pts',(-1.9532151699708,70.7168045459569,12.8859259005856));
#53049=CARTESIAN_POINT('Ctrl Pts',(-1.91988458772862,70.7359289508103,12.7355123366635));
#53050=CARTESIAN_POINT('Ctrl Pts',(-1.8696091510795,70.7551146490957,12.590575892318));
#53051=CARTESIAN_POINT('Ctrl Pts',(-1.8581578190305,70.7594846121691,12.5575634420874));
#53052=CARTESIAN_POINT('Ctrl Pts',(-1.84582736992532,70.7638578024727,12.5248350970751));
#53053=CARTESIAN_POINT('Ctrl Pts',(-1.83262171414446,70.7682343868168,12.4924393355125));
#53054=CARTESIAN_POINT('Ctrl Pts',(-1.81839550540839,70.7729492001864,12.4575399807359));
#53055=CARTESIAN_POINT('Ctrl Pts',(-1.80315332895003,70.777668016289,12.4230260852078));
#53056=CARTESIAN_POINT('Ctrl Pts',(-1.78690283692899,70.7823825107768,12.3889586203893));
#53057=CARTESIAN_POINT('Ctrl Pts',(-1.78690182115909,70.7823828054659,12.3889564909334));
#53058=CARTESIAN_POINT('Ctrl Pts',(-1.78690080538529,70.7823831001548,12.3889543614794));
#53059=CARTESIAN_POINT('Ctrl Pts',(-1.78689978960751,70.7823833948438,12.388952232027));
#53060=CARTESIAN_POINT('Ctrl Pts',(-1.74550545441033,70.7943923745589,12.3021741327641));
#53061=CARTESIAN_POINT('Ctrl Pts',(-1.6975318256225,70.8063799624736,12.218222764267));
#53062=CARTESIAN_POINT('Ctrl Pts',(-1.64368964950784,70.8183742497046,12.1379277482001));
#53063=CARTESIAN_POINT('Ctrl Pts',(-1.63290887041808,70.8207758569633,12.1218503365371));
#53064=CARTESIAN_POINT('Ctrl Pts',(-1.62189296865058,70.8231777298505,12.1059194580783));
#53065=CARTESIAN_POINT('Ctrl Pts',(-1.61064787764368,70.8255800893088,12.0901416761132));
#53066=CARTESIAN_POINT('Ctrl Pts',(-1.54009393665742,70.8406529710973,11.9911487291488));
#53067=CARTESIAN_POINT('Ctrl Pts',(-1.4605174170031,70.8557465159916,11.8981815621156));
#53068=CARTESIAN_POINT('Ctrl Pts',(-1.37328510870703,70.8709351750474,11.8127095566969));
#53069=CARTESIAN_POINT('Ctrl Pts',(-1.30099894827056,70.883521450325,11.7418820936019));
#53070=CARTESIAN_POINT('Ctrl Pts',(-1.22345672961429,70.8961742533405,11.6761972236881));
#53071=CARTESIAN_POINT('Ctrl Pts',(-1.14135866360981,70.9089326401881,11.6164470701242));
#53072=CARTESIAN_POINT('Ctrl Pts',(-1.12973467647591,70.9107390569746,11.6079872482298));
#53073=CARTESIAN_POINT('Ctrl Pts',(-1.11801931508906,70.9125475893433,11.5996464713191));
#53074=CARTESIAN_POINT('Ctrl Pts',(-1.10621452707645,70.9143583471047,11.5914270632553));
#53075=CARTESIAN_POINT('Ctrl Pts',(-1.10078039265814,70.9151918988011,11.5876433978298));
#53076=CARTESIAN_POINT('Ctrl Pts',(-1.09532728269988,70.9160259169017,11.5838854298758));
#53077=CARTESIAN_POINT('Ctrl Pts',(-1.08985537693032,70.9168604098746,11.5801533805886));
#53078=CARTESIAN_POINT('Ctrl Pts',(-1.01625744140572,70.9280844628101,11.5299567700513));
#53079=CARTESIAN_POINT('Ctrl Pts',(-0.93923646562749,70.9393967051461,11.4844380068382));
#53080=CARTESIAN_POINT('Ctrl Pts',(-0.859395350069275,70.9506694405085,
11.4441790152186));
#53081=CARTESIAN_POINT('Ctrl Pts',(-0.835028922366022,70.9541097267483,
11.4318925159401));
#53082=CARTESIAN_POINT('Ctrl Pts',(-0.810399897410274,70.9575463516296,
11.4200955467953));
#53083=CARTESIAN_POINT('Ctrl Pts',(-0.785525510500858,70.9609757349325,
11.4088036780356));
#53084=CARTESIAN_POINT('Ctrl Pts',(-0.762132153311586,70.9642009315509,
11.3981841311021));
#53085=CARTESIAN_POINT('Ctrl Pts',(-0.738523661806519,70.967419583261,11.3880122786022));
#53086=CARTESIAN_POINT('Ctrl Pts',(-0.714717770134932,70.9706286150032,
11.3783018029276));
#53087=CARTESIAN_POINT('Ctrl Pts',(-0.714716722865029,70.970628756175,11.3783013757439));
#53088=CARTESIAN_POINT('Ctrl Pts',(-0.714715675594629,70.9706288973469,
11.3783009485611));
#53089=CARTESIAN_POINT('Ctrl Pts',(-0.714714628323901,70.9706290385188,
11.3783005213791));
#53090=CARTESIAN_POINT('Ctrl Pts',(-0.637105405154823,70.9810907434083,
11.3466437036312));
#53091=CARTESIAN_POINT('Ctrl Pts',(-0.557226499885859,70.9914732155707,
11.3198241702613));
#53092=CARTESIAN_POINT('Ctrl Pts',(-0.475813234330459,71.0018390425587,
11.2979662624588));
#53093=CARTESIAN_POINT('Ctrl Pts',(-0.451818659763821,71.0048941172681,
11.291524177191));
#53094=CARTESIAN_POINT('Ctrl Pts',(-0.427691015240452,71.0079477337291,
11.285512798002));
#53095=CARTESIAN_POINT('Ctrl Pts',(-0.403449600131215,71.0110014624199,
11.2799345969682));
#53096=CARTESIAN_POINT('Ctrl Pts',(-0.295355884253575,71.0246181956008,
11.2550611118629));
#53097=CARTESIAN_POINT('Ctrl Pts',(-0.184991029156832,71.0383072748101,
11.2388246119196));
#53098=CARTESIAN_POINT('Ctrl Pts',(-0.07382045547731,71.0521996774235,11.2313724643906));
#53099=CARTESIAN_POINT('Ctrl Pts',(-0.0310994279747684,71.0575382998168,
11.2285087263617));
#53100=CARTESIAN_POINT('Ctrl Pts',(0.0117424070116354,71.0628810203524,
11.226930962945));
#53101=CARTESIAN_POINT('Ctrl Pts',(0.0546335509162594,71.0682293716919,
11.2266456339177));
#53102=CARTESIAN_POINT('Ctrl Pts',(0.165674313258151,71.082075703497,11.2259069463981));
#53103=CARTESIAN_POINT('Ctrl Pts',(0.277077544205819,71.0960740139967,11.2338758835229));
#53104=CARTESIAN_POINT('Ctrl Pts',(0.387446675908198,71.1102697790105,11.2507520614417));
#53105=CARTESIAN_POINT('Ctrl Pts',(0.469551691496286,71.1208301910547,11.2633064670959));
#53106=CARTESIAN_POINT('Ctrl Pts',(0.551086850323243,71.1314192058162,11.2807598778748));
#53107=CARTESIAN_POINT('Ctrl Pts',(0.631369457466356,71.1419445439166,11.3031163186117));
#53108=CARTESIAN_POINT('Ctrl Pts',(0.657909466524091,71.1454240344122,11.3105069622488));
#53109=CARTESIAN_POINT('Ctrl Pts',(0.684312800191152,71.1488965830908,11.3184330683517));
#53110=CARTESIAN_POINT('Ctrl Pts',(0.710555509033363,71.1523589076908,11.3268937387277));
#53111=CARTESIAN_POINT('Ctrl Pts',(0.737811912617902,71.1559549738288,11.3356812251017));
#53112=CARTESIAN_POINT('Ctrl Pts',(0.764893414727017,71.1595399798575,11.3450449920988));
#53113=CARTESIAN_POINT('Ctrl Pts',(0.791770462418447,71.1631103669693,11.3549821775479));
#53114=CARTESIAN_POINT('Ctrl Pts',(0.791775501359393,71.1631110363497,11.3549840405833));
#53115=CARTESIAN_POINT('Ctrl Pts',(0.791780540293847,71.1631117057296,11.3549859036391));
#53116=CARTESIAN_POINT('Ctrl Pts',(0.791785579221842,71.163112375109,11.3549877667152));
#53117=CARTESIAN_POINT('Ctrl Pts',(0.872396842029561,71.1738209065673,11.3847927009848));
#53118=CARTESIAN_POINT('Ctrl Pts',(0.951351908195907,71.1843979836468,11.419813974218));
#53119=CARTESIAN_POINT('Ctrl Pts',(1.02801671639817,71.194959265503,11.4596562735348));
#53120=CARTESIAN_POINT('Ctrl Pts',(1.05011940307327,71.1980041137095,11.4711429240445));
#53121=CARTESIAN_POINT('Ctrl Pts',(1.07203165928233,71.2010476242585,11.4830299669435));
#53122=CARTESIAN_POINT('Ctrl Pts',(1.09373817003166,71.2040925074142,11.4953071389792));
#53123=CARTESIAN_POINT('Ctrl Pts',(1.17076089443873,71.2148968784554,11.5388710838769));
#53124=CARTESIAN_POINT('Ctrl Pts',(1.24514461388718,71.2259201288154,11.5874360518204));
#53125=CARTESIAN_POINT('Ctrl Pts',(1.31641777296803,71.2369917159873,11.6404960142158));
#53126=CARTESIAN_POINT('Ctrl Pts',(1.32787419490414,71.2387713589242,11.6490248534725));
#53127=CARTESIAN_POINT('Ctrl Pts',(1.33925031396308,71.2405522626534,11.6576699179167));
#53128=CARTESIAN_POINT('Ctrl Pts',(1.3505442430379,71.2423337327342,11.6664292093449));
#53129=CARTESIAN_POINT('Ctrl Pts',(1.42865171810356,71.2546541686949,11.7270074308202));
#53130=CARTESIAN_POINT('Ctrl Pts',(1.50285916325863,71.2670061407611,11.7930685481099));
#53131=CARTESIAN_POINT('Ctrl Pts',(1.57240659892121,71.2794577260796,11.8640979704692));
#53132=CARTESIAN_POINT('Ctrl Pts',(1.5811968343051,71.2810315061163,11.8730755170282));
#53133=CARTESIAN_POINT('Ctrl Pts',(1.58991256127224,71.2826068747412,11.8821324528914));
#53134=CARTESIAN_POINT('Ctrl Pts',(1.59855218723446,71.2841839670128,11.8912677546883));
#53135=CARTESIAN_POINT('Ctrl Pts',(1.65899979691212,71.2952181782716,11.9551833871148));
#53136=CARTESIAN_POINT('Ctrl Pts',(1.71568819992305,71.3064094743598,12.0229634916327));
#53137=CARTESIAN_POINT('Ctrl Pts',(1.76808256701075,71.3176009568167,12.0940940114363));
#53138=CARTESIAN_POINT('Ctrl Pts',(1.78201294070464,71.3205764967741,12.1130058673663));
#53139=CARTESIAN_POINT('Ctrl Pts',(1.79564005369749,71.3235520771964,12.1321545766696));
#53140=CARTESIAN_POINT('Ctrl Pts',(1.80895447139048,71.3265248094507,12.1515305530256));
#53141=CARTESIAN_POINT('Ctrl Pts',(1.85328472667293,71.3364224995154,12.2160427230665));
#53142=CARTESIAN_POINT('Ctrl Pts',(1.89414300930226,71.346287426131,12.2830723463133));
#53143=CARTESIAN_POINT('Ctrl Pts',(1.93114510948473,71.3560608208897,12.3522197824008));
#53144=CARTESIAN_POINT('Ctrl Pts',(1.93611964086167,71.3573747479005,12.3615159058305));
#53145=CARTESIAN_POINT('Ctrl Pts',(1.94102455125582,71.35868702262,12.3708502887935));
#53146=CARTESIAN_POINT('Ctrl Pts',(1.94585897866666,71.3599975041675,12.3802219460974));
#53147=CARTESIAN_POINT('Ctrl Pts',(1.94585962985694,71.3599976806874,12.3802232084459));
#53148=CARTESIAN_POINT('Ctrl Pts',(1.94586028104596,71.3599978572073,12.3802244707951));
#53149=CARTESIAN_POINT('Ctrl Pts',(1.94586093223373,71.3599980337272,12.380225733145));
#53150=CARTESIAN_POINT('Ctrl Pts',(1.98619576175937,71.370931744641,12.4584161888338));
#53151=CARTESIAN_POINT('Ctrl Pts',(2.0217086491527,71.3817242349857,12.539322072039));
#53152=CARTESIAN_POINT('Ctrl Pts',(2.05217280790861,71.3925449886504,12.6222710572936));
#53153=CARTESIAN_POINT('Ctrl Pts',(2.06038003658161,71.3954601651518,12.6446180157517));
#53154=CARTESIAN_POINT('Ctrl Pts',(2.06822080311025,71.3983773562506,12.6671129733622));
#53155=CARTESIAN_POINT('Ctrl Pts',(2.07569065099517,71.4012997935818,12.6897421371436));
#53156=CARTESIAN_POINT('Ctrl Pts',(2.09153592110757,71.4074989571544,12.7377438124197));
#53157=CARTESIAN_POINT('Ctrl Pts',(2.10565957213874,71.4138124411617,12.7863718679594));
#53158=CARTESIAN_POINT('Ctrl Pts',(2.11810832935687,71.4201325350876,12.8354888385054));
#53159=CARTESIAN_POINT('Ctrl Pts',(2.14267259448761,71.4326035360179,12.9324079337828));
#53160=CARTESIAN_POINT('Ctrl Pts',(2.16072569386879,71.4451031594844,13.0312526015205));
#53161=CARTESIAN_POINT('Ctrl Pts',(2.17208083446691,71.4576591703852,13.1311612395562));
#53162=CARTESIAN_POINT('Ctrl Pts',(2.17359503021924,71.4593335008972,13.1444839486876));
#53163=CARTESIAN_POINT('Ctrl Pts',(2.17499004738872,71.4610088333506,13.1578255752569));
#53164=CARTESIAN_POINT('Ctrl Pts',(2.17626537266087,71.462685232893,13.1711840706296));
#53165=CARTESIAN_POINT('Ctrl Pts',(2.18527813737428,71.474532402373,13.2655889870447));
#53166=CARTESIAN_POINT('Ctrl Pts',(2.18821857238941,71.4865700961145,13.3608429088672));
#53167=CARTESIAN_POINT('Ctrl Pts',(2.18501020941626,71.4986391581974,13.4560936714542));
#53168=CARTESIAN_POINT('Ctrl Pts',(2.18434840391752,71.5011287055828,13.4757415351674));
#53169=CARTESIAN_POINT('Ctrl Pts',(2.18342506209214,71.5036196100868,13.4953894145309));
#53170=CARTESIAN_POINT('Ctrl Pts',(2.18223963969097,71.5061105101725,13.5150300748985));
#53171=CARTESIAN_POINT('Ctrl Pts',(2.17691261588212,71.5173040594499,13.6032908208534));
#53172=CARTESIAN_POINT('Ctrl Pts',(2.16629030045941,71.5284959395751,13.6914037443961));
#53173=CARTESIAN_POINT('Ctrl Pts',(2.15030415455817,71.5396240769922,13.7786439086661));
#53174=CARTESIAN_POINT('Ctrl Pts',(2.14578077443653,71.5427728531822,13.8033290596278));
#53175=CARTESIAN_POINT('Ctrl Pts',(2.1408282253218,71.545916538471,13.8279444804834));
#53176=CARTESIAN_POINT('Ctrl Pts',(2.13544561019691,71.549053756753,13.8524741441037));
#53177=CARTESIAN_POINT('Ctrl Pts',(2.12803121764441,71.5533751818086,13.8862630275815));
#53178=CARTESIAN_POINT('Ctrl Pts',(2.11980078157287,71.5576844542003,13.9198879844507));
#53179=CARTESIAN_POINT('Ctrl Pts',(2.11075327030379,71.5619785174693,13.953304851992));
#53180=CARTESIAN_POINT('Ctrl Pts',(2.11075235061384,71.5619789539657,13.9533082488551));
#53181=CARTESIAN_POINT('Ctrl Pts',(2.11075143091544,71.561979390462,13.9533116457163));
#53182=CARTESIAN_POINT('Ctrl Pts',(2.11075051120861,71.5619798269581,13.9533150425754));
#53183=CARTESIAN_POINT('Ctrl Pts',(2.08957577910432,71.5720294291065,14.0315221186651));
#53184=CARTESIAN_POINT('Ctrl Pts',(2.06392338841043,71.5819768958523,14.1086902093775));
#53185=CARTESIAN_POINT('Ctrl Pts',(2.03396025847612,71.5919861059351,14.1843500081339));
#53186=CARTESIAN_POINT('Ctrl Pts',(2.02376865458318,71.5953906202388,14.2100847928923));
#53187=CARTESIAN_POINT('Ctrl Pts',(2.0130784186635,71.5988022211228,14.2356446483217));
#53188=CARTESIAN_POINT('Ctrl Pts',(2.00189651879196,71.6022271799728,14.261009792523));
#53189=CARTESIAN_POINT('Ctrl Pts',(1.95863636229423,71.6154775450764,14.3591416055727));
#53190=CARTESIAN_POINT('Ctrl Pts',(1.90804853165839,71.6288708767552,14.4544124267342));
#53191=CARTESIAN_POINT('Ctrl Pts',(1.85078153392663,71.6423234260279,14.5459243130061));
#53192=CARTESIAN_POINT('Ctrl Pts',(1.83853215476964,71.6452009188806,14.5654986548908));
#53193=CARTESIAN_POINT('Ctrl Pts',(1.82597700665506,71.6480811400064,14.5849010797434));
#53194=CARTESIAN_POINT('Ctrl Pts',(1.81312214043868,71.6509633009607,14.6041228878331));
#53195=CARTESIAN_POINT('Ctrl Pts',(1.74555966945489,71.666111332264,14.7051486651113));
#53196=CARTESIAN_POINT('Ctrl Pts',(1.66963839935241,71.6814304867716,14.801130603571));
#53197=CARTESIAN_POINT('Ctrl Pts',(1.58630743542294,71.6968001766533,14.8906800925929));
#53198=CARTESIAN_POINT('Ctrl Pts',(1.57847428137015,71.6982449355149,14.8990977912463));
#53199=CARTESIAN_POINT('Ctrl Pts',(1.57057564463731,71.6996901464177,14.9074586885919));
#53200=CARTESIAN_POINT('Ctrl Pts',(1.56261230585935,71.7011357126583,14.9157616535523));
#53201=CARTESIAN_POINT('Ctrl Pts',(1.49019630791816,71.7142812191883,14.991266100901));
#53202=CARTESIAN_POINT('Ctrl Pts',(1.41243396089567,71.7274470391968,15.0619806279928));
#53203=CARTESIAN_POINT('Ctrl Pts',(1.3299595783442,71.7405764813823,15.1270113030264));
#53204=CARTESIAN_POINT('Ctrl Pts',(1.307680840418,71.7441231269287,15.1445779864185));
#53205=CARTESIAN_POINT('Ctrl Pts',(1.28505835030234,71.747667133117,15.1617302002453));
#53206=CARTESIAN_POINT('Ctrl Pts',(1.26210475420861,71.7512074164063,15.1784509681943));
#53207=CARTESIAN_POINT('Ctrl Pts',(1.2238596562881,71.7571062080603,15.2063109777939));
#53208=CARTESIAN_POINT('Ctrl Pts',(1.18469629591523,71.7629947807052,15.232971940542));
#53209=CARTESIAN_POINT('Ctrl Pts',(1.14467692932067,71.768868991772,15.2583540662385));
#53210=CARTESIAN_POINT('Ctrl Pts',(1.14467076444827,71.7688698966779,15.2583579762845));
#53211=CARTESIAN_POINT('Ctrl Pts',(1.14466459955562,71.7688708015835,15.2583618863002));
#53212=CARTESIAN_POINT('Ctrl Pts',(1.1446584346426,71.7688717064887,15.2583657962856));
#53213=CARTESIAN_POINT('Ctrl Pts',(1.10071341999499,71.7753220933381,15.2862371325845));
#53214=CARTESIAN_POINT('Ctrl Pts',(1.05571839411559,71.7817545254206,15.3125819795612));
#53215=CARTESIAN_POINT('Ctrl Pts',(1.00978071557335,71.7882093696722,15.3373356118852));
#53216=CARTESIAN_POINT('Ctrl Pts',(0.880191475056821,71.8064183517271,15.4071650964105));
#53217=CARTESIAN_POINT('Ctrl Pts',(0.743087453138814,71.8248188944842,15.4643302827042));
#53218=CARTESIAN_POINT('Ctrl Pts',(0.601240848352391,71.843353052873,15.5081262725566));
#53219=CARTESIAN_POINT('Ctrl Pts',(0.459347343337411,71.8618933394046,15.5519367431357));
#53220=CARTESIAN_POINT('Ctrl Pts',(0.312700705102145,71.8805844082547,15.5823503811493));
#53221=CARTESIAN_POINT('Ctrl Pts',(0.1641159504501,71.899352922242,15.5986382270688));
#53222=CARTESIAN_POINT('Ctrl Pts',(0.0321111188423181,71.916027139824,15.6131085834852));
#53223=CARTESIAN_POINT('Ctrl Pts',(-0.101423215562088,71.932761667862,15.6164281715104));
#53224=CARTESIAN_POINT('Ctrl Pts',(-0.234482419868063,71.9494967982338,
15.6081083003707));
#53225=CARTESIAN_POINT('Ctrl Pts',(-0.243288383689666,71.9506043424535,
15.6075576846907));
#53226=CARTESIAN_POINT('Ctrl Pts',(-0.252092280033786,71.9517118910096,
15.6069561026561));
#53227=CARTESIAN_POINT('Ctrl Pts',(-0.260893533916475,71.9528194273214,
15.6063034180066));
#53228=CARTESIAN_POINT('Ctrl Pts',(-0.330418216456274,71.9615683069137,
15.6011475966137));
#53229=CARTESIAN_POINT('Ctrl Pts',(-0.399776517792103,71.9703161707563,
15.5928027171852));
#53230=CARTESIAN_POINT('Ctrl Pts',(-0.468680029306107,71.9790543660095,
15.5812047536984));
#53231=CARTESIAN_POINT('Ctrl Pts',(-0.476242589928811,71.9800134336953,
15.5799318098376));
#53232=CARTESIAN_POINT('Ctrl Pts',(-0.483799671584185,71.9809723852518,
15.5786196828546));
#53233=CARTESIAN_POINT('Ctrl Pts',(-0.491350900777853,71.9819310858116,
15.5772684232766));
#53234=CARTESIAN_POINT('Ctrl Pts',(-0.491355026516865,71.9819316096135,
15.5772676849936));
#53235=CARTESIAN_POINT('Ctrl Pts',(-0.491359152254362,71.9819321334154,
15.5772669466988));
#53236=CARTESIAN_POINT('Ctrl Pts',(-0.491363277990312,71.9819326572172,
15.5772662083924));
#53237=CARTESIAN_POINT('Ctrl Pts',(-0.599984076087746,71.9957231110571,
15.5578283581625));
#53238=CARTESIAN_POINT('Ctrl Pts',(-0.707545851576862,72.0094797114707,
15.5302639013997));
#53239=CARTESIAN_POINT('Ctrl Pts',(-0.812963944553361,72.0232380427708,
15.4950649743857));
#53240=CARTESIAN_POINT('Ctrl Pts',(-0.855848862106878,72.0288350412254,
15.480745771293));
#53241=CARTESIAN_POINT('Ctrl Pts',(-0.898378762592077,72.0344322873196,
15.4651636734896));
#53242=CARTESIAN_POINT('Ctrl Pts',(-0.940479812768093,72.0400320146097,
15.4483541203874));
#53243=CARTESIAN_POINT('Ctrl Pts',(-1.05991870548102,72.0559182032971,15.400666131581));
#53244=CARTESIAN_POINT('Ctrl Pts',(-1.17585534434287,72.0719457058116,15.342970078193));
#53245=CARTESIAN_POINT('Ctrl Pts',(-1.286696153303,72.0880627897628,15.2761931399249));
#53246=CARTESIAN_POINT('Ctrl Pts',(-1.31543473728105,72.0922415951591,15.2588793484953));
#53247=CARTESIAN_POINT('Ctrl Pts',(-1.34383101040018,72.0964264420064,15.240955182115));
#53248=CARTESIAN_POINT('Ctrl Pts',(-1.37185775388227,72.1006164696211,15.2224369452993));
#53249=CARTESIAN_POINT('Ctrl Pts',(-1.48286036129561,72.117211476125,15.1490936911122));
#53250=CARTESIAN_POINT('Ctrl Pts',(-1.58809465719197,72.1338459986869,15.066477464604));
#53251=CARTESIAN_POINT('Ctrl Pts',(-1.68595660883222,72.1505301337724,14.9754582562636));
#53252=CARTESIAN_POINT('Ctrl Pts',(-1.70681201011313,72.1540856967506,14.9560611148578));
#53253=CARTESIAN_POINT('Ctrl Pts',(-1.72733249353319,72.1576435137915,14.9362821807924));
#53254=CARTESIAN_POINT('Ctrl Pts',(-1.74750235772902,72.1612036840118,14.9161296223245));
#53255=CARTESIAN_POINT('Ctrl Pts',(-1.77049418539539,72.1652619572543,14.8931575216287));
#53256=CARTESIAN_POINT('Ctrl Pts',(-1.79303100671763,72.1693233872736,14.8696993952342));
#53257=CARTESIAN_POINT('Ctrl Pts',(-1.81508151286912,72.1733973014865,14.8457586729703));
#53258=CARTESIAN_POINT('Ctrl Pts',(-1.85712541155155,72.181165070409,14.8001106822016));
#53259=CARTESIAN_POINT('Ctrl Pts',(-1.89732243389114,72.1890650989457,14.752631215339));
#53260=CARTESIAN_POINT('Ctrl Pts',(-1.93561044495043,72.1969626246315,14.7035378686259));
#53261=CARTESIAN_POINT('Ctrl Pts',(-1.94050771329313,72.1979727659644,14.6972585324566));
#53262=CARTESIAN_POINT('Ctrl Pts',(-1.94537380547937,72.1989828749059,14.6909527511329));
#53263=CARTESIAN_POINT('Ctrl Pts',(-1.95020863905481,72.1999926770107,14.6846209413863));
#53264=CARTESIAN_POINT('Ctrl Pts',(-1.95021287859332,72.1999935624797,14.6846153891888));
#53265=CARTESIAN_POINT('Ctrl Pts',(-1.95021711810784,72.1999944479484,14.6846098369711));
#53266=CARTESIAN_POINT('Ctrl Pts',(-1.95022135759829,72.1999953334168,14.6846042847335));
#53267=CARTESIAN_POINT('Ctrl Pts',(-2.02012671004489,72.2145959052262,14.5930529221521));
#53268=CARTESIAN_POINT('Ctrl Pts',(-2.08350271444183,72.2291185208218,14.4960806229705));
#53269=CARTESIAN_POINT('Ctrl Pts',(-2.13981592348098,72.2436382301198,14.3948233216095));
#53270=CARTESIAN_POINT('Ctrl Pts',(-2.15568285604744,72.247729335071,14.3662928435925));
#53271=CARTESIAN_POINT('Ctrl Pts',(-2.17098883835595,72.2518201700969,14.3374223900523));
#53272=CARTESIAN_POINT('Ctrl Pts',(-2.18572142668799,72.2559123209899,14.3082379124049));
#53273=CARTESIAN_POINT('Ctrl Pts',(-2.18572719673364,72.2559139236885,14.3082264822498));
#53274=CARTESIAN_POINT('Ctrl Pts',(-2.18573296669124,72.2559155263873,14.3082150520466));
#53275=CARTESIAN_POINT('Ctrl Pts',(-2.18573873656072,72.2559171290863,14.3082036217953));
#53276=CARTESIAN_POINT('Ctrl Pts',(-2.23476047601701,72.2695339182556,14.2110903674256));
#53277=CARTESIAN_POINT('Ctrl Pts',(-2.27742353843653,72.2831703516847,14.1105036799087));
#53278=CARTESIAN_POINT('Ctrl Pts',(-2.31321095092577,72.296784221078,14.0072753291497));
#53279=CARTESIAN_POINT('Ctrl Pts',(-2.32634447211919,72.3017803364651,13.9693918489494));
#53280=CARTESIAN_POINT('Ctrl Pts',(-2.33855163565415,72.3067734455887,13.9311528495216));
#53281=CARTESIAN_POINT('Ctrl Pts',(-2.34980584038207,72.3117616912306,13.8926004503245));
#53282=CARTESIAN_POINT('Ctrl Pts',(-2.34980928625165,72.311763218557,13.892588646155));
#53283=CARTESIAN_POINT('Ctrl Pts',(-2.34981273203262,72.3117647458824,13.8925768419563));
#53284=CARTESIAN_POINT('Ctrl Pts',(-2.34981617772495,72.3117662732069,13.8925650377283));
#53285=CARTESIAN_POINT('Ctrl Pts',(-2.37274164238379,72.3219281275906,13.8140271459381));
#53286=CARTESIAN_POINT('Ctrl Pts',(-2.39174539427942,72.332048545218,13.7341892736926));
#53287=CARTESIAN_POINT('Ctrl Pts',(-2.4066798856095,72.3422167273012,13.6534209894091));
#53288=CARTESIAN_POINT('Ctrl Pts',(-2.41905169904031,72.3506401043606,13.5865121056583));
#53289=CARTESIAN_POINT('Ctrl Pts',(-2.4286303555641,72.3590961491279,13.5189655055544));
#53290=CARTESIAN_POINT('Ctrl Pts',(-2.43532692904267,72.367632225426,13.4510177600665));
#53291=CARTESIAN_POINT('Ctrl Pts',(-2.43532751033381,72.3676329663938,13.4510118619124));
#53292=CARTESIAN_POINT('Ctrl Pts',(-2.43532809160323,72.3676337073623,13.4510059637553));
#53293=CARTESIAN_POINT('Ctrl Pts',(-2.43532867285094,72.3676344483313,13.4510000655951));
#53294=CARTESIAN_POINT('Ctrl Pts',(-2.43685242895941,72.3695769180901,13.4355378840728));
#53295=CARTESIAN_POINT('Ctrl Pts',(-2.43822752235068,72.3715229059429,13.4200562506372));
#53296=CARTESIAN_POINT('Ctrl Pts',(-2.43945255372853,72.373472621177,13.4045578859649));
#53297=CARTESIAN_POINT('Ctrl Pts',(-2.4455198139933,72.3831290511928,13.3277985360858));
#53298=CARTESIAN_POINT('Ctrl Pts',(-2.44790520255198,72.3928785634079,13.2506233464808));
#53299=CARTESIAN_POINT('Ctrl Pts',(-2.44659781380402,72.4026310200357,13.1734055148817));
#53300=CARTESIAN_POINT('Ctrl Pts',(-2.44633392768895,72.4045994765455,13.1578197041377));
#53301=CARTESIAN_POINT('Ctrl Pts',(-2.44591959423343,72.4065680740621,13.1422319876076));
#53302=CARTESIAN_POINT('Ctrl Pts',(-2.44535470772765,72.408536103423,13.1266451784564));
#53303=CARTESIAN_POINT('Ctrl Pts',(-2.44380192716608,72.4139458940714,13.0837995908572));
#53304=CARTESIAN_POINT('Ctrl Pts',(-2.44111186504103,72.4193508130069,13.0409635853769));
#53305=CARTESIAN_POINT('Ctrl Pts',(-2.43728466864259,72.4247344546358,12.9982043293178));
#53306=CARTESIAN_POINT('Ctrl Pts',(-2.43728253046173,72.4247374623726,12.9981804405456));
#53307=CARTESIAN_POINT('Ctrl Pts',(-2.43728039192522,72.4247404701038,12.9981565517893));
#53308=CARTESIAN_POINT('Ctrl Pts',(-2.43727825303304,72.4247434778295,12.9981326630488));
#53309=CARTESIAN_POINT('Ctrl Pts',(-2.42898557216907,72.43640470559,12.9055138282334));
#53310=CARTESIAN_POINT('Ctrl Pts',(-2.41534357920754,72.4479824797458,12.8131291710771));
#53311=CARTESIAN_POINT('Ctrl Pts',(-2.3964964848232,72.4595253844034,12.7215935711713));
#53312=CARTESIAN_POINT('Ctrl Pts',(-2.38767962564182,72.4649252706052,12.6787723023861));
#53313=CARTESIAN_POINT('Ctrl Pts',(-2.3777241637851,72.4703174560377,12.6361373888414));
#53314=CARTESIAN_POINT('Ctrl Pts',(-2.36664778503021,72.4757065424221,12.5937543546988));
#53315=CARTESIAN_POINT('Ctrl Pts',(-2.33923788833977,72.4890425165993,12.4888721894186));
#53316=CARTESIAN_POINT('Ctrl Pts',(-2.30482530756836,72.5024462168457,12.3855591051039));
#53317=CARTESIAN_POINT('Ctrl Pts',(-2.26370876476586,72.5159725324142,12.2847530831423));
#53318=CARTESIAN_POINT('Ctrl Pts',(-2.25166244364125,72.5199354711699,12.2552189436191));
#53319=CARTESIAN_POINT('Ctrl Pts',(-2.23904084444868,72.5239088908104,12.2259002943049));
#53320=CARTESIAN_POINT('Ctrl Pts',(-2.22585196595221,72.5278940616467,12.1968214169595));
#53321=CARTESIAN_POINT('Ctrl Pts',(-2.18333437932186,72.5407412378729,12.1030785193374));
#53322=CARTESIAN_POINT('Ctrl Pts',(-2.13508628031869,72.5536090363629,12.0117609457507));
#53323=CARTESIAN_POINT('Ctrl Pts',(-2.08136896746144,72.5665109076533,11.9234977558));
#53324=CARTESIAN_POINT('Ctrl Pts',(-2.06607621375076,72.570183934645,11.8983701544022));
#53325=CARTESIAN_POINT('Ctrl Pts',(-2.05033990200067,72.5738597246151,11.8734902495142));
#53326=CARTESIAN_POINT('Ctrl Pts',(-2.03416539392586,72.5775385913636,11.8488729526678));
#53327=CARTESIAN_POINT('Ctrl Pts',(1.35925139903161,68.5015684297319,11.2018017462371));
#53328=CARTESIAN_POINT('Ctrl Pts',(1.81201504569449,68.5705202281901,11.5183578934431));
#53329=CARTESIAN_POINT('Ctrl Pts',(2.4871255928394,68.7068329045687,12.4537467086246));
#53330=CARTESIAN_POINT('Ctrl Pts',(2.42336085847789,68.9065763946622,14.1441642030493));
#53331=CARTESIAN_POINT('Ctrl Pts',(1.35774589260468,69.1016690675509,15.4062116397971));
#53332=CARTESIAN_POINT('Ctrl Pts',(-0.221166469575229,69.2922152826969,
15.7370705160361));
#53333=CARTESIAN_POINT('Ctrl Pts',(-1.63549669696357,69.4783571664629,15.0420008198722));
#53334=CARTESIAN_POINT('Ctrl Pts',(-2.3066978913788,69.6602591510739,13.6560348131309));
#53335=CARTESIAN_POINT('Ctrl Pts',(-1.98918266931016,69.8381154442101,12.1835559119558));
#53336=CARTESIAN_POINT('Ctrl Pts',(-0.900255468145694,70.0057067926906,
11.274956447888));
#53337=CARTESIAN_POINT('Ctrl Pts',(0.420880950868389,70.1637298446908,11.183392327644));
#53338=CARTESIAN_POINT('Ctrl Pts',(1.50237204011775,70.3127965825961,11.8007288591049));
#53339=CARTESIAN_POINT('Ctrl Pts',(2.14764777535062,70.483880181877,13.0834385708106));
#53340=CARTESIAN_POINT('Ctrl Pts',(1.68418285768135,70.6757162506824,14.7103694985184));
#53341=CARTESIAN_POINT('Ctrl Pts',(-0.0330782420554639,70.8873605170864,
15.4592990478547));
#53342=CARTESIAN_POINT('Ctrl Pts',(-1.6707310055211,71.0956282386167,14.6202665191846));
#53343=CARTESIAN_POINT('Ctrl Pts',(-2.06050794163202,71.3014160745871,12.8448001592972));
#53344=CARTESIAN_POINT('Ctrl Pts',(-0.939643177328641,71.5056429104108,
11.4241772577033));
#53345=CARTESIAN_POINT('Ctrl Pts',(0.405518300920993,71.658307121143,11.3989157803725));
#53346=CARTESIAN_POINT('Ctrl Pts',(1.112140023751,71.7601738993637,11.8201165612096));
#53347=CARTESIAN_POINT('Ctrl Pts',(1.41249129287616,71.8111398715806,12.0998255829605));
#53348=CARTESIAN_POINT('Ctrl Pts',(1.64338713283149,71.8621472327744,12.4403692775591));
#53349=CARTESIAN_POINT('Ctrl Pts',(1.89705351737498,71.9472687575764,13.0780800622876));
#53350=CARTESIAN_POINT('Ctrl Pts',(1.83265904354054,72.0667825484646,14.0874300328648));
#53351=CARTESIAN_POINT('Ctrl Pts',(0.96215776514328,72.2215130192343,15.0670008052881));
#53352=CARTESIAN_POINT('Ctrl Pts',(-0.337956441766793,72.3776743394961,
15.3063172669432));
#53353=CARTESIAN_POINT('Ctrl Pts',(-1.52424768912109,72.5356499306958,14.6886989506691));
#53354=CARTESIAN_POINT('Ctrl Pts',(-2.08756836957837,72.6957944328977,13.4555231657513));
#53355=CARTESIAN_POINT('Ctrl Pts',(-1.76878172405223,72.8584427198578,12.1159502014204));
#53356=CARTESIAN_POINT('Ctrl Pts',(-0.674972234182401,73.0239265058316,
11.2404721033924));
#53357=CARTESIAN_POINT('Ctrl Pts',(0.752502222318795,73.192553636038,11.222102813825));
#53358=CARTESIAN_POINT('Ctrl Pts',(1.9128224007105,73.3646026686541,12.1029513221996));
#53359=CARTESIAN_POINT('Ctrl Pts',(2.29555630198192,73.5403436305485,13.5401202935886));
#53360=CARTESIAN_POINT('Ctrl Pts',(1.69942781075577,73.7200063918782,14.9399925255078));
#53361=CARTESIAN_POINT('Ctrl Pts',(0.33633086029822,73.9038061569606,15.6934571496578));
#53362=CARTESIAN_POINT('Ctrl Pts',(-1.23229046294891,74.0919248239957,15.4456602078211));
#53363=CARTESIAN_POINT('Ctrl Pts',(-2.48091999765483,74.3059137887571,14.1213831739387));
#53364=CARTESIAN_POINT('Ctrl Pts',(-2.44805375166388,74.5038696724368,12.3829147385172));
#53365=CARTESIAN_POINT('Ctrl Pts',(-1.56312085739856,74.6726204857052,11.3087811705623));
#53366=CARTESIAN_POINT('Ctrl Pts',(-0.992890126921472,74.7523693988593,
11.0014174397873));
#53367=CARTESIAN_POINT('Ctrl Pts',(-0.733503873481175,74.78666297405,10.9114679132036));
#53368=CARTESIAN_POINT('Ctrl Pts',(1.19498081016287,82.2340164369994,10.482675015848));
#53369=CARTESIAN_POINT('Ctrl Pts',(1.72598823950189,82.3066323787876,10.7204975998541));
#53370=CARTESIAN_POINT('Ctrl Pts',(2.62667932021033,82.4489632634736,11.4943972620624));
#53371=CARTESIAN_POINT('Ctrl Pts',(3.13961817930498,82.6588420064339,13.1654943300609));
#53372=CARTESIAN_POINT('Ctrl Pts',(2.70364992086808,82.8640080375243,14.8177084226806));
#53373=CARTESIAN_POINT('Ctrl Pts',(1.47859444808645,83.0663675786054,15.9753243882897));
#53374=CARTESIAN_POINT('Ctrl Pts',(-0.148581296960598,83.265798455397,16.3080276235447));
#53375=CARTESIAN_POINT('Ctrl Pts',(-1.68357605211574,83.4621940706116,15.7402832040705));
#53376=CARTESIAN_POINT('Ctrl Pts',(-2.67007897214778,83.655461159339,14.4707656858787));
#53377=CARTESIAN_POINT('Ctrl Pts',(-2.85891941300041,83.8666402933621,12.7190213299314));
#53378=CARTESIAN_POINT('Ctrl Pts',(-1.84603430281946,84.0942739879358,11.0522678886856));
#53379=CARTESIAN_POINT('Ctrl Pts',(0.151482086621562,84.336683926515,10.4633967604406));
#53380=CARTESIAN_POINT('Ctrl Pts',(1.97167797911635,84.5731173043586,11.3592888645195));
#53381=CARTESIAN_POINT('Ctrl Pts',(2.69573223495876,84.8035699798368,13.2004961804263));
#53382=CARTESIAN_POINT('Ctrl Pts',(1.99918277764129,85.0280847473626,14.9997242915337));
#53383=CARTESIAN_POINT('Ctrl Pts',(0.460113177574641,85.2285334817215,15.7643099300201));
#53384=CARTESIAN_POINT('Ctrl Pts',(-0.997754222001919,85.406604631475,15.4897739817101));
#53385=CARTESIAN_POINT('Ctrl Pts',(-2.04757701996071,85.5768355775209,14.5349258191164));
#53386=CARTESIAN_POINT('Ctrl Pts',(-2.30990438101913,85.7305593231813,13.2552846444736));
#53387=CARTESIAN_POINT('Ctrl Pts',(-1.88543687624611,85.8813849837293,12.0945359749286));
#53388=CARTESIAN_POINT('Ctrl Pts',(-1.04530190918308,86.017391015636,11.3343139025098));
#53389=CARTESIAN_POINT('Ctrl Pts',(-0.0516858839223906,86.1388075906432,
11.1567759640611));
#53390=CARTESIAN_POINT('Ctrl Pts',(1.0831281897424,86.2826143370863,11.4262298525765));
#53391=CARTESIAN_POINT('Ctrl Pts',(1.94436773624321,86.4239758161431,12.3037970364228));
#53392=CARTESIAN_POINT('Ctrl Pts',(2.05173254243784,86.5856935562115,13.6502755336076));
#53393=CARTESIAN_POINT('Ctrl Pts',(1.53497337091036,86.7222956550306,14.6619025754067));
#53394=CARTESIAN_POINT('Ctrl Pts',(0.572769711474274,86.8570741630587,15.241996329925));
#53395=CARTESIAN_POINT('Ctrl Pts',(-0.443480299089395,86.9791287379262,
15.2286754209456));
#53396=CARTESIAN_POINT('Ctrl Pts',(-1.0756340334284,87.067071681156,14.8834129767296));
#53397=CARTESIAN_POINT('Ctrl Pts',(-1.57789463619398,87.1545918000081,14.391654854311));
#53398=CARTESIAN_POINT('Ctrl Pts',(-1.93160007404001,87.2524891088848,13.6570681730652));
#53399=CARTESIAN_POINT('Ctrl Pts',(-1.8143716581144,87.3820297380612,12.5849378774665));
#53400=CARTESIAN_POINT('Ctrl Pts',(-1.08170690016791,87.5251166129853,11.6442906211455));
#53401=CARTESIAN_POINT('Ctrl Pts',(0.215983600329857,87.6817468300896,11.298789702101));
#53402=CARTESIAN_POINT('Ctrl Pts',(1.51453851662001,87.8522043046485,11.9740541069845));
#53403=CARTESIAN_POINT('Ctrl Pts',(2.01541164598604,88.022810735053,13.3507388599802));
#53404=CARTESIAN_POINT('Ctrl Pts',(1.45918555813443,88.19409616606,14.7109522605905));
#53405=CARTESIAN_POINT('Ctrl Pts',(0.118244489973287,88.366622968629,15.3433638174458));
#53406=CARTESIAN_POINT('Ctrl Pts',(-1.31110040792424,88.5408973526556,14.9039500226772));
#53407=CARTESIAN_POINT('Ctrl Pts',(-2.08169099810388,88.7174617667036,13.5973159668313));
#53408=CARTESIAN_POINT('Ctrl Pts',(-1.81686385850973,88.8669016282602,12.3443338848999));
#53409=CARTESIAN_POINT('Ctrl Pts',(-1.13020678008131,88.9880846501656,11.6322033391202));
#53410=CARTESIAN_POINT('Ctrl Pts',(-0.566646546821027,89.0645455077854,
11.369180962554));
#53411=CARTESIAN_POINT('Ctrl Pts',(0.169750362747802,89.1569914263112,11.2509573070016));
#53412=CARTESIAN_POINT('Ctrl Pts',(1.00960082538348,89.2607654928535,11.4321878451837));
#53413=CARTESIAN_POINT('Ctrl Pts',(2.08830318520032,89.4346617692564,12.3934859611261));
#53414=CARTESIAN_POINT('Ctrl Pts',(2.24388338663252,89.600432357722,13.8708609404721));
#53415=CARTESIAN_POINT('Ctrl Pts',(1.58763714078365,89.7383934335917,14.8013457360256));
#53416=CARTESIAN_POINT('Ctrl Pts',(0.967463015391611,89.8386609176866,15.3110237752385));
#53417=CARTESIAN_POINT('Ctrl Pts',(0.0702839024881292,89.952800674869,15.6303519455016));
#53418=CARTESIAN_POINT('Ctrl Pts',(-1.19203032177318,90.1079507396483,15.356422665022));
#53419=CARTESIAN_POINT('Ctrl Pts',(-2.14007301474896,90.266169579479,14.4410255702375));
#53420=CARTESIAN_POINT('Ctrl Pts',(-2.46919738320312,90.4275439920485,13.1380722770788));
#53421=CARTESIAN_POINT('Ctrl Pts',(-2.05448680883129,90.5921473637104,11.8318607370155));
#53422=CARTESIAN_POINT('Ctrl Pts',(-0.992366573357415,90.7600372906474,
10.9226765107351));
#53423=CARTESIAN_POINT('Ctrl Pts',(-0.0534675979651628,90.8741828745936,
10.7780340477837));
#53424=CARTESIAN_POINT('Ctrl Pts',(0.404552238010835,90.9318150127178,10.8366690372188));
#53425=CARTESIAN_POINT('Ctrl Pts',(1.09092693438828,82.3007689497503,10.6418050319898));
#53426=CARTESIAN_POINT('Ctrl Pts',(1.59144193186989,82.3689958494283,10.8615507258058));
#53427=CARTESIAN_POINT('Ctrl Pts',(2.44170527637221,82.5025601160605,11.5817113845902));
#53428=CARTESIAN_POINT('Ctrl Pts',(2.93320795887768,82.6990780757878,13.1427952373425));
#53429=CARTESIAN_POINT('Ctrl Pts',(2.53714311960989,82.8908092014927,14.6896184836951));
#53430=CARTESIAN_POINT('Ctrl Pts',(1.40246086876332,83.0795927252857,15.7779590132722));
#53431=CARTESIAN_POINT('Ctrl Pts',(-0.110779940039283,83.265371108554,16.0993529543373));
#53432=CARTESIAN_POINT('Ctrl Pts',(-1.54287138803243,83.4481022462018,15.5822415579395));
#53433=CARTESIAN_POINT('Ctrl Pts',(-2.46910424843797,83.6277575655426,14.4095457148995));
#53434=CARTESIAN_POINT('Ctrl Pts',(-2.65763851847854,83.8239427479212,12.783843019403));
#53435=CARTESIAN_POINT('Ctrl Pts',(-1.72998411638569,84.0353418599503,11.2284215222705));
#53436=CARTESIAN_POINT('Ctrl Pts',(0.120398789033176,84.2605110232883,10.6655946771609));
#53437=CARTESIAN_POINT('Ctrl Pts',(1.81973633994219,84.4803193348133,11.4831765154348));
#53438=CARTESIAN_POINT('Ctrl Pts',(2.50974551050697,84.6949030131653,13.1909391184697));
#53439=CARTESIAN_POINT('Ctrl Pts',(1.8761801922996,84.9044369388084,14.876091597299));
#53440=CARTESIAN_POINT('Ctrl Pts',(0.442943858324112,85.0920834801847,15.6062822964452));
#53441=CARTESIAN_POINT('Ctrl Pts',(-0.928757782177521,85.2593421026985,
15.3624189358734));
#53442=CARTESIAN_POINT('Ctrl Pts',(-1.9273104586054,85.4197698003848,14.4731596758825));
#53443=CARTESIAN_POINT('Ctrl Pts',(-2.18893445549896,85.5652612914026,13.2650373897583));
#53444=CARTESIAN_POINT('Ctrl Pts',(-1.79750693525794,85.708628960392,12.1575362726721));
#53445=CARTESIAN_POINT('Ctrl Pts',(-1.00407430876644,85.8384401934296,11.4230188211684));
#53446=CARTESIAN_POINT('Ctrl Pts',(-0.0530396829851482,85.9549193837048,
11.241705895162));
#53447=CARTESIAN_POINT('Ctrl Pts',(1.04269874870432,86.0934463163342,11.4887610721776));
#53448=CARTESIAN_POINT('Ctrl Pts',(1.88784008915594,86.2304017149048,12.3278656793438));
#53449=CARTESIAN_POINT('Ctrl Pts',(2.00925658113287,86.388298190667,13.6408958019134));
#53450=CARTESIAN_POINT('Ctrl Pts',(1.5141869042575,86.5225448053115,14.6412674792069));
#53451=CARTESIAN_POINT('Ctrl Pts',(0.569943927398302,86.6558988636545,15.2274692057216));
#53452=CARTESIAN_POINT('Ctrl Pts',(-0.442474907701717,86.7775073163584,
15.2276295219295));
#53453=CARTESIAN_POINT('Ctrl Pts',(-1.08059670664969,86.865674160951,14.8898130646209));
#53454=CARTESIAN_POINT('Ctrl Pts',(-1.59202319075267,86.953731069283,14.4015536673542));
#53455=CARTESIAN_POINT('Ctrl Pts',(-1.959495328548,87.0526718366557,13.6642829173165));
#53456=CARTESIAN_POINT('Ctrl Pts',(-1.85526539888215,87.184535161682,12.5716123493504));
#53457=CARTESIAN_POINT('Ctrl Pts',(-1.11790566111324,87.3312254586828,11.5971429409853));
#53458=CARTESIAN_POINT('Ctrl Pts',(0.217555757790785,87.4931099341109,11.220397012999));
#53459=CARTESIAN_POINT('Ctrl Pts',(1.58160777082197,87.6708613923171,11.9041881844393));
#53460=CARTESIAN_POINT('Ctrl Pts',(2.1295848131522,87.8502603315557,13.343619575246));
#53461=CARTESIAN_POINT('Ctrl Pts',(1.56147398870172,88.0317657967935,14.7931214983046));
#53462=CARTESIAN_POINT('Ctrl Pts',(0.140883975998077,88.2158505766912,15.488448435748));
#53463=CARTESIAN_POINT('Ctrl Pts',(-1.39976173027164,88.4029283983156,15.0386864184388));
#53464=CARTESIAN_POINT('Ctrl Pts',(-2.25057505170216,88.5934288956208,13.6408160242912));
#53465=CARTESIAN_POINT('Ctrl Pts',(-1.98209790536562,88.7553327392467,12.2797577791271));
#53466=CARTESIAN_POINT('Ctrl Pts',(-1.24650932068784,88.8869313391437,11.4969890384965));
#53467=CARTESIAN_POINT('Ctrl Pts',(-0.637504828814648,88.9700746021111,
11.2032694363274));
#53468=CARTESIAN_POINT('Ctrl Pts',(0.162096212239786,89.070681500301,11.0645677160771));
#53469=CARTESIAN_POINT('Ctrl Pts',(1.07919346721318,89.1837246869346,11.2504526561831));
#53470=CARTESIAN_POINT('Ctrl Pts',(2.26799185493347,89.3733161811301,12.2838066555285));
#53471=CARTESIAN_POINT('Ctrl Pts',(2.45699812867301,89.5541602756378,13.8931639381941));
#53472=CARTESIAN_POINT('Ctrl Pts',(1.75330953186089,89.7045894476644,14.9158667687635));
#53473=CARTESIAN_POINT('Ctrl Pts',(1.08391027807925,89.8138804379689,15.4791011190795));
#53474=CARTESIAN_POINT('Ctrl Pts',(0.110595832794049,89.938226094315,15.8379510560887));
#53475=CARTESIAN_POINT('Ctrl Pts',(-1.26592796379711,90.1070398976702,15.5550459780666));
#53476=CARTESIAN_POINT('Ctrl Pts',(-2.30627773892431,90.2789125402582,14.5718470411942));
#53477=CARTESIAN_POINT('Ctrl Pts',(-2.6777912572662,90.4538666744987,13.1631880283135));
#53478=CARTESIAN_POINT('Ctrl Pts',(-2.24365046799695,90.6319112907103,11.7459518731515));
#53479=CARTESIAN_POINT('Ctrl Pts',(-1.10765396453851,90.8130402539771,10.7538573219242));
#53480=CARTESIAN_POINT('Ctrl Pts',(-0.0992408494391709,90.9358356281587,
10.5885159276331));
#53481=CARTESIAN_POINT('Ctrl Pts',(0.393261874122084,90.9977379954965,10.6465837081081));
#53482=CARTESIAN_POINT('Ctrl Pts',(0.986873058613682,82.3675214625011,10.8009350481316));
#53483=CARTESIAN_POINT('Ctrl Pts',(1.45689562423789,82.4313593200691,11.0026038517577));
#53484=CARTESIAN_POINT('Ctrl Pts',(2.25673123253409,82.5561569686474,11.6690255071179));
#53485=CARTESIAN_POINT('Ctrl Pts',(2.72679773845037,82.7393141451417,13.120096144624));
#53486=CARTESIAN_POINT('Ctrl Pts',(2.37063631835171,82.9176103654609,14.5615285447094));
#53487=CARTESIAN_POINT('Ctrl Pts',(1.32632728944021,83.0928178719662,15.5805936382548));
#53488=CARTESIAN_POINT('Ctrl Pts',(-0.0729785831179774,83.264943761711,
15.8906782851302));
#53489=CARTESIAN_POINT('Ctrl Pts',(-1.40216672394912,83.4340104217921,15.4241999118085));
#53490=CARTESIAN_POINT('Ctrl Pts',(-2.26812952472817,83.6000539717464,14.3483257439206));
#53491=CARTESIAN_POINT('Ctrl Pts',(-2.45635762395667,83.7812452024802,12.8486647088747));
#53492=CARTESIAN_POINT('Ctrl Pts',(-1.61393392995191,83.9764097319649,11.4045751558552));
#53493=CARTESIAN_POINT('Ctrl Pts',(0.0893154914447954,84.1843381200616,
10.8677925938811));
#53494=CARTESIAN_POINT('Ctrl Pts',(1.66779470076804,84.3875213652679,11.6070641663502));
#53495=CARTESIAN_POINT('Ctrl Pts',(2.3237587860552,84.5862360464939,13.1813820565129));
#53496=CARTESIAN_POINT('Ctrl Pts',(1.75317760695792,84.780789130254,14.7524589030643));
#53497=CARTESIAN_POINT('Ctrl Pts',(0.425774539073593,84.9556334786481,15.4482546628703));
#53498=CARTESIAN_POINT('Ctrl Pts',(-0.859761342353121,85.112079573922,15.2350638900366));
#53499=CARTESIAN_POINT('Ctrl Pts',(-1.80704389725007,85.2627040232489,14.4113935326486));
#53500=CARTESIAN_POINT('Ctrl Pts',(-2.06796452997879,85.3999632596242,13.2747901350428));
#53501=CARTESIAN_POINT('Ctrl Pts',(-1.70957699426978,85.5358729370547,12.2205365704158));
#53502=CARTESIAN_POINT('Ctrl Pts',(-0.962846708349784,85.6594893712233,
11.511723739827));
#53503=CARTESIAN_POINT('Ctrl Pts',(-0.0543934820478983,85.7710311767666,
11.3266358262627));
#53504=CARTESIAN_POINT('Ctrl Pts',(1.00226930766624,85.904278295582,11.5512922917787));
#53505=CARTESIAN_POINT('Ctrl Pts',(1.83131244206865,86.0368276136668,12.3519343222649));
#53506=CARTESIAN_POINT('Ctrl Pts',(1.96678061982792,86.1909028251225,13.6315160702192));
#53507=CARTESIAN_POINT('Ctrl Pts',(1.49340043760464,86.3227939555925,14.6206323830071));
#53508=CARTESIAN_POINT('Ctrl Pts',(0.56711814332234,86.4547235642503,15.2129420815183));
#53509=CARTESIAN_POINT('Ctrl Pts',(-0.441469516314034,86.5758858947906,
15.2265836229135));
#53510=CARTESIAN_POINT('Ctrl Pts',(-1.08555937987099,86.6642766407459,14.896213152512));
#53511=CARTESIAN_POINT('Ctrl Pts',(-1.60615174531136,86.7528703385578,14.4114524803976));
#53512=CARTESIAN_POINT('Ctrl Pts',(-1.98739058305599,86.8528545644265,13.6714976615677));
#53513=CARTESIAN_POINT('Ctrl Pts',(-1.8961591396499,86.9870405853029,12.5582868212341));
#53514=CARTESIAN_POINT('Ctrl Pts',(-1.15410442205856,87.1373343043804,11.5499952608252));
#53515=CARTESIAN_POINT('Ctrl Pts',(0.219127915251716,87.3044730381322,11.1420043238971));
#53516=CARTESIAN_POINT('Ctrl Pts',(1.64867702502392,87.4895184799861,11.8343222618939));
#53517=CARTESIAN_POINT('Ctrl Pts',(2.24375798031837,87.6777099280584,13.3365002905118));
#53518=CARTESIAN_POINT('Ctrl Pts',(1.66376241926902,87.869435427527,14.8752907360187));
#53519=CARTESIAN_POINT('Ctrl Pts',(0.16352346202287,88.0650781847536,15.63353305405));
#53520=CARTESIAN_POINT('Ctrl Pts',(-1.48842305261904,88.2649594439756,15.1734228142003));
#53521=CARTESIAN_POINT('Ctrl Pts',(-2.41945910530045,88.4693960245382,13.684316081751));
#53522=CARTESIAN_POINT('Ctrl Pts',(-2.14733195222152,88.6437638502332,12.2151816733544));
#53523=CARTESIAN_POINT('Ctrl Pts',(-1.36281186129439,88.7857780281219,11.3617747378727));
#53524=CARTESIAN_POINT('Ctrl Pts',(-0.708363110808276,88.875603696437,11.0373579101007));
#53525=CARTESIAN_POINT('Ctrl Pts',(0.154442061731767,88.9843715742907,10.8781781251525));
#53526=CARTESIAN_POINT('Ctrl Pts',(1.14878610904288,89.1066838810156,11.0687174671823));
#53527=CARTESIAN_POINT('Ctrl Pts',(2.44768052466662,89.3119705930039,12.1741273499311));
#53528=CARTESIAN_POINT('Ctrl Pts',(2.6701128707135,89.5078881935536,13.9154669359159));
#53529=CARTESIAN_POINT('Ctrl Pts',(1.91898192293812,89.6707854617373,15.0303878015014));
#53530=CARTESIAN_POINT('Ctrl Pts',(1.20035754076689,89.7890999582511,15.6471784629207));
#53531=CARTESIAN_POINT('Ctrl Pts',(0.150907763099969,89.9236515137611,16.0455501666756));
#53532=CARTESIAN_POINT('Ctrl Pts',(-1.33982560582105,90.1061290556921,15.7536692911111));
#53533=CARTESIAN_POINT('Ctrl Pts',(-2.47248246309965,90.2916555010373,14.7026685121508));
#53534=CARTESIAN_POINT('Ctrl Pts',(-2.88638513132925,90.4801893569489,13.188303779548));
#53535=CARTESIAN_POINT('Ctrl Pts',(-2.43281412716261,90.6716752177104,11.6600430092875));
#53536=CARTESIAN_POINT('Ctrl Pts',(-1.22294135571961,90.8660432173068,10.5850381331131));
#53537=CARTESIAN_POINT('Ctrl Pts',(-0.145014100913177,90.9974883817239,
10.3989978074825));
#53538=CARTESIAN_POINT('Ctrl Pts',(0.381971510233331,91.0636609782751,10.4564983789973));
#53539=CARTESIAN_POINT('Ctrl Pts',(0.882819182839093,82.434273975252,10.9600650642734));
#53540=CARTESIAN_POINT('Ctrl Pts',(1.32234931660589,82.49372279071,11.1436569777094));
#53541=CARTESIAN_POINT('Ctrl Pts',(2.07175718869597,82.6097538212342,11.7563396296457));
#53542=CARTESIAN_POINT('Ctrl Pts',(2.52038751802309,82.7795502144957,13.0973970519055));
#53543=CARTESIAN_POINT('Ctrl Pts',(2.20412951709352,82.9444115294294,14.4334386057238));
#53544=CARTESIAN_POINT('Ctrl Pts',(1.2501937101171,83.1060430186465,15.3832282632374));
#53545=CARTESIAN_POINT('Ctrl Pts',(-0.0351772261966642,83.2645164148681,
15.6820036159229));
#53546=CARTESIAN_POINT('Ctrl Pts',(-1.26146205986579,83.4199185973822,15.2661582656774));
#53547=CARTESIAN_POINT('Ctrl Pts',(-2.06715480101835,83.5723503779501,14.2871057729414));
#53548=CARTESIAN_POINT('Ctrl Pts',(-2.2550767294348,83.7385476570392,12.9134863983464));
#53549=CARTESIAN_POINT('Ctrl Pts',(-1.49788374351813,83.9174776039795,11.5807287894401));
#53550=CARTESIAN_POINT('Ctrl Pts',(0.0582321938564075,84.1081652168351,
11.0699905106014));
#53551=CARTESIAN_POINT('Ctrl Pts',(1.51585306159387,84.2947233957224,11.7309518172656));
#53552=CARTESIAN_POINT('Ctrl Pts',(2.13777206160342,84.4775690798224,13.1718249945562));
#53553=CARTESIAN_POINT('Ctrl Pts',(1.63017502161623,84.6571413216995,14.6288262088296));
#53554=CARTESIAN_POINT('Ctrl Pts',(0.408605219823062,84.8191834771113,15.2902270292953));
#53555=CARTESIAN_POINT('Ctrl Pts',(-0.790764902528728,84.9648170451454,
15.1077088441999));
#53556=CARTESIAN_POINT('Ctrl Pts',(-1.68677733589476,85.105638246113,14.3496273894146));
#53557=CARTESIAN_POINT('Ctrl Pts',(-1.94699460445861,85.2346652278456,13.2845428803274));
#53558=CARTESIAN_POINT('Ctrl Pts',(-1.6216470532816,85.3631169137173,12.2835368681594));
#53559=CARTESIAN_POINT('Ctrl Pts',(-0.92161910793314,85.4805385490169,11.6004286584856));
#53560=CARTESIAN_POINT('Ctrl Pts',(-0.0557472811106569,85.5871429698282,
11.4115657573635));
#53561=CARTESIAN_POINT('Ctrl Pts',(0.961839866628155,85.7151102748299,11.6138235113798));
#53562=CARTESIAN_POINT('Ctrl Pts',(1.77478479498137,85.8432535124287,12.3760029651859));
#53563=CARTESIAN_POINT('Ctrl Pts',(1.92430465852295,85.993507459578,13.622136338525));
#53564=CARTESIAN_POINT('Ctrl Pts',(1.47261397095176,86.1230431058733,14.5999972868073));
#53565=CARTESIAN_POINT('Ctrl Pts',(0.564292359246367,86.2535482648462,15.1984149573149));
#53566=CARTESIAN_POINT('Ctrl Pts',(-0.440464124926358,86.3742644732228,
15.2255377238975));
#53567=CARTESIAN_POINT('Ctrl Pts',(-1.0905220530923,86.4628791205409,14.9026132404033));
#53568=CARTESIAN_POINT('Ctrl Pts',(-1.62028029987006,86.5520096078327,14.4213512934408));
#53569=CARTESIAN_POINT('Ctrl Pts',(-2.01528583756397,86.6530372921974,13.678712405819));
#53570=CARTESIAN_POINT('Ctrl Pts',(-1.93705288041765,86.7895460089237,12.5449612931179));
#53571=CARTESIAN_POINT('Ctrl Pts',(-1.19030318300388,86.943443150078,11.502847580665));
#53572=CARTESIAN_POINT('Ctrl Pts',(0.220700072712643,87.1158361421535,11.0636116347951));
#53573=CARTESIAN_POINT('Ctrl Pts',(1.71574627922587,87.3081755676547,11.7644563393486));
#53574=CARTESIAN_POINT('Ctrl Pts',(2.35793114748454,87.5051595245611,13.3293810057776));
#53575=CARTESIAN_POINT('Ctrl Pts',(1.76605084983632,87.7071050582604,14.9574599737328));
#53576=CARTESIAN_POINT('Ctrl Pts',(0.186162948047658,87.9143057928158,15.778617672352));
#53577=CARTESIAN_POINT('Ctrl Pts',(-1.57708437496644,88.1269904896355,15.3081592099618));
#53578=CARTESIAN_POINT('Ctrl Pts',(-2.58834315889874,88.3453631534556,13.7278161392108));
#53579=CARTESIAN_POINT('Ctrl Pts',(-2.31256599907742,88.5321949612197,12.1506055675816));
#53580=CARTESIAN_POINT('Ctrl Pts',(-1.47911440190093,88.6846247171001,11.226560437249));
#53581=CARTESIAN_POINT('Ctrl Pts',(-0.779221392801904,88.7811327907629,
10.871446383874));
#53582=CARTESIAN_POINT('Ctrl Pts',(0.146787911223744,88.8980616482805,10.691788534228));
#53583=CARTESIAN_POINT('Ctrl Pts',(1.21837875087259,89.0296430750967,10.8869822781816));
#53584=CARTESIAN_POINT('Ctrl Pts',(2.62736919439976,89.2506250048775,12.0644480443334));
#53585=CARTESIAN_POINT('Ctrl Pts',(2.88322761275398,89.4616161114694,13.9377699336378));
#53586=CARTESIAN_POINT('Ctrl Pts',(2.08465431401534,89.63698147581,15.1449088342394));
#53587=CARTESIAN_POINT('Ctrl Pts',(1.31680480345452,89.7643194785334,15.8152558067619));
#53588=CARTESIAN_POINT('Ctrl Pts',(0.191219693405885,89.9090769332071,16.2531492772627));
#53589=CARTESIAN_POINT('Ctrl Pts',(-1.41372324784499,90.1052182137141,15.9522926041556));
#53590=CARTESIAN_POINT('Ctrl Pts',(-2.638687187275,90.3043984618164,14.8334899831074));
#53591=CARTESIAN_POINT('Ctrl Pts',(-3.09497900539232,90.5065120393991,13.2134195307825));
#53592=CARTESIAN_POINT('Ctrl Pts',(-2.62197778632827,90.7114391447102,11.5741341454235));
#53593=CARTESIAN_POINT('Ctrl Pts',(-1.33822874690071,90.9190461806365,10.416218944302));
#53594=CARTESIAN_POINT('Ctrl Pts',(-0.190787352387184,91.0591411352891,
10.2094796873319));
#53595=CARTESIAN_POINT('Ctrl Pts',(0.37068114634458,91.1295839610538,10.2664130498865));
#53596=CARTESIAN_POINT('Ctrl Pts',(0.920533865651003,82.4393565600724,10.9761000835092));
#53597=CARTESIAN_POINT('Ctrl Pts',(0.930994513306672,82.4407797944805,10.9806730010019));
#53598=CARTESIAN_POINT('Ctrl Pts',(0.941423665733055,82.4422018898699,10.9853165122668));
#53599=CARTESIAN_POINT('Ctrl Pts',(0.951820353857793,82.4436229114634,10.9900301168068));
#53600=CARTESIAN_POINT('Ctrl Pts',(1.02615204531446,82.453782583214,11.0237302907574));
#53601=CARTESIAN_POINT('Ctrl Pts',(1.09881834405504,82.4638831712601,11.0610046463177));
#53602=CARTESIAN_POINT('Ctrl Pts',(1.1694201192702,82.4739548102459,11.1016609610774));
#53603=CARTESIAN_POINT('Ctrl Pts',(1.23335157916184,82.4830749008089,11.1384761480679));
#53604=CARTESIAN_POINT('Ctrl Pts',(1.29558946004411,82.4921711969464,11.178064012004));
#53605=CARTESIAN_POINT('Ctrl Pts',(1.35582412660719,82.5012626039083,11.2202475575312));
#53606=CARTESIAN_POINT('Ctrl Pts',(1.42322871684646,82.5114361899167,11.2674523444644));
#53607=CARTESIAN_POINT('Ctrl Pts',(1.48812697663125,82.5216063052533,11.3179140070938));
#53608=CARTESIAN_POINT('Ctrl Pts',(1.55011210052986,82.5318142072745,11.3714148650172));
#53609=CARTESIAN_POINT('Ctrl Pts',(1.57821000765237,82.5364414575704,11.3956668474664));
#53610=CARTESIAN_POINT('Ctrl Pts',(1.60570885058393,82.5410763797476,11.4205428057615));
#53611=CARTESIAN_POINT('Ctrl Pts',(1.63256866727547,82.5457223547656,11.4460196295166));
#53612=CARTESIAN_POINT('Ctrl Pts',(1.68097537945571,82.5540953223878,11.4919339143734));
#53613=CARTESIAN_POINT('Ctrl Pts',(1.72731518937305,82.5625081638741,11.5398143925773));
#53614=CARTESIAN_POINT('Ctrl Pts',(1.7715643694936,82.5709132106333,11.5894150810159));
#53615=CARTESIAN_POINT('Ctrl Pts',(1.81569939097242,82.5792965731778,11.6388878044345));
#53616=CARTESIAN_POINT('Ctrl Pts',(1.85775518464244,82.5876721800752,11.6900715580635));
#53617=CARTESIAN_POINT('Ctrl Pts',(1.89773094642547,82.5959989594274,11.7427682864444));
#53618=CARTESIAN_POINT('Ctrl Pts',(1.91033667158171,82.5986246777945,11.7593853675198));
#53619=CARTESIAN_POINT('Ctrl Pts',(1.92273569868281,82.6012455876238,11.7761532549623));
#53620=CARTESIAN_POINT('Ctrl Pts',(1.93492831235468,82.6038605304053,11.7930667633059));
#53621=CARTESIAN_POINT('Ctrl Pts',(1.94582122437246,82.606196726927,11.8081773346121));
#53622=CARTESIAN_POINT('Ctrl Pts',(1.95656549789998,82.6085228755565,11.8233952376663));
#53623=CARTESIAN_POINT('Ctrl Pts',(1.96712724119019,82.610848366971,11.8387322038599));
#53624=CARTESIAN_POINT('Ctrl Pts',(1.96715436113799,82.6108543382585,11.8387715854005));
#53625=CARTESIAN_POINT('Ctrl Pts',(1.96718147988153,82.6108603095415,11.8388109677247));
#53626=CARTESIAN_POINT('Ctrl Pts',(1.96720859742029,82.61086628082,11.8388503508325));
#53627=CARTESIAN_POINT('Ctrl Pts',(2.04383660407255,82.6277397581419,11.9501380705541));
#53628=CARTESIAN_POINT('Ctrl Pts',(2.11078017326571,82.6445646537931,12.0675952760296));
#53629=CARTESIAN_POINT('Ctrl Pts',(2.16755235526014,82.661334864107,12.1893717483931));
#53630=CARTESIAN_POINT('Ctrl Pts',(2.22793839858296,82.6791725904542,12.3188999623443));
#53631=CARTESIAN_POINT('Ctrl Pts',(2.27681893361483,82.6969483090552,12.4533119179796));
#53632=CARTESIAN_POINT('Ctrl Pts',(2.31365407565392,82.7146619567084,12.5904314693233));
#53633=CARTESIAN_POINT('Ctrl Pts',(2.34880641410517,82.7315663611178,12.7212867507283));
#53634=CARTESIAN_POINT('Ctrl Pts',(2.37299160473249,82.7484143374262,12.8546084560198));
#53635=CARTESIAN_POINT('Ctrl Pts',(2.38574068823176,82.7652115237532,12.9885594457077));
#53636=CARTESIAN_POINT('Ctrl Pts',(2.38923264560951,82.7698122512269,13.0252484474484));
#53637=CARTESIAN_POINT('Ctrl Pts',(2.39186681884341,82.7744087884096,13.0619816538601));
#53638=CARTESIAN_POINT('Ctrl Pts',(2.39385078342915,82.7789577812924,13.0987563954806));
#53639=CARTESIAN_POINT('Ctrl Pts',(2.39385087309786,82.7789579868921,13.0987580575786));
#53640=CARTESIAN_POINT('Ctrl Pts',(2.39385096276524,82.7789581924915,13.0987597196767));
#53641=CARTESIAN_POINT('Ctrl Pts',(2.3938510524313,82.7789583980909,13.098761381775));
#53642=CARTESIAN_POINT('Ctrl Pts',(2.39752709562371,82.7873873662675,13.166902497685));
#53643=CARTESIAN_POINT('Ctrl Pts',(2.39828854108446,82.7957891942172,13.2350848776881));
#53644=CARTESIAN_POINT('Ctrl Pts',(2.39605616560726,82.8041987158248,13.3030783290674));
#53645=CARTESIAN_POINT('Ctrl Pts',(2.39521945688256,82.8073506587535,13.3285627131114));
#53646=CARTESIAN_POINT('Ctrl Pts',(2.39396213470044,82.8105036170795,13.3540200372025));
#53647=CARTESIAN_POINT('Ctrl Pts',(2.39228000488214,82.8136591892446,13.3794363069799));
#53648=CARTESIAN_POINT('Ctrl Pts',(2.38582315035503,82.8257718515364,13.4769966467281));
#53649=CARTESIAN_POINT('Ctrl Pts',(2.37310613543231,82.8379259190769,13.5739780393391));
#53650=CARTESIAN_POINT('Ctrl Pts',(2.35445818219782,82.8500908714037,13.6696283756344));
#53651=CARTESIAN_POINT('Ctrl Pts',(2.33923615030137,82.8600209312879,13.7477062457193));
#53652=CARTESIAN_POINT('Ctrl Pts',(2.32006269363205,82.8699583679949,13.8248982501427));
#53653=CARTESIAN_POINT('Ctrl Pts',(2.29711475887482,82.8798899526932,13.9008207825145));
#53654=CARTESIAN_POINT('Ctrl Pts',(2.26972748757379,82.8917428277976,13.9914307225341));
#53655=CARTESIAN_POINT('Ctrl Pts',(2.23696730721706,82.9035860950502,14.0802302740837));
#53656=CARTESIAN_POINT('Ctrl Pts',(2.19914064222399,82.9153963320166,14.1665197842907));
#53657=CARTESIAN_POINT('Ctrl Pts',(2.16873815448171,82.924888593221,14.2358733944184));
#53658=CARTESIAN_POINT('Ctrl Pts',(2.13506345482034,82.9343596099332,14.3036063662027));
#53659=CARTESIAN_POINT('Ctrl Pts',(2.09828154655871,82.9437995142575,14.3693790747516));
#53660=CARTESIAN_POINT('Ctrl Pts',(2.09827926593422,82.9438000995691,14.369383152921));
#53661=CARTESIAN_POINT('Ctrl Pts',(2.09827698529767,82.9438006848806,14.3693872310829));
#53662=CARTESIAN_POINT('Ctrl Pts',(2.09827470464909,82.943801270192,14.3693913092375));
#53663=CARTESIAN_POINT('Ctrl Pts',(2.09693217075603,82.9441458214716,14.3717919687587));
#53664=CARTESIAN_POINT('Ctrl Pts',(2.09558546479307,82.9444903396463,14.374190068563));
#53665=CARTESIAN_POINT('Ctrl Pts',(2.09423459446982,82.9448348255343,14.3765855912899));
#53666=CARTESIAN_POINT('Ctrl Pts',(2.04022528568224,82.9586077572339,14.4723612734103));
#53667=CARTESIAN_POINT('Ctrl Pts',(1.97962952520666,82.9723175346397,14.5640780526061));
#53668=CARTESIAN_POINT('Ctrl Pts',(1.91316752949104,82.9859834432265,14.6510156889316));
#53669=CARTESIAN_POINT('Ctrl Pts',(1.87270278139702,82.9943038004846,14.7039468342565));
#53670=CARTESIAN_POINT('Ctrl Pts',(1.83006374203318,83.0026077717938,14.7551053957788));
#53671=CARTESIAN_POINT('Ctrl Pts',(1.78541721884374,83.0108985437968,14.8043204535108));
#53672=CARTESIAN_POINT('Ctrl Pts',(1.65763162308314,83.0346280789104,14.9451819366323));
#53673=CARTESIAN_POINT('Ctrl Pts',(1.51336634790013,83.0582549027632,15.0700837180756));
#53674=CARTESIAN_POINT('Ctrl Pts',(1.35699330054957,83.0817754177794,15.1752608586358));
#53675=CARTESIAN_POINT('Ctrl Pts',(1.30429717907158,83.0897015913593,15.2107044818789));
#53676=CARTESIAN_POINT('Ctrl Pts',(1.25028177908284,83.0976059460742,15.2440258520453));
#53677=CARTESIAN_POINT('Ctrl Pts',(1.19506856748379,83.1054958017013,15.2750223457027));
#53678=CARTESIAN_POINT('Ctrl Pts',(1.19506406440212,83.1054964451826,15.2750248737162));
#53679=CARTESIAN_POINT('Ctrl Pts',(1.19505956131248,83.1054970886637,15.2750274017142));
#53680=CARTESIAN_POINT('Ctrl Pts',(1.1950550582149,83.1054977321447,15.2750299296967));
#53681=CARTESIAN_POINT('Ctrl Pts',(1.1347180566568,83.1141197338409,15.3089023658992));
#53682=CARTESIAN_POINT('Ctrl Pts',(1.07295896734627,83.1227234186035,15.3399797628626));
#53683=CARTESIAN_POINT('Ctrl Pts',(1.00999286229148,83.1313199199441,15.3680862300822));
#53684=CARTESIAN_POINT('Ctrl Pts',(0.995778869549489,83.1332604974588,15.3744309947888));
#53685=CARTESIAN_POINT('Ctrl Pts',(0.981503556850033,83.1352006824813,15.3806242744179));
#53686=CARTESIAN_POINT('Ctrl Pts',(0.967169734092123,83.1371405568294,15.3866639028358));
#53687=CARTESIAN_POINT('Ctrl Pts',(0.883478264771382,83.1484669794617,15.4219277249845));
#53688=CARTESIAN_POINT('Ctrl Pts',(0.797774212518988,83.1597853120529,15.4519580355328));
#53689=CARTESIAN_POINT('Ctrl Pts',(0.710743099405598,83.171086254001,15.4767512079966));
#53690=CARTESIAN_POINT('Ctrl Pts',(0.652124685216517,83.1786978226935,15.4934502527469));
#53691=CARTESIAN_POINT('Ctrl Pts',(0.59290321784703,83.1863016382014,15.5077739015619));
#53692=CARTESIAN_POINT('Ctrl Pts',(0.533275044503793,83.1938965479578,15.51972279897));
#53693=CARTESIAN_POINT('Ctrl Pts',(0.436752412107777,83.2061907478537,15.5390649818242));
#53694=CARTESIAN_POINT('Ctrl Pts',(0.33917125756754,83.2184569160692,15.5523664089726));
#53695=CARTESIAN_POINT('Ctrl Pts',(0.241390583592281,83.2306917323916,15.559404755261));
#53696=CARTESIAN_POINT('Ctrl Pts',(0.195580195304286,83.2364237616728,15.5627022307566));
#53697=CARTESIAN_POINT('Ctrl Pts',(0.149726630899953,83.2421488480259,15.5646254222749));
#53698=CARTESIAN_POINT('Ctrl Pts',(0.103921117916872,83.247866324241,15.5651541213653));
#53699=CARTESIAN_POINT('Ctrl Pts',(0.0607635922639142,83.2532532768228,
15.5656522567002));
#53700=CARTESIAN_POINT('Ctrl Pts',(0.0176523014704029,83.2586332082964,
15.5649035786488));
#53701=CARTESIAN_POINT('Ctrl Pts',(-0.0253295424226451,83.2640045459169,
15.5629001654344));
#53702=CARTESIAN_POINT('Ctrl Pts',(-0.0253674153657417,83.2640092788074,
15.5628984001505));
#53703=CARTESIAN_POINT('Ctrl Pts',(-0.0254052882083584,83.2640140116914,
15.5628966338927));
#53704=CARTESIAN_POINT('Ctrl Pts',(-0.025443160950471,83.2640187445686,
15.5628948666609));
#53705=CARTESIAN_POINT('Ctrl Pts',(-0.102628557979231,83.273664441926,15.5592932133354));
#53706=CARTESIAN_POINT('Ctrl Pts',(-0.17953270492342,83.2832960245341,15.5518071478355));
#53707=CARTESIAN_POINT('Ctrl Pts',(-0.255746825396155,83.292912320685,15.5404684889302));
#53708=CARTESIAN_POINT('Ctrl Pts',(-0.294626486742618,83.2978179514977,
15.5346842167294));
#53709=CARTESIAN_POINT('Ctrl Pts',(-0.333325787768408,83.3027195064199,
15.5278976329917));
#53710=CARTESIAN_POINT('Ctrl Pts',(-0.371785817460665,83.3076162188687,
15.5201152844023));
#53711=CARTESIAN_POINT('Ctrl Pts',(-0.417916676564152,83.313489577622,15.5107807511441));
#53712=CARTESIAN_POINT('Ctrl Pts',(-0.463697662900614,83.3193558862578,
15.499983461912));
#53713=CARTESIAN_POINT('Ctrl Pts',(-0.509026553977117,83.325213952138,15.4877233112308));
#53714=CARTESIAN_POINT('Ctrl Pts',(-0.580017665418723,83.3343884675045,
15.4685222740415));
#53715=CARTESIAN_POINT('Ctrl Pts',(-0.649902559680175,83.3435431400438,
15.4457301312203));
#53716=CARTESIAN_POINT('Ctrl Pts',(-0.718388236301924,83.3526802822629,
15.4196147550527));
#53717=CARTESIAN_POINT('Ctrl Pts',(-0.757687564455145,83.3579234742436,
15.4046288954032));
#53718=CARTESIAN_POINT('Ctrl Pts',(-0.796527047443576,83.3631610125617,
15.3885483859335));
#53719=CARTESIAN_POINT('Ctrl Pts',(-0.834857972488083,83.3683942942767,
15.3714199738278));
#53720=CARTESIAN_POINT('Ctrl Pts',(-0.900204612771983,83.3773160037669,
15.3422194214485));
#53721=CARTESIAN_POINT('Ctrl Pts',(-0.964154981785965,83.386233016291,15.3101017265351));
#53722=CARTESIAN_POINT('Ctrl Pts',(-1.02631379660646,83.3951374072177,15.2750876881961));
#53723=CARTESIAN_POINT('Ctrl Pts',(-1.04641301710453,83.398016666051,15.2637658044193));
#53724=CARTESIAN_POINT('Ctrl Pts',(-1.06632462917669,83.4008945582043,15.2521413717555));
#53725=CARTESIAN_POINT('Ctrl Pts',(-1.08603449675238,83.403770680953,15.2402159565468));
#53726=CARTESIAN_POINT('Ctrl Pts',(-1.1165315839713,83.4082209070127,15.221763756077));
#53727=CARTESIAN_POINT('Ctrl Pts',(-1.14654451282116,83.4126667380911,15.2025915369825));
#53728=CARTESIAN_POINT('Ctrl Pts',(-1.17602742366442,83.4171070602856,15.1827217267305));
#53729=CARTESIAN_POINT('Ctrl Pts',(-1.18115537816718,83.4178793642929,15.1792657761464));
#53730=CARTESIAN_POINT('Ctrl Pts',(-1.18626732394777,83.4186515049187,15.1757887122118));
#53731=CARTESIAN_POINT('Ctrl Pts',(-1.19136337777988,83.4194235303912,15.1722904085955));
#53732=CARTESIAN_POINT('Ctrl Pts',(-1.20370360741183,83.4212930105666,15.1638191735244));
#53733=CARTESIAN_POINT('Ctrl Pts',(-1.21595052391483,83.4231617944611,15.1552235063429));
#53734=CARTESIAN_POINT('Ctrl Pts',(-1.22810567416795,83.4250303944022,15.1465034350886));
#53735=CARTESIAN_POINT('Ctrl Pts',(-1.3048196415846,83.4368235612503,15.0914690465254));
#53736=CARTESIAN_POINT('Ctrl Pts',(-1.3778034004921,83.4485983575214,15.0315266355163));
#53737=CARTESIAN_POINT('Ctrl Pts',(-1.44655635735356,83.4603445874994,14.9673737889971));
#53738=CARTESIAN_POINT('Ctrl Pts',(-1.46682813418681,83.4638079578563,14.948458352524));
#53739=CARTESIAN_POINT('Ctrl Pts',(-1.48673238395627,83.4672688566375,14.9291770775887));
#53740=CARTESIAN_POINT('Ctrl Pts',(-1.50625700994449,83.4707270522028,14.9095482865858));
#53741=CARTESIAN_POINT('Ctrl Pts',(-1.55111765444156,83.4786727553343,14.8644483079424));
#53742=CARTESIAN_POINT('Ctrl Pts',(-1.59404661937215,83.4866129941764,14.8175620406124));
#53743=CARTESIAN_POINT('Ctrl Pts',(-1.63479702237727,83.4945348551692,14.768981806382));
#53744=CARTESIAN_POINT('Ctrl Pts',(-1.65962609684212,83.499361616673,14.7393820438207));
#53745=CARTESIAN_POINT('Ctrl Pts',(-1.68364569267376,83.5041814271582,14.7091541429046));
#53746=CARTESIAN_POINT('Ctrl Pts',(-1.70679447914964,83.5089901673716,14.678326641304));
#53747=CARTESIAN_POINT('Ctrl Pts',(-1.75589190588166,83.5191892666008,14.612943041056));
#53748=CARTESIAN_POINT('Ctrl Pts',(-1.80124541987183,83.5293612597565,14.5449417134995));
#53749=CARTESIAN_POINT('Ctrl Pts',(-1.8426741934976,83.5395229198191,14.4747652361496));
#53750=CARTESIAN_POINT('Ctrl Pts',(-1.86260765044563,83.5444122031759,14.4409998198075));
#53751=CARTESIAN_POINT('Ctrl Pts',(-1.88163269427647,83.5492991862322,14.4067300963384));
#53752=CARTESIAN_POINT('Ctrl Pts',(-1.8997296875192,83.5541862481475,14.3720011160247));
#53753=CARTESIAN_POINT('Ctrl Pts',(-1.92158429925602,83.5600880484774,14.3300610892704));
#53754=CARTESIAN_POINT('Ctrl Pts',(-1.94204849094845,83.5659844261093,14.287444637675));
#53755=CARTESIAN_POINT('Ctrl Pts',(-1.96106096675531,83.5718746730521,14.2442382822083));
#53756=CARTESIAN_POINT('Ctrl Pts',(-1.99815646377279,83.5833672130095,14.1599377814934));
#53757=CARTESIAN_POINT('Ctrl Pts',(-2.02972387459205,83.5948362906809,14.073392176862));
#53758=CARTESIAN_POINT('Ctrl Pts',(-2.05567441802314,83.6062770112547,13.9853995832281));
#53759=CARTESIAN_POINT('Ctrl Pts',(-2.082910325879,83.6182844057117,13.8930486011156));
#53760=CARTESIAN_POINT('Ctrl Pts',(-2.10396279000991,83.6302614193266,13.7990979105521));
#53761=CARTESIAN_POINT('Ctrl Pts',(-2.11875188980933,83.6422080216074,13.7044276981067));
#53762=CARTESIAN_POINT('Ctrl Pts',(-2.13568049761226,83.6558829137463,13.5960617448815));
#53763=CARTESIAN_POINT('Ctrl Pts',(-2.14440607927575,83.6695174237031,13.4867574548221));
#53764=CARTESIAN_POINT('Ctrl Pts',(-2.14480094308811,83.6831222411339,13.3777440851263));
#53765=CARTESIAN_POINT('Ctrl Pts',(-2.1449848087353,83.68945723179,13.3269827513613));
#53766=CARTESIAN_POINT('Ctrl Pts',(-2.14336126039987,83.6957863688328,13.2762797618052));
#53767=CARTESIAN_POINT('Ctrl Pts',(-2.13991520788354,83.7021084497047,13.2257776338899));
#53768=CARTESIAN_POINT('Ctrl Pts',(-2.13735460109351,83.7068061039427,13.1882517717509));
#53769=CARTESIAN_POINT('Ctrl Pts',(-2.13378782571262,83.711499651679,13.1508385175056));
#53770=CARTESIAN_POINT('Ctrl Pts',(-2.12921075693525,83.7161880527221,13.1136005849409));
#53771=CARTESIAN_POINT('Ctrl Pts',(-2.12749003241444,83.7179506320126,13.0996011834057));
#53772=CARTESIAN_POINT('Ctrl Pts',(-2.12562663483203,83.7197124004024,13.0856272189981));
#53773=CARTESIAN_POINT('Ctrl Pts',(-2.12362006952077,83.7214735974353,13.0716796777322));
#53774=CARTESIAN_POINT('Ctrl Pts',(-2.12170821201978,83.7231516677871,13.0583904460088));
#53775=CARTESIAN_POINT('Ctrl Pts',(-2.11966627769195,83.7248293207514,13.0451243973671));
#53776=CARTESIAN_POINT('Ctrl Pts',(-2.11749488714512,83.7265069918328,13.0318801072292));
#53777=CARTESIAN_POINT('Ctrl Pts',(-2.10743796819187,83.7342772209703,12.9705384233463));
#53778=CARTESIAN_POINT('Ctrl Pts',(-2.09483566207979,83.7420931254287,12.9096366888758));
#53779=CARTESIAN_POINT('Ctrl Pts',(-2.07967270917475,83.7499239804326,12.8494260098162));
#53780=CARTESIAN_POINT('Ctrl Pts',(-2.06847733416977,83.7557057934427,12.8049702144578));
#53781=CARTESIAN_POINT('Ctrl Pts',(-2.05588647717042,83.7614956354928,12.7608921651894));
#53782=CARTESIAN_POINT('Ctrl Pts',(-2.04190468002499,83.7672790925443,12.7173075817562));
#53783=CARTESIAN_POINT('Ctrl Pts',(-2.02043797771301,83.7761586199448,12.6503907706897));
#53784=CARTESIAN_POINT('Ctrl Pts',(-1.99565768808357,83.7850145658778,12.5846513691579));
#53785=CARTESIAN_POINT('Ctrl Pts',(-1.9676515739853,83.7938109299173,12.5204627342433));
#53786=CARTESIAN_POINT('Ctrl Pts',(-1.9538485678395,83.7981462784942,12.4888269236089));
#53787=CARTESIAN_POINT('Ctrl Pts',(-1.93926241902684,83.8024670525039,12.4575684725663));
#53788=CARTESIAN_POINT('Ctrl Pts',(-1.92390657318214,83.8067683519166,12.4267356533827));
#53789=CARTESIAN_POINT('Ctrl Pts',(-1.89166098374728,83.8158006081858,12.3619901200809));
#53790=CARTESIAN_POINT('Ctrl Pts',(-1.85601110579874,83.8247473695038,12.2991102096693));
#53791=CARTESIAN_POINT('Ctrl Pts',(-1.81727422075553,83.8336388418575,12.238344897837));
#53792=CARTESIAN_POINT('Ctrl Pts',(-1.79796068687771,83.8380719745767,12.2080483753531));
#53793=CARTESIAN_POINT('Ctrl Pts',(-1.77787917342235,83.8424914562996,12.1782769483276));
#53794=CARTESIAN_POINT('Ctrl Pts',(-1.75706515116445,83.8469015828313,12.1490586139349));
#53795=CARTESIAN_POINT('Ctrl Pts',(-1.71277251746687,83.856286415643,12.08688144479));
#53796=CARTESIAN_POINT('Ctrl Pts',(-1.66531380074296,83.8656823428975,12.0270797276552));
#53797=CARTESIAN_POINT('Ctrl Pts',(-1.61500751869232,83.8751276643025,11.969942402271));
#53798=CARTESIAN_POINT('Ctrl Pts',(-1.59336574893447,83.8791910429265,11.9453619166908));
#53799=CARTESIAN_POINT('Ctrl Pts',(-1.57119653894742,83.8832636510564,11.9212740518963));
#53800=CARTESIAN_POINT('Ctrl Pts',(-1.54852306630582,83.8873489352535,11.8976998295399));
#53801=CARTESIAN_POINT('Ctrl Pts',(-1.49732767543146,83.8965732708729,11.8444705978659));
#53802=CARTESIAN_POINT('Ctrl Pts',(-1.44338996086774,83.9057839105178,11.7940717731439));
#53803=CARTESIAN_POINT('Ctrl Pts',(-1.38703478780361,83.914966322146,11.7469233471102));
#53804=CARTESIAN_POINT('Ctrl Pts',(-1.38343386813591,83.9155530495897,11.7439107098424));
#53805=CARTESIAN_POINT('Ctrl Pts',(-1.37982308897923,83.9161396618501,11.7409113290383));
#53806=CARTESIAN_POINT('Ctrl Pts',(-1.37620253927408,83.9167261551632,11.7379253082228));
#53807=CARTESIAN_POINT('Ctrl Pts',(-1.37612089191015,83.9167393812302,11.7378579701808));
#53808=CARTESIAN_POINT('Ctrl Pts',(-1.37603923957738,83.9167526072368,11.737790638933));
#53809=CARTESIAN_POINT('Ctrl Pts',(-1.37595758227736,83.9167658331827,11.7377233144798));
#53810=CARTESIAN_POINT('Ctrl Pts',(-1.31802902337669,83.9261484602153,11.6899626299106));
#53811=CARTESIAN_POINT('Ctrl Pts',(-1.25743212616101,83.9355275036484,11.6454873917573));
#53812=CARTESIAN_POINT('Ctrl Pts',(-1.19470546146937,83.9449119543165,11.604431264857));
#53813=CARTESIAN_POINT('Ctrl Pts',(-1.17671609789645,83.947603318441,11.5926567890844));
#53814=CARTESIAN_POINT('Ctrl Pts',(-1.15855158918339,83.9502951516034,11.5811632006949));
#53815=CARTESIAN_POINT('Ctrl Pts',(-1.14022464344702,83.9529877242921,11.5699528728668));
#53816=CARTESIAN_POINT('Ctrl Pts',(-1.09406051506142,83.9597701021678,11.5417149427421));
#53817=CARTESIAN_POINT('Ctrl Pts',(-1.04695490462354,83.9666268406677,11.5150804142541));
#53818=CARTESIAN_POINT('Ctrl Pts',(-0.998974241279411,83.9735062868492,
11.4902348779045));
#53819=CARTESIAN_POINT('Ctrl Pts',(-0.960745749746977,83.9789874709714,
11.4704392496292));
#53820=CARTESIAN_POINT('Ctrl Pts',(-0.921962617620407,83.9844829431642,
11.4517799302311));
#53821=CARTESIAN_POINT('Ctrl Pts',(-0.88268051519462,83.9899636398392,11.434358889804));
#53822=CARTESIAN_POINT('Ctrl Pts',(-0.816695114645877,83.9991700199222,
11.4050953254942));
#53823=CARTESIAN_POINT('Ctrl Pts',(-0.749301312910663,84.0083340447604,
11.3793265531328));
#53824=CARTESIAN_POINT('Ctrl Pts',(-0.680845101544926,84.01741093097,11.3572724133502));
#53825=CARTESIAN_POINT('Ctrl Pts',(-0.658885316737399,84.0203226677417,
11.350197757098));
#53826=CARTESIAN_POINT('Ctrl Pts',(-0.63681656120727,84.0232253855314,11.3435055292045));
#53827=CARTESIAN_POINT('Ctrl Pts',(-0.61465129680208,84.0261174586991,11.337203426556));
#53828=CARTESIAN_POINT('Ctrl Pts',(-0.586163091571372,84.0298345347708,
11.3291035640706));
#53829=CARTESIAN_POINT('Ctrl Pts',(-0.557514326792003,84.0335343414654,
11.3216473411737));
#53830=CARTESIAN_POINT('Ctrl Pts',(-0.528729632709615,84.0372142064508,
11.3148495329407));
#53831=CARTESIAN_POINT('Ctrl Pts',(-0.465587636856985,84.0452863443369,
11.2999378865628));
#53832=CARTESIAN_POINT('Ctrl Pts',(-0.40178544084305,84.0532626606676,11.2881948406741));
#53833=CARTESIAN_POINT('Ctrl Pts',(-0.337666692143502,84.0611911519319,
11.2795709196196));
#53834=CARTESIAN_POINT('Ctrl Pts',(-0.306667368869647,84.06502431881,11.2754015351248));
#53835=CARTESIAN_POINT('Ctrl Pts',(-0.275593292892654,84.0688464065403,
11.2719610487364));
#53836=CARTESIAN_POINT('Ctrl Pts',(-0.244478997263503,84.072663396452,11.2692433684568));
#53837=CARTESIAN_POINT('Ctrl Pts',(-0.181914129491077,84.080338629469,11.2637786358023));
#53838=CARTESIAN_POINT('Ctrl Pts',(-0.119189614352646,84.0879938376136,
11.2612358390966));
#53839=CARTESIAN_POINT('Ctrl Pts',(-0.0566277683661131,84.0956727428236,
11.2615605645425));
#53840=CARTESIAN_POINT('Ctrl Pts',(-0.0237304160100429,84.0997105976282,
11.2617313172952));
#53841=CARTESIAN_POINT('Ctrl Pts',(0.00912273728367127,84.1037551056446,
11.2626945690433));
#53842=CARTESIAN_POINT('Ctrl Pts',(0.0418902000078147,84.1078132896965,
11.2644403680562));
#53843=CARTESIAN_POINT('Ctrl Pts',(0.0419056063519559,84.107815197741,11.264441188882));
#53844=CARTESIAN_POINT('Ctrl Pts',(0.0419210126854209,84.1078171057897,
11.2644420098812));
#53845=CARTESIAN_POINT('Ctrl Pts',(0.0419364190082416,84.1078190138425,
11.2644428310537));
#53846=CARTESIAN_POINT('Ctrl Pts',(0.11244951656894,84.1165519679687,11.2682012500287));
#53847=CARTESIAN_POINT('Ctrl Pts',(0.182742589941573,84.1253708535697,11.2755933293198));
#53848=CARTESIAN_POINT('Ctrl Pts',(0.252423154216101,84.1342327116647,11.2865505888385));
#53849=CARTESIAN_POINT('Ctrl Pts',(0.311066974026106,84.1416909349831,11.2957723217495));
#53850=CARTESIAN_POINT('Ctrl Pts',(0.36927598288803,84.1491795139062,11.307518873596));
#53851=CARTESIAN_POINT('Ctrl Pts',(0.426797171757144,84.1566702369035,11.3217282112539));
#53852=CARTESIAN_POINT('Ctrl Pts',(0.497941490212501,84.1659350381507,11.3393028418074));
#53853=CARTESIAN_POINT('Ctrl Pts',(0.568033257380841,84.175201088505,11.3606482678425));
#53854=CARTESIAN_POINT('Ctrl Pts',(0.6366482686779,84.1844109178024,11.3856681260411));
#53855=CARTESIAN_POINT('Ctrl Pts',(0.689440677073762,84.1914969629744,11.4049184117593));
#53856=CARTESIAN_POINT('Ctrl Pts',(0.741357765843272,84.1985495835019,11.4263437266034));
#53857=CARTESIAN_POINT('Ctrl Pts',(0.792188040999814,84.2055398094129,11.4498901643867));
#53858=CARTESIAN_POINT('Ctrl Pts',(0.858837515049693,84.2147055060184,11.480764632195));
#53859=CARTESIAN_POINT('Ctrl Pts',(0.923639760751696,84.2237643972766,11.5153000606163));
#53860=CARTESIAN_POINT('Ctrl Pts',(0.986267076755456,84.2327703292168,11.5531856368514));
#53861=CARTESIAN_POINT('Ctrl Pts',(1.03580120012658,84.2398934341535,11.5831506573403));
#53862=CARTESIAN_POINT('Ctrl Pts',(1.08397572511079,84.2469835299394,11.6152120160499));
#53863=CARTESIAN_POINT('Ctrl Pts',(1.13064244971601,84.2540699419949,11.6492341550756));
#53864=CARTESIAN_POINT('Ctrl Pts',(1.18898779521535,84.2629297701321,11.6917705334665));
#53865=CARTESIAN_POINT('Ctrl Pts',(1.24497295725207,84.2717853438818,11.7373664374954));
#53866=CARTESIAN_POINT('Ctrl Pts',(1.29826907067271,84.2806930341029,11.7857151232982));
#53867=CARTESIAN_POINT('Ctrl Pts',(1.32510955955017,84.2851790415237,11.8100640350713));
#53868=CARTESIAN_POINT('Ctrl Pts',(1.35126880282397,84.2896783694891,11.8351114349608));
#53869=CARTESIAN_POINT('Ctrl Pts',(1.37670914154942,84.2941988365226,11.8608205516891));
#53870=CARTESIAN_POINT('Ctrl Pts',(1.37671939860801,84.2942006590885,11.8608309171139));
#53871=CARTESIAN_POINT('Ctrl Pts',(1.37672965554978,84.2942024816579,11.8608412826462));
#53872=CARTESIAN_POINT('Ctrl Pts',(1.37673991237473,84.2942043042308,11.8608516482861));
#53873=CARTESIAN_POINT('Ctrl Pts',(1.42519115891715,84.3028137839123,11.9098169156571));
#53874=CARTESIAN_POINT('Ctrl Pts',(1.47107438780239,84.3115059336939,11.961229336335));
#53875=CARTESIAN_POINT('Ctrl Pts',(1.51414983245555,84.3202183653974,12.0148077257121));
#53876=CARTESIAN_POINT('Ctrl Pts',(1.54021921899898,84.3254911548401,12.0472335254756));
#53877=CARTESIAN_POINT('Ctrl Pts',(1.56525978374168,84.3307712580808,12.0804517127647));
#53878=CARTESIAN_POINT('Ctrl Pts',(1.58921607951863,84.336043799453,12.114391041236));
#53879=CARTESIAN_POINT('Ctrl Pts',(1.63014859721911,84.3450526376745,12.1723808981122));
#53880=CARTESIAN_POINT('Ctrl Pts',(1.66791850612996,84.3540388540006,12.2324828660429));
#53881=CARTESIAN_POINT('Ctrl Pts',(1.70228293889561,84.3629343762338,12.2943846515697));
#53882=CARTESIAN_POINT('Ctrl Pts',(1.71235776328242,84.365542329199,12.3125327648432));
#53883=CARTESIAN_POINT('Ctrl Pts',(1.72213967286767,84.368142442784,12.3308353075211));
#53884=CARTESIAN_POINT('Ctrl Pts',(1.73162207870361,84.3707328924981,12.349283710003));
#53885=CARTESIAN_POINT('Ctrl Pts',(1.76665572128149,84.3803035532534,12.4174430727075));
#53886=CARTESIAN_POINT('Ctrl Pts',(1.79760864253359,84.3897436393863,12.4876088936978));
#53887=CARTESIAN_POINT('Ctrl Pts',(1.8243893325239,84.3991173094973,12.5592399400937));
#53888=CARTESIAN_POINT('Ctrl Pts',(1.83613596899814,84.4032288202636,12.5906589910064));
#53889=CARTESIAN_POINT('Ctrl Pts',(1.84708005500493,84.4073276386148,12.6223606004483));
#53890=CARTESIAN_POINT('Ctrl Pts',(1.85721419484448,84.4114195764118,12.6543022099861));
#53891=CARTESIAN_POINT('Ctrl Pts',(1.87914681723638,84.4202754761696,12.7234312403403));
#53892=CARTESIAN_POINT('Ctrl Pts',(1.89733714776918,84.429131228048,12.7936688366494));
#53893=CARTESIAN_POINT('Ctrl Pts',(1.91172596705363,84.4380582798587,12.8645489414833));
#53894=CARTESIAN_POINT('Ctrl Pts',(1.91879856644955,84.4424462327543,12.899388950015));
#53895=CARTESIAN_POINT('Ctrl Pts',(1.92495305738059,84.4468515157404,12.9343849044072));
#53896=CARTESIAN_POINT('Ctrl Pts',(1.93018399265379,84.4512832086093,12.9694857532766));
#53897=CARTESIAN_POINT('Ctrl Pts',(1.94033215932514,84.4598808217552,13.0375824216598));
#53898=CARTESIAN_POINT('Ctrl Pts',(1.94681973089025,84.4684651833917,13.1060811090079));
#53899=CARTESIAN_POINT('Ctrl Pts',(1.94951938827062,84.4770235061186,13.1745130007201));
#53900=CARTESIAN_POINT('Ctrl Pts',(1.94952148319877,84.4770301473581,13.1745661037166));
#53901=CARTESIAN_POINT('Ctrl Pts',(1.94952357584832,84.4770367885819,13.1746192066731));
#53902=CARTESIAN_POINT('Ctrl Pts',(1.94952566621936,84.4770434297901,13.1746723095892));
#53903=CARTESIAN_POINT('Ctrl Pts',(1.95321377855843,84.4887607380318,13.2683635813158));
#53904=CARTESIAN_POINT('Ctrl Pts',(1.94997710535719,84.5005654525547,13.3622008441398));
#53905=CARTESIAN_POINT('Ctrl Pts',(1.94023064075133,84.5124864410356,13.4552283662948));
#53906=CARTESIAN_POINT('Ctrl Pts',(1.93889149641256,84.5141243605153,13.4680101579169));
#53907=CARTESIAN_POINT('Ctrl Pts',(1.93742952483265,84.5157644806227,13.4807767086174));
#53908=CARTESIAN_POINT('Ctrl Pts',(1.93584586179906,84.5174068815216,13.4935255863242));
#53909=CARTESIAN_POINT('Ctrl Pts',(1.93078145231806,84.5226591293216,13.5342953307461));
#53910=CARTESIAN_POINT('Ctrl Pts',(1.92441474003774,84.5278965434236,13.5748785418289));
#53911=CARTESIAN_POINT('Ctrl Pts',(1.91674824229219,84.5330985451104,13.6151934729252));
#53912=CARTESIAN_POINT('Ctrl Pts',(1.90072584242437,84.5439703347992,13.6994486267263));
#53913=CARTESIAN_POINT('Ctrl Pts',(1.8790235834995,84.5546856545393,13.78253754425));
#53914=CARTESIAN_POINT('Ctrl Pts',(1.85200845167572,84.5653055336086,13.86378565604));
#53915=CARTESIAN_POINT('Ctrl Pts',(1.84567881643702,84.5677937672854,13.8828220581135));
#53916=CARTESIAN_POINT('Ctrl Pts',(1.83905736303953,84.5702767861689,13.9017575639899));
#53917=CARTESIAN_POINT('Ctrl Pts',(1.83214849970748,84.5727554200334,13.9205837604938));
#53918=CARTESIAN_POINT('Ctrl Pts',(1.80276168665853,84.583298275854,14.0006608861357));
#53919=CARTESIAN_POINT('Ctrl Pts',(1.76817737507296,84.5937627800115,14.0787579868579));
#53920=CARTESIAN_POINT('Ctrl Pts',(1.72877618720114,84.6042221585337,14.1541803414388));
#53921=CARTESIAN_POINT('Ctrl Pts',(1.71877371941299,84.6068773981953,14.1733272177882));
#53922=CARTESIAN_POINT('Ctrl Pts',(1.70846074517972,84.6095323429264,14.192301966208));
#53923=CARTESIAN_POINT('Ctrl Pts',(1.69784329734153,84.6121882626014,14.2110937120938));
#53924=CARTESIAN_POINT('Ctrl Pts',(1.6593259326395,84.6218232547671,14.2792653236433));
#53925=CARTESIAN_POINT('Ctrl Pts',(1.61680242456352,84.6314719811794,14.3450252545571));
#53926=CARTESIAN_POINT('Ctrl Pts',(1.57059790327892,84.6411879864025,14.4078184499548));
#53927=CARTESIAN_POINT('Ctrl Pts',(1.55518597834373,84.6444288455004,14.4287636732144));
#53928=CARTESIAN_POINT('Ctrl Pts',(1.5393645425185,84.6476772306958,14.4493792380232));
#53929=CARTESIAN_POINT('Ctrl Pts',(1.52314571628208,84.650935249667,14.4696458332225));
#53930=CARTESIAN_POINT('Ctrl Pts',(1.51321437916295,84.6529302451291,14.482055756496));
#53931=CARTESIAN_POINT('Ctrl Pts',(1.50313420107118,84.6549287667643,14.4943345436136));
#53932=CARTESIAN_POINT('Ctrl Pts',(1.49290815883134,84.6569312013671,14.506477572868));
#53933=CARTESIAN_POINT('Ctrl Pts',(1.49290573429091,84.6569316761337,14.5064804519159));
#53934=CARTESIAN_POINT('Ctrl Pts',(1.49290330974226,84.6569321509006,14.5064833309562));
#53935=CARTESIAN_POINT('Ctrl Pts',(1.49290088518542,84.6569326256676,14.5064862099888));
#53936=CARTESIAN_POINT('Ctrl Pts',(1.45024439600519,84.6652854497019,14.5571385283166));
#53937=CARTESIAN_POINT('Ctrl Pts',(1.40498648153156,84.6737130343868,14.6054928961033));
#53938=CARTESIAN_POINT('Ctrl Pts',(1.35736068401196,84.6821171446992,14.6513015909629));
#53939=CARTESIAN_POINT('Ctrl Pts',(1.33661729455568,84.6857775502425,14.6712535423726));
#53940=CARTESIAN_POINT('Ctrl Pts',(1.31542527026016,84.6894334213537,14.6907222036987));
#53941=CARTESIAN_POINT('Ctrl Pts',(1.29380661699577,84.6930762686412,14.7096856787528));
#53942=CARTESIAN_POINT('Ctrl Pts',(1.21819377269838,84.7058173973959,14.7760118401961));
#53943=CARTESIAN_POINT('Ctrl Pts',(1.13733310798374,84.7183994754612,14.8361805171429));
#53944=CARTESIAN_POINT('Ctrl Pts',(1.05237565193126,84.7308790234823,14.8897122344806));
#53945=CARTESIAN_POINT('Ctrl Pts',(1.03074457149719,84.7340564503919,14.9033419844438));
#53946=CARTESIAN_POINT('Ctrl Pts',(1.00884764583026,84.737227257367,14.9165414830533));
#53947=CARTESIAN_POINT('Ctrl Pts',(0.986703343889802,84.7403924316647,14.929302767917));
#53948=CARTESIAN_POINT('Ctrl Pts',(0.897700508179527,84.7531139655734,14.9805931876028));
#53949=CARTESIAN_POINT('Ctrl Pts',(0.804705082511613,84.7657460769024,15.0248040056999));
#53950=CARTESIAN_POINT('Ctrl Pts',(0.708987808209041,84.778359764823,15.0613999764066));
#53951=CARTESIAN_POINT('Ctrl Pts',(0.686393878910136,84.7813372082902,15.0700384043268));
#53952=CARTESIAN_POINT('Ctrl Pts',(0.663648114616261,84.784313656368,15.0782526849068));
#53953=CARTESIAN_POINT('Ctrl Pts',(0.640766884118675,84.7872901001448,15.0860360142635));
#53954=CARTESIAN_POINT('Ctrl Pts',(0.555343153654182,84.7984022180423,15.1150939370509));
#53955=CARTESIAN_POINT('Ctrl Pts',(0.46803366463815,84.8095155007575,15.1381429345199));
#53956=CARTESIAN_POINT('Ctrl Pts',(0.379741860209001,84.8206689781605,15.1548254304413));
#53957=CARTESIAN_POINT('Ctrl Pts',(0.345706641857807,84.8249684829814,15.1612562922296));
#53958=CARTESIAN_POINT('Ctrl Pts',(0.311525238234077,84.8292739996287,15.1667415968204));
#53959=CARTESIAN_POINT('Ctrl Pts',(0.277248428798174,84.8335879080472,15.171262700616));
#53960=CARTESIAN_POINT('Ctrl Pts',(0.277228626528439,84.8335904002622,15.1712653125312));
#53961=CARTESIAN_POINT('Ctrl Pts',(0.277208824226786,84.83359289248,15.1712679241245));
#53962=CARTESIAN_POINT('Ctrl Pts',(0.277189021893341,84.8335953847006,15.1712705353961));
#53963=CARTESIAN_POINT('Ctrl Pts',(0.233350133862176,84.8391127233394,15.1770514319758));
#53964=CARTESIAN_POINT('Ctrl Pts',(0.189338665706105,84.8446426258861,15.1812538886977));
#53965=CARTESIAN_POINT('Ctrl Pts',(0.145258156107619,84.8501541848413,15.1838692224844));
#53966=CARTESIAN_POINT('Ctrl Pts',(0.0304069274952764,84.8645144842874,
15.1906834426777));
#53967=CARTESIAN_POINT('Ctrl Pts',(-0.0849308408675299,84.8788334517048,
15.1868143314595));
#53968=CARTESIAN_POINT('Ctrl Pts',(-0.198933758964356,84.8931556939499,
15.1726946107426));
#53969=CARTESIAN_POINT('Ctrl Pts',(-0.223228356926069,84.8962078361499,
15.1696856269036));
#53970=CARTESIAN_POINT('Ctrl Pts',(-0.247462405555277,84.8992601386906,
15.1662109498615));
#53971=CARTESIAN_POINT('Ctrl Pts',(-0.271618367075097,84.9023130519731,
15.1622744760133));
#53972=CARTESIAN_POINT('Ctrl Pts',(-0.364907236343795,84.9141032192932,
15.147072050976));
#53973=CARTESIAN_POINT('Ctrl Pts',(-0.457026917293188,84.9258838533372,
15.1249613059293));
#53974=CARTESIAN_POINT('Ctrl Pts',(-0.546873661499603,84.9376491320311,
15.0961755835741));
#53975=CARTESIAN_POINT('Ctrl Pts',(-0.615648390383315,84.9466550660754,
15.0741410594721));
#53976=CARTESIAN_POINT('Ctrl Pts',(-0.683094787328754,84.9556525017402,
15.0481942569581));
#53977=CARTESIAN_POINT('Ctrl Pts',(-0.748707450847617,84.9646368100891,
15.0184586558434));
#53978=CARTESIAN_POINT('Ctrl Pts',(-0.791487566201658,84.9704946693335,
14.9990707453764));
#53979=CARTESIAN_POINT('Ctrl Pts',(-0.833497079961818,84.9763481286158,
14.9780688999819));
#53980=CARTESIAN_POINT('Ctrl Pts',(-0.874636646032348,84.982197574172,14.9555393532476));
#53981=CARTESIAN_POINT('Ctrl Pts',(-0.924245481152777,84.9892512261149,
14.9283717217912));
#53982=CARTESIAN_POINT('Ctrl Pts',(-0.97258930392851,84.9962990375357,14.8989826808508));
#53983=CARTESIAN_POINT('Ctrl Pts',(-1.01949348913406,85.0033416679318,14.8675220679944));
#53984=CARTESIAN_POINT('Ctrl Pts',(-1.05768897855176,85.0090766937848,14.8419027442567));
#53985=CARTESIAN_POINT('Ctrl Pts',(-1.09493703556075,85.0148093498287,14.8149050405272));
#53986=CARTESIAN_POINT('Ctrl Pts',(-1.13114809258377,85.0205410247945,14.7866021628256));
#53987=CARTESIAN_POINT('Ctrl Pts',(-1.18079463350689,85.0283993382252,14.7477979938349));
#53988=CARTESIAN_POINT('Ctrl Pts',(-1.22848950474429,85.0362554172582,14.7065422562557));
#53989=CARTESIAN_POINT('Ctrl Pts',(-1.27398630056078,85.0441110927398,14.6630287743675));
#53990=CARTESIAN_POINT('Ctrl Pts',(-1.32466816608288,85.0528620450036,14.6145562523386));
#53991=CARTESIAN_POINT('Ctrl Pts',(-1.37262196931536,85.0616127845679,14.5632784958926));
#53992=CARTESIAN_POINT('Ctrl Pts',(-1.41745419185327,85.0703558398986,14.5095270121629));
#53993=CARTESIAN_POINT('Ctrl Pts',(-1.45012075667082,85.0767263825015,14.470361514048));
#53994=CARTESIAN_POINT('Ctrl Pts',(-1.48113202213731,85.0830932242741,14.4298806369453));
#53995=CARTESIAN_POINT('Ctrl Pts',(-1.51033674457732,85.0894520383892,14.3882280783937));
#53996=CARTESIAN_POINT('Ctrl Pts',(-1.5183179595479,85.0911898074269,14.376845055509));
#53997=CARTESIAN_POINT('Ctrl Pts',(-1.5261641850647,85.0929269493669,14.3653747431672));
#53998=CARTESIAN_POINT('Ctrl Pts',(-1.53387239419349,85.0946633543111,14.3538203086066));
#53999=CARTESIAN_POINT('Ctrl Pts',(-1.54397549056108,85.0969392482562,14.3386759911796));
#54000=CARTESIAN_POINT('Ctrl Pts',(-1.55384693578398,85.099215102824,14.3233789956478));
#54001=CARTESIAN_POINT('Ctrl Pts',(-1.56348446782898,85.1014908120453,14.3079375425852));
#54002=CARTESIAN_POINT('Ctrl Pts',(-1.60584304572334,85.111492937679,14.2400697534772));
#54003=CARTESIAN_POINT('Ctrl Pts',(-1.64367824027177,85.1214920067102,14.1694110929465));
#54004=CARTESIAN_POINT('Ctrl Pts',(-1.67681194118092,85.1314758558772,14.096697829742));
#54005=CARTESIAN_POINT('Ctrl Pts',(-1.67977505246016,85.1323687007833,14.0901951607241));
#54006=CARTESIAN_POINT('Ctrl Pts',(-1.68270059459859,85.1332614240155,14.0836760742639));
#54007=CARTESIAN_POINT('Ctrl Pts',(-1.68558845876882,85.1341540169019,14.0771411045514));
#54008=CARTESIAN_POINT('Ctrl Pts',(-1.71053382662586,85.1418642333748,14.020692042614));
#54009=CARTESIAN_POINT('Ctrl Pts',(-1.73277695401505,85.1497096690635,13.9630881628073));
#54010=CARTESIAN_POINT('Ctrl Pts',(-1.7521451336866,85.1575209055195,13.9045489350716));
#54011=CARTESIAN_POINT('Ctrl Pts',(-1.75531802257158,85.1588005397314,13.8949590578519));
#54012=CARTESIAN_POINT('Ctrl Pts',(-1.75841371544478,85.1600792417608,13.8853441835167));
#54013=CARTESIAN_POINT('Ctrl Pts',(-1.76143140981071,85.1613562499825,13.8757054010843));
#54014=CARTESIAN_POINT('Ctrl Pts',(-1.78711647398328,85.172225487932,13.7936650367198));
#54015=CARTESIAN_POINT('Ctrl Pts',(-1.80710976981629,85.1829063505651,13.7098598581591));
#54016=CARTESIAN_POINT('Ctrl Pts',(-1.82131724798675,85.1935080294538,13.6250864076034));
#54017=CARTESIAN_POINT('Ctrl Pts',(-1.82442537749334,85.1958273285284,13.6065407614384));
#54018=CARTESIAN_POINT('Ctrl Pts',(-1.82725652043322,85.1981428589666,13.5879485953943));
#54019=CARTESIAN_POINT('Ctrl Pts',(-1.82980953101542,85.2004557989677,13.5693179618627));
#54020=CARTESIAN_POINT('Ctrl Pts',(-1.8409357181689,85.2105357428215,13.4881244419824));
#54021=CARTESIAN_POINT('Ctrl Pts',(-1.84689003772633,85.2207240542008,13.4062065620465));
#54022=CARTESIAN_POINT('Ctrl Pts',(-1.84744767118077,85.2309365956636,13.3243157245479));
#54023=CARTESIAN_POINT('Ctrl Pts',(-1.8476067617552,85.2338501925342,13.3009525990486));
#54024=CARTESIAN_POINT('Ctrl Pts',(-1.8473268300071,85.2367657388299,13.2775918996761));
#54025=CARTESIAN_POINT('Ctrl Pts',(-1.84660325967835,85.2396812268938,13.254251562075));
#54026=CARTESIAN_POINT('Ctrl Pts',(-1.84525068982847,85.2451311480641,13.210621474341));
#54027=CARTESIAN_POINT('Ctrl Pts',(-1.8423460763394,85.2505783880291,13.1670660463023));
#54028=CARTESIAN_POINT('Ctrl Pts',(-1.83787331074505,85.2560199081706,13.1237159040522));
#54029=CARTESIAN_POINT('Ctrl Pts',(-1.8378683536336,85.2560259389409,13.1236678596192));
#54030=CARTESIAN_POINT('Ctrl Pts',(-1.83786339459672,85.2560319697041,13.1236198154383));
#54031=CARTESIAN_POINT('Ctrl Pts',(-1.8378584336345,85.2560380004604,13.1235717715096));
#54032=CARTESIAN_POINT('Ctrl Pts',(-1.82797948276968,85.2680472724092,13.0279000872513));
#54033=CARTESIAN_POINT('Ctrl Pts',(-1.81044219892233,85.28005266257,12.9330379411312));
#54034=CARTESIAN_POINT('Ctrl Pts',(-1.78571394556554,85.2921023437014,12.8401665668285));
#54035=CARTESIAN_POINT('Ctrl Pts',(-1.78409750453677,85.2928900094812,12.8340957336947));
#54036=CARTESIAN_POINT('Ctrl Pts',(-1.78245035058582,85.293677865537,12.8280333953093));
#54037=CARTESIAN_POINT('Ctrl Pts',(-1.78077261990269,85.2944659257482,12.8219798764064));
#54038=CARTESIAN_POINT('Ctrl Pts',(-1.76631134890319,85.3012586442652,12.7698013126855));
#54039=CARTESIAN_POINT('Ctrl Pts',(-1.74961557956881,85.3081305891139,12.7182583022491));
#54040=CARTESIAN_POINT('Ctrl Pts',(-1.73067981586692,85.3149635245604,12.6675575414924));
#54041=CARTESIAN_POINT('Ctrl Pts',(-1.69540238770607,85.3276933195207,12.5731017554225));
#54042=CARTESIAN_POINT('Ctrl Pts',(-1.65234437070366,85.3402888608063,12.4815558298799));
#54043=CARTESIAN_POINT('Ctrl Pts',(-1.60208024214139,85.3529049691793,12.3942033494227));
#54044=CARTESIAN_POINT('Ctrl Pts',(-1.60207728341293,85.3529057118091,12.3941982075396));
#54045=CARTESIAN_POINT('Ctrl Pts',(-1.6020743246595,85.3529064544391,12.394193065671));
#54046=CARTESIAN_POINT('Ctrl Pts',(-1.6020713658811,85.3529071970693,12.3941879238167));
#54047=CARTESIAN_POINT('Ctrl Pts',(-1.55393748472671,85.3649884238915,12.3105394146255));
#54048=CARTESIAN_POINT('Ctrl Pts',(-1.49919060049532,85.3771228765528,12.2306974760314));
#54049=CARTESIAN_POINT('Ctrl Pts',(-1.43866195428871,85.3892315961811,12.1555799556733));
#54050=CARTESIAN_POINT('Ctrl Pts',(-1.42326560832809,85.3923116260219,12.1364727163144));
#54051=CARTESIAN_POINT('Ctrl Pts',(-1.40749543808891,85.395389974111,12.1176711391185));
#54052=CARTESIAN_POINT('Ctrl Pts',(-1.39136565169905,85.3984653071638,12.099190255997));
#54053=CARTESIAN_POINT('Ctrl Pts',(-1.35810659243762,85.4048065370958,12.0610833169411));
#54054=CARTESIAN_POINT('Ctrl Pts',(-1.32331641102166,85.4111350656515,12.0243374978035));
#54055=CARTESIAN_POINT('Ctrl Pts',(-1.28711150508702,85.4174404648073,11.9890756728186));
#54056=CARTESIAN_POINT('Ctrl Pts',(-1.21026713566218,85.430823579874,11.9142329785544));
#54057=CARTESIAN_POINT('Ctrl Pts',(-1.12703675666197,85.4441024937404,11.8460620040289));
#54058=CARTESIAN_POINT('Ctrl Pts',(-1.03860274557366,85.4574053086368,11.7856639216873));
#54059=CARTESIAN_POINT('Ctrl Pts',(-1.02851505306579,85.458922764472,11.7787742954538));
#54060=CARTESIAN_POINT('Ctrl Pts',(-1.01835959564601,85.4604405376539,11.7719858043035));
#54061=CARTESIAN_POINT('Ctrl Pts',(-1.00813808582199,85.46195882316,11.7653000811902));
#54062=CARTESIAN_POINT('Ctrl Pts',(-0.994262190381637,85.4640199248264,
11.7562240839588));
#54063=CARTESIAN_POINT('Ctrl Pts',(-0.980264984472829,85.466081951658,11.7473377229105));
#54064=CARTESIAN_POINT('Ctrl Pts',(-0.966151166278289,85.4681453614856,
11.7386452804256));
#54065=CARTESIAN_POINT('Ctrl Pts',(-0.940392368458494,85.4719112422581,
11.7227809079757));
#54066=CARTESIAN_POINT('Ctrl Pts',(-0.914245017282329,85.4756817621344,
11.7075624545021));
#54067=CARTESIAN_POINT('Ctrl Pts',(-0.887741119288026,85.479461189823,11.6930162484083));
#54068=CARTESIAN_POINT('Ctrl Pts',(-0.883792159728891,85.4800243072597,
11.6908489302419));
#54069=CARTESIAN_POINT('Ctrl Pts',(-0.879835197767357,85.4805876560108,
11.6886964736288));
#54070=CARTESIAN_POINT('Ctrl Pts',(-0.875870294913486,85.4811512272568,
11.6865589593512));
#54071=CARTESIAN_POINT('Ctrl Pts',(-0.856700558214391,85.4838760134103,
11.6762243843558));
#54072=CARTESIAN_POINT('Ctrl Pts',(-0.837345201296476,85.4866060015936,
11.6662390695374));
#54073=CARTESIAN_POINT('Ctrl Pts',(-0.817814529132744,85.4893401868611,
11.6566048832587));
#54074=CARTESIAN_POINT('Ctrl Pts',(-0.746638371608368,85.4993044522829,
11.621494757276));
#54075=CARTESIAN_POINT('Ctrl Pts',(-0.673158530375076,85.5093202081103,
11.5910629328178));
#54076=CARTESIAN_POINT('Ctrl Pts',(-0.598021337714578,85.5192973541955,
11.5654695330317));
#54077=CARTESIAN_POINT('Ctrl Pts',(-0.471464483992447,85.5361022969004,
11.5223614524889));
#54078=CARTESIAN_POINT('Ctrl Pts',(-0.340174224350369,85.5527999218405,
11.4929617275192));
#54079=CARTESIAN_POINT('Ctrl Pts',(-0.207167320122267,85.5694565224654,
11.4777640481892));
#54080=CARTESIAN_POINT('Ctrl Pts',(-0.181477797397712,85.5726736495969,
11.4748287033605));
#54081=CARTESIAN_POINT('Ctrl Pts',(-0.155724129085211,85.5758892563297,
11.4724232758611));
#54082=CARTESIAN_POINT('Ctrl Pts',(-0.129927918261811,85.5791038343749,
11.470551501836));
#54083=CARTESIAN_POINT('Ctrl Pts',(-0.0492570413694765,85.5891565832656,
11.4646980199824));
#54084=CARTESIAN_POINT('Ctrl Pts',(0.031825063993792,85.5991988281697,11.4640642794784));
#54085=CARTESIAN_POINT('Ctrl Pts',(0.112634651844854,85.6092404307314,11.4687636308537));
#54086=CARTESIAN_POINT('Ctrl Pts',(0.112652623295684,85.609242663909,11.4687646759545));
#54087=CARTESIAN_POINT('Ctrl Pts',(0.112670594731866,85.6092448970854,11.4687657213194));
#54088=CARTESIAN_POINT('Ctrl Pts',(0.112688566153371,85.6092471302604,11.4687667669486));
#54089=CARTESIAN_POINT('Ctrl Pts',(0.143724140611242,85.6131036904697,11.4705725061627));
#54090=CARTESIAN_POINT('Ctrl Pts',(0.174715989893316,85.6169562827353,11.4731660658191));
#54091=CARTESIAN_POINT('Ctrl Pts',(0.205623145273929,85.6208032910311,11.4765451390782));
#54092=CARTESIAN_POINT('Ctrl Pts',(0.29075584452018,85.6313997434127,11.4858526804534));
#54093=CARTESIAN_POINT('Ctrl Pts',(0.375255485367746,85.6419536962468,11.501120936313));
#54094=CARTESIAN_POINT('Ctrl Pts',(0.458217992881756,85.6525722944883,11.5222495823753));
#54095=CARTESIAN_POINT('Ctrl Pts',(0.510912467054124,85.6593168043585,11.5356696552202));
#54096=CARTESIAN_POINT('Ctrl Pts',(0.56298461294796,85.6660876117512,11.5514542628319));
#54097=CARTESIAN_POINT('Ctrl Pts',(0.61418084935393,85.6729114254548,11.5695679816851));
#54098=CARTESIAN_POINT('Ctrl Pts',(0.614181367021844,85.6729114944534,11.569568164841));
#54099=CARTESIAN_POINT('Ctrl Pts',(0.614181884689718,85.672911563452,11.5695683479971));
#54100=CARTESIAN_POINT('Ctrl Pts',(0.614182402357452,85.6729116324507,11.5695685311534));
#54101=CARTESIAN_POINT('Ctrl Pts',(0.693738687769726,85.6835154889403,11.5977163899175));
#54102=CARTESIAN_POINT('Ctrl Pts',(0.771285993621759,85.6942295421365,11.6315422815696));
#54103=CARTESIAN_POINT('Ctrl Pts',(0.84616769083285,85.7049409977878,11.670540646632));
#54104=CARTESIAN_POINT('Ctrl Pts',(0.888237717285468,85.710958906561,11.6924507035736));
#54105=CARTESIAN_POINT('Ctrl Pts',(0.929466225656976,85.7169759433611,11.7159924317119));
#54106=CARTESIAN_POINT('Ctrl Pts',(0.969737048758562,85.7229717276922,11.741069015838));
#54107=CARTESIAN_POINT('Ctrl Pts',(1.08513929120223,85.7401535706178,11.812929827664));
#54108=CARTESIAN_POINT('Ctrl Pts',(1.19276131724192,85.7571688119804,11.8974403571697));
#54109=CARTESIAN_POINT('Ctrl Pts',(1.2902550715294,85.7740559112678,11.9923977871438));
#54110=CARTESIAN_POINT('Ctrl Pts',(1.38122592859114,85.7898131657369,12.0810020146891));
#54111=CARTESIAN_POINT('Ctrl Pts',(1.46337607084306,85.8054590702191,12.178701700058));
#54112=CARTESIAN_POINT('Ctrl Pts',(1.53476837406012,85.8210220936813,12.2837180051361));
#54113=CARTESIAN_POINT('Ctrl Pts',(1.53988742725632,85.822138011524,12.2912480052613));
#54114=CARTESIAN_POINT('Ctrl Pts',(1.54495116389373,85.8232535018488,12.2988156298782));
#54115=CARTESIAN_POINT('Ctrl Pts',(1.54995886674597,85.8243685745973,12.3064202269441));
#54116=CARTESIAN_POINT('Ctrl Pts',(1.59851553354426,85.835180760843,12.3801574067962));
#54117=CARTESIAN_POINT('Ctrl Pts',(1.64183205644228,85.8460018353106,12.4573960826899));
#54118=CARTESIAN_POINT('Ctrl Pts',(1.67924132530039,85.8569743091173,12.5374343967329));
#54119=CARTESIAN_POINT('Ctrl Pts',(1.68810875094259,85.8595752045254,12.5564065343867));
#54120=CARTESIAN_POINT('Ctrl Pts',(1.69664449412662,85.8621846198134,12.5755359644325));
#54121=CARTESIAN_POINT('Ctrl Pts',(1.70484010279699,85.8648044767534,12.594813334006));
#54122=CARTESIAN_POINT('Ctrl Pts',(1.70485234315749,85.8648083895798,12.5948421252725));
#54123=CARTESIAN_POINT('Ctrl Pts',(1.70486458275931,85.8648123024294,12.5948709168689));
#54124=CARTESIAN_POINT('Ctrl Pts',(1.70487682160245,85.8648162153023,12.5948997087954));
#54125=CARTESIAN_POINT('Ctrl Pts',(1.72779095621515,85.8721420790203,12.6488053002183));
#54126=CARTESIAN_POINT('Ctrl Pts',(1.74805965311354,85.8794788974896,12.7039665537236));
#54127=CARTESIAN_POINT('Ctrl Pts',(1.76562216590808,85.8868175658139,12.7600372081266));
#54128=CARTESIAN_POINT('Ctrl Pts',(1.78291244949569,85.8940424804925,12.8152387346342));
#54129=CARTESIAN_POINT('Ctrl Pts',(1.7975816587997,85.901269699012,12.8713249993773));
#54130=CARTESIAN_POINT('Ctrl Pts',(1.80959903861607,85.908493030258,12.9279776106178));
#54131=CARTESIAN_POINT('Ctrl Pts',(1.81942218280065,85.9143974641202,12.974286105244));
#54132=CARTESIAN_POINT('Ctrl Pts',(1.82747933074973,85.9203133829409,13.0209777274232));
#54133=CARTESIAN_POINT('Ctrl Pts',(1.8337621508321,85.9262359622378,13.0679168192808));
#54134=CARTESIAN_POINT('Ctrl Pts',(1.84424409691159,85.9361169004198,13.146227677052));
#54135=CARTESIAN_POINT('Ctrl Pts',(1.84976760624578,85.9459140879283,13.2252480455859));
#54136=CARTESIAN_POINT('Ctrl Pts',(1.85030224302454,85.9557598786602,13.3043850444585));
#54137=CARTESIAN_POINT('Ctrl Pts',(1.85037689590171,85.9571346748497,13.3154351721182));
#54138=CARTESIAN_POINT('Ctrl Pts',(1.85035420036891,85.9585104216572,13.3264876003774));
#54139=CARTESIAN_POINT('Ctrl Pts',(1.85023399555252,85.9598874822514,13.3375407366125));
#54140=CARTESIAN_POINT('Ctrl Pts',(1.84925342482349,85.9711208533536,13.4277066898715));
#54141=CARTESIAN_POINT('Ctrl Pts',(1.84176383598627,85.9823729208819,13.517921232015));
#54142=CARTESIAN_POINT('Ctrl Pts',(1.82766289675517,85.9936318843678,13.6070941099045));
#54143=CARTESIAN_POINT('Ctrl Pts',(1.82765574538415,85.9936375944147,13.6071393344334));
#54144=CARTESIAN_POINT('Ctrl Pts',(1.82764859231378,85.9936433044635,13.6071845586945));
#54145=CARTESIAN_POINT('Ctrl Pts',(1.82764143754412,85.993649014514,13.6072297826876));
#54146=CARTESIAN_POINT('Ctrl Pts',(1.81401739509538,86.0045220368684,13.6933448682657));
#54147=CARTESIAN_POINT('Ctrl Pts',(1.79421743148949,86.0154099384373,13.7785545676331));
#54148=CARTESIAN_POINT('Ctrl Pts',(1.76858430112525,86.0263033140579,13.8620023507837));
#54149=CARTESIAN_POINT('Ctrl Pts',(1.74374594861024,86.0368589309451,13.9428627617065));
#54150=CARTESIAN_POINT('Ctrl Pts',(1.71343311483025,86.0474197062229,14.0220691362845));
#54151=CARTESIAN_POINT('Ctrl Pts',(1.67796781209554,86.0579833269728,14.0988988079675));
#54152=CARTESIAN_POINT('Ctrl Pts',(1.64152004434362,86.0688395826938,14.1778568264822));
#54153=CARTESIAN_POINT('Ctrl Pts',(1.59963401777733,86.0796986852896,14.2543051112353));
#54154=CARTESIAN_POINT('Ctrl Pts',(1.55264416598259,86.0906938445333,14.327527131553));
#54155=CARTESIAN_POINT('Ctrl Pts',(1.50804735545421,86.1011290558565,14.3970201910518));
#54156=CARTESIAN_POINT('Ctrl Pts',(1.45883989384623,86.1115889042444,14.4636015287737));
#54157=CARTESIAN_POINT('Ctrl Pts',(1.4052349504777,86.1219992676407,14.5266672531493));
#54158=CARTESIAN_POINT('Ctrl Pts',(1.40235853756719,86.1225578822347,14.5300513265651));
#54159=CARTESIAN_POINT('Ctrl Pts',(1.39946944913583,86.1231163561666,14.5334252793147));
#54160=CARTESIAN_POINT('Ctrl Pts',(1.39656771389387,86.1236746845869,14.5367890190033));
#54161=CARTESIAN_POINT('Ctrl Pts',(1.39656494206585,86.1236752179196,14.5367922321524));
#54162=CARTESIAN_POINT('Ctrl Pts',(1.39656217022662,86.1236757512522,14.5367954452917));
#54163=CARTESIAN_POINT('Ctrl Pts',(1.39655939837615,86.1236762845845,14.5367986584214));
#54164=CARTESIAN_POINT('Ctrl Pts',(1.38123047217407,86.1266257264846,14.55456795324));
#54165=CARTESIAN_POINT('Ctrl Pts',(1.36555833065369,86.1295691303106,14.5720410264516));
#54166=CARTESIAN_POINT('Ctrl Pts',(1.34955505731457,86.1325059203192,14.5892111711369));
#54167=CARTESIAN_POINT('Ctrl Pts',(1.29375609819163,86.1427456895323,14.6490786858092));
#54168=CARTESIAN_POINT('Ctrl Pts',(1.23392824442023,86.1529058263795,14.7052724636152));
#54169=CARTESIAN_POINT('Ctrl Pts',(1.17059813120406,86.163044554318,14.7574500355268));
#54170=CARTESIAN_POINT('Ctrl Pts',(1.16667592349548,86.163672473563,14.7606815357465));
#54171=CARTESIAN_POINT('Ctrl Pts',(1.16274027004173,86.164300310863,14.7638976200291));
#54172=CARTESIAN_POINT('Ctrl Pts',(1.15879129130522,86.1649280801157,14.7670982024371));
#54173=CARTESIAN_POINT('Ctrl Pts',(1.09127884774159,86.1756605350288,14.8218159291218));
#54174=CARTESIAN_POINT('Ctrl Pts',(1.01987269787036,86.1863733647325,14.8720037640754));
#54175=CARTESIAN_POINT('Ctrl Pts',(0.945251604395908,86.1972037988522,14.9171692115491));
#54176=CARTESIAN_POINT('Ctrl Pts',(0.871359207707871,86.2079284706173,14.9618936052283));
#54177=CARTESIAN_POINT('Ctrl Pts',(0.794308857734811,86.2187200572444,15.0016847114781));
#54178=CARTESIAN_POINT('Ctrl Pts',(0.714843889454336,86.2295214956863,15.0360130145325));
#54179=CARTESIAN_POINT('Ctrl Pts',(0.655457380330701,86.237593728476,15.0616675655461));
#54180=CARTESIAN_POINT('Ctrl Pts',(0.594724679377242,86.2456711957035,15.0842699273015));
#54181=CARTESIAN_POINT('Ctrl Pts',(0.532996297408288,86.2537458065404,15.1036100910029));
#54182=CARTESIAN_POINT('Ctrl Pts',(0.532966724735384,86.253749674904,15.1036193564383));
#54183=CARTESIAN_POINT('Ctrl Pts',(0.53293715183407,86.253753543267,15.1036286211255));
#54184=CARTESIAN_POINT('Ctrl Pts',(0.532907578704435,86.2537574116292,15.1036378850645));
#54185=CARTESIAN_POINT('Ctrl Pts',(0.461793619796277,86.2630595909761,15.1259147081811));
#54186=CARTESIAN_POINT('Ctrl Pts',(0.38917133601737,86.2723823597116,15.1439193552667));
#54187=CARTESIAN_POINT('Ctrl Pts',(0.315674590734811,86.2817671702878,15.1575840066373));
#54188=CARTESIAN_POINT('Ctrl Pts',(0.300082603228587,86.2837581135424,15.1604828979097));
#54189=CARTESIAN_POINT('Ctrl Pts',(0.284451311816776,86.2857518491895,15.1631866447373));
#54190=CARTESIAN_POINT('Ctrl Pts',(0.268786836554964,86.2877487731267,15.1656948904237));
#54191=CARTESIAN_POINT('Ctrl Pts',(0.179942946359099,86.2990746865736,15.1799208571813));
#54192=CARTESIAN_POINT('Ctrl Pts',(0.0900295736881363,86.3104029506445,
15.1878531222001));
#54193=CARTESIAN_POINT('Ctrl Pts',(-3.5632935687461E-5,86.3217050596061,
15.1894668163097));
#54194=CARTESIAN_POINT('Ctrl Pts',(-0.0504520453204218,86.3280317178972,
15.1903701248208));
#54195=CARTESIAN_POINT('Ctrl Pts',(-0.100919683814972,86.3343506980785,
15.1892943044232));
#54196=CARTESIAN_POINT('Ctrl Pts',(-0.151304027318804,86.3406620734973,
15.1862310563657));
#54197=CARTESIAN_POINT('Ctrl Pts',(-0.241739297716183,86.351990412876,15.180732807364));
#54198=CARTESIAN_POINT('Ctrl Pts',(-0.331935073873759,86.3632980542052,
15.1688279446061));
#54199=CARTESIAN_POINT('Ctrl Pts',(-0.420963465396249,86.374594132703,15.1504427296073));
#54200=CARTESIAN_POINT('Ctrl Pts',(-0.450369245384569,86.3783251896541,
15.1443701545776));
#54201=CARTESIAN_POINT('Ctrl Pts',(-0.479645316965722,86.3820546740564,
15.1375909503703));
#54202=CARTESIAN_POINT('Ctrl Pts',(-0.508751498098799,86.3857819891471,
15.1301048276641));
#54203=CARTESIAN_POINT('Ctrl Pts',(-0.508752376006733,86.3857821015713,
15.1301046018658));
#54204=CARTESIAN_POINT('Ctrl Pts',(-0.50875325391444,86.3857822139955,15.1301043760669));
#54205=CARTESIAN_POINT('Ctrl Pts',(-0.508754131822008,86.3857823264197,
15.1301041502673));
#54206=CARTESIAN_POINT('Ctrl Pts',(-0.598882470889278,86.3973240964749,
15.1069229612656));
#54207=CARTESIAN_POINT('Ctrl Pts',(-0.687411283745175,86.4088929854641,
15.076956900895));
#54208=CARTESIAN_POINT('Ctrl Pts',(-0.773434460536162,86.4205016940216,
15.0406636234198));
#54209=CARTESIAN_POINT('Ctrl Pts',(-0.859773546252864,86.432153034051,15.0042370636046));
#54210=CARTESIAN_POINT('Ctrl Pts',(-0.94358831382734,86.4438442774286,14.9614369579727));
#54211=CARTESIAN_POINT('Ctrl Pts',(-1.02396527228439,86.4555881931186,14.9127258073221));
#54212=CARTESIAN_POINT('Ctrl Pts',(-1.09166140359485,86.4654793071133,14.8716996660742));
#54213=CARTESIAN_POINT('Ctrl Pts',(-1.15691892419963,86.4754077168827,14.8264806556248));
#54214=CARTESIAN_POINT('Ctrl Pts',(-1.21919476591611,86.485382666733,14.7773424303357));
#54215=CARTESIAN_POINT('Ctrl Pts',(-1.21920363688529,86.4853840876287,14.7773354307727));
#54216=CARTESIAN_POINT('Ctrl Pts',(-1.21921250779405,86.4853855085253,14.77732843113));
#54217=CARTESIAN_POINT('Ctrl Pts',(-1.21922137864223,86.4853869294228,14.7773214314079));
#54218=CARTESIAN_POINT('Ctrl Pts',(-1.26750307732052,86.4931205018568,14.7392237807633));
#54219=CARTESIAN_POINT('Ctrl Pts',(-1.31399705510086,86.500806458136,14.6987715625188));
#54220=CARTESIAN_POINT('Ctrl Pts',(-1.3584675226408,86.5084867176979,14.6561233562593));
#54221=CARTESIAN_POINT('Ctrl Pts',(-1.37843910964283,86.5119359050018,14.6369701427018));
#54222=CARTESIAN_POINT('Ctrl Pts',(-1.39800273845863,86.5153839815182,14.617373883547));
#54223=CARTESIAN_POINT('Ctrl Pts',(-1.41713772518216,86.5188349302985,14.5973480917732));
#54224=CARTESIAN_POINT('Ctrl Pts',(-1.41713928566028,86.518835211727,14.597346458649));
#54225=CARTESIAN_POINT('Ctrl Pts',(-1.41714084613556,86.5188354931555,14.5973448255219));
#54226=CARTESIAN_POINT('Ctrl Pts',(-1.41714240660789,86.5188357745839,14.5973431923921));
#54227=CARTESIAN_POINT('Ctrl Pts',(-1.47850189589284,86.5299018509344,14.5331267307454));
#54228=CARTESIAN_POINT('Ctrl Pts',(-1.5353902446252,86.540951619425,14.4645682733434));
#54229=CARTESIAN_POINT('Ctrl Pts',(-1.58741924090239,86.5520416805986,14.3923558074855));
#54230=CARTESIAN_POINT('Ctrl Pts',(-1.64111607342621,86.5634872436525,14.3178285061199));
#54231=CARTESIAN_POINT('Ctrl Pts',(-1.68966094579571,86.5749808199838,14.2393778432421));
#54232=CARTESIAN_POINT('Ctrl Pts',(-1.73259464990787,86.5865149313903,14.1576980759503));
#54233=CARTESIAN_POINT('Ctrl Pts',(-1.77573685917616,86.59810505757,14.0756216353925));
#54234=CARTESIAN_POINT('Ctrl Pts',(-1.81320580051726,86.609735890265,13.9902799352213));
#54235=CARTESIAN_POINT('Ctrl Pts',(-1.84443755951744,86.6213704244995,13.9025484558282));
#54236=CARTESIAN_POINT('Ctrl Pts',(-1.86808029660624,86.6301778770051,13.8361348957822));
#54237=CARTESIAN_POINT('Ctrl Pts',(-1.88814605498083,86.6389868820435,13.7683531610034));
#54238=CARTESIAN_POINT('Ctrl Pts',(-1.90439634024991,86.6477722337329,13.6996719007873));
#54239=CARTESIAN_POINT('Ctrl Pts',(-1.90792712384656,86.64968107257,13.6847491678658));
#54240=CARTESIAN_POINT('Ctrl Pts',(-1.9112779747624,86.6515887945627,13.6697840129319));
#54241=CARTESIAN_POINT('Ctrl Pts',(-1.91444677126181,86.6534951408393,13.6547813008456));
#54242=CARTESIAN_POINT('Ctrl Pts',(-1.91444982625446,86.6534969787212,13.6547668369395));
#54243=CARTESIAN_POINT('Ctrl Pts',(-1.91445288107791,86.6534988166019,13.6547523729984));
#54244=CARTESIAN_POINT('Ctrl Pts',(-1.91445593573215,86.6535006544812,13.6547379090224));
#54245=CARTESIAN_POINT('Ctrl Pts',(-1.93029411741999,86.6630299384141,13.5797431434025));
#54246=CARTESIAN_POINT('Ctrl Pts',(-1.94162247145959,86.6725943602713,13.503577754203));
#54247=CARTESIAN_POINT('Ctrl Pts',(-1.9484268665014,86.6821810365732,13.426884617186));
#54248=CARTESIAN_POINT('Ctrl Pts',(-1.94934130353894,86.6834693820945,13.4165778897573));
#54249=CARTESIAN_POINT('Ctrl Pts',(-1.95017411083732,86.6847581292951,13.4062616480156));
#54250=CARTESIAN_POINT('Ctrl Pts',(-1.95092532388645,86.6860472466744,13.3959374650937));
#54251=CARTESIAN_POINT('Ctrl Pts',(-1.95727090017054,86.6969365578737,13.3087279971827));
#54252=CARTESIAN_POINT('Ctrl Pts',(-1.95779056419137,86.7078640774532,13.2209521335627));
#54253=CARTESIAN_POINT('Ctrl Pts',(-1.95253420314447,86.7188045509795,13.1334461240541));
#54254=CARTESIAN_POINT('Ctrl Pts',(-1.94728560633413,86.7297288641956,13.0460693707653));
#54255=CARTESIAN_POINT('Ctrl Pts',(-1.93628233798267,86.7406691970177,12.9589607298055));
#54256=CARTESIAN_POINT('Ctrl Pts',(-1.91955696237647,86.7516552330178,12.8728427032526));
#54257=CARTESIAN_POINT('Ctrl Pts',(-1.91139040986356,86.7570194198688,12.8307935796508));
#54258=CARTESIAN_POINT('Ctrl Pts',(-1.90185949099508,86.7623922177723,12.7889789405383));
#54259=CARTESIAN_POINT('Ctrl Pts',(-1.89096277940852,86.7677752089414,12.7474747208012));
#54260=CARTESIAN_POINT('Ctrl Pts',(-1.87592358955661,86.7752045903213,12.6901923163507));
#54261=CARTESIAN_POINT('Ctrl Pts',(-1.85828093715202,86.782653842073,12.6334969487871));
#54262=CARTESIAN_POINT('Ctrl Pts',(-1.83804155738532,86.7900899697769,12.5776275467205));
#54263=CARTESIAN_POINT('Ctrl Pts',(-1.83804050637181,86.7900903559285,12.5776246454708));
#54264=CARTESIAN_POINT('Ctrl Pts',(-1.83803945535132,86.7900907420803,12.5776217442233));
#54265=CARTESIAN_POINT('Ctrl Pts',(-1.83803840432384,86.790091128232,12.5776188429781));
#54266=CARTESIAN_POINT('Ctrl Pts',(-1.79449266735854,86.8060900075022,12.4574156503374));
#54267=CARTESIAN_POINT('Ctrl Pts',(-1.73895084814189,86.8221283598989,12.3411716114307));
#54268=CARTESIAN_POINT('Ctrl Pts',(-1.67268003308299,86.8382021014664,12.2309915644402));
#54269=CARTESIAN_POINT('Ctrl Pts',(-1.60364918014691,86.8549452800329,12.1162227538629));
#54270=CARTESIAN_POINT('Ctrl Pts',(-1.52297725085347,86.8717265116971,12.0080350920145));
#54271=CARTESIAN_POINT('Ctrl Pts',(-1.43210104189571,86.8885485525361,11.9088177404275));
#54272=CARTESIAN_POINT('Ctrl Pts',(-1.3850676727566,86.8972548714454,11.8574673773818));
#54273=CARTESIAN_POINT('Ctrl Pts',(-1.33530102994277,86.9059722716785,11.8085198265075));
#54274=CARTESIAN_POINT('Ctrl Pts',(-1.28299987689475,86.9147023588632,11.7623058938006));
#54275=CARTESIAN_POINT('Ctrl Pts',(-1.25472676418535,86.919421695332,11.7373234287492));
#54276=CARTESIAN_POINT('Ctrl Pts',(-1.22571252189455,86.9241448233599,11.7131394463543));
#54277=CARTESIAN_POINT('Ctrl Pts',(-1.19599069435505,86.9288635364696,11.6898049290109));
#54278=CARTESIAN_POINT('Ctrl Pts',(-1.19598921671075,86.9288637710642,11.6898037689168));
#54279=CARTESIAN_POINT('Ctrl Pts',(-1.19598773906459,86.9288640056588,11.6898026088248));
#54280=CARTESIAN_POINT('Ctrl Pts',(-1.1959862614168,86.9288642402533,11.6898014487349));
#54281=CARTESIAN_POINT('Ctrl Pts',(-1.12041920220244,86.9408614297019,11.6304743331618));
#54282=CARTESIAN_POINT('Ctrl Pts',(-1.04021649755475,86.9528377927844,11.5765944927885));
#54283=CARTESIAN_POINT('Ctrl Pts',(-0.956382458435333,86.9648219511491,
11.5285893231278));
#54284=CARTESIAN_POINT('Ctrl Pts',(-0.94174133505533,86.9669149141397,11.5202055017199));
#54285=CARTESIAN_POINT('Ctrl Pts',(-0.926989542819542,86.9690081125826,
11.5120007684551));
#54286=CARTESIAN_POINT('Ctrl Pts',(-0.912132536345169,86.9711016959369,
11.5039772782886));
#54287=CARTESIAN_POINT('Ctrl Pts',(-0.810786332434802,86.9853829527905,
11.4492455076661));
#54288=CARTESIAN_POINT('Ctrl Pts',(-0.70454250358182,86.9996834798607,11.402946387786));
#54289=CARTESIAN_POINT('Ctrl Pts',(-0.595002221820435,87.014080947552,11.3656916042025));
#54290=CARTESIAN_POINT('Ctrl Pts',(-0.498075757091853,87.0268205135081,
11.3327267951943));
#54291=CARTESIAN_POINT('Ctrl Pts',(-0.39857100478865,87.0396097075564,11.3068307766587));
#54292=CARTESIAN_POINT('Ctrl Pts',(-0.297506797444648,87.0524921020393,
11.2884158931856));
#54293=CARTESIAN_POINT('Ctrl Pts',(-0.286596111482307,87.0538828591069,
11.286427859876));
#54294=CARTESIAN_POINT('Ctrl Pts',(-0.275667245422533,87.0552747017216,
11.2845270685171));
#54295=CARTESIAN_POINT('Ctrl Pts',(-0.264721479711684,87.0566676841916,
11.2827140745979));
#54296=CARTESIAN_POINT('Ctrl Pts',(-0.247350619328251,87.0588783384885,
11.2798368648093));
#54297=CARTESIAN_POINT('Ctrl Pts',(-0.229936804679973,87.0610953683484,
11.2771819347456));
#54298=CARTESIAN_POINT('Ctrl Pts',(-0.212485123333405,87.0633157544152,
11.2747504305229));
#54299=CARTESIAN_POINT('Ctrl Pts',(-0.124714877192573,87.0744828063306,
11.262521595955));
#54300=CARTESIAN_POINT('Ctrl Pts',(-0.0359624166409045,87.08573690229,11.2559445350597));
#54301=CARTESIAN_POINT('Ctrl Pts',(0.0529835866622808,87.0969516821591,
11.2552698032056));
#54302=CARTESIAN_POINT('Ctrl Pts',(0.0784856186886829,87.1001671124738,
11.2550763483823));
#54303=CARTESIAN_POINT('Ctrl Pts',(0.104003647599614,87.1033793268467,11.2553677784251));
#54304=CARTESIAN_POINT('Ctrl Pts',(0.129519357546692,87.1065853867447,11.2561492489883));
#54305=CARTESIAN_POINT('Ctrl Pts',(0.157463490542975,87.1100965790404,11.2570050949512));
#54306=CARTESIAN_POINT('Ctrl Pts',(0.185402461192954,87.1136002283852,11.2584487481659));
#54307=CARTESIAN_POINT('Ctrl Pts',(0.213307864462586,87.1170923527583,11.2604858640906));
#54308=CARTESIAN_POINT('Ctrl Pts',(0.213309293345847,87.1170925315709,11.2604859684001));
#54309=CARTESIAN_POINT('Ctrl Pts',(0.21331072222907,87.1170927103835,11.2604860727113));
#54310=CARTESIAN_POINT('Ctrl Pts',(0.213312151112264,87.1170928891961,11.260486177024));
#54311=CARTESIAN_POINT('Ctrl Pts',(0.296036961065724,87.1274451948233,11.2665253327291));
#54312=CARTESIAN_POINT('Ctrl Pts',(0.378652570307991,87.1377197497415,11.2777966697319));
#54313=CARTESIAN_POINT('Ctrl Pts',(0.460461010227518,87.1480100039539,11.2941051753275));
#54314=CARTESIAN_POINT('Ctrl Pts',(0.485688943100611,87.1511832931985,11.2991343616173));
#54315=CARTESIAN_POINT('Ctrl Pts',(0.510839999722393,87.1543580568021,11.3046422105368));
#54316=CARTESIAN_POINT('Ctrl Pts',(0.535893458079764,87.157536984341,11.3106220448498));
#54317=CARTESIAN_POINT('Ctrl Pts',(0.643826829621318,87.1712321940907,11.3363839045286));
#54318=CARTESIAN_POINT('Ctrl Pts',(0.749936585598241,87.185105181435,11.3709434084497));
#54319=CARTESIAN_POINT('Ctrl Pts',(0.852883685134752,87.1990028563483,11.4136672463958));
#54320=CARTESIAN_POINT('Ctrl Pts',(0.892380207461054,87.2043348164518,11.4300586068799));
#54321=CARTESIAN_POINT('Ctrl Pts',(0.931414528729908,87.2096708258374,11.4476528139777));
#54322=CARTESIAN_POINT('Ctrl Pts',(0.969919890804015,87.2150124051974,11.4664239213957));
#54323=CARTESIAN_POINT('Ctrl Pts',(1.0577844924855,87.2272012463752,11.5092573292008));
#54324=CARTESIAN_POINT('Ctrl Pts',(1.14291873269584,87.2394221753485,11.558228356988));
#54325=CARTESIAN_POINT('Ctrl Pts',(1.22440430680299,87.2517810800493,11.6130665127217));
#54326=CARTESIAN_POINT('Ctrl Pts',(1.2355027562513,87.2534643801986,11.6205355464238));
#54327=CARTESIAN_POINT('Ctrl Pts',(1.24653344464948,87.2551502353235,11.6281134447766));
#54328=CARTESIAN_POINT('Ctrl Pts',(1.25749397836516,87.2568389085591,11.6357995444945));
#54329=CARTESIAN_POINT('Ctrl Pts',(1.32334447416327,87.266984397154,11.6819773575743));
#54330=CARTESIAN_POINT('Ctrl Pts',(1.38666333379533,87.2772155382505,11.7320570775736));
#54331=CARTESIAN_POINT('Ctrl Pts',(1.44689953367254,87.2874052651517,11.7857499483419));
#54332=CARTESIAN_POINT('Ctrl Pts',(1.46948304521282,87.2912255561981,11.805880261494));
#54333=CARTESIAN_POINT('Ctrl Pts',(1.4916337159685,87.2950400554505,11.8265182121352));
#54334=CARTESIAN_POINT('Ctrl Pts',(1.51332427436683,87.2988421751302,11.8476478780693));
#54335=CARTESIAN_POINT('Ctrl Pts',(1.53376060318231,87.3024244419645,11.8675557473303));
#54336=CARTESIAN_POINT('Ctrl Pts',(1.55378722881955,87.3059956890905,11.8878990493415));
#54337=CARTESIAN_POINT('Ctrl Pts',(1.57337921717829,87.3095523818425,11.9086622815454));
#54338=CARTESIAN_POINT('Ctrl Pts',(1.57338250129789,87.3095529780354,11.9086657619955));
#54339=CARTESIAN_POINT('Ctrl Pts',(1.57338578540575,87.3095535742279,11.9086692424579));
#54340=CARTESIAN_POINT('Ctrl Pts',(1.57338906950178,87.30955417042,11.9086727229324));
#54341=CARTESIAN_POINT('Ctrl Pts',(1.62920314855619,87.3196866123056,11.9678243058351));
#54342=CARTESIAN_POINT('Ctrl Pts',(1.6816140911376,87.329701740186,12.0305038231267));
#54343=CARTESIAN_POINT('Ctrl Pts',(1.7302587584328,87.3397655313493,12.0961918407241));
#54344=CARTESIAN_POINT('Ctrl Pts',(1.7482039264464,87.3434780949935,12.1204243533058));
#54345=CARTESIAN_POINT('Ctrl Pts',(1.76563652037205,87.3471972312119,12.145065783603));
#54346=CARTESIAN_POINT('Ctrl Pts',(1.78253833906196,87.3509310937594,12.1700882671692));
#54347=CARTESIAN_POINT('Ctrl Pts',(1.83968116910642,87.3635547928344,12.2546859990433));
#54348=CARTESIAN_POINT('Ctrl Pts',(1.8907778241375,87.3763114616047,12.3436289523395));
#54349=CARTESIAN_POINT('Ctrl Pts',(1.93547034572799,87.3890968990374,12.4359588687816));
#54350=CARTESIAN_POINT('Ctrl Pts',(1.98052972878572,87.4019872865638,12.5290466813417));
#54351=CARTESIAN_POINT('Ctrl Pts',(2.01909805218481,87.4149119224749,12.6256147479312));
#54352=CARTESIAN_POINT('Ctrl Pts',(2.0506955219477,87.4278824573006,12.7247403476088));
#54353=CARTESIAN_POINT('Ctrl Pts',(2.05330000026777,87.4289515769803,12.7329109535865));
#54354=CARTESIAN_POINT('Ctrl Pts',(2.0558570884594,87.4300210086279,12.7410989415673));
#54355=CARTESIAN_POINT('Ctrl Pts',(2.05836650191244,87.4310907588341,12.7493037971863));
#54356=CARTESIAN_POINT('Ctrl Pts',(2.08765426114887,87.4435759818033,12.8450639580521));
#54357=CARTESIAN_POINT('Ctrl Pts',(2.11039846001263,87.4561894719074,12.9431372367724));
#54358=CARTESIAN_POINT('Ctrl Pts',(2.12612571186193,87.4688913063265,13.0425177242568));
#54359=CARTESIAN_POINT('Ctrl Pts',(2.12798518732701,87.4703930785172,13.0542677477165));
#54360=CARTESIAN_POINT('Ctrl Pts',(2.12974663119914,87.4718960865658,13.0660360299565));
#54361=CARTESIAN_POINT('Ctrl Pts',(2.13140930857862,87.4734002652213,13.0778208990135));
#54362=CARTESIAN_POINT('Ctrl Pts',(2.14235788618078,87.4833051433054,13.1554231777202));
#54363=CARTESIAN_POINT('Ctrl Pts',(2.14906760410476,87.4931764870455,13.233732958017));
#54364=CARTESIAN_POINT('Ctrl Pts',(2.15137219723108,87.5029556838565,13.3122203737897));
#54365=CARTESIAN_POINT('Ctrl Pts',(2.15164317447582,87.5041055353325,13.3214490326062));
#54366=CARTESIAN_POINT('Ctrl Pts',(2.15185330697249,87.5052541144115,13.3306801610893));
#54367=CARTESIAN_POINT('Ctrl Pts',(2.1520023708274,87.5064013270745,13.3399129105828));
#54368=CARTESIAN_POINT('Ctrl Pts',(2.15325866661982,87.5160699247523,13.4177256328426));
#54369=CARTESIAN_POINT('Ctrl Pts',(2.15019300464485,87.5256315510694,13.4957652625546));
#54370=CARTESIAN_POINT('Ctrl Pts',(2.14282132818636,87.5352799618495,13.5735395986408));
#54371=CARTESIAN_POINT('Ctrl Pts',(2.13954913455313,87.5395627689563,13.6080626394718));
#54372=CARTESIAN_POINT('Ctrl Pts',(2.13542859535056,87.5438625896556,13.6425327388421));
#54373=CARTESIAN_POINT('Ctrl Pts',(2.13046187476708,87.5481959501403,13.6769036507229));
#54374=CARTESIAN_POINT('Ctrl Pts',(2.11855989613429,87.5585801791359,13.7592682315196));
#54375=CARTESIAN_POINT('Ctrl Pts',(2.10191380634633,87.5689773604948,13.8410909731399));
#54376=CARTESIAN_POINT('Ctrl Pts',(2.08066693163373,87.5793978013831,13.9219092546352));
#54377=CARTESIAN_POINT('Ctrl Pts',(2.0601672445737,87.5894517872105,13.9998854041534));
#54378=CARTESIAN_POINT('Ctrl Pts',(2.03538435874549,87.5995270017667,14.0769234410713));
#54379=CARTESIAN_POINT('Ctrl Pts',(2.00642797456428,87.6096297977829,14.1525778250149));
#54380=CARTESIAN_POINT('Ctrl Pts',(1.97126548028827,87.6218978870882,14.2444469211605));
#54381=CARTESIAN_POINT('Ctrl Pts',(1.92993666546603,87.6342186032873,14.33427543214));
#54382=CARTESIAN_POINT('Ctrl Pts',(1.88260852340114,87.6466944811642,14.421097995489));
#54383=CARTESIAN_POINT('Ctrl Pts',(1.87457850659219,87.6488112240721,14.4358289063735));
#54384=CARTESIAN_POINT('Ctrl Pts',(1.86637586239482,87.6509324217059,14.4504731900229));
#54385=CARTESIAN_POINT('Ctrl Pts',(1.85800150360941,87.653058560142,14.465026018273));
#54386=CARTESIAN_POINT('Ctrl Pts',(1.81415844388124,87.6641897305197,14.5412157940559));
#54387=CARTESIAN_POINT('Ctrl Pts',(1.7656914553528,87.6753170692972,14.6149425619963));
#54388=CARTESIAN_POINT('Ctrl Pts',(1.7128562404809,87.6863794436326,14.6855371206224));
#54389=CARTESIAN_POINT('Ctrl Pts',(1.69708168377139,87.6896822418084,14.7066139321983));
#54390=CARTESIAN_POINT('Ctrl Pts',(1.68091795671351,87.692979262648,14.7274118231789));
#54391=CARTESIAN_POINT('Ctrl Pts',(1.66437235769046,87.6962689140814,14.7479137494339));
#54392=CARTESIAN_POINT('Ctrl Pts',(1.64386945753701,87.7003453693843,14.7733192331745));
#54393=CARTESIAN_POINT('Ctrl Pts',(1.62278064909653,87.7044106310044,14.7982692560839));
#54394=CARTESIAN_POINT('Ctrl Pts',(1.60112164566226,87.708462148479,14.8227301643944));
#54395=CARTESIAN_POINT('Ctrl Pts',(1.60111834920994,87.708462765111,14.8227338872905));
#54396=CARTESIAN_POINT('Ctrl Pts',(1.60111505274426,87.7084633817426,14.8227376101755));
#54397=CARTESIAN_POINT('Ctrl Pts',(1.60111175626517,87.7084639983738,14.8227413330495));
#54398=CARTESIAN_POINT('Ctrl Pts',(1.55102800237049,87.7178325411397,14.8793033503187));
#54399=CARTESIAN_POINT('Ctrl Pts',(1.49785170670597,87.7271117866214,14.9333308644897));
#54400=CARTESIAN_POINT('Ctrl Pts',(1.44185651869029,87.7364740387544,14.9845187815763));
#54401=CARTESIAN_POINT('Ctrl Pts',(1.41746833175872,87.7405516811949,15.0068132060579));
#54402=CARTESIAN_POINT('Ctrl Pts',(1.39254582061987,87.7446449859022,15.0285684545397));
#54403=CARTESIAN_POINT('Ctrl Pts',(1.36711373179781,87.7487677953584,15.0497570945603));
#54404=CARTESIAN_POINT('Ctrl Pts',(1.28170789454909,87.7626129810955,15.1209126159878));
#54405=CARTESIAN_POINT('Ctrl Pts',(1.19066969954911,87.7765114730761,15.1858723448039));
#54406=CARTESIAN_POINT('Ctrl Pts',(1.09504508815827,87.7904557390402,15.2440257369143));
#54407=CARTESIAN_POINT('Ctrl Pts',(1.08168541959868,87.7924038857451,15.2521503194136));
#54408=CARTESIAN_POINT('Ctrl Pts',(1.06823617222237,87.7943529279763,15.2601419909981));
#54409=CARTESIAN_POINT('Ctrl Pts',(1.05470014565361,87.7963028472321,15.2679990255087));
#54410=CARTESIAN_POINT('Ctrl Pts',(0.953908641202112,87.8108222702217,15.3265038108556));
#54411=CARTESIAN_POINT('Ctrl Pts',(0.848301459582856,87.8253907966777,15.37754590955));
#54412=CARTESIAN_POINT('Ctrl Pts',(0.739103056852967,87.8400855357775,15.4202742295696));
#54413=CARTESIAN_POINT('Ctrl Pts',(0.72723775368231,87.8416822398507,15.4249170124156));
#54414=CARTESIAN_POINT('Ctrl Pts',(0.715330095557562,87.8432804291626,15.429461614958));
#54415=CARTESIAN_POINT('Ctrl Pts',(0.703381687256164,87.8448801990184,15.4339069300187));
#54416=CARTESIAN_POINT('Ctrl Pts',(0.607605843093734,87.8577036065003,15.4695396094328));
#54417=CARTESIAN_POINT('Ctrl Pts',(0.509227792878079,87.8705804910181,15.4988256786442));
#54418=CARTESIAN_POINT('Ctrl Pts',(0.409159293207726,87.8834337315559,15.5212967277769));
#54419=CARTESIAN_POINT('Ctrl Pts',(0.383995983096763,87.8866658183629,15.5269473169205));
#54420=CARTESIAN_POINT('Ctrl Pts',(0.358725697059983,87.8898964288577,15.5321672167157));
#54421=CARTESIAN_POINT('Ctrl Pts',(0.333362726689558,87.8931243749597,15.5369494596605));
#54422=CARTESIAN_POINT('Ctrl Pts',(0.274532216139257,87.9006117360391,15.5480420797249));
#54423=CARTESIAN_POINT('Ctrl Pts',(0.215205024517501,87.9080847462132,15.5567788167315));
#54424=CARTESIAN_POINT('Ctrl Pts',(0.15556690485264,87.9155339187731,15.5630710699745));
#54425=CARTESIAN_POINT('Ctrl Pts',(0.104027553548264,87.9219715047273,15.5685088445422));
#54426=CARTESIAN_POINT('Ctrl Pts',(0.0522328186884648,87.9283902497721,
15.5721275529634));
#54427=CARTESIAN_POINT('Ctrl Pts',(0.000304409078912486,87.9348303106135,
15.5739164701182));
#54428=CARTESIAN_POINT('Ctrl Pts',(-0.148983585838682,87.9533447187647,
15.5790593939458));
#54429=CARTESIAN_POINT('Ctrl Pts',(-0.299391094048801,87.9720339484778,
15.5690851092438));
#54430=CARTESIAN_POINT('Ctrl Pts',(-0.448022467706194,87.9908509514967,
15.5446043392803));
#54431=CARTESIAN_POINT('Ctrl Pts',(-0.479347198187735,87.9948167195141,
15.539444906906));
#54432=CARTESIAN_POINT('Ctrl Pts',(-0.510593150090845,87.9987881792857,
15.5336409876383));
#54433=CARTESIAN_POINT('Ctrl Pts',(-0.541733374692063,88.0027649169591,
15.5271980525233));
#54434=CARTESIAN_POINT('Ctrl Pts',(-0.696464452009511,88.0225247264113,
15.4951840801066));
#54435=CARTESIAN_POINT('Ctrl Pts',(-0.8485795645406,88.0424219689274,15.4473842006064));
#54436=CARTESIAN_POINT('Ctrl Pts',(-0.994687792787653,88.0623859643358,
15.3845062365982));
#54437=CARTESIAN_POINT('Ctrl Pts',(-1.01503446511505,88.0651661012097,15.3757500060585));
#54438=CARTESIAN_POINT('Ctrl Pts',(-1.03526472751729,88.0679475429864,15.3667013922551));
#54439=CARTESIAN_POINT('Ctrl Pts',(-1.05536950139901,88.0707301089724,15.3573623201597));
#54440=CARTESIAN_POINT('Ctrl Pts',(-1.17551588968003,88.0873587592295,15.301551904745));
#54441=CARTESIAN_POINT('Ctrl Pts',(-1.29117517789633,88.1040261432729,15.2353679457917));
#54442=CARTESIAN_POINT('Ctrl Pts',(-1.4003793554562,88.120696826086,15.1592530954929));
#54443=CARTESIAN_POINT('Ctrl Pts',(-1.41130445319503,88.1223646087952,15.1516383485348));
#54444=CARTESIAN_POINT('Ctrl Pts',(-1.42216498158317,88.1240324265296,15.1439242297858));
#54445=CARTESIAN_POINT('Ctrl Pts',(-1.43295899592136,88.1257002451571,15.136111196351));
#54446=CARTESIAN_POINT('Ctrl Pts',(-1.43911012786573,88.1266506767681,15.1316588213552));
#54447=CARTESIAN_POINT('Ctrl Pts',(-1.44523964616295,88.1276011111596,15.1271743283995));
#54448=CARTESIAN_POINT('Ctrl Pts',(-1.45134725134598,88.1285514229008,15.1226579149591));
#54449=CARTESIAN_POINT('Ctrl Pts',(-1.45135770520861,88.1285530494677,15.1226501846026));
#54450=CARTESIAN_POINT('Ctrl Pts',(-1.45136815900826,88.1285546760345,15.1226424541515));
#54451=CARTESIAN_POINT('Ctrl Pts',(-1.45137861274486,88.1285563026012,15.1226347236059));
#54452=CARTESIAN_POINT('Ctrl Pts',(-1.54677226478709,88.1433992384115,15.0520910509509));
#54453=CARTESIAN_POINT('Ctrl Pts',(-1.6369183130347,88.1582358741482,14.9736734098144));
#54454=CARTESIAN_POINT('Ctrl Pts',(-1.72086861026843,88.1730991471263,14.8885464037324));
#54455=CARTESIAN_POINT('Ctrl Pts',(-1.73266016938776,88.1751868248094,14.8765895654847));
#54456=CARTESIAN_POINT('Ctrl Pts',(-1.74432950094035,88.1772750224463,14.8645004438381));
#54457=CARTESIAN_POINT('Ctrl Pts',(-1.75587398753047,88.179363825816,14.8522823465881));
#54458=CARTESIAN_POINT('Ctrl Pts',(-1.85064134368983,88.1965105712642,14.7519853983751));
#54459=CARTESIAN_POINT('Ctrl Pts',(-1.93699614621711,88.2136998169039,14.642992568439));
#54460=CARTESIAN_POINT('Ctrl Pts',(-2.01354772692068,88.2309824128667,14.5271011040686));
#54461=CARTESIAN_POINT('Ctrl Pts',(-2.08816594384959,88.2478285247666,14.414136559782));
#54462=CARTESIAN_POINT('Ctrl Pts',(-2.15347112698357,88.2647642414885,14.2946185688211));
#54463=CARTESIAN_POINT('Ctrl Pts',(-2.20821667601837,88.2818222288054,14.1701914439778));
#54464=CARTESIAN_POINT('Ctrl Pts',(-2.24970388707577,88.2947490937744,14.0758982186718));
#54465=CARTESIAN_POINT('Ctrl Pts',(-2.28512774333354,88.3077460182186,13.9787852163484));
#54466=CARTESIAN_POINT('Ctrl Pts',(-2.31395576790492,88.3208164870905,13.8795564772651));
#54467=CARTESIAN_POINT('Ctrl Pts',(-2.33345309418025,88.3296564683225,13.8124448686634));
#54468=CARTESIAN_POINT('Ctrl Pts',(-2.34993357542916,88.3385295904087,13.7443630982527));
#54469=CARTESIAN_POINT('Ctrl Pts',(-2.36333624981357,88.3473466042889,13.6755779354622));
#54470=CARTESIAN_POINT('Ctrl Pts',(-2.36334412537992,88.3473517852681,13.6755375165057));
#54471=CARTESIAN_POINT('Ctrl Pts',(-2.36335199988244,88.3473569662362,13.6754970972799));
#54472=CARTESIAN_POINT('Ctrl Pts',(-2.36335987332104,88.3473621471933,13.675456677785));
#54473=CARTESIAN_POINT('Ctrl Pts',(-2.38166744939442,88.3594090772867,13.58147195083));
#54474=CARTESIAN_POINT('Ctrl Pts',(-2.39421984738105,88.3713961678827,13.4860287760251));
#54475=CARTESIAN_POINT('Ctrl Pts',(-2.40101479196471,88.383357134674,13.3898891010969));
#54476=CARTESIAN_POINT('Ctrl Pts',(-2.40326525750871,88.38731857149,13.3580479251796));
#54477=CARTESIAN_POINT('Ctrl Pts',(-2.40488448099111,88.3912771153413,13.3261306518563));
#54478=CARTESIAN_POINT('Ctrl Pts',(-2.40587331290976,88.3952339088243,13.2941657917042));
#54479=CARTESIAN_POINT('Ctrl Pts',(-2.40920889778045,88.4085811928567,13.1863400814845));
#54480=CARTESIAN_POINT('Ctrl Pts',(-2.40536807839736,88.421910403757,13.0779700159226));
#54481=CARTESIAN_POINT('Ctrl Pts',(-2.39438836203394,88.4352856038816,12.9700894145612));
#54482=CARTESIAN_POINT('Ctrl Pts',(-2.39209862184288,88.4380749048321,12.9475916978081));
#54483=CARTESIAN_POINT('Ctrl Pts',(-2.38949849321608,88.4408661835501,12.9251154272601));
#54484=CARTESIAN_POINT('Ctrl Pts',(-2.38658846293994,88.4436599856111,12.9026702230902));
#54485=CARTESIAN_POINT('Ctrl Pts',(-2.37149981622855,88.4581459834459,12.7862907617282));
#54486=CARTESIAN_POINT('Ctrl Pts',(-2.34807116697853,88.4727071846531,12.6707431350032));
#54487=CARTESIAN_POINT('Ctrl Pts',(-2.31637745037266,88.4874116194763,12.55728259153));
#54488=CARTESIAN_POINT('Ctrl Pts',(-2.31250278139908,88.4892092886513,12.5434116387166));
#54489=CARTESIAN_POINT('Ctrl Pts',(-2.30850457460238,88.4910090900563,12.5295719422792));
#54490=CARTESIAN_POINT('Ctrl Pts',(-2.30438296280211,88.492811140838,12.5157658491687));
#54491=CARTESIAN_POINT('Ctrl Pts',(-2.28365152169375,88.5018753398616,12.4463220926658));
#54492=CARTESIAN_POINT('Ctrl Pts',(-2.25979030090262,88.5110019937939,12.3777268029861));
#54493=CARTESIAN_POINT('Ctrl Pts',(-2.23281244892046,88.520204065096,12.3102647269031));
#54494=CARTESIAN_POINT('Ctrl Pts',(-2.20408902789713,88.5300015452095,12.2384375993868));
#54495=CARTESIAN_POINT('Ctrl Pts',(-2.17182714020991,88.5398852265671,12.1678819029796));
#54496=CARTESIAN_POINT('Ctrl Pts',(-2.13619996140862,88.5497612773889,12.0989198439989));
#54497=CARTESIAN_POINT('Ctrl Pts',(-2.10985953763744,88.5570629884023,12.0479337732854));
#54498=CARTESIAN_POINT('Ctrl Pts',(-2.08167962138334,88.5643606575904,11.9978177248025));
#54499=CARTESIAN_POINT('Ctrl Pts',(-2.0517256356387,88.5716186150092,11.9486842696441));
#54500=CARTESIAN_POINT('Ctrl Pts',(-2.05169777747856,88.5716253651406,11.948638573967));
#54501=CARTESIAN_POINT('Ctrl Pts',(-2.05166991775728,88.5716321152547,11.948592879143));
#54502=CARTESIAN_POINT('Ctrl Pts',(-2.0516420564749,88.5716388653515,11.9485471851723));
#54503=CARTESIAN_POINT('Ctrl Pts',(-1.99058740264741,88.5864308918092,11.848414336839));
#54504=CARTESIAN_POINT('Ctrl Pts',(-1.92203241919673,88.6011404162034,11.7523767411012));
#54505=CARTESIAN_POINT('Ctrl Pts',(-1.84679973993252,88.6158179381924,11.6614367274794));
#54506=CARTESIAN_POINT('Ctrl Pts',(-1.77012497813778,88.6307768033194,11.5687535484372));
#54507=CARTESIAN_POINT('Ctrl Pts',(-1.68651548947329,88.6457033916041,11.4813644561497));
#54508=CARTESIAN_POINT('Ctrl Pts',(-1.59682250097743,88.6606501759218,11.4002908092098));
#54509=CARTESIAN_POINT('Ctrl Pts',(-1.54726366564214,88.6689088507103,11.3554944925066));
#54510=CARTESIAN_POINT('Ctrl Pts',(-1.49584705316933,88.6771735858944,11.312625635855));
#54511=CARTESIAN_POINT('Ctrl Pts',(-1.44271181452407,88.6854515692555,11.2718531617868));
#54512=CARTESIAN_POINT('Ctrl Pts',(-1.44269427247012,88.6854543021468,11.2718397011727));
#54513=CARTESIAN_POINT('Ctrl Pts',(-1.44267673022984,88.6854570350394,11.2718262407881));
#54514=CARTESIAN_POINT('Ctrl Pts',(-1.4426591878032,88.6854597679333,11.2718127806328));
#54515=CARTESIAN_POINT('Ctrl Pts',(-1.36786877183948,88.6971111932671,11.2144267283396));
#54516=CARTESIAN_POINT('Ctrl Pts',(-1.2896871105259,88.7087872796394,11.161207841561));
#54517=CARTESIAN_POINT('Ctrl Pts',(-1.20855202025243,88.7205536779918,11.1125764916225));
#54518=CARTESIAN_POINT('Ctrl Pts',(-1.19943449935656,88.7218759219491,11.1071115645759));
#54519=CARTESIAN_POINT('Ctrl Pts',(-1.19027965083921,88.7231993090832,11.1017045379434));
#54520=CARTESIAN_POINT('Ctrl Pts',(-1.18108807079193,88.7245239333106,11.0963559860755));
#54521=CARTESIAN_POINT('Ctrl Pts',(2.14925682029349,84.6483054938945,12.0236057114313));
#54522=CARTESIAN_POINT('Ctrl Pts',(2.19287098933027,84.6596480578688,12.1033343061839));
#54523=CARTESIAN_POINT('Ctrl Pts',(2.231937200779,84.6709868370664,12.1854677976133));
#54524=CARTESIAN_POINT('Ctrl Pts',(2.26636389384606,84.6822750513171,12.2693676919591));
#54525=CARTESIAN_POINT('Ctrl Pts',(2.28133677449313,84.6871845290983,12.3058574907874));
#54526=CARTESIAN_POINT('Ctrl Pts',(2.29543272638349,84.6920844693855,12.3426812535786));
#54527=CARTESIAN_POINT('Ctrl Pts',(2.30864723184453,84.6969711503224,12.3797860363184));
#54528=CARTESIAN_POINT('Ctrl Pts',(2.33932749547344,84.7083166115547,12.4659326211987));
#54529=CARTESIAN_POINT('Ctrl Pts',(2.36533388486355,84.719520070483,12.553580991922));
#54530=CARTESIAN_POINT('Ctrl Pts',(2.38649618898333,84.7306901567562,12.6421726883889));
#54531=CARTESIAN_POINT('Ctrl Pts',(2.39561515887648,84.735503417158,12.6803474073746));
#54532=CARTESIAN_POINT('Ctrl Pts',(2.40383466156047,84.7403103987368,12.7186966317093));
#54533=CARTESIAN_POINT('Ctrl Pts',(2.41114129373365,84.7451194157271,12.7571727164414));
#54534=CARTESIAN_POINT('Ctrl Pts',(2.43050120968639,84.7578615604718,12.8591203373082));
#54535=CARTESIAN_POINT('Ctrl Pts',(2.44345244131896,84.7706202824875,12.9619613477901));
#54536=CARTESIAN_POINT('Ctrl Pts',(2.44983626164971,84.7834913703342,13.0648855278049));
#54537=CARTESIAN_POINT('Ctrl Pts',(2.45140607708422,84.7866564394172,13.0901951320858));
#54538=CARTESIAN_POINT('Ctrl Pts',(2.45257865729089,84.7898282702867,13.1155095460192));
#54539=CARTESIAN_POINT('Ctrl Pts',(2.45335146297043,84.793008222476,13.1408162738566));
#54540=CARTESIAN_POINT('Ctrl Pts',(2.45388624577805,84.7952087546472,13.1583285713498));
#54541=CARTESIAN_POINT('Ctrl Pts',(2.45422965394671,84.7974131765683,13.1758375459544));
#54542=CARTESIAN_POINT('Ctrl Pts',(2.45438086824742,84.7996219230911,13.1933393515316));
#54543=CARTESIAN_POINT('Ctrl Pts',(2.45507531434162,84.8097655099656,13.273715747599));
#54544=CARTESIAN_POINT('Ctrl Pts',(2.45171514020669,84.8200035295251,13.3539544503281));
#54545=CARTESIAN_POINT('Ctrl Pts',(2.44439434627238,84.8302222778438,13.4336888791006));
#54546=CARTESIAN_POINT('Ctrl Pts',(2.43991491833263,84.8364748984118,13.4824765695079));
#54547=CARTESIAN_POINT('Ctrl Pts',(2.43395257145794,84.8427204305586,13.5310764656673));
#54548=CARTESIAN_POINT('Ctrl Pts',(2.42652634875635,84.8489340469272,13.5794138375531));
#54549=CARTESIAN_POINT('Ctrl Pts',(2.42500943331347,84.8502032696537,13.5892874582116));
#54550=CARTESIAN_POINT('Ctrl Pts',(2.42343150243139,84.8514711047787,13.5991497927408));
#54551=CARTESIAN_POINT('Ctrl Pts',(2.42181229469839,84.8527210817197,13.609006013937));
#54552=CARTESIAN_POINT('Ctrl Pts',(2.42180681093135,84.8527253150137,13.6090393939782));
#54553=CARTESIAN_POINT('Ctrl Pts',(2.42180132644769,84.8527295483047,13.6090727738877));
#54554=CARTESIAN_POINT('Ctrl Pts',(2.42179584124735,84.8527337815928,13.6091061536658));
#54555=CARTESIAN_POINT('Ctrl Pts',(2.40512791559537,84.8655975105884,13.7105375735987));
#54556=CARTESIAN_POINT('Ctrl Pts',(2.3818380810386,84.8784339362426,13.810753609036));
#54557=CARTESIAN_POINT('Ctrl Pts',(2.3523566788582,84.8912395537273,13.9089464545139));
#54558=CARTESIAN_POINT('Ctrl Pts',(2.336004608446,84.8983422809823,13.9634098180066));
#54559=CARTESIAN_POINT('Ctrl Pts',(2.31774871045274,84.9054355227729,14.0172507522878));
#54560=CARTESIAN_POINT('Ctrl Pts',(2.29766920602148,84.9125186231545,14.0703323703706));
#54561=CARTESIAN_POINT('Ctrl Pts',(2.25006071059923,84.9293126507782,14.1961888615083));
#54562=CARTESIAN_POINT('Ctrl Pts',(2.19229863809479,84.9459664925921,14.3178270217157));
#54563=CARTESIAN_POINT('Ctrl Pts',(2.12535334232426,84.962551052568,14.43359904628));
#54564=CARTESIAN_POINT('Ctrl Pts',(2.11089565313255,84.9661326995046,14.458601489379));
#54565=CARTESIAN_POINT('Ctrl Pts',(2.09600980491567,84.9697110866686,14.4833302121407));
#54566=CARTESIAN_POINT('Ctrl Pts',(2.08070583222711,84.9732868808465,14.507768434203));
#54567=CARTESIAN_POINT('Ctrl Pts',(2.02343999421288,84.9866671223257,14.5992136618216));
#54568=CARTESIAN_POINT('Ctrl Pts',(1.96027162876379,85.0000545294258,14.6865616750671));
#54569=CARTESIAN_POINT('Ctrl Pts',(1.89166144165137,85.013514996597,14.7689479802724));
#54570=CARTESIAN_POINT('Ctrl Pts',(1.87257221339513,85.0172600662591,14.7918701008997));
#54571=CARTESIAN_POINT('Ctrl Pts',(1.85306176095778,85.021010755739,14.8144078274359));
#54572=CARTESIAN_POINT('Ctrl Pts',(1.83314013504474,85.0247684008789,14.8365418326155));
#54573=CARTESIAN_POINT('Ctrl Pts',(1.78384715231707,85.0340661127114,14.8913090057256));
#54574=CARTESIAN_POINT('Ctrl Pts',(1.73213235121993,85.0433032183397,14.9437255234051));
#54575=CARTESIAN_POINT('Ctrl Pts',(1.67812973885351,85.0524810305914,14.9935538779059));
#54576=CARTESIAN_POINT('Ctrl Pts',(1.67810460485974,85.0524853021454,14.993577069109));
#54577=CARTESIAN_POINT('Ctrl Pts',(1.67807947036516,85.0524895736968,14.9936002597336));
#54578=CARTESIAN_POINT('Ctrl Pts',(1.67805433536979,85.0524938452456,14.9936234497798));
#54579=CARTESIAN_POINT('Ctrl Pts',(1.58086365874157,85.0690108451512,15.08329349929));
#54580=CARTESIAN_POINT('Ctrl Pts',(1.47618206021756,85.0854886548041,15.1643111625791));
#54581=CARTESIAN_POINT('Ctrl Pts',(1.36580274476862,85.1019180544506,15.2359968338182));
#54582=CARTESIAN_POINT('Ctrl Pts',(1.28658124915673,85.1137097711025,15.2874471084136));
#54583=CARTESIAN_POINT('Ctrl Pts',(1.20442853410608,85.125476173868,15.3340897167976));
#54584=CARTESIAN_POINT('Ctrl Pts',(1.12000583506295,85.1372153841286,15.3756916061252));
#54585=CARTESIAN_POINT('Ctrl Pts',(0.996577261945724,85.1543784692754,15.4365148432035));
#54586=CARTESIAN_POINT('Ctrl Pts',(0.868290307002927,85.1714844210568,15.4865678900596));
#54587=CARTESIAN_POINT('Ctrl Pts',(0.737167175096835,85.1885334620103,15.5251526957638));
#54588=CARTESIAN_POINT('Ctrl Pts',(0.625148580642901,85.2030984710719,15.5581157255469));
#54589=CARTESIAN_POINT('Ctrl Pts',(0.511071003745848,85.2175733420559,15.5827947611205));
#54590=CARTESIAN_POINT('Ctrl Pts',(0.39611249836126,85.2320031511263,15.5986955767301));
#54591=CARTESIAN_POINT('Ctrl Pts',(0.366333917902216,85.2357410148796,15.6028144865525));
#54592=CARTESIAN_POINT('Ctrl Pts',(0.336496385881311,85.239475831078,15.6063441544405));
#54593=CARTESIAN_POINT('Ctrl Pts',(0.306620746534905,85.2432083328465,15.6092755516791));
#54594=CARTESIAN_POINT('Ctrl Pts',(0.29544148056242,85.2446050102373,15.6103724610714));
#54595=CARTESIAN_POINT('Ctrl Pts',(0.284256833063029,85.246001651423,15.6113851010353));
#54596=CARTESIAN_POINT('Ctrl Pts',(0.273067872309848,85.2473979471003,15.6123136170645));
#54597=CARTESIAN_POINT('Ctrl Pts',(0.273057256352567,85.2473992718896,15.6123144980298));
#54598=CARTESIAN_POINT('Ctrl Pts',(0.273046640391623,85.2474005966785,15.6123153789195));
#54599=CARTESIAN_POINT('Ctrl Pts',(0.273036024426925,85.247401921467,15.6123162597336));
#54600=CARTESIAN_POINT('Ctrl Pts',(0.142388609612776,85.2637056863887,15.6231561674791));
#54601=CARTESIAN_POINT('Ctrl Pts',(0.011176502177052,85.2799507951204,15.6225366570752));
#54602=CARTESIAN_POINT('Ctrl Pts',(-0.11875750278832,85.2961599142673,15.6109905900159));
#54603=CARTESIAN_POINT('Ctrl Pts',(-0.153269989257969,85.3004653076506,
15.6079237755722));
#54604=CARTESIAN_POINT('Ctrl Pts',(-0.187692105702657,85.3047681392327,
15.6040862809233));
#54605=CARTESIAN_POINT('Ctrl Pts',(-0.221988927493997,85.3090687842354,
15.5994885635788));
#54606=CARTESIAN_POINT('Ctrl Pts',(-0.363094838903275,85.3267627395658,
15.5805723765269));
#54607=CARTESIAN_POINT('Ctrl Pts',(-0.502082635392263,85.3444214525854,
15.5487840486862));
#54608=CARTESIAN_POINT('Ctrl Pts',(-0.636562216114298,85.362078928714,15.5048537957376));
#54609=CARTESIAN_POINT('Ctrl Pts',(-0.656308226545274,85.3646716249876,
15.4984033946559));
#54610=CARTESIAN_POINT('Ctrl Pts',(-0.675956961236127,85.3672642824483,
15.4916912604578));
#54611=CARTESIAN_POINT('Ctrl Pts',(-0.69550077484739,85.3698569961539,15.4847197579916));
#54612=CARTESIAN_POINT('Ctrl Pts',(-0.778857614981396,85.3809152484562,
15.4549854170833));
#54613=CARTESIAN_POINT('Ctrl Pts',(-0.860308282720603,85.3919747902219,
15.4205322578276));
#54614=CARTESIAN_POINT('Ctrl Pts',(-0.939270356083257,85.4030420703751,
15.3815429803886));
#54615=CARTESIAN_POINT('Ctrl Pts',(-1.00540509097031,85.4123114779233,15.348887486212));
#54616=CARTESIAN_POINT('Ctrl Pts',(-1.06979766462332,85.4215867848494,15.3130479343755));
#54617=CARTESIAN_POINT('Ctrl Pts',(-1.13217977256314,85.4308033614711,15.274253321012));
#54618=CARTESIAN_POINT('Ctrl Pts',(-1.14839640811455,85.4331992706355,15.2641684084137));
#54619=CARTESIAN_POINT('Ctrl Pts',(-1.16447742505608,85.4355912449487,15.2538836798832));
#54620=CARTESIAN_POINT('Ctrl Pts',(-1.18041861045527,85.4379782209009,15.2434028764948));
#54621=CARTESIAN_POINT('Ctrl Pts',(-1.18042501130412,85.4379791793411,15.2433986681479));
#54622=CARTESIAN_POINT('Ctrl Pts',(-1.18043141213124,85.4379801377805,15.2433944597689));
#54623=CARTESIAN_POINT('Ctrl Pts',(-1.18043781293661,85.4379810962193,15.2433902513577));
#54624=CARTESIAN_POINT('Ctrl Pts',(-1.24921416677233,85.4482794760413,15.198171070387));
#54625=CARTESIAN_POINT('Ctrl Pts',(-1.31548179104275,85.4584987891364,15.1492373230104));
#54626=CARTESIAN_POINT('Ctrl Pts',(-1.37885416306956,85.4686706593374,15.0969467637316));
#54627=CARTESIAN_POINT('Ctrl Pts',(-1.40593323842989,85.4730171092322,15.0746029575893));
#54628=CARTESIAN_POINT('Ctrl Pts',(-1.43248354583059,85.4773548432448,15.0516468824975));
#54629=CARTESIAN_POINT('Ctrl Pts',(-1.45847454204963,85.4816860870913,15.0281093092908));
#54630=CARTESIAN_POINT('Ctrl Pts',(-1.52224430076374,85.4923129354312,14.9703591041253));
#54631=CARTESIAN_POINT('Ctrl Pts',(-1.58264666015608,85.5029020136033,14.9091046547943));
#54632=CARTESIAN_POINT('Ctrl Pts',(-1.63925983456805,85.5134987315104,14.8447737486644));
#54633=CARTESIAN_POINT('Ctrl Pts',(-1.66132902818519,85.5176295901246,14.8196959953376));
#54634=CARTESIAN_POINT('Ctrl Pts',(-1.68282215637449,85.5217615402645,14.7941512317421));
#54635=CARTESIAN_POINT('Ctrl Pts',(-1.70371345048146,85.5258970048648,14.7681667857281));
#54636=CARTESIAN_POINT('Ctrl Pts',(-1.76028445623371,85.537095324629,14.6978041630301));
#54637=CARTESIAN_POINT('Ctrl Pts',(-1.81244692662518,85.5483211266438,14.6242103361006));
#54638=CARTESIAN_POINT('Ctrl Pts',(-1.85972127513458,85.559624746755,14.547900063256));
#54639=CARTESIAN_POINT('Ctrl Pts',(-1.89367710308096,85.5677438174935,14.4930885517925));
#54640=CARTESIAN_POINT('Ctrl Pts',(-1.92511333523625,85.5759046014839,14.4368689671084));
#54641=CARTESIAN_POINT('Ctrl Pts',(-1.95403426143239,85.5840476265648,14.379509940392));
#54642=CARTESIAN_POINT('Ctrl Pts',(-1.97873669193148,85.5910028848352,14.3305174786241));
#54643=CARTESIAN_POINT('Ctrl Pts',(-2.00160476850795,85.5979452903245,14.2806930952608));
#54644=CARTESIAN_POINT('Ctrl Pts',(-2.02265084584226,85.6048415150376,14.2301758752017));
#54645=CARTESIAN_POINT('Ctrl Pts',(-2.04252541445498,85.61135386834,14.1824706453748));
#54646=CARTESIAN_POINT('Ctrl Pts',(-2.0608382214117,85.6177998058383,14.1341696797806));
#54647=CARTESIAN_POINT('Ctrl Pts',(-2.07736330535239,85.6242383657981,14.0853321146169));
#54648=CARTESIAN_POINT('Ctrl Pts',(-2.07737361122409,85.6242423812072,14.0853016570602));
#54649=CARTESIAN_POINT('Ctrl Pts',(-2.07738391640524,85.6242463966153,14.085271199281));
#54650=CARTESIAN_POINT('Ctrl Pts',(-2.07739422089578,85.6242504120224,14.0852407412793));
#54651=CARTESIAN_POINT('Ctrl Pts',(-2.1056363322918,85.635255669621,14.0017627398374));
#54652=CARTESIAN_POINT('Ctrl Pts',(-2.12868661691511,85.6462530293967,13.9166120894235));
#54653=CARTESIAN_POINT('Ctrl Pts',(-2.14654462688974,85.6572293599512,13.830517545662));
#54654=CARTESIAN_POINT('Ctrl Pts',(-2.1554400693894,85.6626968962244,13.7876320805596));
#54655=CARTESIAN_POINT('Ctrl Pts',(-2.16304797070316,85.6681592180648,13.7445127102601));
#54656=CARTESIAN_POINT('Ctrl Pts',(-2.16937291772459,85.6736147227104,13.7012506486903));
#54657=CARTESIAN_POINT('Ctrl Pts',(-2.18348150270599,85.6857839077877,13.6047492123843));
#54658=CARTESIAN_POINT('Ctrl Pts',(-2.19120685055952,85.6979185862962,13.5075430979988));
#54659=CARTESIAN_POINT('Ctrl Pts',(-2.19272683986784,85.7099902568241,13.4105047651033));
#54660=CARTESIAN_POINT('Ctrl Pts',(-2.1932627237712,85.7142462169727,13.3762931556381));
#54661=CARTESIAN_POINT('Ctrl Pts',(-2.19302736957254,85.7184943969047,13.342101936231));
#54662=CARTESIAN_POINT('Ctrl Pts',(-2.19202867229371,85.7227337162504,13.3079677997703));
#54663=CARTESIAN_POINT('Ctrl Pts',(-2.18972666727752,85.7325053804033,13.2292883490288));
#54664=CARTESIAN_POINT('Ctrl Pts',(-2.18325512765311,85.7422675366945,13.1509103876415));
#54665=CARTESIAN_POINT('Ctrl Pts',(-2.17252809072558,85.7520617636974,13.0733018247896));
#54666=CARTESIAN_POINT('Ctrl Pts',(-2.16041077600243,85.7631253716506,12.9856348028857));
#54667=CARTESIAN_POINT('Ctrl Pts',(-2.14301603860399,85.7741841235684,12.8989044883875));
#54668=CARTESIAN_POINT('Ctrl Pts',(-2.12049810978086,85.7852055215527,12.8137492567095));
#54669=CARTESIAN_POINT('Ctrl Pts',(-2.10991922310414,85.7903833565663,12.7737434660825));
#54670=CARTESIAN_POINT('Ctrl Pts',(-2.09820942748147,85.7955530435581,12.7340845889984));
#54671=CARTESIAN_POINT('Ctrl Pts',(-2.08538332695612,85.8007117279222,12.6948351177941));
#54672=CARTESIAN_POINT('Ctrl Pts',(-2.08087301405098,85.8025257851732,12.6810329963977));
#54673=CARTESIAN_POINT('Ctrl Pts',(-2.07622196108099,85.8043392611061,12.6672831277786));
#54674=CARTESIAN_POINT('Ctrl Pts',(-2.07143054132808,85.8061521035593,12.6535889336444));
#54675=CARTESIAN_POINT('Ctrl Pts',(-2.03761720726742,85.8189454405303,12.5569481914783));
#54676=CARTESIAN_POINT('Ctrl Pts',(-1.99678759074661,85.8317154373978,12.4630196046196));
#54677=CARTESIAN_POINT('Ctrl Pts',(-1.94965472372998,85.8444511391352,12.3726400604358));
#54678=CARTESIAN_POINT('Ctrl Pts',(-1.92466095163749,85.8512046690351,12.3247132978148));
#54679=CARTESIAN_POINT('Ctrl Pts',(-1.89789554386139,85.8579485588001,12.2777842042162));
#54680=CARTESIAN_POINT('Ctrl Pts',(-1.86946983044227,85.8646811993344,12.2319746290926));
#54681=CARTESIAN_POINT('Ctrl Pts',(-1.84427599796428,85.8706483676955,12.1913734049637));
#54682=CARTESIAN_POINT('Ctrl Pts',(-1.81777343950555,85.8766078475087,12.1516435507219));
#54683=CARTESIAN_POINT('Ctrl Pts',(-1.79002936519016,85.8825606311471,12.112856091873));
#54684=CARTESIAN_POINT('Ctrl Pts',(-1.73338972844886,85.8947132623378,12.0336713422091));
#54685=CARTESIAN_POINT('Ctrl Pts',(-1.67157844640131,85.9068376065722,11.9584157437827));
#54686=CARTESIAN_POINT('Ctrl Pts',(-1.60516341445492,85.9189396249287,11.8877212899944));
#54687=CARTESIAN_POINT('Ctrl Pts',(-1.55877487549976,85.9273924545595,11.8383437270035));
#54688=CARTESIAN_POINT('Ctrl Pts',(-1.51013566687496,85.9358350725433,11.7911882303987));
#54689=CARTESIAN_POINT('Ctrl Pts',(-1.45945516253797,85.9442662349374,11.746492423482));
#54690=CARTESIAN_POINT('Ctrl Pts',(-1.40689565818163,85.9530099860579,11.7001395016024));
#54691=CARTESIAN_POINT('Ctrl Pts',(-1.35214290410151,85.9617410168069,11.6564345510999));
#54692=CARTESIAN_POINT('Ctrl Pts',(-1.29544445557113,85.9704565291059,11.6156446939042));
#54693=CARTESIAN_POINT('Ctrl Pts',(-1.26602067521519,85.9749794627351,11.5944767108291));
#54694=CARTESIAN_POINT('Ctrl Pts',(-1.23607299956117,85.9794982164894,11.5740936820641));
#54695=CARTESIAN_POINT('Ctrl Pts',(-1.20563653337144,85.9840124069116,11.5545320720605));
#54696=CARTESIAN_POINT('Ctrl Pts',(-1.14789912716765,85.9925757415794,11.517424064326));
#54697=CARTESIAN_POINT('Ctrl Pts',(-1.08838658087924,86.0011250138468,11.4832623636639));
#54698=CARTESIAN_POINT('Ctrl Pts',(-1.02745354005985,86.0096568784892,11.4521231749894));
#54699=CARTESIAN_POINT('Ctrl Pts',(-0.94386043544844,86.0213616128005,11.409403799403));
#54700=CARTESIAN_POINT('Ctrl Pts',(-0.857598536648726,86.0330332693885,
11.3723694275982));
#54701=CARTESIAN_POINT('Ctrl Pts',(-0.76944192380994,86.0446822694564,11.3411524244976));
#54702=CARTESIAN_POINT('Ctrl Pts',(-0.691317422046363,86.0550056280456,
11.3134878768789));
#54703=CARTESIAN_POINT('Ctrl Pts',(-0.611699432378367,86.0653117654048,
11.2903921933378));
#54704=CARTESIAN_POINT('Ctrl Pts',(-0.531153098320537,86.0756035528523,
11.2719893478682));
#54705=CARTESIAN_POINT('Ctrl Pts',(-0.458525437424364,86.0848835338408,
11.255395723392));
#54706=CARTESIAN_POINT('Ctrl Pts',(-0.38514209479568,86.094151937621,11.2426181124793));
#54707=CARTESIAN_POINT('Ctrl Pts',(-0.311435688106232,86.1034086958724,
11.2337551633241));
#54708=CARTESIAN_POINT('Ctrl Pts',(-0.238682851706116,86.112545695611,11.2250068778104));
#54709=CARTESIAN_POINT('Ctrl Pts',(-0.165620646191976,86.121670678586,11.2200741771137));
#54710=CARTESIAN_POINT('Ctrl Pts',(-0.0926926687191226,86.1307804095427,
11.2190476294884));
#54711=CARTESIAN_POINT('Ctrl Pts',(-0.0562286799826961,86.135335275021,
11.2185343556758));
#54712=CARTESIAN_POINT('Ctrl Pts',(-0.0197983505282224,86.1398863186216,
11.2189975242646));
#54713=CARTESIAN_POINT('Ctrl Pts',(0.0165385415952809,86.1444325963023,
11.2204469529167));
#54714=CARTESIAN_POINT('Ctrl Pts',(0.0399353092095739,86.1473598747841,
11.221380217799));
#54715=CARTESIAN_POINT('Ctrl Pts',(0.0632933654262581,86.1502851805774,
11.2227223403635));
#54716=CARTESIAN_POINT('Ctrl Pts',(0.0865968599813805,86.1532082693327,
11.2244755760557));
#54717=CARTESIAN_POINT('Ctrl Pts',(0.0994853976637726,86.1548249513064,
11.2254452436836));
#54718=CARTESIAN_POINT('Ctrl Pts',(0.11235721855426,86.1564409516198,11.2265406589319));
#54719=CARTESIAN_POINT('Ctrl Pts',(0.125209734053258,86.1580562396112,11.2277621732103));
#54720=CARTESIAN_POINT('Ctrl Pts',(0.128217964667065,86.1584343102532,11.2280480780705));
#54721=CARTESIAN_POINT('Ctrl Pts',(0.131225481812053,86.1588123851195,11.2283409236405));
#54722=CARTESIAN_POINT('Ctrl Pts',(0.134232252914399,86.1591904631379,11.2286406963865));
#54723=CARTESIAN_POINT('Ctrl Pts',(0.208296467641036,86.1685034605656,11.236024841129));
#54724=CARTESIAN_POINT('Ctrl Pts',(0.281912245284535,86.1777978241537,11.2474397120406));
#54725=CARTESIAN_POINT('Ctrl Pts',(0.354666541325209,86.1870585500772,11.2625926851528));
#54726=CARTESIAN_POINT('Ctrl Pts',(0.394190407050775,86.1920894514513,11.2708245574575));
#54727=CARTESIAN_POINT('Ctrl Pts',(0.433460589407465,86.1971104925907,11.2801588611131));
#54728=CARTESIAN_POINT('Ctrl Pts',(0.472415368569644,86.2021197389829,11.2905441633557));
#54729=CARTESIAN_POINT('Ctrl Pts',(0.534557023315216,86.2101106162652,11.3071110616995));
#54730=CARTESIAN_POINT('Ctrl Pts',(0.595835813232674,86.2180940280176,11.3265969447972));
#54731=CARTESIAN_POINT('Ctrl Pts',(0.6559314307771,86.2260751400724,11.3489557008859));
#54732=CARTESIAN_POINT('Ctrl Pts',(0.668305522587851,86.2277185047195,11.3535595191329));
#54733=CARTESIAN_POINT('Ctrl Pts',(0.680629304585579,86.2293617496992,11.3582850437761));
#54734=CARTESIAN_POINT('Ctrl Pts',(0.692899759446579,86.231004885655,11.3631317129012));
#54735=CARTESIAN_POINT('Ctrl Pts',(0.765403576032029,86.2407138678654,11.391769771822));
#54736=CARTESIAN_POINT('Ctrl Pts',(0.836055207746743,86.2504213336074,11.4246483009801));
#54737=CARTESIAN_POINT('Ctrl Pts',(0.904500120349563,86.2601222775762,11.4613903906077));
#54738=CARTESIAN_POINT('Ctrl Pts',(0.938664938422471,86.2649645802869,11.4797304944958));
#54739=CARTESIAN_POINT('Ctrl Pts',(0.972280452183966,86.2698053410186,11.499033886941));
#54740=CARTESIAN_POINT('Ctrl Pts',(1.00530510272826,86.2746444305799,11.5192577787572));
#54741=CARTESIAN_POINT('Ctrl Pts',(1.06566332829293,86.2834886985573,11.5562204173897));
#54742=CARTESIAN_POINT('Ctrl Pts',(1.12404746474599,86.2923269766047,11.596254733523));
#54743=CARTESIAN_POINT('Ctrl Pts',(1.18020954435636,86.3011525071915,11.639042249067));
#54744=CARTESIAN_POINT('Ctrl Pts',(1.21812799415023,86.3071111618706,11.6679307138678));
#54745=CARTESIAN_POINT('Ctrl Pts',(1.25503449232313,86.3130641449343,11.6980747398789));
#54746=CARTESIAN_POINT('Ctrl Pts',(1.29086261803481,86.3190111209621,11.7293852566626));
#54747=CARTESIAN_POINT('Ctrl Pts',(1.33996474078547,86.3271613979055,11.7722960371726));
#54748=CARTESIAN_POINT('Ctrl Pts',(1.38715976654319,86.3352962476721,11.8172746685806));
#54749=CARTESIAN_POINT('Ctrl Pts',(1.43210367693323,86.3434197286818,11.8642591724474));
#54750=CARTESIAN_POINT('Ctrl Pts',(1.46722021146806,86.3497669401049,11.9009701069949));
#54751=CARTESIAN_POINT('Ctrl Pts',(1.50096157546203,86.35610708799,11.9389049525626));
#54752=CARTESIAN_POINT('Ctrl Pts',(1.53315161550813,86.3624394499366,11.9780157327345));
#54753=CARTESIAN_POINT('Ctrl Pts',(1.57078773637092,86.3698431542882,12.023743481053));
#54754=CARTESIAN_POINT('Ctrl Pts',(1.60629743009283,86.377235316054,12.0710738570216));
#54755=CARTESIAN_POINT('Ctrl Pts',(1.63946452713218,86.384608410176,12.1198220306397));
#54756=CARTESIAN_POINT('Ctrl Pts',(1.63947500513543,86.3846107394514,12.119837430948));
#54757=CARTESIAN_POINT('Ctrl Pts',(1.63948548291179,86.3846130687265,12.1198528314077));
#54758=CARTESIAN_POINT('Ctrl Pts',(1.6394959604613,86.3846153980011,12.1198682320187));
#54759=CARTESIAN_POINT('Ctrl Pts',(1.67022382831318,86.3914465413803,12.1650341307656));
#54760=CARTESIAN_POINT('Ctrl Pts',(1.69899746025832,86.3982737087366,12.2114985087682));
#54761=CARTESIAN_POINT('Ctrl Pts',(1.72590647901298,86.4050960556312,12.2589798079562));
#54762=CARTESIAN_POINT('Ctrl Pts',(1.74453701810428,86.4098195277753,12.2918536265333));
#54763=CARTESIAN_POINT('Ctrl Pts',(1.76227457177008,86.4145408243226,12.3252156347984));
#54764=CARTESIAN_POINT('Ctrl Pts',(1.77915760078136,86.4192614835819,12.358984027978));
#54765=CARTESIAN_POINT('Ctrl Pts',(1.80599207024908,86.426764662465,12.4126566784926));
#54766=CARTESIAN_POINT('Ctrl Pts',(1.83037459651115,86.4342610632331,12.4675115617748));
#54767=CARTESIAN_POINT('Ctrl Pts',(1.85212092003114,86.4417461899231,12.5233549926801));
#54768=CARTESIAN_POINT('Ctrl Pts',(1.85342475374555,86.4421949720138,12.5267031700341));
#54769=CARTESIAN_POINT('Ctrl Pts',(1.85471910483101,86.4426437116355,12.5300548867865));
#54770=CARTESIAN_POINT('Ctrl Pts',(1.85600393140411,86.4430924070764,12.5334100956869));
#54771=CARTESIAN_POINT('Ctrl Pts',(1.88345940271119,86.4526805842379,12.6051075867109));
#54772=CARTESIAN_POINT('Ctrl Pts',(1.90656724760835,86.462249602248,12.6784082342829));
#54773=CARTESIAN_POINT('Ctrl Pts',(1.92532599157067,86.4717990261399,12.7527206972875));
#54774=CARTESIAN_POINT('Ctrl Pts',(1.92893798087512,86.4736377642255,12.7670295349207));
#54775=CARTESIAN_POINT('Ctrl Pts',(1.93238877781421,86.4754757953809,12.7813760310092));
#54776=CARTESIAN_POINT('Ctrl Pts',(1.93567843562627,86.477313144432,12.7957561739071));
#54777=CARTESIAN_POINT('Ctrl Pts',(1.94676872399542,86.4835073238803,12.8442353594752));
#54778=CARTESIAN_POINT('Ctrl Pts',(1.95602776336883,86.489693485882,12.8930943654376));
#54779=CARTESIAN_POINT('Ctrl Pts',(1.96346201828368,86.4958720801445,12.9421725457636));
#54780=CARTESIAN_POINT('Ctrl Pts',(1.9634626427527,86.4958725991395,12.9421766682754));
#54781=CARTESIAN_POINT('Ctrl Pts',(1.96346326720883,86.4958731181344,12.9421807907887));
#54782=CARTESIAN_POINT('Ctrl Pts',(1.96346389165207,86.4958736371292,12.9421849133036));
#54783=CARTESIAN_POINT('Ctrl Pts',(1.97980904419184,86.5094586186453,13.0500940566911));
#54784=CARTESIAN_POINT('Ctrl Pts',(1.98731687215541,86.523004321378,13.1590501095082));
#54785=CARTESIAN_POINT('Ctrl Pts',(1.98606675423098,86.5365162111106,13.2675656801686));
#54786=CARTESIAN_POINT('Ctrl Pts',(1.98592165106773,86.5380845575068,13.2801612539596));
#54787=CARTESIAN_POINT('Ctrl Pts',(1.98565855348114,86.5396524552529,13.2927509506411));
#54788=CARTESIAN_POINT('Ctrl Pts',(1.98527758153155,86.5412199183297,13.3053324891015));
#54789=CARTESIAN_POINT('Ctrl Pts',(1.98200427250365,86.5546875530095,13.4134330027269));
#54790=CARTESIAN_POINT('Ctrl Pts',(1.9700285914733,86.5681226133291,13.5209272274796));
#54791=CARTESIAN_POINT('Ctrl Pts',(1.94939563689838,86.5815289559032,13.6263512189734));
#54792=CARTESIAN_POINT('Ctrl Pts',(1.93702813098904,86.5895647910234,13.6895429365265));
#54793=CARTESIAN_POINT('Ctrl Pts',(1.92154959718462,86.5975901872483,13.7519910158248));
#54794=CARTESIAN_POINT('Ctrl Pts',(1.90310360485767,86.6056252202187,13.8134428707539));
#54795=CARTESIAN_POINT('Ctrl Pts',(1.90310313421279,86.6056254252306,13.8134444386826));
#54796=CARTESIAN_POINT('Ctrl Pts',(1.90310266356597,86.6056256302425,13.8134460066107));
#54797=CARTESIAN_POINT('Ctrl Pts',(1.90310219291721,86.6056258352544,13.8134475745382));
#54798=CARTESIAN_POINT('Ctrl Pts',(1.88322106565787,86.6142859394332,13.879679908975));
#54799=CARTESIAN_POINT('Ctrl Pts',(1.85987118572338,86.6229700370676,13.9448473259692));
#54800=CARTESIAN_POINT('Ctrl Pts',(1.83321509731142,86.6316621062262,14.0086036405804));
#54801=CARTESIAN_POINT('Ctrl Pts',(1.82023954841902,86.635893198448,14.0396386958612));
#54802=CARTESIAN_POINT('Ctrl Pts',(1.80648118824268,86.6401261010684,14.070338872207));
#54803=CARTESIAN_POINT('Ctrl Pts',(1.79196237419654,86.644358518421,14.1006616505208));
#54804=CARTESIAN_POINT('Ctrl Pts',(1.7612003388457,86.653326039584,14.1649086596403));
#54805=CARTESIAN_POINT('Ctrl Pts',(1.72702084431151,86.6622913395971,14.2274623376558));
#54806=CARTESIAN_POINT('Ctrl Pts',(1.68962141635329,86.6712349621095,14.2879479750166));
#54807=CARTESIAN_POINT('Ctrl Pts',(1.67151087394331,86.6755658800847,14.3172379337251));
#54808=CARTESIAN_POINT('Ctrl Pts',(1.65264573837256,86.6798916154611,14.3460423212767));
#54809=CARTESIAN_POINT('Ctrl Pts',(1.63305141385878,86.6842094013902,14.3743153998403));
#54810=CARTESIAN_POINT('Ctrl Pts',(1.59149760888243,86.6933661566691,14.4342742921148));
#54811=CARTESIAN_POINT('Ctrl Pts',(1.54666032422409,86.7024876153277,14.4918478973936));
#54812=CARTESIAN_POINT('Ctrl Pts',(1.49877179469734,86.7115535415646,14.5466349552409));
#54813=CARTESIAN_POINT('Ctrl Pts',(1.48613823530509,86.7139452399252,14.5610884278382));
#54814=CARTESIAN_POINT('Ctrl Pts',(1.47329245360296,86.716333037697,14.5753477214595));
#54815=CARTESIAN_POINT('Ctrl Pts',(1.46023903547238,86.7187164865721,14.5894049591195));
#54816=CARTESIAN_POINT('Ctrl Pts',(1.41325526961805,86.7272953432941,14.6400018185911));
#54817=CARTESIAN_POINT('Ctrl Pts',(1.36357366042792,86.7358192158463,14.6879893655017));
#54818=CARTESIAN_POINT('Ctrl Pts',(1.31157081868928,86.7443078715575,14.7331579898203));
#54819=CARTESIAN_POINT('Ctrl Pts',(1.28411715180015,86.7487892560057,14.7570036937169));
#54820=CARTESIAN_POINT('Ctrl Pts',(1.2560159093463,86.7532609375692,14.7800643605444));
#54821=CARTESIAN_POINT('Ctrl Pts',(1.2273178425336,86.7577265764004,14.8023126050758));
#54822=CARTESIAN_POINT('Ctrl Pts',(1.17439232635883,86.7659621917724,14.8433432373304));
#54823=CARTESIAN_POINT('Ctrl Pts',(1.11944030892327,86.7741773740838,14.8816097757969));
#54824=CARTESIAN_POINT('Ctrl Pts',(1.06281422527155,86.7823917988784,14.9169269152696));
#54825=CARTESIAN_POINT('Ctrl Pts',(1.03305716092283,86.7867084874331,14.9354861078559));
#54826=CARTESIAN_POINT('Ctrl Pts',(1.00283730149674,86.7910250727261,14.9532315306584));
#54827=CARTESIAN_POINT('Ctrl Pts',(0.972201963296686,86.7953451119987,14.9701405604313));
#54828=CARTESIAN_POINT('Ctrl Pts',(0.910907554326699,86.8039885371901,15.0039717190566));
#54829=CARTESIAN_POINT('Ctrl Pts',(0.848021729394301,86.8126752636963,15.0345737226639));
#54830=CARTESIAN_POINT('Ctrl Pts',(0.783848924808002,86.8213883418196,15.0615990991142));
#54831=CARTESIAN_POINT('Ctrl Pts',(0.783848520579898,86.8213883967038,15.0615992693486));
#54832=CARTESIAN_POINT('Ctrl Pts',(0.783848116351681,86.821388451588,15.0615994395828));
#54833=CARTESIAN_POINT('Ctrl Pts',(0.783847712123454,86.8213885064722,15.0615996098169));
#54834=CARTESIAN_POINT('Ctrl Pts',(0.721414990646742,86.8298653217929,15.087892123917));
#54835=CARTESIAN_POINT('Ctrl Pts',(0.657516237819578,86.8383405656427,15.1106698963487));
#54836=CARTESIAN_POINT('Ctrl Pts',(0.592633671262873,86.8468293039448,15.1300234260879));
#54837=CARTESIAN_POINT('Ctrl Pts',(0.577895031346258,86.8487575947603,15.1344197488766));
#54838=CARTESIAN_POINT('Ctrl Pts',(0.563105513678014,86.8506866034954,15.1386395573276));
#54839=CARTESIAN_POINT('Ctrl Pts',(0.548270556918788,86.8526165447307,15.1426842140146));
#54840=CARTESIAN_POINT('Ctrl Pts',(0.461094783647308,86.8639576037097,15.1664521346111));
#54841=CARTESIAN_POINT('Ctrl Pts',(0.37226458310481,86.8752806243441,15.1839658043471));
#54842=CARTESIAN_POINT('Ctrl Pts',(0.282698134797612,86.8865587791263,15.195203053839));
#54843=CARTESIAN_POINT('Ctrl Pts',(0.272753347866309,86.8878110208799,15.1964507537758));
#54844=CARTESIAN_POINT('Ctrl Pts',(0.262799536699278,86.8890627025563,15.197621073035));
#54845=CARTESIAN_POINT('Ctrl Pts',(0.252837997486953,86.8903137822262,15.1987139805477));
#54846=CARTESIAN_POINT('Ctrl Pts',(0.151596656409499,86.9030287834805,15.2098214429493));
#54847=CARTESIAN_POINT('Ctrl Pts',(0.0495542348767872,86.9156819229246,
15.2129326990221));
#54848=CARTESIAN_POINT('Ctrl Pts',(-0.0519316765197526,86.9282562131738,
15.2081145534845));
#54849=CARTESIAN_POINT('Ctrl Pts',(-0.12577716399082,86.9374058042872,15.2046086648243));
#54850=CARTESIAN_POINT('Ctrl Pts',(-0.199325178028885,86.9465381530459,
15.1969949063302));
#54851=CARTESIAN_POINT('Ctrl Pts',(-0.272112643727955,86.9556902110132,
15.185419349973));
#54852=CARTESIAN_POINT('Ctrl Pts',(-0.297826380840842,86.9589233722498,
15.1813300358275));
#54853=CARTESIAN_POINT('Ctrl Pts',(-0.323445645008111,86.9621590502286,
15.1767461231077));
#54854=CARTESIAN_POINT('Ctrl Pts',(-0.348951420595469,86.9653990604897,
15.171673402345));
#54855=CARTESIAN_POINT('Ctrl Pts',(-0.414296657323316,86.9736998955998,
15.1586772031915));
#54856=CARTESIAN_POINT('Ctrl Pts',(-0.478875702308195,86.9819941913341,
15.1423604742402));
#54857=CARTESIAN_POINT('Ctrl Pts',(-0.54233299428946,86.990285143946,15.122737145446));
#54858=CARTESIAN_POINT('Ctrl Pts',(-0.601424607188846,86.9980057028764,
15.1044638452042));
#54859=CARTESIAN_POINT('Ctrl Pts',(-0.659541456820396,87.005723176856,15.0833220070137));
#54860=CARTESIAN_POINT('Ctrl Pts',(-0.716346504498371,87.0134336695245,
15.0593409104506));
#54861=CARTESIAN_POINT('Ctrl Pts',(-0.756521593973039,87.018886877391,15.0423803983218));
#54862=CARTESIAN_POINT('Ctrl Pts',(-0.796044236638958,87.0243371173727,
15.0239979434333));
#54863=CARTESIAN_POINT('Ctrl Pts',(-0.834781273075395,87.0297808148747,
15.0042158688955));
#54864=CARTESIAN_POINT('Ctrl Pts',(-0.842694572762417,87.0308928671559,
15.0001747367221));
#54865=CARTESIAN_POINT('Ctrl Pts',(-0.850575023390869,87.0320046354225,
14.9960752616351));
#54866=CARTESIAN_POINT('Ctrl Pts',(-0.858421481083709,87.0331160844941,
14.9919176945264));
#54867=CARTESIAN_POINT('Ctrl Pts',(-0.871869504001222,87.0350209940943,
14.9847920513447));
#54868=CARTESIAN_POINT('Ctrl Pts',(-0.885226167153093,87.0369261692669,
14.9774912591352));
#54869=CARTESIAN_POINT('Ctrl Pts',(-0.898487724760393,87.0388314679397,
14.9700193179692));
#54870=CARTESIAN_POINT('Ctrl Pts',(-0.957724092911548,87.047342004708,14.9366438525206));
#54871=CARTESIAN_POINT('Ctrl Pts',(-1.01506075333272,87.0558549640507,14.8998503526552));
#54872=CARTESIAN_POINT('Ctrl Pts',(-1.07017472155257,87.0643573017716,14.8600243674868));
#54873=CARTESIAN_POINT('Ctrl Pts',(-1.11798186153755,87.0717324275837,14.825478380154));
#54874=CARTESIAN_POINT('Ctrl Pts',(-1.16411199520861,87.0790986962611,14.7886568310092));
#54875=CARTESIAN_POINT('Ctrl Pts',(-1.20840348567075,87.0864532140857,14.7498029301005));
#54876=CARTESIAN_POINT('Ctrl Pts',(-1.26404616884484,87.0956925758896,14.7009914027443));
#54877=CARTESIAN_POINT('Ctrl Pts',(-1.31678836032053,87.1049133973009,14.6489741308252));
#54878=CARTESIAN_POINT('Ctrl Pts',(-1.36637013897849,87.1141192370507,14.594182850602));
#54879=CARTESIAN_POINT('Ctrl Pts',(-1.41492233008917,87.1231339134694,14.5405293355286));
#54880=CARTESIAN_POINT('Ctrl Pts',(-1.46044816149065,87.1321347906823,14.4842129136124));
#54881=CARTESIAN_POINT('Ctrl Pts',(-1.5027129202905,87.1411293042985,14.4255986400942));
#54882=CARTESIAN_POINT('Ctrl Pts',(-1.54108354214404,87.1492950927834,14.3723848944524));
#54883=CARTESIAN_POINT('Ctrl Pts',(-1.57676605792366,87.1574556736497,14.3172762698622));
#54884=CARTESIAN_POINT('Ctrl Pts',(-1.60956384536974,87.1656148278677,14.2605489621672));
#54885=CARTESIAN_POINT('Ctrl Pts',(-1.65172019680466,87.1761021259267,14.1876350095697));
#54886=CARTESIAN_POINT('Ctrl Pts',(-1.6891043370142,87.1865858576639,14.112054063435));
#54887=CARTESIAN_POINT('Ctrl Pts',(-1.7212562882911,87.1970656158005,14.0344520515893));
#54888=CARTESIAN_POINT('Ctrl Pts',(-1.74400080531818,87.2044790705961,13.979555841261));
#54889=CARTESIAN_POINT('Ctrl Pts',(-1.76412704221989,87.2118908720056,13.923645613687));
#54890=CARTESIAN_POINT('Ctrl Pts',(-1.78146519609074,87.2192969185211,13.8669827924128));
#54891=CARTESIAN_POINT('Ctrl Pts',(-1.79082264284032,87.2232939810924,13.8364017203618));
#54892=CARTESIAN_POINT('Ctrl Pts',(-1.79936815660371,87.2272893570071,13.8056016005041));
#54893=CARTESIAN_POINT('Ctrl Pts',(-1.80707658092626,87.2312823862284,13.7746241054396));
#54894=CARTESIAN_POINT('Ctrl Pts',(-1.81228345944445,87.2339795934922,13.7536994589944));
#54895=CARTESIAN_POINT('Ctrl Pts',(-1.81710844901457,87.2366757471703,13.7326937530584));
#54896=CARTESIAN_POINT('Ctrl Pts',(-1.82154402001871,87.2393705891091,13.7116203057941));
#54897=CARTESIAN_POINT('Ctrl Pts',(-1.8227088833876,87.2400783046787,13.7060860269489));
#54898=CARTESIAN_POINT('Ctrl Pts',(-1.82384688503378,87.2407859262489,13.7005471038925));
#54899=CARTESIAN_POINT('Ctrl Pts',(-1.82495789188927,87.2414934483205,13.6950037848465));
#54900=CARTESIAN_POINT('Ctrl Pts',(-1.82849882850422,87.2437484216329,13.6773364398777));
#54901=CARTESIAN_POINT('Ctrl Pts',(-1.83176749276105,87.2460036280045,13.6596146915391));
#54902=CARTESIAN_POINT('Ctrl Pts',(-1.83476522961432,87.2482588636572,13.6418473814649));
#54903=CARTESIAN_POINT('Ctrl Pts',(-1.85052148869291,87.2601124982372,13.5484614859171));
#54904=CARTESIAN_POINT('Ctrl Pts',(-1.858995252252,87.2720661047975,13.4538717853143));
#54905=CARTESIAN_POINT('Ctrl Pts',(-1.86049494309029,87.2841335328508,13.3591675845272));
#54906=CARTESIAN_POINT('Ctrl Pts',(-1.86066832354394,87.2855286578305,13.3482187563581));
#54907=CARTESIAN_POINT('Ctrl Pts',(-1.86074854517825,87.2869253067998,13.3372683859944));
#54908=CARTESIAN_POINT('Ctrl Pts',(-1.86073612666572,87.2883235032261,13.3263181449444));
#54909=CARTESIAN_POINT('Ctrl Pts',(-1.86064011634269,87.299133275347,13.2416593601076));
#54910=CARTESIAN_POINT('Ctrl Pts',(-1.85481726974304,87.3099420578236,13.1569945172455));
#54911=CARTESIAN_POINT('Ctrl Pts',(-1.84339274582698,87.3206951048813,13.073114438799));
#54912=CARTESIAN_POINT('Ctrl Pts',(-1.84013719955878,87.323759306285,13.0492118693467));
#54913=CARTESIAN_POINT('Ctrl Pts',(-1.83642689728324,87.3268189405755,13.0253733261439));
#54914=CARTESIAN_POINT('Ctrl Pts',(-1.83226506783929,87.329872642938,13.001617801452));
#54915=CARTESIAN_POINT('Ctrl Pts',(-1.81700736138336,87.3410678384354,12.9145275380628));
#54916=CARTESIAN_POINT('Ctrl Pts',(-1.79567938969836,87.352182746695,12.8285491371846));
#54917=CARTESIAN_POINT('Ctrl Pts',(-1.76844235872489,87.3631643408786,12.7445658358575));
#54918=CARTESIAN_POINT('Ctrl Pts',(-1.76198621289887,87.3657673695831,12.7246588041092));
#54919=CARTESIAN_POINT('Ctrl Pts',(-1.75519805973124,87.3683628785936,12.7048640974078));
#54920=CARTESIAN_POINT('Ctrl Pts',(-1.74808007397611,87.3709501072558,12.6851939066978));
#54921=CARTESIAN_POINT('Ctrl Pts',(-1.74048231479114,87.373711722832,12.6641978865766));
#54922=CARTESIAN_POINT('Ctrl Pts',(-1.73250877200948,87.3764640732795,12.6433431848717));
#54923=CARTESIAN_POINT('Ctrl Pts',(-1.72416207515673,87.3792064987491,12.6226439922819));
#54924=CARTESIAN_POINT('Ctrl Pts',(-1.69900946105979,87.3874707463603,12.5602673644356));
#54925=CARTESIAN_POINT('Ctrl Pts',(-1.67046335546784,87.3956456577967,12.4992940896072));
#54926=CARTESIAN_POINT('Ctrl Pts',(-1.63875379046976,87.4037990054521,12.4400890054315));
#54927=CARTESIAN_POINT('Ctrl Pts',(-1.61934357112186,87.4087898738673,12.4038480897826));
#54928=CARTESIAN_POINT('Ctrl Pts',(-1.59874775495104,87.4137727941147,12.3682687028105));
#54929=CARTESIAN_POINT('Ctrl Pts',(-1.57701513166543,87.4187645446387,12.3334258341915));
#54930=CARTESIAN_POINT('Ctrl Pts',(-1.54481145156513,87.426161384629,12.2817952242997));
#54931=CARTESIAN_POINT('Ctrl Pts',(-1.51011578198423,87.4335774190229,12.2317891981794));
#54932=CARTESIAN_POINT('Ctrl Pts',(-1.473138259013,87.4410791254027,12.1836603400649));
#54933=CARTESIAN_POINT('Ctrl Pts',(-1.46272989641304,87.4431906913986,12.1701131209294));
#54934=CARTESIAN_POINT('Ctrl Pts',(-1.45214068606608,87.4453090801691,12.1567143190081));
#54935=CARTESIAN_POINT('Ctrl Pts',(-1.44137514837776,87.4474358559827,12.1434688465559));
#54936=CARTESIAN_POINT('Ctrl Pts',(-1.44137425478021,87.4474360325166,12.1434677471104));
#54937=CARTESIAN_POINT('Ctrl Pts',(-1.44137336118143,87.4474362090505,12.143466647666));
#54938=CARTESIAN_POINT('Ctrl Pts',(-1.44137246758145,87.4474363855844,12.1434655482226));
#54939=CARTESIAN_POINT('Ctrl Pts',(-1.39101091584534,87.4573854946928,12.0815030647946));
#54940=CARTESIAN_POINT('Ctrl Pts',(-1.33647766114576,87.467392088894,12.0229029464975));
#54941=CARTESIAN_POINT('Ctrl Pts',(-1.27841784629724,87.4774419721174,11.9680691834789));
#54942=CARTESIAN_POINT('Ctrl Pts',(-1.26329237318812,87.4800601209841,11.9537841463981));
#54943=CARTESIAN_POINT('Ctrl Pts',(-1.24792777761632,87.4826812052219,11.9397545561443));
#54944=CARTESIAN_POINT('Ctrl Pts',(-1.23233589478026,87.4853049682812,11.9259871749623));
#54945=CARTESIAN_POINT('Ctrl Pts',(-1.18930223958667,87.4925465641801,11.8879891511871));
#54946=CARTESIAN_POINT('Ctrl Pts',(-1.14449165882802,87.4997752125975,11.8520203055084));
#54947=CARTESIAN_POINT('Ctrl Pts',(-1.09807718852408,87.5069390398801,11.8182605077424));
#54948=CARTESIAN_POINT('Ctrl Pts',(-1.04481898304741,87.5151591613837,11.779522884874));
#54949=CARTESIAN_POINT('Ctrl Pts',(-0.989444610882565,87.5232931326331,
11.7436921266958));
#54950=CARTESIAN_POINT('Ctrl Pts',(-0.932350031533391,87.5314234278476,
11.7108513383722));
#54951=CARTESIAN_POINT('Ctrl Pts',(-0.902344114133361,87.5356962847357,
11.6935919418933));
#54952=CARTESIAN_POINT('Ctrl Pts',(-0.871862264367964,87.5399682327544,
11.6771580391405));
#54953=CARTESIAN_POINT('Ctrl Pts',(-0.840956431741857,87.5442519439667,
11.6615602120205));
#54954=CARTESIAN_POINT('Ctrl Pts',(-0.765170396769674,87.5547562876508,
11.6233118501041));
#54955=CARTESIAN_POINT('Ctrl Pts',(-0.686821867297662,87.5653245554962,
11.5901000346244));
#54956=CARTESIAN_POINT('Ctrl Pts',(-0.60662585798347,87.5759007361351,11.5624241040996));
#54957=CARTESIAN_POINT('Ctrl Pts',(-0.591470758289319,87.5778993776303,
11.5571940248249));
#54958=CARTESIAN_POINT('Ctrl Pts',(-0.576249829363261,87.5798982871302,
11.5521616209458));
#54959=CARTESIAN_POINT('Ctrl Pts',(-0.560968099442974,87.5818970663421,
11.5473302197285));
#54960=CARTESIAN_POINT('Ctrl Pts',(-0.512918338158728,87.5881817516815,
11.5321390289164));
#54961=CARTESIAN_POINT('Ctrl Pts',(-0.464270820839121,87.5944646868323,
11.5189370519895));
#54962=CARTESIAN_POINT('Ctrl Pts',(-0.415211156722598,87.6007417399278,
11.5078130698807));
#54963=CARTESIAN_POINT('Ctrl Pts',(-0.415204728478864,87.6007425624044,
11.5078116123153));
#54964=CARTESIAN_POINT('Ctrl Pts',(-0.415198300228143,87.6007433848809,
11.5078101547856));
#54965=CARTESIAN_POINT('Ctrl Pts',(-0.415191871970263,87.6007442073574,
11.5078086972915));
#54966=CARTESIAN_POINT('Ctrl Pts',(-0.342013499774578,87.6101071618813,
11.4912167924111));
#54967=CARTESIAN_POINT('Ctrl Pts',(-0.267776092093042,87.6194751514263,
11.4792174936022));
#54968=CARTESIAN_POINT('Ctrl Pts',(-0.193127907198049,87.6288868543772,
11.4717089230663));
#54969=CARTESIAN_POINT('Ctrl Pts',(-0.165660691881416,87.6323499428878,
11.4689461027255));
#54970=CARTESIAN_POINT('Ctrl Pts',(-0.138137640107208,87.6358189881235,
11.4667908242157));
#54971=CARTESIAN_POINT('Ctrl Pts',(-0.110590144787841,87.639296049334,11.4652365025014));
#54972=CARTESIAN_POINT('Ctrl Pts',(-0.0476869054798448,87.6472357335367,
11.4616872915976));
#54973=CARTESIAN_POINT('Ctrl Pts',(0.0153469194529463,87.6552271176462,
11.461258093696));
#54974=CARTESIAN_POINT('Ctrl Pts',(0.0782235425313569,87.6631729756329,
11.46403749939));
#54975=CARTESIAN_POINT('Ctrl Pts',(0.117717443844533,87.6681639073308,11.4657832924815));
#54976=CARTESIAN_POINT('Ctrl Pts',(0.157148304694915,87.6731367448581,11.4687952727436));
#54977=CARTESIAN_POINT('Ctrl Pts',(0.19643443378675,87.6780660744701,11.473096436831));
#54978=CARTESIAN_POINT('Ctrl Pts',(0.258913712979031,87.6859055070682,11.4799368570527));
#54979=CARTESIAN_POINT('Ctrl Pts',(0.321042510094577,87.6936371567403,11.4900390146791));
#54980=CARTESIAN_POINT('Ctrl Pts',(0.382499517997052,87.701366890297,11.5032417822576));
#54981=CARTESIAN_POINT('Ctrl Pts',(0.420344625002122,87.7061268453219,11.5113720210834));
#54982=CARTESIAN_POINT('Ctrl Pts',(0.45793601954607,87.7108862059206,11.5206781857904));
#54983=CARTESIAN_POINT('Ctrl Pts',(0.495207915089243,87.7156709452667,11.5311257413606));
#54984=CARTESIAN_POINT('Ctrl Pts',(0.564662168559991,87.724587060063,11.5505942218914));
#54985=CARTESIAN_POINT('Ctrl Pts',(0.633005826499264,87.7335729138838,11.574053893625));
#54986=CARTESIAN_POINT('Ctrl Pts',(0.699650543610617,87.7425720167499,11.6014808758488));
#54987=CARTESIAN_POINT('Ctrl Pts',(0.726842547412994,87.7462437802439,11.6126714793541));
#54988=CARTESIAN_POINT('Ctrl Pts',(0.753751596036412,87.7499177120451,11.6245219608091));
#54989=CARTESIAN_POINT('Ctrl Pts',(0.780337490612665,87.7535898219369,11.6370282006477));
#54990=CARTESIAN_POINT('Ctrl Pts',(0.780342623922537,87.7535905309625,11.637030615402));
#54991=CARTESIAN_POINT('Ctrl Pts',(0.780347757220298,87.7535912399879,11.6370330301808));
#54992=CARTESIAN_POINT('Ctrl Pts',(0.780352890506075,87.7535919490133,11.637035444984));
#54993=CARTESIAN_POINT('Ctrl Pts',(0.845149084363128,87.7625418007781,11.6675169075431));
#54994=CARTESIAN_POINT('Ctrl Pts',(0.908191355610745,87.7715038926297,11.7019756421812));
#54995=CARTESIAN_POINT('Ctrl Pts',(0.969038721500143,87.7804952283994,11.7399995261093));
#54996=CARTESIAN_POINT('Ctrl Pts',(0.988865924246788,87.783425068248,11.7523896640362));
#54997=CARTESIAN_POINT('Ctrl Pts',(1.00846034970323,87.7863580284901,11.7651580339999));
#54998=CARTESIAN_POINT('Ctrl Pts',(1.02780758733243,87.7892947413097,11.7782895534611));
#54999=CARTESIAN_POINT('Ctrl Pts',(1.07935239418913,87.7971187158729,11.8132744772697));
#55000=CARTESIAN_POINT('Ctrl Pts',(1.12919874277126,87.805067212262,11.8507433490639));
#55001=CARTESIAN_POINT('Ctrl Pts',(1.1770597969767,87.8130203292175,11.8905859275645));
#55002=CARTESIAN_POINT('Ctrl Pts',(1.2030573924211,87.81734037441,11.9122279756664));
#55003=CARTESIAN_POINT('Ctrl Pts',(1.22846846239111,87.8216616649534,11.9345698767102));
#55004=CARTESIAN_POINT('Ctrl Pts',(1.25324230398937,87.8259641561577,11.9575896824997));
#55005=CARTESIAN_POINT('Ctrl Pts',(1.29843034189763,87.833811995778,11.9995783200927));
#55006=CARTESIAN_POINT('Ctrl Pts',(1.34150266569588,87.8415978526089,12.0438253121523));
#55007=CARTESIAN_POINT('Ctrl Pts',(1.38221287964598,87.849273068026,12.0901586822617));
#55008=CARTESIAN_POINT('Ctrl Pts',(1.42907158746814,87.8581074769324,12.1434898156975));
#55009=CARTESIAN_POINT('Ctrl Pts',(1.47280826837788,87.8667962940535,12.1995957113147));
#55010=CARTESIAN_POINT('Ctrl Pts',(1.51315182483763,87.875451535543,12.2580557607923));
#55011=CARTESIAN_POINT('Ctrl Pts',(1.52746736513253,87.8785227684529,12.2787997721631));
#55012=CARTESIAN_POINT('Ctrl Pts',(1.54135593784631,87.8815898355959,12.2998405968929));
#55013=CARTESIAN_POINT('Ctrl Pts',(1.554806184572,87.8846579438377,12.3211608065961));
#55014=CARTESIAN_POINT('Ctrl Pts',(1.58625856364909,87.8918324816316,12.3710164955856));
#55015=CARTESIAN_POINT('Ctrl Pts',(1.61530778467838,87.8990122165708,12.4223904699846));
#55016=CARTESIAN_POINT('Ctrl Pts',(1.64187713257101,87.9063567629279,12.4749710935669));
#55017=CARTESIAN_POINT('Ctrl Pts',(1.64187731304286,87.9063568128156,12.4749714507199));
#55018=CARTESIAN_POINT('Ctrl Pts',(1.64187749351458,87.9063568627034,12.4749718078729));
#55019=CARTESIAN_POINT('Ctrl Pts',(1.6418776739862,87.9063569125911,12.4749721650261));
#55020=CARTESIAN_POINT('Ctrl Pts',(1.67730216625862,87.9161492934952,12.5450771977862));
#55021=CARTESIAN_POINT('Ctrl Pts',(1.70814817108906,87.925967252164,12.6176216607258));
#55022=CARTESIAN_POINT('Ctrl Pts',(1.73428736600347,87.9358261368229,12.6918722517605));
#55023=CARTESIAN_POINT('Ctrl Pts',(1.74642716092138,87.9404048867909,12.7263563646281));
#55024=CARTESIAN_POINT('Ctrl Pts',(1.75755245209159,87.9449924866275,12.7612082692873));
#55025=CARTESIAN_POINT('Ctrl Pts',(1.76765412568267,87.9495905875376,12.7963539180686));
#55026=CARTESIAN_POINT('Ctrl Pts',(1.79008450091673,87.9598004926438,12.8743934709112));
#55027=CARTESIAN_POINT('Ctrl Pts',(1.80750655283606,87.9701045834727,12.9538701551679));
#55028=CARTESIAN_POINT('Ctrl Pts',(1.81973107546707,87.980385882292,13.0341223380985));
#55029=CARTESIAN_POINT('Ctrl Pts',(1.82497045288055,87.9847924024026,13.0685180758562));
#55030=CARTESIAN_POINT('Ctrl Pts',(1.8292549235937,87.9891946458021,13.1030556274193));
#55031=CARTESIAN_POINT('Ctrl Pts',(1.83256928930156,87.9935830047605,13.1376800255061));
#55032=CARTESIAN_POINT('Ctrl Pts',(1.83925384484729,88.0024336361624,13.2075120032204));
#55033=CARTESIAN_POINT('Ctrl Pts',(1.8419944645236,88.0112285812271,13.2777043565843));
#55034=CARTESIAN_POINT('Ctrl Pts',(1.84068559032576,88.0199224757906,13.3478415445535));
#55035=CARTESIAN_POINT('Ctrl Pts',(1.83932265563101,88.028975454719,13.4208756123289));
#55036=CARTESIAN_POINT('Ctrl Pts',(1.83356649796163,88.0379217844587,13.4938703271618));
#55037=CARTESIAN_POINT('Ctrl Pts',(1.82344883881245,88.0468916383222,13.5662803970993));
#55038=CARTESIAN_POINT('Ctrl Pts',(1.81869376825403,88.0511072664029,13.6003114893328));
#55039=CARTESIAN_POINT('Ctrl Pts',(1.81297541791176,88.0553281874975,13.6342141987128));
#55040=CARTESIAN_POINT('Ctrl Pts',(1.80629704617942,88.0595684223687,13.6679358503882));
#55041=CARTESIAN_POINT('Ctrl Pts',(1.80629558330172,88.0595693511796,13.6679432370168));
#55042=CARTESIAN_POINT('Ctrl Pts',(1.806294120378,88.0595702799918,13.6679506236375));
#55043=CARTESIAN_POINT('Ctrl Pts',(1.80629265740831,88.0595712088052,13.6679580102498));
#55044=CARTESIAN_POINT('Ctrl Pts',(1.79016685367163,88.0698091938604,13.7493780568618));
#55045=CARTESIAN_POINT('Ctrl Pts',(1.76844788885588,88.0801916177454,13.8298081726634));
#55046=CARTESIAN_POINT('Ctrl Pts',(1.74145615672971,88.0906541470781,13.9085141050726));
#55047=CARTESIAN_POINT('Ctrl Pts',(1.72776654791466,88.0959605102678,13.9484320110843));
#55048=CARTESIAN_POINT('Ctrl Pts',(1.71272141550676,88.1012874255911,13.9879060619226));
#55049=CARTESIAN_POINT('Ctrl Pts',(1.69636745940177,88.1066261760139,14.0268391250695));
#55050=CARTESIAN_POINT('Ctrl Pts',(1.65636758146645,88.1196841397183,14.1220648773907));
#55051=CARTESIAN_POINT('Ctrl Pts',(1.6085350209467,88.1328099107082,14.2140570169254));
#55052=CARTESIAN_POINT('Ctrl Pts',(1.55351118181306,88.1458809240025,14.3015262562322));
#55053=CARTESIAN_POINT('Ctrl Pts',(1.54047893831842,88.1489767572024,14.3222431026553));
#55054=CARTESIAN_POINT('Ctrl Pts',(1.52704340476911,88.1520694839144,14.3427060322565));
#55055=CARTESIAN_POINT('Ctrl Pts',(1.51321335128793,88.1551574118775,14.3628975762197));
#55056=CARTESIAN_POINT('Ctrl Pts',(1.46295848126945,88.1663781507289,14.4362684723428));
#55057=CARTESIAN_POINT('Ctrl Pts',(1.4074923193835,88.1775357371721,14.5060644133476));
#55058=CARTESIAN_POINT('Ctrl Pts',(1.34718108012025,88.1885732098478,14.5715037031576));
#55059=CARTESIAN_POINT('Ctrl Pts',(1.34133852868256,88.1896424467369,14.5778430260008));
#55060=CARTESIAN_POINT('Ctrl Pts',(1.33545049497421,88.1907105539787,14.5841414261415));
#55061=CARTESIAN_POINT('Ctrl Pts',(1.32951730389984,88.1917774782276,14.5903981679766));
#55062=CARTESIAN_POINT('Ctrl Pts',(1.28832435836357,88.1991849174837,14.6338374610005));
#55063=CARTESIAN_POINT('Ctrl Pts',(1.24495035848387,88.2065370847293,14.6752741735538));
#55064=CARTESIAN_POINT('Ctrl Pts',(1.19957882997783,88.21391659331,14.7144876613134));
#55065=CARTESIAN_POINT('Ctrl Pts',(1.19955451748868,88.213920547645,14.7145086739953));
#55066=CARTESIAN_POINT('Ctrl Pts',(1.19953020442998,88.2139245019899,14.7145296860377));
#55067=CARTESIAN_POINT('Ctrl Pts',(1.19950589080182,88.2139284563447,14.7145506974405));
#55068=CARTESIAN_POINT('Ctrl Pts',(1.11593767417127,88.2275199440433,14.7867688564188));
#55069=CARTESIAN_POINT('Ctrl Pts',(1.02563776716874,88.2412286460027,14.8514295213002));
#55070=CARTESIAN_POINT('Ctrl Pts',(0.930258331206905,88.2550166677362,14.9077789696688));
#55071=CARTESIAN_POINT('Ctrl Pts',(0.91569495183748,88.2571219453491,14.9163829038982));
#55072=CARTESIAN_POINT('Ctrl Pts',(0.901013232173689,88.259229067882,14.924793124328));
#55073=CARTESIAN_POINT('Ctrl Pts',(0.886219137823221,88.2613378957927,14.933007010672));
#55074=CARTESIAN_POINT('Ctrl Pts',(0.772572838848434,88.2775376361449,14.9961050118797));
#55075=CARTESIAN_POINT('Ctrl Pts',(0.652292830893653,88.2938360567285,15.0476168609656));
#55076=CARTESIAN_POINT('Ctrl Pts',(0.527979550470253,88.3101507799825,15.0863944018198));
#55077=CARTESIAN_POINT('Ctrl Pts',(0.424448048992129,88.3237381279225,15.1186893988996));
#55078=CARTESIAN_POINT('Ctrl Pts',(0.318119568450548,88.3373355083416,15.1421548104238));
#55079=CARTESIAN_POINT('Ctrl Pts',(0.21043485802571,88.3509009945917,15.1561212148862));
#55080=CARTESIAN_POINT('Ctrl Pts',(0.193733636880033,88.353004916169,15.1582873163561));
#55081=CARTESIAN_POINT('Ctrl Pts',(0.176999815718304,88.3551080656399,15.1602248287819));
#55082=CARTESIAN_POINT('Ctrl Pts',(0.160238800968447,88.3572102812538,15.16193114556));
#55083=CARTESIAN_POINT('Ctrl Pts',(0.141476024033436,88.3595635637501,15.1638412471597));
#55084=CARTESIAN_POINT('Ctrl Pts',(0.122678954636867,88.3619157260795,15.1654616709255));
#55085=CARTESIAN_POINT('Ctrl Pts',(0.10385496296275,88.3642666004607,15.1667887242495));
#55086=CARTESIAN_POINT('Ctrl Pts',(0.0922631908627425,88.3657142636628,
15.1676059207275));
#55087=CARTESIAN_POINT('Ctrl Pts',(0.0806612020310315,88.3671614397823,
15.1683118679641));
#55088=CARTESIAN_POINT('Ctrl Pts',(0.0690508883100946,88.3686087156104,
15.1689060565451));
#55089=CARTESIAN_POINT('Ctrl Pts',(0.0690284406559001,88.3686115138076,
15.1689072053633));
#55090=CARTESIAN_POINT('Ctrl Pts',(0.0690059929749823,88.3686143120047,
15.1689083537636));
#55091=CARTESIAN_POINT('Ctrl Pts',(0.0689835452673973,88.3686171102018,
15.1689095017459));
#55092=CARTESIAN_POINT('Ctrl Pts',(-0.070287697526535,88.3859778310131,
15.1760318739227));
#55093=CARTESIAN_POINT('Ctrl Pts',(-0.210584287670222,88.4033360018279,
15.1670707961934));
#55094=CARTESIAN_POINT('Ctrl Pts',(-0.348542202327559,88.42073729513,15.1429176745781));
#55095=CARTESIAN_POINT('Ctrl Pts',(-0.358190763821437,88.4219543144573,
15.1412284429037));
#55096=CARTESIAN_POINT('Ctrl Pts',(-0.36782789330803,88.4231715456873,15.139464881447));
#55097=CARTESIAN_POINT('Ctrl Pts',(-0.377452442644003,88.4243890048776,
15.1376272862118));
#55098=CARTESIAN_POINT('Ctrl Pts',(-0.525784711087892,88.443152323256,15.1093065139653));
#55099=CARTESIAN_POINT('Ctrl Pts',(-0.67112756312192,88.4619706881551,15.0634013115342));
#55100=CARTESIAN_POINT('Ctrl Pts',(-0.809209684749959,88.4808904252129,
15.0010065114326));
#55101=CARTESIAN_POINT('Ctrl Pts',(-0.915286597597981,88.4954248723616,
14.95307381968));
#55102=CARTESIAN_POINT('Ctrl Pts',(-1.01707635697222,88.5100191074381,14.8954089399599));
#55103=CARTESIAN_POINT('Ctrl Pts',(-1.11262549323639,88.5246831062465,14.8285262668702));
#55104=CARTESIAN_POINT('Ctrl Pts',(-1.11264320870511,88.524685825053,14.8285138663614));
#55105=CARTESIAN_POINT('Ctrl Pts',(-1.11266092395628,88.5246885438601,14.8285014655372));
#55106=CARTESIAN_POINT('Ctrl Pts',(-1.11267863898987,88.5246912626678,14.8284890643975));
#55107=CARTESIAN_POINT('Ctrl Pts',(-1.14330389067457,88.5293914609561,14.8070503229886));
#55108=CARTESIAN_POINT('Ctrl Pts',(-1.17327906528719,88.5340934965997,14.784668819843));
#55109=CARTESIAN_POINT('Ctrl Pts',(-1.20256533457562,88.5387822359258,14.7613880173182));
#55110=CARTESIAN_POINT('Ctrl Pts',(-1.28076835270619,88.5513025594575,14.6992213751961));
#55111=CARTESIAN_POINT('Ctrl Pts',(-1.3540720573365,88.5637289006479,14.6306356532594));
#55112=CARTESIAN_POINT('Ctrl Pts',(-1.42175796014288,88.5761351624016,14.5566053511265));
#55113=CARTESIAN_POINT('Ctrl Pts',(-1.43743837137839,88.5790092510689,14.5394551686926));
#55114=CARTESIAN_POINT('Ctrl Pts',(-1.45281720496687,88.58188227308,14.5220125780203));
#55115=CARTESIAN_POINT('Ctrl Pts',(-1.46788535457596,88.5847551667695,14.5042893392683));
#55116=CARTESIAN_POINT('Ctrl Pts',(-1.54742303947419,88.5999198232771,14.4107366857705));
#55117=CARTESIAN_POINT('Ctrl Pts',(-1.61830131596351,88.6150824282435,14.3093661358428));
#55118=CARTESIAN_POINT('Ctrl Pts',(-1.67907078711494,88.6303616915243,14.2020380497371));
#55119=CARTESIAN_POINT('Ctrl Pts',(-1.72593318368016,88.6421443001519,14.1192719627797));
#55120=CARTESIAN_POINT('Ctrl Pts',(-1.76678510767278,88.6540094323558,14.0329658365348));
#55121=CARTESIAN_POINT('Ctrl Pts',(-1.80094213854806,88.6659640695943,13.9440350260138));
#55122=CARTESIAN_POINT('Ctrl Pts',(-1.81020183570973,88.6692048758842,13.9199265964265));
#55123=CARTESIAN_POINT('Ctrl Pts',(-1.81896979445852,88.6724522611031,13.8956253788955));
#55124=CARTESIAN_POINT('Ctrl Pts',(-1.82723302397085,88.6757063666283,13.8711497962955));
#55125=CARTESIAN_POINT('Ctrl Pts',(-1.83276921354094,88.6778865487279,13.8547516719411));
#55126=CARTESIAN_POINT('Ctrl Pts',(-1.83807983876247,88.6800728975008,13.8382761995627));
#55127=CARTESIAN_POINT('Ctrl Pts',(-1.84316024200901,88.6822630488197,13.8217285750483));
#55128=CARTESIAN_POINT('Ctrl Pts',(-1.84316638864592,88.6822656986222,13.8217085545431));
#55129=CARTESIAN_POINT('Ctrl Pts',(-1.84317253494513,88.6822683484268,13.82168853393));
#55130=CARTESIAN_POINT('Ctrl Pts',(-1.84317868090663,88.6822709982337,13.8216685132089));
#55131=CARTESIAN_POINT('Ctrl Pts',(-1.86892231542519,88.6933702638707,13.7378075702968));
#55132=CARTESIAN_POINT('Ctrl Pts',(-1.88874221743413,88.7045085538322,13.6520510803805));
#55133=CARTESIAN_POINT('Ctrl Pts',(-1.90260347940684,88.7155397309517,13.5651986453666));
#55134=CARTESIAN_POINT('Ctrl Pts',(-1.91714044322766,88.727108650362,13.4741123714014));
#55135=CARTESIAN_POINT('Ctrl Pts',(-1.92513147837901,88.7385629232425,13.381790520261));
#55136=CARTESIAN_POINT('Ctrl Pts',(-1.92658457169027,88.7499864935363,13.2891274507891));
#55137=CARTESIAN_POINT('Ctrl Pts',(-1.92669666596446,88.7508677286303,13.281979252228));
#55138=CARTESIAN_POINT('Ctrl Pts',(-1.92676982938156,88.7517487820746,13.2748290153574));
#55139=CARTESIAN_POINT('Ctrl Pts',(-1.92680405313675,88.7526296929277,13.2676771474935));
#55140=CARTESIAN_POINT('Ctrl Pts',(-1.9272815806858,88.764921131969,13.1678864052528));
#55141=CARTESIAN_POINT('Ctrl Pts',(-1.92017781361939,88.7771855323595,13.0677812152398));
#55142=CARTESIAN_POINT('Ctrl Pts',(-1.90552280605296,88.7896695333862,12.9686089262628));
#55143=CARTESIAN_POINT('Ctrl Pts',(-1.8932155739099,88.8001535606385,12.8853243303956));
#55144=CARTESIAN_POINT('Ctrl Pts',(-1.87553987749642,88.8106760280621,12.8026900340916));
#55145=CARTESIAN_POINT('Ctrl Pts',(-1.85250168192507,88.8212112017768,12.7215222233453));
#55146=CARTESIAN_POINT('Ctrl Pts',(-1.8485508230959,88.8230178964009,12.7076026192366));
#55147=CARTESIAN_POINT('Ctrl Pts',(-1.84444237869501,88.8248249636679,12.6937261229755));
#55148=CARTESIAN_POINT('Ctrl Pts',(-1.84017653107027,88.8266322725088,12.679896816798));
#55149=CARTESIAN_POINT('Ctrl Pts',(-1.82788403118873,88.8318402278008,12.6400461799487));
#55150=CARTESIAN_POINT('Ctrl Pts',(-1.81428462719994,88.8370499829996,12.6005891431198));
#55151=CARTESIAN_POINT('Ctrl Pts',(-1.79938852578499,88.8422591879168,12.5616287924912));
#55152=CARTESIAN_POINT('Ctrl Pts',(-1.79938643079468,88.8422599205403,12.5616233131007));
#55153=CARTESIAN_POINT('Ctrl Pts',(-1.7993843357787,88.8422606531638,12.5616178337199));
#55154=CARTESIAN_POINT('Ctrl Pts',(-1.79938224073711,88.8422613857873,12.561612354349));
#55155=CARTESIAN_POINT('Ctrl Pts',(-1.75550406698741,88.8576053197836,12.446853397281));
#55156=CARTESIAN_POINT('Ctrl Pts',(-1.70034180852954,88.8731353030725,12.3361735205915));
#55157=CARTESIAN_POINT('Ctrl Pts',(-1.63522825572563,88.8886956056469,12.2313434824035));
#55158=CARTESIAN_POINT('Ctrl Pts',(-1.62643500288793,88.890796945059,12.2171867210063));
#55159=CARTESIAN_POINT('Ctrl Pts',(-1.617458928175,88.892896337484,12.2031358116288));
#55160=CARTESIAN_POINT('Ctrl Pts',(-1.60830260955541,88.894993274374,12.1891943641998));
#55161=CARTESIAN_POINT('Ctrl Pts',(-1.54062215107708,88.9104931336528,12.0861438268552));
#55162=CARTESIAN_POINT('Ctrl Pts',(-1.46308219877645,88.9258613603039,11.9890520800018));
#55163=CARTESIAN_POINT('Ctrl Pts',(-1.37699019122256,88.9412219523006,11.8996963459718));
#55164=CARTESIAN_POINT('Ctrl Pts',(-1.31131188603211,88.952940318241,11.8315281926566));
#55165=CARTESIAN_POINT('Ctrl Pts',(-1.24065405095072,88.9646548994021,11.7678683169257));
#55166=CARTESIAN_POINT('Ctrl Pts',(-1.16569620874684,88.9764421092307,11.7095709213478));
#55167=CARTESIAN_POINT('Ctrl Pts',(-1.14618501867988,88.979510267072,11.6943963707993));
#55168=CARTESIAN_POINT('Ctrl Pts',(-1.12638263452638,88.9825833522257,11.6795849184114));
#55169=CARTESIAN_POINT('Ctrl Pts',(-1.10630132330414,88.9856627252353,11.6651511174682));
#55170=CARTESIAN_POINT('Ctrl Pts',(-1.0644720027289,88.9920770514396,11.6350855465456));
#55171=CARTESIAN_POINT('Ctrl Pts',(-1.02143273510767,88.998514613264,11.6066601662151));
#55172=CARTESIAN_POINT('Ctrl Pts',(-0.977289395214185,89.0049551134961,
11.5800067458424));
#55173=CARTESIAN_POINT('Ctrl Pts',(-0.97728531593376,89.0049557086619,11.5800042828032));
#55174=CARTESIAN_POINT('Ctrl Pts',(-0.977281236643895,89.0049563038278,
11.5800018197791));
#55175=CARTESIAN_POINT('Ctrl Pts',(-0.977277157344618,89.0049568989936,
11.5799993567702));
#55176=CARTESIAN_POINT('Ctrl Pts',(-0.88357127860379,89.0186284969469,11.5234214005323));
#55177=CARTESIAN_POINT('Ctrl Pts',(-0.784840679583591,89.032320993757,11.4747921042201));
#55178=CARTESIAN_POINT('Ctrl Pts',(-0.682527944527905,89.0460419552663,
11.4344753065681));
#55179=CARTESIAN_POINT('Ctrl Pts',(-0.625672812331476,89.0536666862448,
11.4120712836574));
#55180=CARTESIAN_POINT('Ctrl Pts',(-0.56771688018984,89.0612994637232,11.3922360142513));
#55181=CARTESIAN_POINT('Ctrl Pts',(-0.50887542212368,89.0689454292853,11.3750286892932));
#55182=CARTESIAN_POINT('Ctrl Pts',(-0.467551151634506,89.0743151797882,
11.3629440099815));
#55183=CARTESIAN_POINT('Ctrl Pts',(-0.425786136417242,89.0796919274121,
11.3521549132987));
#55184=CARTESIAN_POINT('Ctrl Pts',(-0.383665898479768,89.0850759437852,
11.3426887221775));
#55185=CARTESIAN_POINT('Ctrl Pts',(-0.318657542679909,89.0933856321715,
11.3280786071685));
#55186=CARTESIAN_POINT('Ctrl Pts',(-0.252811363603994,89.1017115284866,
11.3166234226641));
#55187=CARTESIAN_POINT('Ctrl Pts',(-0.18650142947116,89.110047498965,11.308425057102));
#55188=CARTESIAN_POINT('Ctrl Pts',(-0.14355625558476,89.115446233052,11.303115441895));
#55189=CARTESIAN_POINT('Ctrl Pts',(-0.100418764458797,89.1208489327816,
11.2991716018796));
#55190=CARTESIAN_POINT('Ctrl Pts',(-0.0571844508449886,89.1262547580831,
11.2966164159531));
#55191=CARTESIAN_POINT('Ctrl Pts',(0.0604709601886317,89.1409658647172,
11.289662877772));
#55192=CARTESIAN_POINT('Ctrl Pts',(0.178885143680646,89.1557053730745,11.2929852068958));
#55193=CARTESIAN_POINT('Ctrl Pts',(0.296359922324314,89.1704838848156,11.3070610843454));
#55194=CARTESIAN_POINT('Ctrl Pts',(0.331361481102446,89.1748871359077,11.3112549858585));
#55195=CARTESIAN_POINT('Ctrl Pts',(0.366269713742105,89.1792926013931,11.3164027192666));
#55196=CARTESIAN_POINT('Ctrl Pts',(0.401039572772554,89.1837003908852,11.3224841858637));
#55197=CARTESIAN_POINT('Ctrl Pts',(0.48654720070858,89.1945402284463,11.3374400067266));
#55198=CARTESIAN_POINT('Ctrl Pts',(0.571217792866004,89.2053941230983,11.3580424414153));
#55199=CARTESIAN_POINT('Ctrl Pts',(0.65438387511388,89.2162637405947,11.3839978508651));
#55200=CARTESIAN_POINT('Ctrl Pts',(0.732063173523896,89.2264162479426,11.4082408828981));
#55201=CARTESIAN_POINT('Ctrl Pts',(0.808426473979414,89.2365818485877,11.4371497096827));
#55202=CARTESIAN_POINT('Ctrl Pts',(0.882998816270637,89.2467715336368,11.4705286918841));
#55203=CARTESIAN_POINT('Ctrl Pts',(0.938928072989054,89.2544137974237,11.4955629285351));
#55204=CARTESIAN_POINT('Ctrl Pts',(0.993849744945934,89.2620695979862,11.5231124143193));
#55205=CARTESIAN_POINT('Ctrl Pts',(1.04755755838892,89.2697437728252,11.5531086165209));
#55206=CARTESIAN_POINT('Ctrl Pts',(1.12368721025552,89.2806217479538,11.595627577628));
#55207=CARTESIAN_POINT('Ctrl Pts',(1.19736134207103,89.2915347285946,11.6430608663885));
#55208=CARTESIAN_POINT('Ctrl Pts',(1.26780855661208,89.3024701535888,11.6950965809544));
#55209=CARTESIAN_POINT('Ctrl Pts',(1.3071334156102,89.3085744977958,11.7241438208133));
#55210=CARTESIAN_POINT('Ctrl Pts',(1.34545485670253,89.3146861324596,11.7546259588067));
#55211=CARTESIAN_POINT('Ctrl Pts',(1.38263475452757,89.3208015576538,11.7864757641263));
#55212=CARTESIAN_POINT('Ctrl Pts',(1.40493679414824,89.3244698424786,11.8055805939321));
#55213=CARTESIAN_POINT('Ctrl Pts',(1.42682784486132,89.3281394352485,11.8251771159743));
#55214=CARTESIAN_POINT('Ctrl Pts',(1.44827864572589,89.3318094905473,11.8452492171506));
#55215=CARTESIAN_POINT('Ctrl Pts',(1.46185725747976,89.3341326791467,11.8579550956247));
#55216=CARTESIAN_POINT('Ctrl Pts',(1.47525947650682,89.3364560529941,11.870851522993));
#55217=CARTESIAN_POINT('Ctrl Pts',(1.48847807565657,89.3387793967194,11.8839342377171));
#55218=CARTESIAN_POINT('Ctrl Pts',(1.48919006313926,89.3389045379414,11.8846389061179));
#55219=CARTESIAN_POINT('Ctrl Pts',(1.48990151699167,89.3390296789076,11.8853441139905));
#55220=CARTESIAN_POINT('Ctrl Pts',(1.49061243900187,89.3391548200955,11.8860498635413));
#55221=CARTESIAN_POINT('Ctrl Pts',(1.53796667828799,89.3474904260729,11.9330595673163));
#55222=CARTESIAN_POINT('Ctrl Pts',(1.58303905039154,89.3558409301251,11.9825522306307));
#55223=CARTESIAN_POINT('Ctrl Pts',(1.62563651172041,89.3642002299135,12.034208949601));
#55224=CARTESIAN_POINT('Ctrl Pts',(1.66017048461133,89.3709771556569,12.0760873075337));
#55225=CARTESIAN_POINT('Ctrl Pts',(1.69307497363486,89.3777591313303,12.1193826302394));
#55226=CARTESIAN_POINT('Ctrl Pts',(1.72427118536988,89.3845466705138,12.1639448302362));
#55227=CARTESIAN_POINT('Ctrl Pts',(1.7723601786545,89.3950096693223,12.2326375085202));
#55228=CARTESIAN_POINT('Ctrl Pts',(1.81639346664075,89.4054859067877,12.3043386438082));
#55229=CARTESIAN_POINT('Ctrl Pts',(1.856114219698,89.415988959184,12.3785926830031));
#55230=CARTESIAN_POINT('Ctrl Pts',(1.88283639958516,89.4230548991247,12.4285471687565));
#55231=CARTESIAN_POINT('Ctrl Pts',(1.90760721690775,89.43013345873,12.4796614282811));
#55232=CARTESIAN_POINT('Ctrl Pts',(1.9303286602954,89.4372260301786,12.5317815956755));
#55233=CARTESIAN_POINT('Ctrl Pts',(1.95628446216158,89.4453282170028,12.5913209794656));
#55234=CARTESIAN_POINT('Ctrl Pts',(1.97956412584269,89.4534482687498,12.6521701956165));
#55235=CARTESIAN_POINT('Ctrl Pts',(2.00001176280668,89.4615857304721,12.7140795605838));
#55236=CARTESIAN_POINT('Ctrl Pts',(2.02192190428606,89.4703052190825,12.7804169543727));
#55237=CARTESIAN_POINT('Ctrl Pts',(2.040576579806,89.4790439672403,12.8479664224331));
#55238=CARTESIAN_POINT('Ctrl Pts',(2.05577954694863,89.4877940034291,12.9163579397568));
#55239=CARTESIAN_POINT('Ctrl Pts',(2.06935354874347,89.4956064919925,12.9774214525693));
#55240=CARTESIAN_POINT('Ctrl Pts',(2.08017563594528,89.5034283277029,13.0391587881085));
#55241=CARTESIAN_POINT('Ctrl Pts',(2.08812177108522,89.5112493390432,13.1012674024404));
#55242=CARTESIAN_POINT('Ctrl Pts',(2.09005648935272,89.5131535922737,13.1163895553614));
#55243=CARTESIAN_POINT('Ctrl Pts',(2.09182208300424,89.5150589979386,13.1315432490946));
#55244=CARTESIAN_POINT('Ctrl Pts',(2.0934187011358,89.5169654566193,13.1467240255892));
#55245=CARTESIAN_POINT('Ctrl Pts',(2.10074709634374,89.5257160040317,13.2164030098854));
#55246=CARTESIAN_POINT('Ctrl Pts',(2.10451285347956,89.534488708651,13.2866526735456));
#55247=CARTESIAN_POINT('Ctrl Pts',(2.10475057987297,89.5432733544065,13.3570336583967));
#55248=CARTESIAN_POINT('Ctrl Pts',(2.10501914391959,89.5531975364809,13.4365444010816));
#55249=CARTESIAN_POINT('Ctrl Pts',(2.10078732204221,89.5631359980126,13.5162144357751));
#55250=CARTESIAN_POINT('Ctrl Pts',(2.09213952711942,89.5730846102658,13.5954956988927));
#55251=CARTESIAN_POINT('Ctrl Pts',(2.08571265698564,89.5804782221093,13.6544159654634));
#55252=CARTESIAN_POINT('Ctrl Pts',(2.07684811118568,89.587876932403,13.7131175816072));
#55253=CARTESIAN_POINT('Ctrl Pts',(2.06558085022872,89.5952817283004,13.7713987939231));
#55254=CARTESIAN_POINT('Ctrl Pts',(2.05436939552993,89.6026498485627,13.829391341905));
#55255=CARTESIAN_POINT('Ctrl Pts',(2.04077868025402,89.6100243673617,13.8869707059215));
#55256=CARTESIAN_POINT('Ctrl Pts',(2.02483599892223,89.6174076406047,13.9439492280045));
#55257=CARTESIAN_POINT('Ctrl Pts',(2.00307053176937,89.6274875254061,14.0217381598037));
#55258=CARTESIAN_POINT('Ctrl Pts',(1.97692397415145,89.6375839353334,14.098410238515));
#55259=CARTESIAN_POINT('Ctrl Pts',(1.94641313496093,89.6477506886991,14.1735369875866));
#55260=CARTESIAN_POINT('Ctrl Pts',(1.94377149502577,89.6486309300302,14.1800414897836));
#55261=CARTESIAN_POINT('Ctrl Pts',(1.9410971101864,89.6495116986406,14.1865343945289));
#55262=CARTESIAN_POINT('Ctrl Pts',(1.93838997466722,89.6503930294411,14.193015415411));
#55263=CARTESIAN_POINT('Ctrl Pts',(1.9089497892047,89.6599775301189,14.2634967250478));
#55264=CARTESIAN_POINT('Ctrl Pts',(1.87562502392566,89.6696089976808,14.3325947961261));
#55265=CARTESIAN_POINT('Ctrl Pts',(1.8385115263671,89.6792235000755,14.3997602950827));
#55266=CARTESIAN_POINT('Ctrl Pts',(1.82827175689371,89.6818761815687,14.4182915376527));
#55267=CARTESIAN_POINT('Ctrl Pts',(1.8177438556117,89.6845275722367,14.4366757891377));
#55268=CARTESIAN_POINT('Ctrl Pts',(1.80693046342033,89.6871763309873,14.4549018348219));
#55269=CARTESIAN_POINT('Ctrl Pts',(1.8068646824474,89.6871924441482,14.4550127090968));
#55270=CARTESIAN_POINT('Ctrl Pts',(1.80679889060703,89.6872085573509,14.4551235780121));
#55271=CARTESIAN_POINT('Ctrl Pts',(1.80673308789959,89.6872246705955,14.4552344415652));
#55272=CARTESIAN_POINT('Ctrl Pts',(1.76972370936136,89.6962872333995,14.5175873653615));
#55273=CARTESIAN_POINT('Ctrl Pts',(1.72927268942425,89.7053630621505,14.5782422687359));
#55274=CARTESIAN_POINT('Ctrl Pts',(1.68570332980984,89.71444840587,14.6368121121542));
#55275=CARTESIAN_POINT('Ctrl Pts',(1.66295094763571,89.7191928688211,14.6673979062335));
#55276=CARTESIAN_POINT('Ctrl Pts',(1.63934899938293,89.7239399221334,14.6974154466037));
#55277=CARTESIAN_POINT('Ctrl Pts',(1.61494840448925,89.728689001459,14.7268123931874));
#55278=CARTESIAN_POINT('Ctrl Pts',(1.56533763931517,89.738344727487,14.7865816332472));
#55279=CARTESIAN_POINT('Ctrl Pts',(1.51242342376077,89.7480091484005,14.8437830380337));
#55280=CARTESIAN_POINT('Ctrl Pts',(1.45664814402652,89.7576945147177,14.8980214692319));
#55281=CARTESIAN_POINT('Ctrl Pts',(1.4475441902962,89.7592754144861,14.9068745699315));
#55282=CARTESIAN_POINT('Ctrl Pts',(1.43836408598314,89.7608568712848,14.9156488128494));
#55283=CARTESIAN_POINT('Ctrl Pts',(1.42910983920534,89.7624389371867,14.9243425814522));
#55284=CARTESIAN_POINT('Ctrl Pts',(1.37930610290667,89.7709531679907,14.9711299828834));
#55285=CARTESIAN_POINT('Ctrl Pts',(1.32736213493766,89.7794681696918,15.0155896551332));
#55286=CARTESIAN_POINT('Ctrl Pts',(1.2734092069618,89.7880180567517,15.0576107838982));
#55287=CARTESIAN_POINT('Ctrl Pts',(1.24821863978466,89.7920099903208,15.0772304061639));
#55288=CARTESIAN_POINT('Ctrl Pts',(1.2225895882429,89.7960095299081,15.0963179304627));
#55289=CARTESIAN_POINT('Ctrl Pts',(1.19653285737242,89.8000201534158,15.1148591442773));
#55290=CARTESIAN_POINT('Ctrl Pts',(1.10396081883357,89.8142687403077,15.1807307215037));
#55291=CARTESIAN_POINT('Ctrl Pts',(1.00595061054925,89.8286342969753,15.239732538508));
#55292=CARTESIAN_POINT('Ctrl Pts',(0.903574269901593,89.8430052181643,15.2907907530602));
#55293=CARTESIAN_POINT('Ctrl Pts',(0.846152658837509,89.8510656884051,15.3194286680227));
#55294=CARTESIAN_POINT('Ctrl Pts',(0.787363081876542,89.8591270242994,15.3455643649816));
#55295=CARTESIAN_POINT('Ctrl Pts',(0.727444049749919,89.867165541212,15.369003265404));
#55296=CARTESIAN_POINT('Ctrl Pts',(0.727402714504093,89.8671710865965,15.3690194347692));
#55297=CARTESIAN_POINT('Ctrl Pts',(0.727361378695082,89.8671766319729,15.3690356028621));
#55298=CARTESIAN_POINT('Ctrl Pts',(0.727320042322842,89.8671821773411,15.3690517696829));
#55299=CARTESIAN_POINT('Ctrl Pts',(0.633926362663027,89.8797111515772,15.4055784118837));
#55300=CARTESIAN_POINT('Ctrl Pts',(0.537655586078528,89.8921986464091,15.4356068382399));
#55301=CARTESIAN_POINT('Ctrl Pts',(0.439549471909447,89.9047021655974,15.4589748238371));
#55302=CARTESIAN_POINT('Ctrl Pts',(0.391781509366459,89.9107901412684,15.4703527187845));
#55303=CARTESIAN_POINT('Ctrl Pts',(0.343578845031173,89.9168818983963,15.4801522981313));
#55304=CARTESIAN_POINT('Ctrl Pts',(0.295063468373458,89.9229839676533,15.4883589325666));
#55305=CARTESIAN_POINT('Ctrl Pts',(0.21733041195195,89.932760919344,15.501507893196));
#55306=CARTESIAN_POINT('Ctrl Pts',(0.138781505009049,89.9425667517482,15.5105715366972));
#55307=CARTESIAN_POINT('Ctrl Pts',(0.0598350709781667,89.9524389190382,
15.5154971229762));
#55308=CARTESIAN_POINT('Ctrl Pts',(-0.0907905799123581,89.9712744958698,
15.5248948829688));
#55309=CARTESIAN_POINT('Ctrl Pts',(-0.242935126360048,89.9903610793247,
15.5192327218574));
#55310=CARTESIAN_POINT('Ctrl Pts',(-0.393543685354344,90.0094943828665,
15.4981219338294));
#55311=CARTESIAN_POINT('Ctrl Pts',(-0.482069985530059,90.0207407594603,
15.4857132103784));
#55312=CARTESIAN_POINT('Ctrl Pts',(-0.570055749724395,90.0320010766183,
15.4679628941004));
#55313=CARTESIAN_POINT('Ctrl Pts',(-0.656768808477112,90.0432243027483,
15.4448295293634));
#55314=CARTESIAN_POINT('Ctrl Pts',(-0.677209396973242,90.0458699174944,
15.4393763762176));
#55315=CARTESIAN_POINT('Ctrl Pts',(-0.697579335379399,90.048513473307,15.4336243185246));
#55316=CARTESIAN_POINT('Ctrl Pts',(-0.717869188378609,90.0511543057617,
15.4275732122971));
#55317=CARTESIAN_POINT('Ctrl Pts',(-0.717876542771937,90.0511552629752,
15.4275710189734));
#55318=CARTESIAN_POINT('Ctrl Pts',(-0.717883897155325,90.0511562201883,
15.4275688256103));
#55319=CARTESIAN_POINT('Ctrl Pts',(-0.717891251528768,90.0511571774009,
15.4275666322078));
#55320=CARTESIAN_POINT('Ctrl Pts',(-0.827736790592108,90.0654541855691,
15.3948057879492));
#55321=CARTESIAN_POINT('Ctrl Pts',(-0.935357513734576,90.0796566860487,
15.3532510554188));
#55322=CARTESIAN_POINT('Ctrl Pts',(-1.03947911611388,90.0939337420625,15.3036333564526));
#55323=CARTESIAN_POINT('Ctrl Pts',(-1.07355714578967,90.0986064893829,15.287393946194));
#55324=CARTESIAN_POINT('Ctrl Pts',(-1.10726283864037,90.1032874756028,15.270290017163));
#55325=CARTESIAN_POINT('Ctrl Pts',(-1.14055784633631,90.1079830971342,15.2523436669056));
#55326=CARTESIAN_POINT('Ctrl Pts',(-1.24204696389607,90.1222961884534,15.1976399927789));
#55327=CARTESIAN_POINT('Ctrl Pts',(-1.33973260938104,90.136747990413,15.1351046176306));
#55328=CARTESIAN_POINT('Ctrl Pts',(-1.4324719090101,90.1512892718812,15.0654270397336));
#55329=CARTESIAN_POINT('Ctrl Pts',(-1.52576652305736,90.1659176252087,14.9953322388925));
#55330=CARTESIAN_POINT('Ctrl Pts',(-1.61405200452164,90.1806357466517,14.9180044120357));
#55331=CARTESIAN_POINT('Ctrl Pts',(-1.69606313870812,90.1953674578192,14.8342235573276));
#55332=CARTESIAN_POINT('Ctrl Pts',(-1.7617816118829,90.2071725081308,14.7670869434116));
#55333=CARTESIAN_POINT('Ctrl Pts',(-1.8234694431867,90.2189855359406,14.6958054663359));
#55334=CARTESIAN_POINT('Ctrl Pts',(-1.88045323053108,90.2307614340735,14.620850866844));
#55335=CARTESIAN_POINT('Ctrl Pts',(-1.89458042316835,90.233680867638,14.6022684223379));
#55336=CARTESIAN_POINT('Ctrl Pts',(-1.90841870829354,90.236598021982,14.5834603467572));
#55337=CARTESIAN_POINT('Ctrl Pts',(-1.92195827198616,90.2395122155635,14.5644340605548));
#55338=CARTESIAN_POINT('Ctrl Pts',(-1.92196095332451,90.2395127926824,14.5644302926409));
#55339=CARTESIAN_POINT('Ctrl Pts',(-1.92196363465126,90.2395133698013,14.5644265247183));
#55340=CARTESIAN_POINT('Ctrl Pts',(-1.92196631596654,90.23951394692,14.5644227567868));
#55341=CARTESIAN_POINT('Ctrl Pts',(-1.96439769823558,90.2486467574422,14.5047958479319));
#55342=CARTESIAN_POINT('Ctrl Pts',(-2.00393984298306,90.2577467821853,14.4429711086769));
#55343=CARTESIAN_POINT('Ctrl Pts',(-2.04045806000607,90.2668733450591,14.3792626217406));
#55344=CARTESIAN_POINT('Ctrl Pts',(-2.11723191437586,90.2860605197375,14.2453254666193));
#55345=CARTESIAN_POINT('Ctrl Pts',(-2.18065510084425,90.3053667354458,14.1030416821444));
#55346=CARTESIAN_POINT('Ctrl Pts',(-2.22975564814591,90.3247803034858,13.9553143987107));
#55347=CARTESIAN_POINT('Ctrl Pts',(-2.27591121519674,90.3430294736195,13.8164475853966));
#55348=CARTESIAN_POINT('Ctrl Pts',(-2.30940974774325,90.3613731262018,13.6727721598186));
#55349=CARTESIAN_POINT('Ctrl Pts',(-2.32943424498219,90.3798185934638,13.5267076351754));
#55350=CARTESIAN_POINT('Ctrl Pts',(-2.34701020656248,90.3960086041321,13.398503443942));
#55351=CARTESIAN_POINT('Ctrl Pts',(-2.35420629851879,90.4122771501022,13.2684594600005));
#55352=CARTESIAN_POINT('Ctrl Pts',(-2.35046331881443,90.4286438543728,13.1382034562168));
#55353=CARTESIAN_POINT('Ctrl Pts',(-2.35020431696362,90.4297763763293,13.1291901703524));
#55354=CARTESIAN_POINT('Ctrl Pts',(-2.34989293127384,90.4309093744856,13.1201758622685));
#55355=CARTESIAN_POINT('Ctrl Pts',(-2.34952903634181,90.4320427289652,13.1111610895567));
#55356=CARTESIAN_POINT('Ctrl Pts',(-2.34952837932184,90.4320447752606,13.1111448131945));
#55357=CARTESIAN_POINT('Ctrl Pts',(-2.34952772213086,90.4320468215568,13.1111285368325));
#55358=CARTESIAN_POINT('Ctrl Pts',(-2.34952706476887,90.4320488678537,13.1111122604705));
#55359=CARTESIAN_POINT('Ctrl Pts',(-2.34569136950774,90.4439889730878,13.0161399848232));
#55360=CARTESIAN_POINT('Ctrl Pts',(-2.33603579895137,90.4559546637623,12.9211722629142));
#55361=CARTESIAN_POINT('Ctrl Pts',(-2.32065263668303,90.4679454242299,12.8269115977101));
#55362=CARTESIAN_POINT('Ctrl Pts',(-2.30526601779872,90.4799388790366,12.7326297520156));
#55363=CARTESIAN_POINT('Ctrl Pts',(-2.2841475829805,90.4919571483405,12.6390547729888));
#55364=CARTESIAN_POINT('Ctrl Pts',(-2.25738210024256,90.503983664951,12.5469301646683));
#55365=CARTESIAN_POINT('Ctrl Pts',(-2.23074507497194,90.5159524618529,12.455247696472));
#55366=CARTESIAN_POINT('Ctrl Pts',(-2.19851342075431,90.5279290824648,12.3650020717527));
#55367=CARTESIAN_POINT('Ctrl Pts',(-2.1607880251354,90.5398858435885,12.2769672126659));
#55368=CARTESIAN_POINT('Ctrl Pts',(-2.13579511881785,90.547807144498,12.218644511214));
#55369=CARTESIAN_POINT('Ctrl Pts',(-2.10839141453715,90.5557194907249,12.1612930342263));
#55370=CARTESIAN_POINT('Ctrl Pts',(-2.07861575088476,90.5636133483745,12.1051455331855));
#55371=CARTESIAN_POINT('Ctrl Pts',(-2.07860974192645,90.5636149414158,12.1051342021872));
#55372=CARTESIAN_POINT('Ctrl Pts',(-2.0786037328715,90.5636165344548,12.1051228712357));
#55373=CARTESIAN_POINT('Ctrl Pts',(-2.07859772372004,90.5636181274914,12.1051115403313));
#55374=CARTESIAN_POINT('Ctrl Pts',(-2.04044817041101,90.5737316413858,12.0331764348937));
#55375=CARTESIAN_POINT('Ctrl Pts',(-1.99840413134336,90.5837520713751,11.9631304559366));
#55376=CARTESIAN_POINT('Ctrl Pts',(-1.95275133842558,90.5937882050271,11.8953265040634));
#55377=CARTESIAN_POINT('Ctrl Pts',(-1.88053299889385,90.609664405832,11.7880671557298));
#55378=CARTESIAN_POINT('Ctrl Pts',(-1.7992771670741,90.6255814097833,11.6864053235378));
#55379=CARTESIAN_POINT('Ctrl Pts',(-1.71023485897269,90.6416652727592,11.5915359226003));
#55380=CARTESIAN_POINT('Ctrl Pts',(-1.69318039702198,90.6447458491166,11.5733653852112));
#55381=CARTESIAN_POINT('Ctrl Pts',(-1.67584042436733,90.6478325277532,11.5554441003856));
#55382=CARTESIAN_POINT('Ctrl Pts',(-1.65822392842862,90.6509261671784,11.5377805595999));
#55383=CARTESIAN_POINT('Ctrl Pts',(-1.55690232746079,90.6687192913317,11.4361883793274));
#55384=CARTESIAN_POINT('Ctrl Pts',(-1.44646841097967,90.6866617835674,11.3430843777608));
#55385=CARTESIAN_POINT('Ctrl Pts',(-1.32863445590084,90.7046686978522,11.2598702682155));
#55386=CARTESIAN_POINT('Ctrl Pts',(-1.31660531051532,90.7065069437953,11.2513753091761));
#55387=CARTESIAN_POINT('Ctrl Pts',(-1.30449900161314,90.7083458653439,11.242983411804));
#55388=CARTESIAN_POINT('Ctrl Pts',(-1.29231732047533,90.7101853750474,11.2346960652191));
#55389=CARTESIAN_POINT('Ctrl Pts',(-1.20417827695615,90.7234949194345,11.1747339965159));
#55390=CARTESIAN_POINT('Ctrl Pts',(-1.1120907816292,90.7368358015747,11.1202407727964));
#55391=CARTESIAN_POINT('Ctrl Pts',(-1.01666699720766,90.7503325163293,11.0718745497284));
#55392=CARTESIAN_POINT('Ctrl Pts',(-0.990650113791305,90.754012337418,11.058687707533));
#55393=CARTESIAN_POINT('Ctrl Pts',(-0.964385361909007,90.7577037136244,
11.0459565830478));
#55394=CARTESIAN_POINT('Ctrl Pts',(-0.937885500959489,90.761409102389,11.0336950931625));
#55395=CARTESIAN_POINT('Ctrl Pts',(-0.8572604977869,90.7726826325209,10.9963898913434));
#55396=CARTESIAN_POINT('Ctrl Pts',(-0.774431577449996,90.7840915228087,
10.9634240026405));
#55397=CARTESIAN_POINT('Ctrl Pts',(-0.689887365874428,90.7954885709355,
10.9350906935229));
#55398=CARTESIAN_POINT('Ctrl Pts',(-0.62448651218742,90.8043049838289,10.913172899631));
#55399=CARTESIAN_POINT('Ctrl Pts',(-0.558059054054031,90.8131144022974,
10.8940262664436));
#55400=CARTESIAN_POINT('Ctrl Pts',(-0.490820708754846,90.8218507127328,
10.8777679086565));
#55401=CARTESIAN_POINT('Ctrl Pts',(-0.465155870456856,90.8251853574752,
10.8715621027024));
#55402=CARTESIAN_POINT('Ctrl Pts',(-0.439375156471158,90.82850937082,10.8657777826168));
#55403=CARTESIAN_POINT('Ctrl Pts',(-0.413493044403973,90.8318197572746,
10.8604218548983));
#55404=CARTESIAN_POINT('Ctrl Pts',(-0.413478074513194,90.8318216719609,
10.8604187570965));
#55405=CARTESIAN_POINT('Ctrl Pts',(-0.413463104582681,90.8318235866456,
10.8604156594385));
#55406=CARTESIAN_POINT('Ctrl Pts',(-0.413448134612573,90.8318255013288,
10.8604125619243));
#55407=CARTESIAN_POINT('Ctrl Pts',(-0.333529509966445,90.8420472217721,
10.8438761848016));
#55408=CARTESIAN_POINT('Ctrl Pts',(-0.252479021499226,90.8522261073672,
10.8314406872672));
#55409=CARTESIAN_POINT('Ctrl Pts',(-0.170791271286606,90.8623925468392,
10.8231091301441));
#55410=CARTESIAN_POINT('Ctrl Pts',(-0.0888772994115235,90.872587140702,
10.8147545000548));
#55411=CARTESIAN_POINT('Ctrl Pts',(-0.006322974021356,90.8827697010739,
10.8105251555397));
#55412=CARTESIAN_POINT('Ctrl Pts',(0.0764170553935699,90.8929762453701,
10.8104036016593));
#55413=CARTESIAN_POINT('Ctrl Pts',(0.159274164449316,90.9031972322349,10.8102818757764));
#55414=CARTESIAN_POINT('Ctrl Pts',(0.242317594805092,90.9134426941975,10.8142782626444));
#55415=CARTESIAN_POINT('Ctrl Pts',(0.325137423376013,90.9237474031384,10.8223751710848));
#55416=CARTESIAN_POINT('Ctrl Pts',(0.350440559585788,90.9268957005744,10.8248489407204));
#55417=CARTESIAN_POINT('Ctrl Pts',(0.375723142416177,90.9300494945329,10.8277055381386));
#55418=CARTESIAN_POINT('Ctrl Pts',(0.400974295891035,90.9332096597013,10.8309447386746));
#55419=CARTESIAN_POINT('Ctrl Pts',(2.7026896336633,109.940943033253,11.4686318458822));
#55420=CARTESIAN_POINT('Ctrl Pts',(3.26735297233184,110.066470556496,12.3011813254344));
#55421=CARTESIAN_POINT('Ctrl Pts',(3.54872189103824,110.31458662676,14.4925410642362));
#55422=CARTESIAN_POINT('Ctrl Pts',(1.2278560935176,110.683943140033,16.8126341319678));
#55423=CARTESIAN_POINT('Ctrl Pts',(-1.98815709271125,111.048104563125,16.4106880643088));
#55424=CARTESIAN_POINT('Ctrl Pts',(-3.4441229434605,111.368813519898,13.9701597426272));
#55425=CARTESIAN_POINT('Ctrl Pts',(-2.93831080545766,111.646687017574,11.690169137757));
#55426=CARTESIAN_POINT('Ctrl Pts',(-1.49830702440856,111.882714715422,10.3371241303155));
#55427=CARTESIAN_POINT('Ctrl Pts',(0.280737125628576,112.096881644401,10.0718010286459));
#55428=CARTESIAN_POINT('Ctrl Pts',(1.74904768178971,112.289662909091,10.662271337796));
#55429=CARTESIAN_POINT('Ctrl Pts',(3.02452688847434,112.518914294108,12.0562658471873));
#55430=CARTESIAN_POINT('Ctrl Pts',(3.11698085316947,112.697773863978,13.6322209732873));
#55431=CARTESIAN_POINT('Ctrl Pts',(2.67727559417373,112.828040954899,14.5802342731525));
#55432=CARTESIAN_POINT('Ctrl Pts',(2.53266799104064,112.865192170059,14.8405243568169));
#55433=CARTESIAN_POINT('Ctrl Pts',(2.38092755732967,112.897610736312,15.0523028856687));
#55434=CARTESIAN_POINT('Ctrl Pts',(2.23522000283791,112.925334087009,15.2199637994609));
#55435=CARTESIAN_POINT('Ctrl Pts',(2.13400663653402,112.943798822738,15.3278891434887));
#55436=CARTESIAN_POINT('Ctrl Pts',(2.0001787117739,112.966847391524,15.455301731792));
#55437=CARTESIAN_POINT('Ctrl Pts',(1.85738520662406,112.989851815714,15.5720267197933));
#55438=CARTESIAN_POINT('Ctrl Pts',(1.73828449576717,113.008229097572,15.6586262836342));
#55439=CARTESIAN_POINT('Ctrl Pts',(1.51431603254412,113.041887977247,15.808876006038));
#55440=CARTESIAN_POINT('Ctrl Pts',(0.956180939097246,113.119679718823,16.0934532359472));
#55441=CARTESIAN_POINT('Ctrl Pts',(0.273313501728111,113.204429118413,16.2098273011314));
#55442=CARTESIAN_POINT('Ctrl Pts',(-0.303493560391393,113.276579576405,
16.1618219259865));
#55443=CARTESIAN_POINT('Ctrl Pts',(-0.681851442858624,113.324549589041,
16.0917776669268));
#55444=CARTESIAN_POINT('Ctrl Pts',(-1.13601080272643,113.384261897672,15.933918065193));
#55445=CARTESIAN_POINT('Ctrl Pts',(-1.62932968530997,113.455513991744,15.6408930038963));
#55446=CARTESIAN_POINT('Ctrl Pts',(-2.19233238507603,113.549976853383,15.1296830484934));
#55447=CARTESIAN_POINT('Ctrl Pts',(-2.77518491629114,113.690435180344,14.1396792195023));
#55448=CARTESIAN_POINT('Ctrl Pts',(-2.81554662440005,113.874922446606,12.5934052944144));
#55449=CARTESIAN_POINT('Ctrl Pts',(-1.8804390341719,114.078615238882,11.163100039376));
#55450=CARTESIAN_POINT('Ctrl Pts',(-0.329416415584754,114.278390904853,
10.5298412194754));
#55451=CARTESIAN_POINT('Ctrl Pts',(1.27457905533916,114.474208054262,10.8825417553195));
#55452=CARTESIAN_POINT('Ctrl Pts',(2.37162054973234,114.666047218268,12.0600861420246));
#55453=CARTESIAN_POINT('Ctrl Pts',(2.56321987131624,114.822601276229,13.3585258539676));
#55454=CARTESIAN_POINT('Ctrl Pts',(2.26157455097497,114.945869817376,14.3109533766938));
#55455=CARTESIAN_POINT('Ctrl Pts',(1.83956712796069,115.037340055854,14.9205049468466));
#55456=CARTESIAN_POINT('Ctrl Pts',(1.26089548214983,115.127834416872,15.3697004555521));
#55457=CARTESIAN_POINT('Ctrl Pts',(0.129036300584683,115.277046540176,15.8016347440481));
#55458=CARTESIAN_POINT('Ctrl Pts',(-1.6256382048639,115.481461223343,15.3540088207721));
#55459=CARTESIAN_POINT('Ctrl Pts',(-2.54430496499387,115.735983946442,13.2862198412236));
#55460=CARTESIAN_POINT('Ctrl Pts',(-1.50310124092006,115.982628746918,11.3521388995005));
#55461=CARTESIAN_POINT('Ctrl Pts',(0.236180153310175,116.182036367951,11.051152222629));
#55462=CARTESIAN_POINT('Ctrl Pts',(1.36095280562168,116.338203952737,11.6748599396884));
#55463=CARTESIAN_POINT('Ctrl Pts',(1.91039880018758,116.453732635065,12.4476155138811));
#55464=CARTESIAN_POINT('Ctrl Pts',(2.06279366972351,116.567757542103,13.3735551461719));
#55465=CARTESIAN_POINT('Ctrl Pts',(1.79847542918091,116.680374431451,14.2604126259241));
#55466=CARTESIAN_POINT('Ctrl Pts',(1.17979853787208,116.791679755757,14.9348521268195));
#55467=CARTESIAN_POINT('Ctrl Pts',(0.337632386723327,116.901777224248,15.2667461038567));
#55468=CARTESIAN_POINT('Ctrl Pts',(-0.555414918986166,117.010790218224,
15.1973087665612));
#55469=CARTESIAN_POINT('Ctrl Pts',(-1.32234103769279,117.118784767411,14.7474799210793));
#55470=CARTESIAN_POINT('Ctrl Pts',(-1.80775797452488,117.225962200641,14.0149830105422));
#55471=CARTESIAN_POINT('Ctrl Pts',(-1.97092422810024,117.367688877029,12.8570909938671));
#55472=CARTESIAN_POINT('Ctrl Pts',(-1.15746163758973,117.543956302063,11.5274758002029));
#55473=CARTESIAN_POINT('Ctrl Pts',(0.372235631248106,117.717274790277,11.3409644660964));
#55474=CARTESIAN_POINT('Ctrl Pts',(1.35279634366171,117.85835091102,11.9701895143167));
#55475=CARTESIAN_POINT('Ctrl Pts',(1.63946046051867,117.926140628132,12.4263768287653));
#55476=CARTESIAN_POINT('Ctrl Pts',(1.74059764913481,117.963005556155,12.7174919546938));
#55477=CARTESIAN_POINT('Ctrl Pts',(2.46682853611889,110.148827126478,11.5762898043294));
#55478=CARTESIAN_POINT('Ctrl Pts',(2.99203546797916,110.264626975476,12.3415064920099));
#55479=CARTESIAN_POINT('Ctrl Pts',(3.25843192948515,110.492593339858,14.353787870894));
#55480=CARTESIAN_POINT('Ctrl Pts',(1.15008059527702,110.829525057485,16.4792175839857));
#55481=CARTESIAN_POINT('Ctrl Pts',(-1.76690846020068,111.15965328974,16.128044193202));
#55482=CARTESIAN_POINT('Ctrl Pts',(-3.09069428562109,111.44884856996,13.9338798976915));
#55483=CARTESIAN_POINT('Ctrl Pts',(-2.64792112441307,111.698505687743,11.8828823533875));
#55484=CARTESIAN_POINT('Ctrl Pts',(-1.364387090511,111.910048500832,10.6624900785378));
#55485=CARTESIAN_POINT('Ctrl Pts',(0.22560775652403,112.101620567308,10.4155318988324));
#55486=CARTESIAN_POINT('Ctrl Pts',(1.54073116051239,112.273844336496,10.9347895473236));
#55487=CARTESIAN_POINT('Ctrl Pts',(2.6872815763924,112.478483531869,12.1719261697143));
#55488=CARTESIAN_POINT('Ctrl Pts',(2.77889252277574,112.638026520578,13.5772495408711));
#55489=CARTESIAN_POINT('Ctrl Pts',(2.39223612973147,112.754241083453,14.4256655835251));
#55490=CARTESIAN_POINT('Ctrl Pts',(2.26476199794164,112.787385971573,14.6587625565873));
#55491=CARTESIAN_POINT('Ctrl Pts',(2.13063450055583,112.816309995904,14.8486316482196));
#55492=CARTESIAN_POINT('Ctrl Pts',(2.0016185710066,112.841046449208,14.9991113435169));
#55493=CARTESIAN_POINT('Ctrl Pts',(1.91194642227727,112.857522512299,15.0960249822623));
#55494=CARTESIAN_POINT('Ctrl Pts',(1.79328146006558,112.878089723521,15.2105312140984));
#55495=CARTESIAN_POINT('Ctrl Pts',(1.66654088102953,112.898619590859,15.3155646046583));
#55496=CARTESIAN_POINT('Ctrl Pts',(1.56075776911136,112.915021115362,15.3935753724432));
#55497=CARTESIAN_POINT('Ctrl Pts',(1.36174741141507,112.945063107886,15.5290360812719));
#55498=CARTESIAN_POINT('Ctrl Pts',(0.865207509480216,113.014505004717,15.7864600922824));
#55499=CARTESIAN_POINT('Ctrl Pts',(0.256010777506312,113.090196121383,15.8946003979176));
#55500=CARTESIAN_POINT('Ctrl Pts',(-0.259785089431699,113.154673519109,
15.8552288750756));
#55501=CARTESIAN_POINT('Ctrl Pts',(-0.598435642469266,113.197551777644,
15.7949356824436));
#55502=CARTESIAN_POINT('Ctrl Pts',(-1.00556611563695,113.250949337017,15.656567674988));
#55503=CARTESIAN_POINT('Ctrl Pts',(-1.44883854704915,113.31470577837,15.3974131488982));
#55504=CARTESIAN_POINT('Ctrl Pts',(-1.95617230760116,113.399287438372,14.9431569756853));
#55505=CARTESIAN_POINT('Ctrl Pts',(-2.48502734798563,113.525200413102,14.0593681219646));
#55506=CARTESIAN_POINT('Ctrl Pts',(-2.53170030021554,113.69095996749,12.6702784722711));
#55507=CARTESIAN_POINT('Ctrl Pts',(-1.69849632391851,113.874606866753,11.3742009089813));
#55508=CARTESIAN_POINT('Ctrl Pts',(-0.298732928026003,114.055469640001,
10.789850139448));
#55509=CARTESIAN_POINT('Ctrl Pts',(1.16312748155585,114.233611654871,11.0990481403683));
#55510=CARTESIAN_POINT('Ctrl Pts',(2.17562557368189,114.409112848813,12.1681746471377));
#55511=CARTESIAN_POINT('Ctrl Pts',(2.36194092480953,114.553242740846,13.3621756745578));
#55512=CARTESIAN_POINT('Ctrl Pts',(2.08943327339976,114.667328450305,14.2459096374332));
#55513=CARTESIAN_POINT('Ctrl Pts',(1.7016995736089,114.752299492816,14.8151631946314));
#55514=CARTESIAN_POINT('Ctrl Pts',(1.16513580383993,114.836691425922,15.2382255534932));
#55515=CARTESIAN_POINT('Ctrl Pts',(0.108551867838543,114.976407891281,15.6507895457554));
#55516=CARTESIAN_POINT('Ctrl Pts',(-1.55298113289362,115.169459669971,15.2450202857454));
#55517=CARTESIAN_POINT('Ctrl Pts',(-2.45397706454464,115.413280794756,13.2740017965845));
#55518=CARTESIAN_POINT('Ctrl Pts',(-1.4615503617417,115.653269049662,11.3806804618505));
#55519=CARTESIAN_POINT('Ctrl Pts',(0.256442440862655,115.85056737016,11.0643865721294));
#55520=CARTESIAN_POINT('Ctrl Pts',(1.38946688731323,116.007124891132,11.6807892864116));
#55521=CARTESIAN_POINT('Ctrl Pts',(1.95126218052327,116.123983761119,12.4582101085309));
#55522=CARTESIAN_POINT('Ctrl Pts',(2.11418980813084,116.240372536293,13.4022205649728));
#55523=CARTESIAN_POINT('Ctrl Pts',(1.848811260865,116.356379449463,14.3179598059507));
#55524=CARTESIAN_POINT('Ctrl Pts',(1.21085031354557,116.472090186163,15.0239715497253));
#55525=CARTESIAN_POINT('Ctrl Pts',(0.329812066379183,116.587595407081,15.378710756044));
#55526=CARTESIAN_POINT('Ctrl Pts',(-0.616220706596642,116.702997505549,
15.3119803645535));
#55527=CARTESIAN_POINT('Ctrl Pts',(-1.43882357083797,116.818354430523,14.8373638391765));
#55528=CARTESIAN_POINT('Ctrl Pts',(-1.96737039240484,116.933817619422,14.0514453373533));
#55529=CARTESIAN_POINT('Ctrl Pts',(-2.15291016394976,117.087869167659,12.7950288806392));
#55530=CARTESIAN_POINT('Ctrl Pts',(-1.27267889437544,117.281528367953,11.3234188443989));
#55531=CARTESIAN_POINT('Ctrl Pts',(0.436407543225603,117.475511187756,11.1026070944465));
#55532=CARTESIAN_POINT('Ctrl Pts',(1.54224885923002,117.633776918282,11.802189669093));
#55533=CARTESIAN_POINT('Ctrl Pts',(1.87412331095756,117.711599788581,12.3238494146484));
#55534=CARTESIAN_POINT('Ctrl Pts',(1.98777482999691,117.752566587265,12.6463749810985));
#55535=CARTESIAN_POINT('Ctrl Pts',(2.23096743857449,110.356711219704,11.6839477627767));
#55536=CARTESIAN_POINT('Ctrl Pts',(2.71671796362648,110.462783394457,12.3818316585855));
#55537=CARTESIAN_POINT('Ctrl Pts',(2.96814196793207,110.670600052954,14.2150346775519));
#55538=CARTESIAN_POINT('Ctrl Pts',(1.07230509703644,110.975106974938,16.1458010360037));
#55539=CARTESIAN_POINT('Ctrl Pts',(-1.54565982769012,111.271202016355,15.8454003220953));
#55540=CARTESIAN_POINT('Ctrl Pts',(-2.73726562778171,111.528883620023,13.8976000527558));
#55541=CARTESIAN_POINT('Ctrl Pts',(-2.35753144336851,111.750324357911,12.0755955690179));
#55542=CARTESIAN_POINT('Ctrl Pts',(-1.23046715661347,111.93738228624,10.9878560267602));
#55543=CARTESIAN_POINT('Ctrl Pts',(0.170478387419463,112.106359490217,10.7592627690187));
#55544=CARTESIAN_POINT('Ctrl Pts',(1.33241463923504,112.258025763899,11.2073077568512));
#55545=CARTESIAN_POINT('Ctrl Pts',(2.35003626431044,112.438052769629,12.2875864922412));
#55546=CARTESIAN_POINT('Ctrl Pts',(2.440804192382,112.578279177178,13.5222781084548));
#55547=CARTESIAN_POINT('Ctrl Pts',(2.10719666528918,112.680441212008,14.2710968938976));
#55548=CARTESIAN_POINT('Ctrl Pts',(1.99685600484262,112.709579773087,14.4770007563578));
#55549=CARTESIAN_POINT('Ctrl Pts',(1.88034144378197,112.735009255498,14.6449604107706));
#55550=CARTESIAN_POINT('Ctrl Pts',(1.76801713917526,112.756758811409,14.778258887573));
#55551=CARTESIAN_POINT('Ctrl Pts',(1.68988620802049,112.771246201861,14.8641608210362));
#55552=CARTESIAN_POINT('Ctrl Pts',(1.58638420835724,112.789332055518,14.965760696405));
#55553=CARTESIAN_POINT('Ctrl Pts',(1.47569655543498,112.807387366005,15.0591024895235));
#55554=CARTESIAN_POINT('Ctrl Pts',(1.38323104245549,112.821813133151,15.1285244612521));
#55555=CARTESIAN_POINT('Ctrl Pts',(1.20917879028598,112.848238238525,15.2491961565059));
#55556=CARTESIAN_POINT('Ctrl Pts',(0.774234079863162,112.90933029061,15.4794669486178));
#55557=CARTESIAN_POINT('Ctrl Pts',(0.238708053284494,112.975963124354,15.5793734947038));
#55558=CARTESIAN_POINT('Ctrl Pts',(-0.216076618472028,113.032767461814,
15.5486358241645));
#55559=CARTESIAN_POINT('Ctrl Pts',(-0.515019842079931,113.070553966245,
15.4980936979603));
#55560=CARTESIAN_POINT('Ctrl Pts',(-0.87512142854749,113.117636776362,15.3792172847831));
#55561=CARTESIAN_POINT('Ctrl Pts',(-1.26834740878835,113.173897564996,15.1539332939003));
#55562=CARTESIAN_POINT('Ctrl Pts',(-1.72001223012634,113.248598023361,14.7566309028774));
#55563=CARTESIAN_POINT('Ctrl Pts',(-2.19486977968014,113.359965645859,13.9790570244268));
#55564=CARTESIAN_POINT('Ctrl Pts',(-2.24785397603106,113.506997488377,12.7471516501278));
#55565=CARTESIAN_POINT('Ctrl Pts',(-1.51655361366513,113.670598494623,11.5853017785865));
#55566=CARTESIAN_POINT('Ctrl Pts',(-0.268049440467267,113.83254837515,11.0498590594206));
#55567=CARTESIAN_POINT('Ctrl Pts',(1.05167590777252,113.99301525548,11.3155545254172));
#55568=CARTESIAN_POINT('Ctrl Pts',(1.97963059763142,114.152178479358,12.2762631522508));
#55569=CARTESIAN_POINT('Ctrl Pts',(2.16066197830282,114.283884205462,13.3658254951479));
#55570=CARTESIAN_POINT('Ctrl Pts',(1.91729199582453,114.388787083235,14.1808658981726));
#55571=CARTESIAN_POINT('Ctrl Pts',(1.56383201925712,114.467258929776,14.7098214424163));
#55572=CARTESIAN_POINT('Ctrl Pts',(1.06937612553001,114.545548434972,15.106750651434));
#55573=CARTESIAN_POINT('Ctrl Pts',(0.0880674350923923,114.675769242385,
15.4999443474628));
#55574=CARTESIAN_POINT('Ctrl Pts',(-1.48032406092335,114.857458116598,15.136031750719));
#55575=CARTESIAN_POINT('Ctrl Pts',(-2.36364916409543,115.090577643069,13.2617837519454));
#55576=CARTESIAN_POINT('Ctrl Pts',(-1.41999948256334,115.323909352405,11.4092220242003));
#55577=CARTESIAN_POINT('Ctrl Pts',(0.276704728415126,115.51909837237,11.0776209216297));
#55578=CARTESIAN_POINT('Ctrl Pts',(1.41798096900478,115.676045829526,11.6867186331346));
#55579=CARTESIAN_POINT('Ctrl Pts',(1.99212556085894,115.794234887173,12.4688047031807));
#55580=CARTESIAN_POINT('Ctrl Pts',(2.16558594653818,115.912987530482,13.4308859837738));
#55581=CARTESIAN_POINT('Ctrl Pts',(1.89914709254908,116.032384467474,14.3755069859774));
#55582=CARTESIAN_POINT('Ctrl Pts',(1.24190208921908,116.15250061657,15.1130909726311));
#55583=CARTESIAN_POINT('Ctrl Pts',(0.321991746035035,116.273413589914,15.4906754082313));
#55584=CARTESIAN_POINT('Ctrl Pts',(-0.677026494207119,116.395204792873,
15.4266519625457));
#55585=CARTESIAN_POINT('Ctrl Pts',(-1.55530610398315,116.517924093635,14.9272477572735));
#55586=CARTESIAN_POINT('Ctrl Pts',(-2.12698281028479,116.641673038203,14.0879076641644));
#55587=CARTESIAN_POINT('Ctrl Pts',(-2.33489609979927,116.80804945829,12.7329667674113));
#55588=CARTESIAN_POINT('Ctrl Pts',(-1.38789615116117,117.019100433844,11.1193618885948));
#55589=CARTESIAN_POINT('Ctrl Pts',(0.5005794552031,117.233747585235,10.8642497227967));
#55590=CARTESIAN_POINT('Ctrl Pts',(1.73170137479832,117.409202925543,11.6341898238695));
#55591=CARTESIAN_POINT('Ctrl Pts',(2.10878616139645,117.49705894903,12.2213220005316));
#55592=CARTESIAN_POINT('Ctrl Pts',(2.23495201085903,117.542127618376,12.575258007503));
#55593=CARTESIAN_POINT('Ctrl Pts',(1.99510634103008,110.564595312929,11.7916057212239));
#55594=CARTESIAN_POINT('Ctrl Pts',(2.44140045927379,110.660939813437,12.4221568251609));
#55595=CARTESIAN_POINT('Ctrl Pts',(2.67785200637898,110.848606766051,14.0762814842097));
#55596=CARTESIAN_POINT('Ctrl Pts',(0.994529598795843,111.120688892391,15.8123844880218));
#55597=CARTESIAN_POINT('Ctrl Pts',(-1.32441119517955,111.38275074297,15.5627564509884));
#55598=CARTESIAN_POINT('Ctrl Pts',(-2.38383696994232,111.608918670085,13.8613202078201));
#55599=CARTESIAN_POINT('Ctrl Pts',(-2.06714176232395,111.80214302808,12.2683087846484));
#55600=CARTESIAN_POINT('Ctrl Pts',(-1.09654722271593,111.96471607165,11.3132219749825));
#55601=CARTESIAN_POINT('Ctrl Pts',(0.115349018314891,112.111098413124,11.1029936392051));
#55602=CARTESIAN_POINT('Ctrl Pts',(1.1240981179577,112.242207191303,11.4798259663788));
#55603=CARTESIAN_POINT('Ctrl Pts',(2.01279095222846,112.397622007389,12.4032468147681));
#55604=CARTESIAN_POINT('Ctrl Pts',(2.10271586198826,112.518531833778,13.4673066760386));
#55605=CARTESIAN_POINT('Ctrl Pts',(1.82215720084688,112.606641340562,14.1165282042701));
#55606=CARTESIAN_POINT('Ctrl Pts',(1.72895001174359,112.6317735746,14.2952389561282));
#55607=CARTESIAN_POINT('Ctrl Pts',(1.63004838700809,112.65370851509,14.4412891733214));
#55608=CARTESIAN_POINT('Ctrl Pts',(1.53441570734393,112.672471173608,14.557406431629));
#55609=CARTESIAN_POINT('Ctrl Pts',(1.46782599376371,112.684969891422,14.6322966598098));
#55610=CARTESIAN_POINT('Ctrl Pts',(1.37948695664889,112.700574387516,14.7209901787116));
#55611=CARTESIAN_POINT('Ctrl Pts',(1.28485222984041,112.71615514115,14.8026403743885));
#55612=CARTESIAN_POINT('Ctrl Pts',(1.20570431579963,112.72860515094,14.863473550061));
#55613=CARTESIAN_POINT('Ctrl Pts',(1.05661016915688,112.751413369165,14.9693562317397));
#55614=CARTESIAN_POINT('Ctrl Pts',(0.683260650246095,112.804155576505,15.1724738049531));
#55615=CARTESIAN_POINT('Ctrl Pts',(0.221405329062661,112.861730127325,15.26414659149));
#55616=CARTESIAN_POINT('Ctrl Pts',(-0.172368147512368,112.910861404517,
15.2420427732535));
#55617=CARTESIAN_POINT('Ctrl Pts',(-0.431604041690608,112.943556154848,
15.2012517134772));
#55618=CARTESIAN_POINT('Ctrl Pts',(-0.744676741458043,112.984324215706,
15.1018668945781));
#55619=CARTESIAN_POINT('Ctrl Pts',(-1.08785627052756,113.033089351621,14.9104534389022));
#55620=CARTESIAN_POINT('Ctrl Pts',(-1.48385215265151,113.09790860835,14.5701048300693));
#55621=CARTESIAN_POINT('Ctrl Pts',(-1.90471221137466,113.194730878618,13.898745926889));
#55622=CARTESIAN_POINT('Ctrl Pts',(-1.96400765184658,113.323035009261,12.8240248279844));
#55623=CARTESIAN_POINT('Ctrl Pts',(-1.33461090341178,113.466590122495,11.7964026481919));
#55624=CARTESIAN_POINT('Ctrl Pts',(-0.237365952908544,113.609627110298,
11.3098679793932));
#55625=CARTESIAN_POINT('Ctrl Pts',(0.940224333989188,113.752418856088,11.532060910466));
#55626=CARTESIAN_POINT('Ctrl Pts',(1.78363562158095,113.895244109902,12.3843516573639));
#55627=CARTESIAN_POINT('Ctrl Pts',(1.95938303179607,114.014525670079,13.369475315738));
#55628=CARTESIAN_POINT('Ctrl Pts',(1.7451507182493,114.110245716165,14.1158221589119));
#55629=CARTESIAN_POINT('Ctrl Pts',(1.42596446490531,114.182218366739,14.6044796902011));
#55630=CARTESIAN_POINT('Ctrl Pts',(0.973616447220085,114.254405444024,14.9752757493749));
#55631=CARTESIAN_POINT('Ctrl Pts',(0.0675830023462311,114.375130593489,
15.3490991491701));
#55632=CARTESIAN_POINT('Ctrl Pts',(-1.40766698895308,114.545456563225,15.0270432156924));
#55633=CARTESIAN_POINT('Ctrl Pts',(-2.27332126364622,114.767874491383,13.2495657073064));
#55634=CARTESIAN_POINT('Ctrl Pts',(-1.378448603385,114.994549655149,11.4377635865502));
#55635=CARTESIAN_POINT('Ctrl Pts',(0.296967015967595,115.187629374578,11.0908552711301));
#55636=CARTESIAN_POINT('Ctrl Pts',(1.44649505069631,115.34496676792,11.6926479798579));
#55637=CARTESIAN_POINT('Ctrl Pts',(2.03298894119462,115.464486013225,12.4793992978305));
#55638=CARTESIAN_POINT('Ctrl Pts',(2.21698208494551,115.585602524672,13.4595514025747));
#55639=CARTESIAN_POINT('Ctrl Pts',(1.94948292423316,115.708389485485,14.433054166004));
#55640=CARTESIAN_POINT('Ctrl Pts',(1.27295386489257,115.832911046977,15.202210395537));
#55641=CARTESIAN_POINT('Ctrl Pts',(0.314171425690885,115.959231772748,15.6026400604184));
#55642=CARTESIAN_POINT('Ctrl Pts',(-0.7378322818176,116.087412080197,15.541323560538));
#55643=CARTESIAN_POINT('Ctrl Pts',(-1.67178863712833,116.217493756747,15.0171316753708));
#55644=CARTESIAN_POINT('Ctrl Pts',(-2.28659522816475,116.349528456984,14.1243699909755));
#55645=CARTESIAN_POINT('Ctrl Pts',(-2.51688203564877,116.52822974892,12.6709046541834));
#55646=CARTESIAN_POINT('Ctrl Pts',(-1.50311340794689,116.756672499734,10.9153049327907));
#55647=CARTESIAN_POINT('Ctrl Pts',(0.564751367180597,116.991983982712,10.6258923511469));
#55648=CARTESIAN_POINT('Ctrl Pts',(1.92115389036661,117.184628932805,11.4661899786458));
#55649=CARTESIAN_POINT('Ctrl Pts',(2.34344901183535,117.282518109478,12.1187945864147));
#55650=CARTESIAN_POINT('Ctrl Pts',(2.48212919172115,117.331688649487,12.5041410339076));
#55651=CARTESIAN_POINT('Ctrl Pts',(2.02616441126019,110.570072536149,11.8332575276011));
#55652=CARTESIAN_POINT('Ctrl Pts',(2.07105841806764,110.5799782663,11.8994551216819));
#55653=CARTESIAN_POINT('Ctrl Pts',(2.11271517883406,110.589880303591,11.9677392355203));
#55654=CARTESIAN_POINT('Ctrl Pts',(2.150854785792,110.599777995315,12.0378250846901));
#55655=CARTESIAN_POINT('Ctrl Pts',(2.21680176610504,110.616892038519,12.1590101330969));
#55656=CARTESIAN_POINT('Ctrl Pts',(2.2722299692091,110.633993066787,12.2855838404137));
#55657=CARTESIAN_POINT('Ctrl Pts',(2.31677087589169,110.651078126608,12.4156052564564));
#55658=CARTESIAN_POINT('Ctrl Pts',(2.36131178257429,110.66816318643,12.5456266724991));
#55659=CARTESIAN_POINT('Ctrl Pts',(2.39496518711439,110.685232280206,12.679094248793));
#55660=CARTESIAN_POINT('Ctrl Pts',(2.41741513700149,110.702282852658,12.8140429117563));
#55661=CARTESIAN_POINT('Ctrl Pts',(2.43988375218285,110.719347601265,12.949103773478));
#55662=CARTESIAN_POINT('Ctrl Pts',(2.45113018384618,110.736393800202,13.0856466048275));
#55663=CARTESIAN_POINT('Ctrl Pts',(2.45108056364822,110.753419241551,13.2216340677291));
#55664=CARTESIAN_POINT('Ctrl Pts',(2.4510338049192,110.76946286957,13.3497794840631));
#55665=CARTESIAN_POINT('Ctrl Pts',(2.44095668751521,110.785488069839,13.4774306472446));
#55666=CARTESIAN_POINT('Ctrl Pts',(2.42083288203555,110.80149325887,13.6029010654533));
#55667=CARTESIAN_POINT('Ctrl Pts',(2.41960137626499,110.802472719871,13.6105794115899));
#55668=CARTESIAN_POINT('Ctrl Pts',(2.41833225938017,110.803452106003,13.618249599689));
#55669=CARTESIAN_POINT('Ctrl Pts',(2.41702553304493,110.804431416933,13.6259112469578));
#55670=CARTESIAN_POINT('Ctrl Pts',(2.39711608043204,110.819352325794,13.7426451024876));
#55671=CARTESIAN_POINT('Ctrl Pts',(2.36847436955913,110.834255763845,13.8573939856762));
#55672=CARTESIAN_POINT('Ctrl Pts',(2.33187245113042,110.849140695019,13.9690689169625));
#55673=CARTESIAN_POINT('Ctrl Pts',(2.29493346737928,110.864162700815,14.0817722573688));
#55674=CARTESIAN_POINT('Ctrl Pts',(2.24971683798023,110.879122738555,14.1917657288957));
#55675=CARTESIAN_POINT('Ctrl Pts',(2.19688540562185,110.894023372537,14.2978493398295));
#55676=CARTESIAN_POINT('Ctrl Pts',(2.14287094573794,110.909257668874,14.4063084273715));
#55677=CARTESIAN_POINT('Ctrl Pts',(2.08089735143869,110.924429872065,14.5106795218075));
#55678=CARTESIAN_POINT('Ctrl Pts',(2.01172744446461,110.939543288332,14.609689996179));
#55679=CARTESIAN_POINT('Ctrl Pts',(1.94246035028488,110.954677939709,14.7088395852574));
#55680=CARTESIAN_POINT('Ctrl Pts',(1.86597744060666,110.969753642001,14.8026124080882));
#55681=CARTESIAN_POINT('Ctrl Pts',(1.78308899230302,110.984774243601,14.8897563710569));
#55682=CARTESIAN_POINT('Ctrl Pts',(1.74400542036187,110.991856759624,14.9308465038273));
#55683=CARTESIAN_POINT('Ctrl Pts',(1.70349826534003,110.998927032353,14.9704633071913));
#55684=CARTESIAN_POINT('Ctrl Pts',(1.66165516189832,111.005985502709,15.0084785524507));
#55685=CARTESIAN_POINT('Ctrl Pts',(1.57189245452912,111.021127482077,15.0900296577731));
#55686=CARTESIAN_POINT('Ctrl Pts',(1.47598082711947,111.036215118535,15.1642072274403));
#55687=CARTESIAN_POINT('Ctrl Pts',(1.37535440147532,111.051253158905,15.2305278229256));
#55688=CARTESIAN_POINT('Ctrl Pts',(1.27713452752472,111.065931553971,15.2952623147571));
#55689=CARTESIAN_POINT('Ctrl Pts',(1.17442386833893,111.080562702085,15.3525109927783));
#55690=CARTESIAN_POINT('Ctrl Pts',(1.06856206414412,111.095151398066,15.4018724805979));
#55691=CARTESIAN_POINT('Ctrl Pts',(1.00819936982575,111.103469912971,15.4300185378375));
#55692=CARTESIAN_POINT('Ctrl Pts',(0.946812152352576,111.111774631939,15.4556011230402));
#55693=CARTESIAN_POINT('Ctrl Pts',(0.884647485524478,111.1200664917,15.4785533978928));
#55694=CARTESIAN_POINT('Ctrl Pts',(0.778155140070371,111.134271017184,15.5178722217082));
#55695=CARTESIAN_POINT('Ctrl Pts',(0.668870322291868,111.148439910411,15.5496459177179));
#55696=CARTESIAN_POINT('Ctrl Pts',(0.557997038053399,111.162573434211,15.573352552203));
#55697=CARTESIAN_POINT('Ctrl Pts',(0.454890603246509,111.175716882249,15.5953984993381));
#55698=CARTESIAN_POINT('Ctrl Pts',(0.350411649690433,111.188829748195,15.6104681156522));
#55699=CARTESIAN_POINT('Ctrl Pts',(0.245551686144082,111.201912534831,15.6181747144393));
#55700=CARTESIAN_POINT('Ctrl Pts',(0.132554486325984,111.216010558572,15.6264793528695));
#55701=CARTESIAN_POINT('Ctrl Pts',(0.0191157451671066,111.230073651892,
15.6262326699005));
#55702=CARTESIAN_POINT('Ctrl Pts',(-0.0934940464264922,111.244102823594,
15.6177560420854));
#55703=CARTESIAN_POINT('Ctrl Pts',(-0.207107639837214,111.2582570511,15.6092038537503));
#55704=CARTESIAN_POINT('Ctrl Pts',(-0.319876196950842,111.272376752,15.5922746446226));
#55705=CARTESIAN_POINT('Ctrl Pts',(-0.430499467262996,111.286463273381,
15.5673513736807));
#55706=CARTESIAN_POINT('Ctrl Pts',(-0.538949137192655,111.30027301332,15.5429178119211));
#55707=CARTESIAN_POINT('Ctrl Pts',(-0.645335908803491,111.314050868474,
15.5108017573914));
#55708=CARTESIAN_POINT('Ctrl Pts',(-0.748456234475894,111.327798357861,
15.4714082566281));
#55709=CARTESIAN_POINT('Ctrl Pts',(-0.792969010146538,111.333732579919,
15.4544037131405));
#55710=CARTESIAN_POINT('Ctrl Pts',(-0.836873522602974,111.339661146824,
15.4360436907805));
#55711=CARTESIAN_POINT('Ctrl Pts',(-0.880075005513976,111.345584192991,
15.4163630345393));
#55712=CARTESIAN_POINT('Ctrl Pts',(-0.967742555981023,111.357603663475,
15.3764256340614));
#55713=CARTESIAN_POINT('Ctrl Pts',(-1.05251344069536,111.369600393746,15.3310492160238));
#55714=CARTESIAN_POINT('Ctrl Pts',(-1.13381079222952,111.381575608866,15.2808146713564));
#55715=CARTESIAN_POINT('Ctrl Pts',(-1.23687530433488,111.396757157592,15.2171299542127));
#55716=CARTESIAN_POINT('Ctrl Pts',(-1.33483881624213,111.411901639041,15.1453343047575));
#55717=CARTESIAN_POINT('Ctrl Pts',(-1.42644767653091,111.427007716472,15.0664071530192));
#55718=CARTESIAN_POINT('Ctrl Pts',(-1.52183861320501,111.442737449066,14.9842214898682));
#55719=CARTESIAN_POINT('Ctrl Pts',(-1.61033830423551,111.458425541663,14.8943038098277));
#55720=CARTESIAN_POINT('Ctrl Pts',(-1.69054419706743,111.474070759423,14.7978142078287));
#55721=CARTESIAN_POINT('Ctrl Pts',(-1.71359526602133,111.478567174595,14.7700832221058));
#55722=CARTESIAN_POINT('Ctrl Pts',(-1.73596141980438,111.483060050031,14.7418097120366));
#55723=CARTESIAN_POINT('Ctrl Pts',(-1.75760974856578,111.487549360252,14.7130219020379));
#55724=CARTESIAN_POINT('Ctrl Pts',(-1.83337735574986,111.503261625946,14.6122666195535));
#55725=CARTESIAN_POINT('Ctrl Pts',(-1.900348686991,111.518930202763,14.5052088222496));
#55726=CARTESIAN_POINT('Ctrl Pts',(-1.95788793805633,111.534554187242,14.3936106861671));
#55727=CARTESIAN_POINT('Ctrl Pts',(-2.01516628970205,111.550107328108,14.2825185679489));
#55728=CARTESIAN_POINT('Ctrl Pts',(-2.06309747735693,111.565616282983,14.1669285606128));
#55729=CARTESIAN_POINT('Ctrl Pts',(-2.10109971794726,111.581080353661,14.0486007782592));
#55730=CARTESIAN_POINT('Ctrl Pts',(-2.13867283810188,111.596369804405,13.9316091505303));
#55731=CARTESIAN_POINT('Ctrl Pts',(-2.16653964038307,111.611615381789,13.8119425199339));
#55732=CARTESIAN_POINT('Ctrl Pts',(-2.18418791701896,111.626816556935,13.6913036358071));
#55733=CARTESIAN_POINT('Ctrl Pts',(-2.18759336745963,111.629749809267,13.6680248902622));
#55734=CARTESIAN_POINT('Ctrl Pts',(-2.19061849851063,111.632681408674,13.6447099149796));
#55735=CARTESIAN_POINT('Ctrl Pts',(-2.19326586556019,111.635611352551,13.62137083067));
#55736=CARTESIAN_POINT('Ctrl Pts',(-2.20853875159818,111.652514448384,13.4867256650321));
#55737=CARTESIAN_POINT('Ctrl Pts',(-2.21127460479025,111.669401214344,13.3509280781189));
#55738=CARTESIAN_POINT('Ctrl Pts',(-2.20180594533087,111.686258620309,13.2162593571699));
#55739=CARTESIAN_POINT('Ctrl Pts',(-2.19192191780219,111.703855521469,13.0756830326308));
#55740=CARTESIAN_POINT('Ctrl Pts',(-2.16873902135966,111.721420426645,12.9363382358816));
#55741=CARTESIAN_POINT('Ctrl Pts',(-2.13268966365534,111.738938750505,12.8008348741085));
#55742=CARTESIAN_POINT('Ctrl Pts',(-2.11529365920093,111.747392405697,12.7354462726159));
#55743=CARTESIAN_POINT('Ctrl Pts',(-2.09490230517816,111.755835217512,12.6709522842583));
#55744=CARTESIAN_POINT('Ctrl Pts',(-2.07156848851267,111.764265569171,12.6076457448401));
#55745=CARTESIAN_POINT('Ctrl Pts',(-2.03725839797215,111.776661575057,12.5145596830789));
#55746=CARTESIAN_POINT('Ctrl Pts',(-1.99658601558772,111.789030637564,12.4240413943406));
#55747=CARTESIAN_POINT('Ctrl Pts',(-1.95009563404642,111.801367552442,12.3368816460376));
#55748=CARTESIAN_POINT('Ctrl Pts',(-1.91126430847799,111.811672022791,12.2640810268427));
#55749=CARTESIAN_POINT('Ctrl Pts',(-1.86836584858189,111.821954361973,12.1936062082923));
#55750=CARTESIAN_POINT('Ctrl Pts',(-1.82171032815555,111.832216330656,12.1259096426039));
#55751=CARTESIAN_POINT('Ctrl Pts',(-1.71916930753833,111.854770419276,11.9771239281903));
#55752=CARTESIAN_POINT('Ctrl Pts',(-1.5984785936281,111.877226132562,11.8417605416273));
#55753=CARTESIAN_POINT('Ctrl Pts',(-1.46349508310159,111.899604249647,11.7238186713924));
#55754=CARTESIAN_POINT('Ctrl Pts',(-1.33345583594095,111.921162686579,11.6101968522957));
#55755=CARTESIAN_POINT('Ctrl Pts',(-1.19015285597994,111.942649116998,11.5127440729284));
#55756=CARTESIAN_POINT('Ctrl Pts',(-1.03799495393243,111.964078910758,11.4339687121288));
#55757=CARTESIAN_POINT('Ctrl Pts',(-1.03212606544161,111.964905480185,11.4309302645547));
#55758=CARTESIAN_POINT('Ctrl Pts',(-1.02624347565069,111.965731969523,11.4279193094611));
#55759=CARTESIAN_POINT('Ctrl Pts',(-1.02034743996064,111.966558377551,11.424936009145));
#55760=CARTESIAN_POINT('Ctrl Pts',(-0.914279455406906,111.981425220029,
11.3712672953711));
#55761=CARTESIAN_POINT('Ctrl Pts',(-0.803856893658385,111.996265733511,
11.3265518361342));
#55762=CARTESIAN_POINT('Ctrl Pts',(-0.690702167200723,112.01107401304,11.2913328576768));
#55763=CARTESIAN_POINT('Ctrl Pts',(-0.63469380078121,112.018403689597,11.273900466542));
#55764=CARTESIAN_POINT('Ctrl Pts',(-0.57801663387521,112.025725471586,11.2587940617592));
#55765=CARTESIAN_POINT('Ctrl Pts',(-0.520869988068662,112.033038657505,
11.2460756243719));
#55766=CARTESIAN_POINT('Ctrl Pts',(-0.434661659822516,112.044070932863,
11.2268892800188));
#55767=CARTESIAN_POINT('Ctrl Pts',(-0.347384900232451,112.055083644211,
11.2131379985066));
#55768=CARTESIAN_POINT('Ctrl Pts',(-0.259754285009278,112.066074050324,
11.2048613130971));
#55769=CARTESIAN_POINT('Ctrl Pts',(-0.172104732923932,112.077066831449,
11.1965828391066));
#55770=CARTESIAN_POINT('Ctrl Pts',(-0.0841014946280306,112.088037297831,
11.1937813409176));
#55771=CARTESIAN_POINT('Ctrl Pts',(0.0035241847171541,112.098982505872,
11.1964691503483));
#55772=CARTESIAN_POINT('Ctrl Pts',(0.070833532300197,112.107390027706,11.1985337814081));
#55773=CARTESIAN_POINT('Ctrl Pts',(0.137920067271792,112.115782646876,11.2038370278667));
#55774=CARTESIAN_POINT('Ctrl Pts',(0.204476565983255,112.124159351449,11.2123021908646));
#55775=CARTESIAN_POINT('Ctrl Pts',(0.311391191145362,112.137615471391,11.2259004081141));
#55776=CARTESIAN_POINT('Ctrl Pts',(0.41701049350247,112.151091212913,11.2476786332973));
#55777=CARTESIAN_POINT('Ctrl Pts',(0.52015968341684,112.164555091108,11.277359160353));
#55778=CARTESIAN_POINT('Ctrl Pts',(0.641972232071245,112.180455063944,11.3124099508543));
#55779=CARTESIAN_POINT('Ctrl Pts',(0.760341260980355,112.196338439093,11.3584803657846));
#55780=CARTESIAN_POINT('Ctrl Pts',(0.873367208190062,112.212153314227,11.414744343162));
#55781=CARTESIAN_POINT('Ctrl Pts',(0.915519447094673,112.218051361634,11.4357276012074));
#55782=CARTESIAN_POINT('Ctrl Pts',(0.956928340724595,112.22393989858,11.4581291137113));
#55783=CARTESIAN_POINT('Ctrl Pts',(0.997494416208606,112.229816296784,11.4819076757352));
#55784=CARTESIAN_POINT('Ctrl Pts',(1.02723895372284,112.234125087928,11.4993429913707));
#55785=CARTESIAN_POINT('Ctrl Pts',(1.05653034425799,112.238427353575,11.5175186823741));
#55786=CARTESIAN_POINT('Ctrl Pts',(1.0853496526665,112.24272208655,11.5364004717887));
#55787=CARTESIAN_POINT('Ctrl Pts',(1.12874878866787,112.24918954572,11.5648346498451));
#55788=CARTESIAN_POINT('Ctrl Pts',(1.17108400605649,112.255635802411,11.5948729432256));
#55789=CARTESIAN_POINT('Ctrl Pts',(1.21226984262544,112.262062150019,11.6263868296338));
#55790=CARTESIAN_POINT('Ctrl Pts',(1.28075499720787,112.27274809077,11.6787891495076));
#55791=CARTESIAN_POINT('Ctrl Pts',(1.34606065426729,112.283378992512,11.7352730013004));
#55792=CARTESIAN_POINT('Ctrl Pts',(1.40709547802075,112.293960799461,11.7956640737622));
#55793=CARTESIAN_POINT('Ctrl Pts',(1.47358143037869,112.305487686398,11.8614487802562));
#55794=CARTESIAN_POINT('Ctrl Pts',(1.53499864940514,112.316956325139,11.9318693556024));
#55795=CARTESIAN_POINT('Ctrl Pts',(1.59110341104185,112.328373946553,12.0059858413882));
#55796=CARTESIAN_POINT('Ctrl Pts',(1.6400490793677,112.338334653889,12.070644897499));
#55797=CARTESIAN_POINT('Ctrl Pts',(1.68495205813288,112.348256530576,12.1381157758824));
#55798=CARTESIAN_POINT('Ctrl Pts',(1.72568000847627,112.35814416662,12.2077610316259));
#55799=CARTESIAN_POINT('Ctrl Pts',(1.79993921911069,112.376172278554,12.3347451217247));
#55800=CARTESIAN_POINT('Ctrl Pts',(1.86059771124178,112.394452726721,12.4696551328169));
#55801=CARTESIAN_POINT('Ctrl Pts',(1.90679617182559,112.412832166683,12.6090877257604));
#55802=CARTESIAN_POINT('Ctrl Pts',(1.95492570256377,112.431979857092,12.7543485241327));
#55803=CARTESIAN_POINT('Ctrl Pts',(1.98736213974189,112.451234856573,12.904514998465));
#55804=CARTESIAN_POINT('Ctrl Pts',(2.00319042751117,112.470431295237,13.0557422024043));
#55805=CARTESIAN_POINT('Ctrl Pts',(2.01850854964172,112.48900900852,13.2020951632027));
#55806=CARTESIAN_POINT('Ctrl Pts',(2.01827389738594,112.50753184538,13.3494399658853));
#55807=CARTESIAN_POINT('Ctrl Pts',(2.00168493092275,112.525857411218,13.4943278262554));
#55808=CARTESIAN_POINT('Ctrl Pts',(1.99504403705843,112.533193500419,13.5523293241235));
#55809=CARTESIAN_POINT('Ctrl Pts',(1.98578241830288,112.540498069348,13.6099376212333));
#55810=CARTESIAN_POINT('Ctrl Pts',(1.97384878709611,112.547762372644,13.6669338487352));
#55811=CARTESIAN_POINT('Ctrl Pts',(1.95170130268851,112.561244106845,13.7727124703485));
#55812=CARTESIAN_POINT('Ctrl Pts',(1.92035116401533,112.57458697814,13.8763818579387));
#55813=CARTESIAN_POINT('Ctrl Pts',(1.88079178001759,112.587737377759,13.9768971580619));
#55814=CARTESIAN_POINT('Ctrl Pts',(1.86229565658681,112.593885891461,14.0238934256951));
#55815=CARTESIAN_POINT('Ctrl Pts',(1.84199429112812,112.600024904622,14.0701690994365));
#55816=CARTESIAN_POINT('Ctrl Pts',(1.82003100565933,112.606132195475,14.1155636062622));
#55817=CARTESIAN_POINT('Ctrl Pts',(1.79806772019048,112.612239486328,14.160958113088));
#55818=CARTESIAN_POINT('Ctrl Pts',(1.77444697332014,112.618315383671,14.2054667607652));
#55819=CARTESIAN_POINT('Ctrl Pts',(1.7492409607065,112.624417619916,14.2489991213253));
#55820=CARTESIAN_POINT('Ctrl Pts',(1.69882893547932,112.636622092406,14.3360638424454));
#55821=CARTESIAN_POINT('Ctrl Pts',(1.64207244780588,112.648932109483,14.4192317980716));
#55822=CARTESIAN_POINT('Ctrl Pts',(1.57976552279001,112.661382636358,14.4977141891418));
#55823=CARTESIAN_POINT('Ctrl Pts',(1.56418879153601,112.664495268077,14.5173347869093));
#55824=CARTESIAN_POINT('Ctrl Pts',(1.54826497583986,112.667616660155,14.5366624552061));
#55825=CARTESIAN_POINT('Ctrl Pts',(1.53200277927876,112.670748758568,14.5556873852558));
#55826=CARTESIAN_POINT('Ctrl Pts',(1.51574058271771,112.673880856982,14.5747123153055));
#55827=CARTESIAN_POINT('Ctrl Pts',(1.49913994586673,112.677023645936,14.5934345229931));
#55828=CARTESIAN_POINT('Ctrl Pts',(1.48221260175302,112.680176475423,14.6118418109419));
#55829=CARTESIAN_POINT('Ctrl Pts',(1.44835791352547,112.686482134398,14.6486563868397));
#55830=CARTESIAN_POINT('Ctrl Pts',(1.41319659887146,112.69282812446,14.6842116298549));
#55831=CARTESIAN_POINT('Ctrl Pts',(1.37681223588142,112.699211097522,14.7184142822241));
#55832=CARTESIAN_POINT('Ctrl Pts',(1.34042787289152,112.705594070583,14.7526169345931));
#55833=CARTESIAN_POINT('Ctrl Pts',(1.30282015964494,112.712014031624,14.7854671449969));
#55834=CARTESIAN_POINT('Ctrl Pts',(1.26407541691761,112.718458396915,14.8168681460656));
#55835=CARTESIAN_POINT('Ctrl Pts',(1.24470304555387,112.721680579561,14.8325686465999));
#55836=CARTESIAN_POINT('Ctrl Pts',(1.2250464318216,112.724908824614,14.8479067314702));
#55837=CARTESIAN_POINT('Ctrl Pts',(1.20511700835775,112.728141268808,14.8628693722048));
#55838=CARTESIAN_POINT('Ctrl Pts',(1.1851875848939,112.731373713001,14.8778320129395));
#55839=CARTESIAN_POINT('Ctrl Pts',(1.16498534336991,112.734610366165,14.8924192263057));
#55840=CARTESIAN_POINT('Ctrl Pts',(1.14452107077328,112.737848258061,14.9066191521569));
#55841=CARTESIAN_POINT('Ctrl Pts',(1.07551966046412,112.748765778155,14.9544984454665));
#55842=CARTESIAN_POINT('Ctrl Pts',(1.00351907227778,112.759699351886,14.9979865816682));
#55843=CARTESIAN_POINT('Ctrl Pts',(0.929049646054122,112.770470348169,15.0365818477437));
#55844=CARTESIAN_POINT('Ctrl Pts',(0.885727266263003,112.77673634504,15.059034535509));
#55845=CARTESIAN_POINT('Ctrl Pts',(0.841568966091264,112.782947462598,15.0798321837866));
#55846=CARTESIAN_POINT('Ctrl Pts',(0.796674188449058,112.789069756842,15.0988824177858));
#55847=CARTESIAN_POINT('Ctrl Pts',(0.776887372027841,112.791768082095,15.1072785721432));
#55848=CARTESIAN_POINT('Ctrl Pts',(0.756966200111399,112.794453444134,15.1153273887977));
#55849=CARTESIAN_POINT('Ctrl Pts',(0.736918996296125,112.797127253964,15.1230191201535));
#55850=CARTESIAN_POINT('Ctrl Pts',(0.645860534818585,112.809272239949,15.1579565223873));
#55851=CARTESIAN_POINT('Ctrl Pts',(0.552198065392748,112.821179417709,15.1855252225106));
#55852=CARTESIAN_POINT('Ctrl Pts',(0.45708651516146,112.832977001361,15.2058637026304));
#55853=CARTESIAN_POINT('Ctrl Pts',(0.363501094122257,112.844585284799,15.2258758380722));
#55854=CARTESIAN_POINT('Ctrl Pts',(0.268513439141321,112.856087470962,15.238886823475));
#55855=CARTESIAN_POINT('Ctrl Pts',(0.173264500148235,112.867599127254,15.2450567386434));
#55856=CARTESIAN_POINT('Ctrl Pts',(0.123678453456399,112.873592028933,15.2482687607914));
#55857=CARTESIAN_POINT('Ctrl Pts',(0.0740222107504112,112.879587387402,
15.2496272954867));
#55858=CARTESIAN_POINT('Ctrl Pts',(0.0244600145184373,112.885600776115,
15.2491594789169));
#55859=CARTESIAN_POINT('Ctrl Pts',(-0.0412455943053918,112.893572847501,
15.2485392850015));
#55860=CARTESIAN_POINT('Ctrl Pts',(-0.106844975386639,112.901622991693,
15.2446804600296));
#55861=CARTESIAN_POINT('Ctrl Pts',(-0.172029570959803,112.909741286633,
15.2376655680879));
#55862=CARTESIAN_POINT('Ctrl Pts',(-0.237214166532639,112.917859581573,
15.2306506761462));
#55863=CARTESIAN_POINT('Ctrl Pts',(-0.301982877658334,112.926046223778,
15.2204802566568));
#55864=CARTESIAN_POINT('Ctrl Pts',(-0.366044349703285,112.934319107027,
15.2071971382874));
#55865=CARTESIAN_POINT('Ctrl Pts',(-0.4498680025377,112.945144073599,15.1898163403256));
#55866=CARTESIAN_POINT('Ctrl Pts',(-0.532491721702338,112.9561206548,15.1671022838396));
#55867=CARTESIAN_POINT('Ctrl Pts',(-0.613238339944968,112.967172236378,
15.1391944730737));
#55868=CARTESIAN_POINT('Ctrl Pts',(-0.655911473821721,112.973012798255,
15.1244456975716));
#55869=CARTESIAN_POINT('Ctrl Pts',(-0.698060521253093,112.978874378959,
15.1082455289309));
#55870=CARTESIAN_POINT('Ctrl Pts',(-0.739585621711384,112.984746166875,
15.0906086159743));
#55871=CARTESIAN_POINT('Ctrl Pts',(-0.805721120318868,112.994097947298,
15.0625189540733));
#55872=CARTESIAN_POINT('Ctrl Pts',(-0.870421140646448,113.003273205557,
15.0309142321559));
#55873=CARTESIAN_POINT('Ctrl Pts',(-0.933111481160008,113.012360497,14.995775707463));
#55874=CARTESIAN_POINT('Ctrl Pts',(-0.984264268635237,113.019775360025,
14.9671040896176));
#55875=CARTESIAN_POINT('Ctrl Pts',(-1.03407813945666,113.027131583293,14.9360802842284));
#55876=CARTESIAN_POINT('Ctrl Pts',(-1.0822286157556,113.034475136326,14.9027164917897));
#55877=CARTESIAN_POINT('Ctrl Pts',(-1.09551238897994,113.03650107876,14.8935120749962));
#55878=CARTESIAN_POINT('Ctrl Pts',(-1.10866659778872,113.038526765791,14.884130539298));
#55879=CARTESIAN_POINT('Ctrl Pts',(-1.12168576942057,113.040551140475,14.8745739213863));
#55880=CARTESIAN_POINT('Ctrl Pts',(-1.18082309055915,113.04974651013,14.8311646478608));
#55881=CARTESIAN_POINT('Ctrl Pts',(-1.23717002182144,113.058914423756,14.7841428010402));
#55882=CARTESIAN_POINT('Ctrl Pts',(-1.29056167062862,113.067958734826,14.7340613357618));
#55883=CARTESIAN_POINT('Ctrl Pts',(-1.32023833118964,113.072985830928,14.7062245732967));
#55884=CARTESIAN_POINT('Ctrl Pts',(-1.34900291901271,113.077974825316,14.6774426155162));
#55885=CARTESIAN_POINT('Ctrl Pts',(-1.37683398123715,113.082909852143,14.6478095523937));
#55886=CARTESIAN_POINT('Ctrl Pts',(-1.43576652310271,113.093359818902,14.5850612562996));
#55887=CARTESIAN_POINT('Ctrl Pts',(-1.49037860544055,113.103700466767,14.518454453204));
#55888=CARTESIAN_POINT('Ctrl Pts',(-1.5403799994995,113.11404766848,14.4486413038854));
#55889=CARTESIAN_POINT('Ctrl Pts',(-1.59082828366944,113.124487348857,14.3782041958426));
#55890=CARTESIAN_POINT('Ctrl Pts',(-1.63658247480435,113.134933726513,14.3045016220919));
#55891=CARTESIAN_POINT('Ctrl Pts',(-1.67729431638225,113.145498604884,14.2282170002687));
#55892=CARTESIAN_POINT('Ctrl Pts',(-1.71800615796016,113.156063483255,14.1519323784454));
#55893=CARTESIAN_POINT('Ctrl Pts',(-1.75367481419996,113.166746881571,14.0730644726455));
#55894=CARTESIAN_POINT('Ctrl Pts',(-1.78391312089489,113.177653109242,13.9923311803759));
#55895=CARTESIAN_POINT('Ctrl Pts',(-1.81639568597374,113.189368786766,13.9056059398844));
#55896=CARTESIAN_POINT('Ctrl Pts',(-1.84294959853395,113.201151265024,13.8164938284703));
#55897=CARTESIAN_POINT('Ctrl Pts',(-1.86312229070193,113.212953778618,13.7259876268165));
#55898=CARTESIAN_POINT('Ctrl Pts',(-1.88328780697174,113.224752093781,13.6355136203343));
#55899=CARTESIAN_POINT('Ctrl Pts',(-1.89707654058327,113.236570421787,13.5436479245573));
#55900=CARTESIAN_POINT('Ctrl Pts',(-1.90408663867269,113.248364731642,13.4513914373198));
#55901=CARTESIAN_POINT('Ctrl Pts',(-1.9103535641621,113.2589086727,13.3689154827672));
#55902=CARTESIAN_POINT('Ctrl Pts',(-1.91120360612133,113.269433451235,13.2861279371684));
#55903=CARTESIAN_POINT('Ctrl Pts',(-1.90638424863131,113.279909496623,13.2037368741416));
#55904=CARTESIAN_POINT('Ctrl Pts',(-1.90101550237794,113.291579772079,13.1119535374928));
#55905=CARTESIAN_POINT('Ctrl Pts',(-1.88861111438651,113.303189521236,13.0206636313188));
#55906=CARTESIAN_POINT('Ctrl Pts',(-1.8696893135162,113.314700554774,12.930815106266));
#55907=CARTESIAN_POINT('Ctrl Pts',(-1.86421797282472,113.318029032155,12.9048349210521));
#55908=CARTESIAN_POINT('Ctrl Pts',(-1.85820194747901,113.321349274027,12.8789750215176));
#55909=CARTESIAN_POINT('Ctrl Pts',(-1.85165429717006,113.324660401611,12.8532577127581));
#55910=CARTESIAN_POINT('Ctrl Pts',(-1.8139098913597,113.343747637085,12.7050084183747));
#55911=CARTESIAN_POINT('Ctrl Pts',(-1.75815042366791,113.362808373553,12.5612993295427));
#55912=CARTESIAN_POINT('Ctrl Pts',(-1.68647983649764,113.381817099869,12.4262346560924));
#55913=CARTESIAN_POINT('Ctrl Pts',(-1.61509127707076,113.400751025792,12.291701469638));
#55914=CARTESIAN_POINT('Ctrl Pts',(-1.52791766723889,113.419633337063,12.1657437558088));
#55915=CARTESIAN_POINT('Ctrl Pts',(-1.42700095731129,113.438443549802,12.0523818342241));
#55916=CARTESIAN_POINT('Ctrl Pts',(-1.3742256782145,113.448280515631,11.9930982224727));
#55917=CARTESIAN_POINT('Ctrl Pts',(-1.31769115211554,113.458097843159,11.9372588477645));
#55918=CARTESIAN_POINT('Ctrl Pts',(-1.25793332652008,113.467893141606,11.8851505147714));
#55919=CARTESIAN_POINT('Ctrl Pts',(-1.17824342337142,113.480955638053,11.8156615738991));
#55920=CARTESIAN_POINT('Ctrl Pts',(-1.09267156863032,113.494102139066,11.752899313121));
#55921=CARTESIAN_POINT('Ctrl Pts',(-1.00257765073903,113.507273859013,11.6975680362558));
#55922=CARTESIAN_POINT('Ctrl Pts',(-0.912702867067373,113.520413541564,
11.6423713409079));
#55923=CARTESIAN_POINT('Ctrl Pts',(-0.818329378978895,113.53357830804,11.594568740537));
#55924=CARTESIAN_POINT('Ctrl Pts',(-0.72078335804855,113.546715920029,11.5548141484263));
#55925=CARTESIAN_POINT('Ctrl Pts',(-0.624393699727143,113.559697791752,
11.5155308284743));
#55926=CARTESIAN_POINT('Ctrl Pts',(-0.524907134494272,113.57265314922,11.4841048235255));
#55927=CARTESIAN_POINT('Ctrl Pts',(-0.423563428596022,113.585537647891,
11.4611363065296));
#55928=CARTESIAN_POINT('Ctrl Pts',(-0.397189752790417,113.588890708527,
11.4551589819823));
#55929=CARTESIAN_POINT('Ctrl Pts',(-0.370690056589949,113.592239002449,
11.4497543218409));
#55930=CARTESIAN_POINT('Ctrl Pts',(-0.344085649406526,113.595581816386,
11.4449326952993));
#55931=CARTESIAN_POINT('Ctrl Pts',(-0.304309169060675,113.600579686549,
11.4377238395618));
#55932=CARTESIAN_POINT('Ctrl Pts',(-0.264298682867311,113.605565300418,
11.4318182612747));
#55933=CARTESIAN_POINT('Ctrl Pts',(-0.224135251006277,113.61053639555,11.4271969543473));
#55934=CARTESIAN_POINT('Ctrl Pts',(-0.101602384479631,113.625702493368,
11.4130980101415));
#55935=CARTESIAN_POINT('Ctrl Pts',(0.0223203186210237,113.640935225879,
11.411305960043));
#55936=CARTESIAN_POINT('Ctrl Pts',(0.145279970667435,113.656210437031,11.4213565568666));
#55937=CARTESIAN_POINT('Ctrl Pts',(0.273664818503302,113.672159617327,11.4318506036729));
#55938=CARTESIAN_POINT('Ctrl Pts',(0.40100068878535,113.68815506243,11.4552540383412));
#55939=CARTESIAN_POINT('Ctrl Pts',(0.524656749220729,113.704174053909,11.4910735016288));
#55940=CARTESIAN_POINT('Ctrl Pts',(0.648312809656087,113.720193045389,11.5268929649164));
#55941=CARTESIAN_POINT('Ctrl Pts',(0.768290962354242,113.736235570847,11.5751273944758));
#55942=CARTESIAN_POINT('Ctrl Pts',(0.881984751217859,113.752283974349,11.6353358343203));
#55943=CARTESIAN_POINT('Ctrl Pts',(0.882892274744216,113.752412075487,11.6358164285215));
#55944=CARTESIAN_POINT('Ctrl Pts',(0.883799397894364,113.752540177027,11.6362977859758));
#55945=CARTESIAN_POINT('Ctrl Pts',(0.884706119714493,113.752668278962,11.6367799057436));
#55946=CARTESIAN_POINT('Ctrl Pts',(1.0015731765502,113.769179292267,11.6989201532376));
#55947=CARTESIAN_POINT('Ctrl Pts',(1.11180876568798,113.785647483982,11.7736386330667));
#55948=CARTESIAN_POINT('Ctrl Pts',(1.21324751846698,113.802093628618,11.8589369614855));
#55949=CARTESIAN_POINT('Ctrl Pts',(1.31494598569875,113.818581880449,11.9444536798991));
#55950=CARTESIAN_POINT('Ctrl Pts',(1.40780070899976,113.835047985294,12.040604518117));
#55951=CARTESIAN_POINT('Ctrl Pts',(1.489625666257,113.851508552278,12.1453250436702));
#55952=CARTESIAN_POINT('Ctrl Pts',(1.52019706814189,113.85765854154,12.1844506769683));
#55953=CARTESIAN_POINT('Ctrl Pts',(1.54922891015762,113.863807713567,12.2247720616797));
#55954=CARTESIAN_POINT('Ctrl Pts',(1.57660788908141,113.869956774867,12.2661797750255));
#55955=CARTESIAN_POINT('Ctrl Pts',(1.61355739161657,113.878255285806,12.3220618593612));
#55956=CARTESIAN_POINT('Ctrl Pts',(1.6474964294779,113.886553606289,12.379922545847));
#55957=CARTESIAN_POINT('Ctrl Pts',(1.6782919101032,113.8948532276,12.4394029605775));
#55958=CARTESIAN_POINT('Ctrl Pts',(1.73060015251952,113.908950705369,12.5404345369508));
#55959=CARTESIAN_POINT('Ctrl Pts',(1.77385041320905,113.923098873948,12.6463124511045));
#55960=CARTESIAN_POINT('Ctrl Pts',(1.80738463447079,113.937272366587,12.7552379913748));
#55961=CARTESIAN_POINT('Ctrl Pts',(1.84108649701919,113.951516714085,12.8647080624866));
#55962=CARTESIAN_POINT('Ctrl Pts',(1.86497526047677,113.965786630972,12.9772547645406));
#55963=CARTESIAN_POINT('Ctrl Pts',(1.87843343938246,113.980060002704,13.09106124097));
#55964=CARTESIAN_POINT('Ctrl Pts',(1.88092944207235,113.982707194013,13.1121682030104));
#55965=CARTESIAN_POINT('Ctrl Pts',(1.88306679711195,113.985354514367,13.1333185578355));
#55966=CARTESIAN_POINT('Ctrl Pts',(1.88484173947483,113.988001836676,13.1545008107529));
#55967=CARTESIAN_POINT('Ctrl Pts',(1.89437491676183,114.002220547905,13.2682702359599));
#55968=CARTESIAN_POINT('Ctrl Pts',(1.89345088064779,114.016439019261,13.3829565767269));
#55969=CARTESIAN_POINT('Ctrl Pts',(1.88243167837123,114.030639723897,13.4966779852143));
#55970=CARTESIAN_POINT('Ctrl Pts',(1.88061871925501,114.032976126867,13.5153882565255));
#55971=CARTESIAN_POINT('Ctrl Pts',(1.87853255565419,114.035312057001,13.5340725027145));
#55972=CARTESIAN_POINT('Ctrl Pts',(1.87617486875342,114.037647445818,13.55272246098));
#55973=CARTESIAN_POINT('Ctrl Pts',(1.86655495834301,114.047176374865,13.6288186243906));
#55974=CARTESIAN_POINT('Ctrl Pts',(1.85221077682933,114.056768339644,13.7043762570556));
#55975=CARTESIAN_POINT('Ctrl Pts',(1.83333831805893,114.066383332898,13.7788221911929));
#55976=CARTESIAN_POINT('Ctrl Pts',(1.81450602722814,114.075977861702,13.8531096753993));
#55977=CARTESIAN_POINT('Ctrl Pts',(1.79116575510658,114.085595317157,13.9262903578577));
#55978=CARTESIAN_POINT('Ctrl Pts',(1.76350377931296,114.095202596919,13.9978452840769));
#55979=CARTESIAN_POINT('Ctrl Pts',(1.75224022547414,114.099114541375,14.0269814083334));
#55980=CARTESIAN_POINT('Ctrl Pts',(1.74025994822911,114.103024875785,14.0558485498393));
#55981=CARTESIAN_POINT('Ctrl Pts',(1.72757452580162,114.10693168425,14.0844139255362));
#55982=CARTESIAN_POINT('Ctrl Pts',(1.7246540013776,114.107831136327,14.0909904410508));
#55983=CARTESIAN_POINT('Ctrl Pts',(1.72169609805543,114.108730402288,14.0975509668185));
#55984=CARTESIAN_POINT('Ctrl Pts',(1.71870115960148,114.109629460138,14.1040952011984));
#55985=CARTESIAN_POINT('Ctrl Pts',(1.68460319538879,114.119865410846,14.1786025986353));
#55986=CARTESIAN_POINT('Ctrl Pts',(1.64570302328899,114.130075418171,14.2509379872603));
#55987=CARTESIAN_POINT('Ctrl Pts',(1.60231893835089,114.140291869123,14.3205285350877));
#55988=CARTESIAN_POINT('Ctrl Pts',(1.55908196278321,114.150473677518,14.3898831110905));
#55989=CARTESIAN_POINT('Ctrl Pts',(1.51139041367417,114.160661886031,14.4565108632169));
#55990=CARTESIAN_POINT('Ctrl Pts',(1.45958440528606,114.170881855668,14.5198003353242));
#55991=CARTESIAN_POINT('Ctrl Pts',(1.44146294455037,114.174456745614,14.5419386493819));
#55992=CARTESIAN_POINT('Ctrl Pts',(1.42283834826223,114.178035461616,14.5636681470598));
#55993=CARTESIAN_POINT('Ctrl Pts',(1.4037262280594,114.181618894535,14.5849615914187));
#55994=CARTESIAN_POINT('Ctrl Pts',(1.34963797453741,114.191760188444,14.645223101111));
#55995=CARTESIAN_POINT('Ctrl Pts',(1.2916537876328,114.20193073026,14.7020775314085));
#55996=CARTESIAN_POINT('Ctrl Pts',(1.23024906046308,114.212102978335,14.7550620501643));
#55997=CARTESIAN_POINT('Ctrl Pts',(1.20128249758313,114.216901551297,14.7800565329173));
#55998=CARTESIAN_POINT('Ctrl Pts',(1.17155430541961,114.221700602415,14.8041904370712));
#55999=CARTESIAN_POINT('Ctrl Pts',(1.14111156484312,114.22649777038,14.8274180150671));
#56000=CARTESIAN_POINT('Ctrl Pts',(1.08268323793745,114.235704907871,14.8719983811796));
#56001=CARTESIAN_POINT('Ctrl Pts',(1.02162475849868,114.244904825821,14.9132392737883));
#56002=CARTESIAN_POINT('Ctrl Pts',(0.958396033709798,114.254084367512,14.9510161522063));
#56003=CARTESIAN_POINT('Ctrl Pts',(0.895142743528231,114.263267475604,14.9888077075588));
#56004=CARTESIAN_POINT('Ctrl Pts',(0.829703764380408,114.272442907348,15.0230456312068));
#56005=CARTESIAN_POINT('Ctrl Pts',(0.762474537595148,114.281633884579,15.053425384448));
#56006=CARTESIAN_POINT('Ctrl Pts',(0.69557730914607,114.290779473974,15.0836551132428));
#56007=CARTESIAN_POINT('Ctrl Pts',(0.626907143147252,114.299940452914,15.1100637585344));
#56008=CARTESIAN_POINT('Ctrl Pts',(0.556901841504499,114.309133156748,15.1323347236969));
#56009=CARTESIAN_POINT('Ctrl Pts',(0.512618724374969,114.314948167483,15.1464226246949));
#56010=CARTESIAN_POINT('Ctrl Pts',(0.467802359643517,114.320775742032,15.1588545741462));
#56011=CARTESIAN_POINT('Ctrl Pts',(0.422574251125431,114.326618658521,15.1695496006069));
#56012=CARTESIAN_POINT('Ctrl Pts',(0.370903099081658,114.333293937152,15.1817682044016));
#56013=CARTESIAN_POINT('Ctrl Pts',(0.318677340747473,114.339968686744,15.1918946382465));
#56014=CARTESIAN_POINT('Ctrl Pts',(0.266059723068317,114.346643823215,15.1998412406741));
#56015=CARTESIAN_POINT('Ctrl Pts',(0.158565375490708,114.360280689945,15.2160756290992));
#56016=CARTESIAN_POINT('Ctrl Pts',(0.0494326964004417,114.373919388781,
15.2232102815474));
#56017=CARTESIAN_POINT('Ctrl Pts',(-0.0597427169427481,114.387565093632,
15.2212594404747));
#56018=CARTESIAN_POINT('Ctrl Pts',(-0.170767016892279,114.401441888616,
15.2192755618908));
#56019=CARTESIAN_POINT('Ctrl Pts',(-0.28183445108275,114.415325944726,15.2078949509118));
#56020=CARTESIAN_POINT('Ctrl Pts',(-0.39122717706073,114.429219030687,15.1871685859229));
#56021=CARTESIAN_POINT('Ctrl Pts',(-0.491373073849375,114.44193775161,15.1681941944318));
#56022=CARTESIAN_POINT('Ctrl Pts',(-0.590114080078031,114.454664000419,
15.1413872200997));
#56023=CARTESIAN_POINT('Ctrl Pts',(-0.686117135667628,114.46739636212,15.1068219806883));
#56024=CARTESIAN_POINT('Ctrl Pts',(-0.789246990602818,114.481073912351,
15.0696907862235));
#56025=CARTESIAN_POINT('Ctrl Pts',(-0.889216089163326,114.494758557921,
15.0236063636402));
#56026=CARTESIAN_POINT('Ctrl Pts',(-0.98465074834828,114.508445266388,14.9694708212781));
#56027=CARTESIAN_POINT('Ctrl Pts',(-1.07262703043059,114.521062335859,14.9195660614539));
#56028=CARTESIAN_POINT('Ctrl Pts',(-1.15674895065018,114.533681120127,14.8628200486013));
#56029=CARTESIAN_POINT('Ctrl Pts',(-1.23595733003204,114.546294984981,14.7999749220962));
#56030=CARTESIAN_POINT('Ctrl Pts',(-1.31918266794619,114.559548546954,14.733942679921));
#56031=CARTESIAN_POINT('Ctrl Pts',(-1.3973579774902,114.572850791295,14.6609217524408));
#56032=CARTESIAN_POINT('Ctrl Pts',(-1.46920564745209,114.586189872428,14.5817105294917));
#56033=CARTESIAN_POINT('Ctrl Pts',(-1.47400615624047,114.587081124381,14.5764180242218));
#56034=CARTESIAN_POINT('Ctrl Pts',(-1.47877843046163,114.587972542245,14.571097897212));
#56035=CARTESIAN_POINT('Ctrl Pts',(-1.48352209509887,114.588864123114,14.5657503919148));
#56036=CARTESIAN_POINT('Ctrl Pts',(-1.55486081320341,114.602272372035,14.4853306737995));
#56037=CARTESIAN_POINT('Ctrl Pts',(-1.61972500331757,114.615717153408,14.3987170746629));
#56038=CARTESIAN_POINT('Ctrl Pts',(-1.67718661091241,114.629190209967,14.3072323840924));
#56039=CARTESIAN_POINT('Ctrl Pts',(-1.7067243286291,114.636115935822,14.2602053502418));
#56040=CARTESIAN_POINT('Ctrl Pts',(-1.73430678768296,114.643049198262,14.2118915549311));
#56041=CARTESIAN_POINT('Ctrl Pts',(-1.75981311677507,114.649989287947,14.1624718054398));
#56042=CARTESIAN_POINT('Ctrl Pts',(-1.79735780595881,114.660204929296,14.0897271494964));
#56043=CARTESIAN_POINT('Ctrl Pts',(-1.83040344750843,114.670435305712,14.01458652634));
#56044=CARTESIAN_POINT('Ctrl Pts',(-1.85898458022629,114.680679658673,13.9375759235067));
#56045=CARTESIAN_POINT('Ctrl Pts',(-1.88759691899623,114.690935196839,13.860481237341));
#56046=CARTESIAN_POINT('Ctrl Pts',(-1.91173453636451,114.70120474346,13.7815128709255));
#56047=CARTESIAN_POINT('Ctrl Pts',(-1.93046590239181,114.711488593118,13.7013890695747));
#56048=CARTESIAN_POINT('Ctrl Pts',(-1.95494309196695,114.724927001042,13.5966873904613));
#56049=CARTESIAN_POINT('Ctrl Pts',(-1.97018939645756,114.738389712462,13.4900147287906));
#56050=CARTESIAN_POINT('Ctrl Pts',(-1.97669816577161,114.751880528984,13.382740900891));
#56051=CARTESIAN_POINT('Ctrl Pts',(-1.97950230514057,114.757692707585,13.3365246732821));
#56052=CARTESIAN_POINT('Ctrl Pts',(-1.98068500018267,114.763510148179,13.2901963152702));
#56053=CARTESIAN_POINT('Ctrl Pts',(-1.98028688445897,114.769333357617,13.2438625847752));
#56054=CARTESIAN_POINT('Ctrl Pts',(-1.97954805877451,114.780140106616,13.1578761539258));
#56055=CARTESIAN_POINT('Ctrl Pts',(-1.97289380418289,114.790974816052,13.0715794340183));
#56056=CARTESIAN_POINT('Ctrl Pts',(-1.9605397664933,114.801824596246,12.9858061993644));
#56057=CARTESIAN_POINT('Ctrl Pts',(-1.94786271893812,114.812958055843,12.8977903294124));
#56058=CARTESIAN_POINT('Ctrl Pts',(-1.92918479688155,114.824107361028,12.8103265434447));
#56059=CARTESIAN_POINT('Ctrl Pts',(-1.90478500616689,114.835262997105,12.7242861190374));
#56060=CARTESIAN_POINT('Ctrl Pts',(-1.88009678708559,114.846550503244,12.637228616272));
#56061=CARTESIAN_POINT('Ctrl Pts',(-1.84955162894026,114.857844478874,12.5516289980619));
#56062=CARTESIAN_POINT('Ctrl Pts',(-1.8134705797214,114.869139784872,12.4683481216365));
#56063=CARTESIAN_POINT('Ctrl Pts',(-1.77754236835707,114.880387244414,12.3854200196108));
#56064=CARTESIAN_POINT('Ctrl Pts',(-1.73612605171753,114.891636026099,12.3047913928028));
#56065=CARTESIAN_POINT('Ctrl Pts',(-1.68955508506549,114.902885753633,12.2272636927215));
#56066=CARTESIAN_POINT('Ctrl Pts',(-1.64330270306537,114.914058523552,12.1502663474324));
#56067=CARTESIAN_POINT('Ctrl Pts',(-1.59196679225601,114.925232233742,12.0763277294864));
#56068=CARTESIAN_POINT('Ctrl Pts',(-1.53587670389948,114.936411078823,12.006181951572));
#56069=CARTESIAN_POINT('Ctrl Pts',(-1.49448130670192,114.944661248254,11.9544132269439));
#56070=CARTESIAN_POINT('Ctrl Pts',(-1.45049655134422,114.952914309089,11.9047092579959));
#56071=CARTESIAN_POINT('Ctrl Pts',(-1.4040520209068,114.961173521084,11.8573471711196));
#56072=CARTESIAN_POINT('Ctrl Pts',(-1.33819344786587,114.972885124393,11.7901874985266));
#56073=CARTESIAN_POINT('Ctrl Pts',(-1.26739146386725,114.984608878134,11.7277382796105));
#56074=CARTESIAN_POINT('Ctrl Pts',(-1.19260201353219,114.996358577999,11.6703739518762));
#56075=CARTESIAN_POINT('Ctrl Pts',(-1.10707777757756,115.009794752475,11.6047759259708));
#56076=CARTESIAN_POINT('Ctrl Pts',(-1.01575429987191,115.023248783164,11.5458756839365));
#56077=CARTESIAN_POINT('Ctrl Pts',(-0.919995153934207,115.036721605789,
11.4944557145685));
#56078=CARTESIAN_POINT('Ctrl Pts',(-0.820781337934725,115.050680482844,
11.4411806844957));
#56079=CARTESIAN_POINT('Ctrl Pts',(-0.716807783998793,115.064659495539,
11.3959350914759));
#56080=CARTESIAN_POINT('Ctrl Pts',(-0.609588924382951,115.078665979716,
11.3595353194296));
#56081=CARTESIAN_POINT('Ctrl Pts',(-0.58708529063664,115.081605731091,11.3518955521209));
#56082=CARTESIAN_POINT('Ctrl Pts',(-0.564438636161258,115.0845467151,11.3446452862742));
#56083=CARTESIAN_POINT('Ctrl Pts',(-0.541662845511286,115.087489035339,
11.3377918074298));
#56084=CARTESIAN_POINT('Ctrl Pts',(-0.433090865926177,115.101515048218,
11.3051213383066));
#56085=CARTESIAN_POINT('Ctrl Pts',(-0.32158728440439,115.115570919231,11.2814705209975));
#56086=CARTESIAN_POINT('Ctrl Pts',(-0.208740093011524,115.129671734795,
11.2670225831313));
#56087=CARTESIAN_POINT('Ctrl Pts',(-0.0954959987621371,115.143822145337,
11.2525238293985));
#56088=CARTESIAN_POINT('Ctrl Pts',(0.0191003291196167,115.158017820759,
11.2472915730283));
#56089=CARTESIAN_POINT('Ctrl Pts',(0.133489161976199,115.1722803876,11.2514841753134));
#56090=CARTESIAN_POINT('Ctrl Pts',(0.247877994832781,115.186542954441,11.2556767775986));
#56091=CARTESIAN_POINT('Ctrl Pts',(0.362059023130047,115.200872423394,11.2692930525077));
#56092=CARTESIAN_POINT('Ctrl Pts',(0.474526150140969,115.215296677043,11.2924828105989));
#56093=CARTESIAN_POINT('Ctrl Pts',(0.50602381165388,115.219336348643,11.2989773585645));
#56094=CARTESIAN_POINT('Ctrl Pts',(0.537387379013572,115.223383491721,11.3062227970019));
#56095=CARTESIAN_POINT('Ctrl Pts',(0.568587127550378,115.227438802565,11.3141998098193));
#56096=CARTESIAN_POINT('Ctrl Pts',(0.685283669077595,115.242606897581,11.344036262072));
#56097=CARTESIAN_POINT('Ctrl Pts',(0.799648242264584,115.257737894668,11.3846662327927));
#56098=CARTESIAN_POINT('Ctrl Pts',(0.909979583555605,115.272847673227,11.435094383272));
#56099=CARTESIAN_POINT('Ctrl Pts',(1.0238062785511,115.288436137351,11.4871201235251));
#56100=CARTESIAN_POINT('Ctrl Pts',(1.13334103054777,115.304001984215,11.5495729775517));
#56101=CARTESIAN_POINT('Ctrl Pts',(1.23676642008008,115.31957053264,11.6213794977147));
#56102=CARTESIAN_POINT('Ctrl Pts',(1.29353921225325,115.328116499624,11.6607958988936));
#56103=CARTESIAN_POINT('Ctrl Pts',(1.34847195375019,115.336663420413,11.7030312412126));
#56104=CARTESIAN_POINT('Ctrl Pts',(1.4012683470544,115.345216495727,11.7479129855167));
#56105=CARTESIAN_POINT('Ctrl Pts',(1.48226718234083,115.358338398479,11.8167693748784));
#56106=CARTESIAN_POINT('Ctrl Pts',(1.55835527482928,115.371540344119,11.8917233631653));
#56107=CARTESIAN_POINT('Ctrl Pts',(1.62837464185511,115.384802618524,11.9721818737286));
#56108=CARTESIAN_POINT('Ctrl Pts',(1.67307949990156,115.393270105733,12.0235517510375));
#56109=CARTESIAN_POINT('Ctrl Pts',(1.71531050678469,115.401762119113,12.077164434722));
#56110=CARTESIAN_POINT('Ctrl Pts',(1.75476984556133,115.410272829667,12.1328549792085));
#56111=CARTESIAN_POINT('Ctrl Pts',(1.81716417373831,115.423730228696,12.2209145923894));
#56112=CARTESIAN_POINT('Ctrl Pts',(1.87262649087647,115.437234543671,12.3141708941146));
#56113=CARTESIAN_POINT('Ctrl Pts',(1.92073481534129,115.450759946289,12.411281384807));
#56114=CARTESIAN_POINT('Ctrl Pts',(1.93704224606978,115.455344694744,12.4441992346302));
#56115=CARTESIAN_POINT('Ctrl Pts',(1.95250500725449,115.459931837736,12.4775596439822));
#56116=CARTESIAN_POINT('Ctrl Pts',(1.96710777417235,115.464520282047,12.5113095315961));
#56117=CARTESIAN_POINT('Ctrl Pts',(2.02284203773276,115.482032960706,12.6401224573922));
#56118=CARTESIAN_POINT('Ctrl Pts',(2.06613025176284,115.499578000723,12.7749773920369));
#56119=CARTESIAN_POINT('Ctrl Pts',(2.09613795233903,115.517181179691,12.9131906279659));
#56120=CARTESIAN_POINT('Ctrl Pts',(2.12402968913341,115.533543087638,13.0416578921684));
#56121=CARTESIAN_POINT('Ctrl Pts',(2.14044852787112,115.549955270481,13.1730279986298));
#56122=CARTESIAN_POINT('Ctrl Pts',(2.14468284862367,115.566441721781,13.3051600237124));
#56123=CARTESIAN_POINT('Ctrl Pts',(2.14632244725498,115.572825546854,13.3563237168141));
#56124=CARTESIAN_POINT('Ctrl Pts',(2.14613462261372,115.579220540859,13.4076016959267));
#56125=CARTESIAN_POINT('Ctrl Pts',(2.14407588116522,115.585628222627,13.4588695760761));
#56126=CARTESIAN_POINT('Ctrl Pts',(2.14147055810292,115.59373709958,13.5237487237737));
#56127=CARTESIAN_POINT('Ctrl Pts',(2.13586729158356,115.601856107239,13.5885460652796));
#56128=CARTESIAN_POINT('Ctrl Pts',(2.12719321699842,115.609986063637,13.6530007834056));
#56129=CARTESIAN_POINT('Ctrl Pts',(2.10699154461732,115.628920500274,13.8031139840954));
#56130=CARTESIAN_POINT('Ctrl Pts',(2.07013478074693,115.647914195593,13.9513654573672));
#56131=CARTESIAN_POINT('Ctrl Pts',(2.01824822471315,115.666978611439,14.0946950219294));
#56132=CARTESIAN_POINT('Ctrl Pts',(1.98042961867447,115.680874111302,14.1991637851355));
#56133=CARTESIAN_POINT('Ctrl Pts',(1.9346262410061,115.694807222267,14.3010187640065));
#56134=CARTESIAN_POINT('Ctrl Pts',(1.88146178409473,115.708783002571,14.3990916206313));
#56135=CARTESIAN_POINT('Ctrl Pts',(1.83036747451932,115.722214586131,14.4933456615536));
#56136=CARTESIAN_POINT('Ctrl Pts',(1.77222890192354,115.735622945604,14.5842203077108));
#56137=CARTESIAN_POINT('Ctrl Pts',(1.70764755970895,115.749035808859,14.6705866225551));
#56138=CARTESIAN_POINT('Ctrl Pts',(1.64306632820495,115.76244864912,14.7569527893432));
#56139=CARTESIAN_POINT('Ctrl Pts',(1.5720435452874,115.77586600016,14.8388103433535));
#56140=CARTESIAN_POINT('Ctrl Pts',(1.49519464604144,115.789320521743,14.9150797911722));
#56141=CARTESIAN_POINT('Ctrl Pts',(1.44760010886154,115.797653259544,14.9623154588983));
#56142=CARTESIAN_POINT('Ctrl Pts',(1.39777106681861,115.806000351625,15.0074087322159));
#56143=CARTESIAN_POINT('Ctrl Pts',(1.34585358646912,115.814370484018,15.0501131939447));
#56144=CARTESIAN_POINT('Ctrl Pts',(1.3071473427463,115.820610701807,15.0819508195884));
#56145=CARTESIAN_POINT('Ctrl Pts',(1.26728031463752,115.826863740542,15.1124608690016));
#56146=CARTESIAN_POINT('Ctrl Pts',(1.22636916842543,115.83313345591,15.1415957736095));
#56147=CARTESIAN_POINT('Ctrl Pts',(1.12810170945666,115.848193141466,15.2115770209762));
#56148=CARTESIAN_POINT('Ctrl Pts',(1.02382909071115,115.863353703261,15.2736274831145));
#56149=CARTESIAN_POINT('Ctrl Pts',(0.914955216940758,115.878572923054,15.3270233660414));
#56150=CARTESIAN_POINT('Ctrl Pts',(0.819226999552299,115.891954542816,15.3739721197823));
#56151=CARTESIAN_POINT('Ctrl Pts',(0.719941095969984,115.905381408066,15.4142287706305));
#56152=CARTESIAN_POINT('Ctrl Pts',(0.618066703704985,115.918820787105,15.4472718233318));
#56153=CARTESIAN_POINT('Ctrl Pts',(0.51392554880499,115.932559199901,15.4810501025758));
#56154=CARTESIAN_POINT('Ctrl Pts',(0.407078861767362,115.946310694998,15.5072896988209));
#56155=CARTESIAN_POINT('Ctrl Pts',(0.29865525520882,115.960036151081,15.5255720386239));
#56156=CARTESIAN_POINT('Ctrl Pts',(0.182916754998672,115.974687607091,15.5450878125065));
#56157=CARTESIAN_POINT('Ctrl Pts',(0.0653436635643293,115.989459403803,
15.5557348502609));
#56158=CARTESIAN_POINT('Ctrl Pts',(-0.052617637522511,116.0043251002,15.5570067734007));
#56159=CARTESIAN_POINT('Ctrl Pts',(-0.106561210549434,116.011123166785,
15.5575884224512));
#56160=CARTESIAN_POINT('Ctrl Pts',(-0.160585503936932,116.017940835553,
15.5562100758667));
#56161=CARTESIAN_POINT('Ctrl Pts',(-0.214550364991037,116.024775405707,
15.5528264578072));
#56162=CARTESIAN_POINT('Ctrl Pts',(-0.33323579887121,116.039806741067,15.5453848343205));
#56163=CARTESIAN_POINT('Ctrl Pts',(-0.451633874569923,116.054919990971,
15.5282403430295));
#56164=CARTESIAN_POINT('Ctrl Pts',(-0.568252849555415,116.070084823131,
15.5019345828368));
#56165=CARTESIAN_POINT('Ctrl Pts',(-0.618392857246718,116.076604901028,
15.4906244935605));
#56166=CARTESIAN_POINT('Ctrl Pts',(-0.668203943852332,116.083134483099,
15.4776215571167));
#56167=CARTESIAN_POINT('Ctrl Pts',(-0.717567805806733,116.089671019621,
15.4629717731698));
#56168=CARTESIAN_POINT('Ctrl Pts',(-0.834150577526599,116.105108376323,
15.4283733371885));
#56169=CARTESIAN_POINT('Ctrl Pts',(-0.948364145641417,116.120416762755,
15.3843060231208));
#56170=CARTESIAN_POINT('Ctrl Pts',(-1.05868732191905,116.135659632901,15.3314168528225));
#56171=CARTESIAN_POINT('Ctrl Pts',(-1.17134192991175,116.151224626758,15.2774099890968));
#56172=CARTESIAN_POINT('Ctrl Pts',(-1.27994059980948,116.166721298147,15.2142059500083));
#56173=CARTESIAN_POINT('Ctrl Pts',(-1.3829147316966,116.182224708343,15.1424762192239));
#56174=CARTESIAN_POINT('Ctrl Pts',(-1.46501198386403,116.194584971577,15.0852889073409));
#56175=CARTESIAN_POINT('Ctrl Pts',(-1.54353541226832,116.206949668497,15.0226822699764));
#56176=CARTESIAN_POINT('Ctrl Pts',(-1.6177072454825,116.219360164099,14.9549803930063));
#56177=CARTESIAN_POINT('Ctrl Pts',(-1.65858238845539,116.22619942855,14.9176707596756));
#56178=CARTESIAN_POINT('Ctrl Pts',(-1.69813562227692,116.233084387951,14.8788675694272));
#56179=CARTESIAN_POINT('Ctrl Pts',(-1.73623654775755,116.240006145925,14.8386078818976));
#56180=CARTESIAN_POINT('Ctrl Pts',(-1.81330527686961,116.254007146783,14.7571725121994));
#56181=CARTESIAN_POINT('Ctrl Pts',(-1.88443502621154,116.268159127004,14.6697767096657));
#56182=CARTESIAN_POINT('Ctrl Pts',(-1.94907960847239,116.282383109819,14.5774327095694));
#56183=CARTESIAN_POINT('Ctrl Pts',(-2.01507679914757,116.296904711988,14.4831565247923));
#56184=CARTESIAN_POINT('Ctrl Pts',(-2.07431366250875,116.311501363033,14.3837217163799));
#56185=CARTESIAN_POINT('Ctrl Pts',(-2.12616402378042,116.326082039708,14.280234204363));
#56186=CARTESIAN_POINT('Ctrl Pts',(-2.15709073675296,116.33477884319,14.2185079501598));
#56187=CARTESIAN_POINT('Ctrl Pts',(-2.18538879693703,116.343469830457,14.1553405405778));
#56188=CARTESIAN_POINT('Ctrl Pts',(-2.21092009295596,116.352134539812,14.0909736700272));
#56189=CARTESIAN_POINT('Ctrl Pts',(-2.25486215680431,116.367047422083,13.9801914702771));
#56190=CARTESIAN_POINT('Ctrl Pts',(-2.29069844177545,116.381944676096,13.8657330971959));
#56191=CARTESIAN_POINT('Ctrl Pts',(-2.31776617764799,116.396846147778,13.7489725582936));
#56192=CARTESIAN_POINT('Ctrl Pts',(-2.34458345574813,116.411609736136,13.6332924047112));
#56193=CARTESIAN_POINT('Ctrl Pts',(-2.36279367397774,116.426377473984,13.5153537393306));
#56194=CARTESIAN_POINT('Ctrl Pts',(-2.37180242101775,116.441170795581,13.3964950169532));
#56195=CARTESIAN_POINT('Ctrl Pts',(-2.37576502392796,116.447677811368,13.3442136156545));
#56196=CARTESIAN_POINT('Ctrl Pts',(-2.37794800011267,116.454189804121,13.291754121448));
#56197=CARTESIAN_POINT('Ctrl Pts',(-2.37830389938607,116.460708723163,13.239229683751));
#56198=CARTESIAN_POINT('Ctrl Pts',(-2.37875671095951,116.469002760856,13.1724027047287));
#56199=CARTESIAN_POINT('Ctrl Pts',(-2.37625184052921,116.47730800462,13.1054707115953));
#56200=CARTESIAN_POINT('Ctrl Pts',(-2.37087518211755,116.485628716616,13.0386819501779));
#56201=CARTESIAN_POINT('Ctrl Pts',(-2.36133029276527,116.500400024228,12.9201154933015));
#56202=CARTESIAN_POINT('Ctrl Pts',(-2.34267915449744,116.515221006775,12.8017184202899));
#56203=CARTESIAN_POINT('Ctrl Pts',(-2.31529268428084,116.530091783787,12.6848953499409));
#56204=CARTESIAN_POINT('Ctrl Pts',(-2.28681456295353,116.54555532431,12.5634155993591));
#56205=CARTESIAN_POINT('Ctrl Pts',(-2.24889100388477,116.561072708035,12.4436391012527));
#56206=CARTESIAN_POINT('Ctrl Pts',(-2.20199445050019,116.576644531451,12.3271461148292));
#56207=CARTESIAN_POINT('Ctrl Pts',(-2.15535223441636,116.592131903128,12.2112849128245));
#56208=CARTESIAN_POINT('Ctrl Pts',(-2.09983465091386,116.607673129599,12.0986729808405));
#56209=CARTESIAN_POINT('Ctrl Pts',(-2.03595400084272,116.623269211091,11.9908465165357));
#56210=CARTESIAN_POINT('Ctrl Pts',(-1.97448327236903,116.63827692453,11.8870878462313));
#56211=CARTESIAN_POINT('Ctrl Pts',(-1.90526922618553,116.653335437877,11.7877612621495));
#56212=CARTESIAN_POINT('Ctrl Pts',(-1.82880326091235,116.668445952396,11.6942030383103));
#56213=CARTESIAN_POINT('Ctrl Pts',(-1.80048378080912,116.674042192681,11.6595533709839));
#56214=CARTESIAN_POINT('Ctrl Pts',(-1.77116991909143,116.679645568285,11.6256945101545));
#56215=CARTESIAN_POINT('Ctrl Pts',(-1.74088766295243,116.685256149272,11.592692791068));
#56216=CARTESIAN_POINT('Ctrl Pts',(-1.65765618047929,116.70067696108,11.5019868016883));
#56217=CARTESIAN_POINT('Ctrl Pts',(-1.56710879023825,116.71615218637,11.4177594726791));
#56218=CARTESIAN_POINT('Ctrl Pts',(-1.47063466401891,116.731682286979,11.3407084361487));
#56219=CARTESIAN_POINT('Ctrl Pts',(-1.41290748548492,116.740975026138,11.2946034428585));
#56220=CARTESIAN_POINT('Ctrl Pts',(-1.35305845127679,116.750287418186,11.251066977279));
#56221=CARTESIAN_POINT('Ctrl Pts',(-1.29138505495245,116.759619604489,11.2102394704746));
#56222=CARTESIAN_POINT('Ctrl Pts',(-1.18962354774155,116.775017772912,11.1428738172807));
#56223=CARTESIAN_POINT('Ctrl Pts',(-1.08223578712878,116.790146385918,11.0827796079039));
#56224=CARTESIAN_POINT('Ctrl Pts',(-0.970545703476898,116.805179784118,
11.0306873682955));
#56225=CARTESIAN_POINT('Ctrl Pts',(-0.856018421282094,116.82059506703,10.977271859678));
#56226=CARTESIAN_POINT('Ctrl Pts',(-0.73696885781619,116.835910228986,10.9322685711069));
#56227=CARTESIAN_POINT('Ctrl Pts',(-0.614794195145899,116.85132342974,10.8964200289001));
#56228=CARTESIAN_POINT('Ctrl Pts',(-0.491954171599043,116.86682057049,10.8603762562179));
#56229=CARTESIAN_POINT('Ctrl Pts',(-0.365955633575362,116.882416841384,
10.833585519513));
#56230=CARTESIAN_POINT('Ctrl Pts',(-0.238172442065973,116.898323679995,
10.8167817358934));
#56231=CARTESIAN_POINT('Ctrl Pts',(-0.196656945584479,116.903491654707,
10.8113223526092));
#56232=CARTESIAN_POINT('Ctrl Pts',(-0.154952671188114,116.90869248821,10.8069170728641));
#56233=CARTESIAN_POINT('Ctrl Pts',(-0.113105562718294,116.913933652364,
10.8035910556126));
#56234=CARTESIAN_POINT('Ctrl Pts',(1.89583865317118,21.7883719873226,13.197232071317));
#56235=CARTESIAN_POINT('Ctrl Pts',(1.91781707633732,21.8441218058461,13.6730473758255));
#56236=CARTESIAN_POINT('Ctrl Pts',(1.69642718260873,21.9440513975239,14.4537819826606));
#56237=CARTESIAN_POINT('Ctrl Pts',(0.672633958004841,22.0991544508714,15.2803835560697));
#56238=CARTESIAN_POINT('Ctrl Pts',(-0.60319738394239,22.250832522417,15.3221596893961));
#56239=CARTESIAN_POINT('Ctrl Pts',(-1.34901622678997,22.3564371611312,14.8505318619346));
#56240=CARTESIAN_POINT('Ctrl Pts',(-1.63086999297234,22.4127847437298,14.497109087338));
#56241=CARTESIAN_POINT('Ctrl Pts',(-1.67292082684555,22.4214691961456,14.4416712469716));
#56242=CARTESIAN_POINT('Ctrl Pts',(-1.74278673487562,22.4366802475148,14.3416803032928));
#56243=CARTESIAN_POINT('Ctrl Pts',(-1.86710205946279,22.4671818233788,14.1308312671578));
#56244=CARTESIAN_POINT('Ctrl Pts',(-2.04999258960691,22.528452716599,13.6722180537393));
#56245=CARTESIAN_POINT('Ctrl Pts',(-2.10140414959869,22.6167364856815,12.9515240914931));
#56246=CARTESIAN_POINT('Ctrl Pts',(-1.80799633762795,22.7240819881822,12.1227672472193));
#56247=CARTESIAN_POINT('Ctrl Pts',(-1.19990303017822,22.8328298152915,11.4720954721768));
#56248=CARTESIAN_POINT('Ctrl Pts',(-0.371002901919627,22.9431012190898,
11.1145961507936));
#56249=CARTESIAN_POINT('Ctrl Pts',(0.467762943195029,23.0455895703631,11.1178807055511));
#56250=CARTESIAN_POINT('Ctrl Pts',(1.1824163516888,23.1399165325713,11.3911664755444));
#56251=CARTESIAN_POINT('Ctrl Pts',(1.72621929731623,23.2257405437626,11.8251312591644));
#56252=CARTESIAN_POINT('Ctrl Pts',(2.05162663549235,23.2980233626201,12.3127044160272));
#56253=CARTESIAN_POINT('Ctrl Pts',(2.21469313453867,23.3563366579963,12.7519562978106));
#56254=CARTESIAN_POINT('Ctrl Pts',(2.35722297838454,23.4442829398336,13.4441616523464));
#56255=CARTESIAN_POINT('Ctrl Pts',(2.15527130903289,23.57796993702,14.5485148077445));
#56256=CARTESIAN_POINT('Ctrl Pts',(1.059145585634,23.7602399209507,15.6184220519286));
#56257=CARTESIAN_POINT('Ctrl Pts',(-0.529239386701929,23.9513951638177,
15.8648208380125));
#56258=CARTESIAN_POINT('Ctrl Pts',(-1.51756572472491,24.0834106661585,15.3439163457973));
#56259=CARTESIAN_POINT('Ctrl Pts',(-1.89463460506064,24.1527410864499,14.9357054885149));
#56260=CARTESIAN_POINT('Ctrl Pts',(2.09579517948206,21.7240373735623,13.1885007805612));
#56261=CARTESIAN_POINT('Ctrl Pts',(2.12135717463155,21.7843405351804,13.7037820948012));
#56262=CARTESIAN_POINT('Ctrl Pts',(1.87919305520299,21.8956866809261,14.5752420688376));
#56263=CARTESIAN_POINT('Ctrl Pts',(0.751099816146643,22.0664628760232,15.485969451142));
#56264=CARTESIAN_POINT('Ctrl Pts',(-0.657449610166076,22.2341318757709,
15.5386353888612));
#56265=CARTESIAN_POINT('Ctrl Pts',(-1.48093958778983,22.3504810823427,15.0191831835147));
#56266=CARTESIAN_POINT('Ctrl Pts',(-1.79271008834924,22.4125981058827,14.6305718396412));
#56267=CARTESIAN_POINT('Ctrl Pts',(-1.83921057775072,22.4221669865294,14.5696025279449));
#56268=CARTESIAN_POINT('Ctrl Pts',(-1.91649095560331,22.4389268751508,14.4596450638053));
#56269=CARTESIAN_POINT('Ctrl Pts',(-2.05404081986639,22.4725216181623,14.2277761229944));
#56270=CARTESIAN_POINT('Ctrl Pts',(-2.2567629418467,22.5399786177802,13.7234303602587));
#56271=CARTESIAN_POINT('Ctrl Pts',(-2.31535246183976,22.6371070814728,12.9307537793653));
#56272=CARTESIAN_POINT('Ctrl Pts',(-1.99544618564001,22.7549947273253,12.019912280396));
#56273=CARTESIAN_POINT('Ctrl Pts',(-1.33067454399223,22.8742133079875,11.3050824355626));
#56274=CARTESIAN_POINT('Ctrl Pts',(-0.424988525149834,22.9948313849074,
10.9118644483054));
#56275=CARTESIAN_POINT('Ctrl Pts',(0.490380343808289,23.1066820811408,10.913245367816));
#56276=CARTESIAN_POINT('Ctrl Pts',(1.26931089246893,23.2094023340903,11.2089165793694));
#56277=CARTESIAN_POINT('Ctrl Pts',(1.86149576703992,23.3026720706013,11.6790480189558));
#56278=CARTESIAN_POINT('Ctrl Pts',(2.21572530831819,23.3810697334384,12.2069903102016));
#56279=CARTESIAN_POINT('Ctrl Pts',(2.39354512758931,23.4442083621846,12.682127093083));
#56280=CARTESIAN_POINT('Ctrl Pts',(2.54968537849172,23.5393281857135,13.4304282224035));
#56281=CARTESIAN_POINT('Ctrl Pts',(2.33419451824951,23.6835362613187,14.6221100361887));
#56282=CARTESIAN_POINT('Ctrl Pts',(1.15975669052109,23.879193993993,15.7729786483405));
#56283=CARTESIAN_POINT('Ctrl Pts',(-0.536296867408047,24.0833794822401,
16.03953727275));
#56284=CARTESIAN_POINT('Ctrl Pts',(-1.5873348158791,24.2236364673292,15.4881545619776));
#56285=CARTESIAN_POINT('Ctrl Pts',(-1.9878959091456,24.2970685263766,15.0568812348725));
#56286=CARTESIAN_POINT('Ctrl Pts',(2.29575170579295,21.6597027598019,13.1797694898055));
#56287=CARTESIAN_POINT('Ctrl Pts',(2.32489727292579,21.7245592645148,13.7345168137768));
#56288=CARTESIAN_POINT('Ctrl Pts',(2.06195892779723,21.8473219643282,14.6967021550147));
#56289=CARTESIAN_POINT('Ctrl Pts',(0.829565674288447,22.033771301175,15.6915553462145));
#56290=CARTESIAN_POINT('Ctrl Pts',(-0.711701836389763,22.2174312291249,
15.7551110883264));
#56291=CARTESIAN_POINT('Ctrl Pts',(-1.61286294878969,22.3445250035544,15.1878345050949));
#56292=CARTESIAN_POINT('Ctrl Pts',(-1.95455018372616,22.4124114680356,14.7640345919444));
#56293=CARTESIAN_POINT('Ctrl Pts',(-2.0055003286559,22.4228647769132,14.6975338089182));
#56294=CARTESIAN_POINT('Ctrl Pts',(-2.09019517633101,22.4411735027868,14.5776098243179));
#56295=CARTESIAN_POINT('Ctrl Pts',(-2.24097958027,22.4778614129459,14.3247209788311));
#56296=CARTESIAN_POINT('Ctrl Pts',(-2.4635332940865,22.5515045189613,13.774642666778));
#56297=CARTESIAN_POINT('Ctrl Pts',(-2.52930077408085,22.6574776772641,12.9099834672373));
#56298=CARTESIAN_POINT('Ctrl Pts',(-2.18289603365208,22.7859074664684,11.9170573135726));
#56299=CARTESIAN_POINT('Ctrl Pts',(-1.46144605780623,22.9155968006837,11.1380693989486));
#56300=CARTESIAN_POINT('Ctrl Pts',(-0.478974148380045,23.0465615507249,
10.7091327458171));
#56301=CARTESIAN_POINT('Ctrl Pts',(0.512997744421549,23.1677745919185,10.7086100300809));
#56302=CARTESIAN_POINT('Ctrl Pts',(1.35620543324907,23.2788881356092,11.0266666831942));
#56303=CARTESIAN_POINT('Ctrl Pts',(1.99677223676361,23.37960359744,11.5329647787473));
#56304=CARTESIAN_POINT('Ctrl Pts',(2.37982398114403,23.4641161042566,12.1012762043759));
#56305=CARTESIAN_POINT('Ctrl Pts',(2.57239712063998,23.5320800663729,12.6122978883554));
#56306=CARTESIAN_POINT('Ctrl Pts',(2.7421477785989,23.6343734315934,13.4166947924605));
#56307=CARTESIAN_POINT('Ctrl Pts',(2.51311772746614,23.7891025856174,14.695705264633));
#56308=CARTESIAN_POINT('Ctrl Pts',(1.26036779540819,23.9981480670354,15.9275352447523));
#56309=CARTESIAN_POINT('Ctrl Pts',(-0.543354348114162,24.2153638006625,
16.2142537074874));
#56310=CARTESIAN_POINT('Ctrl Pts',(-1.6571039070333,24.3638622684998,15.632392778158));
#56311=CARTESIAN_POINT('Ctrl Pts',(-2.08115721323056,24.4413959663033,15.1780569812301));
#56312=CARTESIAN_POINT('Ctrl Pts',(2.49570823210383,21.5953681460417,13.1710381990497));
#56313=CARTESIAN_POINT('Ctrl Pts',(2.52843737122002,21.6647779938492,13.7652515327526));
#56314=CARTESIAN_POINT('Ctrl Pts',(2.24472480039148,21.7989572477304,14.8181622411917));
#56315=CARTESIAN_POINT('Ctrl Pts',(0.908031532430251,22.0010797263267,15.8971412412869));
#56316=CARTESIAN_POINT('Ctrl Pts',(-0.765954062613445,22.2007305824788,
15.9715867877915));
#56317=CARTESIAN_POINT('Ctrl Pts',(-1.74478630978955,22.338568924766,15.3564858266751));
#56318=CARTESIAN_POINT('Ctrl Pts',(-2.11639027910306,22.4122248301885,14.8974973442476));
#56319=CARTESIAN_POINT('Ctrl Pts',(-2.17179007956105,22.4235625672971,14.8254650898915));
#56320=CARTESIAN_POINT('Ctrl Pts',(-2.2638993970587,22.4434201304229,14.6955745848305));
#56321=CARTESIAN_POINT('Ctrl Pts',(-2.42791834067359,22.4832012077294,14.4216658346677));
#56322=CARTESIAN_POINT('Ctrl Pts',(-2.67030364632629,22.5630304201425,13.8258549732975));
#56323=CARTESIAN_POINT('Ctrl Pts',(-2.74324908632193,22.6778482730553,12.8892131551093));
#56324=CARTESIAN_POINT('Ctrl Pts',(-2.37034588166413,22.8168202056115,11.8142023467493));
#56325=CARTESIAN_POINT('Ctrl Pts',(-1.59221757162024,22.9569802933797,10.9710563623344));
#56326=CARTESIAN_POINT('Ctrl Pts',(-0.532959771610249,23.0982917165424,
10.5064010433289));
#56327=CARTESIAN_POINT('Ctrl Pts',(0.535615145034812,23.2288671026962,10.5039746923458));
#56328=CARTESIAN_POINT('Ctrl Pts',(1.4430999740292,23.3483739371282,10.8444167870192));
#56329=CARTESIAN_POINT('Ctrl Pts',(2.1320487064873,23.4565351242787,11.3868815385387));
#56330=CARTESIAN_POINT('Ctrl Pts',(2.54392265396986,23.5471624750749,11.9955620985503));
#56331=CARTESIAN_POINT('Ctrl Pts',(2.75124911369062,23.6199517705612,12.5424686836278));
#56332=CARTESIAN_POINT('Ctrl Pts',(2.93461017870607,23.7294186774733,13.4029613625176));
#56333=CARTESIAN_POINT('Ctrl Pts',(2.69204093668275,23.8946689099161,14.7693004930773));
#56334=CARTESIAN_POINT('Ctrl Pts',(1.36097890029528,24.1171021400777,16.0820918411643));
#56335=CARTESIAN_POINT('Ctrl Pts',(-0.55041182882028,24.3473481190849,16.3889701422247));
#56336=CARTESIAN_POINT('Ctrl Pts',(-1.7268729981875,24.5040880696705,15.7766309943384));
#56337=CARTESIAN_POINT('Ctrl Pts',(-2.17441851731554,24.5857234062301,15.2992327275877));
#56338=CARTESIAN_POINT('',(1.9,21.8,13.3));
#56339=CARTESIAN_POINT('Ctrl Pts',(-3.1635730752188,29.2100860618195,12.4907938897549));
#56340=CARTESIAN_POINT('Ctrl Pts',(-2.98085158893828,29.3019317286879,11.7779528294547));
#56341=CARTESIAN_POINT('Ctrl Pts',(-2.12224476023707,29.4834174338966,10.5004848443473));
#56342=CARTESIAN_POINT('Ctrl Pts',(0.0593203066058203,29.7539464610308,
9.80303601328355));
#56343=CARTESIAN_POINT('Ctrl Pts',(2.1830045028505,30.0213429575011,10.5869226484086));
#56344=CARTESIAN_POINT('Ctrl Pts',(3.36867072083526,30.2873651789924,12.5013119695689));
#56345=CARTESIAN_POINT('Ctrl Pts',(3.12820931026034,30.5516392506713,14.7255047004695));
#56346=CARTESIAN_POINT('Ctrl Pts',(1.58055854613697,30.8138087120526,16.3181541366838));
#56347=CARTESIAN_POINT('Ctrl Pts',(-0.593576583725148,31.0735240541513,
16.6192226195957));
#56348=CARTESIAN_POINT('Ctrl Pts',(-2.69414652544478,31.3590120613392,15.4093240673898));
#56349=CARTESIAN_POINT('Ctrl Pts',(-3.29228396144786,31.6123375258171,13.2621475022427));
#56350=CARTESIAN_POINT('Ctrl Pts',(-2.59121784125708,31.8344343538493,11.5764220916364));
#56351=CARTESIAN_POINT('Ctrl Pts',(-1.26416080201115,32.0543699991392,10.3503143566391));
#56352=CARTESIAN_POINT('Ctrl Pts',(1.11608957290045,32.3250666810991,10.167546191111));
#56353=CARTESIAN_POINT('Ctrl Pts',(3.06291956153987,32.6425883170784,12.194735374529));
#56354=CARTESIAN_POINT('Ctrl Pts',(2.72096138219714,32.9523804802361,14.9138117217176));
#56355=CARTESIAN_POINT('Ctrl Pts',(0.661085756377314,33.2289591199972,16.2180280599844));
#56356=CARTESIAN_POINT('Ctrl Pts',(-1.37468245683901,33.4743218620618,15.7903827762575));
#56357=CARTESIAN_POINT('Ctrl Pts',(-2.55899077373492,33.6904057619936,14.3988045569796));
#56358=CARTESIAN_POINT('Ctrl Pts',(-2.63218467362997,33.9017075317211,12.6113846899565));
#56359=CARTESIAN_POINT('Ctrl Pts',(-1.61587194033675,34.1082261165484,11.1894758647939));
#56360=CARTESIAN_POINT('Ctrl Pts',(0.0216236752264965,34.3099896601507,
10.7039018687867));
#56361=CARTESIAN_POINT('Ctrl Pts',(1.57455705156837,34.5070605714621,11.3135848522268));
#56362=CARTESIAN_POINT('Ctrl Pts',(2.40467660737928,34.6995310564001,12.7155627750386));
#56363=CARTESIAN_POINT('Ctrl Pts',(2.20227690752673,34.8875249955867,14.2941075319982));
#56364=CARTESIAN_POINT('Ctrl Pts',(1.09822533438088,35.071196858881,15.3888766878108));
#56365=CARTESIAN_POINT('Ctrl Pts',(-0.410767088927198,35.2507283443733,
15.5694539058736));
#56366=CARTESIAN_POINT('Ctrl Pts',(-1.68341513267947,35.426332789423,14.8014468984984));
#56367=CARTESIAN_POINT('Ctrl Pts',(-2.20404781770678,35.5982453338191,13.4424781480868));
#56368=CARTESIAN_POINT('Ctrl Pts',(-1.78749563440858,35.7667271053238,12.0784119565304));
#56369=CARTESIAN_POINT('Ctrl Pts',(-0.643778855103036,35.932070046999,11.2723067128195));
#56370=CARTESIAN_POINT('Ctrl Pts',(0.73153021794509,36.0945712336176,11.3404925776424));
#56371=CARTESIAN_POINT('Ctrl Pts',(1.64179858012663,36.2367845423708,12.1262687862789));
#56372=CARTESIAN_POINT('Ctrl Pts',(1.9482293952285,36.3598159578115,13.0895347694922));
#56373=CARTESIAN_POINT('Ctrl Pts',(1.85369636211229,36.4469825000565,13.798453582504));
#56374=CARTESIAN_POINT('Ctrl Pts',(1.47997487612049,36.5510130076167,14.5486099218439));
#56375=CARTESIAN_POINT('Ctrl Pts',(0.566464679004626,36.6888005486365,15.2755886466896));
#56376=CARTESIAN_POINT('Ctrl Pts',(-1.08230306928676,36.8765589250003,15.0981146135781));
#56377=CARTESIAN_POINT('Ctrl Pts',(-2.07361092665276,37.0801652535577,13.5967024919891));
#56378=CARTESIAN_POINT('Ctrl Pts',(-1.53672541544744,37.2835003657197,11.878050082411));
#56379=CARTESIAN_POINT('Ctrl Pts',(-0.287225265330017,37.4364977401447,
11.3697244603319));
#56380=CARTESIAN_POINT('Ctrl Pts',(0.527796451225459,37.5389857152615,11.5096660141286));
#56381=CARTESIAN_POINT('Ctrl Pts',(0.911332139704861,37.5903389447939,11.6650339396913));
#56382=CARTESIAN_POINT('Ctrl Pts',(1.25141660620714,37.6418223573826,11.9028228864947));
#56383=CARTESIAN_POINT('Ctrl Pts',(1.81663055575573,37.745068412759,12.5140494449059));
#56384=CARTESIAN_POINT('Ctrl Pts',(2.08083561316247,37.9010949500106,13.8665607540922));
#56385=CARTESIAN_POINT('Ctrl Pts',(1.09046525980936,38.0772682104256,15.0644393884671));
#56386=CARTESIAN_POINT('Ctrl Pts',(0.0831693118407307,38.2024111697257,
15.2788956384127));
#56387=CARTESIAN_POINT('Ctrl Pts',(-0.493207305974611,38.2744972359008,
15.2113913577473));
#56388=CARTESIAN_POINT('Ctrl Pts',(-1.13701083528365,38.3590598197545,14.9858687442177));
#56389=CARTESIAN_POINT('Ctrl Pts',(-1.62678194860183,38.438406077977,14.5394092422429));
#56390=CARTESIAN_POINT('Ctrl Pts',(-1.89003400591192,38.5124054303739,14.0059075559346));
#56391=CARTESIAN_POINT('Ctrl Pts',(-2.0123635600116,38.5619472407965,13.6273203186704));
#56392=CARTESIAN_POINT('Ctrl Pts',(-2.07807778344679,38.6491924001683,12.9236404751012));
#56393=CARTESIAN_POINT('Ctrl Pts',(-1.70129941197566,38.7817933966652,11.8800756686743));
#56394=CARTESIAN_POINT('Ctrl Pts',(-0.530033200738386,38.9492091008822,
11.08169568024));
#56395=CARTESIAN_POINT('Ctrl Pts',(0.971298069111551,39.1268911505188,11.1790603421398));
#56396=CARTESIAN_POINT('Ctrl Pts',(2.12042035653773,39.3086127292394,12.2018320841821));
#56397=CARTESIAN_POINT('Ctrl Pts',(2.40348688354293,39.4945780381313,13.7505416118132));
#56398=CARTESIAN_POINT('Ctrl Pts',(1.65633965148822,39.6849522632223,15.1783632769377));
#56399=CARTESIAN_POINT('Ctrl Pts',(0.153843856789891,39.8798713203778,15.8603192806378));
#56400=CARTESIAN_POINT('Ctrl Pts',(-1.5117895621889,40.082247120361,15.4578268916728));
#56401=CARTESIAN_POINT('Ctrl Pts',(-2.23537839550422,40.2213853862984,14.5227049097605));
#56402=CARTESIAN_POINT('Ctrl Pts',(-2.40936181605783,40.2932541501529,13.973655276375));
#56403=CARTESIAN_POINT('Ctrl Pts',(-2.92629472497856,29.4179684483559,12.5960680234318));
#56404=CARTESIAN_POINT('Ctrl Pts',(-2.76138775259638,29.5026895656743,11.9375438339818));
#56405=CARTESIAN_POINT('Ctrl Pts',(-1.97719584338124,29.6696011470536,10.758957925939));
#56406=CARTESIAN_POINT('Ctrl Pts',(0.015402096841181,29.9170685318067,10.1112724173248));
#56407=CARTESIAN_POINT('Ctrl Pts',(1.95218792289976,30.160475832036,10.8151677022721));
#56408=CARTESIAN_POINT('Ctrl Pts',(3.03574990303937,30.4015596582338,12.5445656333449));
#56409=CARTESIAN_POINT('Ctrl Pts',(2.82945645491073,30.640115457994,14.5535401432159));
#56410=CARTESIAN_POINT('Ctrl Pts',(1.44515074433655,30.875958282617,15.9940382879077));
#56411=CARTESIAN_POINT('Ctrl Pts',(-0.503543948338917,31.1089181877232,
16.2753332904309));
#56412=CARTESIAN_POINT('Ctrl Pts',(-2.38977678760907,31.3643973010523,15.2037252502747));
#56413=CARTESIAN_POINT('Ctrl Pts',(-2.93561468713809,31.5906395890231,13.2892387819801));
#56414=CARTESIAN_POINT('Ctrl Pts',(-2.31979249603111,31.7888143338793,11.7809918345825));
#56415=CARTESIAN_POINT('Ctrl Pts',(-1.14312719269392,31.9850045730985,10.6794452452593));
#56416=CARTESIAN_POINT('Ctrl Pts',(0.979061516434718,32.2264711689806,10.501921826214));
#56417=CARTESIAN_POINT('Ctrl Pts',(2.73106530068917,32.5100878415069,12.2999468250575));
#56418=CARTESIAN_POINT('Ctrl Pts',(2.44365929372652,32.787535794297,14.7375889155685));
#56419=CARTESIAN_POINT('Ctrl Pts',(0.600736122514384,33.0362449227899,15.9254527144148));
#56420=CARTESIAN_POINT('Ctrl Pts',(-1.24209186022815,33.2579671676477,15.5536554486613));
#56421=CARTESIAN_POINT('Ctrl Pts',(-2.32798389553084,33.4542136726261,14.2984585777842));
#56422=CARTESIAN_POINT('Ctrl Pts',(-2.40845416463362,33.6472578291654,12.6659148675607));
#56423=CARTESIAN_POINT('Ctrl Pts',(-1.48469324396317,33.837219137125,11.3499581269052));
#56424=CARTESIAN_POINT('Ctrl Pts',(0.0293175997728939,34.0242361660808,
10.8866770372192));
#56425=CARTESIAN_POINT('Ctrl Pts',(1.4862388177494,34.2084721656006,11.4438683239473));
#56426=CARTESIAN_POINT('Ctrl Pts',(2.28151421256803,34.3901049120333,12.7599797022223));
#56427=CARTESIAN_POINT('Ctrl Pts',(2.10215476067396,34.5693315081312,14.2667586136253));
#56428=CARTESIAN_POINT('Ctrl Pts',(1.04753394126703,34.7463652392864,15.3317290281059));
#56429=CARTESIAN_POINT('Ctrl Pts',(-0.422450344249625,34.9214325139325,
15.521267960528));
#56430=CARTESIAN_POINT('Ctrl Pts',(-1.68574655436693,35.0947769203036,14.7745304523423));
#56431=CARTESIAN_POINT('Ctrl Pts',(-2.21864288212407,35.2666485810103,13.4204718245856));
#56432=CARTESIAN_POINT('Ctrl Pts',(-1.80906271554523,35.4373090813338,12.0348032210116));
#56433=CARTESIAN_POINT('Ctrl Pts',(-0.642302665493085,35.6070351214264,
11.1969323185357));
#56434=CARTESIAN_POINT('Ctrl Pts',(0.789341950991395,35.7760953652428,11.2553442171803));
#56435=CARTESIAN_POINT('Ctrl Pts',(1.75615824041296,35.9260332895441,12.0758907724877));
#56436=CARTESIAN_POINT('Ctrl Pts',(2.09012664466646,36.0571669403208,13.100444798061));
#56437=CARTESIAN_POINT('Ctrl Pts',(1.99369880813117,36.1508702947937,13.8633320157786));
#56438=CARTESIAN_POINT('Ctrl Pts',(1.59431997007155,36.2634037419873,14.6772718381349));
#56439=CARTESIAN_POINT('Ctrl Pts',(0.604424275445722,36.4136786035501,15.4777199943844));
#56440=CARTESIAN_POINT('Ctrl Pts',(-1.22018400546081,36.6212451623359,15.2974085367834));
#56441=CARTESIAN_POINT('Ctrl Pts',(-2.34526308970448,36.8494970463802,13.6232597140238));
#56442=CARTESIAN_POINT('Ctrl Pts',(-1.75053035885031,37.0802123528408,11.6681136226245));
#56443=CARTESIAN_POINT('Ctrl Pts',(-0.322212675623461,37.2555496913766,
11.076003369181));
#56444=CARTESIAN_POINT('Ctrl Pts',(0.617280561858399,37.3735732858669,11.232771728576));
#56445=CARTESIAN_POINT('Ctrl Pts',(1.06059919597652,37.432818095883,11.4099591023423));
#56446=CARTESIAN_POINT('Ctrl Pts',(1.45487125813752,37.4923081870011,11.6829606520691));
#56447=CARTESIAN_POINT('Ctrl Pts',(2.11223415117922,37.6117895248485,12.387289389157));
#56448=CARTESIAN_POINT('Ctrl Pts',(2.42724419526393,37.7929549642751,13.9563315796829));
#56449=CARTESIAN_POINT('Ctrl Pts',(1.28030667711334,37.998112670535,15.3568131965243));
#56450=CARTESIAN_POINT('Ctrl Pts',(0.107531631002896,38.1439241470239,15.611556567592));
#56451=CARTESIAN_POINT('Ctrl Pts',(-0.564258585336392,38.2278995539426,
15.5356922322688));
#56452=CARTESIAN_POINT('Ctrl Pts',(-1.3152122433605,38.3263864203009,15.2760924235049));
#56453=CARTESIAN_POINT('Ctrl Pts',(-1.8872897452656,38.4187324752531,14.7586807581235));
#56454=CARTESIAN_POINT('Ctrl Pts',(-2.19582729846917,38.504752419654,14.1397159838506));
#56455=CARTESIAN_POINT('Ctrl Pts',(-2.33973729772146,38.5623090280121,13.7004335879123));
#56456=CARTESIAN_POINT('Ctrl Pts',(-2.41926993441258,38.6635838660802,12.883831736637));
#56457=CARTESIAN_POINT('Ctrl Pts',(-1.98711383676784,38.8171825551677,11.6733444960647));
#56458=CARTESIAN_POINT('Ctrl Pts',(-0.638418491717066,39.0103777078726,
10.7475025569123));
#56459=CARTESIAN_POINT('Ctrl Pts',(1.08598908609963,39.2144028706223,10.8539224233017));
#56460=CARTESIAN_POINT('Ctrl Pts',(2.40151564006302,39.4218705163401,12.0176971105041));
#56461=CARTESIAN_POINT('Ctrl Pts',(2.72774771937741,39.6328055416103,13.7735316474361));
#56462=CARTESIAN_POINT('Ctrl Pts',(1.89084099938846,39.8472061753517,15.384068077044));
#56463=CARTESIAN_POINT('Ctrl Pts',(0.213666374113039,40.0650504690902,16.1509694319914));
#56464=CARTESIAN_POINT('Ctrl Pts',(-1.63409073970178,40.2893948535753,15.7098779610265));
#56465=CARTESIAN_POINT('Ctrl Pts',(-2.43214397021945,40.4423057604741,14.6842115864192));
#56466=CARTESIAN_POINT('Ctrl Pts',(-2.62499374027519,40.5209217307929,14.0844157329642));
#56467=CARTESIAN_POINT('Ctrl Pts',(-2.68901637473833,29.6258508348922,12.7013421571086));
#56468=CARTESIAN_POINT('Ctrl Pts',(-2.54192391625449,29.7034474026606,12.097134838509));
#56469=CARTESIAN_POINT('Ctrl Pts',(-1.83214692652542,29.8557848602106,11.0174310075307));
#56470=CARTESIAN_POINT('Ctrl Pts',(-0.0285161129234559,30.0801906025827,
10.4195088213662));
#56471=CARTESIAN_POINT('Ctrl Pts',(1.72137134294901,30.2996087065708,11.0434127561354));
#56472=CARTESIAN_POINT('Ctrl Pts',(2.70282908524349,30.5157541374752,12.5878192971209));
#56473=CARTESIAN_POINT('Ctrl Pts',(2.53070359956114,30.7285916653165,14.3815755859622));
#56474=CARTESIAN_POINT('Ctrl Pts',(1.30974294253613,30.9381078531812,15.6699224391317));
#56475=CARTESIAN_POINT('Ctrl Pts',(-0.413511312952687,31.1443123212953,
15.9314439612661));
#56476=CARTESIAN_POINT('Ctrl Pts',(-2.08540704977334,31.3697825407651,14.9981264331597));
#56477=CARTESIAN_POINT('Ctrl Pts',(-2.57894541282835,31.5689416522291,13.3163300617175));
#56478=CARTESIAN_POINT('Ctrl Pts',(-2.04836715080512,31.7431943139094,11.9855615775284));
#56479=CARTESIAN_POINT('Ctrl Pts',(-1.02209358337669,31.915639147058,11.0085761338793));
#56480=CARTESIAN_POINT('Ctrl Pts',(0.842033459968995,32.1278756568622,10.8362974613168));
#56481=CARTESIAN_POINT('Ctrl Pts',(2.39921103983848,32.3775873659353,12.4051582755859));
#56482=CARTESIAN_POINT('Ctrl Pts',(2.16635720525591,32.622691108358,14.5613661094194));
#56483=CARTESIAN_POINT('Ctrl Pts',(0.540386488651459,32.8435307255826,15.632877368845));
#56484=CARTESIAN_POINT('Ctrl Pts',(-1.10950126361728,33.0416124732336,15.3169281210652));
#56485=CARTESIAN_POINT('Ctrl Pts',(-2.09697701732676,33.2180215832585,14.1981125985888));
#56486=CARTESIAN_POINT('Ctrl Pts',(-2.18472365563727,33.3928081266097,12.7204450451649));
#56487=CARTESIAN_POINT('Ctrl Pts',(-1.35351454758958,33.5662121577014,11.5104403890166));
#56488=CARTESIAN_POINT('Ctrl Pts',(0.0370115243192905,33.7384826720109,
11.0694522056516));
#56489=CARTESIAN_POINT('Ctrl Pts',(1.39792058393044,33.9098837597389,11.5741517956677));
#56490=CARTESIAN_POINT('Ctrl Pts',(2.15835181775678,34.0806787676664,12.8043966294061));
#56491=CARTESIAN_POINT('Ctrl Pts',(2.00203261382117,34.2511380206756,14.2394096952522));
#56492=CARTESIAN_POINT('Ctrl Pts',(0.996842548153175,34.4215336196919,15.274581368401));
#56493=CARTESIAN_POINT('Ctrl Pts',(-0.434133599572046,34.5921366834918,
15.4730820151823));
#56494=CARTESIAN_POINT('Ctrl Pts',(-1.6880779760544,34.7632210511842,14.747614006186));
#56495=CARTESIAN_POINT('Ctrl Pts',(-2.23323794654136,34.9350518282015,13.3984655010846));
#56496=CARTESIAN_POINT('Ctrl Pts',(-1.83062979668189,35.1078910573438,11.9911944854927));
#56497=CARTESIAN_POINT('Ctrl Pts',(-0.64082647588313,35.2820001958536,11.121557924252));
#56498=CARTESIAN_POINT('Ctrl Pts',(0.847153684037699,35.4576194968682,11.1701958567181));
#56499=CARTESIAN_POINT('Ctrl Pts',(1.87051790069932,35.6152820367172,12.0255127586967));
#56500=CARTESIAN_POINT('Ctrl Pts',(2.23202389410442,35.7545179228302,13.1113548266299));
#56501=CARTESIAN_POINT('Ctrl Pts',(2.13370125415005,35.8547580895309,13.9282104490533));
#56502=CARTESIAN_POINT('Ctrl Pts',(1.70866506402261,35.975794476358,14.8059337544259));
#56503=CARTESIAN_POINT('Ctrl Pts',(0.642383871886817,36.1385566584636,15.6798513420792));
#56504=CARTESIAN_POINT('Ctrl Pts',(-1.35806494163484,36.3659313996715,15.4967024599889));
#56505=CARTESIAN_POINT('Ctrl Pts',(-2.61691525275619,36.6188288392025,13.6498169360587));
#56506=CARTESIAN_POINT('Ctrl Pts',(-1.96433530225319,36.8769243399619,11.4581771628379));
#56507=CARTESIAN_POINT('Ctrl Pts',(-0.3572000859169,37.0746016426084,10.7822822780298));
#56508=CARTESIAN_POINT('Ctrl Pts',(0.706764672491346,37.2081608564722,10.9558774430233));
#56509=CARTESIAN_POINT('Ctrl Pts',(1.20986625224818,37.2752972469721,11.1548842649935));
#56510=CARTESIAN_POINT('Ctrl Pts',(1.65832591006791,37.3427940166194,11.4630984176435));
#56511=CARTESIAN_POINT('Ctrl Pts',(2.40783774660274,37.4785106369379,12.260529333408));
#56512=CARTESIAN_POINT('Ctrl Pts',(2.7736527773654,37.6848149785396,14.0461024052735));
#56513=CARTESIAN_POINT('Ctrl Pts',(1.47014809441732,37.9189571306446,15.6491870045816));
#56514=CARTESIAN_POINT('Ctrl Pts',(0.131893950165078,38.0854371243222,15.9442174967714));
#56515=CARTESIAN_POINT('Ctrl Pts',(-0.635309864698155,38.1813018719843,
15.8599931067902));
#56516=CARTESIAN_POINT('Ctrl Pts',(-1.49341365143733,38.2937130208473,15.5663161027921));
#56517=CARTESIAN_POINT('Ctrl Pts',(-2.14779754192937,38.3990588725292,14.9779522740042));
#56518=CARTESIAN_POINT('Ctrl Pts',(-2.50162059102639,38.4970994089341,14.2735244117667));
#56519=CARTESIAN_POINT('Ctrl Pts',(-2.6671110354313,38.5626708152278,13.7735468571544));
#56520=CARTESIAN_POINT('Ctrl Pts',(-2.76046208537834,38.6779753319921,12.8440229981729));
#56521=CARTESIAN_POINT('Ctrl Pts',(-2.27292826156003,38.8525717136702,11.4666133234551));
#56522=CARTESIAN_POINT('Ctrl Pts',(-0.746803782695733,39.0715463148632,
10.4133094335848));
#56523=CARTESIAN_POINT('Ctrl Pts',(1.20068010308772,39.3019145907256,10.5287845044635));
#56524=CARTESIAN_POINT('Ctrl Pts',(2.68261092358831,39.5351283034409,11.833562136826));
#56525=CARTESIAN_POINT('Ctrl Pts',(3.05200855521192,39.7710330450894,13.796521683059));
#56526=CARTESIAN_POINT('Ctrl Pts',(2.12534234728874,40.0094600874809,15.5897728771503));
#56527=CARTESIAN_POINT('Ctrl Pts',(0.273488891436192,40.2502296178026,16.441619583345));
#56528=CARTESIAN_POINT('Ctrl Pts',(-1.75639191721469,40.4965425867897,15.9619290303801));
#56529=CARTESIAN_POINT('Ctrl Pts',(-2.62890954493469,40.66322613465,14.8457182630777));
#56530=CARTESIAN_POINT('Ctrl Pts',(-2.84062566449253,40.7485893114329,14.1951761895533));
#56531=CARTESIAN_POINT('Ctrl Pts',(-2.45173802449808,29.8337332214285,12.8066162907855));
#56532=CARTESIAN_POINT('Ctrl Pts',(-2.32246007991259,29.9042052396469,12.2567258430361));
#56533=CARTESIAN_POINT('Ctrl Pts',(-1.68709800966959,30.0419685733677,11.2759040891224));
#56534=CARTESIAN_POINT('Ctrl Pts',(-0.0724343226880954,30.2433126733586,
10.7277452254075));
#56535=CARTESIAN_POINT('Ctrl Pts',(1.49055476299827,30.4387415811056,11.2716578099989));
#56536=CARTESIAN_POINT('Ctrl Pts',(2.36990826744761,30.6299486167167,12.6310729608969));
#56537=CARTESIAN_POINT('Ctrl Pts',(2.23195074421154,30.8170678726391,14.2096110287086));
#56538=CARTESIAN_POINT('Ctrl Pts',(1.17433514073571,31.0002574237457,15.3458065903555));
#56539=CARTESIAN_POINT('Ctrl Pts',(-0.323478677566458,31.1797064548672,
15.5875546321013));
#56540=CARTESIAN_POINT('Ctrl Pts',(-1.78103731193763,31.3751677804782,14.7925276160446));
#56541=CARTESIAN_POINT('Ctrl Pts',(-2.22227613851859,31.5472437154351,13.3434213414549));
#56542=CARTESIAN_POINT('Ctrl Pts',(-1.77694180557915,31.6975742939395,12.1901313204743));
#56543=CARTESIAN_POINT('Ctrl Pts',(-0.901059974059453,31.8462737210174,
11.3377070224995));
#56544=CARTESIAN_POINT('Ctrl Pts',(0.705005403503267,32.0292801447437,11.1706730964197));
#56545=CARTESIAN_POINT('Ctrl Pts',(2.06735677898778,32.2450868903637,12.5103697261144));
#56546=CARTESIAN_POINT('Ctrl Pts',(1.88905511678531,32.4578464224189,14.3851433032702));
#56547=CARTESIAN_POINT('Ctrl Pts',(0.480036854788531,32.6508165283753,15.3403020232754));
#56548=CARTESIAN_POINT('Ctrl Pts',(-0.976910667006417,32.8252577788194,
15.080200793469));
#56549=CARTESIAN_POINT('Ctrl Pts',(-1.86597013912268,32.981829493891,14.0977666193934));
#56550=CARTESIAN_POINT('Ctrl Pts',(-1.9609931466409,33.138358424054,12.7749752227692));
#56551=CARTESIAN_POINT('Ctrl Pts',(-1.222335851216,33.295205178278,11.6709226511278));
#56552=CARTESIAN_POINT('Ctrl Pts',(0.0447054488656896,33.4527291779409,
11.2522273740842));
#56553=CARTESIAN_POINT('Ctrl Pts',(1.30960235011147,33.6112953538774,11.7044352673884));
#56554=CARTESIAN_POINT('Ctrl Pts',(2.03518942294553,33.7712526232996,12.8488135565898));
#56555=CARTESIAN_POINT('Ctrl Pts',(1.90191046696839,33.9329445332202,14.2120607768793));
#56556=CARTESIAN_POINT('Ctrl Pts',(0.946151155039321,34.0967020000973,15.2174337086961));
#56557=CARTESIAN_POINT('Ctrl Pts',(-0.445816854894472,34.262840853051,15.4248960698368));
#56558=CARTESIAN_POINT('Ctrl Pts',(-1.69040939774186,34.4316651820648,14.7206975600299));
#56559=CARTESIAN_POINT('Ctrl Pts',(-2.24783301095865,34.6034550753927,13.3764591775835));
#56560=CARTESIAN_POINT('Ctrl Pts',(-1.85219687781853,34.7784730333538,11.9475857499739));
#56561=CARTESIAN_POINT('Ctrl Pts',(-0.639350286273178,34.956965270281,11.0461835299682));
#56562=CARTESIAN_POINT('Ctrl Pts',(0.904965417084006,35.1391436284935,11.0850474962561));
#56563=CARTESIAN_POINT('Ctrl Pts',(1.98487756098567,35.3045307838904,11.9751347449056));
#56564=CARTESIAN_POINT('Ctrl Pts',(2.37392114354237,35.4518689053395,13.1222648551988));
#56565=CARTESIAN_POINT('Ctrl Pts',(2.27370370016894,35.5586458842682,13.9930888823279));
#56566=CARTESIAN_POINT('Ctrl Pts',(1.82301015797368,35.6881852107287,14.9345956707169));
#56567=CARTESIAN_POINT('Ctrl Pts',(0.680343468327914,35.8634347133772,15.8819826897739));
#56568=CARTESIAN_POINT('Ctrl Pts',(-1.49594587780887,36.1106176370072,15.6959963831942));
#56569=CARTESIAN_POINT('Ctrl Pts',(-2.8885674158079,36.388160632025,13.6763741580934));
#56570=CARTESIAN_POINT('Ctrl Pts',(-2.17814024565606,36.6736363270831,11.2482407030514));
#56571=CARTESIAN_POINT('Ctrl Pts',(-0.392187496210338,36.8936535938402,
10.4885611868789));
#56572=CARTESIAN_POINT('Ctrl Pts',(0.796248783124293,37.0427484270776,10.6789831574706));
#56573=CARTESIAN_POINT('Ctrl Pts',(1.35913330851984,37.1177763980612,10.8998094276445));
#56574=CARTESIAN_POINT('Ctrl Pts',(1.8617805619983,37.1932798462378,11.2432361832178));
#56575=CARTESIAN_POINT('Ctrl Pts',(2.70344134202624,37.3452317490274,12.133769277659));
#56576=CARTESIAN_POINT('Ctrl Pts',(3.12006135946686,37.576674992804,14.1358732308642));
#56577=CARTESIAN_POINT('Ctrl Pts',(1.65998951172128,37.8398015907541,15.9415608126388));
#56578=CARTESIAN_POINT('Ctrl Pts',(0.156256269327249,38.0269501016204,16.2768784259508));
#56579=CARTESIAN_POINT('Ctrl Pts',(-0.70636114405993,38.134704190026,16.1842939813117));
#56580=CARTESIAN_POINT('Ctrl Pts',(-1.67161505951417,38.2610396213937,15.8565397820794));
#56581=CARTESIAN_POINT('Ctrl Pts',(-2.40830533859313,38.3793852698053,15.1972237898848));
#56582=CARTESIAN_POINT('Ctrl Pts',(-2.80741388358363,38.4894463982141,14.4073328396828));
#56583=CARTESIAN_POINT('Ctrl Pts',(-2.99448477314115,38.5630326024434,13.8466601263963));
#56584=CARTESIAN_POINT('Ctrl Pts',(-3.10165423634411,38.692366797904,12.8042142597087));
#56585=CARTESIAN_POINT('Ctrl Pts',(-2.55874268635221,38.8879608721727,11.2598821508456));
#56586=CARTESIAN_POINT('Ctrl Pts',(-0.85518907367441,39.1327149218537,10.0791163102571));
#56587=CARTESIAN_POINT('Ctrl Pts',(1.3153711200758,39.3894263108291,10.2036465856254));
#56588=CARTESIAN_POINT('Ctrl Pts',(2.9637062071136,39.6483860905416,11.649427163148));
#56589=CARTESIAN_POINT('Ctrl Pts',(3.37626939104641,39.9092605485685,13.8195117186819));
#56590=CARTESIAN_POINT('Ctrl Pts',(2.35984369518899,40.1717139996104,15.7954776772565));
#56591=CARTESIAN_POINT('Ctrl Pts',(0.333311408759341,40.435408766515,16.7322697346985));
#56592=CARTESIAN_POINT('Ctrl Pts',(-1.87869309472757,40.703690320004,16.2139800997338));
#56593=CARTESIAN_POINT('Ctrl Pts',(-2.82567511964993,40.8841465088258,15.0072249397364));
#56594=CARTESIAN_POINT('Ctrl Pts',(-3.05625758870988,40.9762568920729,14.3059366461423));
#56595=CARTESIAN_POINT('Ctrl Pts',(-2.44274827128758,29.838337858154,12.7680189512445));
#56596=CARTESIAN_POINT('Ctrl Pts',(-2.42196823404112,29.8489350089282,12.6853451231868));
#56597=CARTESIAN_POINT('Ctrl Pts',(-2.39698720300911,29.8595261018564,12.6038716896438));
#56598=CARTESIAN_POINT('Ctrl Pts',(-2.36787154345866,29.8701089694672,12.5240551021937));
#56599=CARTESIAN_POINT('Ctrl Pts',(-2.31025919725116,29.8910497223843,12.3661187565886));
#56600=CARTESIAN_POINT('Ctrl Pts',(-2.23645492891969,29.9119582841016,12.2146710441957));
#56601=CARTESIAN_POINT('Ctrl Pts',(-2.14864857255502,29.932817762837,12.0724757850767));
#56602=CARTESIAN_POINT('Ctrl Pts',(-2.06203074205937,29.9533948926501,11.9322052470248));
#56603=CARTESIAN_POINT('Ctrl Pts',(-1.96178841628673,29.9739242552252,11.8009397307871));
#56604=CARTESIAN_POINT('Ctrl Pts',(-1.85006327768778,29.9943894361018,11.68130383456));
#56605=CARTESIAN_POINT('Ctrl Pts',(-1.79581670015234,30.0043260182813,11.6232162993635));
#56606=CARTESIAN_POINT('Ctrl Pts',(-1.73886360095515,30.0142474672897,11.5678698348704));
#56607=CARTESIAN_POINT('Ctrl Pts',(-1.67945137841709,30.0241518912863,11.515560943049));
#56608=CARTESIAN_POINT('Ctrl Pts',(-1.64243351653922,30.0303230221383,11.4829689400956));
#56609=CARTESIAN_POINT('Ctrl Pts',(-1.60446101984903,30.0364875434917,11.4515561004382));
#56610=CARTESIAN_POINT('Ctrl Pts',(-1.56561882847456,30.0426450002698,11.4213583465077));
#56611=CARTESIAN_POINT('Ctrl Pts',(-1.45706661729979,30.059853235048,11.3369647310686));
#56612=CARTESIAN_POINT('Ctrl Pts',(-1.34152150050918,30.0769963094119,11.2619269962897));
#56613=CARTESIAN_POINT('Ctrl Pts',(-1.22082683447683,30.09408254954,11.1971234500698));
#56614=CARTESIAN_POINT('Ctrl Pts',(-1.09768405092722,30.1115153594475,11.1310054572227));
#56615=CARTESIAN_POINT('Ctrl Pts',(-0.969181964878691,30.1288890092631,
11.0755416740165));
#56616=CARTESIAN_POINT('Ctrl Pts',(-0.837309041203365,30.1462130613069,
11.0316212565457));
#56617=CARTESIAN_POINT('Ctrl Pts',(-0.762543115457978,30.1560350077127,
11.0067203854662));
#56618=CARTESIAN_POINT('Ctrl Pts',(-0.686694124051804,30.1658410243016,
10.9855291380402));
#56619=CARTESIAN_POINT('Ctrl Pts',(-0.610126278689872,30.1756329466738,
10.9682023184446));
#56620=CARTESIAN_POINT('Ctrl Pts',(-0.474744503754916,30.1929463218185,
10.9375662782146));
#56621=CARTESIAN_POINT('Ctrl Pts',(-0.337116377370077,30.2102156045636,
10.9190142580986));
#56622=CARTESIAN_POINT('Ctrl Pts',(-0.199388743815463,30.2274514298725,
10.9122941898254));
#56623=CARTESIAN_POINT('Ctrl Pts',(-0.159208742874418,30.232479727094,10.9103337092554));
#56624=CARTESIAN_POINT('Ctrl Pts',(-0.119020181269218,30.2375051802885,
10.9093799156681));
#56625=CARTESIAN_POINT('Ctrl Pts',(-0.0788760557749174,30.242528061848,
10.9094257637442));
#56626=CARTESIAN_POINT('Ctrl Pts',(0.0678310697193201,30.2608842349174,
10.9095933160168));
#56627=CARTESIAN_POINT('Ctrl Pts',(0.214244052085658,30.2791737309075,10.9231318775133));
#56628=CARTESIAN_POINT('Ctrl Pts',(0.35778396157455,30.2973981541035,10.9498237837861));
#56629=CARTESIAN_POINT('Ctrl Pts',(0.429694880758075,30.3065282631323,10.9631959499081));
#56630=CARTESIAN_POINT('Ctrl Pts',(0.500884521694379,30.315642047562,10.979868550339));
#56631=CARTESIAN_POINT('Ctrl Pts',(0.571028493519116,30.3247397523455,10.9998093390544));
#56632=CARTESIAN_POINT('Ctrl Pts',(0.717608994568639,30.3437513094454,11.0414797880635));
#56633=CARTESIAN_POINT('Ctrl Pts',(0.859621141625087,30.3626926187303,11.0974254453251));
#56634=CARTESIAN_POINT('Ctrl Pts',(0.994627001001719,30.3815664136494,11.1660292863854));
#56635=CARTESIAN_POINT('Ctrl Pts',(1.12273921019856,30.3994764775102,11.2311300877743));
#56636=CARTESIAN_POINT('Ctrl Pts',(1.24454136035637,30.4173257532032,11.3076281085764));
#56637=CARTESIAN_POINT('Ctrl Pts',(1.35798428375087,30.4351169376783,11.3941042276715));
#56638=CARTESIAN_POINT('Ctrl Pts',(1.36408858742464,30.4360742718998,11.3987574618767));
#56639=CARTESIAN_POINT('Ctrl Pts',(1.3701686979687,30.4370314379966,11.4034395804063));
#56640=CARTESIAN_POINT('Ctrl Pts',(1.37622429993115,30.4379884364142,11.4081503599416));
#56641=CARTESIAN_POINT('Ctrl Pts',(1.44635601674792,30.4490717180495,11.4627072905992));
#56642=CARTESIAN_POINT('Ctrl Pts',(1.51327887302001,30.4601379581592,11.5211715138177));
#56643=CARTESIAN_POINT('Ctrl Pts',(1.57648124486681,30.4711863237015,11.5832172662626));
#56644=CARTESIAN_POINT('Ctrl Pts',(1.67691112938004,30.4887424065359,11.6818092584696));
#56645=CARTESIAN_POINT('Ctrl Pts',(1.76794459317642,30.5062533435147,11.7894464993758));
#56646=CARTESIAN_POINT('Ctrl Pts',(1.84846801190238,30.5237160607871,11.9040329244706));
#56647=CARTESIAN_POINT('Ctrl Pts',(1.92946837864217,30.5412822114265,12.0192980560675));
#56648=CARTESIAN_POINT('Ctrl Pts',(1.99983309317883,30.5587995713156,12.1415935824012));
#56649=CARTESIAN_POINT('Ctrl Pts',(2.05846999096913,30.5762652652364,12.2687553226759));
#56650=CARTESIAN_POINT('Ctrl Pts',(2.10222528400445,30.5892982970707,12.3636443672583));
#56651=CARTESIAN_POINT('Ctrl Pts',(2.13945102208768,30.6023025653927,12.4612422930058));
#56652=CARTESIAN_POINT('Ctrl Pts',(2.16971195499725,30.6152769569668,12.5606457179209));
#56653=CARTESIAN_POINT('Ctrl Pts',(2.18052629082065,30.6199136093796,12.5961694746484));
#56654=CARTESIAN_POINT('Ctrl Pts',(2.19045129627119,30.6245464467463,12.631923811111));
#56655=CARTESIAN_POINT('Ctrl Pts',(2.19948820868409,30.6291754219654,12.6678632506624));
#56656=CARTESIAN_POINT('Ctrl Pts',(2.23322305814674,30.6464554148488,12.8020253989318));
#56657=CARTESIAN_POINT('Ctrl Pts',(2.25463691153548,30.6636810587727,12.9390103776527));
#56658=CARTESIAN_POINT('Ctrl Pts',(2.26369433941869,30.6808537617852,13.0764695738017));
#56659=CARTESIAN_POINT('Ctrl Pts',(2.27294068816789,30.6983846549999,13.2167959095747));
#56660=CARTESIAN_POINT('Ctrl Pts',(2.26930961671449,30.7158603786077,13.3576149318399));
#56661=CARTESIAN_POINT('Ctrl Pts',(2.25281502826568,30.7332826999064,13.4964154152252));
#56662=CARTESIAN_POINT('Ctrl Pts',(2.24530913109389,30.741210763863,13.5595768671716));
#56663=CARTESIAN_POINT('Ctrl Pts',(2.23514026573485,30.7491277730461,13.6223203079521));
#56664=CARTESIAN_POINT('Ctrl Pts',(2.22231329878194,30.757033909312,13.6844096143821));
#56665=CARTESIAN_POINT('Ctrl Pts',(2.19406213713589,30.7744470307822,13.8211601836231));
#56666=CARTESIAN_POINT('Ctrl Pts',(2.15291407120517,30.7918073982712,13.9547354647172));
#56667=CARTESIAN_POINT('Ctrl Pts',(2.10014400624926,30.809117156191,14.0830014177723));
#56668=CARTESIAN_POINT('Ctrl Pts',(2.09289656173198,30.811494479589,14.1006174729923));
#56669=CARTESIAN_POINT('Ctrl Pts',(2.08542996170936,30.8138708486099,14.1181334333907));
#56670=CARTESIAN_POINT('Ctrl Pts',(2.07774756551514,30.8162462690207,14.1355438241986));
#56671=CARTESIAN_POINT('Ctrl Pts',(2.02467765540868,30.8326556476153,14.2558146162445));
#56672=CARTESIAN_POINT('Ctrl Pts',(1.96120585753199,30.8490178230599,14.3712740668969));
#56673=CARTESIAN_POINT('Ctrl Pts',(1.88835924779461,30.8653347463125,14.48005627632));
#56674=CARTESIAN_POINT('Ctrl Pts',(1.8418770836055,30.8757462933759,14.5494683263453));
#56675=CARTESIAN_POINT('Ctrl Pts',(1.79157910837346,30.8861394205734,14.6161618235882));
#56676=CARTESIAN_POINT('Ctrl Pts',(1.73774244381333,30.8965146738698,14.6796559969216));
#56677=CARTESIAN_POINT('Ctrl Pts',(1.65276651649938,30.9128909998771,14.7798753604747));
#56678=CARTESIAN_POINT('Ctrl Pts',(1.55897310285119,30.929222790903,14.8721217226433));
#56679=CARTESIAN_POINT('Ctrl Pts',(1.45818189935036,30.9455123441436,14.9552484286278));
#56680=CARTESIAN_POINT('Ctrl Pts',(1.35899011513395,30.9615434043345,15.0370560268728));
#56681=CARTESIAN_POINT('Ctrl Pts',(1.25302215367939,30.9775335605754,15.1100304370351));
#56682=CARTESIAN_POINT('Ctrl Pts',(1.14203363308923,30.9934850837824,15.1731235323804));
#56683=CARTESIAN_POINT('Ctrl Pts',(1.12828417076023,30.9954611878539,15.180939621225));
#56684=CARTESIAN_POINT('Ctrl Pts',(1.11445767230228,30.9974366990959,15.1886041290523));
#56685=CARTESIAN_POINT('Ctrl Pts',(1.10055748367544,30.9994116218689,15.1961151198218));
#56686=CARTESIAN_POINT('Ctrl Pts',(1.01945222563121,31.0109349634163,15.239940485137));
#56687=CARTESIAN_POINT('Ctrl Pts',(0.935736602491525,31.0224359380682,15.2785957311915));
#56688=CARTESIAN_POINT('Ctrl Pts',(0.850042474603389,31.0339140990372,15.3116694251567));
#56689=CARTESIAN_POINT('Ctrl Pts',(0.697695191681105,31.0543200087496,15.3704679395469));
#56690=CARTESIAN_POINT('Ctrl Pts',(0.53909305013005,31.0746538032239,15.4116226011244));
#56691=CARTESIAN_POINT('Ctrl Pts',(0.378368286442902,31.0949133795375,15.4348761056207));
#56692=CARTESIAN_POINT('Ctrl Pts',(0.210968964531451,31.1160142930453,15.4590952787925));
#56693=CARTESIAN_POINT('Ctrl Pts',(0.0412688522094594,31.1370346971868,
15.463895194311));
#56694=CARTESIAN_POINT('Ctrl Pts',(-0.126042124647733,31.1579724194978,
15.4490351635858));
#56695=CARTESIAN_POINT('Ctrl Pts',(-0.155858747679507,31.1617037477407,
15.4463869456225));
#56696=CARTESIAN_POINT('Ctrl Pts',(-0.185599483668016,31.16543245056,15.4431144788636));
#56697=CARTESIAN_POINT('Ctrl Pts',(-0.215237792528509,31.1691585162582,
15.4392165752889));
#56698=CARTESIAN_POINT('Ctrl Pts',(-0.241067690235736,31.1724057965361,
15.435819537655));
#56699=CARTESIAN_POINT('Ctrl Pts',(-0.26681979264175,31.1756510738736,15.4319474699778));
#56700=CARTESIAN_POINT('Ctrl Pts',(-0.292478263844604,31.1788943402646,
15.4276076162629));
#56701=CARTESIAN_POINT('Ctrl Pts',(-0.404942206081367,31.1931099387376,
15.4085855531928));
#56702=CARTESIAN_POINT('Ctrl Pts',(-0.515745857045101,31.2072831735665,
15.3805525726697));
#56703=CARTESIAN_POINT('Ctrl Pts',(-0.623480220379473,31.2214215485108,
15.3440899505627));
#56704=CARTESIAN_POINT('Ctrl Pts',(-0.732116475755987,31.2356782820499,
15.3073220837066));
#56705=CARTESIAN_POINT('Ctrl Pts',(-0.837630583917693,31.2498995747238,
15.2619832741019));
#56706=CARTESIAN_POINT('Ctrl Pts',(-0.938587011709799,31.264093035378,15.2087209901736));
#56707=CARTESIAN_POINT('Ctrl Pts',(-1.02874118139081,31.276767806942,15.1611577285975));
#56708=CARTESIAN_POINT('Ctrl Pts',(-1.11526033311846,31.2894203850643,15.1072768321492));
#56709=CARTESIAN_POINT('Ctrl Pts',(-1.19714077195967,31.3020560818323,15.0475692572935));
#56710=CARTESIAN_POINT('Ctrl Pts',(-1.2887998903919,31.3162008133813,14.9807310264236));
#56711=CARTESIAN_POINT('Ctrl Pts',(-1.37464498386398,31.330324398641,14.9065918943779));
#56712=CARTESIAN_POINT('Ctrl Pts',(-1.45380783575241,31.3444342064886,14.8264398549102));
#56713=CARTESIAN_POINT('Ctrl Pts',(-1.47311040217982,31.3478746523134,14.8068960912735));
#56714=CARTESIAN_POINT('Ctrl Pts',(-1.49201589588182,31.3513142777609,14.7869949336528));
#56715=CARTESIAN_POINT('Ctrl Pts',(-1.51051217688639,31.3547531871258,14.7667552233025));
#56716=CARTESIAN_POINT('Ctrl Pts',(-1.59341041892996,31.3701659904255,14.6760431278765));
#56717=CARTESIAN_POINT('Ctrl Pts',(-1.66839697393664,31.3855608261987,14.5782105380559));
#56718=CARTESIAN_POINT('Ctrl Pts',(-1.73426396540107,31.4009219748068,14.4748066584378));
#56719=CARTESIAN_POINT('Ctrl Pts',(-1.78136888379819,31.411907532756,14.4008571550058));
#56720=CARTESIAN_POINT('Ctrl Pts',(-1.8238100093497,31.4228758696061,14.324059535432));
#56721=CARTESIAN_POINT('Ctrl Pts',(-1.86115467699472,31.4338213642457,14.2449938261685));
#56722=CARTESIAN_POINT('Ctrl Pts',(-1.91439815727384,31.4494267040368,14.132267330061));
#56723=CARTESIAN_POINT('Ctrl Pts',(-1.95727950591873,31.4649855913012,14.0149300293415));
#56724=CARTESIAN_POINT('Ctrl Pts',(-1.98947075991055,31.4804820573484,13.8950139757259));
#56725=CARTESIAN_POINT('Ctrl Pts',(-2.02139363255055,31.4958493279778,13.7760976729303));
#56726=CARTESIAN_POINT('Ctrl Pts',(-2.04280382665317,31.5111552129038,13.654646979972));
#56727=CARTESIAN_POINT('Ctrl Pts',(-2.05343045590844,31.5263846168744,13.5326520605381));
#56728=CARTESIAN_POINT('Ctrl Pts',(-2.06203008984398,31.5387090610662,13.4339272792433));
#56729=CARTESIAN_POINT('Ctrl Pts',(-2.06356855702891,31.550983427265,13.3348465698476));
#56730=CARTESIAN_POINT('Ctrl Pts',(-2.05792666153141,31.5631999535903,13.2364585189257));
#56731=CARTESIAN_POINT('Ctrl Pts',(-2.05465700605132,31.570279813943,13.1794395560583));
#56732=CARTESIAN_POINT('Ctrl Pts',(-2.04897624877365,31.5773402524126,13.1226530653411));
#56733=CARTESIAN_POINT('Ctrl Pts',(-2.04096326871604,31.5843798059197,13.0662885712664));
#56734=CARTESIAN_POINT('Ctrl Pts',(-2.01971503210113,31.6030467809409,12.9168253131316));
#56735=CARTESIAN_POINT('Ctrl Pts',(-1.98187006982237,31.6219887666393,12.769983414429));
#56736=CARTESIAN_POINT('Ctrl Pts',(-1.92874023134007,31.6409279597721,12.6292055825379));
#56737=CARTESIAN_POINT('Ctrl Pts',(-1.88143333025758,31.657791450453,12.503856754871));
#56738=CARTESIAN_POINT('Ctrl Pts',(-1.82201060129564,31.6746528082086,12.3833146748631));
#56739=CARTESIAN_POINT('Ctrl Pts',(-1.75138393764471,31.6913244567762,12.269978209581));
#56740=CARTESIAN_POINT('Ctrl Pts',(-1.74242152111319,31.6934400637015,12.25559598398));
#56741=CARTESIAN_POINT('Ctrl Pts',(-1.73327864082616,31.6955526272835,12.2413297586781));
#56742=CARTESIAN_POINT('Ctrl Pts',(-1.72395920171074,31.6976617745041,12.2271828790924));
#56743=CARTESIAN_POINT('Ctrl Pts',(-1.64133954993399,31.7163600037378,12.1017665047132));
#56744=CARTESIAN_POINT('Ctrl Pts',(-1.54502778443523,31.7348138805689,11.9860617173297));
#56745=CARTESIAN_POINT('Ctrl Pts',(-1.43778289097727,31.7532672501976,11.8824706610493));
#56746=CARTESIAN_POINT('Ctrl Pts',(-1.33743650048451,31.7705336110932,11.7855430755028));
#56747=CARTESIAN_POINT('Ctrl Pts',(-1.22751550117257,31.7877994957642,11.6992227228509));
#56748=CARTESIAN_POINT('Ctrl Pts',(-1.11030205415889,31.8052541547949,11.6255177712851));
#56749=CARTESIAN_POINT('Ctrl Pts',(-1.10224399339743,31.8064541084403,11.6204507845761));
#56750=CARTESIAN_POINT('Ctrl Pts',(-1.09415148531256,31.8076549499904,11.6154434300847));
#56751=CARTESIAN_POINT('Ctrl Pts',(-1.08602527998824,31.808856739018,11.6104963641596));
#56752=CARTESIAN_POINT('Ctrl Pts',(-1.06702481750994,31.8116667279873,11.5989292751264));
#56753=CARTESIAN_POINT('Ctrl Pts',(-1.04783273466549,31.814473144343,11.587681052775));
#56754=CARTESIAN_POINT('Ctrl Pts',(-1.02845837876467,31.8172761349334,11.5767607902904));
#56755=CARTESIAN_POINT('Ctrl Pts',(-0.932432776307541,31.8311686669748,
11.5226364214886));
#56756=CARTESIAN_POINT('Ctrl Pts',(-0.831925975220367,31.8449771046457,
11.4765709736407));
#56757=CARTESIAN_POINT('Ctrl Pts',(-0.728418797670314,31.858718963986,11.4389723918552));
#56758=CARTESIAN_POINT('Ctrl Pts',(-0.621971400335677,31.8728511739056,
11.4003057866084));
#56759=CARTESIAN_POINT('Ctrl Pts',(-0.512351751409975,31.8869129825135,
11.3705945925219));
#56760=CARTESIAN_POINT('Ctrl Pts',(-0.401210092076274,31.9009225319703,
11.3502436116426));
#56761=CARTESIAN_POINT('Ctrl Pts',(-0.292675692779608,31.9146034329379,
11.3303700421991));
#56762=CARTESIAN_POINT('Ctrl Pts',(-0.182691166041161,31.9282345021004,
11.3194230274057));
#56763=CARTESIAN_POINT('Ctrl Pts',(-0.0728127663338156,31.9418316621078,
11.317735693246));
#56764=CARTESIAN_POINT('Ctrl Pts',(0.0437903629785101,31.9562609895356,
11.3159450916015));
#56765=CARTESIAN_POINT('Ctrl Pts',(0.160272454760996,31.9706521517856,11.3245826806894));
#56766=CARTESIAN_POINT('Ctrl Pts',(0.274808143983138,31.9850228251252,11.3431313784676));
#56767=CARTESIAN_POINT('Ctrl Pts',(0.381688629761689,31.9984330080815,11.360440339915));
#56768=CARTESIAN_POINT('Ctrl Pts',(0.486873017161923,32.0118253421599,11.3863791828463));
#56769=CARTESIAN_POINT('Ctrl Pts',(0.588897233847645,32.0252130151719,11.4204822323603));
#56770=CARTESIAN_POINT('Ctrl Pts',(0.596204612076822,32.0261718933038,11.4229248277525));
#56771=CARTESIAN_POINT('Ctrl Pts',(0.603495791630528,32.0271307470184,11.4254092871624));
#56772=CARTESIAN_POINT('Ctrl Pts',(0.610770241051819,32.0280895809249,11.4279354310596));
#56773=CARTESIAN_POINT('Ctrl Pts',(0.703451489250528,32.0403057526409,11.4601201581727));
#56774=CARTESIAN_POINT('Ctrl Pts',(0.793790709316334,32.052477282463,11.4991421659039));
#56775=CARTESIAN_POINT('Ctrl Pts',(0.880635423141395,32.0646158795974,11.5447626760918));
#56776=CARTESIAN_POINT('Ctrl Pts',(0.9709443166876,32.0772386775563,11.5922029590593));
#56777=CARTESIAN_POINT('Ctrl Pts',(1.0574729549825,32.0898258752061,11.6467793001905));
#56778=CARTESIAN_POINT('Ctrl Pts',(1.1392501848813,32.1023897826209,11.7076411287499));
#56779=CARTESIAN_POINT('Ctrl Pts',(1.22205093153323,32.1151109388168,11.7692646987039));
#56780=CARTESIAN_POINT('Ctrl Pts',(1.29997950085949,32.1278082267835,11.8373315058902));
#56781=CARTESIAN_POINT('Ctrl Pts',(1.37204471200167,32.140493354182,11.9109079805667));
#56782=CARTESIAN_POINT('Ctrl Pts',(1.44313956607502,32.153007676516,11.9834937490319));
#56783=CARTESIAN_POINT('Ctrl Pts',(1.50852688728067,32.165510166579,12.061441002164));
#56784=CARTESIAN_POINT('Ctrl Pts',(1.56728690689341,32.1780109501769,12.1438150100309));
#56785=CARTESIAN_POINT('Ctrl Pts',(1.5792518897322,32.1805564166727,12.160588380717));
#56786=CARTESIAN_POINT('Ctrl Pts',(1.59094222109023,32.1831018085915,12.1775451923054));
#56787=CARTESIAN_POINT('Ctrl Pts',(1.6023503594251,32.1856472054933,12.1946774015542));
#56788=CARTESIAN_POINT('Ctrl Pts',(1.65837536411523,32.198147568758,12.2788131365305));
#56789=CARTESIAN_POINT('Ctrl Pts',(1.70759069972438,32.2106481500889,12.3671801108344));
#56790=CARTESIAN_POINT('Ctrl Pts',(1.74962554120705,32.223157648365,12.4585038781202));
#56791=CARTESIAN_POINT('Ctrl Pts',(1.7711114065368,32.2295518058263,12.5051834918905));
#56792=CARTESIAN_POINT('Ctrl Pts',(1.79072200965433,32.2359482733096,12.5526353940308));
#56793=CARTESIAN_POINT('Ctrl Pts',(1.80841311943544,32.2423480863489,12.6006887752399));
#56794=CARTESIAN_POINT('Ctrl Pts',(1.84263044751356,32.2547263093723,12.693631407468));
#56795=CARTESIAN_POINT('Ctrl Pts',(1.8698543877587,32.2671506035997,12.7892761903362));
#56796=CARTESIAN_POINT('Ctrl Pts',(1.88961745460196,32.2796024374238,12.8864421648003));
#56797=CARTESIAN_POINT('Ctrl Pts',(1.9041958679578,32.288787650527,12.9581175657436));
#56798=CARTESIAN_POINT('Ctrl Pts',(1.91471528070787,32.2979878603318,13.0306196649456));
#56799=CARTESIAN_POINT('Ctrl Pts',(1.92100302500379,32.3071958304518,13.1034643427965));
#56800=CARTESIAN_POINT('Ctrl Pts',(1.929607641116,32.3197967003864,13.2031504081363));
#56801=CARTESIAN_POINT('Ctrl Pts',(1.93028508731108,32.332412077683,13.3034776626971));
#56802=CARTESIAN_POINT('Ctrl Pts',(1.92325688603922,32.3450239724341,13.4031967692286));
#56803=CARTESIAN_POINT('Ctrl Pts',(1.91616768070292,32.3577453371348,13.5037814273522));
#56804=CARTESIAN_POINT('Ctrl Pts',(1.90123879798748,32.3704631561137,13.603746011088));
#56805=CARTESIAN_POINT('Ctrl Pts',(1.87875011820394,32.3831596370036,13.7018138996038));
#56806=CARTESIAN_POINT('Ctrl Pts',(1.85671101886068,32.3956022973258,13.797921272655));
#56807=CARTESIAN_POINT('Ctrl Pts',(1.82741189099095,32.4080244653577,13.8922059091036));
#56808=CARTESIAN_POINT('Ctrl Pts',(1.79115973386811,32.4204100398556,13.9834895606174));
#56809=CARTESIAN_POINT('Ctrl Pts',(1.78287518904698,32.4232404603108,14.0043502089876));
#56810=CARTESIAN_POINT('Ctrl Pts',(1.77422769435617,32.4260689723749,14.0250542706439));
#56811=CARTESIAN_POINT('Ctrl Pts',(1.76522119840476,32.4288953886433,14.0455879505822));
#56812=CARTESIAN_POINT('Ctrl Pts',(1.73494946027227,32.4383952578036,14.114603712688));
#56813=CARTESIAN_POINT('Ctrl Pts',(1.70062150205205,32.4478714334674,14.181693485297));
#56814=CARTESIAN_POINT('Ctrl Pts',(1.66260821968523,32.4573169635298,14.2464279481209));
#56815=CARTESIAN_POINT('Ctrl Pts',(1.60951641862903,32.4705091998147,14.336840272649));
#56816=CARTESIAN_POINT('Ctrl Pts',(1.54901546843582,32.4836859639085,14.4230562711579));
#56817=CARTESIAN_POINT('Ctrl Pts',(1.48193781563378,32.4968456700971,14.5038310671862));
#56818=CARTESIAN_POINT('Ctrl Pts',(1.41238016704888,32.5104919171006,14.5875922699407));
#56819=CARTESIAN_POINT('Ctrl Pts',(1.33575093107518,32.52411982678,14.6655012662401));
#56820=CARTESIAN_POINT('Ctrl Pts',(1.25303283309184,32.5377272887717,14.7361782469831));
#56821=CARTESIAN_POINT('Ctrl Pts',(1.22974157025398,32.5415587958001,14.7560790446949));
#56822=CARTESIAN_POINT('Ctrl Pts',(1.20596785715059,32.5453886793708,14.7754065734702));
#56823=CARTESIAN_POINT('Ctrl Pts',(1.18173429457685,32.5492168868397,14.7941303591961));
#56824=CARTESIAN_POINT('Ctrl Pts',(1.09534944980345,32.5628632133734,14.860874624245));
#56825=CARTESIAN_POINT('Ctrl Pts',(1.00311865038569,32.5764882753401,14.9199439829922));
#56826=CARTESIAN_POINT('Ctrl Pts',(0.906622652138212,32.5900893986078,14.9707896365649));
#56827=CARTESIAN_POINT('Ctrl Pts',(0.81108545122454,32.603555379269,15.0211300808235));
#56828=CARTESIAN_POINT('Ctrl Pts',(0.711368759496013,32.6169978965796,15.0634089499655));
#56829=CARTESIAN_POINT('Ctrl Pts',(0.609029104604093,32.6304139103144,15.0971378774218));
#56830=CARTESIAN_POINT('Ctrl Pts',(0.511871895826564,32.643150541572,15.1291587832005));
#56831=CARTESIAN_POINT('Ctrl Pts',(0.412351793888545,32.6558632839847,15.1534736836662));
#56832=CARTESIAN_POINT('Ctrl Pts',(0.311802793307576,32.6685491354378,15.1697081915185));
#56833=CARTESIAN_POINT('Ctrl Pts',(0.208558134510143,32.6815750869367,15.1863779367599));
#56834=CARTESIAN_POINT('Ctrl Pts',(0.103949096816314,32.6945739279686,15.1946208003383));
#56835=CARTESIAN_POINT('Ctrl Pts',(-0.000630729312437852,32.7075672723265,
15.1939083446255));
#56836=CARTESIAN_POINT('Ctrl Pts',(-0.108565855569122,32.7209774902976,
15.1931730307495));
#56837=CARTESIAN_POINT('Ctrl Pts',(-0.216469187659061,32.7343818782785,
15.1828970181674));
#56838=CARTESIAN_POINT('Ctrl Pts',(-0.322774198061109,32.7478011574229,
15.1635746582427));
#56839=CARTESIAN_POINT('Ctrl Pts',(-0.429563384388784,32.7612815559057,
15.1441642928564));
#56840=CARTESIAN_POINT('Ctrl Pts',(-0.534738489088845,32.7747769922733,
15.1156245921934));
#56841=CARTESIAN_POINT('Ctrl Pts',(-0.636690050051503,32.7883051517794,
15.0785041312197));
#56842=CARTESIAN_POINT('Ctrl Pts',(-0.729799500108899,32.8006600336469,
15.044603073948));
#56843=CARTESIAN_POINT('Ctrl Pts',(-0.820219225911066,32.8130421740493,
15.0035455200694));
#56844=CARTESIAN_POINT('Ctrl Pts',(-0.90672160595063,32.8254625387955,14.9557872785077));
#56845=CARTESIAN_POINT('Ctrl Pts',(-0.992623125835422,32.8377966295886,
14.9083607737653));
#56846=CARTESIAN_POINT('Ctrl Pts',(-1.07491738151294,32.8500285650052,14.8544705816298));
#56847=CARTESIAN_POINT('Ctrl Pts',(-1.15243288169613,32.8622104398304,14.7944450637593));
#56848=CARTESIAN_POINT('Ctrl Pts',(-1.15914061004674,32.8632645865099,14.7892508140024));
#56849=CARTESIAN_POINT('Ctrl Pts',(-1.16581252965613,32.86431835469,14.7840106424791));
#56850=CARTESIAN_POINT('Ctrl Pts',(-1.17244786797231,32.8653717760498,14.7787247741989));
#56851=CARTESIAN_POINT('Ctrl Pts',(-1.24908094773948,32.8775379866099,14.7176770406468));
#56852=CARTESIAN_POINT('Ctrl Pts',(-1.32083679360994,32.8896584354967,14.6505303561686));
#56853=CARTESIAN_POINT('Ctrl Pts',(-1.3870201362254,32.9017786069914,14.5782416312114));
#56854=CARTESIAN_POINT('Ctrl Pts',(-1.45282361211481,32.9138292134009,14.5063678155078));
#56855=CARTESIAN_POINT('Ctrl Pts',(-1.51311717830069,32.9258795506478,14.4294104113911));
#56856=CARTESIAN_POINT('Ctrl Pts',(-1.5672020311935,32.9379683126868,14.3483584759315));
#56857=CARTESIAN_POINT('Ctrl Pts',(-1.62047948805187,32.949876609808,14.268516509766));
#56858=CARTESIAN_POINT('Ctrl Pts',(-1.66773094040675,32.9618221869895,14.1847013810081));
#56859=CARTESIAN_POINT('Ctrl Pts',(-1.70829171716438,32.9738362028301,14.0979083023651));
#56860=CARTESIAN_POINT('Ctrl Pts',(-1.71708953534038,32.976442097869,14.0790824862472));
#56861=CARTESIAN_POINT('Ctrl Pts',(-1.7255726275999,32.9790511909054,14.0601167502762));
#56862=CARTESIAN_POINT('Ctrl Pts',(-1.73373432566236,32.981663763421,14.0410215561971));
#56863=CARTESIAN_POINT('Ctrl Pts',(-1.77656675841202,32.9953744931885,13.9408103489242));
#56864=CARTESIAN_POINT('Ctrl Pts',(-1.8109159376224,33.0090631847566,13.8368942431182));
#56865=CARTESIAN_POINT('Ctrl Pts',(-1.83585249184895,33.0227376840039,13.7306630244244));
#56866=CARTESIAN_POINT('Ctrl Pts',(-1.86269959886161,33.0374598762242,13.6162927361141));
#56867=CARTESIAN_POINT('Ctrl Pts',(-1.878634692129,33.0521656495421,13.4992392863367));
#56868=CARTESIAN_POINT('Ctrl Pts',(-1.883725334327,33.0668631824395,13.3816644247428));
#56869=CARTESIAN_POINT('Ctrl Pts',(-1.88546801883735,33.071894603216,13.3414149076608));
#56870=CARTESIAN_POINT('Ctrl Pts',(-1.88594018725234,33.0769250387225,13.3011045808627));
#56871=CARTESIAN_POINT('Ctrl Pts',(-1.88514570139615,33.0819547552135,13.2608209354391));
#56872=CARTESIAN_POINT('Ctrl Pts',(-1.88282680887894,33.0966351574431,13.1432437083416));
#56873=CARTESIAN_POINT('Ctrl Pts',(-1.86971355688606,33.1113096089662,13.0258933344761));
#56874=CARTESIAN_POINT('Ctrl Pts',(-1.84584025664775,33.1259822303606,12.9108475780895));
#56875=CARTESIAN_POINT('Ctrl Pts',(-1.83891474206808,33.1302386780396,12.8774734297634));
#56876=CARTESIAN_POINT('Ctrl Pts',(-1.8310840467261,33.1344949564262,12.8442932527195));
#56877=CARTESIAN_POINT('Ctrl Pts',(-1.8223498458544,33.1387511284261,12.8113577463972));
#56878=CARTESIAN_POINT('Ctrl Pts',(-1.82073903271537,33.1395360769154,12.8052835849365));
#56879=CARTESIAN_POINT('Ctrl Pts',(-1.81909742698397,33.1403210550766,12.7992172539458));
#56880=CARTESIAN_POINT('Ctrl Pts',(-1.81742503007901,33.1411060616138,12.7931590691915));
#56881=CARTESIAN_POINT('Ctrl Pts',(-1.78341351893815,33.157070727961,12.6699538553742));
#56882=CARTESIAN_POINT('Ctrl Pts',(-1.73666257370683,33.1730470449138,12.5501188149469));
#56883=CARTESIAN_POINT('Ctrl Pts',(-1.67844835802018,33.1890253691034,12.4360236729034));
#56884=CARTESIAN_POINT('Ctrl Pts',(-1.61980323463689,33.2051219665153,12.3210839867176));
#56885=CARTESIAN_POINT('Ctrl Pts',(-1.54952556666188,33.221220599866,12.211970972486));
#56886=CARTESIAN_POINT('Ctrl Pts',(-1.46896446342868,33.2373124658053,12.111082370773));
#56887=CARTESIAN_POINT('Ctrl Pts',(-1.43201039406103,33.2446939427999,12.0648039034174));
#56888=CARTESIAN_POINT('Ctrl Pts',(-1.39289306392564,33.2520740104948,12.0202554815113));
#56889=CARTESIAN_POINT('Ctrl Pts',(-1.35174485230098,33.25945189343,11.9776655040048));
#56890=CARTESIAN_POINT('Ctrl Pts',(-1.28441558434642,33.2715240452313,11.9079771288725));
#56891=CARTESIAN_POINT('Ctrl Pts',(-1.21164898751506,33.2835903304337,11.8435330764808));
#56892=CARTESIAN_POINT('Ctrl Pts',(-1.1344413983556,33.2956475381849,11.7849360748564));
#56893=CARTESIAN_POINT('Ctrl Pts',(-1.04148000362451,33.3101649562435,11.7143826609062));
#56894=CARTESIAN_POINT('Ctrl Pts',(-0.941877414275713,33.3247120648009,
11.6522161259233));
#56895=CARTESIAN_POINT('Ctrl Pts',(-0.83734978707031,33.3392824870544,11.5995868551751));
#56896=CARTESIAN_POINT('Ctrl Pts',(-0.744966745445939,33.3521600387746,
11.5530723380069));
#56897=CARTESIAN_POINT('Ctrl Pts',(-0.648737949632954,33.3650557953688,
11.5140077083481));
#56898=CARTESIAN_POINT('Ctrl Pts',(-0.549871499941875,33.3779650443768,
11.4831626102079));
#56899=CARTESIAN_POINT('Ctrl Pts',(-0.438312571300595,33.3925315833127,
11.4483576170772));
#56900=CARTESIAN_POINT('Ctrl Pts',(-0.323396167968655,33.4071153107072,
11.4240193541309));
#56901=CARTESIAN_POINT('Ctrl Pts',(-0.207184444008096,33.4217090321553,
11.4102901892089));
#56902=CARTESIAN_POINT('Ctrl Pts',(-0.123751815319772,33.4321863962393,
11.4004335217393));
#56903=CARTESIAN_POINT('Ctrl Pts',(-0.0396519762126377,33.4426689014923,
11.3960441046249));
#56904=CARTESIAN_POINT('Ctrl Pts',(0.0443529895522357,33.4531537285205,
11.3971580099636));
#56905=CARTESIAN_POINT('Ctrl Pts',(0.161853849845441,33.4678192448338,11.3987160706615));
#56906=CARTESIAN_POINT('Ctrl Pts',(0.279401484675227,33.4825002502203,11.4109723352032));
#56907=CARTESIAN_POINT('Ctrl Pts',(0.394948071017141,33.4971989223994,11.4341338283749));
#56908=CARTESIAN_POINT('Ctrl Pts',(0.514048517686451,33.5123496808717,11.4580076983836));
#56909=CARTESIAN_POINT('Ctrl Pts',(0.63102160742065,33.5275192259303,11.4934689829188));
#56910=CARTESIAN_POINT('Ctrl Pts',(0.743781082859313,33.5427073447054,11.5396253014745));
#56911=CARTESIAN_POINT('Ctrl Pts',(0.855553128008094,33.5577624617219,11.5853774309647));
#56912=CARTESIAN_POINT('Ctrl Pts',(0.963183479473169,33.572835827222,11.6416380078028));
#56913=CARTESIAN_POINT('Ctrl Pts',(1.06464020010924,33.5879246703803,11.707488152597));
#56914=CARTESIAN_POINT('Ctrl Pts',(1.11819237326572,33.5958890549621,11.7422460112612));
#56915=CARTESIAN_POINT('Ctrl Pts',(1.17002466495448,33.6038577087437,11.779674763905));
#56916=CARTESIAN_POINT('Ctrl Pts',(1.2198406027858,33.6118299347862,11.8196338311499));
#56917=CARTESIAN_POINT('Ctrl Pts',(1.23077720451177,33.6135801590095,11.8284064533834));
#56918=CARTESIAN_POINT('Ctrl Pts',(1.24161921329453,33.6153307798915,11.8373021545097));
#56919=CARTESIAN_POINT('Ctrl Pts',(1.25236346546683,33.6170817856626,11.8463195476875));
#56920=CARTESIAN_POINT('Ctrl Pts',(1.34818864605216,33.6326985490752,11.9267433236571));
#56921=CARTESIAN_POINT('Ctrl Pts',(1.43623527057538,33.6483458472314,12.0168506157618));
#56922=CARTESIAN_POINT('Ctrl Pts',(1.51497948581664,33.6640158393301,12.114719325643));
#56923=CARTESIAN_POINT('Ctrl Pts',(1.59432892343071,33.6798062698606,12.2133402473869));
#56924=CARTESIAN_POINT('Ctrl Pts',(1.66423150396073,33.6956197442337,12.3198408590462));
#56925=CARTESIAN_POINT('Ctrl Pts',(1.72316823935652,33.7114492409151,12.4322227978785));
#56926=CARTESIAN_POINT('Ctrl Pts',(1.75583922438526,33.7202241627973,12.4945205925635));
#56927=CARTESIAN_POINT('Ctrl Pts',(1.78514127758445,33.729004025984,12.5586252496628));
#56928=CARTESIAN_POINT('Ctrl Pts',(1.81082243501288,33.7377877653431,12.6241947529243));
#56929=CARTESIAN_POINT('Ctrl Pts',(1.84406234849377,33.7491568298857,12.7090633816638));
#56930=CARTESIAN_POINT('Ctrl Pts',(1.87123582420496,33.760532379776,12.7963857198891));
#56931=CARTESIAN_POINT('Ctrl Pts',(1.89221941649866,33.7719123269017,12.8852340922583));
#56932=CARTESIAN_POINT('Ctrl Pts',(1.91979504835822,33.7868673083046,13.0019943673095));
#56933=CARTESIAN_POINT('Ctrl Pts',(1.93667000491097,33.8018622643777,13.1216242748102));
#56934=CARTESIAN_POINT('Ctrl Pts',(1.94246100425419,33.8168893377621,13.2420074258643));
#56935=CARTESIAN_POINT('Ctrl Pts',(1.94791422876764,33.8310399187047,13.3553689221148));
#56936=CARTESIAN_POINT('Ctrl Pts',(1.94353893132823,33.8452189754154,13.4693969758569));
#56937=CARTESIAN_POINT('Ctrl Pts',(1.92905494235689,33.85941951799,13.5823104299314));
#56938=CARTESIAN_POINT('Ctrl Pts',(1.91373349001847,33.8744411350781,13.7017525330971));
#56939=CARTESIAN_POINT('Ctrl Pts',(1.88710026331683,33.8894867991923,13.8199459974798));
#56940=CARTESIAN_POINT('Ctrl Pts',(1.84989387070444,33.9045476817596,13.9348618491369));
#56941=CARTESIAN_POINT('Ctrl Pts',(1.82591104626476,33.9142557581721,14.0089353215195));
#56942=CARTESIAN_POINT('Ctrl Pts',(1.79753617067424,33.9239701471483,14.0816471192062));
#56943=CARTESIAN_POINT('Ctrl Pts',(1.7649772391965,33.9336883689359,14.1524592800049));
#56944=CARTESIAN_POINT('Ctrl Pts',(1.71738845989287,33.9478927144375,14.2559597371549));
#56945=CARTESIAN_POINT('Ctrl Pts',(1.66083542209935,33.9621352393784,14.3556498016173));
#56946=CARTESIAN_POINT('Ctrl Pts',(1.59586126139288,33.9764102392548,14.449816937735));
#56947=CARTESIAN_POINT('Ctrl Pts',(1.58716866014967,33.978320027397,14.4624151360893));
#56948=CARTESIAN_POINT('Ctrl Pts',(1.57832540722809,33.9802303931489,14.4749144652241));
#56949=CARTESIAN_POINT('Ctrl Pts',(1.56933287225282,33.9821413194679,14.4873108132865));
#56950=CARTESIAN_POINT('Ctrl Pts',(1.5019605950614,33.9964580230454,14.5801845357819));
#56951=CARTESIAN_POINT('Ctrl Pts',(1.42620477900407,34.0108063984482,14.6672769838926));
#56952=CARTESIAN_POINT('Ctrl Pts',(1.34333605945917,34.0251777889364,14.747330386248));
#56953=CARTESIAN_POINT('Ctrl Pts',(1.26766405149073,34.0383010998975,14.8204315724882));
#56954=CARTESIAN_POINT('Ctrl Pts',(1.18606193623612,34.0514435727229,14.8876625063986));
#56955=CARTESIAN_POINT('Ctrl Pts',(1.09953154996117,34.0645967734331,14.9480816900527));
#56956=CARTESIAN_POINT('Ctrl Pts',(1.02738510699994,34.0755635180144,14.9984573947608));
#56957=CARTESIAN_POINT('Ctrl Pts',(0.951813477723499,34.0865376889597,15.0440978257523));
#56958=CARTESIAN_POINT('Ctrl Pts',(0.873525894036174,34.0975135015488,15.0845424501372));
#56959=CARTESIAN_POINT('Ctrl Pts',(0.787769630833399,34.1095364128321,15.1288455144358));
#56960=CARTESIAN_POINT('Ctrl Pts',(0.698708695046754,34.12160084351,15.1671765144296));
#56961=CARTESIAN_POINT('Ctrl Pts',(0.607157766262662,34.1337023607202,15.1988590604772));
#56962=CARTESIAN_POINT('Ctrl Pts',(0.57205723886613,34.1383420693722,15.2110061144755));
#56963=CARTESIAN_POINT('Ctrl Pts',(0.536591208756782,34.1429871705226,15.2221756861145));
#56964=CARTESIAN_POINT('Ctrl Pts',(0.500807535832861,34.1476371941549,15.2323291427542));
#56965=CARTESIAN_POINT('Ctrl Pts',(0.406723295000572,34.1598632712329,15.2590251239576));
#56966=CARTESIAN_POINT('Ctrl Pts',(0.310439509622285,34.1721237919042,15.27869614959));
#56967=CARTESIAN_POINT('Ctrl Pts',(0.213020585639545,34.1844061040476,15.2912643606359));
#56968=CARTESIAN_POINT('Ctrl Pts',(0.115639236100466,34.1966836789076,15.3038277241274));
#56969=CARTESIAN_POINT('Ctrl Pts',(0.017124022998488,34.2089830255298,15.3092926359667));
#56970=CARTESIAN_POINT('Ctrl Pts',(-0.0814129547883811,34.2212857146177,
15.3075978231872));
#56971=CARTESIAN_POINT('Ctrl Pts',(-0.179346761227685,34.2335130956363,
15.3059133848126));
#56972=CARTESIAN_POINT('Ctrl Pts',(-0.277301313740047,34.2457437686831,
15.2971556374653));
#56973=CARTESIAN_POINT('Ctrl Pts',(-0.374145174267623,34.2579540207722,
15.2812962511804));
#56974=CARTESIAN_POINT('Ctrl Pts',(-0.389865757957571,34.2599361008833,
15.2787218101368));
#56975=CARTESIAN_POINT('Ctrl Pts',(-0.405557004185956,34.2619176309858,
15.2759603217363));
#56976=CARTESIAN_POINT('Ctrl Pts',(-0.421213997593287,34.2638984958387,
15.2730117706197));
#56977=CARTESIAN_POINT('Ctrl Pts',(-0.528484965322997,34.2774700216221,
15.2528103230338));
#56978=CARTESIAN_POINT('Ctrl Pts',(-0.634408224075304,34.2910967149944,
15.2241298800896));
#56979=CARTESIAN_POINT('Ctrl Pts',(-0.737525673046703,34.3047670915336,
15.1869054434143));
#56980=CARTESIAN_POINT('Ctrl Pts',(-0.765105948676489,34.3084234344385,
15.1769492213209));
#56981=CARTESIAN_POINT('Ctrl Pts',(-0.792485268849016,34.3120828755897,
15.1663819527556));
#56982=CARTESIAN_POINT('Ctrl Pts',(-0.819635259472576,34.3157451367173,
15.1552028010352));
#56983=CARTESIAN_POINT('Ctrl Pts',(-0.924165319229743,34.3298451922132,
15.1121619980538));
#56984=CARTESIAN_POINT('Ctrl Pts',(-1.02529795183968,34.3439874686245,15.0600469893191));
#56985=CARTESIAN_POINT('Ctrl Pts',(-1.12166850413609,34.3581527213183,14.9997648521849));
#56986=CARTESIAN_POINT('Ctrl Pts',(-1.2180390564325,34.3723179740122,14.9394827150508));
#56987=CARTESIAN_POINT('Ctrl Pts',(-1.30964599532968,34.3865061987767,14.8710331408026));
#56988=CARTESIAN_POINT('Ctrl Pts',(-1.39511168057473,34.4006927818407,14.7953790118328));
#56989=CARTESIAN_POINT('Ctrl Pts',(-1.45900496212402,34.4112985277999,14.7388207504818));
#56990=CARTESIAN_POINT('Ctrl Pts',(-1.51946550307793,34.4219032450792,14.6782371434713));
#56991=CARTESIAN_POINT('Ctrl Pts',(-1.57592471557605,34.432494682015,14.6140865465418));
#56992=CARTESIAN_POINT('Ctrl Pts',(-1.64030234483855,34.444571570272,14.5409388145178));
#56993=CARTESIAN_POINT('Ctrl Pts',(-1.69979667045605,34.456725822996,14.4632206315149));
#56994=CARTESIAN_POINT('Ctrl Pts',(-1.75355035369345,34.4689396714447,14.3814837337769));
#56995=CARTESIAN_POINT('Ctrl Pts',(-1.77885528939668,34.4746894290626,14.3430054971748));
#56996=CARTESIAN_POINT('Ctrl Pts',(-1.80288757563606,34.4804523129785,14.3036372784954));
#56997=CARTESIAN_POINT('Ctrl Pts',(-1.8255558752418,34.4862260391538,14.2634401176226));
#56998=CARTESIAN_POINT('Ctrl Pts',(-1.87419314992058,34.4986141896016,14.1771927859445));
#56999=CARTESIAN_POINT('Ctrl Pts',(-1.91655123609662,34.5110526305101,14.0871258591308));
#57000=CARTESIAN_POINT('Ctrl Pts',(-1.95232334393682,34.5235145318038,13.9942455739322));
#57001=CARTESIAN_POINT('Ctrl Pts',(-1.9881487064555,34.5359949853883,13.9012270159277));
#57002=CARTESIAN_POINT('Ctrl Pts',(-2.01736730005151,34.5484989653802,13.8053868797165));
#57003=CARTESIAN_POINT('Ctrl Pts',(-2.03967635811788,34.5609937519823,13.7077874915789));
#57004=CARTESIAN_POINT('Ctrl Pts',(-2.06191038413533,34.573446514872,13.6105163594368));
#57005=CARTESIAN_POINT('Ctrl Pts',(-2.07728016684792,34.5858901361617,13.511498321101));
#57006=CARTESIAN_POINT('Ctrl Pts',(-2.08550835859991,34.5982866090211,13.4118309465753));
#57007=CARTESIAN_POINT('Ctrl Pts',(-2.08686771362955,34.6003345933461,13.3953651967562));
#57008=CARTESIAN_POINT('Ctrl Pts',(-2.08803222165053,34.6023812785661,13.3788818146423));
#57009=CARTESIAN_POINT('Ctrl Pts',(-2.08900072334537,34.6044264787915,13.362385851687));
#57010=CARTESIAN_POINT('Ctrl Pts',(-2.09505087338117,34.6172026755528,13.2593369345847));
#57011=CARTESIAN_POINT('Ctrl Pts',(-2.09379275692534,34.6300709245727,13.1555496116575));
#57012=CARTESIAN_POINT('Ctrl Pts',(-2.08489850256943,34.6430128630142,13.0521857152708));
#57013=CARTESIAN_POINT('Ctrl Pts',(-2.07600424821351,34.6559548014558,12.9488218188842));
#57014=CARTESIAN_POINT('Ctrl Pts',(-2.05947303519056,34.6689704298532,12.8458825466293));
#57015=CARTESIAN_POINT('Ctrl Pts',(-2.03502060520216,34.6820384222808,12.7445609029007));
#57016=CARTESIAN_POINT('Ctrl Pts',(-2.01078754340807,34.6949891788384,12.6441482381995));
#57017=CARTESIAN_POINT('Ctrl Pts',(-1.97877453893384,34.7079913583367,12.5453256332383));
#57018=CARTESIAN_POINT('Ctrl Pts',(-1.93960121624929,34.721021283644,12.4491543456727));
#57019=CARTESIAN_POINT('Ctrl Pts',(-1.90066566372906,34.7339721212643,12.3535667885971));
#57020=CARTESIAN_POINT('Ctrl Pts',(-1.85465672409422,34.7469503629058,12.2605997747385));
#57021=CARTESIAN_POINT('Ctrl Pts',(-1.80223260483086,34.7599300032335,12.1712873498045));
#57022=CARTESIAN_POINT('Ctrl Pts',(-1.77511199135633,34.7666447714225,12.1250832782981));
#57023=CARTESIAN_POINT('Ctrl Pts',(-1.74627526809702,34.7733598693225,12.0798570375199));
#57024=CARTESIAN_POINT('Ctrl Pts',(-1.7158184117152,34.7800714128729,12.0357491438004));
#57025=CARTESIAN_POINT('Ctrl Pts',(-1.65345660760091,34.7938136047442,11.9454362174255));
#57026=CARTESIAN_POINT('Ctrl Pts',(-1.58402369302544,34.8075815743873,11.8594688178559));
#57027=CARTESIAN_POINT('Ctrl Pts',(-1.50826910434011,34.8213778510084,11.779084292947));
#57028=CARTESIAN_POINT('Ctrl Pts',(-1.43238478499475,34.8351977539221,11.6985621085556));
#57029=CARTESIAN_POINT('Ctrl Pts',(-1.3501581967844,34.8490460627832,11.6236427885949));
#57030=CARTESIAN_POINT('Ctrl Pts',(-1.26237706405678,34.8629276107525,11.5555321768382));
#57031=CARTESIAN_POINT('Ctrl Pts',(-1.22019422314461,34.869598328154,11.5228019190836));
#57032=CARTESIAN_POINT('Ctrl Pts',(-1.17672911137699,34.8762767549658,11.4916433157153));
#57033=CARTESIAN_POINT('Ctrl Pts',(-1.13207088971541,34.8829636125416,11.462186235914));
#57034=CARTESIAN_POINT('Ctrl Pts',(-1.0391654958356,34.8968747158901,11.4009047629921));
#57035=CARTESIAN_POINT('Ctrl Pts',(-0.941096546679065,34.9108221682274,
11.3469906830712));
#57036=CARTESIAN_POINT('Ctrl Pts',(-0.839269891050978,34.924814044204,11.3007966198672));
#57037=CARTESIAN_POINT('Ctrl Pts',(-0.756439250854729,34.9361957009768,
11.2632201738487));
#57038=CARTESIAN_POINT('Ctrl Pts',(-0.671122639783257,34.9476067954979,
11.2307510245286));
#57039=CARTESIAN_POINT('Ctrl Pts',(-0.584072161961717,34.9590527132191,
11.2035539354153));
#57040=CARTESIAN_POINT('Ctrl Pts',(-0.488628455221114,34.9716022229025,
11.1737345586296));
#57041=CARTESIAN_POINT('Ctrl Pts',(-0.390726602951209,34.9841200356052,
11.1503536926679));
#57042=CARTESIAN_POINT('Ctrl Pts',(-0.291416536690167,34.9966287025253,
11.1336927912598));
#57043=CARTESIAN_POINT('Ctrl Pts',(-0.191662750098081,35.0091932585414,
11.1169574484485));
#57044=CARTESIAN_POINT('Ctrl Pts',(-0.0904893084113526,35.0217485877063,
11.1070017677132));
#57045=CARTESIAN_POINT('Ctrl Pts',(0.0110549133221134,35.034321965954,11.1040609066534));
#57046=CARTESIAN_POINT('Ctrl Pts',(0.111663768368748,35.0467795255076,11.1011471351061));
#57047=CARTESIAN_POINT('Ctrl Pts',(0.212635769790514,35.0592548166334,11.1051189721538));
#57048=CARTESIAN_POINT('Ctrl Pts',(0.312980537213609,35.0717785761591,11.1161641752063));
#57049=CARTESIAN_POINT('Ctrl Pts',(0.354563238902439,35.0769684008979,11.1207412886465));
#57050=CARTESIAN_POINT('Ctrl Pts',(0.39603865297577,35.0821665979529,11.1265326427681));
#57051=CARTESIAN_POINT('Ctrl Pts',(0.437338275206494,35.0873755604995,11.1335498581336));
#57052=CARTESIAN_POINT('Ctrl Pts',(0.537969048597282,35.1000677330017,11.1506480244398));
#57053=CARTESIAN_POINT('Ctrl Pts',(0.637552716687777,35.1128235383902,11.1750251213683));
#57054=CARTESIAN_POINT('Ctrl Pts',(0.735171372142909,35.1256804609482,11.2060979429132));
#57055=CARTESIAN_POINT('Ctrl Pts',(0.773683488592057,35.1307527219461,11.2183566665779));
#57056=CARTESIAN_POINT('Ctrl Pts',(0.811890305850365,35.1358407657357,11.2316573654777));
#57057=CARTESIAN_POINT('Ctrl Pts',(0.849737658810937,35.1409470657411,11.2459637968681));
#57058=CARTESIAN_POINT('Ctrl Pts',(0.947707097989359,35.1541649345924,11.2829965864906));
#57059=CARTESIAN_POINT('Ctrl Pts',(1.0433989754111,35.1672842684333,11.327229906532));
#57060=CARTESIAN_POINT('Ctrl Pts',(1.1357935857753,35.1803579422975,11.378068771267));
#57061=CARTESIAN_POINT('Ctrl Pts',(1.22877077542611,35.1935140500998,11.4292281922492));
#57062=CARTESIAN_POINT('Ctrl Pts',(1.31840915379737,35.2066239238815,11.4870753732865));
#57063=CARTESIAN_POINT('Ctrl Pts',(1.4037225305533,35.2197481807154,11.5510048238215));
#57064=CARTESIAN_POINT('Ctrl Pts',(1.48969353405072,35.2329736041257,11.615427065966));
#57065=CARTESIAN_POINT('Ctrl Pts',(1.57127304533912,35.2462136380493,11.6860245968205));
#57066=CARTESIAN_POINT('Ctrl Pts',(1.64750089208874,35.2595370691274,11.7621973008937));
#57067=CARTESIAN_POINT('Ctrl Pts',(1.71688416473284,35.2716641760898,11.8315303821772));
#57068=CARTESIAN_POINT('Ctrl Pts',(1.78183472093203,35.283860465245,11.9054822158681));
#57069=CARTESIAN_POINT('Ctrl Pts',(1.84165717256322,35.2961825380909,11.9836242232698));
#57070=CARTESIAN_POINT('Ctrl Pts',(1.89007784060195,35.3061561012357,12.046872854797));
#57071=CARTESIAN_POINT('Ctrl Pts',(1.93513961567416,35.3162121575097,12.1128669436503));
#57072=CARTESIAN_POINT('Ctrl Pts',(1.9767321176533,35.3263827890248,12.1811670535072));
#57073=CARTESIAN_POINT('Ctrl Pts',(2.04732472143141,35.3436448272904,12.2970889712496));
#57074=CARTESIAN_POINT('Ctrl Pts',(2.10750078383594,35.3608568635775,12.4198550539506));
#57075=CARTESIAN_POINT('Ctrl Pts',(2.15653326971147,35.3779993238944,12.5473875107866));
#57076=CARTESIAN_POINT('Ctrl Pts',(2.20490833640097,35.3949119410347,12.6732100342494));
#57077=CARTESIAN_POINT('Ctrl Pts',(2.24243678990059,35.4117568252121,12.803673780373));
#57078=CARTESIAN_POINT('Ctrl Pts',(2.26837232234277,35.4285132705407,12.9367900497168));
#57079=CARTESIAN_POINT('Ctrl Pts',(2.28097724825192,35.436657069105,13.0014858764218));
#57080=CARTESIAN_POINT('Ctrl Pts',(2.29084311874697,35.4447799499595,13.066808175581));
#57081=CARTESIAN_POINT('Ctrl Pts',(2.29787990453227,35.4528793804603,13.1325273964819));
#57082=CARTESIAN_POINT('Ctrl Pts',(2.30982452833639,35.4666277953348,13.244082784739));
#57083=CARTESIAN_POINT('Ctrl Pts',(2.3138378028793,35.4805105310546,13.3567710192135));
#57084=CARTESIAN_POINT('Ctrl Pts',(2.309470334525,35.4945049157327,13.4693880880878));
#57085=CARTESIAN_POINT('Ctrl Pts',(2.3077677789381,35.4999602999246,13.513289223537));
#57086=CARTESIAN_POINT('Ctrl Pts',(2.30479214590153,35.5054326336883,13.5571793091859));
#57087=CARTESIAN_POINT('Ctrl Pts',(2.30051887843916,35.5109205083467,13.6009863588756));
#57088=CARTESIAN_POINT('Ctrl Pts',(2.28952026653867,35.5250452978801,13.7137377235598));
#57089=CARTESIAN_POINT('Ctrl Pts',(2.26992175982311,35.5392731515272,13.8259386567223));
#57090=CARTESIAN_POINT('Ctrl Pts',(2.2422376442469,35.5535788875883,13.9363518841804));
#57091=CARTESIAN_POINT('Ctrl Pts',(2.22466925455505,35.5626573335029,14.0064203175309));
#57092=CARTESIAN_POINT('Ctrl Pts',(2.20384570461758,35.5717671119679,14.0757687630312));
#57093=CARTESIAN_POINT('Ctrl Pts',(2.17990896535464,35.5809014569378,14.1440838286613));
#57094=CARTESIAN_POINT('Ctrl Pts',(2.14635034373073,35.5937075464916,14.2398595904938));
#57095=CARTESIAN_POINT('Ctrl Pts',(2.10651065587268,35.6064377600827,14.3336643377711));
#57096=CARTESIAN_POINT('Ctrl Pts',(2.06068536231229,35.6190900050523,14.4247557447538));
#57097=CARTESIAN_POINT('Ctrl Pts',(2.0287405426921,35.6279098870855,14.4882555794286));
#57098=CARTESIAN_POINT('Ctrl Pts',(1.99388597884577,35.6366918727779,14.5504365845222));
#57099=CARTESIAN_POINT('Ctrl Pts',(1.95620943234504,35.6454351476554,14.6110386821541));
#57100=CARTESIAN_POINT('Ctrl Pts',(1.89941929774933,35.6586139499401,14.7023846679447));
#57101=CARTESIAN_POINT('Ctrl Pts',(1.83649321646789,35.6720045307769,14.7902445266212));
#57102=CARTESIAN_POINT('Ctrl Pts',(1.76776005935783,35.6855415139324,14.8735973647063));
#57103=CARTESIAN_POINT('Ctrl Pts',(1.69878203809106,35.6991267230403,14.9572471500475));
#57104=CARTESIAN_POINT('Ctrl Pts',(1.62395523020483,35.7128593721322,15.0363564294859));
#57105=CARTESIAN_POINT('Ctrl Pts',(1.54366230589861,35.7266690324148,15.1098820020039));
#57106=CARTESIAN_POINT('Ctrl Pts',(1.53437299398596,35.7282667104528,15.1183883801509));
#57107=CARTESIAN_POINT('Ctrl Pts',(1.52501057637243,35.7298654145769,15.1268200222165));
#57108=CARTESIAN_POINT('Ctrl Pts',(1.51557569077079,35.7314650320618,15.1351753160586));
#57109=CARTESIAN_POINT('Ctrl Pts',(1.4330658322613,35.7454539894191,15.208243940505));
#57110=CARTESIAN_POINT('Ctrl Pts',(1.34500969791181,35.7595131518695,15.2754720724962));
#57111=CARTESIAN_POINT('Ctrl Pts',(1.25246982545419,35.7735646598664,15.3363452613834));
#57112=CARTESIAN_POINT('Ctrl Pts',(1.16060338199091,35.787513912558,15.3967754653248));
#57113=CARTESIAN_POINT('Ctrl Pts',(1.06431899290268,35.8014556019814,15.4509418100831));
#57114=CARTESIAN_POINT('Ctrl Pts',(0.964698194865835,35.815309503174,15.498368792203));
#57115=CARTESIAN_POINT('Ctrl Pts',(0.895275351458995,35.8249638849098,15.5314192798306));
#57116=CARTESIAN_POINT('Ctrl Pts',(0.82423316316403,35.8345755496419,15.5611975082448));
#57117=CARTESIAN_POINT('Ctrl Pts',(0.751946479824379,35.8441162488206,15.5875547054492));
#57118=CARTESIAN_POINT('Ctrl Pts',(0.645472004486849,35.8581691959538,15.6263774680114));
#57119=CARTESIAN_POINT('Ctrl Pts',(0.535849238912219,35.8723112393953,15.6580927100499));
#57120=CARTESIAN_POINT('Ctrl Pts',(0.42419202346629,35.8865253717002,15.6821180843425));
#57121=CARTESIAN_POINT('Ctrl Pts',(0.31002375074205,35.9010591653924,15.7066837648817));
#57122=CARTESIAN_POINT('Ctrl Pts',(0.193729462674567,35.9156683284442,15.7232090673018));
#57123=CARTESIAN_POINT('Ctrl Pts',(0.0765387231235699,35.9303339918097,
15.7311091299798));
#57124=CARTESIAN_POINT('Ctrl Pts',(0.002302801237708,35.9396241374661,15.7361135222901));
#57125=CARTESIAN_POINT('Ctrl Pts',(-0.0722921063576966,35.9489369413425,
15.7376576178362));
#57126=CARTESIAN_POINT('Ctrl Pts',(-0.146928518635182,35.9582674656181,
15.7356023796385));
#57127=CARTESIAN_POINT('Ctrl Pts',(-0.263654577318513,35.9728597442512,
15.7323881327697));
#57128=CARTESIAN_POINT('Ctrl Pts',(-0.380481892466343,35.987495395391,15.7203675215166));
#57129=CARTESIAN_POINT('Ctrl Pts',(-0.496150807410281,36.0021549648982,
15.6999452043));
#57130=CARTESIAN_POINT('Ctrl Pts',(-0.61201357287156,36.0168391025026,15.6794886611485));
#57131=CARTESIAN_POINT('Ctrl Pts',(-0.726712811269431,36.0315472370525,
15.6506025637267));
#57132=CARTESIAN_POINT('Ctrl Pts',(-0.838990868169627,36.0462591964778,
15.6137450642979));
#57133=CARTESIAN_POINT('Ctrl Pts',(-0.948098901842568,36.0605557830833,
15.577928187877));
#57134=CARTESIAN_POINT('Ctrl Pts',(-1.05491953278933,36.074855977133,15.5345842283449));
#57135=CARTESIAN_POINT('Ctrl Pts',(-1.15832294224657,36.0891407325821,15.4841752608046));
#57136=CARTESIAN_POINT('Ctrl Pts',(-1.21709541126144,36.0972599072923,15.4555237927496));
#57137=CARTESIAN_POINT('Ctrl Pts',(-1.2747644534909,36.1053740850071,15.4245906504352));
#57138=CARTESIAN_POINT('Ctrl Pts',(-1.3311281040744,36.1134796962468,15.3914659386035));
#57139=CARTESIAN_POINT('Ctrl Pts',(-1.41782930028274,36.1259481255129,15.3405119618804));
#57140=CARTESIAN_POINT('Ctrl Pts',(-1.50170128593061,36.1382167085011,15.284051015274));
#57141=CARTESIAN_POINT('Ctrl Pts',(-1.58201073434815,36.1504911003073,15.2224436482496));
#57142=CARTESIAN_POINT('Ctrl Pts',(-1.6623201827657,36.1627654921136,15.1608362812252));
#57143=CARTESIAN_POINT('Ctrl Pts',(-1.73906775288705,36.1750457212604,15.0940833947862));
#57144=CARTESIAN_POINT('Ctrl Pts',(-1.81156843952179,36.1875454226321,15.0225226611708));
#57145=CARTESIAN_POINT('Ctrl Pts',(-2.47103868931813,45.357839245202,11.1663882923918));
#57146=CARTESIAN_POINT('Ctrl Pts',(-1.99114009165886,45.4494249512674,10.6112764926156));
#57147=CARTESIAN_POINT('Ctrl Pts',(-0.656229362054297,45.6306288317189,
9.85038323946594));
#57148=CARTESIAN_POINT('Ctrl Pts',(1.60578641174988,45.9008551469128,10.1937481051622));
#57149=CARTESIAN_POINT('Ctrl Pts',(3.16037369235198,46.168185471263,11.8386895923522));
#57150=CARTESIAN_POINT('Ctrl Pts',(3.3728671597752,46.4341378756677,14.0798681764736));
#57151=CARTESIAN_POINT('Ctrl Pts',(2.17028512256952,46.698340609565,15.9655340763413));
#57152=CARTESIAN_POINT('Ctrl Pts',(0.0773201111634047,46.9604366782597,
16.7050573116982));
#57153=CARTESIAN_POINT('Ctrl Pts',(-2.00387794111447,47.2200782068993,16.0098611361731));
#57154=CARTESIAN_POINT('Ctrl Pts',(-3.34740888722012,47.5054828051186,13.9930892616668));
#57155=CARTESIAN_POINT('Ctrl Pts',(-2.93140857362281,47.7587315319614,11.8055319684882));
#57156=CARTESIAN_POINT('Ctrl Pts',(-1.72466235251619,47.9530101577763,10.7548847842084));
#57157=CARTESIAN_POINT('Ctrl Pts',(-0.905164464225716,48.0632135666546,
10.4157099355514));
#57158=CARTESIAN_POINT('Ctrl Pts',(-0.0334441790798442,48.1728678644929,
10.2648701783387));
#57159=CARTESIAN_POINT('Ctrl Pts',(1.06769726965044,48.3088763459659,10.443208013525));
#57160=CARTESIAN_POINT('Ctrl Pts',(2.16156427422588,48.4703285006447,11.1953451702359));
#57161=CARTESIAN_POINT('Ctrl Pts',(2.81802762807523,48.6299590209922,12.3269396060619));
#57162=CARTESIAN_POINT('Ctrl Pts',(2.974514026944,48.8402909027348,14.0516430479399));
#57163=CARTESIAN_POINT('Ctrl Pts',(1.72043482337078,49.0983753877132,15.9523988771148));
#57164=CARTESIAN_POINT('Ctrl Pts',(-0.70728189930077,49.3748770710527,16.207909252572));
#57165=CARTESIAN_POINT('Ctrl Pts',(-2.33912222864486,49.6201738927179,14.9205630045294));
#57166=CARTESIAN_POINT('Ctrl Pts',(-2.78256706964164,49.8362026228524,13.148512449524));
#57167=CARTESIAN_POINT('Ctrl Pts',(-2.05415847844708,50.0474536524228,11.514775663013));
#57168=CARTESIAN_POINT('Ctrl Pts',(-0.512761213530604,50.2539262122794,
10.6922180050034));
#57169=CARTESIAN_POINT('Ctrl Pts',(1.17083770430258,50.4556490739761,10.9841762156852));
#57170=CARTESIAN_POINT('Ctrl Pts',(2.10312483044396,50.6198448176698,12.013824403281));
#57171=CARTESIAN_POINT('Ctrl Pts',(2.35342838183667,50.7489044626185,13.0320232163277));
#57172=CARTESIAN_POINT('Ctrl Pts',(2.28589273790721,50.8445659743367,13.8060200922857));
#57173=CARTESIAN_POINT('Ctrl Pts',(1.97284878571603,50.9391095454929,14.5069955309913));
#57174=CARTESIAN_POINT('Ctrl Pts',(1.2838833323123,51.0637032271118,15.2491157464924));
#57175=CARTESIAN_POINT('Ctrl Pts',(0.0559027336712221,51.2167483942124,
15.6590700042074));
#57176=CARTESIAN_POINT('Ctrl Pts',(-1.37675602413113,51.3962674798406,15.1503729666643));
#57177=CARTESIAN_POINT('Ctrl Pts',(-2.17574776022075,51.571865285863,13.8974135292959));
#57178=CARTESIAN_POINT('Ctrl Pts',(-2.03865062584112,51.7437789248239,12.4485435208909));
#57179=CARTESIAN_POINT('Ctrl Pts',(-1.06007972412022,51.9122667185844,11.4111368238105));
#57180=CARTESIAN_POINT('Ctrl Pts',(0.323635636007865,52.0776220908781,11.1968858539816));
#57181=CARTESIAN_POINT('Ctrl Pts',(1.52332687478463,52.240143186124,11.8680021577416));
#57182=CARTESIAN_POINT('Ctrl Pts',(2.11356223942205,52.417937375268,13.2553851052613));
#57183=CARTESIAN_POINT('Ctrl Pts',(1.49608399064576,52.6104181125041,14.8368849598406));
#57184=CARTESIAN_POINT('Ctrl Pts',(-0.243334784363091,52.8174139408632,
15.4076636569798));
#57185=CARTESIAN_POINT('Ctrl Pts',(-1.76917851156779,53.0222997300687,14.4310069810067));
#57186=CARTESIAN_POINT('Ctrl Pts',(-1.99104716195834,53.2259785337442,12.6470991678428));
#57187=CARTESIAN_POINT('Ctrl Pts',(-0.746338998632108,53.4293896457581,
11.343670999249));
#57188=CARTESIAN_POINT('Ctrl Pts',(0.74872675692419,53.5994584735607,11.4560002347665));
#57189=CARTESIAN_POINT('Ctrl Pts',(1.47519207623104,53.7191897502424,12.1215132223007));
#57190=CARTESIAN_POINT('Ctrl Pts',(1.7087783122541,53.7792769266905,12.5452878158475));
#57191=CARTESIAN_POINT('Ctrl Pts',(1.79980890764077,53.8136861005568,12.8059893771045));
#57192=CARTESIAN_POINT('Ctrl Pts',(1.95692666292302,53.8998241968474,13.4795291061361));
#57193=CARTESIAN_POINT('Ctrl Pts',(1.69127030416465,54.0125675191503,14.435805987514));
#57194=CARTESIAN_POINT('Ctrl Pts',(0.76219646379196,54.1530019391863,15.11932691662));
#57195=CARTESIAN_POINT('Ctrl Pts',(-0.379980518396253,54.2946959603654,
15.3548666883329));
#57196=CARTESIAN_POINT('Ctrl Pts',(-1.60280114527924,54.4504647292807,14.7380741477106));
#57197=CARTESIAN_POINT('Ctrl Pts',(-2.119511433952,54.6214417658209,13.3998286427744));
#57198=CARTESIAN_POINT('Ctrl Pts',(-1.84805341422617,54.7704180108169,12.1845180963029));
#57199=CARTESIAN_POINT('Ctrl Pts',(-1.15058454821746,54.8857021713809,11.5177200975638));
#57200=CARTESIAN_POINT('Ctrl Pts',(-0.607910694635962,54.9584165398788,
11.3000406935775));
#57201=CARTESIAN_POINT('Ctrl Pts',(-0.384084660020667,54.9872958550554,
11.240750409036));
#57202=CARTESIAN_POINT('Ctrl Pts',(-0.155451669286306,55.0162505934249,
11.2001667278884));
#57203=CARTESIAN_POINT('Ctrl Pts',(0.136236732568041,55.0525881695729,11.185156402327));
#57204=CARTESIAN_POINT('Ctrl Pts',(0.603307105703516,55.1110457654735,11.2384407723527));
#57205=CARTESIAN_POINT('Ctrl Pts',(1.16239040941207,55.1847091028723,11.4506788670608));
#57206=CARTESIAN_POINT('Ctrl Pts',(1.90854826039242,55.3038866520108,12.0680945425943));
#57207=CARTESIAN_POINT('Ctrl Pts',(2.38882431469308,55.4553824358178,13.2562329772914));
#57208=CARTESIAN_POINT('Ctrl Pts',(1.95430780379812,55.6414163194288,14.7710242764318));
#57209=CARTESIAN_POINT('Ctrl Pts',(0.650492552779959,55.8318581708404,15.7187839912398));
#57210=CARTESIAN_POINT('Ctrl Pts',(-0.999202214726866,56.0268417285148,
15.6629550914944));
#57211=CARTESIAN_POINT('Ctrl Pts',(-2.2951136204419,56.2264758696457,14.5776809166717));
#57212=CARTESIAN_POINT('Ctrl Pts',(-2.5366416601022,56.3627161449828,13.4507655792797));
#57213=CARTESIAN_POINT('Ctrl Pts',(-2.46825949632321,56.4316314111821,12.90289162838));
#57214=CARTESIAN_POINT('Ctrl Pts',(-2.30565904042138,45.5654608789673,11.3661975024612));
#57215=CARTESIAN_POINT('Ctrl Pts',(-1.86577890195538,45.6499463997848,10.8516310251641));
#57216=CARTESIAN_POINT('Ctrl Pts',(-0.641242660313543,45.816608935898,10.1460569362544));
#57217=CARTESIAN_POINT('Ctrl Pts',(1.42969953062964,46.063816421259,10.4501733917502));
#57218=CARTESIAN_POINT('Ctrl Pts',(2.85245049954171,46.3071808960092,11.9406026138709));
#57219=CARTESIAN_POINT('Ctrl Pts',(3.05558437982819,46.5482196321492,13.9708984611688));
#57220=CARTESIAN_POINT('Ctrl Pts',(1.97903980437475,46.7867293039377,15.6790675364112));
#57221=CARTESIAN_POINT('Ctrl Pts',(0.0997422031405143,47.0225246979377,
16.354867546064));
#57222=CARTESIAN_POINT('Ctrl Pts',(-1.77088105666362,47.2554368056156,15.7419502206933));
#57223=CARTESIAN_POINT('Ctrl Pts',(-2.98401760525766,47.51086192616,13.9441081235967));
#57224=CARTESIAN_POINT('Ctrl Pts',(-2.62426560333524,47.7370551058119,11.9878883323483));
#57225=CARTESIAN_POINT('Ctrl Pts',(-1.55347588276063,47.9104210528862,11.0433510057079));
#57226=CARTESIAN_POINT('Ctrl Pts',(-0.824271881901055,48.0087424085889,
10.735919171988));
#57227=CARTESIAN_POINT('Ctrl Pts',(-0.0474552309468843,48.1065648952709,
10.5962142445523));
#57228=CARTESIAN_POINT('Ctrl Pts',(0.936010136026854,48.2279002678246,10.7487686199371));
#57229=CARTESIAN_POINT('Ctrl Pts',(1.91678341410505,48.3719800511437,11.4133823393088));
#57230=CARTESIAN_POINT('Ctrl Pts',(2.50997870829564,48.5145262047812,12.4199295311954));
#57231=CARTESIAN_POINT('Ctrl Pts',(2.66061544197642,48.7025352976575,13.9605793923149));
#57232=CARTESIAN_POINT('Ctrl Pts',(1.55042730245208,48.933693873436,15.6717751203539));
#57233=CARTESIAN_POINT('Ctrl Pts',(-0.631040980438996,49.1823525442919,
15.9192311347505));
#57234=CARTESIAN_POINT('Ctrl Pts',(-2.11517929405329,49.4040324788164,14.7675119280446));
#57235=CARTESIAN_POINT('Ctrl Pts',(-2.53099693059846,49.6002436807348,13.161177305678));
#57236=CARTESIAN_POINT('Ctrl Pts',(-1.87785797182935,49.7932546220171,11.6628436256107));
#57237=CARTESIAN_POINT('Ctrl Pts',(-0.466299333288858,49.9831863709573,
10.8940833058664));
#57238=CARTESIAN_POINT('Ctrl Pts',(1.09679132198281,50.1701774524991,11.1511725961288));
#57239=CARTESIAN_POINT('Ctrl Pts',(1.97694730497387,50.323687610072,12.1062558702991));
#57240=CARTESIAN_POINT('Ctrl Pts',(2.2200660234861,50.4451967754876,13.0632246528585));
#57241=CARTESIAN_POINT('Ctrl Pts',(2.16179884776509,50.5357033682336,13.7960456107689));
#57242=CARTESIAN_POINT('Ctrl Pts',(1.86920332174121,50.6256087662742,14.4650083959747));
#57243=CARTESIAN_POINT('Ctrl Pts',(1.21604893869049,50.7447179086067,15.179547360442));
#57244=CARTESIAN_POINT('Ctrl Pts',(0.0359275727558463,50.8922368104418,
15.5854154119932));
#57245=CARTESIAN_POINT('Ctrl Pts',(-1.36579376356038,51.067295942977,15.1021068853405));
#57246=CARTESIAN_POINT('Ctrl Pts',(-2.16587787421377,51.2406358526476,13.8723096856617));
#57247=CARTESIAN_POINT('Ctrl Pts',(-2.04192832362877,51.4125085559133,12.4223936332311));
#57248=CARTESIAN_POINT('Ctrl Pts',(-1.0600778722892,51.5831728303628,11.362580099908));
#57249=CARTESIAN_POINT('Ctrl Pts',(0.358428055786465,51.7529069167004,11.1300684810987));
#57250=CARTESIAN_POINT('Ctrl Pts',(1.61263354696483,51.9219803428794,11.817572736803));
#57251=CARTESIAN_POINT('Ctrl Pts',(2.24744796919837,52.1094203899309,13.2748358269744));
#57252=CARTESIAN_POINT('Ctrl Pts',(1.6028084901359,52.3154665330345,14.9742750114912));
#57253=CARTESIAN_POINT('Ctrl Pts',(-0.284517802825563,52.5407640288737,
15.6132793684068));
#57254=CARTESIAN_POINT('Ctrl Pts',(-1.98108779736915,52.7672380367141,14.548338131115));
#57255=CARTESIAN_POINT('Ctrl Pts',(-2.24593225158725,52.9955367730046,12.5507060938727));
#57256=CARTESIAN_POINT('Ctrl Pts',(-0.844661895156112,53.2263011523758,
11.0610922239078));
#57257=CARTESIAN_POINT('Ctrl Pts',(0.869573113428819,53.4211666368392,11.1785206660127));
#57258=CARTESIAN_POINT('Ctrl Pts',(1.71083328229292,53.5591559476084,11.9415268412979));
#57259=CARTESIAN_POINT('Ctrl Pts',(1.98294590990857,53.6285762213412,12.4299124325736));
#57260=CARTESIAN_POINT('Ctrl Pts',(2.08959007456053,53.6683724708866,12.7309834583897));
#57261=CARTESIAN_POINT('Ctrl Pts',(2.27496720013922,53.7680712698251,13.5097709453007));
#57262=CARTESIAN_POINT('Ctrl Pts',(1.97222340842641,53.8989493845487,14.6215803669993));
#57263=CARTESIAN_POINT('Ctrl Pts',(0.89465038188734,54.0623411214105,15.421687269184));
#57264=CARTESIAN_POINT('Ctrl Pts',(-0.434402098507794,54.2273460490297,
15.7017375528132));
#57265=CARTESIAN_POINT('Ctrl Pts',(-1.86204774275957,54.4088330168871,14.988814832024));
#57266=CARTESIAN_POINT('Ctrl Pts',(-2.46935470263096,54.6077827186442,13.4337565694896));
#57267=CARTESIAN_POINT('Ctrl Pts',(-2.15929713050285,54.7807996593003,12.0210948829219));
#57268=CARTESIAN_POINT('Ctrl Pts',(-1.35423216557829,54.9143161276471,11.2458975817384));
#57269=CARTESIAN_POINT('Ctrl Pts',(-0.728176554458024,54.9983343641993,
10.9918842512178));
#57270=CARTESIAN_POINT('Ctrl Pts',(-0.470018856663394,55.031676775866,10.9223861532286));
#57271=CARTESIAN_POINT('Ctrl Pts',(-0.206362891446336,55.0650888123121,
10.8744933195446));
#57272=CARTESIAN_POINT('Ctrl Pts',(0.129892479094305,55.1069852111824,10.8558462463508));
#57273=CARTESIAN_POINT('Ctrl Pts',(0.668033059027686,55.1743021874798,10.9150750738386));
#57274=CARTESIAN_POINT('Ctrl Pts',(1.31164732367071,55.2589776680331,11.1565853466934));
#57275=CARTESIAN_POINT('Ctrl Pts',(2.16980807937479,55.395599927025,11.8612187217518));
#57276=CARTESIAN_POINT('Ctrl Pts',(2.72219984855538,55.5685285024121,13.2158867534057));
#57277=CARTESIAN_POINT('Ctrl Pts',(2.23437211680906,55.7795085295374,14.93536151132));
#57278=CARTESIAN_POINT('Ctrl Pts',(0.769178714778771,55.9939526145872,16.0068421910926));
#57279=CARTESIAN_POINT('Ctrl Pts',(-1.07457772221616,56.2118379980202,15.9496147996879));
#57280=CARTESIAN_POINT('Ctrl Pts',(-2.51436848419478,56.4331159822358,14.7506091228876));
#57281=CARTESIAN_POINT('Ctrl Pts',(-2.78329272553774,56.5828508457323,13.5127385387917));
#57282=CARTESIAN_POINT('Ctrl Pts',(-2.71099830929853,56.6582558952658,12.9129240239044));
#57283=CARTESIAN_POINT('Ctrl Pts',(-2.14027939152463,45.7730825127326,11.5660067125305));
#57284=CARTESIAN_POINT('Ctrl Pts',(-1.74041771225189,45.8504678483019,11.0919855577126));
#57285=CARTESIAN_POINT('Ctrl Pts',(-0.626255958572784,46.0025890400772,
10.441730633043));
#57286=CARTESIAN_POINT('Ctrl Pts',(1.25361264950939,46.226777695605,10.7065986783383));
#57287=CARTESIAN_POINT('Ctrl Pts',(2.54452730673143,46.4461763207554,12.0425156353896));
#57288=CARTESIAN_POINT('Ctrl Pts',(2.73830159988116,46.6623013886306,13.8619287458641));
#57289=CARTESIAN_POINT('Ctrl Pts',(1.78779448617996,46.8751179983104,15.3926009964812));
#57290=CARTESIAN_POINT('Ctrl Pts',(0.122164295117624,47.0846127176156,16.0046777804299));
#57291=CARTESIAN_POINT('Ctrl Pts',(-1.53788417221276,47.290795404332,15.4740393052136));
#57292=CARTESIAN_POINT('Ctrl Pts',(-2.62062632329518,47.5162410472015,13.8951269855267));
#57293=CARTESIAN_POINT('Ctrl Pts',(-2.31712263304767,47.7153786796623,12.1702446962084));
#57294=CARTESIAN_POINT('Ctrl Pts',(-1.38228941300507,47.8678319479962,11.3318172272074));
#57295=CARTESIAN_POINT('Ctrl Pts',(-0.743379299576394,47.9542712505232,
11.0561284084246));
#57296=CARTESIAN_POINT('Ctrl Pts',(-0.0614662828139273,48.0402619260491,
10.927558310766));
#57297=CARTESIAN_POINT('Ctrl Pts',(0.804323002403269,48.1469241896833,11.0543292263492));
#57298=CARTESIAN_POINT('Ctrl Pts',(1.67200255398421,48.2736316016426,11.6314195083817));
#57299=CARTESIAN_POINT('Ctrl Pts',(2.20192978851605,48.3990933885702,12.5129194563287));
#57300=CARTESIAN_POINT('Ctrl Pts',(2.34671685700884,48.5647796925803,13.8695157366898));
#57301=CARTESIAN_POINT('Ctrl Pts',(1.38041978153337,48.7690123591587,15.391151363593));
#57302=CARTESIAN_POINT('Ctrl Pts',(-0.554800061577224,48.989828017531,15.630553016929));
#57303=CARTESIAN_POINT('Ctrl Pts',(-1.89123635946174,49.187891064915,14.6144608515597));
#57304=CARTESIAN_POINT('Ctrl Pts',(-2.27942679155528,49.3642847386172,13.1738421618322));
#57305=CARTESIAN_POINT('Ctrl Pts',(-1.70155746521163,49.5390555916114,11.8109115882085));
#57306=CARTESIAN_POINT('Ctrl Pts',(-0.419837453047116,49.7124465296351,
11.0959486067296));
#57307=CARTESIAN_POINT('Ctrl Pts',(1.02274493966303,49.884705831022,11.3181689765725));
#57308=CARTESIAN_POINT('Ctrl Pts',(1.85076977950379,50.0275304024743,12.1986873373171));
#57309=CARTESIAN_POINT('Ctrl Pts',(2.08670366513554,50.1414890883567,13.0944260893894));
#57310=CARTESIAN_POINT('Ctrl Pts',(2.03770495762297,50.2268407621304,13.7860711292522));
#57311=CARTESIAN_POINT('Ctrl Pts',(1.76555785776637,50.3121079870555,14.423021260958));
#57312=CARTESIAN_POINT('Ctrl Pts',(1.14821454506869,50.4257325901016,15.1099789743916));
#57313=CARTESIAN_POINT('Ctrl Pts',(0.0159524118404732,50.5677252266712,
15.5117608197789));
#57314=CARTESIAN_POINT('Ctrl Pts',(-1.35483150298962,50.7383244061134,15.0538408040168));
#57315=CARTESIAN_POINT('Ctrl Pts',(-2.15600798820678,50.9094064194321,13.8472058420274));
#57316=CARTESIAN_POINT('Ctrl Pts',(-2.0452060214164,51.0812381870027,12.3962437455714));
#57317=CARTESIAN_POINT('Ctrl Pts',(-1.06007602045816,51.2540789421413,11.3140233760055));
#57318=CARTESIAN_POINT('Ctrl Pts',(0.393220475565066,51.4281917425227,11.0632511082158));
#57319=CARTESIAN_POINT('Ctrl Pts',(1.70194021914503,51.6038174996348,11.7671433158644));
#57320=CARTESIAN_POINT('Ctrl Pts',(2.3813336989747,51.8009034045937,13.2942865486876));
#57321=CARTESIAN_POINT('Ctrl Pts',(1.70953298962604,52.0205149535647,15.1116650631418));
#57322=CARTESIAN_POINT('Ctrl Pts',(-0.325700821288032,52.2641141168841,
15.8188950798337));
#57323=CARTESIAN_POINT('Ctrl Pts',(-2.19299708317051,52.5121763433595,14.6656692812233));
#57324=CARTESIAN_POINT('Ctrl Pts',(-2.50081734121616,52.7650950122649,12.4543130199027));
#57325=CARTESIAN_POINT('Ctrl Pts',(-0.942984791680106,53.0232126589936,
10.7785134485666));
#57326=CARTESIAN_POINT('Ctrl Pts',(0.990419469933448,53.2428748001176,10.9010410972588));
#57327=CARTESIAN_POINT('Ctrl Pts',(1.94647448835483,53.3991221449744,11.7615404602951));
#57328=CARTESIAN_POINT('Ctrl Pts',(2.25711350756306,53.4778755159918,12.3145370492997));
#57329=CARTESIAN_POINT('Ctrl Pts',(2.37937124148029,53.5230588412163,12.6559775396749));
#57330=CARTESIAN_POINT('Ctrl Pts',(2.59300773735541,53.6363183428028,13.5400127844654));
#57331=CARTESIAN_POINT('Ctrl Pts',(2.25317651268817,53.7853312499472,14.8073547464846));
#57332=CARTESIAN_POINT('Ctrl Pts',(1.02710429998273,53.9716803036347,15.7240476217481));
#57333=CARTESIAN_POINT('Ctrl Pts',(-0.488823678619321,54.159996137694,16.0486084172937));
#57334=CARTESIAN_POINT('Ctrl Pts',(-2.12129434023988,54.3672013044936,15.2395555163373));
#57335=CARTESIAN_POINT('Ctrl Pts',(-2.81919797130991,54.5941236714676,13.4676844962047));
#57336=CARTESIAN_POINT('Ctrl Pts',(-2.47054084677949,54.7911813077835,11.857671669541));
#57337=CARTESIAN_POINT('Ctrl Pts',(-1.55787978293911,54.9429300839132,10.9740750659129));
#57338=CARTESIAN_POINT('Ctrl Pts',(-0.848442414280066,55.0382521885198,
10.6837278088581));
#57339=CARTESIAN_POINT('Ctrl Pts',(-0.555953053306101,55.0760576966764,
10.6040218974212));
#57340=CARTESIAN_POINT('Ctrl Pts',(-0.257274113606343,55.1139270311992,
10.5488199112007));
#57341=CARTESIAN_POINT('Ctrl Pts',(0.123548225620592,55.1613822527919,10.5265360903747));
#57342=CARTESIAN_POINT('Ctrl Pts',(0.73275901235188,55.2375586094862,10.5917093753247));
#57343=CARTESIAN_POINT('Ctrl Pts',(1.46090423792938,55.3332462331937,10.862491826326));
#57344=CARTESIAN_POINT('Ctrl Pts',(2.43106789835719,55.4873132020393,11.6543429009093));
#57345=CARTESIAN_POINT('Ctrl Pts',(3.0555753824177,55.6816745690064,13.17554052952));
#57346=CARTESIAN_POINT('Ctrl Pts',(2.51443642982003,55.917600739646,15.0996987462084));
#57347=CARTESIAN_POINT('Ctrl Pts',(0.887864876777604,56.1560470583341,16.2949003909454));
#57348=CARTESIAN_POINT('Ctrl Pts',(-1.14995322970545,56.3968342675258,16.2362745078813));
#57349=CARTESIAN_POINT('Ctrl Pts',(-2.73362334794766,56.6397560948261,14.9235373291036));
#57350=CARTESIAN_POINT('Ctrl Pts',(-3.02994379097328,56.8029855464817,13.5747114983036));
#57351=CARTESIAN_POINT('Ctrl Pts',(-2.95373712227385,56.8848803793494,12.9229564194287));
#57352=CARTESIAN_POINT('Ctrl Pts',(-1.97489974262787,45.9807041464979,11.7658159225998));
#57353=CARTESIAN_POINT('Ctrl Pts',(-1.61505652254841,46.0509892968192,11.3323400902612));
#57354=CARTESIAN_POINT('Ctrl Pts',(-0.611269256832031,46.1885691442562,
10.7374043298315));
#57355=CARTESIAN_POINT('Ctrl Pts',(1.07752576838915,46.3897389699512,10.9630239649263));
#57356=CARTESIAN_POINT('Ctrl Pts',(2.23660411392116,46.5851717455016,12.1444286569083));
#57357=CARTESIAN_POINT('Ctrl Pts',(2.42101881993414,46.776383145112,13.7529590305592));
#57358=CARTESIAN_POINT('Ctrl Pts',(1.59654916798518,46.9635066926831,15.1061344565511));
#57359=CARTESIAN_POINT('Ctrl Pts',(0.144586387094734,47.1467007372936,15.6544880147957));
#57360=CARTESIAN_POINT('Ctrl Pts',(-1.30488728776191,47.3261540030483,15.2061283897338));
#57361=CARTESIAN_POINT('Ctrl Pts',(-2.25723504133272,47.5216201682429,13.8461458474566));
#57362=CARTESIAN_POINT('Ctrl Pts',(-2.00997966276009,47.6937022535128,12.3526010600685));
#57363=CARTESIAN_POINT('Ctrl Pts',(-1.2111029432495,47.8252428431062,11.620283448707));
#57364=CARTESIAN_POINT('Ctrl Pts',(-0.662486717251731,47.8998000924574,
11.3763376448611));
#57365=CARTESIAN_POINT('Ctrl Pts',(-0.0754773346809657,47.9739589568271,
11.2589023769796));
#57366=CARTESIAN_POINT('Ctrl Pts',(0.672635868779688,48.065948111542,11.3598898327613));
#57367=CARTESIAN_POINT('Ctrl Pts',(1.42722169386338,48.1752831521415,11.8494566774546));
#57368=CARTESIAN_POINT('Ctrl Pts',(1.89388086873647,48.2836605723592,12.6059093814622));
#57369=CARTESIAN_POINT('Ctrl Pts',(2.03281827204126,48.4270240875031,13.7784520810649));
#57370=CARTESIAN_POINT('Ctrl Pts',(1.21041226061467,48.6043308448814,15.1105276068321));
#57371=CARTESIAN_POINT('Ctrl Pts',(-0.47855914271545,48.7973034907702,15.3418748991076));
#57372=CARTESIAN_POINT('Ctrl Pts',(-1.66729342487016,48.9717496510135,14.4614097750748));
#57373=CARTESIAN_POINT('Ctrl Pts',(-2.0278566525121,49.1283257964996,13.1865070179862));
#57374=CARTESIAN_POINT('Ctrl Pts',(-1.5252569585939,49.2848565612056,11.9589795508061));
#57375=CARTESIAN_POINT('Ctrl Pts',(-0.373375572805371,49.441706688313,11.2978139075926));
#57376=CARTESIAN_POINT('Ctrl Pts',(0.948698557343252,49.599234209545,11.4851653570161));
#57377=CARTESIAN_POINT('Ctrl Pts',(1.7245922540337,49.7313731948764,12.2911188043351));
#57378=CARTESIAN_POINT('Ctrl Pts',(1.95334130678497,49.8377814012258,13.1256275259203));
#57379=CARTESIAN_POINT('Ctrl Pts',(1.91361106748085,49.9179781560273,13.7760966477355));
#57380=CARTESIAN_POINT('Ctrl Pts',(1.66191239379154,49.9986072078368,14.3810341259414));
#57381=CARTESIAN_POINT('Ctrl Pts',(1.08038015144688,50.1067472715965,15.0404105883413));
#57382=CARTESIAN_POINT('Ctrl Pts',(-0.00402274907490241,50.2432136429006,
15.4381062275646));
#57383=CARTESIAN_POINT('Ctrl Pts',(-1.34386924241886,50.4093528692499,15.0055747226929));
#57384=CARTESIAN_POINT('Ctrl Pts',(-2.14613810219979,50.5781769862165,13.822101998393));
#57385=CARTESIAN_POINT('Ctrl Pts',(-2.04848371920403,50.7499678180921,12.3700938579116));
#57386=CARTESIAN_POINT('Ctrl Pts',(-1.06007416862713,50.9249850539197,11.265466652103));
#57387=CARTESIAN_POINT('Ctrl Pts',(0.428012895343668,51.103476568345,10.996433735333));
#57388=CARTESIAN_POINT('Ctrl Pts',(1.79124689132523,51.2856546563901,11.7167138949258));
#57389=CARTESIAN_POINT('Ctrl Pts',(2.51521942875102,51.4923864192564,13.3137372704007));
#57390=CARTESIAN_POINT('Ctrl Pts',(1.81625748911618,51.725563374095,15.2490551147924));
#57391=CARTESIAN_POINT('Ctrl Pts',(-0.366883839750501,51.9874642048946,
16.0245107912607));
#57392=CARTESIAN_POINT('Ctrl Pts',(-2.40490636897185,52.2571146500049,14.7830004313315));
#57393=CARTESIAN_POINT('Ctrl Pts',(-2.75570243084506,52.5346532515253,12.3579199459325));
#57394=CARTESIAN_POINT('Ctrl Pts',(-1.0413076882041,52.8201241656114,10.4959346732253));
#57395=CARTESIAN_POINT('Ctrl Pts',(1.11126582643808,53.0645829633961,10.623561528505));
#57396=CARTESIAN_POINT('Ctrl Pts',(2.18211569441672,53.2390883423404,11.5815540792923));
#57397=CARTESIAN_POINT('Ctrl Pts',(2.53128110521754,53.3271748106425,12.1991616660258));
#57398=CARTESIAN_POINT('Ctrl Pts',(2.66915240840004,53.377745211546,12.58097162096));
#57399=CARTESIAN_POINT('Ctrl Pts',(2.91104827457162,53.5045654157805,13.57025462363));
#57400=CARTESIAN_POINT('Ctrl Pts',(2.53412961694995,53.6717131153456,14.99312912597));
#57401=CARTESIAN_POINT('Ctrl Pts',(1.15955821807812,53.8810194858589,16.0264079743121));
#57402=CARTESIAN_POINT('Ctrl Pts',(-0.543245258730856,54.0926462263583,
16.395479281774));
#57403=CARTESIAN_POINT('Ctrl Pts',(-2.38054093772021,54.3255695921,15.4902962006507));
#57404=CARTESIAN_POINT('Ctrl Pts',(-3.16904123998887,54.5804646242909,13.5016124229199));
#57405=CARTESIAN_POINT('Ctrl Pts',(-2.78178456305616,54.8015629562669,11.69424845616));
#57406=CARTESIAN_POINT('Ctrl Pts',(-1.76152740029993,54.9715440401794,10.7022525500875));
#57407=CARTESIAN_POINT('Ctrl Pts',(-0.968708274102122,55.0781700128403,
10.3755713664983));
#57408=CARTESIAN_POINT('Ctrl Pts',(-0.641887249948822,55.120438617487,10.2856576416139));
#57409=CARTESIAN_POINT('Ctrl Pts',(-0.308185335766365,55.1627652500864,
10.2231465028569));
#57410=CARTESIAN_POINT('Ctrl Pts',(0.117203972146864,55.2157792944013,10.1972259343985));
#57411=CARTESIAN_POINT('Ctrl Pts',(0.797484965676056,55.3008150314925,10.2683436768106));
#57412=CARTESIAN_POINT('Ctrl Pts',(1.61016115218803,55.4075147983545,10.5683983059585));
#57413=CARTESIAN_POINT('Ctrl Pts',(2.69232771733956,55.5790264770535,11.4474670800669));
#57414=CARTESIAN_POINT('Ctrl Pts',(3.38895091628001,55.7948206356007,13.1351943056343));
#57415=CARTESIAN_POINT('Ctrl Pts',(2.79450074283097,56.0556929497546,15.2640359810966));
#57416=CARTESIAN_POINT('Ctrl Pts',(1.00655103877642,56.318141502081,16.5829585907982));
#57417=CARTESIAN_POINT('Ctrl Pts',(-1.22532873719474,56.5818305370312,16.5229342160748));
#57418=CARTESIAN_POINT('Ctrl Pts',(-2.95287821170053,56.8463962074163,15.0964655353195));
#57419=CARTESIAN_POINT('Ctrl Pts',(-3.27659485640882,57.0231202472312,13.6366844578155));
#57420=CARTESIAN_POINT('Ctrl Pts',(-3.19647593524917,57.1115048634331,12.932988814953));
#57421=CARTESIAN_POINT('Ctrl Pts',(-1.95241364042681,45.9847503099714,11.7382273262856));
#57422=CARTESIAN_POINT('Ctrl Pts',(-1.8971421670987,45.9953436461596,11.6735188111325));
#57423=CARTESIAN_POINT('Ctrl Pts',(-1.83865442762089,46.0059232379815,11.6117345120665));
#57424=CARTESIAN_POINT('Ctrl Pts',(-1.77721585694918,46.0164890647086,11.5532444801427));
#57425=CARTESIAN_POINT('Ctrl Pts',(-1.64756344227922,46.0387858879122,11.4298142995552));
#57426=CARTESIAN_POINT('Ctrl Pts',(-1.50476811437305,46.0610213831347,11.3210572491992));
#57427=CARTESIAN_POINT('Ctrl Pts',(-1.35265282291184,46.0831958590439,11.2288377615449));
#57428=CARTESIAN_POINT('Ctrl Pts',(-1.20240674226712,46.1050978523524,11.137751477937));
#57429=CARTESIAN_POINT('Ctrl Pts',(-1.04307002516613,46.1269403212354,11.0627994520531));
#57430=CARTESIAN_POINT('Ctrl Pts',(-0.878344943658423,46.148723958966,11.0057329629921));
#57431=CARTESIAN_POINT('Ctrl Pts',(-0.823649496877625,46.1559570153244,
10.9867845606794));
#57432=CARTESIAN_POINT('Ctrl Pts',(-0.768360021367818,46.1631835884625,
10.9698076438706));
#57433=CARTESIAN_POINT('Ctrl Pts',(-0.71261202736178,46.1704037122867,10.9548650191242));
#57434=CARTESIAN_POINT('Ctrl Pts',(-0.66491427331565,46.176581220491,10.9420801709397));
#57435=CARTESIAN_POINT('Ctrl Pts',(-0.616880865738027,46.1827540075846,
10.930784497145));
#57436=CARTESIAN_POINT('Ctrl Pts',(-0.56860365505536,46.1889220994543,10.9209716054323));
#57437=CARTESIAN_POINT('Ctrl Pts',(-0.431265107463782,46.2064690282601,
10.893055984864));
#57438=CARTESIAN_POINT('Ctrl Pts',(-0.291751219692949,46.2239557050407,
10.8771188680412));
#57439=CARTESIAN_POINT('Ctrl Pts',(-0.152216507090954,46.2413863885295,
10.8730912299346));
#57440=CARTESIAN_POINT('Ctrl Pts',(-0.0102360917695286,46.2591225893281,
10.868992997169));
#57441=CARTESIAN_POINT('Ctrl Pts',(0.131764428199893,46.2768008194013,10.8772253772626));
#57442=CARTESIAN_POINT('Ctrl Pts',(0.271508687144479,46.2944261648867,10.8976631512315));
#57443=CARTESIAN_POINT('Ctrl Pts',(0.344537665980979,46.3036369975331,10.9083437314136));
#57444=CARTESIAN_POINT('Ctrl Pts',(0.416950487390888,46.3128333969747,10.9223567501107));
#57445=CARTESIAN_POINT('Ctrl Pts',(0.488423636868789,46.322016148492,10.939678813146));
#57446=CARTESIAN_POINT('Ctrl Pts',(0.625333006365584,46.3396060368582,10.9728598433073));
#57447=CARTESIAN_POINT('Ctrl Pts',(0.758792220052205,46.357145819602,11.0181848126039));
#57448=CARTESIAN_POINT('Ctrl Pts',(0.886906146962075,46.3746414549503,11.0744382700336));
#57449=CARTESIAN_POINT('Ctrl Pts',(0.922014005139931,46.3794358929896,11.0898537557118));
#57450=CARTESIAN_POINT('Ctrl Pts',(0.956720662856293,46.3842270184074,11.1060897099406));
#57451=CARTESIAN_POINT('Ctrl Pts',(0.990987645700955,46.389014959637,11.1231206684141));
#57452=CARTESIAN_POINT('Ctrl Pts',(1.11975164580951,46.4070064608965,11.1871173835225));
#57453=CARTESIAN_POINT('Ctrl Pts',(1.24256507675794,46.4249354693607,11.262486210778));
#57454=CARTESIAN_POINT('Ctrl Pts',(1.35732849364204,46.4428028920159,11.3479832212788));
#57455=CARTESIAN_POINT('Ctrl Pts',(1.4182011948596,46.4522801131578,11.3933324633676));
#57456=CARTESIAN_POINT('Ctrl Pts',(1.47680927481519,46.4617400153292,11.4415303145385));
#57457=CARTESIAN_POINT('Ctrl Pts',(1.53284192491298,46.4711827841931,11.4923857831166));
#57458=CARTESIAN_POINT('Ctrl Pts',(1.6392516195938,46.4891152244756,11.5889636689529));
#57459=CARTESIAN_POINT('Ctrl Pts',(1.73637042168925,46.5069858512471,11.6951278292034));
#57460=CARTESIAN_POINT('Ctrl Pts',(1.82297362114317,46.5247963431438,11.8087410688735));
#57461=CARTESIAN_POINT('Ctrl Pts',(1.90839933305812,46.5423646773326,11.9208095830045));
#57462=CARTESIAN_POINT('Ctrl Pts',(1.98359284293436,46.5598745051721,12.0401246246244));
#57463=CARTESIAN_POINT('Ctrl Pts',(2.04742465939072,46.5773277830352,12.1646161671583));
#57464=CARTESIAN_POINT('Ctrl Pts',(2.05618755650694,46.5797237868895,12.1817064935758));
#57465=CARTESIAN_POINT('Ctrl Pts',(2.06473641007925,46.5821187254778,12.1988943657412));
#57466=CARTESIAN_POINT('Ctrl Pts',(2.07306837637378,46.5845126043074,12.2161744218087));
#57467=CARTESIAN_POINT('Ctrl Pts',(2.11160201547555,46.5955838040237,12.2960911450196));
#57468=CARTESIAN_POINT('Ctrl Pts',(2.14554167347974,46.6066369948493,12.3780773092497));
#57469=CARTESIAN_POINT('Ctrl Pts',(2.17457606972679,46.6176715277991,12.4616120935857));
#57470=CARTESIAN_POINT('Ctrl Pts',(2.21973917011656,46.6348357806779,12.5915507297779));
#57471=CARTESIAN_POINT('Ctrl Pts',(2.2530307354994,46.6519548760391,12.725237010723));
#57472=CARTESIAN_POINT('Ctrl Pts',(2.27437953802083,46.6690266578218,12.8604588311141));
#57473=CARTESIAN_POINT('Ctrl Pts',(2.29577493171289,46.6861356966963,12.9959757567177));
#57474=CARTESIAN_POINT('Ctrl Pts',(2.3051753512887,46.7031972175615,13.1330334363911));
#57475=CARTESIAN_POINT('Ctrl Pts',(2.3025595800891,46.720209314466,13.2693972267247));
#57476=CARTESIAN_POINT('Ctrl Pts',(2.30042405253179,46.7340980680974,13.3807252481215));
#57477=CARTESIAN_POINT('Ctrl Pts',(2.29028047142328,46.7479538853357,13.4915902788484));
#57478=CARTESIAN_POINT('Ctrl Pts',(2.27214231801973,46.7617758427502,13.6007828735325));
#57479=CARTESIAN_POINT('Ctrl Pts',(2.26605711820078,46.7664129946634,13.6374160821408));
#57480=CARTESIAN_POINT('Ctrl Pts',(2.25907228475214,46.7710463362792,13.6738611409023));
#57481=CARTESIAN_POINT('Ctrl Pts',(2.25120957080458,46.7756758366425,13.7100774197308));
#57482=CARTESIAN_POINT('Ctrl Pts',(2.2210005603269,46.793462649938,13.8492224978668));
#57483=CARTESIAN_POINT('Ctrl Pts',(2.17776659788189,46.8111909930459,13.985265270644));
#57484=CARTESIAN_POINT('Ctrl Pts',(2.12261993130273,46.8288630348613,14.1158844579314));
#57485=CARTESIAN_POINT('Ctrl Pts',(2.06598742150198,46.8470112230183,14.250022980948));
#57486=CARTESIAN_POINT('Ctrl Pts',(1.99679213031932,46.8651000380505,14.3784402361469));
#57487=CARTESIAN_POINT('Ctrl Pts',(1.91629136575179,46.88313210643,14.4986320939029));
#57488=CARTESIAN_POINT('Ctrl Pts',(1.88585063708702,46.8899507907463,14.5440816961437));
#57489=CARTESIAN_POINT('Ctrl Pts',(1.8537938087849,46.8967613633154,14.5883553540662));
#57490=CARTESIAN_POINT('Ctrl Pts',(1.82019050855776,46.9035639746694,14.6313187155398));
#57491=CARTESIAN_POINT('Ctrl Pts',(1.73100455685324,46.9216186705947,14.7453470477436));
#57492=CARTESIAN_POINT('Ctrl Pts',(1.63092320563563,46.9396172750017,14.8501422182976));
#57493=CARTESIAN_POINT('Ctrl Pts',(1.52223787899297,46.9575628219442,14.9442418774281));
#57494=CARTESIAN_POINT('Ctrl Pts',(1.51188162730683,46.9592727915098,14.953208310926));
#57495=CARTESIAN_POINT('Ctrl Pts',(1.501447273049,46.9609822794534,14.9620776692662));
#57496=CARTESIAN_POINT('Ctrl Pts',(1.49093680841019,46.9626912884685,14.9708487102848));
#57497=CARTESIAN_POINT('Ctrl Pts',(1.38006322227004,46.9807194123196,15.063373332681));
#57498=CARTESIAN_POINT('Ctrl Pts',(1.26055089980399,46.9986943927912,15.1450935129852));
#57499=CARTESIAN_POINT('Ctrl Pts',(1.13468374163679,47.0166184141626,15.2144752016254));
#57500=CARTESIAN_POINT('Ctrl Pts',(1.07265992579405,47.0254508706738,15.2486645576237));
#57501=CARTESIAN_POINT('Ctrl Pts',(1.00909365887041,47.0342709560681,15.2798583357467));
#57502=CARTESIAN_POINT('Ctrl Pts',(0.944261256667278,47.0430789466427,15.3078764650197));
#57503=CARTESIAN_POINT('Ctrl Pts',(0.812475281708041,47.0609831054559,15.3648294138124));
#57504=CARTESIAN_POINT('Ctrl Pts',(0.675457283418255,47.078837283571,15.4086575150184));
#57505=CARTESIAN_POINT('Ctrl Pts',(0.536001779571398,47.0966439332634,15.4389983175078));
#57506=CARTESIAN_POINT('Ctrl Pts',(0.40699792754375,47.1131160432818,15.4670651939434));
#57507=CARTESIAN_POINT('Ctrl Pts',(0.275909476634552,47.1295474859783,15.4835910086528));
#57508=CARTESIAN_POINT('Ctrl Pts',(0.144946080722838,47.1459402512969,15.4883285461524));
#57509=CARTESIAN_POINT('Ctrl Pts',(0.052400211512539,47.1575242721954,15.4916763482063));
#57510=CARTESIAN_POINT('Ctrl Pts',(-0.0401751944031819,47.16907224139,15.4891450692736));
#57511=CARTESIAN_POINT('Ctrl Pts',(-0.132013920397452,47.1805906345695,
15.4806224156613));
#57512=CARTESIAN_POINT('Ctrl Pts',(-0.302049520997157,47.2019164628736,
15.4648430751927));
#57513=CARTESIAN_POINT('Ctrl Pts',(-0.469560729760759,47.2231409413218,
15.4285225448653));
#57514=CARTESIAN_POINT('Ctrl Pts',(-0.630324528041842,47.2443051016368,
15.3737808941178));
#57515=CARTESIAN_POINT('Ctrl Pts',(-0.798772123195201,47.2664808149916,
15.3164228351411));
#57516=CARTESIAN_POINT('Ctrl Pts',(-0.959810524721762,47.2885903429389,
15.2388406836729));
#57517=CARTESIAN_POINT('Ctrl Pts',(-1.10857004406211,47.3106800499252,15.1435280009256));
#57518=CARTESIAN_POINT('Ctrl Pts',(-1.14179459733405,47.3156136545092,15.1222404805069));
#57519=CARTESIAN_POINT('Ctrl Pts',(-1.17440665457436,47.3205462659255,15.1000687222124));
#57520=CARTESIAN_POINT('Ctrl Pts',(-1.20635200726083,47.3254783924175,15.0770408546523));
#57521=CARTESIAN_POINT('Ctrl Pts',(-1.28232251514563,47.3372076776825,15.0222773711744));
#57522=CARTESIAN_POINT('Ctrl Pts',(-1.3545961616888,47.3488715301593,14.9626333442155));
#57523=CARTESIAN_POINT('Ctrl Pts',(-1.42240277269893,47.3604896246544,14.8984908981873));
#57524=CARTESIAN_POINT('Ctrl Pts',(-1.5073465397739,47.375044027211,14.8181373616534));
#57525=CARTESIAN_POINT('Ctrl Pts',(-1.58527821899684,47.3895266455885,14.7307232409101));
#57526=CARTESIAN_POINT('Ctrl Pts',(-1.6554807059147,47.4039757275965,14.6377529363878));
#57527=CARTESIAN_POINT('Ctrl Pts',(-1.72591693999175,47.4184729194653,14.5444730766698));
#57528=CARTESIAN_POINT('Ctrl Pts',(-1.78857168988701,47.4329363652546,14.4456010916711));
#57529=CARTESIAN_POINT('Ctrl Pts',(-1.84276115801007,47.4474039676963,14.3426893008476));
#57530=CARTESIAN_POINT('Ctrl Pts',(-1.8952760752046,47.4614244954953,14.2429576673655));
#57531=CARTESIAN_POINT('Ctrl Pts',(-1.93984036957768,47.475448934269,14.1394331900176));
#57532=CARTESIAN_POINT('Ctrl Pts',(-1.97587791985858,47.4895109490354,14.0335425918392));
#57533=CARTESIAN_POINT('Ctrl Pts',(-1.98602212383801,47.4934692632116,14.0037354651324));
#57534=CARTESIAN_POINT('Ctrl Pts',(-1.99549100902068,47.4974305492356,13.9737408854396));
#57535=CARTESIAN_POINT('Ctrl Pts',(-2.00427248941019,47.5013955444323,13.9435906943912));
#57536=CARTESIAN_POINT('Ctrl Pts',(-2.03063765510875,47.5132998875177,13.8530689659838));
#57537=CARTESIAN_POINT('Ctrl Pts',(-2.05090427372228,47.5251676359854,13.7609038126534));
#57538=CARTESIAN_POINT('Ctrl Pts',(-2.06467398077651,47.5369983931114,13.6679110418037));
#57539=CARTESIAN_POINT('Ctrl Pts',(-2.08331667921734,47.5530159624438,13.542008858315));
#57540=CARTESIAN_POINT('Ctrl Pts',(-2.09004753037163,47.5689657217592,13.4145893286777));
#57541=CARTESIAN_POINT('Ctrl Pts',(-2.0853251332468,47.5848469350357,13.2877517923853));
#57542=CARTESIAN_POINT('Ctrl Pts',(-2.080469850256,47.6011750376193,13.1573451119905));
#57543=CARTESIAN_POINT('Ctrl Pts',(-2.0635077757518,47.6174306848979,13.0275550939873));
#57544=CARTESIAN_POINT('Ctrl Pts',(-2.03499220175551,47.6336132009398,12.9006765006415));
#57545=CARTESIAN_POINT('Ctrl Pts',(-2.00676774037093,47.6496305113117,12.7750931980263));
#57546=CARTESIAN_POINT('Ctrl Pts',(-1.96722491767763,47.6655761794401,12.6523637092149));
#57547=CARTESIAN_POINT('Ctrl Pts',(-1.91694860837323,47.6814496221164,12.5347033318195));
#57548=CARTESIAN_POINT('Ctrl Pts',(-1.88677704915636,47.6909755105976,12.4640935934918));
#57549=CARTESIAN_POINT('Ctrl Pts',(-1.85274085457809,47.7004753891121,12.3953091388544));
#57550=CARTESIAN_POINT('Ctrl Pts',(-1.81497392706467,47.7099491365865,12.3288235383124));
#57551=CARTESIAN_POINT('Ctrl Pts',(-1.78679056988097,47.7170188673408,12.2792090329497));
#57552=CARTESIAN_POINT('Ctrl Pts',(-1.75652979937312,47.724074046305,12.2308746093299));
#57553=CARTESIAN_POINT('Ctrl Pts',(-1.72434746508382,47.7311146195406,12.1839532034194));
#57554=CARTESIAN_POINT('Ctrl Pts',(-1.65491285062346,47.7463049249984,12.082718479423));
#57555=CARTESIAN_POINT('Ctrl Pts',(-1.57635114487308,47.7616179338749,11.9879144256428));
#57556=CARTESIAN_POINT('Ctrl Pts',(-1.49018644155164,47.7769591100884,11.9009221587838));
#57557=CARTESIAN_POINT('Ctrl Pts',(-1.4559767182022,47.783049972981,11.8663838702727));
#57558=CARTESIAN_POINT('Ctrl Pts',(-1.42056894123929,47.7891453089514,11.8330765223171));
#57559=CARTESIAN_POINT('Ctrl Pts',(-1.38405974379315,47.7952393381944,11.8010846975313));
#57560=CARTESIAN_POINT('Ctrl Pts',(-1.291106066256,47.8107549471034,11.7196324067941));
#57561=CARTESIAN_POINT('Ctrl Pts',(-1.19101258933282,47.826261822322,11.6467114019376));
#57562=CARTESIAN_POINT('Ctrl Pts',(-1.08551772136646,47.8416672343656,11.5835119067454));
#57563=CARTESIAN_POINT('Ctrl Pts',(-1.07937807937506,47.8425638060804,11.5798337915726));
#57564=CARTESIAN_POINT('Ctrl Pts',(-1.0732201420744,47.8434600351941,11.5761885890833));
#57565=CARTESIAN_POINT('Ctrl Pts',(-1.06704425165267,47.8443559038265,11.5725765284172));
#57566=CARTESIAN_POINT('Ctrl Pts',(-0.984182526285751,47.8563757447734,
11.5241136253402));
#57567=CARTESIAN_POINT('Ctrl Pts',(-0.898114350906959,47.8683270587626,
11.4816288003348));
#57568=CARTESIAN_POINT('Ctrl Pts',(-0.809594952477851,47.8801958143893,
11.4456461415384));
#57569=CARTESIAN_POINT('Ctrl Pts',(-0.759797690759056,47.8868726732554,
11.4254038228013));
#57570=CARTESIAN_POINT('Ctrl Pts',(-0.709224300952944,47.8935234177675,
11.4072196096752));
#57571=CARTESIAN_POINT('Ctrl Pts',(-0.65803506781527,47.9001456523423,11.3910910199214));
#57572=CARTESIAN_POINT('Ctrl Pts',(-0.556989608908551,47.9132176733626,
11.3592538414116));
#57573=CARTESIAN_POINT('Ctrl Pts',(-0.453567639932314,47.9262319211411,
11.3354679413944));
#57574=CARTESIAN_POINT('Ctrl Pts',(-0.349152492158056,47.9392851887089,
11.3198053610108));
#57575=CARTESIAN_POINT('Ctrl Pts',(-0.306643092427297,47.944599423096,11.31342882557));
#57576=CARTESIAN_POINT('Ctrl Pts',(-0.263969510184714,47.9499200773217,
11.3083982854292));
#57577=CARTESIAN_POINT('Ctrl Pts',(-0.221226672214552,47.9552534808775,
11.3047166934343));
#57578=CARTESIAN_POINT('Ctrl Pts',(-0.0941688513748754,47.9711076137719,
11.2937727533895));
#57579=CARTESIAN_POINT('Ctrl Pts',(0.0336667007323784,47.987073378859,11.2947215717854));
#57580=CARTESIAN_POINT('Ctrl Pts',(0.159977082598235,48.0030097641556,11.30753003906));
#57581=CARTESIAN_POINT('Ctrl Pts',(0.277107148884844,48.0177878832507,11.3194075791224));
#57582=CARTESIAN_POINT('Ctrl Pts',(0.392926303456317,48.0325407724067,11.3414822374556));
#57583=CARTESIAN_POINT('Ctrl Pts',(0.505635732065545,48.0471617049776,11.3737411872782));
#57584=CARTESIAN_POINT('Ctrl Pts',(0.554022137755661,48.0534385034999,11.3875900254145));
#57585=CARTESIAN_POINT('Ctrl Pts',(0.601835856642591,48.0596910546578,11.4033161257713));
#57586=CARTESIAN_POINT('Ctrl Pts',(0.648968025783451,48.0659112574905,11.4208298094681));
#57587=CARTESIAN_POINT('Ctrl Pts',(0.792745122678298,48.0848860409917,11.4742554557677));
#57588=CARTESIAN_POINT('Ctrl Pts',(0.929914752706283,48.1037959420619,11.5443812200174));
#57589=CARTESIAN_POINT('Ctrl Pts',(1.0572203088745,48.122757211789,11.6287132239111));
#57590=CARTESIAN_POINT('Ctrl Pts',(1.17368682969203,48.1401040832207,11.7058650418106));
#57591=CARTESIAN_POINT('Ctrl Pts',(1.28189670087718,48.1574938913579,11.794909079678));
#57592=CARTESIAN_POINT('Ctrl Pts',(1.37931897278784,48.1750092485061,11.8939281093346));
#57593=CARTESIAN_POINT('Ctrl Pts',(1.44817970563592,48.1873895831634,11.9639174743364));
#57594=CARTESIAN_POINT('Ctrl Pts',(1.51178307075387,48.1997032029502,12.0388925787864));
#57595=CARTESIAN_POINT('Ctrl Pts',(1.56921941560834,48.2119536546085,12.1181775659105));
#57596=CARTESIAN_POINT('Ctrl Pts',(1.64793677992031,48.2287430806872,12.2268388191942));
#57597=CARTESIAN_POINT('Ctrl Pts',(1.71506824146787,48.2454138784686,12.3435963825234));
#57598=CARTESIAN_POINT('Ctrl Pts',(1.76975360272235,48.2619748990657,12.4657448884544));
#57599=CARTESIAN_POINT('Ctrl Pts',(1.79332319336232,48.269112759493,12.5183913411071));
#57600=CARTESIAN_POINT('Ctrl Pts',(1.81458124833026,48.2762302216107,12.5720387813991));
#57601=CARTESIAN_POINT('Ctrl Pts',(1.83346141180619,48.2833279657749,12.6264690528864));
#57602=CARTESIAN_POINT('Ctrl Pts',(1.86759929129462,48.2961616435777,12.7248863177013));
#57603=CARTESIAN_POINT('Ctrl Pts',(1.89399287542128,48.3088998382903,12.8258755189266));
#57604=CARTESIAN_POINT('Ctrl Pts',(1.91217778741452,48.3216474325737,12.9281520763732));
#57605=CARTESIAN_POINT('Ctrl Pts',(1.91764729273875,48.3254815470765,12.9589139615946));
#57606=CARTESIAN_POINT('Ctrl Pts',(1.92237425929101,48.3293164669574,12.9897919553678));
#57607=CARTESIAN_POINT('Ctrl Pts',(1.92634626748762,48.3331549282506,13.020750204952));
#57608=CARTESIAN_POINT('Ctrl Pts',(1.93922945297624,48.3456049551347,13.1211631074573));
#57609=CARTESIAN_POINT('Ctrl Pts',(1.94416821334328,48.3580927182959,13.2224235142376));
#57610=CARTESIAN_POINT('Ctrl Pts',(1.94124327456912,48.3707074724205,13.3232142749551));
#57611=CARTESIAN_POINT('Ctrl Pts',(1.93975556789633,48.3771236935231,13.3744793094918));
#57612=CARTESIAN_POINT('Ctrl Pts',(1.93623392363029,48.3835726662027,13.4256221544924));
#57613=CARTESIAN_POINT('Ctrl Pts',(1.93069244633872,48.3900654906189,13.4764656414149));
#57614=CARTESIAN_POINT('Ctrl Pts',(1.9195958753464,48.4030670934918,13.5782775468776));
#57615=CARTESIAN_POINT('Ctrl Pts',(1.90062231617946,48.4159740217048,13.6792652673937));
#57616=CARTESIAN_POINT('Ctrl Pts',(1.87381672141904,48.428819389061,13.7780564811559));
#57617=CARTESIAN_POINT('Ctrl Pts',(1.85561139991501,48.4375434649357,13.8451516463402));
#57618=CARTESIAN_POINT('Ctrl Pts',(1.83379425904398,48.4462391002347,13.9112327574732));
#57619=CARTESIAN_POINT('Ctrl Pts',(1.80839081469691,48.4549160542697,13.9758624728608));
#57620=CARTESIAN_POINT('Ctrl Pts',(1.77084002294634,48.4677421297241,14.071396643356));
#57621=CARTESIAN_POINT('Ctrl Pts',(1.72545042400657,48.4805275074423,14.1637591733987));
#57622=CARTESIAN_POINT('Ctrl Pts',(1.67309195688153,48.4933016388624,14.2519334979011));
#57623=CARTESIAN_POINT('Ctrl Pts',(1.6205358691939,48.5061239846627,14.3404406254929));
#57624=CARTESIAN_POINT('Ctrl Pts',(1.56095847103348,48.5189350110995,14.4247267175243));
#57625=CARTESIAN_POINT('Ctrl Pts',(1.4952920782572,48.531761794563,14.5037685682419));
#57626=CARTESIAN_POINT('Ctrl Pts',(1.43148393269753,48.5442256018729,14.5805736690349));
#57627=CARTESIAN_POINT('Ctrl Pts',(1.36192713639654,48.5567042823722,14.652426058278));
#57628=CARTESIAN_POINT('Ctrl Pts',(1.2875196963635,48.5692200943733,14.718407959033));
#57629=CARTESIAN_POINT('Ctrl Pts',(1.21831432097887,48.5808608855011,14.7797768518254));
#57630=CARTESIAN_POINT('Ctrl Pts',(1.1449135718977,48.5925337765941,14.8360668230429));
#57631=CARTESIAN_POINT('Ctrl Pts',(1.06806755633897,48.6042546205366,14.8865691212847));
#57632=CARTESIAN_POINT('Ctrl Pts',(0.997855878415097,48.6149635702968,14.9327114108072));
#57633=CARTESIAN_POINT('Ctrl Pts',(0.924597377811292,48.6256213621673,14.9742971533863));
#57634=CARTESIAN_POINT('Ctrl Pts',(0.848780767190351,48.6362346500015,15.0107513008384));
#57635=CARTESIAN_POINT('Ctrl Pts',(0.751475927923849,48.6498559957507,15.0575374197294));
#57636=CARTESIAN_POINT('Ctrl Pts',(0.649955872521592,48.6634040823214,15.0958688731996));
#57637=CARTESIAN_POINT('Ctrl Pts',(0.545925605715438,48.6768917648121,15.1254196313063));
#57638=CARTESIAN_POINT('Ctrl Pts',(0.496346508051243,48.6833197703148,15.1395030319088));
#57639=CARTESIAN_POINT('Ctrl Pts',(0.446197952127165,48.6897340371865,15.151592479276));
#57640=CARTESIAN_POINT('Ctrl Pts',(0.39566769098551,48.6961358496051,15.1616552427937));
#57641=CARTESIAN_POINT('Ctrl Pts',(0.285443684121811,48.710100420538,15.1836056164902));
#57642=CARTESIAN_POINT('Ctrl Pts',(0.173402081440556,48.7240058432638,15.1959092671239));
#57643=CARTESIAN_POINT('Ctrl Pts',(0.0612786825161412,48.7378643888788,
15.1985578236115));
#57644=CARTESIAN_POINT('Ctrl Pts',(-0.0480306448107308,48.7513751128975,
15.201139906663));
#57645=CARTESIAN_POINT('Ctrl Pts',(-0.157416299553511,48.7648412835544,
15.1945452811103));
#57646=CARTESIAN_POINT('Ctrl Pts',(-0.265259931271808,48.7782726460466,
15.1788127927061));
#57647=CARTESIAN_POINT('Ctrl Pts',(-0.361009084575653,48.7901977042614,
15.1648446759052));
#57648=CARTESIAN_POINT('Ctrl Pts',(-0.45554187461286,48.8020953041717,15.1436738368278));
#57649=CARTESIAN_POINT('Ctrl Pts',(-0.547732499780266,48.8139711442149,
15.1153613345604));
#57650=CARTESIAN_POINT('Ctrl Pts',(-0.549470603064334,48.8141950437333,
15.1148275486892));
#57651=CARTESIAN_POINT('Ctrl Pts',(-0.551207874248608,48.8144189354851,
15.1142912253172));
#57652=CARTESIAN_POINT('Ctrl Pts',(-0.552944306625827,48.8146428195046,
15.1137523689517));
#57653=CARTESIAN_POINT('Ctrl Pts',(-0.664401504574121,48.8290133678834,
15.079164543144));
#57654=CARTESIAN_POINT('Ctrl Pts',(-0.772601599312067,48.843484458884,15.0339363505538));
#57655=CARTESIAN_POINT('Ctrl Pts',(-0.87577886749647,48.8580031014277,14.9792130748679));
#57656=CARTESIAN_POINT('Ctrl Pts',(-0.980104126932079,48.8726832841527,
14.9238809262894));
#57657=CARTESIAN_POINT('Ctrl Pts',(-1.07929375723489,48.88741205545,14.8588430427353));
#57658=CARTESIAN_POINT('Ctrl Pts',(-1.17157210490308,48.9021401953873,14.7852989387065));
#57659=CARTESIAN_POINT('Ctrl Pts',(-1.2345600849423,48.912193428977,14.7350987056765));
#57660=CARTESIAN_POINT('Ctrl Pts',(-1.29432902552041,48.9222464846687,14.6809354960996));
#57661=CARTESIAN_POINT('Ctrl Pts',(-1.35032798481397,48.9322852629655,14.6231886578157));
#57662=CARTESIAN_POINT('Ctrl Pts',(-1.423174139881,48.9453441913763,14.5480687772086));
#57663=CARTESIAN_POINT('Ctrl Pts',(-1.48964008048988,48.9583788276777,14.4668858839713));
#57664=CARTESIAN_POINT('Ctrl Pts',(-1.54908346976911,48.9713613939306,14.3809105942702));
#57665=CARTESIAN_POINT('Ctrl Pts',(-1.61918775705424,48.9866723236292,14.2795160324576));
#57666=CARTESIAN_POINT('Ctrl Pts',(-1.67953046460898,49.0019620494912,14.1713370847684));
#57667=CARTESIAN_POINT('Ctrl Pts',(-1.72890459112104,49.0172519579631,14.0584172512926));
#57668=CARTESIAN_POINT('Ctrl Pts',(-1.76437360470154,49.0282358073908,13.9772987507743));
#57669=CARTESIAN_POINT('Ctrl Pts',(-1.7941821594327,49.0392196723324,13.8937348653189));
#57670=CARTESIAN_POINT('Ctrl Pts',(-1.81789005333813,49.0502102248727,13.8084980951964));
#57671=CARTESIAN_POINT('Ctrl Pts',(-1.85030248460895,49.065236044132,13.6919659829656));
#57672=CARTESIAN_POINT('Ctrl Pts',(-1.87130998121406,49.0802745152564,13.5723064933686));
#57673=CARTESIAN_POINT('Ctrl Pts',(-1.88083583906007,49.0953394774193,13.4518206289011));
#57674=CARTESIAN_POINT('Ctrl Pts',(-1.88761187874116,49.1060556546981,13.3661152770219));
#57675=CARTESIAN_POINT('Ctrl Pts',(-1.88857902809562,49.1167851575353,13.2799925802247));
#57676=CARTESIAN_POINT('Ctrl Pts',(-1.88372494476212,49.1275317726247,13.1942859874444));
#57677=CARTESIAN_POINT('Ctrl Pts',(-1.87755267939483,49.1411967543679,13.0853047858414));
#57678=CARTESIAN_POINT('Ctrl Pts',(-1.86203948095439,49.1548733590618,12.9767539644173));
#57679=CARTESIAN_POINT('Ctrl Pts',(-1.83710075861715,49.1685569018034,12.8703323036927));
#57680=CARTESIAN_POINT('Ctrl Pts',(-1.81005128630724,49.1833985847689,12.7549033845196));
#57681=CARTESIAN_POINT('Ctrl Pts',(-1.7719122407144,49.1982484328727,12.6419806903053));
#57682=CARTESIAN_POINT('Ctrl Pts',(-1.72364873600501,49.2131003184208,12.5335051899417));
#57683=CARTESIAN_POINT('Ctrl Pts',(-1.67524198645834,49.2279962839821,12.4247077370907));
#57684=CARTESIAN_POINT('Ctrl Pts',(-1.61665127013422,49.2428943005386,12.3203853663485));
#57685=CARTESIAN_POINT('Ctrl Pts',(-1.54889859525585,49.2577880297835,12.2224801538035));
#57686=CARTESIAN_POINT('Ctrl Pts',(-1.5081735481019,49.2667404117652,12.1636308994432));
#57687=CARTESIAN_POINT('Ctrl Pts',(-1.46413914973447,49.2756912416321,12.1070997655727));
#57688=CARTESIAN_POINT('Ctrl Pts',(-1.41702412181492,49.2846391126802,12.053302361519));
#57689=CARTESIAN_POINT('Ctrl Pts',(-1.4125881924468,49.2854815641382,12.0482372794187));
#57690=CARTESIAN_POINT('Ctrl Pts',(-1.40812459934876,49.2863240574281,12.0431960154616));
#57691=CARTESIAN_POINT('Ctrl Pts',(-1.40363352034152,49.2871665912809,12.0381789214648));
#57692=CARTESIAN_POINT('Ctrl Pts',(-1.3159668703761,49.3036129998704,11.9402443666394));
#57693=CARTESIAN_POINT('Ctrl Pts',(-1.21782338407748,49.3200747933399,11.8515220987113));
#57694=CARTESIAN_POINT('Ctrl Pts',(-1.11158589337901,49.3365428984598,11.7736691031812));
#57695=CARTESIAN_POINT('Ctrl Pts',(-1.00365240246168,49.3532739042723,11.6945732441704));
#57696=CARTESIAN_POINT('Ctrl Pts',(-0.887366003576533,49.3700114222832,
11.6266974114595));
#57697=CARTESIAN_POINT('Ctrl Pts',(-0.765256969791259,49.3867468451802,
11.5717380804842));
#57698=CARTESIAN_POINT('Ctrl Pts',(-0.718831634849412,49.3931095817388,
11.5508427767576));
#57699=CARTESIAN_POINT('Ctrl Pts',(-0.671564840019194,49.399472024888,11.5318140446093));
#57700=CARTESIAN_POINT('Ctrl Pts',(-0.623596072871047,49.405833736296,11.5147431601453));
#57701=CARTESIAN_POINT('Ctrl Pts',(-0.532872850951344,49.4178656268398,
11.4824570345751));
#57702=CARTESIAN_POINT('Ctrl Pts',(-0.439638967352969,49.4298948854296,
11.4571749515759));
#57703=CARTESIAN_POINT('Ctrl Pts',(-0.345025518837569,49.4419189000586,
11.4390557052432));
#57704=CARTESIAN_POINT('Ctrl Pts',(-0.284024353342111,49.4496712747771,
11.4273734849929));
#57705=CARTESIAN_POINT('Ctrl Pts',(-0.222389419767029,49.4574286193781,
11.4186556387847));
#57706=CARTESIAN_POINT('Ctrl Pts',(-0.160426678944839,49.4651909312848,
11.4129638843323));
#57707=CARTESIAN_POINT('Ctrl Pts',(-0.0509246993106248,49.4789086672828,
11.4029052850537));
#57708=CARTESIAN_POINT('Ctrl Pts',(0.0596021490212685,49.4926420138928,
11.4023002259455));
#57709=CARTESIAN_POINT('Ctrl Pts',(0.169418358914458,49.506389161536,11.4112375241642));
#57710=CARTESIAN_POINT('Ctrl Pts',(0.217924371137122,49.5124613007243,11.4151851444386));
#57711=CARTESIAN_POINT('Ctrl Pts',(0.266291423310214,49.5185361101893,11.4209938662932));
#57712=CARTESIAN_POINT('Ctrl Pts',(0.314368958306638,49.5246133272254,11.4286682717846));
#57713=CARTESIAN_POINT('Ctrl Pts',(0.422761076254026,49.538314579293,11.4459704289203));
#57714=CARTESIAN_POINT('Ctrl Pts',(0.529681050610087,49.5520281843259,11.4727590782111));
#57715=CARTESIAN_POINT('Ctrl Pts',(0.633557827194764,49.5657502923738,11.5084987179536));
#57716=CARTESIAN_POINT('Ctrl Pts',(0.680110637362215,49.5718999122605,11.5245155863922));
#57717=CARTESIAN_POINT('Ctrl Pts',(0.726052331747924,49.5780512168516,11.5423295073784));
#57718=CARTESIAN_POINT('Ctrl Pts',(0.771242460898877,49.5842037467633,11.5618889939815));
#57719=CARTESIAN_POINT('Ctrl Pts',(0.809264810044399,49.5893804002676,11.5783460752667));
#57720=CARTESIAN_POINT('Ctrl Pts',(0.846755103796012,49.5945579200084,11.5960388568935));
#57721=CARTESIAN_POINT('Ctrl Pts',(0.883622318728723,49.5997359852152,11.6149284240134));
#57722=CARTESIAN_POINT('Ctrl Pts',(0.974386618590373,49.6124839908345,11.6614331121886));
#57723=CARTESIAN_POINT('Ctrl Pts',(1.06166785697727,49.6252207027794,11.715139708312));
#57724=CARTESIAN_POINT('Ctrl Pts',(1.14410657474425,49.6379612282381,11.775622065151));
#57725=CARTESIAN_POINT('Ctrl Pts',(1.15692341031759,49.6399420113501,11.7850253218208));
#57726=CARTESIAN_POINT('Ctrl Pts',(1.16962312605051,49.6419228773749,11.7945922827835));
#57727=CARTESIAN_POINT('Ctrl Pts',(1.18220054132778,49.6439038728195,11.8043212610649));
#57728=CARTESIAN_POINT('Ctrl Pts',(1.26367653017654,49.6567366814052,11.8673451899483));
#57729=CARTESIAN_POINT('Ctrl Pts',(1.34002165985689,49.6695753222382,11.9371720643496));
#57730=CARTESIAN_POINT('Ctrl Pts',(1.41040025016923,49.6824295639781,12.0127526220316));
#57731=CARTESIAN_POINT('Ctrl Pts',(1.48079841329015,49.695287380578,12.0883541992281));
#57732=CARTESIAN_POINT('Ctrl Pts',(1.54522548452235,49.7081608107212,12.1697127558005));
#57733=CARTESIAN_POINT('Ctrl Pts',(1.60283895157809,49.7210546571543,12.2557268981212));
#57734=CARTESIAN_POINT('Ctrl Pts',(1.65818525223575,49.7334411136165,12.3383562697764));
#57735=CARTESIAN_POINT('Ctrl Pts',(1.70724251943844,49.7458463830365,12.4252815367258));
#57736=CARTESIAN_POINT('Ctrl Pts',(1.74927539554209,49.7582703635106,12.515482559182));
#57737=CARTESIAN_POINT('Ctrl Pts',(1.78916920388077,49.7700620832733,12.6010932200595));
#57738=CARTESIAN_POINT('Ctrl Pts',(1.82277928288667,49.7818855126595,12.6897593564606));
#57739=CARTESIAN_POINT('Ctrl Pts',(1.84959117159127,49.7937196540585,12.78057038105));
#57740=CARTESIAN_POINT('Ctrl Pts',(1.87549737767598,49.8051540483041,12.8683138870632));
#57741=CARTESIAN_POINT('Ctrl Pts',(1.89505805837168,49.8165984759503,12.9580592310516));
#57742=CARTESIAN_POINT('Ctrl Pts',(1.90825323336579,49.8280400743436,13.0488085486734));
#57743=CARTESIAN_POINT('Ctrl Pts',(1.91216170154511,49.8314291255128,13.0756888909483));
#57744=CARTESIAN_POINT('Ctrl Pts',(1.91551184574708,49.8348179682363,13.1026576218624));
#57745=CARTESIAN_POINT('Ctrl Pts',(1.91830350256686,49.8382063687107,13.1296896098372));
#57746=CARTESIAN_POINT('Ctrl Pts',(1.92953580783151,49.8518396878985,13.2384535304924));
#57747=CARTESIAN_POINT('Ctrl Pts',(1.93169044802515,49.8654785041309,13.348306963276));
#57748=CARTESIAN_POINT('Ctrl Pts',(1.9245084160203,49.8791350497271,13.4576550741967));
#57749=CARTESIAN_POINT('Ctrl Pts',(1.92360157678391,49.8808593933908,13.4714619128938));
#57750=CARTESIAN_POINT('Ctrl Pts',(1.92254587695862,49.8825840113469,13.4852606279965));
#57751=CARTESIAN_POINT('Ctrl Pts',(1.92134079226722,49.8843089209617,13.4990479505969));
#57752=CARTESIAN_POINT('Ctrl Pts',(1.91342147776945,49.8956443082728,13.5896524902889));
#57753=CARTESIAN_POINT('Ctrl Pts',(1.89905036197541,49.9069925388944,13.6797669564011));
#57754=CARTESIAN_POINT('Ctrl Pts',(1.87844238405721,49.9183567502638,13.768533416587));
#57755=CARTESIAN_POINT('Ctrl Pts',(1.85806813861979,49.9295920705153,13.8562931013857));
#57756=CARTESIAN_POINT('Ctrl Pts',(1.83147583519971,49.9408551558828,13.9427357798033));
#57757=CARTESIAN_POINT('Ctrl Pts',(1.79901109730714,49.9521347064582,14.0270300623742));
#57758=CARTESIAN_POINT('Ctrl Pts',(1.76649233280349,49.9634330280427,14.1114646243596));
#57759=CARTESIAN_POINT('Ctrl Pts',(1.72808276981835,49.9747478657175,14.1937439181842));
#57760=CARTESIAN_POINT('Ctrl Pts',(1.68411841978781,49.9860745920622,14.2730826788711));
#57761=CARTESIAN_POINT('Ctrl Pts',(1.66732052166656,49.9904023074738,14.3033964312218));
#57762=CARTESIAN_POINT('Ctrl Pts',(1.64971149644335,49.9947318285754,14.3332814061617));
#57763=CARTESIAN_POINT('Ctrl Pts',(1.63130911220971,49.9990631575573,14.3626955469288));
#57764=CARTESIAN_POINT('Ctrl Pts',(1.62163280526315,50.0013406487879,14.378162034913));
#57765=CARTESIAN_POINT('Ctrl Pts',(1.61174083809686,50.0036182017112,14.3934972853071));
#57766=CARTESIAN_POINT('Ctrl Pts',(1.60163402672504,50.0058959343056,14.4086945746061));
#57767=CARTESIAN_POINT('Ctrl Pts',(1.55666321793511,50.016030829794,14.4763157427519));
#57768=CARTESIAN_POINT('Ctrl Pts',(1.50743724227319,50.0261698123625,14.541209282367));
#57769=CARTESIAN_POINT('Ctrl Pts',(1.45431001726312,50.0363191647339,14.6028716824512));
#57770=CARTESIAN_POINT('Ctrl Pts',(1.40127456235842,50.0464509854698,14.664427569068));
#57771=CARTESIAN_POINT('Ctrl Pts',(1.34435038650263,50.0565931378105,14.7227628433547));
#57772=CARTESIAN_POINT('Ctrl Pts',(1.28391790547149,50.0667452221655,14.7773339478466));
#57773=CARTESIAN_POINT('Ctrl Pts',(1.25729144758455,50.0712182148663,14.8013778922752));
#57774=CARTESIAN_POINT('Ctrl Pts',(1.22998438643742,50.0756930490622,14.824690609789));
#57775=CARTESIAN_POINT('Ctrl Pts',(1.20203166275937,50.0801692812514,14.8472235002155));
#57776=CARTESIAN_POINT('Ctrl Pts',(1.12804255291437,50.0920175876617,14.9068666507039));
#57777=CARTESIAN_POINT('Ctrl Pts',(1.04977223436755,50.1038849490447,14.9614104879932));
#57778=CARTESIAN_POINT('Ctrl Pts',(0.96783739781816,50.1157763050814,15.0100683364991));
#57779=CARTESIAN_POINT('Ctrl Pts',(0.938590872010946,50.1200209080593,15.0274366877644));
#57780=CARTESIAN_POINT('Ctrl Pts',(0.908877794999064,50.1242685118152,15.0440547594811));
#57781=CARTESIAN_POINT('Ctrl Pts',(0.878727474825673,50.1285191529968,15.0598858023556));
#57782=CARTESIAN_POINT('Ctrl Pts',(0.793422786706762,50.1405455466871,15.1046767752954));
#57783=CARTESIAN_POINT('Ctrl Pts',(0.704614297266369,50.1525967170587,15.1431686163929));
#57784=CARTESIAN_POINT('Ctrl Pts',(0.613299149750707,50.1646691980739,15.1750659712351));
#57785=CARTESIAN_POINT('Ctrl Pts',(0.522111477449071,50.1767248260025,15.2069187976257));
#57786=CARTESIAN_POINT('Ctrl Pts',(0.428424044611456,50.1888017024246,15.2321943006212));
#57787=CARTESIAN_POINT('Ctrl Pts',(0.333281062570076,50.2008900790611,15.2505937858019));
#57788=CARTESIAN_POINT('Ctrl Pts',(0.238669253175742,50.2129109676404,15.2688905487109));
#57789=CARTESIAN_POINT('Ctrl Pts',(0.142618408570352,50.2249432204352,15.2803866693137));
#57790=CARTESIAN_POINT('Ctrl Pts',(0.046204394392973,50.2369711067171,15.2848019797074));
#57791=CARTESIAN_POINT('Ctrl Pts',(0.0273405857746152,50.2393244134105,
15.2856658538129));
#57792=CARTESIAN_POINT('Ctrl Pts',(0.00846301594625596,50.2416775342161,
15.2862587437213));
#57793=CARTESIAN_POINT('Ctrl Pts',(-0.0104200573975599,50.2440303240055,
15.2865786720814));
#57794=CARTESIAN_POINT('Ctrl Pts',(-0.106807620890628,50.2560400043727,
15.2882117280234));
#57795=CARTESIAN_POINT('Ctrl Pts',(-0.203498122787935,50.2680945843605,
15.2830885050845));
#57796=CARTESIAN_POINT('Ctrl Pts',(-0.299485996380947,50.2801882117298,
15.2708992987964));
#57797=CARTESIAN_POINT('Ctrl Pts',(-0.336200589439534,50.2848139273629,
15.2662370249922));
#57798=CARTESIAN_POINT('Ctrl Pts',(-0.37281186034304,50.2894453019465,15.2605411428792));
#57799=CARTESIAN_POINT('Ctrl Pts',(-0.40926168203733,50.2940818082829,15.2537950599671));
#57800=CARTESIAN_POINT('Ctrl Pts',(-0.505010731284271,50.3062613211832,
15.236073957505));
#57801=CARTESIAN_POINT('Ctrl Pts',(-0.599648307088963,50.3184766205361,
15.2111032485417));
#57802=CARTESIAN_POINT('Ctrl Pts',(-0.692179824458452,50.3307144389555,
15.1792970548347));
#57803=CARTESIAN_POINT('Ctrl Pts',(-0.78483404415089,50.3429684854536,15.1474486842137));
#57804=CARTESIAN_POINT('Ctrl Pts',(-0.87537560604112,50.3552451097819,15.1087460560846));
#57805=CARTESIAN_POINT('Ctrl Pts',(-0.962776741130743,50.3675257196077,
15.0636478012151));
#57806=CARTESIAN_POINT('Ctrl Pts',(-1.0494068711561,50.3796979966028,15.0189473785117));
#57807=CARTESIAN_POINT('Ctrl Pts',(-1.13295050533364,50.3918741775708,14.9679633451565));
#57808=CARTESIAN_POINT('Ctrl Pts',(-1.21239495140534,50.4040310889802,14.9111913742513));
#57809=CARTESIAN_POINT('Ctrl Pts',(-1.2264718097698,50.4061851869508,14.9011318794343));
#57810=CARTESIAN_POINT('Ctrl Pts',(-1.24041996478418,50.408338667228,14.890890793895));
#57811=CARTESIAN_POINT('Ctrl Pts',(-1.25423379087638,50.4104913845365,14.8804710471741));
#57812=CARTESIAN_POINT('Ctrl Pts',(-1.34117925715569,50.4240407812718,14.8148882223206));
#57813=CARTESIAN_POINT('Ctrl Pts',(-1.42318024899639,50.437645038114,14.7423348026361));
#57814=CARTESIAN_POINT('Ctrl Pts',(-1.49891581544433,50.4512937034892,14.6633880757765));
#57815=CARTESIAN_POINT('Ctrl Pts',(-1.51914701857044,50.4549396644895,14.6422990770121));
#57816=CARTESIAN_POINT('Ctrl Pts',(-1.53893094679464,50.4585887653775,14.620754084337));
#57817=CARTESIAN_POINT('Ctrl Pts',(-1.558242059404,50.4622407435146,14.5987646089574));
#57818=CARTESIAN_POINT('Ctrl Pts',(-1.63288880051887,50.4763573960387,14.513764707133));
#57819=CARTESIAN_POINT('Ctrl Pts',(-1.70047167800137,50.4905175015514,14.4221188719292));
#57820=CARTESIAN_POINT('Ctrl Pts',(-1.76009939321026,50.5047025029048,14.3253128965409));
#57821=CARTESIAN_POINT('Ctrl Pts',(-1.8182349901732,50.5185325401403,14.2309293846276));
#57822=CARTESIAN_POINT('Ctrl Pts',(-1.86880721828935,50.5323862156151,14.1316410694346));
#57823=CARTESIAN_POINT('Ctrl Pts',(-1.91113795400556,50.5462404940161,14.0287752659255));
#57824=CARTESIAN_POINT('Ctrl Pts',(-1.94478507797625,50.5572527435081,13.9470110729708));
#57825=CARTESIAN_POINT('Ctrl Pts',(-1.97322493243461,50.5682652694524,13.8629877245061));
#57826=CARTESIAN_POINT('Ctrl Pts',(-1.99612549706287,50.5792641314507,13.7773936504254));
#57827=CARTESIAN_POINT('Ctrl Pts',(-2.02626276085829,50.5937386918325,13.6647513976352));
#57828=CARTESIAN_POINT('Ctrl Pts',(-2.04712883468148,50.6082867669309,13.5493023740913));
#57829=CARTESIAN_POINT('Ctrl Pts',(-2.05795982560911,50.6228939413266,13.432532945082));
#57830=CARTESIAN_POINT('Ctrl Pts',(-2.06039053292552,50.6261721054311,13.406327373743));
#57831=CARTESIAN_POINT('Ctrl Pts',(-2.0623159026598,50.6294532294161,13.3800554921823));
#57832=CARTESIAN_POINT('Ctrl Pts',(-2.06372746576267,50.6327371214468,13.3537344183884));
#57833=CARTESIAN_POINT('Ctrl Pts',(-2.07004524593896,50.6474349468084,13.2359283083419));
#57834=CARTESIAN_POINT('Ctrl Pts',(-2.06606711496515,50.6621885566942,13.1171341445939));
#57835=CARTESIAN_POINT('Ctrl Pts',(-2.05205326534908,50.6769783447938,12.9993851820754));
#57836=CARTESIAN_POINT('Ctrl Pts',(-2.05069601058759,50.6784107499408,12.9879810822444));
#57837=CARTESIAN_POINT('Ctrl Pts',(-2.0492446528101,50.6798434911776,12.9765868092299));
#57838=CARTESIAN_POINT('Ctrl Pts',(-2.04769945043919,50.6812765485945,12.9652042232842));
#57839=CARTESIAN_POINT('Ctrl Pts',(-2.03194857141904,50.6958842882845,12.8491768746707));
#57840=CARTESIAN_POINT('Ctrl Pts',(-2.00644258990089,50.7105252071379,12.7343629603841));
#57841=CARTESIAN_POINT('Ctrl Pts',(-1.971414945706,50.725175952002,12.6222505812766));
#57842=CARTESIAN_POINT('Ctrl Pts',(-1.96749237097443,50.7268166173372,12.609695663711));
#57843=CARTESIAN_POINT('Ctrl Pts',(-1.96345044163711,50.7284574018316,12.5971746326607));
#57844=CARTESIAN_POINT('Ctrl Pts',(-1.95928952687661,50.7300982696216,12.5846895813309));
#57845=CARTESIAN_POINT('Ctrl Pts',(-1.94164973720009,50.7370545675437,12.5317604317967));
#57846=CARTESIAN_POINT('Ctrl Pts',(-1.92187127034554,50.744012377997,12.4794779791356));
#57847=CARTESIAN_POINT('Ctrl Pts',(-1.90002458491759,50.7509688439665,12.4280317948976));
#57848=CARTESIAN_POINT('Ctrl Pts',(-1.85785924507542,50.764395217165,12.328737746419));
#57849=CARTESIAN_POINT('Ctrl Pts',(-1.80806813568785,50.7779138527103,12.2322626922288));
#57850=CARTESIAN_POINT('Ctrl Pts',(-1.75102971121399,50.7915034847982,12.1399629132644));
#57851=CARTESIAN_POINT('Ctrl Pts',(-1.69905782948915,50.8038859928718,12.0558618315844));
#57852=CARTESIAN_POINT('Ctrl Pts',(-1.64106911183378,50.8163273896247,11.9752284416276));
#57853=CARTESIAN_POINT('Ctrl Pts',(-1.5773822155289,50.8288083149998,11.8991079060624));
#57854=CARTESIAN_POINT('Ctrl Pts',(-1.50691721254408,50.842617567685,11.8148859691019));
#57855=CARTESIAN_POINT('Ctrl Pts',(-1.42947566304557,50.8564752768747,11.7361897647438));
#57856=CARTESIAN_POINT('Ctrl Pts',(-1.34620116056982,50.8703507651883,11.6638070823509));
#57857=CARTESIAN_POINT('Ctrl Pts',(-1.2629885637345,50.8842159385678,11.591478208701));
#57858=CARTESIAN_POINT('Ctrl Pts',(-1.17395204342079,50.898098857206,11.5254547521015));
#57859=CARTESIAN_POINT('Ctrl Pts',(-1.08028227234088,50.9119643914035,11.4665101279605));
#57860=CARTESIAN_POINT('Ctrl Pts',(-1.04634056534299,50.9169886366181,11.445151250506));
#57861=CARTESIAN_POINT('Ctrl Pts',(-1.01179094998515,50.9220105568077,11.4247216168608));
#57862=CARTESIAN_POINT('Ctrl Pts',(-0.976691501791933,50.9270283371022,
11.4052571049783));
#57863=CARTESIAN_POINT('Ctrl Pts',(-0.884937477897842,50.9401453961086,
11.3543746159281));
#57864=CARTESIAN_POINT('Ctrl Pts',(-0.789167206110581,50.9532737375235,
11.3099416664974));
#57865=CARTESIAN_POINT('Ctrl Pts',(-0.690438375184751,50.9664180064903,
11.2726169599394));
#57866=CARTESIAN_POINT('Ctrl Pts',(-0.592043153771279,50.9795178603341,
11.2354183753768));
#57867=CARTESIAN_POINT('Ctrl Pts',(-0.490710572213136,50.992633538247,11.2052802004869));
#57868=CARTESIAN_POINT('Ctrl Pts',(-0.387495446867673,51.005772276969,11.1828042558989));
#57869=CARTESIAN_POINT('Ctrl Pts',(-0.325448366228293,51.0136705416686,
11.1692929924902));
#57870=CARTESIAN_POINT('Ctrl Pts',(-0.262721040796763,51.0215771905168,
11.1585496764105));
#57871=CARTESIAN_POINT('Ctrl Pts',(-0.19954130283245,51.0294942462609,11.1506960304855));
#57872=CARTESIAN_POINT('Ctrl Pts',(-0.0949346514238878,51.0426025103515,
11.1376927539915));
#57873=CARTESIAN_POINT('Ctrl Pts',(0.0109104768394059,51.0557391746088,
11.1326131283539));
#57874=CARTESIAN_POINT('Ctrl Pts',(0.116743595274185,51.0689153793944,11.1352504856376));
#57875=CARTESIAN_POINT('Ctrl Pts',(0.213817704011632,51.0810010890005,11.1376695687329));
#57876=CARTESIAN_POINT('Ctrl Pts',(0.310881342433441,51.0931200967982,11.1465802513686));
#57877=CARTESIAN_POINT('Ctrl Pts',(0.406995758654726,51.1052827788823,11.1617947627978));
#57878=CARTESIAN_POINT('Ctrl Pts',(0.475225197012527,51.1139167903049,11.1725951984714));
#57879=CARTESIAN_POINT('Ctrl Pts',(0.543114902989226,51.122550766893,11.1866681096965));
#57880=CARTESIAN_POINT('Ctrl Pts',(0.610317925577959,51.1311896951867,11.2039733231974));
#57881=CARTESIAN_POINT('Ctrl Pts',(0.720705572369544,51.1453799939026,11.2323988570796));
#57882=CARTESIAN_POINT('Ctrl Pts',(0.829238241388482,51.1595834110016,11.2695473147213));
#57883=CARTESIAN_POINT('Ctrl Pts',(0.934470959369924,51.1738257667431,11.3150044503832));
#57884=CARTESIAN_POINT('Ctrl Pts',(1.03984233068126,51.1880868880367,11.3605214798057));
#57885=CARTESIAN_POINT('Ctrl Pts',(1.14190435883492,51.2023870583837,11.4143679537695));
#57886=CARTESIAN_POINT('Ctrl Pts',(1.23924938699954,51.2167567973926,11.4761000902931));
#57887=CARTESIAN_POINT('Ctrl Pts',(1.27788759182712,51.2224604365985,11.5006028202262));
#57888=CARTESIAN_POINT('Ctrl Pts',(1.31578318420242,51.2281750861814,11.5263476861861));
#57889=CARTESIAN_POINT('Ctrl Pts',(1.35285032883315,51.2339028502947,11.5533062962545));
#57890=CARTESIAN_POINT('Ctrl Pts',(1.44658576544506,51.2483872265617,11.6214792594105));
#57891=CARTESIAN_POINT('Ctrl Pts',(1.53501985110568,51.2629551626989,11.6974132567916));
#57892=CARTESIAN_POINT('Ctrl Pts',(1.61730548063149,51.2776437369066,11.7798474230589));
#57893=CARTESIAN_POINT('Ctrl Pts',(1.63586064267326,51.2809559662249,11.7984360796893));
#57894=CARTESIAN_POINT('Ctrl Pts',(1.65410336719204,51.2842743472626,11.8173553037568));
#57895=CARTESIAN_POINT('Ctrl Pts',(1.67202429616646,51.287599335277,11.8365907362258));
#57896=CARTESIAN_POINT('Ctrl Pts',(1.74730869978597,51.3015673466487,11.9173972649422));
#57897=CARTESIAN_POINT('Ctrl Pts',(1.81684091453586,51.3154633698883,12.0041923127625));
#57898=CARTESIAN_POINT('Ctrl Pts',(1.87981515976553,51.3293199286473,12.0958702323521));
#57899=CARTESIAN_POINT('Ctrl Pts',(1.94326560255564,51.3432812676931,12.1882414004514));
#57900=CARTESIAN_POINT('Ctrl Pts',(2.00005877031958,51.357202544524,12.285568209684));
#57901=CARTESIAN_POINT('Ctrl Pts',(2.0494234544693,51.3711221643026,12.3867219798677));
#57902=CARTESIAN_POINT('Ctrl Pts',(2.09864971396905,51.3850027517541,12.4875921024302));
#57903=CARTESIAN_POINT('Ctrl Pts',(2.14048952988282,51.3988817041221,12.592266729379));
#57904=CARTESIAN_POINT('Ctrl Pts',(2.17422535347785,51.4128020754618,12.6996467516589));
#57905=CARTESIAN_POINT('Ctrl Pts',(2.19881412754627,51.4229481110212,12.777912014692));
#57906=CARTESIAN_POINT('Ctrl Pts',(2.2190987512973,51.4331162540573,12.8576149130984));
#57907=CARTESIAN_POINT('Ctrl Pts',(2.23481506548427,51.4433247841335,12.9383406646595));
#57908=CARTESIAN_POINT('Ctrl Pts',(2.25000922374029,51.4531941478846,13.0163843987032));
#57909=CARTESIAN_POINT('Ctrl Pts',(2.26093395368737,51.4631012689016,13.0953840515804));
#57910=CARTESIAN_POINT('Ctrl Pts',(2.26767989392229,51.4730637999864,13.1748713078923));
#57911=CARTESIAN_POINT('Ctrl Pts',(2.27801605302903,51.4883284336492,13.2966620293613));
#57912=CARTESIAN_POINT('Ctrl Pts',(2.27839959800904,51.5036301509547,13.4199225311563));
#57913=CARTESIAN_POINT('Ctrl Pts',(2.26898183281624,51.5189755570549,13.5429175800468));
#57914=CARTESIAN_POINT('Ctrl Pts',(2.25941221926975,51.534568386467,13.6678957528848));
#57915=CARTESIAN_POINT('Ctrl Pts',(2.23972308856393,51.5502063253031,13.7925983831649));
#57916=CARTESIAN_POINT('Ctrl Pts',(2.21012819997815,51.5658978695212,13.915205273457));
#57917=CARTESIAN_POINT('Ctrl Pts',(2.18127044876477,51.5811985751781,14.0347583215058));
#57918=CARTESIAN_POINT('Ctrl Pts',(2.14299489697288,51.5965502601759,14.1523175527705));
#57919=CARTESIAN_POINT('Ctrl Pts',(2.09554325266421,51.6119621762579,14.2662152151626));
#57920=CARTESIAN_POINT('Ctrl Pts',(2.0485582186183,51.6272225410435,14.3789928780488));
#57921=CARTESIAN_POINT('Ctrl Pts',(1.99257709650871,51.6425419658411,14.4881796253961));
#57922=CARTESIAN_POINT('Ctrl Pts',(1.92787003969126,51.6579306647238,14.5921921555573));
#57923=CARTESIAN_POINT('Ctrl Pts',(1.86255948817896,51.6734628873363,14.6971747655405));
#57924=CARTESIAN_POINT('Ctrl Pts',(1.7883614277045,51.6890656867666,14.7968859216486));
#57925=CARTESIAN_POINT('Ctrl Pts',(1.7066345985162,51.7047506996867,14.8902798816078));
#57926=CARTESIAN_POINT('Ctrl Pts',(1.66581357159012,51.7125850711055,14.936928422755));
#57927=CARTESIAN_POINT('Ctrl Pts',(1.62311439888885,51.7204399711188,14.9820017033674));
#57928=CARTESIAN_POINT('Ctrl Pts',(1.57870657579314,51.7283169522183,15.0253743524037));
#57929=CARTESIAN_POINT('Ctrl Pts',(1.50047847559116,51.7421929142401,15.1017789067888));
#57930=CARTESIAN_POINT('Ctrl Pts',(1.41654901118027,51.756100645792,15.1731573813177));
#57931=CARTESIAN_POINT('Ctrl Pts',(1.32777894335815,51.7700336438041,15.2386647004963));
#57932=CARTESIAN_POINT('Ctrl Pts',(1.23747687650584,51.784207098312,15.3053025488264));
#57933=CARTESIAN_POINT('Ctrl Pts',(1.14216653685236,51.7984066987655,15.3658640092509));
#57934=CARTESIAN_POINT('Ctrl Pts',(1.04280039150845,51.8126258034887,15.4194885002371));
#57935=CARTESIAN_POINT('Ctrl Pts',(0.944082085006813,51.8267522037168,15.4727633748821));
#57936=CARTESIAN_POINT('Ctrl Pts',(0.841361704843203,51.8408978556128,15.5191907371094));
#57937=CARTESIAN_POINT('Ctrl Pts',(0.735604232794058,51.8550564392127,15.5579664995614));
#57938=CARTESIAN_POINT('Ctrl Pts',(0.672327759979994,51.8635277577199,15.5811666898752));
#57939=CARTESIAN_POINT('Ctrl Pts',(0.607964582592411,51.8720037091988,15.6016285497847));
#57940=CARTESIAN_POINT('Ctrl Pts',(0.542724481630528,51.8804829711198,15.6191882969655));
#57941=CARTESIAN_POINT('Ctrl Pts',(0.433306805066517,51.8947039966041,15.6486386918797));
#57942=CARTESIAN_POINT('Ctrl Pts',(0.321422964300072,51.9089343250588,15.6699231722959));
#57943=CARTESIAN_POINT('Ctrl Pts',(0.208379630461429,51.9231677789593,15.6831294558649));
#57944=CARTESIAN_POINT('Ctrl Pts',(0.0975655914236256,51.9371205390436,
15.696075302146));
#57945=CARTESIAN_POINT('Ctrl Pts',(-0.0143615258194681,51.9510763040823,
15.7012587366926));
#57946=CARTESIAN_POINT('Ctrl Pts',(-0.126183054695298,51.965029402954,15.6988098364548));
#57947=CARTESIAN_POINT('Ctrl Pts',(-0.198236902745661,51.97402028759,15.6972318515409));
#57948=CARTESIAN_POINT('Ctrl Pts',(-0.270247206108331,51.9830100681522,
15.6924858204689));
#57949=CARTESIAN_POINT('Ctrl Pts',(-0.341893915334161,51.9919972563659,
15.6846164396408));
#57950=CARTESIAN_POINT('Ctrl Pts',(-0.452329377343791,52.0058500109903,
15.67248666122));
#57951=CARTESIAN_POINT('Ctrl Pts',(-0.562480536841933,52.0197557230553,
15.6528594899942));
#57952=CARTESIAN_POINT('Ctrl Pts',(-0.671147032885876,52.0337055294602,
15.6257021304772));
#57953=CARTESIAN_POINT('Ctrl Pts',(-0.782314303434172,52.0479763669231,
15.5979197905406));
#57954=CARTESIAN_POINT('Ctrl Pts',(-0.891926596930965,52.0622933521822,
15.5622565487633));
#57955=CARTESIAN_POINT('Ctrl Pts',(-0.99868441702179,52.076646931506,15.5187296367709));
#57956=CARTESIAN_POINT('Ctrl Pts',(-1.07193701850435,52.0864957371969,15.4888633512357));
#57957=CARTESIAN_POINT('Ctrl Pts',(-1.14384539681097,52.0963617704336,15.4552958631548));
#57958=CARTESIAN_POINT('Ctrl Pts',(-1.21399056123118,52.1062419256841,15.4180469111777));
#57959=CARTESIAN_POINT('Ctrl Pts',(-1.31504572326384,52.120475846126,15.3643839265842));
#57960=CARTESIAN_POINT('Ctrl Pts',(-1.41243978109377,52.1347390801274,15.3030779985422));
#57961=CARTESIAN_POINT('Ctrl Pts',(-1.50527291662462,52.1490222468805,15.235008197586));
#57962=CARTESIAN_POINT('Ctrl Pts',(-1.5984260151893,52.1633546426652,15.166703784065));
#57963=CARTESIAN_POINT('Ctrl Pts',(-1.68698581781993,52.1777071093187,15.0915896966614));
#57964=CARTESIAN_POINT('Ctrl Pts',(-1.77007593847986,52.1920700892426,15.0105950709922));
#57965=CARTESIAN_POINT('Ctrl Pts',(-1.85100589705314,52.2060596629849,14.9317061291059));
#57966=CARTESIAN_POINT('Ctrl Pts',(-1.92674628733797,52.2200592105307,14.8472393949193));
#57967=CARTESIAN_POINT('Ctrl Pts',(-1.99652887804495,52.2340598218168,14.7580781735643));
#57968=CARTESIAN_POINT('Ctrl Pts',(-2.04046443220278,52.2428746939672,14.7019417127374));
#57969=CARTESIAN_POINT('Ctrl Pts',(-2.08203915034671,52.2516899862194,14.6439447809136));
#57970=CARTESIAN_POINT('Ctrl Pts',(-2.12107165008936,52.2605034578968,14.58431058459));
#57971=CARTESIAN_POINT('Ctrl Pts',(-2.17629436357354,52.272972652144,14.49994083735));
#57972=CARTESIAN_POINT('Ctrl Pts',(-2.22650631414255,52.2852457466958,14.4118971504242));
#57973=CARTESIAN_POINT('Ctrl Pts',(-2.2712142963379,52.2975259079814,14.3208300079618));
#57974=CARTESIAN_POINT('Ctrl Pts',(-2.31592227853324,52.309806069267,14.2297628654994));
#57975=CARTESIAN_POINT('Ctrl Pts',(-2.35512731139636,52.3220933259785,14.1356727343629));
#57976=CARTESIAN_POINT('Ctrl Pts',(-2.38836719431143,52.3345987243418,14.039166525391));
#57977=CARTESIAN_POINT('Ctrl Pts',(-1.22475759790445,61.5085174595755,10.2717937103395));
#57978=CARTESIAN_POINT('Ctrl Pts',(-0.558011100714539,61.5982486649959,
10.0030310024535));
#57979=CARTESIAN_POINT('Ctrl Pts',(0.957582776261939,61.7776481271537,9.92475194519782));
#57980=CARTESIAN_POINT('Ctrl Pts',(2.81969758661395,62.0461398867496,11.2283079993549));
#57981=CARTESIAN_POINT('Ctrl Pts',(3.48222140378021,62.3136428581871,13.3935715300134));
#57982=CARTESIAN_POINT('Ctrl Pts',(2.67681707758244,62.579773345974,15.497292108503));
#57983=CARTESIAN_POINT('Ctrl Pts',(0.759902248054433,62.8441604986882,16.6530507103859));
#57984=CARTESIAN_POINT('Ctrl Pts',(-1.44458547024767,63.1064443544619,16.3863495812049));
#57985=CARTESIAN_POINT('Ctrl Pts',(-3.00432898132876,63.3662787322575,14.8364237012945));
#57986=CARTESIAN_POINT('Ctrl Pts',(-3.26685589537852,63.6138139233043,12.7543667878087));
#57987=CARTESIAN_POINT('Ctrl Pts',(-2.47105982748424,63.811474368391,11.3089218924462));
#57988=CARTESIAN_POINT('Ctrl Pts',(-1.00806246152439,64.0353924428549,10.2305976232193));
#57989=CARTESIAN_POINT('Ctrl Pts',(1.2619356887499,64.293423364255,10.1359463299035));
#57990=CARTESIAN_POINT('Ctrl Pts',(3.17140149111836,64.6184082729688,12.2928073226734));
#57991=CARTESIAN_POINT('Ctrl Pts',(2.73437323989231,64.9360819775815,15.0617858882019));
#57992=CARTESIAN_POINT('Ctrl Pts',(0.366119910750528,65.2460149715181,16.4456710631955));
#57993=CARTESIAN_POINT('Ctrl Pts',(-2.13523691433573,65.5478718326797,15.5180124762315));
#57994=CARTESIAN_POINT('Ctrl Pts',(-2.98478079778392,65.841387878141,13.0674399329054));
#57995=CARTESIAN_POINT('Ctrl Pts',(-1.66701189783808,66.1264296862307,10.9156975846686));
#57996=CARTESIAN_POINT('Ctrl Pts',(0.751927388912868,66.4029443584298,10.5875584960911));
#57997=CARTESIAN_POINT('Ctrl Pts',(2.49274638058045,66.6709882204905,12.19252620218));
#57998=CARTESIAN_POINT('Ctrl Pts',(2.35910723949879,66.9307237214747,14.4856574268905));
#57999=CARTESIAN_POINT('Ctrl Pts',(0.71660521689825,67.1614233848501,15.6875003337387));
#58000=CARTESIAN_POINT('Ctrl Pts',(-0.996423457277477,67.3655344712751,
15.4400425861523));
#58001=CARTESIAN_POINT('Ctrl Pts',(-2.05297602182105,67.5450863880253,14.3512624693526));
#58002=CARTESIAN_POINT('Ctrl Pts',(-2.21336612279098,67.7206997564268,12.8715592664714));
#58003=CARTESIAN_POINT('Ctrl Pts',(-1.44710288542824,67.892614429265,11.6346115739884));
#58004=CARTESIAN_POINT('Ctrl Pts',(-0.109789305964637,68.0610877835164,
11.1391611146274));
#58005=CARTESIAN_POINT('Ctrl Pts',(1.22398483030438,68.2264079408537,11.5627232550221));
#58006=CARTESIAN_POINT('Ctrl Pts',(2.00193544971486,68.3888854005119,12.6965891887889));
#58007=CARTESIAN_POINT('Ctrl Pts',(1.91987771499495,68.5488359593493,14.0479937472136));
#58008=CARTESIAN_POINT('Ctrl Pts',(1.03645178894531,68.7066105132279,15.0496273315261));
#58009=CARTESIAN_POINT('Ctrl Pts',(-0.260707618104073,68.8625671064471,
15.2940633739598));
#58010=CARTESIAN_POINT('Ctrl Pts',(-1.4240215170718,69.0170673179846,14.6948442918268));
#58011=CARTESIAN_POINT('Ctrl Pts',(-1.90763689933083,69.1534481987426,13.6471050935586));
#58012=CARTESIAN_POINT('Ctrl Pts',(-1.81977406488792,69.2426201973106,12.9197483588915));
#58013=CARTESIAN_POINT('Ctrl Pts',(-1.69804219571952,69.2850346430207,12.6023842455621));
#58014=CARTESIAN_POINT('Ctrl Pts',(-1.64242831287433,69.3019970791238,12.4783116538297));
#58015=CARTESIAN_POINT('Ctrl Pts',(-1.52735037370308,69.3316743635896,12.2698368113331));
#58016=CARTESIAN_POINT('Ctrl Pts',(-1.23065205270035,69.3909991147362,11.8947040913177));
#58017=CARTESIAN_POINT('Ctrl Pts',(-0.645158799006976,69.4757025248837,
11.5193939124166));
#58018=CARTESIAN_POINT('Ctrl Pts',(0.044810345871984,69.5604396628484,11.4303795861512));
#58019=CARTESIAN_POINT('Ctrl Pts',(0.580700809085593,69.6283146835187,11.5411475348396));
#58020=CARTESIAN_POINT('Ctrl Pts',(0.861510638146726,69.666531265754,11.6677365653311));
#58021=CARTESIAN_POINT('Ctrl Pts',(1.03443845903176,69.69203334437,11.7767096136909));
#58022=CARTESIAN_POINT('Ctrl Pts',(1.14565717774328,69.709040761661,11.8555746554773));
#58023=CARTESIAN_POINT('Ctrl Pts',(1.32809052278142,69.7388195747815,12.0096995333949));
#58024=CARTESIAN_POINT('Ctrl Pts',(1.82067835896352,69.832521589919,12.5831930627474));
#58025=CARTESIAN_POINT('Ctrl Pts',(2.03046072987068,69.9865805680574,13.9254562576328));
#58026=CARTESIAN_POINT('Ctrl Pts',(0.810259096530256,70.1944780346027,15.2994738528175));
#58027=CARTESIAN_POINT('Ctrl Pts',(-1.05830745474474,70.4057338895888,15.2249363050774));
#58028=CARTESIAN_POINT('Ctrl Pts',(-2.07493719267882,70.5972153712582,13.8764528995484));
#58029=CARTESIAN_POINT('Ctrl Pts',(-1.94180353342299,70.7679921684942,12.450736958435));
#58030=CARTESIAN_POINT('Ctrl Pts',(-1.16039001901908,70.9167953919606,11.4835575608119));
#58031=CARTESIAN_POINT('Ctrl Pts',(0.100587899379937,71.0745421465401,11.0884895976554));
#58032=CARTESIAN_POINT('Ctrl Pts',(1.44344797546005,71.2418455914631,11.5364757461608));
#58033=CARTESIAN_POINT('Ctrl Pts',(2.27501583067712,71.4194119422884,12.7892555436196));
#58034=CARTESIAN_POINT('Ctrl Pts',(2.15695780511918,71.6010238110375,14.3220345011878));
#58035=CARTESIAN_POINT('Ctrl Pts',(1.09667342325315,71.7868784116616,15.4844988867453));
#58036=CARTESIAN_POINT('Ctrl Pts',(-0.49121362380328,71.9771479946895,15.7544990355271));
#58037=CARTESIAN_POINT('Ctrl Pts',(-1.94315347613286,72.1719682245206,14.9722576142499));
#58038=CARTESIAN_POINT('Ctrl Pts',(-2.62186916830043,72.3714469815617,13.4254905457947));
#58039=CARTESIAN_POINT('Ctrl Pts',(-2.33801236899026,72.5075907029867,12.3091065046127));
#58040=CARTESIAN_POINT('Ctrl Pts',(-2.03365423424493,72.5764593847717,11.8488939074775));
#58041=CARTESIAN_POINT('Ctrl Pts',(-1.16855233243332,61.7161262168237,10.525919406708));
#58042=CARTESIAN_POINT('Ctrl Pts',(-0.554998030824625,61.7988802657359,
10.2746212855555));
#58043=CARTESIAN_POINT('Ctrl Pts',(0.838410518237986,61.9638525873806,10.196079471243));
#58044=CARTESIAN_POINT('Ctrl Pts',(2.54752277558488,62.2094399693199,11.3802377323902));
#58045=CARTESIAN_POINT('Ctrl Pts',(3.16045683740201,62.4529270793634,13.3481442920267));
#58046=CARTESIAN_POINT('Ctrl Pts',(2.44047887098306,62.6940925191325,15.2583700375192));
#58047=CARTESIAN_POINT('Ctrl Pts',(0.715779595689003,62.9327332534007,16.3109031130561));
#58048=CARTESIAN_POINT('Ctrl Pts',(-1.26860182455947,63.1686623612665,16.0820261164684));
#58049=CARTESIAN_POINT('Ctrl Pts',(-2.67561081487942,63.4017112264679,14.6998608482283));
#58050=CARTESIAN_POINT('Ctrl Pts',(-2.92163267124444,63.6232113919738,12.8381512919378));
#58051=CARTESIAN_POINT('Ctrl Pts',(-2.21872134954113,63.7997944393218,11.5423534614023));
#58052=CARTESIAN_POINT('Ctrl Pts',(-0.918841957931743,63.9996769886031,
10.5713624439231));
#58053=CARTESIAN_POINT('Ctrl Pts',(1.10544430662327,64.2298315981922,10.4739099322025));
#58054=CARTESIAN_POINT('Ctrl Pts',(2.82170825137881,64.51970605799,12.386084982752));
#58055=CARTESIAN_POINT('Ctrl Pts',(2.44933207825223,64.8034347666427,14.861988589747));
#58056=CARTESIAN_POINT('Ctrl Pts',(0.338060403298642,65.0809899103029,16.1176314364466));
#58057=CARTESIAN_POINT('Ctrl Pts',(-1.91793964377472,65.3524085900801,15.3018101953666));
#58058=CARTESIAN_POINT('Ctrl Pts',(-2.70511906831274,65.617817100817,13.0925450247269));
#58059=CARTESIAN_POINT('Ctrl Pts',(-1.52283152014212,65.8773964748908,11.1221290228538));
#58060=CARTESIAN_POINT('Ctrl Pts',(0.696638563926616,66.1314053760008,10.7997873793317));
#58061=CARTESIAN_POINT('Ctrl Pts',(2.32681777167293,66.3801709599473,12.2734845553138));
#58062=CARTESIAN_POINT('Ctrl Pts',(2.22322828832599,66.6240853182049,14.4283580565722));
#58063=CARTESIAN_POINT('Ctrl Pts',(0.671999738656957,66.8436213521831,15.5881093952669));
#58064=CARTESIAN_POINT('Ctrl Pts',(-0.98168785283175,67.0403488125919,15.3648459972412));
#58065=CARTESIAN_POINT('Ctrl Pts',(-2.02163523086829,67.2154312967404,14.3123594021697));
#58066=CARTESIAN_POINT('Ctrl Pts',(-2.19335801564648,67.3887819673487,12.8531399104545));
#58067=CARTESIAN_POINT('Ctrl Pts',(-1.43842230298015,67.5606555223828,11.6093759169369));
#58068=CARTESIAN_POINT('Ctrl Pts',(-0.0881736940427007,67.7313096264736,
11.0953138370229));
#58069=CARTESIAN_POINT('Ctrl Pts',(1.285019963464,67.9010179476805,11.5180318096301));
#58070=CARTESIAN_POINT('Ctrl Pts',(2.10476272204221,68.0700606754811,12.6908480644406));
#58071=CARTESIAN_POINT('Ctrl Pts',(2.03032672148608,68.2387109111275,14.1166691843227));
#58072=CARTESIAN_POINT('Ctrl Pts',(1.09526545073582,68.4072597306901,15.1946230376736));
#58073=CARTESIAN_POINT('Ctrl Pts',(-0.306217453601036,68.5759923130744,
15.4702676537639));
#58074=CARTESIAN_POINT('Ctrl Pts',(-1.5853325914691,68.7451861618208,14.8237290916841));
#58075=CARTESIAN_POINT('Ctrl Pts',(-2.12944594400514,68.8962437383695,13.6669630662597));
#58076=CARTESIAN_POINT('Ctrl Pts',(-2.03617398744539,68.9958751434108,12.8535321776987));
#58077=CARTESIAN_POINT('Ctrl Pts',(-1.90149875738473,69.0434408618903,12.4968846241885));
#58078=CARTESIAN_POINT('Ctrl Pts',(-1.8398000356147,69.0624786705015,12.3572951814658));
#58079=CARTESIAN_POINT('Ctrl Pts',(-1.71169761948827,69.0958262736986,12.1223446655951));
#58080=CARTESIAN_POINT('Ctrl Pts',(-1.37973281194231,69.1626459611235,11.6980269719962));
#58081=CARTESIAN_POINT('Ctrl Pts',(-0.719622242441448,69.2584844300639,
11.2695961091932));
#58082=CARTESIAN_POINT('Ctrl Pts',(0.0649084390206912,69.3548948427999,
11.1640051083998));
#58083=CARTESIAN_POINT('Ctrl Pts',(0.677588055410269,69.4324078644648,11.2874874815619));
#58084=CARTESIAN_POINT('Ctrl Pts',(0.999777033894293,69.4761562418558,11.4308378696215));
#58085=CARTESIAN_POINT('Ctrl Pts',(1.19860894090253,69.5053887889003,11.5548233552111));
#58086=CARTESIAN_POINT('Ctrl Pts',(1.32660386294558,69.5248947079024,11.6446756441626));
#58087=CARTESIAN_POINT('Ctrl Pts',(1.53686134829739,69.5590761839442,11.8206234250448));
#58088=CARTESIAN_POINT('Ctrl Pts',(2.10636022605492,69.6668006528317,12.4771751346531));
#58089=CARTESIAN_POINT('Ctrl Pts',(2.35791538563205,69.8447713562475,14.0265754559266));
#58090=CARTESIAN_POINT('Ctrl Pts',(0.949121047530638,70.0862200241309,15.6301546468009));
#58091=CARTESIAN_POINT('Ctrl Pts',(-1.22826102218047,70.3322944313609,15.5534418241006));
#58092=CARTESIAN_POINT('Ctrl Pts',(-2.41979078179111,70.5554983884945,13.9862112724621));
#58093=CARTESIAN_POINT('Ctrl Pts',(-2.27116036733893,70.7543056449801,12.3257473977465));
#58094=CARTESIAN_POINT('Ctrl Pts',(-1.36738576107812,70.9271998805336,11.1985433894428));
#58095=CARTESIAN_POINT('Ctrl Pts',(0.0921491958576946,71.1099725263237,
10.7355364493605));
#58096=CARTESIAN_POINT('Ctrl Pts',(1.64396370259509,71.3030831353856,11.2475534497753));
#58097=CARTESIAN_POINT('Ctrl Pts',(2.60363156558085,71.5070216091218,12.6835255182203));
#58098=CARTESIAN_POINT('Ctrl Pts',(2.47410443308142,71.7144050735568,14.434342871696));
#58099=CARTESIAN_POINT('Ctrl Pts',(1.27500325606336,71.9252579488303,15.7567695849295));
#58100=CARTESIAN_POINT('Ctrl Pts',(-0.512870675643372,72.1395798951614,
16.0660444961377));
#58101=CARTESIAN_POINT('Ctrl Pts',(-2.13839595577138,72.3573483133845,15.1961519408739));
#58102=CARTESIAN_POINT('Ctrl Pts',(-2.89569133798197,72.5785162363284,13.4832292970027));
#58103=CARTESIAN_POINT('Ctrl Pts',(-2.58704794005515,72.7281825608065,12.2549998685691));
#58104=CARTESIAN_POINT('Ctrl Pts',(-2.25606553638399,72.8035544420155,11.7498921642414));
#58105=CARTESIAN_POINT('Ctrl Pts',(-1.11234706696219,61.9237349740717,10.7800451030764));
#58106=CARTESIAN_POINT('Ctrl Pts',(-0.551984960934711,61.9995118664758,
10.5462115686574));
#58107=CARTESIAN_POINT('Ctrl Pts',(0.719238260214036,62.1500570476074,10.4674069972882));
#58108=CARTESIAN_POINT('Ctrl Pts',(2.27534796455583,62.3727400518901,11.5321674654256));
#58109=CARTESIAN_POINT('Ctrl Pts',(2.83869227102382,62.5922113005396,13.3027170540399));
#58110=CARTESIAN_POINT('Ctrl Pts',(2.2041406643837,62.8084116922911,15.0194479665355));
#58111=CARTESIAN_POINT('Ctrl Pts',(0.671656943323573,63.0213060081133,15.9687555157265));
#58112=CARTESIAN_POINT('Ctrl Pts',(-1.09261817887129,63.230880368071,15.7777026517318));
#58113=CARTESIAN_POINT('Ctrl Pts',(-2.3468926484301,63.4371437206783,14.5632979951621));
#58114=CARTESIAN_POINT('Ctrl Pts',(-2.57640944711034,63.6326088606432,12.9219357960667));
#58115=CARTESIAN_POINT('Ctrl Pts',(-1.96638287159801,63.7881145102524,11.7757850303583));
#58116=CARTESIAN_POINT('Ctrl Pts',(-0.829621454339106,63.9639615343511,
10.9121272646271));
#58117=CARTESIAN_POINT('Ctrl Pts',(0.948952924496643,64.1662398321294,10.8118735345015));
#58118=CARTESIAN_POINT('Ctrl Pts',(2.47201501163925,64.421003843011,12.4793626428307));
#58119=CARTESIAN_POINT('Ctrl Pts',(2.16429091661214,64.6707875557039,14.6621912912922));
#58120=CARTESIAN_POINT('Ctrl Pts',(0.310000895846759,64.9159648490878,15.7895918096977));
#58121=CARTESIAN_POINT('Ctrl Pts',(-1.70064237321371,65.1569453474805,15.0856079145018));
#58122=CARTESIAN_POINT('Ctrl Pts',(-2.42545733884156,65.394246323493,13.1176501165484));
#58123=CARTESIAN_POINT('Ctrl Pts',(-1.37865114244613,65.6283632635507,11.3285604610391));
#58124=CARTESIAN_POINT('Ctrl Pts',(0.641349738940361,65.8598663935718,11.0120162625725));
#58125=CARTESIAN_POINT('Ctrl Pts',(2.16088916276543,66.0893536994043,12.3544429084476));
#58126=CARTESIAN_POINT('Ctrl Pts',(2.0873493371532,66.3174469149352,14.3710586862541));
#58127=CARTESIAN_POINT('Ctrl Pts',(0.627394260415668,66.5258193195164,15.4887184567952));
#58128=CARTESIAN_POINT('Ctrl Pts',(-0.966952248386021,66.7151631539086,
15.2896494083299));
#58129=CARTESIAN_POINT('Ctrl Pts',(-1.99029443991551,66.8857762054556,14.2734563349868));
#58130=CARTESIAN_POINT('Ctrl Pts',(-2.17334990850197,67.0568641782707,12.8347205544376));
#58131=CARTESIAN_POINT('Ctrl Pts',(-1.42974172053206,67.2286966155006,11.5841402598853));
#58132=CARTESIAN_POINT('Ctrl Pts',(-0.0665580821207584,67.4015314694309,
11.0514665594181));
#58133=CARTESIAN_POINT('Ctrl Pts',(1.34605509662363,67.5756279545075,11.4733403642385));
#58134=CARTESIAN_POINT('Ctrl Pts',(2.20758999436957,67.7512359504503,12.6851069400924));
#58135=CARTESIAN_POINT('Ctrl Pts',(2.14077572797721,67.9285858629059,14.1853446214317));
#58136=CARTESIAN_POINT('Ctrl Pts',(1.15407911252636,68.1079089481521,15.339618743821));
#58137=CARTESIAN_POINT('Ctrl Pts',(-0.351727289097983,68.2894175197017,
15.6464719335678));
#58138=CARTESIAN_POINT('Ctrl Pts',(-1.74664366586638,68.473305005657,14.9526138915416));
#58139=CARTESIAN_POINT('Ctrl Pts',(-2.35125498867944,68.6390392779964,13.6868210389609));
#58140=CARTESIAN_POINT('Ctrl Pts',(-2.25257391000286,68.7491300895112,12.7873159965059));
#58141=CARTESIAN_POINT('Ctrl Pts',(-2.10495531904991,68.8018470807597,12.391385002815));
#58142=CARTESIAN_POINT('Ctrl Pts',(-2.03717175835508,68.8229602618792,12.2362787091018));
#58143=CARTESIAN_POINT('Ctrl Pts',(-1.89604486527342,68.8599781838076,11.9748525198571));
#58144=CARTESIAN_POINT('Ctrl Pts',(-1.52881357118424,68.9342928075108,11.5013498526747));
#58145=CARTESIAN_POINT('Ctrl Pts',(-0.794085685875897,69.0412663352442,
11.0197983059699));
#58146=CARTESIAN_POINT('Ctrl Pts',(0.0850065321694228,69.1493500227514,
10.8976306306484));
#58147=CARTESIAN_POINT('Ctrl Pts',(0.774475301734965,69.2365010454107,11.033827428284));
#58148=CARTESIAN_POINT('Ctrl Pts',(1.13804342964187,69.2857812179576,11.1939391739118));
#58149=CARTESIAN_POINT('Ctrl Pts',(1.36277942277332,69.3187442334309,11.3329370967313));
#58150=CARTESIAN_POINT('Ctrl Pts',(1.50755054814791,69.3407486541439,11.4337766328478));
#58151=CARTESIAN_POINT('Ctrl Pts',(1.74563217381336,69.3793327931068,11.6315473166949));
#58152=CARTESIAN_POINT('Ctrl Pts',(2.39204209314634,69.5010797157444,12.371157206559));
#58153=CARTESIAN_POINT('Ctrl Pts',(2.68537004139343,69.7029621444375,14.1276946542204));
#58154=CARTESIAN_POINT('Ctrl Pts',(1.08798299853103,69.9779620136592,15.9608354407845));
#58155=CARTESIAN_POINT('Ctrl Pts',(-1.39821458961621,70.258854973133,15.8819473431239));
#58156=CARTESIAN_POINT('Ctrl Pts',(-2.76464437090339,70.513781405731,14.0959696453757));
#58157=CARTESIAN_POINT('Ctrl Pts',(-2.60051720125486,70.7406191214659,12.2007578370582));
#58158=CARTESIAN_POINT('Ctrl Pts',(-1.57438150313715,70.9376043691068,10.9135292180737));
#58159=CARTESIAN_POINT('Ctrl Pts',(0.083710492335456,71.1454029061075,10.3825833010656));
#58160=CARTESIAN_POINT('Ctrl Pts',(1.84447942973013,71.3643206793081,10.9586311533899));
#58161=CARTESIAN_POINT('Ctrl Pts',(2.9322473004846,71.5946312759554,12.5777954928207));
#58162=CARTESIAN_POINT('Ctrl Pts',(2.79125106104368,71.8277863360761,14.5466512422041));
#58163=CARTESIAN_POINT('Ctrl Pts',(1.45333308887358,72.0636374859992,16.0290402831137));
#58164=CARTESIAN_POINT('Ctrl Pts',(-0.53452772748346,72.3020117956332,16.3775899567483));
#58165=CARTESIAN_POINT('Ctrl Pts',(-2.33363843540989,72.5427284022483,15.4200462674978));
#58166=CARTESIAN_POINT('Ctrl Pts',(-3.16951350766352,72.785585491095,13.5409680482108));
#58167=CARTESIAN_POINT('Ctrl Pts',(-2.83608351112003,72.9487744186263,12.2008932325256));
#58168=CARTESIAN_POINT('Ctrl Pts',(-2.47847683852305,73.0306494992593,11.6508904210054));
#58169=CARTESIAN_POINT('Ctrl Pts',(-1.05614180149106,62.1313437313199,11.0341707994449));
#58170=CARTESIAN_POINT('Ctrl Pts',(-0.548971891044798,62.2001434672158,
10.8178018517592));
#58171=CARTESIAN_POINT('Ctrl Pts',(0.600066002190081,62.3362615078341,10.7387345233335));
#58172=CARTESIAN_POINT('Ctrl Pts',(2.00317315352676,62.5360401344603,11.6840971984608));
#58173=CARTESIAN_POINT('Ctrl Pts',(2.51692770464562,62.7314955217158,13.2572898160531));
#58174=CARTESIAN_POINT('Ctrl Pts',(1.96780245778434,62.9227308654496,14.7805258955518));
#58175=CARTESIAN_POINT('Ctrl Pts',(0.627534290958144,63.1098787628258,15.6266079183967));
#58176=CARTESIAN_POINT('Ctrl Pts',(-0.916634533183098,63.2930983748755,
15.4733791869953));
#58177=CARTESIAN_POINT('Ctrl Pts',(-2.01817448198077,63.4725762148886,14.4267351420959));
#58178=CARTESIAN_POINT('Ctrl Pts',(-2.23118622297626,63.6420063293127,13.0057203001957));
#58179=CARTESIAN_POINT('Ctrl Pts',(-1.71404439365489,63.7764345811831,12.0092165993144));
#58180=CARTESIAN_POINT('Ctrl Pts',(-0.74040095074646,63.9282460800993,11.252892085331));
#58181=CARTESIAN_POINT('Ctrl Pts',(0.79246154237002,64.1026480660666,11.1498371368005));
#58182=CARTESIAN_POINT('Ctrl Pts',(2.12232177189969,64.3223016280321,12.5726403029094));
#58183=CARTESIAN_POINT('Ctrl Pts',(1.87924975497206,64.538140344765,14.4623939928372));
#58184=CARTESIAN_POINT('Ctrl Pts',(0.281941388394872,64.7509397878726,15.4615521829488));
#58185=CARTESIAN_POINT('Ctrl Pts',(-1.48334510265271,64.9614821048809,14.8694056336369));
#58186=CARTESIAN_POINT('Ctrl Pts',(-2.14579560937037,65.170675546169,13.14275520837));
#58187=CARTESIAN_POINT('Ctrl Pts',(-1.23447076475016,65.3793300522108,11.5349918992243));
#58188=CARTESIAN_POINT('Ctrl Pts',(0.586060913954109,65.5883274111427,11.2242451458131));
#58189=CARTESIAN_POINT('Ctrl Pts',(1.99496055385793,65.7985364388612,12.4354012615815));
#58190=CARTESIAN_POINT('Ctrl Pts',(1.9514703859804,66.0108085116655,14.3137593159358));
#58191=CARTESIAN_POINT('Ctrl Pts',(0.582788782174383,66.2080172868495,15.3893275183234));
#58192=CARTESIAN_POINT('Ctrl Pts',(-0.952216643940287,66.3899774952253,
15.2144528194188));
#58193=CARTESIAN_POINT('Ctrl Pts',(-1.95895364896274,66.5561211141707,14.2345532678041));
#58194=CARTESIAN_POINT('Ctrl Pts',(-2.15334180135745,66.7249463891927,12.8163011984208));
#58195=CARTESIAN_POINT('Ctrl Pts',(-1.42106113808395,66.8967377086185,11.5589046028338));
#58196=CARTESIAN_POINT('Ctrl Pts',(-0.0449424701988081,67.0717533123881,
11.0076192818134));
#58197=CARTESIAN_POINT('Ctrl Pts',(1.40709022978329,67.2502379613344,11.4286489188467));
#58198=CARTESIAN_POINT('Ctrl Pts',(2.31041726669693,67.4324112254196,12.6793658157442));
#58199=CARTESIAN_POINT('Ctrl Pts',(2.25122473446836,67.6184608146842,14.2540200585407));
#58200=CARTESIAN_POINT('Ctrl Pts',(1.21289277431689,67.8085581656143,15.4846144499685));
#58201=CARTESIAN_POINT('Ctrl Pts',(-0.397237124594922,68.0028427263292,
15.8226762133719));
#58202=CARTESIAN_POINT('Ctrl Pts',(-1.90795474026366,68.2014238494934,15.0814986913989));
#58203=CARTESIAN_POINT('Ctrl Pts',(-2.57306403335372,68.3818348176235,13.706679011662));
#58204=CARTESIAN_POINT('Ctrl Pts',(-2.4689738325603,68.5023850356115,12.7210998153131));
#58205=CARTESIAN_POINT('Ctrl Pts',(-2.30841188071509,68.5602532996293,12.2858853814415));
#58206=CARTESIAN_POINT('Ctrl Pts',(-2.23454348109542,68.5834418532569,12.1152622367379));
#58207=CARTESIAN_POINT('Ctrl Pts',(-2.08039211105857,68.6241300939167,11.8273603741192));
#58208=CARTESIAN_POINT('Ctrl Pts',(-1.67789433042616,68.705939653898,11.304672733353));
#58209=CARTESIAN_POINT('Ctrl Pts',(-0.868549129310337,68.8240482404245,
10.7700005027465));
#58210=CARTESIAN_POINT('Ctrl Pts',(0.105104625318163,68.943805202703,10.631256152897));
#58211=CARTESIAN_POINT('Ctrl Pts',(0.871362548059674,69.0405942263567,10.7801673750063));
#58212=CARTESIAN_POINT('Ctrl Pts',(1.27630982538946,69.0954061940594,10.9570404782022));
#58213=CARTESIAN_POINT('Ctrl Pts',(1.52694990464411,69.1320996779613,11.1110508382515));
#58214=CARTESIAN_POINT('Ctrl Pts',(1.68849723335025,69.1566026003853,11.222877621533));
#58215=CARTESIAN_POINT('Ctrl Pts',(1.95440299932936,69.1995894022695,11.442471208345));
#58216=CARTESIAN_POINT('Ctrl Pts',(2.67772396023776,69.335358778657,12.2651392784647));
#58217=CARTESIAN_POINT('Ctrl Pts',(3.01282469715482,69.5611529326277,14.2288138525143));
#58218=CARTESIAN_POINT('Ctrl Pts',(1.22684494953145,69.8697040031874,16.2915162347679));
#58219=CARTESIAN_POINT('Ctrl Pts',(-1.56816815705193,70.1854155149051,16.2104528621472));
#58220=CARTESIAN_POINT('Ctrl Pts',(-3.10949796001566,70.4720644229672,14.2057280182894));
#58221=CARTESIAN_POINT('Ctrl Pts',(-2.92987403517079,70.7269325979517,12.0757682763698));
#58222=CARTESIAN_POINT('Ctrl Pts',(-1.78137724519618,70.9480088576798,10.6285150467044));
#58223=CARTESIAN_POINT('Ctrl Pts',(0.0752717888132247,71.1808332858912,
10.0296301527708));
#58224=CARTESIAN_POINT('Ctrl Pts',(2.04499515686519,71.4255582232306,10.6697088570044));
#58225=CARTESIAN_POINT('Ctrl Pts',(3.26086303538833,71.6822409427889,12.4720654674214));
#58226=CARTESIAN_POINT('Ctrl Pts',(3.10839768900593,71.9411675985953,14.6589596127122));
#58227=CARTESIAN_POINT('Ctrl Pts',(1.63166292168379,72.2020170231681,16.3013109812979));
#58228=CARTESIAN_POINT('Ctrl Pts',(-0.55618477932355,72.4644436961051,16.6891354173588));
#58229=CARTESIAN_POINT('Ctrl Pts',(-2.5288809150484,72.7281084911122,15.6439405941217));
#58230=CARTESIAN_POINT('Ctrl Pts',(-3.44333567734506,72.9926547458617,13.5987067994188));
#58231=CARTESIAN_POINT('Ctrl Pts',(-3.08511908218492,73.1693662764461,12.1467865964821));
#58232=CARTESIAN_POINT('Ctrl Pts',(-2.70088814066211,73.2577445565031,11.5518886777693));
#58233=CARTESIAN_POINT('Ctrl Pts',(-1.05593533999082,62.1312800345432,11.0339552088038));
#58234=CARTESIAN_POINT('Ctrl Pts',(-0.548797894764382,62.2000722428305,
10.8176652497803));
#58235=CARTESIAN_POINT('Ctrl Pts',(0.600192035121667,62.3361862873998,10.7386582030159));
#58236=CARTESIAN_POINT('Ctrl Pts',(2.00329796012928,62.5359652527017,11.6840275306112));
#58237=CARTESIAN_POINT('Ctrl Pts',(2.51707525078404,62.7314316525048,13.2573106468538));
#58238=CARTESIAN_POINT('Ctrl Pts',(1.96791083140091,62.9226784440387,14.7806354540074));
#58239=CARTESIAN_POINT('Ctrl Pts',(0.627554523537033,63.1098381475148,15.6267648112371));
#58240=CARTESIAN_POINT('Ctrl Pts',(-0.916715231028849,63.2930698446158,
15.4735187354625));
#58241=CARTESIAN_POINT('Ctrl Pts',(-2.01832521671403,63.4725599672086,14.4267977634151));
#58242=CARTESIAN_POINT('Ctrl Pts',(-2.23134452615484,63.6420020200743,13.0056818805518));
#58243=CARTESIAN_POINT('Ctrl Pts',(-1.71416010424544,63.7764399370507,12.0091095585455));
#58244=CARTESIAN_POINT('Ctrl Pts',(-0.740441863084698,63.9282624575314,
11.2527358265671));
#58245=CARTESIAN_POINT('Ctrl Pts',(0.792533301977947,64.1026772262679,11.149682162544));
#58246=CARTESIAN_POINT('Ctrl Pts',(2.12248212481777,64.3223468882384,12.5725975301495));
#58247=CARTESIAN_POINT('Ctrl Pts',(1.8793804614795,64.5382011705544,14.4624856105072));
#58248=CARTESIAN_POINT('Ctrl Pts',(0.281954255168914,64.7510154606255,15.4617026065356));
#58249=CARTESIAN_POINT('Ctrl Pts',(-1.48344474498909,64.9615717351561,14.8695047738624));
#58250=CARTESIAN_POINT('Ctrl Pts',(-2.14592384912253,65.1707780652413,13.1427436963524));
#58251=CARTESIAN_POINT('Ctrl Pts',(-1.23453687910888,65.3794442471611,11.534897239449));
#58252=CARTESIAN_POINT('Ctrl Pts',(0.586086266816036,65.588451926184,11.2241478276014));
#58253=CARTESIAN_POINT('Ctrl Pts',(1.99503664093542,65.7986697940167,12.4353641378779));
#58254=CARTESIAN_POINT('Ctrl Pts',(1.95153269369428,66.010949121655,14.3137855907395));
#58255=CARTESIAN_POINT('Ctrl Pts',(0.582809236154573,66.2081630159558,15.389373094346));
#58256=CARTESIAN_POINT('Ctrl Pts',(-0.952223400997341,66.3901266101162,
15.2144873010475));
#58257=CARTESIAN_POINT('Ctrl Pts',(-1.95896802037949,66.5562722785337,14.234571106926));
#58258=CARTESIAN_POINT('Ctrl Pts',(-2.15335097613695,66.7250985911228,12.8163096446735));
#58259=CARTESIAN_POINT('Ctrl Pts',(-1.42106511859191,66.8968899294033,11.5589161747225));
#58260=CARTESIAN_POINT('Ctrl Pts',(-0.0449523821045983,67.0719045331833,
11.0076393881183));
#58261=CARTESIAN_POINT('Ctrl Pts',(1.40706224193395,67.2503871699235,11.4286694122474));
#58262=CARTESIAN_POINT('Ctrl Pts',(2.31037011493275,67.4325574234846,12.6793684483545));
#58263=CARTESIAN_POINT('Ctrl Pts',(2.25117408773437,67.6186030234855,14.2539885672063));
#58264=CARTESIAN_POINT('Ctrl Pts',(1.21286580513013,67.8086954338427,15.4845479617384));
#58265=CARTESIAN_POINT('Ctrl Pts',(-0.397216255918911,68.0029741360882,
15.8225954143537));
#58266=CARTESIAN_POINT('Ctrl Pts',(-1.90788077057091,68.2015485214395,15.0814395908748));
#58267=CARTESIAN_POINT('Ctrl Pts',(-2.4982095699917,68.3616759780349,13.8611890279));
#58268=CARTESIAN_POINT('Ctrl Pts',(-2.49283646883181,68.4555325144937,13.1030816010796));
#58269=CARTESIAN_POINT('Ctrl Pts',(-2.46701393303641,68.4808270900767,12.9018894245279));
#58270=CARTESIAN_POINT('Ctrl Pts',(0.247287541580098,77.6548572027072,10.0427241822324));
#58271=CARTESIAN_POINT('Ctrl Pts',(0.964069001324889,77.7445925079294,10.0979779665913));
#58272=CARTESIAN_POINT('Ctrl Pts',(2.35704967373067,77.9240000776253,10.7009273106633));
#58273=CARTESIAN_POINT('Ctrl Pts',(3.4467728248986,78.192503630638,12.6958819746852));
#58274=CARTESIAN_POINT('Ctrl Pts',(3.07923969920137,78.4600209528315,14.9304288566278));
#58275=CARTESIAN_POINT('Ctrl Pts',(1.42315265705318,78.7261651385104,16.4576833059984));
#58276=CARTESIAN_POINT('Ctrl Pts',(-0.806764227344182,78.9905667981157,
16.6425893403264));
#58277=CARTESIAN_POINT('Ctrl Pts',(-2.66532596956275,79.2528650228532,15.4237333446468));
#58278=CARTESIAN_POINT('Ctrl Pts',(-3.37042528836801,79.5127146681829,13.3446071043689));
#58279=CARTESIAN_POINT('Ctrl Pts',(-2.5847048075285,79.7983491753509,11.0520674671235));
#58280=CARTESIAN_POINT('Ctrl Pts',(-0.137666389072941,80.1081393123657,
9.82774503828806));
#58281=CARTESIAN_POINT('Ctrl Pts',(2.53491771752001,80.439918590107,11.0372481405381));
#58282=CARTESIAN_POINT('Ctrl Pts',(3.0843688080165,80.6768938598906,13.0523003042481));
#58283=CARTESIAN_POINT('Ctrl Pts',(2.70076310244372,80.863947802345,14.5066703222784));
#58284=CARTESIAN_POINT('Ctrl Pts',(1.97786813303724,81.0228941830997,15.6027318765835));
#58285=CARTESIAN_POINT('Ctrl Pts',(0.302161778549171,81.2380000656201,16.3168978017426));
#58286=CARTESIAN_POINT('Ctrl Pts',(-1.58085531198438,81.4682050832055,15.8160551896125));
#58287=CARTESIAN_POINT('Ctrl Pts',(-2.73467581966542,81.6938241351438,14.2940760892576));
#58288=CARTESIAN_POINT('Ctrl Pts',(-2.70879358569799,81.914758094417,12.4242532818977));
#58289=CARTESIAN_POINT('Ctrl Pts',(-1.5638821754899,82.1309391180892,10.9962972897096));
#58290=CARTESIAN_POINT('Ctrl Pts',(-0.112332637144442,82.3070995697092,
10.65403698097));
#58291=CARTESIAN_POINT('Ctrl Pts',(0.971767836276392,82.4456316622513,10.9480842940185));
#58292=CARTESIAN_POINT('Ctrl Pts',(2.05531843922359,82.6053950292879,11.669616155466));
#58293=CARTESIAN_POINT('Ctrl Pts',(2.58022303152249,82.772929767339,13.0429223676538));
#58294=CARTESIAN_POINT('Ctrl Pts',(2.10894229679348,82.9692944639935,14.5905689471349));
#58295=CARTESIAN_POINT('Ctrl Pts',(1.03068522636296,83.1404274052572,15.5507677597493));
#58296=CARTESIAN_POINT('Ctrl Pts',(-0.560032659422088,83.3284650308457,
15.6518101151826));
#58297=CARTESIAN_POINT('Ctrl Pts',(-1.8447489750784,83.512170284916,14.772879306662));
#58298=CARTESIAN_POINT('Ctrl Pts',(-2.25261977308136,83.6717741940494,13.489840670357));
#58299=CARTESIAN_POINT('Ctrl Pts',(-1.91138106357061,83.8480453771256,12.0775888075753));
#58300=CARTESIAN_POINT('Ctrl Pts',(-0.72049864066441,84.0205323353866,11.1412811543025));
#58301=CARTESIAN_POINT('Ctrl Pts',(0.862171558101919,84.2077261938883,11.3140639157902));
#58302=CARTESIAN_POINT('Ctrl Pts',(1.8664262479419,84.3730421625329,12.283684323027));
#58303=CARTESIAN_POINT('Ctrl Pts',(2.06128816907136,84.5355159613324,13.6464327914842));
#58304=CARTESIAN_POINT('Ctrl Pts',(1.38720207749988,84.6954633805368,14.8205992727919));
#58305=CARTESIAN_POINT('Ctrl Pts',(0.151211699798348,84.8532298820947,15.326232344394));
#58306=CARTESIAN_POINT('Ctrl Pts',(-1.11958576901327,85.009179694123,14.9693938082164));
#58307=CARTESIAN_POINT('Ctrl Pts',(-1.89575588946321,85.1636728011368,13.9162459886775));
#58308=CARTESIAN_POINT('Ctrl Pts',(-1.86375037275616,85.3000452442271,12.7629372015215));
#58309=CARTESIAN_POINT('Ctrl Pts',(-1.4047981936709,85.4019466736085,12.062882842335));
#58310=CARTESIAN_POINT('Ctrl Pts',(-0.973350991123209,85.4697837447249,
11.7271521694353));
#58311=CARTESIAN_POINT('Ctrl Pts',(-0.479131804993002,85.5375812762284,
11.4936252857917));
#58312=CARTESIAN_POINT('Ctrl Pts',(0.212066650498646,85.6222764554439,11.4174503611125));
#58313=CARTESIAN_POINT('Ctrl Pts',(1.00124737159773,85.723955620617,11.6892758599415));
#58314=CARTESIAN_POINT('Ctrl Pts',(1.50026311536417,85.8088213091389,12.1762090409978));
#58315=CARTESIAN_POINT('Ctrl Pts',(1.74529030119219,85.8768560281014,12.6664088610162));
#58316=CARTESIAN_POINT('Ctrl Pts',(1.94992832551134,85.979067489764,13.4654738216233));
#58317=CARTESIAN_POINT('Ctrl Pts',(1.54155537527295,86.133122989655,14.7611755398965));
#58318=CARTESIAN_POINT('Ctrl Pts',(-0.161706220391905,86.3409986454679,
15.4503179358885));
#58319=CARTESIAN_POINT('Ctrl Pts',(-1.80233989822033,86.552223249788,14.554166040512));
#58320=CARTESIAN_POINT('Ctrl Pts',(-2.11499875684585,86.7436966602518,12.8951618407757));
#58321=CARTESIAN_POINT('Ctrl Pts',(-1.36195053022674,86.9144564975112,11.6765763097194));
#58322=CARTESIAN_POINT('Ctrl Pts',(-0.232848814881847,87.0632468330563,
11.1571740292811));
#58323=CARTESIAN_POINT('Ctrl Pts',(1.07249419248516,87.2209790231122,11.363039966774));
#58324=CARTESIAN_POINT('Ctrl Pts',(2.07652075315406,87.3882686374323,12.3607198540593));
#58325=CARTESIAN_POINT('Ctrl Pts',(2.26531128235019,87.5658187484789,13.8523567274988));
#58326=CARTESIAN_POINT('Ctrl Pts',(1.47889922862541,87.7474173482421,15.1732495990815));
#58327=CARTESIAN_POINT('Ctrl Pts',(0.0127680510151906,87.9332577758032,
15.7439964436861));
#58328=CARTESIAN_POINT('Ctrl Pts',(-1.52981989797465,88.1235131031462,15.2808950263592));
#58329=CARTESIAN_POINT('Ctrl Pts',(-2.48339938369146,88.3183210263946,13.9353972421663));
#58330=CARTESIAN_POINT('Ctrl Pts',(-2.40474239046522,88.5177875734279,12.2482339471135));
#58331=CARTESIAN_POINT('Ctrl Pts',(-1.65476716887248,88.6539234702229,11.3740678808263));
#58332=CARTESIAN_POINT('Ctrl Pts',(-1.17773130173033,88.7227885365479,11.0968781559722));
#58333=CARTESIAN_POINT('Ctrl Pts',(0.184803675495247,77.862472667449,10.2953881670292));
#58334=CARTESIAN_POINT('Ctrl Pts',(0.846167896041115,77.9452305174071,10.3426706699363));
#58335=CARTESIAN_POINT('Ctrl Pts',(2.12976813845044,78.1102104375581,10.8911235114185));
#58336=CARTESIAN_POINT('Ctrl Pts',(3.13541597804943,78.3558092526022,12.7111536714507));
#58337=CARTESIAN_POINT('Ctrl Pts',(2.81105501535664,78.599309525502,14.7468282838804));
#58338=CARTESIAN_POINT('Ctrl Pts',(1.3174660878423,78.8404879419078,16.1386573044603));
#58339=CARTESIAN_POINT('Ctrl Pts',(-0.694485932762879,79.079142259978,16.3163710055547));
#58340=CARTESIAN_POINT('Ctrl Pts',(-2.37242298386509,79.3150850725898,15.229252877698));
#58341=CARTESIAN_POINT('Ctrl Pts',(-3.01564346814379,79.5481480850051,13.3680196060162));
#58342=CARTESIAN_POINT('Ctrl Pts',(-2.32463299882677,79.8037412444127,11.3123399690757));
#58343=CARTESIAN_POINT('Ctrl Pts',(-0.145960813747356,80.0803886369846,
10.2058035594949));
#58344=CARTESIAN_POINT('Ctrl Pts',(2.2448406691886,80.376321418116,11.2692709379055));
#58345=CARTESIAN_POINT('Ctrl Pts',(2.74720689877205,80.5877004008594,13.0633520002669));
#58346=CARTESIAN_POINT('Ctrl Pts',(2.41359112629158,80.754675913076,14.3640425134037));
#58347=CARTESIAN_POINT('Ctrl Pts',(1.77467578964236,80.8966446736528,15.3475444027645));
#58348=CARTESIAN_POINT('Ctrl Pts',(0.280266482960803,81.089066666713,15.9972992631639));
#58349=CARTESIAN_POINT('Ctrl Pts',(-1.41186855660018,81.2955160386158,15.5607616424528));
#58350=CARTESIAN_POINT('Ctrl Pts',(-2.46067898716311,81.498529477346,14.199207170258));
#58351=CARTESIAN_POINT('Ctrl Pts',(-2.45065374611866,81.698160141879,12.5094141597136));
#58352=CARTESIAN_POINT('Ctrl Pts',(-1.42141928360188,81.8944830257032,11.2041161942034));
#58353=CARTESIAN_POINT('Ctrl Pts',(-0.0978562227218405,82.0554116780197,
10.8803746487815));
#58354=CARTESIAN_POINT('Ctrl Pts',(0.89975624661569,82.1826084511176,11.1429047439257));
#58355=CARTESIAN_POINT('Ctrl Pts',(1.90330680638142,82.329832284588,11.8000378769176));
#58356=CARTESIAN_POINT('Ctrl Pts',(2.40255550468052,82.4853171492715,13.0701031156741));
#58357=CARTESIAN_POINT('Ctrl Pts',(1.97314920561762,82.6691658414288,14.5229682427947));
#58358=CARTESIAN_POINT('Ctrl Pts',(0.963543218920492,82.8306537998472,15.4380219300933));
#58359=CARTESIAN_POINT('Ctrl Pts',(-0.551987846154585,83.0099144809128,
15.548159807256));
#58360=CARTESIAN_POINT('Ctrl Pts',(-1.79825228513438,83.1869738653656,14.7122634879005));
#58361=CARTESIAN_POINT('Ctrl Pts',(-2.20715491105176,83.3426053314291,13.4645232622311));
#58362=CARTESIAN_POINT('Ctrl Pts',(-1.88252472097578,83.5162453863774,12.0706692194223));
#58363=CARTESIAN_POINT('Ctrl Pts',(-0.704083095511786,83.6883202304834,
11.1243417314447));
#58364=CARTESIAN_POINT('Ctrl Pts',(0.900949647343497,83.8779374958976,11.2844042859749));
#58365=CARTESIAN_POINT('Ctrl Pts',(1.94079100521003,84.0476417923649,12.2709767567351));
#58366=CARTESIAN_POINT('Ctrl Pts',(2.15586901925411,84.2166812486924,13.6870647569731));
#58367=CARTESIAN_POINT('Ctrl Pts',(1.45555116861922,84.3853283298918,14.9313227792802));
#58368=CARTESIAN_POINT('Ctrl Pts',(0.139421890731178,84.5538699300146,15.482377466424));
#58369=CARTESIAN_POINT('Ctrl Pts',(-1.23870833428518,84.7225961199578,15.1071712083794));
#58370=CARTESIAN_POINT('Ctrl Pts',(-2.09762284605641,84.8917831351255,13.960184736452));
#58371=CARTESIAN_POINT('Ctrl Pts',(-2.0714028319448,85.0428328228877,12.6823062984053));
#58372=CARTESIAN_POINT('Ctrl Pts',(-1.56323576511282,85.1566891462768,11.8968515809312));
#58373=CARTESIAN_POINT('Ctrl Pts',(-1.08076080089141,85.2328581275125,11.5172616832284));
#58374=CARTESIAN_POINT('Ctrl Pts',(-0.525465502422548,85.3092207324986,
11.2512630571995));
#58375=CARTESIAN_POINT('Ctrl Pts',(0.256192788495037,85.4050520677571,11.160632154595));
#58376=CARTESIAN_POINT('Ctrl Pts',(1.15585653050521,85.5207387464336,11.4649965691636));
#58377=CARTESIAN_POINT('Ctrl Pts',(1.72949109010161,85.6177796698734,12.0187932605256));
#58378=CARTESIAN_POINT('Ctrl Pts',(2.01332360175128,85.6958323950965,12.5799038605807));
#58379=CARTESIAN_POINT('Ctrl Pts',(2.25306236695033,85.8133417315253,13.497370825771));
#58380=CARTESIAN_POINT('Ctrl Pts',(1.7900960149886,85.9913056754938,14.9971579306732));
#58381=CARTESIAN_POINT('Ctrl Pts',(-0.184091351432346,86.2327348191477,
15.8082302617226));
#58382=CARTESIAN_POINT('Ctrl Pts',(-2.10043413195707,86.4787852330779,14.7729907970524));
#58383=CARTESIAN_POINT('Ctrl Pts',(-2.47275342454578,86.7019769498762,12.8404470847727));
#58384=CARTESIAN_POINT('Ctrl Pts',(-1.60144586883462,86.9007689105388,11.4183199337594));
#58385=CARTESIAN_POINT('Ctrl Pts',(-0.291719036302049,87.0736507381159,
10.8098947257727));
#58386=CARTESIAN_POINT('Ctrl Pts',(1.22174090202642,87.2564100022132,11.043035987828));
#58387=CARTESIAN_POINT('Ctrl Pts',(2.38453426877103,87.4495072117008,12.1908837927305));
#58388=CARTESIAN_POINT('Ctrl Pts',(2.60676095777434,87.6534314516664,13.9035461000159));
#58389=CARTESIAN_POINT('Ctrl Pts',(1.7132379478211,87.8608015674409,15.4147166578918));
#58390=CARTESIAN_POINT('Ctrl Pts',(0.0516842488560093,88.0716411492593,
16.0671514745576));
#58391=CARTESIAN_POINT('Ctrl Pts',(-1.68754739984842,88.2859506018957,15.5504356901444));
#58392=CARTESIAN_POINT('Ctrl Pts',(-2.75775208799366,88.503706693754,14.0493169297074));
#58393=CARTESIAN_POINT('Ctrl Pts',(-2.67572823382123,88.7248631301323,12.1783780710712));
#58394=CARTESIAN_POINT('Ctrl Pts',(-1.85388558078155,88.8745225725434,11.2150008714402));
#58395=CARTESIAN_POINT('Ctrl Pts',(-1.3330573230966,88.949891053716,10.9094060841414));
#58396=CARTESIAN_POINT('Ctrl Pts',(0.122319809410396,78.0700881321905,10.548052151826));
#58397=CARTESIAN_POINT('Ctrl Pts',(0.728266790757343,78.1458685268846,10.5873633732813));
#58398=CARTESIAN_POINT('Ctrl Pts',(1.90248660317024,78.2964207974908,11.0813197121736));
#58399=CARTESIAN_POINT('Ctrl Pts',(2.82405913120026,78.5191148745665,12.7264253682162));
#58400=CARTESIAN_POINT('Ctrl Pts',(2.54287033151193,78.7385980981725,14.5632277111332));
#58401=CARTESIAN_POINT('Ctrl Pts',(1.21177951863141,78.9548107453053,15.8196313029222));
#58402=CARTESIAN_POINT('Ctrl Pts',(-0.582207638181581,79.16771772184,15.990152670783));
#58403=CARTESIAN_POINT('Ctrl Pts',(-2.07951999816744,79.3773051223264,15.0347724107492));
#58404=CARTESIAN_POINT('Ctrl Pts',(-2.66086164791958,79.5835815018273,13.3914321076634));
#58405=CARTESIAN_POINT('Ctrl Pts',(-2.06456119012503,79.8091333134742,11.5726124710281));
#58406=CARTESIAN_POINT('Ctrl Pts',(-0.154255238421772,80.0526379616033,
10.5838620807018));
#58407=CARTESIAN_POINT('Ctrl Pts',(1.95476362085717,80.312724246125,11.501293735273));
#58408=CARTESIAN_POINT('Ctrl Pts',(2.41004498952759,80.4985069418283,13.074403696286));
#58409=CARTESIAN_POINT('Ctrl Pts',(2.12641915013944,80.6454040238068,14.2214147045289));
#58410=CARTESIAN_POINT('Ctrl Pts',(1.57148344624747,80.7703951642059,15.0923569289456));
#58411=CARTESIAN_POINT('Ctrl Pts',(0.258371187372433,80.9401332678059,15.677700724585));
#58412=CARTESIAN_POINT('Ctrl Pts',(-1.24288180121598,81.1228269940261,15.3054680952933));
#58413=CARTESIAN_POINT('Ctrl Pts',(-2.1866821546608,81.3032348195481,14.1043382512586));
#58414=CARTESIAN_POINT('Ctrl Pts',(-2.19251390653934,81.4815621893412,12.5945750375294));
#58415=CARTESIAN_POINT('Ctrl Pts',(-1.27895639171386,81.6580269333169,11.4119350986974));
#58416=CARTESIAN_POINT('Ctrl Pts',(-0.0833798082992409,81.8037237863302,
11.1067123165931));
#58417=CARTESIAN_POINT('Ctrl Pts',(0.827744656954988,81.9195852399837,11.3377251938329));
#58418=CARTESIAN_POINT('Ctrl Pts',(1.75129517353926,82.0542695398883,11.9304595983692));
#58419=CARTESIAN_POINT('Ctrl Pts',(2.22488797783857,82.197704531204,13.0972838636943));
#58420=CARTESIAN_POINT('Ctrl Pts',(1.83735611444177,82.3690372188642,14.4553675384547));
#58421=CARTESIAN_POINT('Ctrl Pts',(0.896401211478014,82.5208801944373,15.3252761004372));
#58422=CARTESIAN_POINT('Ctrl Pts',(-0.543943032887081,82.6913639309801,
15.4445094993294));
#58423=CARTESIAN_POINT('Ctrl Pts',(-1.75175559519037,82.8617774458153,14.6516476691391));
#58424=CARTESIAN_POINT('Ctrl Pts',(-2.16169004902218,83.0134364688086,13.4392058541051));
#58425=CARTESIAN_POINT('Ctrl Pts',(-1.85366837838093,83.1844453956293,12.0637496312695));
#58426=CARTESIAN_POINT('Ctrl Pts',(-0.687667550359165,83.3561081255805,
11.1074023085868));
#58427=CARTESIAN_POINT('Ctrl Pts',(0.939727736585077,83.5481487979069,11.2547446561599));
#58428=CARTESIAN_POINT('Ctrl Pts',(2.01515576247816,83.7222414221968,12.258269190443));
#58429=CARTESIAN_POINT('Ctrl Pts',(2.25044986943687,83.8978465360525,13.7276967224621));
#58430=CARTESIAN_POINT('Ctrl Pts',(1.52390025973857,84.0751932792468,15.0420462857686));
#58431=CARTESIAN_POINT('Ctrl Pts',(0.127632081664017,84.2545099779345,15.638522588454));
#58432=CARTESIAN_POINT('Ctrl Pts',(-1.35783089955709,84.4360125457928,15.2449486085422));
#58433=CARTESIAN_POINT('Ctrl Pts',(-2.29948980264962,84.619893469114,14.0041234842265));
#58434=CARTESIAN_POINT('Ctrl Pts',(-2.27905529113342,84.7856204015483,12.6016753952892));
#58435=CARTESIAN_POINT('Ctrl Pts',(-1.72167333655474,84.9114316189451,11.7308203195274));
#58436=CARTESIAN_POINT('Ctrl Pts',(-1.18817061065961,84.9959325103001,11.3073711970217));
#58437=CARTESIAN_POINT('Ctrl Pts',(-0.571799199852085,85.0808601887689,
11.0089008286074));
#58438=CARTESIAN_POINT('Ctrl Pts',(0.300318926491433,85.1878276800704,10.9038139480775));
#58439=CARTESIAN_POINT('Ctrl Pts',(1.31046568941269,85.3175218722502,11.2407172783856));
#58440=CARTESIAN_POINT('Ctrl Pts',(1.95871906483905,85.4267380306077,11.8613774800535));
#58441=CARTESIAN_POINT('Ctrl Pts',(2.28135690231037,85.5148087620915,12.4933988601451));
#58442=CARTESIAN_POINT('Ctrl Pts',(2.55619640838934,85.6476159732867,13.5292678299187));
#58443=CARTESIAN_POINT('Ctrl Pts',(2.03863665470422,85.8494883613327,15.2331403214501));
#58444=CARTESIAN_POINT('Ctrl Pts',(-0.206476482472782,86.1244709928276,
16.1661425875569));
#58445=CARTESIAN_POINT('Ctrl Pts',(-2.39852836569383,86.4053472163679,14.9918155535928));
#58446=CARTESIAN_POINT('Ctrl Pts',(-2.8305080922457,86.6602572395007,12.7857323287695));
#58447=CARTESIAN_POINT('Ctrl Pts',(-1.8409412074425,86.8870813235665,11.1600635577994));
#58448=CARTESIAN_POINT('Ctrl Pts',(-0.350589257722249,87.0840546431753,
10.4626154222644));
#58449=CARTESIAN_POINT('Ctrl Pts',(1.37098761156767,87.2918409813142,10.723032008882));
#58450=CARTESIAN_POINT('Ctrl Pts',(2.692547784388,87.5107457859693,12.0210477314016));
#58451=CARTESIAN_POINT('Ctrl Pts',(2.94821063319851,87.741044154854,13.9547354725332));
#58452=CARTESIAN_POINT('Ctrl Pts',(1.94757666701682,87.9741857866397,15.6561837167021));
#58453=CARTESIAN_POINT('Ctrl Pts',(0.0906004466968272,88.2100245227155,
16.3903065054292));
#58454=CARTESIAN_POINT('Ctrl Pts',(-1.84527490172218,88.4483881006452,15.8199763539294));
#58455=CARTESIAN_POINT('Ctrl Pts',(-3.03210479229587,88.6890923611134,14.1632366172487));
#58456=CARTESIAN_POINT('Ctrl Pts',(-2.94671407717725,88.9319386868365,12.1085221950291));
#58457=CARTESIAN_POINT('Ctrl Pts',(-2.05300399269063,89.0951216748638,11.055933862054));
#58458=CARTESIAN_POINT('Ctrl Pts',(-1.48838334446287,89.1769935708843,10.7219340123104));
#58459=CARTESIAN_POINT('Ctrl Pts',(0.0598359433255453,78.2777035969321,
10.8007161366229));
#58460=CARTESIAN_POINT('Ctrl Pts',(0.61036568547357,78.3465065363623,10.8320560766263));
#58461=CARTESIAN_POINT('Ctrl Pts',(1.67520506789003,78.4826311574234,11.2715159129288));
#58462=CARTESIAN_POINT('Ctrl Pts',(2.51270228435107,78.6824204965308,12.7416970649818));
#58463=CARTESIAN_POINT('Ctrl Pts',(2.2746856476672,78.877886670843,14.3796271383859));
#58464=CARTESIAN_POINT('Ctrl Pts',(1.10609294942053,79.0691335487028,15.5006053013841));
#58465=CARTESIAN_POINT('Ctrl Pts',(-0.46992934360028,79.256293183702,15.6639343360112));
#58466=CARTESIAN_POINT('Ctrl Pts',(-1.78661701246979,79.439525172063,14.8402919438003));
#58467=CARTESIAN_POINT('Ctrl Pts',(-2.30607982769537,79.6190149186495,13.4148446093108));
#58468=CARTESIAN_POINT('Ctrl Pts',(-1.80448938142329,79.8145253825358,11.8328849729804));
#58469=CARTESIAN_POINT('Ctrl Pts',(-0.162549663096186,80.024887286222,10.9619206019087));
#58470=CARTESIAN_POINT('Ctrl Pts',(1.66468657252576,80.2491270741339,11.7333165326405));
#58471=CARTESIAN_POINT('Ctrl Pts',(2.07288308028313,80.4093134827971,13.0854553923048));
#58472=CARTESIAN_POINT('Ctrl Pts',(1.83924717398731,80.5361321345376,14.0787868956542));
#58473=CARTESIAN_POINT('Ctrl Pts',(1.36829110285259,80.6441456547589,14.8371694551268));
#58474=CARTESIAN_POINT('Ctrl Pts',(0.236475891784066,80.7911998688987,15.3581021860063));
#58475=CARTESIAN_POINT('Ctrl Pts',(-1.07389504583177,80.9501379494364,15.0501745481337));
#58476=CARTESIAN_POINT('Ctrl Pts',(-1.91268532215848,81.1079401617502,14.009469332259));
#58477=CARTESIAN_POINT('Ctrl Pts',(-1.93437406696,81.2649642368032,12.6797359153453));
#58478=CARTESIAN_POINT('Ctrl Pts',(-1.13649349982583,81.4215708409309,11.6197540031912));
#58479=CARTESIAN_POINT('Ctrl Pts',(-0.0689033938766367,81.5520358946408,
11.3330499844046));
#58480=CARTESIAN_POINT('Ctrl Pts',(0.755733067294288,81.6565620288498,11.53254564374));
#58481=CARTESIAN_POINT('Ctrl Pts',(1.59928354069709,81.7787067951883,12.0608813198208));
#58482=CARTESIAN_POINT('Ctrl Pts',(2.04722045099659,81.9100919131365,13.1244646117146));
#58483=CARTESIAN_POINT('Ctrl Pts',(1.70156302326592,82.0689085962994,14.3877668341146));
#58484=CARTESIAN_POINT('Ctrl Pts',(0.82925920403554,82.2111065890273,15.2125302707812));
#58485=CARTESIAN_POINT('Ctrl Pts',(-0.53589821961958,82.3728133810471,15.3408591914028));
#58486=CARTESIAN_POINT('Ctrl Pts',(-1.70525890524636,82.536581026265,14.5910318503777));
#58487=CARTESIAN_POINT('Ctrl Pts',(-2.11622518699259,82.6842676061882,13.4138884459793));
#58488=CARTESIAN_POINT('Ctrl Pts',(-1.8248120357861,82.8526454048811,12.0568300431165));
#58489=CARTESIAN_POINT('Ctrl Pts',(-0.67125200520654,83.0238960206773,11.0904628857288));
#58490=CARTESIAN_POINT('Ctrl Pts',(0.978505825826656,83.2183600999162,11.2250850263446));
#58491=CARTESIAN_POINT('Ctrl Pts',(2.0895205197463,83.3968410520288,12.245561624151));
#58492=CARTESIAN_POINT('Ctrl Pts',(2.34503071961963,83.5790118234125,13.768328687951));
#58493=CARTESIAN_POINT('Ctrl Pts',(1.59224935085791,83.7650582286018,15.1527697922569));
#58494=CARTESIAN_POINT('Ctrl Pts',(0.115842272596848,83.9551500258546,15.7946677104839));
#58495=CARTESIAN_POINT('Ctrl Pts',(-1.47695346482901,84.1494289716277,15.3827260087051));
#58496=CARTESIAN_POINT('Ctrl Pts',(-2.50135675924282,84.3480038031027,14.0480622320009));
#58497=CARTESIAN_POINT('Ctrl Pts',(-2.48670775032206,84.528407980209,12.5210444921729));
#58498=CARTESIAN_POINT('Ctrl Pts',(-1.88011090799667,84.6661740916134,11.5647890581236));
#58499=CARTESIAN_POINT('Ctrl Pts',(-1.29558042042781,84.7590068930878,11.0974807108149));
#58500=CARTESIAN_POINT('Ctrl Pts',(-0.618132897281633,84.8524996450391,
10.7665386000152));
#58501=CARTESIAN_POINT('Ctrl Pts',(0.344445064487824,84.9706032923835,10.6469957415602));
#58502=CARTESIAN_POINT('Ctrl Pts',(1.46507484832016,85.1143049980667,11.0164379876078));
#58503=CARTESIAN_POINT('Ctrl Pts',(2.18794703957648,85.2356963913422,11.7039616995813));
#58504=CARTESIAN_POINT('Ctrl Pts',(2.54939020286947,85.3337851290867,12.4068938597097));
#58505=CARTESIAN_POINT('Ctrl Pts',(2.85933044982833,85.481890215048,13.5611648340663));
#58506=CARTESIAN_POINT('Ctrl Pts',(2.28717729441986,85.7076710471716,15.4691227122269));
#58507=CARTESIAN_POINT('Ctrl Pts',(-0.228861613513224,86.0162071665075,
16.5240549133912));
#58508=CARTESIAN_POINT('Ctrl Pts',(-2.69662259943057,86.3319091996579,15.2106403101332));
#58509=CARTESIAN_POINT('Ctrl Pts',(-3.18826275994563,86.6185375291251,12.7310175727665));
#58510=CARTESIAN_POINT('Ctrl Pts',(-2.08043654605037,86.8733937365941,10.9018071818394));
#58511=CARTESIAN_POINT('Ctrl Pts',(-0.409459479142451,87.0944585482347,
10.115336118756));
#58512=CARTESIAN_POINT('Ctrl Pts',(1.52023432110892,87.3272719604151,10.403028029936));
#58513=CARTESIAN_POINT('Ctrl Pts',(3.00056130000496,87.5719843602378,11.8512116700728));
#58514=CARTESIAN_POINT('Ctrl Pts',(3.28966030862267,87.8286568580416,14.0059248450504));
#58515=CARTESIAN_POINT('Ctrl Pts',(2.18191538621251,88.0875700058385,15.8976507755124));
#58516=CARTESIAN_POINT('Ctrl Pts',(0.129516644537648,88.3484078961716,16.7134615363008));
#58517=CARTESIAN_POINT('Ctrl Pts',(-2.00300240359594,88.6108255993947,16.0895170177145));
#58518=CARTESIAN_POINT('Ctrl Pts',(-3.30645749659806,88.8744780284728,14.2771563047898));
#58519=CARTESIAN_POINT('Ctrl Pts',(-3.21769992053326,89.1390142435408,12.038666318987));
#58520=CARTESIAN_POINT('Ctrl Pts',(-2.2521224045997,89.3157207771843,10.896866852668));
#58521=CARTESIAN_POINT('Ctrl Pts',(-1.64370936582915,89.4040960880525,10.5344619404795));
#58522=CARTESIAN_POINT('Ctrl Pts',(0.0622069118415443,78.2779999202659,
10.8008522795397));
#58523=CARTESIAN_POINT('Ctrl Pts',(0.611894146152642,78.3467019602469,10.8326872595339));
#58524=CARTESIAN_POINT('Ctrl Pts',(1.67560584825159,78.4827267656738,11.2722194612178));
#58525=CARTESIAN_POINT('Ctrl Pts',(2.51270228435107,78.6824204965308,12.7416970649818));
#58526=CARTESIAN_POINT('Ctrl Pts',(2.2746856476672,78.877886670843,14.3796271383859));
#58527=CARTESIAN_POINT('Ctrl Pts',(1.10609294942053,79.0691335487028,15.5006053013841));
#58528=CARTESIAN_POINT('Ctrl Pts',(-0.46992934360028,79.256293183702,15.6639343360112));
#58529=CARTESIAN_POINT('Ctrl Pts',(-1.78661701246979,79.439525172063,14.8402919438003));
#58530=CARTESIAN_POINT('Ctrl Pts',(-2.30607982769537,79.6190149186495,13.4148446093108));
#58531=CARTESIAN_POINT('Ctrl Pts',(-1.80448938142329,79.8145253825358,11.8328849729804));
#58532=CARTESIAN_POINT('Ctrl Pts',(-0.162549663096186,80.024887286222,10.9619206019087));
#58533=CARTESIAN_POINT('Ctrl Pts',(1.66468657252576,80.2491270741339,11.7333165326405));
#58534=CARTESIAN_POINT('Ctrl Pts',(2.07288308028313,80.4093134827971,13.0854553923048));
#58535=CARTESIAN_POINT('Ctrl Pts',(1.83924717398731,80.5361321345376,14.0787868956542));
#58536=CARTESIAN_POINT('Ctrl Pts',(1.36829110285259,80.6441456547589,14.8371694551268));
#58537=CARTESIAN_POINT('Ctrl Pts',(0.236475891784066,80.7911998688987,15.3581021860063));
#58538=CARTESIAN_POINT('Ctrl Pts',(-1.07389504583177,80.9501379494364,15.0501745481337));
#58539=CARTESIAN_POINT('Ctrl Pts',(-1.91268532215848,81.1079401617502,14.009469332259));
#58540=CARTESIAN_POINT('Ctrl Pts',(-1.93437406696,81.2649642368032,12.6797359153453));
#58541=CARTESIAN_POINT('Ctrl Pts',(-1.13649349982583,81.4215708409309,11.6197540031912));
#58542=CARTESIAN_POINT('Ctrl Pts',(-0.0689033938766367,81.5520358946408,
11.3330499844046));
#58543=CARTESIAN_POINT('Ctrl Pts',(0.755733067294288,81.6565620288498,11.53254564374));
#58544=CARTESIAN_POINT('Ctrl Pts',(1.59928354069709,81.7787067951883,12.0608813198208));
#58545=CARTESIAN_POINT('Ctrl Pts',(2.04722045099659,81.9100919131365,13.1244646117146));
#58546=CARTESIAN_POINT('Ctrl Pts',(1.70156302326592,82.0689085962994,14.3877668341146));
#58547=CARTESIAN_POINT('Ctrl Pts',(0.82925920403554,82.2111065890273,15.2125302707812));
#58548=CARTESIAN_POINT('Ctrl Pts',(-0.53589821961958,82.3728133810471,15.3408591914028));
#58549=CARTESIAN_POINT('Ctrl Pts',(-1.70525890524636,82.536581026265,14.5910318503777));
#58550=CARTESIAN_POINT('Ctrl Pts',(-2.11622518699259,82.6842676061882,13.4138884459793));
#58551=CARTESIAN_POINT('Ctrl Pts',(-1.8248120357861,82.8526454048811,12.0568300431165));
#58552=CARTESIAN_POINT('Ctrl Pts',(-0.67125200520654,83.0238960206773,11.0904628857288));
#58553=CARTESIAN_POINT('Ctrl Pts',(0.978505825826656,83.2183600999162,11.2250850263446));
#58554=CARTESIAN_POINT('Ctrl Pts',(2.0895205197463,83.3968410520288,12.245561624151));
#58555=CARTESIAN_POINT('Ctrl Pts',(2.34503071961963,83.5790118234125,13.768328687951));
#58556=CARTESIAN_POINT('Ctrl Pts',(1.59224935085791,83.7650582286018,15.1527697922569));
#58557=CARTESIAN_POINT('Ctrl Pts',(0.115842272596848,83.9551500258546,15.7946677104839));
#58558=CARTESIAN_POINT('Ctrl Pts',(-1.47695346482901,84.1494289716277,15.3827260087051));
#58559=CARTESIAN_POINT('Ctrl Pts',(-2.50135675924282,84.3480038031027,14.0480622320009));
#58560=CARTESIAN_POINT('Ctrl Pts',(-2.48835484466458,84.5081238298553,12.6927381742385));
#58561=CARTESIAN_POINT('Ctrl Pts',(-2.14702439884612,84.6019727171383,12.01597911337));
#58562=CARTESIAN_POINT('Ctrl Pts',(-2.03459967169508,84.6272597203354,11.8472323735682));
#58563=CARTESIAN_POINT('Ctrl Pts',(1.62567980018093,93.7945759308532,10.4657523090101));
#58564=CARTESIAN_POINT('Ctrl Pts',(2.26361473188923,93.8863901894122,10.832065737273));
#58565=CARTESIAN_POINT('Ctrl Pts',(3.2658443372097,94.0678999317249,12.0003103131008));
#58566=CARTESIAN_POINT('Ctrl Pts',(3.35691835987926,94.338517066757,14.2896228282011));
#58567=CARTESIAN_POINT('Ctrl Pts',(2.03466811379621,94.6061000245314,16.1290171211605));
#58568=CARTESIAN_POINT('Ctrl Pts',(-0.127985735322314,94.8723118052565,
16.7623211593336));
#58569=CARTESIAN_POINT('Ctrl Pts',(-2.20934172455679,95.1367830226765,15.9374225661859));
#58570=CARTESIAN_POINT('Ctrl Pts',(-3.33304091563268,95.3991528151441,14.0199424862732));
#58571=CARTESIAN_POINT('Ctrl Pts',(-3.04384750747191,95.6590737429842,11.8424470121058));
#58572=CARTESIAN_POINT('Ctrl Pts',(-1.3167115394671,95.9447928973861,10.1387096135308));
#58573=CARTESIAN_POINT('Ctrl Pts',(0.914025025367711,96.1983215575206,10.1341696855316));
#58574=CARTESIAN_POINT('Ctrl Pts',(2.35325644232377,96.4206034690197,11.259890544272));
#58575=CARTESIAN_POINT('Ctrl Pts',(3.1822047885405,96.640723635659,12.8669508643349));
#58576=CARTESIAN_POINT('Ctrl Pts',(2.72392992072032,96.911636589393,15.2118032510287));
#58577=CARTESIAN_POINT('Ctrl Pts',(0.249363689211224,97.2294224043132,16.5493006915505));
#58578=CARTESIAN_POINT('Ctrl Pts',(-2.28232071173272,97.5394610680848,15.4944322266632));
#58579=CARTESIAN_POINT('Ctrl Pts',(-2.9911795578159,97.8162518841324,13.1596802537136));
#58580=CARTESIAN_POINT('Ctrl Pts',(-2.03593613645396,98.0617968089958,11.3100136953354));
#58581=CARTESIAN_POINT('Ctrl Pts',(-0.378017756006219,98.278031770538,10.5386546999244));
#58582=CARTESIAN_POINT('Ctrl Pts',(1.36543463028554,98.4894735789785,10.9445531049755));
#58583=CARTESIAN_POINT('Ctrl Pts',(2.46579833874375,98.696118620997,12.3037545886731));
#58584=CARTESIAN_POINT('Ctrl Pts',(2.49752216123743,98.8979956906054,14.0123482012642));
#58585=CARTESIAN_POINT('Ctrl Pts',(1.49556695346512,99.0951648208613,15.3473452032655));
#58586=CARTESIAN_POINT('Ctrl Pts',(-0.077661314976231,99.2877179951242,
15.7740783614512));
#58587=CARTESIAN_POINT('Ctrl Pts',(-1.54584306935538,99.4757795604173,15.1581600696454));
#58588=CARTESIAN_POINT('Ctrl Pts',(-2.30721550472451,99.6595021625455,13.8018948294568));
#58589=CARTESIAN_POINT('Ctrl Pts',(-2.0792914703476,99.8390693946257,12.2989815972528));
#58590=CARTESIAN_POINT('Ctrl Pts',(-1.0000027499426,100.014689084747,11.2767295564262));
#58591=CARTESIAN_POINT('Ctrl Pts',(0.448470956356669,100.18660318479,11.1369560862804));
#58592=CARTESIAN_POINT('Ctrl Pts',(1.6519323745928,100.355071356998,11.9015096877094));
#58593=CARTESIAN_POINT('Ctrl Pts',(2.12414762484912,100.520379107224,13.2186356429174));
#58594=CARTESIAN_POINT('Ctrl Pts',(1.69158115151593,100.682831846705,14.5246426040201));
#58595=CARTESIAN_POINT('Ctrl Pts',(0.567850360925065,100.842758317436,15.2777758714163));
#58596=CARTESIAN_POINT('Ctrl Pts',(-0.766897362161647,101.000495068412,
15.1812500512025));
#58597=CARTESIAN_POINT('Ctrl Pts',(-1.63301226775241,101.139083491954,14.3962551082184));
#58598=CARTESIAN_POINT('Ctrl Pts',(-1.99790763286353,101.29378375243,13.1740789195566));
#58599=CARTESIAN_POINT('Ctrl Pts',(-1.50166663647508,101.447270514397,11.9203648333942));
#58600=CARTESIAN_POINT('Ctrl Pts',(-0.183210996391025,101.616923102518,
11.3342112094097));
#58601=CARTESIAN_POINT('Ctrl Pts',(1.06606422218322,101.769308904291,11.6402003542304));
#58602=CARTESIAN_POINT('Ctrl Pts',(1.86759638968297,101.921786212033,12.6534070722283));
#58603=CARTESIAN_POINT('Ctrl Pts',(1.87476424258217,102.07475394688,13.94808787474));
#58604=CARTESIAN_POINT('Ctrl Pts',(1.08122962577802,102.228598071457,14.9803147482856));
#58605=CARTESIAN_POINT('Ctrl Pts',(-0.191662859422608,102.383699978547,
15.3087123354403));
#58606=CARTESIAN_POINT('Ctrl Pts',(-1.40653911672816,102.54044013001,14.7803154183345));
#58607=CARTESIAN_POINT('Ctrl Pts',(-2.12819221058885,102.71681720939,13.4692876035973));
#58608=CARTESIAN_POINT('Ctrl Pts',(-1.65992697799525,102.914185604843,11.7906537263468));
#58609=CARTESIAN_POINT('Ctrl Pts',(0.125034229719186,103.134459810349,11.0065966617667));
#58610=CARTESIAN_POINT('Ctrl Pts',(1.75438201985768,103.341615287336,11.8326420188669));
#58611=CARTESIAN_POINT('Ctrl Pts',(2.27797020089514,103.534559255831,13.3831006340595));
#58612=CARTESIAN_POINT('Ctrl Pts',(1.78571770818503,103.712037241146,14.8005586192802));
#58613=CARTESIAN_POINT('Ctrl Pts',(0.494270562277235,103.893566032069,15.6353564465742));
#58614=CARTESIAN_POINT('Ctrl Pts',(-1.07234386693872,104.079339269911,15.4951771393443));
#58615=CARTESIAN_POINT('Ctrl Pts',(-2.24884450357346,104.269528147654,14.3956742992569));
#58616=CARTESIAN_POINT('Ctrl Pts',(-2.50597583289488,104.464274125644,12.7669262238946));
#58617=CARTESIAN_POINT('Ctrl Pts',(-1.68681015579904,104.663681949589,11.2904932986803));
#58618=CARTESIAN_POINT('Ctrl Pts',(-0.627211848440459,104.799780780842,
10.840195813604));
#58619=CARTESIAN_POINT('Ctrl Pts',(-0.0768417822340009,104.868628219523,
10.8036689183428));
#58620=CARTESIAN_POINT('Ctrl Pts',(1.46045405682495,94.0029659022257,10.6668376125859));
#58621=CARTESIAN_POINT('Ctrl Pts',(2.0507217959542,94.0876436018886,11.001428431865));
#58622=CARTESIAN_POINT('Ctrl Pts',(2.97733933924797,94.2545490062617,12.0713852943386));
#58623=CARTESIAN_POINT('Ctrl Pts',(3.070789585288,94.5020541295736,14.1648644902778));
#58624=CARTESIAN_POINT('Ctrl Pts',(1.87574246782933,94.7455856884425,15.8450121964185));
#58625=CARTESIAN_POINT('Ctrl Pts',(-0.0808875490336731,94.9867962122503,
16.4290464283818));
#58626=CARTESIAN_POINT('Ctrl Pts',(-1.96339697661919,95.2254836409508,15.6946328486544));
#58627=CARTESIAN_POINT('Ctrl Pts',(-2.98369333070791,95.4614604001256,13.9756265091926));
#58628=CARTESIAN_POINT('Ctrl Pts',(-2.73559538172536,95.6945574625247,12.0212543429719));
#58629=CARTESIAN_POINT('Ctrl Pts',(-1.19933236447556,95.9501904660232,10.4877100732131));
#58630=CARTESIAN_POINT('Ctrl Pts',(0.792576929541223,96.1765696942838,10.4715620063823));
#58631=CARTESIAN_POINT('Ctrl Pts',(2.0830646340336,96.3748674559486,11.4675188239778));
#58632=CARTESIAN_POINT('Ctrl Pts',(2.83180362082271,96.571179582596,12.8959840254328));
#58633=CARTESIAN_POINT('Ctrl Pts',(2.43734837739185,96.8127941299477,14.9900696749655));
#58634=CARTESIAN_POINT('Ctrl Pts',(0.236241808260255,97.0965847023887,16.2004855511167));
#58635=CARTESIAN_POINT('Ctrl Pts',(-2.0380656366222,97.3741979176357,15.2734889467748));
#58636=CARTESIAN_POINT('Ctrl Pts',(-2.69244372297225,97.6230498986325,13.1794400922548));
#58637=CARTESIAN_POINT('Ctrl Pts',(-1.84270351097513,97.8448918272664,11.5013006210743));
#58638=CARTESIAN_POINT('Ctrl Pts',(-0.342863154852027,98.0412412451055,
10.788621893397));
#58639=CARTESIAN_POINT('Ctrl Pts',(1.2528646694032,98.2343783206733,11.1461289618806));
#58640=CARTESIAN_POINT('Ctrl Pts',(2.2755495541587,98.4244231979741,12.3875957155746));
#58641=CARTESIAN_POINT('Ctrl Pts',(2.31869670558774,98.6115172489426,13.9709051527683));
#58642=CARTESIAN_POINT('Ctrl Pts',(1.39309287730542,98.7958183772439,15.2271343783831));
#58643=CARTESIAN_POINT('Ctrl Pts',(-0.0878663793999987,98.9775060287232,
15.6431191081459));
#58644=CARTESIAN_POINT('Ctrl Pts',(-1.4928633284236,99.1567779325714,15.0686219996598));
#58645=CARTESIAN_POINT('Ctrl Pts',(-2.23865523362967,99.33384542954,13.7680710682018));
#58646=CARTESIAN_POINT('Ctrl Pts',(-2.02981918752864,99.5089370971803,12.3004509925281));
#58647=CARTESIAN_POINT('Ctrl Pts',(-0.973603534998877,99.6822906696519,
11.2815431673196));
#58648=CARTESIAN_POINT('Ctrl Pts',(0.473392355753049,99.8541637345571,11.1286001848778));
#58649=CARTESIAN_POINT('Ctrl Pts',(1.6995472292461,100.024815758553,11.8921649619359));
#58650=CARTESIAN_POINT('Ctrl Pts',(2.19633062747038,100.194517842491,13.2400455689458));
#58651=CARTESIAN_POINT('Ctrl Pts',(1.7580296324876,100.363545819897,14.6030409780728));
#58652=CARTESIAN_POINT('Ctrl Pts',(0.579731615323981,100.532184012228,15.4072839311937));
#58653=CARTESIAN_POINT('Ctrl Pts',(-0.847450930810139,100.700711000255,
15.3160247299797));
#58654=CARTESIAN_POINT('Ctrl Pts',(-1.79134987561612,100.850673253478,14.4736763066588));
#58655=CARTESIAN_POINT('Ctrl Pts',(-2.19937715193843,101.019766916766,13.1405706996597));
#58656=CARTESIAN_POINT('Ctrl Pts',(-1.66218454769459,101.189504468116,11.7493907868574));
#58657=CARTESIAN_POINT('Ctrl Pts',(-0.190544567415407,101.379427278415,
11.0823963921818));
#58658=CARTESIAN_POINT('Ctrl Pts',(1.22377517797031,101.551642707134,11.4192058409893));
#58659=CARTESIAN_POINT('Ctrl Pts',(2.14439907420247,101.725403514285,12.5682324039414));
#58660=CARTESIAN_POINT('Ctrl Pts',(2.16126111529323,101.900962890033,14.0542982782834));
#58661=CARTESIAN_POINT('Ctrl Pts',(1.25160786092212,102.078556211253,15.2509714585909));
#58662=CARTESIAN_POINT('Ctrl Pts',(-0.222627569799362,102.258406121726,
15.639321465208));
#58663=CARTESIAN_POINT('Ctrl Pts',(-1.63877585618237,102.440724413414,15.0313321790294));
#58664=CARTESIAN_POINT('Ctrl Pts',(-2.48666797944368,102.646253989519,13.5072005727598));
#58665=CARTESIAN_POINT('Ctrl Pts',(-1.94851042751775,102.876377989224,11.5474888158579));
#58666=CARTESIAN_POINT('Ctrl Pts',(0.126561907913205,103.132819912367,10.6273830725664));
#58667=CARTESIAN_POINT('Ctrl Pts',(2.01968962832455,103.373117655503,11.5798462181864));
#58668=CARTESIAN_POINT('Ctrl Pts',(2.63002557592199,103.595883122873,13.368059706764));
#58669=CARTESIAN_POINT('Ctrl Pts',(2.06965165021159,103.799773192147,14.9983479377696));
#58670=CARTESIAN_POINT('Ctrl Pts',(0.597346362413307,104.007110012382,15.9563763703115));
#58671=CARTESIAN_POINT('Ctrl Pts',(-1.1809445934538,104.217917207411,15.8025070400524));
#58672=CARTESIAN_POINT('Ctrl Pts',(-2.51010932623597,104.432195681752,14.5674651013056));
#58673=CARTESIAN_POINT('Ctrl Pts',(-2.80272521150328,104.649922000431,12.7471845670932));
#58674=CARTESIAN_POINT('Ctrl Pts',(-1.89885716503994,104.871050085879,11.1073396892158));
#58675=CARTESIAN_POINT('Ctrl Pts',(-0.735145083543213,105.020692283243,
10.6089271762419));
#58676=CARTESIAN_POINT('Ctrl Pts',(-0.132850003595063,105.096052450379,
10.566386044137));
#58677=CARTESIAN_POINT('Ctrl Pts',(1.29522831346895,94.2113558735981,10.8679229161619));
#58678=CARTESIAN_POINT('Ctrl Pts',(1.83782886001918,94.2888970143649,11.1707911264571));
#58679=CARTESIAN_POINT('Ctrl Pts',(2.68883434128623,94.4411980807984,12.1424602755765));
#58680=CARTESIAN_POINT('Ctrl Pts',(2.78466081069676,94.6655911923902,14.0401061523546));
#58681=CARTESIAN_POINT('Ctrl Pts',(1.71681682186247,94.8850713523536,15.5610072716766));
#58682=CARTESIAN_POINT('Ctrl Pts',(-0.0337893627450391,95.101280619244,
16.0957716974301));
#58683=CARTESIAN_POINT('Ctrl Pts',(-1.71745222868159,95.3141842592252,15.4518431311229));
#58684=CARTESIAN_POINT('Ctrl Pts',(-2.63434574578315,95.5237679851071,13.931310532112));
#58685=CARTESIAN_POINT('Ctrl Pts',(-2.42734325597883,95.7300411820652,12.2000616738379));
#58686=CARTESIAN_POINT('Ctrl Pts',(-1.08195318948404,95.9555880346603,10.8367105328952));
#58687=CARTESIAN_POINT('Ctrl Pts',(0.671128833714733,96.1548178310472,10.8089543272328));
#58688=CARTESIAN_POINT('Ctrl Pts',(1.81287282574344,96.3291314428775,11.6751471036834));
#58689=CARTESIAN_POINT('Ctrl Pts',(2.48140245310491,96.501635529533,12.9250171865306));
#58690=CARTESIAN_POINT('Ctrl Pts',(2.15076683406338,96.7139516705026,14.7683360989023));
#58691=CARTESIAN_POINT('Ctrl Pts',(0.223119927309282,96.9637470004642,15.8516704106827));
#58692=CARTESIAN_POINT('Ctrl Pts',(-1.7938105615117,97.2089347671866,15.0525456668865));
#58693=CARTESIAN_POINT('Ctrl Pts',(-2.39370788812863,97.4298479131326,13.1991999307961));
#58694=CARTESIAN_POINT('Ctrl Pts',(-1.64947088549632,97.627986845537,11.692587546813));
#58695=CARTESIAN_POINT('Ctrl Pts',(-0.307708553697835,97.8044507196731,
11.0385890868694));
#58696=CARTESIAN_POINT('Ctrl Pts',(1.14029470852087,97.9792830623682,11.3477048187857));
#58697=CARTESIAN_POINT('Ctrl Pts',(2.08530076957367,98.1527277749512,12.4714368424759));
#58698=CARTESIAN_POINT('Ctrl Pts',(2.13987124993805,98.3250388072801,13.9294621042721));
#58699=CARTESIAN_POINT('Ctrl Pts',(1.29061880114571,98.4964719336266,15.1069235535006));
#58700=CARTESIAN_POINT('Ctrl Pts',(-0.0980714438237656,98.6672940623222,
15.5121598548408));
#58701=CARTESIAN_POINT('Ctrl Pts',(-1.43988358749184,98.8377763047257,14.9790839296742));
#58702=CARTESIAN_POINT('Ctrl Pts',(-2.17009496253482,99.0081886965343,13.7342473069468));
#58703=CARTESIAN_POINT('Ctrl Pts',(-1.98034690470969,99.178804799735,12.3019203878032));
#58704=CARTESIAN_POINT('Ctrl Pts',(-0.947204320055155,99.3498922545572,
11.2863567782128));
#58705=CARTESIAN_POINT('Ctrl Pts',(0.498313755149421,99.5217242843239,11.1202442834754));
#58706=CARTESIAN_POINT('Ctrl Pts',(1.74716208389938,99.6945601601093,11.8828202361623));
#58707=CARTESIAN_POINT('Ctrl Pts',(2.26851363009162,99.8686565777578,13.261455494974));
#58708=CARTESIAN_POINT('Ctrl Pts',(1.82447811345925,100.04425979309,14.6814393521253));
#58709=CARTESIAN_POINT('Ctrl Pts',(0.591612869722885,100.221609707021,15.5367919909709));
#58710=CARTESIAN_POINT('Ctrl Pts',(-0.928004499458635,100.400926932099,
15.4507994087571));
#58711=CARTESIAN_POINT('Ctrl Pts',(-1.94968748347984,100.562263015001,14.5510975050992));
#58712=CARTESIAN_POINT('Ctrl Pts',(-2.40084667101332,100.745750081104,13.1070624797628));
#58713=CARTESIAN_POINT('Ctrl Pts',(-1.82270245891412,100.931738421836,11.5784167403206));
#58714=CARTESIAN_POINT('Ctrl Pts',(-0.197878138439787,101.141931454312,
10.830581574954));
#58715=CARTESIAN_POINT('Ctrl Pts',(1.38148613375741,101.333976509975,11.1982113277482));
#58716=CARTESIAN_POINT('Ctrl Pts',(2.42120175872198,101.529020816538,12.4830577356546));
#58717=CARTESIAN_POINT('Ctrl Pts',(2.44775798800427,101.727171833185,14.1605086818266));
#58718=CARTESIAN_POINT('Ctrl Pts',(1.42198609606622,101.928514351047,15.5216281688963));
#58719=CARTESIAN_POINT('Ctrl Pts',(-0.253592280176116,102.133112264904,
15.9699305949757));
#58720=CARTESIAN_POINT('Ctrl Pts',(-1.87101259563657,102.34100869682,15.2823489397244));
#58721=CARTESIAN_POINT('Ctrl Pts',(-2.84514374829853,102.575690769647,13.5451135419222));
#58722=CARTESIAN_POINT('Ctrl Pts',(-2.23709387704024,102.838570373607,11.304323905369));
#58723=CARTESIAN_POINT('Ctrl Pts',(0.128089586107228,103.131180014383,10.248169483366));
#58724=CARTESIAN_POINT('Ctrl Pts',(2.28499723679145,103.404620023671,11.3270504175059));
#58725=CARTESIAN_POINT('Ctrl Pts',(2.98208095094885,103.657206989915,13.3530187794686));
#58726=CARTESIAN_POINT('Ctrl Pts',(2.35358559223816,103.887509143148,15.196137256259));
#58727=CARTESIAN_POINT('Ctrl Pts',(0.700422162549388,104.120653992695,16.2773962940487));
#58728=CARTESIAN_POINT('Ctrl Pts',(-1.28954531996889,104.35649514491,16.1098369407604));
#58729=CARTESIAN_POINT('Ctrl Pts',(-2.77137414889849,104.594863215849,14.7392559033545));
#58730=CARTESIAN_POINT('Ctrl Pts',(-3.09947459011168,104.835569875216,12.7274429102918));
#58731=CARTESIAN_POINT('Ctrl Pts',(-2.11090417428086,105.078418222169,10.924186079751));
#58732=CARTESIAN_POINT('Ctrl Pts',(-0.843078318645966,105.241603785644,
10.3776585388797));
#58733=CARTESIAN_POINT('Ctrl Pts',(-0.188858224956125,105.323476681233,
10.3291031699311));
#58734=CARTESIAN_POINT('Ctrl Pts',(1.13000257011297,94.4197458449706,11.0690082197377));
#58735=CARTESIAN_POINT('Ctrl Pts',(1.62493592408414,94.4901504268412,11.3401538210491));
#58736=CARTESIAN_POINT('Ctrl Pts',(2.40032934332449,94.6278471553352,12.2135352568143));
#58737=CARTESIAN_POINT('Ctrl Pts',(2.49853203610551,94.8291282552068,13.9153478144313));
#58738=CARTESIAN_POINT('Ctrl Pts',(1.5578911758956,95.0245570162647,15.2770023469347));
#58739=CARTESIAN_POINT('Ctrl Pts',(0.0133088235436025,95.2157650262378,
15.7624969664783));
#58740=CARTESIAN_POINT('Ctrl Pts',(-1.47150748074399,95.4028848774996,15.2090534135915));
#58741=CARTESIAN_POINT('Ctrl Pts',(-2.28499816085838,95.5860755700886,13.8869945550315));
#58742=CARTESIAN_POINT('Ctrl Pts',(-2.11909113023227,95.7655249016057,12.3788690047039));
#58743=CARTESIAN_POINT('Ctrl Pts',(-0.964574014492501,95.9609856032976,
11.1857109925774));
#58744=CARTESIAN_POINT('Ctrl Pts',(0.549680737888245,96.1330659678105,11.1463466480834));
#58745=CARTESIAN_POINT('Ctrl Pts',(1.54268101745328,96.2833954298063,11.8827753833891));
#58746=CARTESIAN_POINT('Ctrl Pts',(2.13100128538712,96.43209147647,12.9540503476284));
#58747=CARTESIAN_POINT('Ctrl Pts',(1.86418529073491,96.6151092110574,14.5466025228392));
#58748=CARTESIAN_POINT('Ctrl Pts',(0.209998046358312,96.8309092985398,15.5028552702488));
#58749=CARTESIAN_POINT('Ctrl Pts',(-1.54955548640118,97.0436716167375,14.8316023869983));
#58750=CARTESIAN_POINT('Ctrl Pts',(-2.094972053285,97.2366459276328,13.2189597693372));
#58751=CARTESIAN_POINT('Ctrl Pts',(-1.45623826001751,97.4110818638077,11.8838744725519));
#58752=CARTESIAN_POINT('Ctrl Pts',(-0.272553952543648,97.5676601942407,
11.288556280342));
#58753=CARTESIAN_POINT('Ctrl Pts',(1.02772474763855,97.7241878040629,11.5492806756908));
#58754=CARTESIAN_POINT('Ctrl Pts',(1.89505198498861,97.8810323519284,12.5552779693774));
#58755=CARTESIAN_POINT('Ctrl Pts',(1.96104579428837,98.0385603656175,13.8880190557761));
#58756=CARTESIAN_POINT('Ctrl Pts',(1.18814472498599,98.1971254900092,14.9867127286182));
#58757=CARTESIAN_POINT('Ctrl Pts',(-0.108276508247538,98.3570820959213,
15.3812006015355));
#58758=CARTESIAN_POINT('Ctrl Pts',(-1.38690384656006,98.5187746768799,14.8895458596885));
#58759=CARTESIAN_POINT('Ctrl Pts',(-2.10153469143998,98.6825319635287,13.7004235456917));
#58760=CARTESIAN_POINT('Ctrl Pts',(-1.93087462189074,98.8486725022897,12.3033897830785));
#58761=CARTESIAN_POINT('Ctrl Pts',(-0.920805105111431,99.0174938394624,
11.291170389106));
#58762=CARTESIAN_POINT('Ctrl Pts',(0.523235154545799,99.1892848340907,11.1118883820729));
#58763=CARTESIAN_POINT('Ctrl Pts',(1.79477693855267,99.3643045616654,11.8734755103888));
#58764=CARTESIAN_POINT('Ctrl Pts',(2.34069663271289,99.542795313025,13.2828654210023));
#58765=CARTESIAN_POINT('Ctrl Pts',(1.89092659443093,99.7249737662826,14.759837726178));
#58766=CARTESIAN_POINT('Ctrl Pts',(0.603494124121801,99.9110354018131,15.6663000507482));
#58767=CARTESIAN_POINT('Ctrl Pts',(-1.00855806810713,100.101142863942,15.5855740875344));
#58768=CARTESIAN_POINT('Ctrl Pts',(-2.10802509134356,100.273852776525,14.6285187035397));
#58769=CARTESIAN_POINT('Ctrl Pts',(-2.60231619008822,100.47173324544,13.0735542598658));
#58770=CARTESIAN_POINT('Ctrl Pts',(-1.98322037013363,100.673972375556,11.4074426937837));
#58771=CARTESIAN_POINT('Ctrl Pts',(-0.20521170946417,100.904435630209,10.5787667577262));
#58772=CARTESIAN_POINT('Ctrl Pts',(1.5391970895445,101.116310312817,10.9772168145072));
#58773=CARTESIAN_POINT('Ctrl Pts',(2.6980044432415,101.332638118791,12.3978830673678));
#58774=CARTESIAN_POINT('Ctrl Pts',(2.73425486071532,101.553380776338,14.2667190853701));
#58775=CARTESIAN_POINT('Ctrl Pts',(1.59236433121031,101.778472490843,15.7922848792018));
#58776=CARTESIAN_POINT('Ctrl Pts',(-0.284556990552873,102.007818408081,
16.3005397247434));
#58777=CARTESIAN_POINT('Ctrl Pts',(-2.10324933509078,102.241292980224,15.5333657004193));
#58778=CARTESIAN_POINT('Ctrl Pts',(-3.20361951715336,102.505127549775,13.5830265110847));
#58779=CARTESIAN_POINT('Ctrl Pts',(-2.52567732656274,102.800762757988,11.0611589948802));
#58780=CARTESIAN_POINT('Ctrl Pts',(0.129617264301245,103.1295401164,9.86895589416567));
#58781=CARTESIAN_POINT('Ctrl Pts',(2.55030484525832,103.436122391839,11.0742546168255));
#58782=CARTESIAN_POINT('Ctrl Pts',(3.33413632597569,103.718530856956,13.3379778521731));
#58783=CARTESIAN_POINT('Ctrl Pts',(2.63751953426473,103.975245094149,15.3939265747484));
#58784=CARTESIAN_POINT('Ctrl Pts',(0.80349796268546,104.234197973009,16.5984162177859));
#58785=CARTESIAN_POINT('Ctrl Pts',(-1.39814604648398,104.495073082409,16.4171668414684));
#58786=CARTESIAN_POINT('Ctrl Pts',(-3.03263897156099,104.757530749947,14.9110467054031));
#58787=CARTESIAN_POINT('Ctrl Pts',(-3.39622396872007,105.021217750003,12.7077012534903));
#58788=CARTESIAN_POINT('Ctrl Pts',(-2.32295118352176,105.285786358458,10.7410324702864));
#58789=CARTESIAN_POINT('Ctrl Pts',(-0.95101155374872,105.462515288045,10.1463899015177));
#58790=CARTESIAN_POINT('Ctrl Pts',(-0.244866446317187,105.550900912088,
10.0918202957253));
#58791=CARTESIAN_POINT('Ctrl Pts',(1.16384208806484,94.4245814674342,11.0879031093561));
#58792=CARTESIAN_POINT('Ctrl Pts',(1.23813215647139,94.4352463283717,11.1301721956053));
#58793=CARTESIAN_POINT('Ctrl Pts',(1.31008885895312,94.4457986760407,11.1762110026006));
#58794=CARTESIAN_POINT('Ctrl Pts',(1.37937803304691,94.4563120296253,11.2257287620783));
#58795=CARTESIAN_POINT('Ctrl Pts',(1.47675945485785,94.4710878634184,11.295322748237));
#58796=CARTESIAN_POINT('Ctrl Pts',(1.56873439650927,94.4859593709836,11.3719505355548));
#58797=CARTESIAN_POINT('Ctrl Pts',(1.65461838219203,94.5008636490935,11.4545758551863));
#58798=CARTESIAN_POINT('Ctrl Pts',(1.69880566651519,94.5085318956151,11.4970865568244));
#58799=CARTESIAN_POINT('Ctrl Pts',(1.74138093416847,94.516208907082,11.5411856574171));
#58800=CARTESIAN_POINT('Ctrl Pts',(1.78225213749528,94.523886700208,11.5867372413334));
#58801=CARTESIAN_POINT('Ctrl Pts',(1.87499141089662,94.5413080848963,11.6900965860755));
#58802=CARTESIAN_POINT('Ctrl Pts',(1.95901578318207,94.5586789124716,11.800897393771));
#58803=CARTESIAN_POINT('Ctrl Pts',(2.03310732138691,94.5759505358216,11.9175028031254));
#58804=CARTESIAN_POINT('Ctrl Pts',(2.05408670808245,94.5808410816775,11.9505202033969));
#58805=CARTESIAN_POINT('Ctrl Pts',(2.07427003233056,94.5857237047095,11.9840029970195));
#58806=CARTESIAN_POINT('Ctrl Pts',(2.09363039773066,94.5905973746505,12.0179141059386));
#58807=CARTESIAN_POINT('Ctrl Pts',(2.13785525671972,94.6017302929322,12.0953772105399));
#58808=CARTESIAN_POINT('Ctrl Pts',(2.17774383806482,94.6128420071046,12.1750806358068));
#58809=CARTESIAN_POINT('Ctrl Pts',(2.21305797123479,94.6238554462755,12.2565231937073));
#58810=CARTESIAN_POINT('Ctrl Pts',(2.21806675245765,94.6254175377773,12.2680746015471));
#58811=CARTESIAN_POINT('Ctrl Pts',(2.22298357177946,94.626977661633,12.279661053157));
#58812=CARTESIAN_POINT('Ctrl Pts',(2.22780781029263,94.6285356072505,12.291281177885));
#58813=CARTESIAN_POINT('Ctrl Pts',(2.22781672452381,94.6285384860235,12.2913026495593));
#58814=CARTESIAN_POINT('Ctrl Pts',(2.22782563843889,94.628541364789,12.2913241213486));
#58815=CARTESIAN_POINT('Ctrl Pts',(2.22783455203788,94.6285442435471,12.2913455932529));
#58816=CARTESIAN_POINT('Ctrl Pts',(2.25606866780065,94.6376628037731,12.3593585509574));
#58817=CARTESIAN_POINT('Ctrl Pts',(2.28116408671351,94.646702650814,12.4285673202461));
#58818=CARTESIAN_POINT('Ctrl Pts',(2.3029763109095,94.6557602078268,12.498685150674));
#58819=CARTESIAN_POINT('Ctrl Pts',(2.3069888938594,94.657426438584,12.5115840466477));
#58820=CARTESIAN_POINT('Ctrl Pts',(2.31089034671451,94.6590932511501,12.5245135672308));
#58821=CARTESIAN_POINT('Ctrl Pts',(2.31467974696626,94.6607612220338,12.5374717373018));
#58822=CARTESIAN_POINT('Ctrl Pts',(2.34630435602342,94.6746813475441,12.6456147244154));
#58823=CARTESIAN_POINT('Ctrl Pts',(2.37012813215105,94.6886884184708,12.7557741957835));
#58824=CARTESIAN_POINT('Ctrl Pts',(2.38624240054443,94.7027315140537,12.8668639407928));
#58825=CARTESIAN_POINT('Ctrl Pts',(2.39057752180477,94.7065094405929,12.8967497229854));
#58826=CARTESIAN_POINT('Ctrl Pts',(2.39435456023409,94.7102900039376,12.92670309968));
#58827=CARTESIAN_POINT('Ctrl Pts',(2.39757499657033,94.7140722783207,12.9567034872774));
#58828=CARTESIAN_POINT('Ctrl Pts',(2.4093599590983,94.7279132480597,13.0664878167119));
#58829=CARTESIAN_POINT('Ctrl Pts',(2.41369253775473,94.7417753550302,13.1768991709058));
#58830=CARTESIAN_POINT('Ctrl Pts',(2.41066283041136,94.7555907348959,13.2868736416682));
#58831=CARTESIAN_POINT('Ctrl Pts',(2.4097227836513,94.7598773215559,13.3209961271803));
#58832=CARTESIAN_POINT('Ctrl Pts',(2.40807401512869,94.7641594609854,13.3550769239517));
#58833=CARTESIAN_POINT('Ctrl Pts',(2.4057192750869,94.7684352653559,13.3890852664348));
#58834=CARTESIAN_POINT('Ctrl Pts',(2.39877851539224,94.7810384954836,13.4893272161194));
#58835=CARTESIAN_POINT('Ctrl Pts',(2.38570406559735,94.7935850145768,13.5889366944001));
#58836=CARTESIAN_POINT('Ctrl Pts',(2.36658259508796,94.806021906971,13.6870815142501));
#58837=CARTESIAN_POINT('Ctrl Pts',(2.35890433225087,94.811015964757,13.7264917532553));
#58838=CARTESIAN_POINT('Ctrl Pts',(2.35025130319088,94.8159924040279,13.7656663340367));
#58839=CARTESIAN_POINT('Ctrl Pts',(2.3406300562542,94.820948033628,13.804553552828));
#58840=CARTESIAN_POINT('Ctrl Pts',(2.33595811646162,94.8233544164263,13.823436629636));
#58841=CARTESIAN_POINT('Ctrl Pts',(2.33105789241856,94.8257558948871,13.8422516379537));
#58842=CARTESIAN_POINT('Ctrl Pts',(2.32593019905366,94.8281521250499,13.8609924524362));
#58843=CARTESIAN_POINT('Ctrl Pts',(2.32592747042772,94.8281534001682,13.8610024250826));
#58844=CARTESIAN_POINT('Ctrl Pts',(2.32592474173736,94.8281546752851,13.861012397708));
#58845=CARTESIAN_POINT('Ctrl Pts',(2.3259220129826,94.8281559504004,13.8610223703123));
#58846=CARTESIAN_POINT('Ctrl Pts',(2.30640662585915,94.8372752637657,13.9323439991563));
#58847=CARTESIAN_POINT('Ctrl Pts',(2.28357429399887,94.8463285543566,14.0026707706559));
#58848=CARTESIAN_POINT('Ctrl Pts',(2.25750079135267,94.8553907428659,14.0716728262931));
#58849=CARTESIAN_POINT('Ctrl Pts',(2.25238156496514,94.8571699972751,14.0852205704841));
#58850=CARTESIAN_POINT('Ctrl Pts',(2.2471374808347,94.8589495754404,14.09871711323));
#58851=CARTESIAN_POINT('Ctrl Pts',(2.24176924538978,94.8607300161108,14.1121597640997));
#58852=CARTESIAN_POINT('Ctrl Pts',(2.19182633343581,94.8772941911647,14.2372222982799));
#58853=CARTESIAN_POINT('Ctrl Pts',(2.13112338733817,94.8939395864207,14.3576440009253));
#58854=CARTESIAN_POINT('Ctrl Pts',(2.06094545719024,94.9106199561259,14.4718988563154));
#58855=CARTESIAN_POINT('Ctrl Pts',(1.99338878329255,94.9266772877442,14.5818861128581));
#58856=CARTESIAN_POINT('Ctrl Pts',(1.91705169652033,94.9427659024484,14.6861574254224));
#58857=CARTESIAN_POINT('Ctrl Pts',(1.83311890325089,94.9588289800573,14.7833506824778));
#58858=CARTESIAN_POINT('Ctrl Pts',(1.76539333323301,94.9717903154893,14.8617761521847));
#58859=CARTESIAN_POINT('Ctrl Pts',(1.69272515930329,94.9847328008935,14.9355917985685));
#58860=CARTESIAN_POINT('Ctrl Pts',(1.61572928392796,94.9976709245923,15.0039820720135));
#58861=CARTESIAN_POINT('Ctrl Pts',(1.59543876744322,95.0010804736222,15.0220047773074));
#58862=CARTESIAN_POINT('Ctrl Pts',(1.57484796678736,95.0044897018255,15.0396508086428));
#58863=CARTESIAN_POINT('Ctrl Pts',(1.55396868625079,95.0078988357666,15.0569055014235));
#58864=CARTESIAN_POINT('Ctrl Pts',(1.52259624465312,95.0130212754636,15.0828317703195));
#58865=CARTESIAN_POINT('Ctrl Pts',(1.49057165165312,95.0181443089837,15.1078749106348));
#58866=CARTESIAN_POINT('Ctrl Pts',(1.45793587909852,95.0232268143161,15.1321138996865));
#58867=CARTESIAN_POINT('Ctrl Pts',(1.45791763697052,95.0232296552389,15.132127448339));
#58868=CARTESIAN_POINT('Ctrl Pts',(1.45789939464426,95.0232324961502,15.1321409967456));
#58869=CARTESIAN_POINT('Ctrl Pts',(1.4578811521197,95.0232353370497,15.1321545449063));
#58870=CARTESIAN_POINT('Ctrl Pts',(1.43842008557607,95.0262659995519,15.1466076791988));
#58871=CARTESIAN_POINT('Ctrl Pts',(1.41873355562059,95.029283362287,15.1607809782664));
#58872=CARTESIAN_POINT('Ctrl Pts',(1.3988312522153,95.0322806589062,15.1746907112598));
#58873=CARTESIAN_POINT('Ctrl Pts',(1.36186797940274,95.0378473458558,15.2005243670391));
#58874=CARTESIAN_POINT('Ctrl Pts',(1.32416532569594,95.0433419253653,15.2254478281681));
#58875=CARTESIAN_POINT('Ctrl Pts',(1.28580327176107,95.0488344411743,15.249210063907));
#58876=CARTESIAN_POINT('Ctrl Pts',(1.26889124922504,95.0512558326696,15.2596857143246));
#58877=CARTESIAN_POINT('Ctrl Pts',(1.25185174888997,95.0536767561581,15.2699357114748));
#58878=CARTESIAN_POINT('Ctrl Pts',(1.23469481319672,95.0561028952065,15.2799388433483));
#58879=CARTESIAN_POINT('Ctrl Pts',(1.16530620576252,95.0659150442419,15.3203949832498));
#58880=CARTESIAN_POINT('Ctrl Pts',(1.09396469403016,95.0758258588412,15.3568131446592));
#58881=CARTESIAN_POINT('Ctrl Pts',(1.02109112390281,95.0858125894788,15.3892182119301));
#58882=CARTESIAN_POINT('Ctrl Pts',(0.985260328694605,95.090722908812,15.4051512769229));
#58883=CARTESIAN_POINT('Ctrl Pts',(0.94905838480203,95.0956516279515,15.4201138743091));
#58884=CARTESIAN_POINT('Ctrl Pts',(0.91253120638146,95.1005963119219,15.4341069509406));
#58885=CARTESIAN_POINT('Ctrl Pts',(0.847516086524827,95.10939740839,15.4590133793509));
#58886=CARTESIAN_POINT('Ctrl Pts',(0.781473143296777,95.1182480463249,15.4808498490037));
#58887=CARTESIAN_POINT('Ctrl Pts',(0.714696263141219,95.1270909750256,15.4996974571892));
#58888=CARTESIAN_POINT('Ctrl Pts',(0.665033561349754,95.1336675585678,15.5137146311365));
#58889=CARTESIAN_POINT('Ctrl Pts',(0.614963849992617,95.1402400039355,15.5260789052132));
#58890=CARTESIAN_POINT('Ctrl Pts',(0.564589439724732,95.1467869856434,15.5368232958241));
#58891=CARTESIAN_POINT('Ctrl Pts',(0.49587615082234,95.1557174057345,15.5514791977434));
#58892=CARTESIAN_POINT('Ctrl Pts',(0.426601235300059,95.164541336616,15.5632716080919));
#58893=CARTESIAN_POINT('Ctrl Pts',(0.357024047331103,95.1733167866231,15.5719815226317));
#58894=CARTESIAN_POINT('Ctrl Pts',(0.307152376719118,95.1796068705573,15.5782246319276));
#58895=CARTESIAN_POINT('Ctrl Pts',(0.257126476871656,95.1858719188813,15.5828837608138));
#58896=CARTESIAN_POINT('Ctrl Pts',(0.207058237683818,95.1921313301595,15.5858780044571));
#58897=CARTESIAN_POINT('Ctrl Pts',(0.14577073648907,95.1997933466875,15.5895431964799));
#58898=CARTESIAN_POINT('Ctrl Pts',(0.0844266935233488,95.2074460632808,
15.5907123431602));
#58899=CARTESIAN_POINT('Ctrl Pts',(0.0232698315542606,95.2150836664526,
15.5893406044066));
#58900=CARTESIAN_POINT('Ctrl Pts',(0.00373966605249472,95.2175227002614,
15.5889025458794));
#58901=CARTESIAN_POINT('Ctrl Pts',(-0.0157812326790508,95.2199614184581,
15.5882052663386));
#58902=CARTESIAN_POINT('Ctrl Pts',(-0.0352857644478857,95.2223996749869,
15.5872510169546));
#58903=CARTESIAN_POINT('Ctrl Pts',(-0.118858048625808,95.2328470248609,
15.5831622850824));
#58904=CARTESIAN_POINT('Ctrl Pts',(-0.20212757240947,95.2432856423306,15.57435170011));
#58905=CARTESIAN_POINT('Ctrl Pts',(-0.284512201205189,95.2537010724677,
15.5610299742258));
#58906=CARTESIAN_POINT('Ctrl Pts',(-0.294743296444043,95.2549945329013,
15.5593755898065));
#58907=CARTESIAN_POINT('Ctrl Pts',(-0.304960752864069,95.2562876359942,
15.5576516980548));
#58908=CARTESIAN_POINT('Ctrl Pts',(-0.315163464674268,95.2575803542851,
15.5558587571799));
#58909=CARTESIAN_POINT('Ctrl Pts',(-0.412099633719754,95.2698624966316,
15.5388239900537));
#58910=CARTESIAN_POINT('Ctrl Pts',(-0.507699861241456,95.282109358852,15.5155569669214));
#58911=CARTESIAN_POINT('Ctrl Pts',(-0.601229851418452,95.294291541424,15.486505910759));
#58912=CARTESIAN_POINT('Ctrl Pts',(-0.616704290937099,95.29630707085,15.4816994437564));
#58913=CARTESIAN_POINT('Ctrl Pts',(-0.632122174381767,95.2983208418937,
15.4767346275083));
#58914=CARTESIAN_POINT('Ctrl Pts',(-0.647480310265967,95.3003327358378,
15.471613461004));
#58915=CARTESIAN_POINT('Ctrl Pts',(-0.707690042210776,95.3082201250359,
15.4515365412012));
#58916=CARTESIAN_POINT('Ctrl Pts',(-0.767012739212091,95.3160591733945,
15.4291118063293));
#58917=CARTESIAN_POINT('Ctrl Pts',(-0.825210479240838,95.3239049988934,
15.4042811838574));
#58918=CARTESIAN_POINT('Ctrl Pts',(-0.871582749652548,95.3301565945989,
15.3844960111138));
#58919=CARTESIAN_POINT('Ctrl Pts',(-0.917239751485826,95.3364123695739,
15.3631832960744));
#58920=CARTESIAN_POINT('Ctrl Pts',(-0.962038500852752,95.3426972625086,
15.3403201667661));
#58921=CARTESIAN_POINT('Ctrl Pts',(-1.01684562864418,95.3503862479177,15.3123492419653));
#58922=CARTESIAN_POINT('Ctrl Pts',(-1.07039430988932,95.3581096649516,15.2820817073528));
#58923=CARTESIAN_POINT('Ctrl Pts',(-1.12256875438812,95.3658159655874,15.2497401217053));
#58924=CARTESIAN_POINT('Ctrl Pts',(-1.16550523980646,95.3721577957315,15.2231249074198));
#58925=CARTESIAN_POINT('Ctrl Pts',(-1.2075120192865,95.3784881524552,15.1951048624561));
#58926=CARTESIAN_POINT('Ctrl Pts',(-1.2485462574634,95.3847816704486,15.1657891575002));
#58927=CARTESIAN_POINT('Ctrl Pts',(-1.28650442894323,95.3906034048298,15.1386710579519));
#58928=CARTESIAN_POINT('Ctrl Pts',(-1.32356327725076,95.3964204635369,15.1103743642508));
#58929=CARTESIAN_POINT('Ctrl Pts',(-1.35961987671512,95.4022300177208,15.080950862646));
#58930=CARTESIAN_POINT('Ctrl Pts',(-1.37565779232735,95.4048140977819,15.0678633379552));
#58931=CARTESIAN_POINT('Ctrl Pts',(-1.39150515784867,95.4073979316919,15.0545466685588));
#58932=CARTESIAN_POINT('Ctrl Pts',(-1.40715667418759,95.4099813311926,15.041008543745));
#58933=CARTESIAN_POINT('Ctrl Pts',(-1.47136461940602,95.4205793314132,14.9854704631157));
#58934=CARTESIAN_POINT('Ctrl Pts',(-1.53227324531738,95.4311699153715,14.9262027716018));
#58935=CARTESIAN_POINT('Ctrl Pts',(-1.58953095433024,95.4417391135738,14.8637684311561));
#58936=CARTESIAN_POINT('Ctrl Pts',(-1.62864806456368,95.4489597393775,14.8211147689738));
#58937=CARTESIAN_POINT('Ctrl Pts',(-1.66605987183824,95.4561699746208,14.7769867410379));
#58938=CARTESIAN_POINT('Ctrl Pts',(-1.70167250251401,95.463367047025,14.7315625019744));
#58939=CARTESIAN_POINT('Ctrl Pts',(-1.73997683466568,95.4711080941382,14.6827049728393));
#58940=CARTESIAN_POINT('Ctrl Pts',(-1.7762005158223,95.4788340079623,14.6323476481508));
#58941=CARTESIAN_POINT('Ctrl Pts',(-1.81024426484934,95.4865438722681,14.5806983708747));
#58942=CARTESIAN_POINT('Ctrl Pts',(-1.86411551659837,95.4987440574076,14.4989679123232));
#58943=CARTESIAN_POINT('Ctrl Pts',(-1.91254280583083,95.5109064364272,14.4139890410822));
#58944=CARTESIAN_POINT('Ctrl Pts',(-1.95518498824451,95.5230438721566,14.3264537180762));
#58945=CARTESIAN_POINT('Ctrl Pts',(-1.98279957081004,95.5309039347076,14.2697668585458));
#58946=CARTESIAN_POINT('Ctrl Pts',(-2.00798817134963,95.5387538769753,14.2120045961421));
#58947=CARTESIAN_POINT('Ctrl Pts',(-2.03064411381718,95.5465958755964,14.1533593567212));
#58948=CARTESIAN_POINT('Ctrl Pts',(-2.06813035770517,95.55957115011,14.0563256645256));
#58949=CARTESIAN_POINT('Ctrl Pts',(-2.09867778680689,95.5725232965738,13.9568841690516));
#58950=CARTESIAN_POINT('Ctrl Pts',(-2.1217652090683,95.58545200991,13.8559834397369));
#58951=CARTESIAN_POINT('Ctrl Pts',(-2.14227665834112,95.5969382054997,13.7663406824167));
#58952=CARTESIAN_POINT('Ctrl Pts',(-2.15689986373622,95.6084053748756,13.6755505235125));
#58953=CARTESIAN_POINT('Ctrl Pts',(-2.16574516758808,95.6198564696486,13.5842996138752));
#58954=CARTESIAN_POINT('Ctrl Pts',(-2.17211995197266,95.6281092398606,13.5185353525704));
#58955=CARTESIAN_POINT('Ctrl Pts',(-2.17549201090315,95.6363548045513,13.4525225851773));
#58956=CARTESIAN_POINT('Ctrl Pts',(-2.17590326200913,95.6445846214129,13.3865967293626));
#58957=CARTESIAN_POINT('Ctrl Pts',(-2.17606264055466,95.6477740505045,13.3610474557932));
#58958=CARTESIAN_POINT('Ctrl Pts',(-2.1757775959806,95.6509611121884,13.335511268976));
#58959=CARTESIAN_POINT('Ctrl Pts',(-2.17505156918613,95.6541453093621,13.3100076794586));
#58960=CARTESIAN_POINT('Ctrl Pts',(-2.17300309787237,95.6631294634148,13.2380497683699));
#58961=CARTESIAN_POINT('Ctrl Pts',(-2.16752924649556,95.6720775411009,13.1663416718358));
#58962=CARTESIAN_POINT('Ctrl Pts',(-2.15857548450997,95.6810176218596,13.0951743479573));
#58963=CARTESIAN_POINT('Ctrl Pts',(-2.15624659691499,95.6833429509459,13.0766636149252));
#58964=CARTESIAN_POINT('Ctrl Pts',(-2.15368217620392,95.6856677074371,13.0581897171597));
#58965=CARTESIAN_POINT('Ctrl Pts',(-2.15088106624707,95.6879923187851,13.039758314068));
#58966=CARTESIAN_POINT('Ctrl Pts',(-2.13474051480207,95.7013871906862,12.9335529117854));
#58967=CARTESIAN_POINT('Ctrl Pts',(-2.11080268605646,95.7147709892224,12.8287124234999));
#58968=CARTESIAN_POINT('Ctrl Pts',(-2.07934926399926,95.7281262603083,12.7264205178026));
#58969=CARTESIAN_POINT('Ctrl Pts',(-2.05792705046345,95.7372222330298,12.6567518171172));
#58970=CARTESIAN_POINT('Ctrl Pts',(-2.03301888080868,95.7463051150478,12.5882642240548));
#58971=CARTESIAN_POINT('Ctrl Pts',(-2.00471254214963,95.7553712266143,12.5213179818491));
#58972=CARTESIAN_POINT('Ctrl Pts',(-1.99475252620534,95.7585612759118,12.4977619279274));
#58973=CARTESIAN_POINT('Ctrl Pts',(-1.98436872862985,95.7617495293799,12.4743999366367));
#58974=CARTESIAN_POINT('Ctrl Pts',(-1.97356473464234,95.76493578494,12.4512495612729));
#58975=CARTESIAN_POINT('Ctrl Pts',(-1.97355279841807,95.7649393051068,12.4512239847988));
#58976=CARTESIAN_POINT('Ctrl Pts',(-1.97354086168094,95.7649428252711,12.451198408583));
#58977=CARTESIAN_POINT('Ctrl Pts',(-1.97352892443098,95.7649463454331,12.4511728326255));
#58978=CARTESIAN_POINT('Ctrl Pts',(-1.93787473334702,95.7754603688591,12.374782535174));
#58979=CARTESIAN_POINT('Ctrl Pts',(-1.89762639969028,95.7859580587182,12.3006573840691));
#58980=CARTESIAN_POINT('Ctrl Pts',(-1.85331695285095,95.796426158897,12.2291776297439));
#58981=CARTESIAN_POINT('Ctrl Pts',(-1.83727577927542,95.8002158837515,12.2033000973426));
#58982=CARTESIAN_POINT('Ctrl Pts',(-1.82070219758726,95.8040017916461,12.1777688086928));
#58983=CARTESIAN_POINT('Ctrl Pts',(-1.80362085265156,95.8077834618331,12.1526002598606));
#58984=CARTESIAN_POINT('Ctrl Pts',(-1.78202255477625,95.8125651484902,12.1207761958413));
#58985=CARTESIAN_POINT('Ctrl Pts',(-1.75958563591836,95.8173432133199,12.0895511217171));
#58986=CARTESIAN_POINT('Ctrl Pts',(-1.73633811654556,95.8221192234617,12.058977289736));
#58987=CARTESIAN_POINT('Ctrl Pts',(-1.66663457668081,95.8364392379103,11.9673071084087));
#58988=CARTESIAN_POINT('Ctrl Pts',(-1.58964146194808,95.8507411093057,11.8814947342166));
#58989=CARTESIAN_POINT('Ctrl Pts',(-1.50652447525991,95.8650199624051,11.8026109896439));
#58990=CARTESIAN_POINT('Ctrl Pts',(-1.46114538740433,95.8728157374337,11.7595431100446));
#58991=CARTESIAN_POINT('Ctrl Pts',(-1.41394159235836,95.8806045476131,11.7185399399839));
#58992=CARTESIAN_POINT('Ctrl Pts',(-1.36510687148839,95.888385133887,11.6797706355735));
#58993=CARTESIAN_POINT('Ctrl Pts',(-1.28959584252985,95.9004159198723,11.6198233272675));
#58994=CARTESIAN_POINT('Ctrl Pts',(-1.21022638718133,95.9124240035505,11.5651294907366));
#58995=CARTESIAN_POINT('Ctrl Pts',(-1.12774807335125,95.9244009269098,11.5163062222698));
#58996=CARTESIAN_POINT('Ctrl Pts',(-1.11380347968499,95.9264258631853,11.5080516810624));
#58997=CARTESIAN_POINT('Ctrl Pts',(-1.0997699745765,95.9284499214416,11.4999648367301));
#58998=CARTESIAN_POINT('Ctrl Pts',(-1.08565111724086,95.9304730762785,11.4920485383264));
#58999=CARTESIAN_POINT('Ctrl Pts',(-1.06139616484,95.9339486779579,11.4784490354481));
#59000=CARTESIAN_POINT('Ctrl Pts',(-1.0369000705869,95.937420739775,11.465333119402));
#59001=CARTESIAN_POINT('Ctrl Pts',(-1.01218504280194,95.9408889018017,11.4527035840313));
#59002=CARTESIAN_POINT('Ctrl Pts',(-1.0121643460679,95.9408918060925,11.4526930078694));
#59003=CARTESIAN_POINT('Ctrl Pts',(-1.01214364918012,95.9408947103805,11.4526824320485));
#59004=CARTESIAN_POINT('Ctrl Pts',(-1.01212295213882,95.9408976146659,11.4526718565687));
#59005=CARTESIAN_POINT('Ctrl Pts',(-0.980130078477351,95.9453869729441,
11.4363245929073));
#59006=CARTESIAN_POINT('Ctrl Pts',(-0.94772828265125,95.9498750213854,11.4207975708423));
#59007=CARTESIAN_POINT('Ctrl Pts',(-0.914959759593808,95.9543615825662,
11.4061156705712));
#59008=CARTESIAN_POINT('Ctrl Pts',(-0.848326045309448,95.9634848572195,
11.3762605090768));
#59009=CARTESIAN_POINT('Ctrl Pts',(-0.780182134957265,95.9726011635176,
11.3499002941302));
#59010=CARTESIAN_POINT('Ctrl Pts',(-0.710906234045462,95.9817091443279,
11.3271548907497));
#59011=CARTESIAN_POINT('Ctrl Pts',(-0.666439205165701,95.9875554031336,
11.3125550010956));
#59012=CARTESIAN_POINT('Ctrl Pts',(-0.62150684637548,95.9933981145678,11.2994445172896));
#59013=CARTESIAN_POINT('Ctrl Pts',(-0.576220351855335,95.9992356586606,
11.2878537721618));
#59014=CARTESIAN_POINT('Ctrl Pts',(-0.522826054268815,96.0061183191484,
11.2741878944833));
#59015=CARTESIAN_POINT('Ctrl Pts',(-0.468934391840693,96.0129944243556,
11.262634800864));
#59016=CARTESIAN_POINT('Ctrl Pts',(-0.414718625558492,96.0198624171801,
11.2532427688084));
#59017=CARTESIAN_POINT('Ctrl Pts',(-0.29434694244602,96.0351109677878,11.232390260693));
#59018=CARTESIAN_POINT('Ctrl Pts',(-0.172377141413166,96.0503195515522,
11.2221941161788));
#59019=CARTESIAN_POINT('Ctrl Pts',(-0.0507252149178954,96.0654809749851,
11.2226095713006));
#59020=CARTESIAN_POINT('Ctrl Pts',(0.00101769105191436,96.0719296694666,
11.2227862791911));
#59021=CARTESIAN_POINT('Ctrl Pts',(0.0527029832957061,96.0783698243123,
11.2248820915687));
#59022=CARTESIAN_POINT('Ctrl Pts',(0.104183178719241,96.0848009594534,11.2288907196644));
#59023=CARTESIAN_POINT('Ctrl Pts',(0.186272301341844,96.0950558980149,11.2352827848187));
#59024=CARTESIAN_POINT('Ctrl Pts',(0.267844000106881,96.1052884101216,11.2465398472509));
#59025=CARTESIAN_POINT('Ctrl Pts',(0.348285412315078,96.1154971448446,11.2625358784358));
#59026=CARTESIAN_POINT('Ctrl Pts',(0.384748555108407,96.1201246438121,11.2697866905885));
#59027=CARTESIAN_POINT('Ctrl Pts',(0.420980163909315,96.1247473462816,11.278011142707));
#59028=CARTESIAN_POINT('Ctrl Pts',(0.456926658271324,96.1293655697248,11.2871975023484));
#59029=CARTESIAN_POINT('Ctrl Pts',(0.508494969858789,96.1359908050843,11.3003761186433));
#59030=CARTESIAN_POINT('Ctrl Pts',(0.559473311276387,96.1426064281092,11.3155337689461));
#59031=CARTESIAN_POINT('Ctrl Pts',(0.609698270949521,96.1492125649547,11.3326328559732));
#59032=CARTESIAN_POINT('Ctrl Pts',(0.663633514182684,96.1563067189353,11.350995109002));
#59033=CARTESIAN_POINT('Ctrl Pts',(0.716698856128576,96.1633897928817,11.3715956364018));
#59034=CARTESIAN_POINT('Ctrl Pts',(0.768756448063106,96.1704729822069,11.3942719800529));
#59035=CARTESIAN_POINT('Ctrl Pts',(0.768768862494322,96.17047467137,11.3942773877927));
#59036=CARTESIAN_POINT('Ctrl Pts',(0.768781276868443,96.1704763605332,11.3942827956505));
#59037=CARTESIAN_POINT('Ctrl Pts',(0.768793691185528,96.1704780496965,11.3942882036265));
#59038=CARTESIAN_POINT('Ctrl Pts',(0.853814957640094,96.1820465312246,11.4313255181957));
#59039=CARTESIAN_POINT('Ctrl Pts',(0.936198354852795,96.1936172508596,11.4741798311531));
#59040=CARTESIAN_POINT('Ctrl Pts',(1.01529734550568,96.2051845723368,11.5222962174482));
#59041=CARTESIAN_POINT('Ctrl Pts',(1.06765635561441,96.2128414779074,11.5541465145964));
#59042=CARTESIAN_POINT('Ctrl Pts',(1.11857538549673,96.2204967750912,11.5883017404707));
#59043=CARTESIAN_POINT('Ctrl Pts',(1.16785982437448,96.2281474195521,11.6245906799445));
#59044=CARTESIAN_POINT('Ctrl Pts',(1.2311908069148,96.2379785719768,11.6712223195563));
#59045=CARTESIAN_POINT('Ctrl Pts',(1.29179889313266,96.2477976271712,11.7214177076016));
#59046=CARTESIAN_POINT('Ctrl Pts',(1.34926661736094,96.2575969719615,11.7748834431036));
#59047=CARTESIAN_POINT('Ctrl Pts',(1.38747278965184,96.264111854192,11.810428979832));
#59048=CARTESIAN_POINT('Ctrl Pts',(1.42428988158487,96.2706178953477,11.8474197352934));
#59049=CARTESIAN_POINT('Ctrl Pts',(1.45958400593841,96.2771113254996,11.885763560152));
#59050=CARTESIAN_POINT('Ctrl Pts',(1.47104336648822,96.2792196242229,11.8982131030139));
#59051=CARTESIAN_POINT('Ctrl Pts',(1.48234259526421,96.2813266706931,11.9108054908799));
#59052=CARTESIAN_POINT('Ctrl Pts',(1.4934792669407,96.2834327268134,11.9235360145983));
#59053=CARTESIAN_POINT('Ctrl Pts',(1.49348443358187,96.283433703877,11.9235419206759));
#59054=CARTESIAN_POINT('Ctrl Pts',(1.49348960018741,96.2834346809402,11.9235478267827));
#59055=CARTESIAN_POINT('Ctrl Pts',(1.49349476675733,96.2834356580031,11.9235537329185));
#59056=CARTESIAN_POINT('Ctrl Pts',(1.54955196201186,96.2940367738654,11.9876352052438));
#59057=CARTESIAN_POINT('Ctrl Pts',(1.60141383309193,96.3045981956347,12.0551335272336));
#59058=CARTESIAN_POINT('Ctrl Pts',(1.64880542222686,96.3151357596347,12.1254293339887));
#59059=CARTESIAN_POINT('Ctrl Pts',(1.67777069941973,96.3215762160061,12.168393445666));
#59060=CARTESIAN_POINT('Ctrl Pts',(1.70506650503284,96.3280078759479,12.212403525441));
#59061=CARTESIAN_POINT('Ctrl Pts',(1.73063201875259,96.3344354421685,12.2573274847705));
#59062=CARTESIAN_POINT('Ctrl Pts',(1.77325818609066,96.3451523210194,12.3322305838773));
#59063=CARTESIAN_POINT('Ctrl Pts',(1.81107681615759,96.3558585099647,12.4096730870144));
#59064=CARTESIAN_POINT('Ctrl Pts',(1.84378220907545,96.3665708757059,12.4890056422043));
#59065=CARTESIAN_POINT('Ctrl Pts',(1.86877617329365,96.3747574303423,12.549632800873));
#59066=CARTESIAN_POINT('Ctrl Pts',(1.89078475316923,96.3829477275824,12.6113645024578));
#59067=CARTESIAN_POINT('Ctrl Pts',(1.90968125808506,96.3911518875422,12.6739288632165));
#59068=CARTESIAN_POINT('Ctrl Pts',(1.9125907471821,96.3924150795483,12.6835618787557));
#59069=CARTESIAN_POINT('Ctrl Pts',(1.91542637278672,96.3936785729357,12.6932145054351));
#59070=CARTESIAN_POINT('Ctrl Pts',(1.91818764680601,96.3949423945857,12.7028857148542));
#59071=CARTESIAN_POINT('Ctrl Pts',(1.91818905954012,96.3949430411872,12.7028906628772));
#59072=CARTESIAN_POINT('Ctrl Pts',(1.91819047225476,96.3949436877888,12.7028956109051));
#59073=CARTESIAN_POINT('Ctrl Pts',(1.91819188494994,96.3949443343905,12.7029005589378));
#59074=CARTESIAN_POINT('Ctrl Pts',(1.92429624476701,96.3977383478278,12.7242813724547));
#59075=CARTESIAN_POINT('Ctrl Pts',(1.93004069192381,96.4005353529886,12.7457621690415));
#59076=CARTESIAN_POINT('Ctrl Pts',(1.93541929227345,96.4033337409118,12.7673314485684));
#59077=CARTESIAN_POINT('Ctrl Pts',(1.95478165646614,96.4134076267929,12.8449784605094));
#59078=CARTESIAN_POINT('Ctrl Pts',(1.96940226796508,96.4234994925514,12.9237697227759));
#59079=CARTESIAN_POINT('Ctrl Pts',(1.97928283481565,96.4335865836525,13.0031205781567));
#59080=CARTESIAN_POINT('Ctrl Pts',(1.98288946460194,96.4372685994491,13.0320854303673));
#59081=CARTESIAN_POINT('Ctrl Pts',(1.98586471178355,96.4409499288741,13.0611243771114));
#59082=CARTESIAN_POINT('Ctrl Pts',(1.98820941786643,96.4446292924097,13.0902074416763));
#59083=CARTESIAN_POINT('Ctrl Pts',(1.99492353019111,96.4551652227943,13.173487373289));
#59084=CARTESIAN_POINT('Ctrl Pts',(1.99646481606683,96.4656849900875,13.2571322183715));
#59085=CARTESIAN_POINT('Ctrl Pts',(1.9928596492666,96.4761605018442,13.3404687148225));
#59086=CARTESIAN_POINT('Ctrl Pts',(1.99160969799698,96.4797924778237,13.3693624013887));
#59087=CARTESIAN_POINT('Ctrl Pts',(1.98974119464507,96.4834190748398,13.3982185749907));
#59088=CARTESIAN_POINT('Ctrl Pts',(1.98725566383167,96.4870389346109,13.4270077853693));
#59089=CARTESIAN_POINT('Ctrl Pts',(1.97980151173059,96.4978949598804,13.5133471507374));
#59090=CARTESIAN_POINT('Ctrl Pts',(1.96679594258491,96.5086903725417,13.599088109065));
#59091=CARTESIAN_POINT('Ctrl Pts',(1.94829282052133,96.5193972636432,13.6834765967547));
#59092=CARTESIAN_POINT('Ctrl Pts',(1.94286298122375,96.522539257619,13.7082408460066));
#59093=CARTESIAN_POINT('Ctrl Pts',(1.9369597083664,96.525673584629,13.7328882876823));
#59094=CARTESIAN_POINT('Ctrl Pts',(1.9305844127389,96.5287994301737,13.7573990147299));
#59095=CARTESIAN_POINT('Ctrl Pts',(1.91343077839771,96.5372099596007,13.8233485916246));
#59096=CARTESIAN_POINT('Ctrl Pts',(1.89285663288248,96.5455607072524,13.8883211413174));
#59097=CARTESIAN_POINT('Ctrl Pts',(1.86906225836649,96.5538832067112,13.9519740874812));
#59098=CARTESIAN_POINT('Ctrl Pts',(1.85209719086988,96.5598170363634,13.9973577779539));
#59099=CARTESIAN_POINT('Ctrl Pts',(1.83349497978107,96.5657366456325,14.0420717676147));
#59100=CARTESIAN_POINT('Ctrl Pts',(1.81332225629261,96.5716555337813,14.086006801809));
#59101=CARTESIAN_POINT('Ctrl Pts',(1.78588406002382,96.5797061876661,14.145765618807));
#59102=CARTESIAN_POINT('Ctrl Pts',(1.75554337688148,96.5877560732731,14.2040807186407));
#59103=CARTESIAN_POINT('Ctrl Pts',(1.72249083697302,96.5958337879808,14.2606441922532));
#59104=CARTESIAN_POINT('Ctrl Pts',(1.70141109533706,96.600985468896,14.2967183763578));
#59105=CARTESIAN_POINT('Ctrl Pts',(1.67922835419628,96.6061485879362,14.3320811519021));
#59106=CARTESIAN_POINT('Ctrl Pts',(1.65599074082823,96.6113318017801,14.3666635818558));
#59107=CARTESIAN_POINT('Ctrl Pts',(1.65131304494949,96.6123751747656,14.373624971888));
#59108=CARTESIAN_POINT('Ctrl Pts',(1.64660456825496,96.6134239217114,14.3805635176563));
#59109=CARTESIAN_POINT('Ctrl Pts',(1.64185061560271,96.614472345387,14.3874675456986));
#59110=CARTESIAN_POINT('Ctrl Pts',(1.64184231942404,96.6144741750035,14.3874795939991));
#59111=CARTESIAN_POINT('Ctrl Pts',(1.64183402310706,96.614476004619,14.3874916421943));
#59112=CARTESIAN_POINT('Ctrl Pts',(1.64182572665163,96.6144778342334,14.3875036902841));
#59113=CARTESIAN_POINT('Ctrl Pts',(1.5948408133683,96.6248394007863,14.4557350526163));
#59114=CARTESIAN_POINT('Ctrl Pts',(1.54339801233543,96.6352440080243,14.5208725954583));
#59115=CARTESIAN_POINT('Ctrl Pts',(1.48809123974865,96.6456718247073,14.5825065833522));
#59116=CARTESIAN_POINT('Ctrl Pts',(1.47805984267335,96.6475631946948,14.593685594113));
#59117=CARTESIAN_POINT('Ctrl Pts',(1.46790146364113,96.6494553219179,14.6047493796719));
#59118=CARTESIAN_POINT('Ctrl Pts',(1.45761981942515,96.651348079647,14.6156955475071));
#59119=CARTESIAN_POINT('Ctrl Pts',(1.38766361293164,96.6642263846881,14.6901731661941));
#59120=CARTESIAN_POINT('Ctrl Pts',(1.31183355965818,96.6770701992615,14.7590824059048));
#59121=CARTESIAN_POINT('Ctrl Pts',(1.23121719354291,96.6898422258653,14.8217255310512));
#59122=CARTESIAN_POINT('Ctrl Pts',(1.14962085059773,96.7027695099031,14.8851301493553));
#59123=CARTESIAN_POINT('Ctrl Pts',(1.06312206621914,96.7156229243032,14.942114893507));
#59124=CARTESIAN_POINT('Ctrl Pts',(0.972882099229031,96.7283769835321,14.9919867057191));
#59125=CARTESIAN_POINT('Ctrl Pts',(0.883954667112826,96.7409455357391,15.0411331354324));
#59126=CARTESIAN_POINT('Ctrl Pts',(0.791395048648228,96.7534172449107,15.0833717561073));
#59127=CARTESIAN_POINT('Ctrl Pts',(0.696332474724466,96.765785423087,15.1180743122479));
#59128=CARTESIAN_POINT('Ctrl Pts',(0.677351449785182,96.7682549617154,15.12500332812));
#59129=CARTESIAN_POINT('Ctrl Pts',(0.658287563029822,96.7707416625033,15.1316832108969));
#59130=CARTESIAN_POINT('Ctrl Pts',(0.639152814130027,96.7732587587901,15.1381405055837));
#59131=CARTESIAN_POINT('Ctrl Pts',(0.566661679031735,96.7827946647978,15.1626036759112));
#59132=CARTESIAN_POINT('Ctrl Pts',(0.49282441715406,96.7923303004171,15.1828190378486));
#59133=CARTESIAN_POINT('Ctrl Pts',(0.418181192380986,96.801858035304,15.1984908859961));
#59134=CARTESIAN_POINT('Ctrl Pts',(0.372795814454764,96.8076511913465,15.2080198519959));
#59135=CARTESIAN_POINT('Ctrl Pts',(0.3271081986575,96.8134419946363,15.2158700313298));
#59136=CARTESIAN_POINT('Ctrl Pts',(0.281260566632972,96.8192262850474,15.2219780794927));
#59137=CARTESIAN_POINT('Ctrl Pts',(0.251704726021794,96.8229551486308,15.2259156546733));
#59138=CARTESIAN_POINT('Ctrl Pts',(0.222083460018819,96.8266811747956,15.2291292646824));
#59139=CARTESIAN_POINT('Ctrl Pts',(0.192436998294307,96.830403003659,15.2316043318055));
#59140=CARTESIAN_POINT('Ctrl Pts',(0.177582023084877,96.832267903289,15.2328445155784));
#59141=CARTESIAN_POINT('Ctrl Pts',(0.162710795323073,96.8341329950944,15.2339001422121));
#59142=CARTESIAN_POINT('Ctrl Pts',(0.147827757845089,96.8359981944933,15.2347724717209));
#59143=CARTESIAN_POINT('Ctrl Pts',(0.0772629933168082,96.8448416417115,
15.2389084370082));
#59144=CARTESIAN_POINT('Ctrl Pts',(0.00643537457473485,96.8536871475861,
15.2389194584622));
#59145=CARTESIAN_POINT('Ctrl Pts',(-0.0641387309311826,96.8625207338574,
15.2349692109548));
#59146=CARTESIAN_POINT('Ctrl Pts',(-0.0771742157732686,96.864152353261,
15.2342395751891));
#59147=CARTESIAN_POINT('Ctrl Pts',(-0.0902010511963878,96.8657835662794,
15.233374938362));
#59148=CARTESIAN_POINT('Ctrl Pts',(-0.103215991010027,96.8674142851885,
15.2323765231221));
#59149=CARTESIAN_POINT('Ctrl Pts',(-0.166641676164636,96.8753612650123,
15.227510947747));
#59150=CARTESIAN_POINT('Ctrl Pts',(-0.229785670077932,96.8832966225723,
15.2194689710231));
#59151=CARTESIAN_POINT('Ctrl Pts',(-0.292387832427161,96.8912816072917,
15.2085109581398));
#59152=CARTESIAN_POINT('Ctrl Pts',(-0.302083567934587,96.8925183105775,
15.2068137964026));
#59153=CARTESIAN_POINT('Ctrl Pts',(-0.311766403639732,96.8937562163189,
15.2050466593504));
#59154=CARTESIAN_POINT('Ctrl Pts',(-0.32143547883787,96.8949955652553,15.2032104804451));
#59155=CARTESIAN_POINT('Ctrl Pts',(-0.39298478617292,96.9041665103697,15.1896231076998));
#59156=CARTESIAN_POINT('Ctrl Pts',(-0.463764328797108,96.9133486001417,
15.1721090777386));
#59157=CARTESIAN_POINT('Ctrl Pts',(-0.533342416148416,96.922490239889,15.1507388991162));
#59158=CARTESIAN_POINT('Ctrl Pts',(-0.55868545034734,96.9258199791442,15.1429550523869));
#59159=CARTESIAN_POINT('Ctrl Pts',(-0.583868589780022,96.9291442892171,
15.1346596058387));
#59160=CARTESIAN_POINT('Ctrl Pts',(-0.60886927308371,96.9324604625022,15.1258560932481));
#59161=CARTESIAN_POINT('Ctrl Pts',(-0.703263780070516,96.9449812619751,
15.0926168725179));
#59162=CARTESIAN_POINT('Ctrl Pts',(-0.795054342654565,96.9573861214602,
15.0521385166626));
#59163=CARTESIAN_POINT('Ctrl Pts',(-0.883112879463809,96.9697181932088,
15.0049849995442));
#59164=CARTESIAN_POINT('Ctrl Pts',(-0.955284732212308,96.9798254298105,
14.9663384717077));
#59165=CARTESIAN_POINT('Ctrl Pts',(-1.02494896921815,96.9898840793762,14.9232085161692));
#59166=CARTESIAN_POINT('Ctrl Pts',(-1.09151383210832,96.999950508479,14.8759547770441));
#59167=CARTESIAN_POINT('Ctrl Pts',(-1.10453113864235,97.0019190815015,14.8667139196254));
#59168=CARTESIAN_POINT('Ctrl Pts',(-1.11743004979981,97.0038879731062,14.8573152712551));
#59169=CARTESIAN_POINT('Ctrl Pts',(-1.13020632708847,97.0058576354751,14.8477613871022));
#59170=CARTESIAN_POINT('Ctrl Pts',(-1.1498824989815,97.0088910241896,14.833047878418));
#59171=CARTESIAN_POINT('Ctrl Pts',(-1.16930221410112,97.0119564434176,14.8180095705093));
#59172=CARTESIAN_POINT('Ctrl Pts',(-1.18841205214264,97.0150214916683,14.8026054837613));
#59173=CARTESIAN_POINT('Ctrl Pts',(-1.24398486563493,97.0239348772453,14.7578092673831));
#59174=CARTESIAN_POINT('Ctrl Pts',(-1.29693707810882,97.0328455603298,14.7099147513584));
#59175=CARTESIAN_POINT('Ctrl Pts',(-1.34676854624776,97.0417400145777,14.6591832773238));
#59176=CARTESIAN_POINT('Ctrl Pts',(-1.34967742339086,97.0422592221313,14.6562218629653));
#59177=CARTESIAN_POINT('Ctrl Pts',(-1.35257567732859,97.0427783744049,14.6532507915937));
#59178=CARTESIAN_POINT('Ctrl Pts',(-1.3554632127988,97.0432974687158,14.6502701188745));
#59179=CARTESIAN_POINT('Ctrl Pts',(-1.35548420701023,97.0433012428602,14.6502484474963));
#59180=CARTESIAN_POINT('Ctrl Pts',(-1.35550520065501,97.0433050170014,14.6502267756106));
#59181=CARTESIAN_POINT('Ctrl Pts',(-1.35552619373324,97.0433087911397,14.6502051032174));
#59182=CARTESIAN_POINT('Ctrl Pts',(-1.39907127316221,97.0511373309756,14.6052509485129));
#59183=CARTESIAN_POINT('Ctrl Pts',(-1.44029344158329,97.0589822101343,14.5580202340714));
#59184=CARTESIAN_POINT('Ctrl Pts',(-1.47915585153603,97.0669126895379,14.5089162135298));
#59185=CARTESIAN_POINT('Ctrl Pts',(-1.50462635225016,97.0721103414993,14.4767333408826));
#59186=CARTESIAN_POINT('Ctrl Pts',(-1.52908428227552,97.0773448936824,14.44374546445));
#59187=CARTESIAN_POINT('Ctrl Pts',(-1.55252975469165,97.0826373060376,14.4100602107336));
#59188=CARTESIAN_POINT('Ctrl Pts',(-1.59225080221582,97.091603649686,14.3529910444578));
#59189=CARTESIAN_POINT('Ctrl Pts',(-1.62887304268975,97.1005957716121,14.2937832759773));
#59190=CARTESIAN_POINT('Ctrl Pts',(-1.66216995717027,97.1095353395864,14.2327791611904));
#59191=CARTESIAN_POINT('Ctrl Pts',(-1.68031818454648,97.114407782417,14.1995293371959));
#59192=CARTESIAN_POINT('Ctrl Pts',(-1.69747814378383,97.1192644930128,14.1657466882876));
#59193=CARTESIAN_POINT('Ctrl Pts',(-1.7136111324771,97.1240919369856,14.1314927698294));
#59194=CARTESIAN_POINT('Ctrl Pts',(-1.72774890789126,97.1283223570279,14.1014751323398));
#59195=CARTESIAN_POINT('Ctrl Pts',(-1.74109927569005,97.1325306439271,14.0710931895949));
#59196=CARTESIAN_POINT('Ctrl Pts',(-1.75363834435648,97.1367085707454,14.0403842715858));
#59197=CARTESIAN_POINT('Ctrl Pts',(-1.78265192617188,97.1463756859663,13.9693283001399));
#59198=CARTESIAN_POINT('Ctrl Pts',(-1.80732281357069,97.1558789228922,13.8965141110427));
#59199=CARTESIAN_POINT('Ctrl Pts',(-1.82758216206067,97.1652840075554,13.8225054486416));
#59200=CARTESIAN_POINT('Ctrl Pts',(-1.83573227138912,97.1690675679343,13.7927325914286));
#59201=CARTESIAN_POINT('Ctrl Pts',(-1.84316839547632,97.1728353129077,13.7627658324143));
#59202=CARTESIAN_POINT('Ctrl Pts',(-1.84988564919904,97.1765917986113,13.732639556223));
#59203=CARTESIAN_POINT('Ctrl Pts',(-1.86656155082962,97.1859174529121,13.6578496437082));
#59204=CARTESIAN_POINT('Ctrl Pts',(-1.87880762938304,97.1951749596988,13.5820800294758));
#59205=CARTESIAN_POINT('Ctrl Pts',(-1.88655046656516,97.2044368823206,13.5059217582517));
#59206=CARTESIAN_POINT('Ctrl Pts',(-1.88958729765734,97.2080695164481,13.4760515956046));
#59207=CARTESIAN_POINT('Ctrl Pts',(-1.89193160827013,97.21170290457,13.4461211222062));
#59208=CARTESIAN_POINT('Ctrl Pts',(-1.89357959499398,97.2153417120222,13.4161639224355));
#59209=CARTESIAN_POINT('Ctrl Pts',(-1.89753812082994,97.2240822638135,13.3442056065407));
#59210=CARTESIAN_POINT('Ctrl Pts',(-1.8974952294512,97.2328672457064,13.2720967317335));
#59211=CARTESIAN_POINT('Ctrl Pts',(-1.893392867159,97.2417399324394,13.2003539629298));
#59212=CARTESIAN_POINT('Ctrl Pts',(-1.89151844720891,97.2457939724873,13.167573806634));
#59213=CARTESIAN_POINT('Ctrl Pts',(-1.88879707332287,97.2498663790102,13.1348696186156));
#59214=CARTESIAN_POINT('Ctrl Pts',(-1.88522576936773,97.25396155984,13.1022881113543));
#59215=CARTESIAN_POINT('Ctrl Pts',(-1.88522410483544,97.2539634685436,13.1022729255927));
#59216=CARTESIAN_POINT('Ctrl Pts',(-1.88522244011855,97.2539653772521,13.1022577398576));
#59217=CARTESIAN_POINT('Ctrl Pts',(-1.88522077521706,97.2539672859656,13.1022425541492));
#59218=CARTESIAN_POINT('Ctrl Pts',(-1.87687837862261,97.2635313622859,13.0261508439112));
#59219=CARTESIAN_POINT('Ctrl Pts',(-1.8638092727973,97.2731792636298,12.9506111981236));
#59220=CARTESIAN_POINT('Ctrl Pts',(-1.84617669575997,97.2828313555678,12.8761466692974));
#59221=CARTESIAN_POINT('Ctrl Pts',(-1.83968311781548,97.2863859472303,12.8487234956451));
#59222=CARTESIAN_POINT('Ctrl Pts',(-1.83257078535585,97.2899410429422,12.8214466178707));
#59223=CARTESIAN_POINT('Ctrl Pts',(-1.82484856185339,97.2934924422361,12.7943437720108));
#59224=CARTESIAN_POINT('Ctrl Pts',(-1.7984871414283,97.3056158843839,12.7018225552653));
#59225=CARTESIAN_POINT('Ctrl Pts',(-1.76491926855089,97.3176303289924,12.6113148964554));
#59226=CARTESIAN_POINT('Ctrl Pts',(-1.72473579061861,97.3295963747473,12.5237921619917));
#59227=CARTESIAN_POINT('Ctrl Pts',(-1.71762473375568,97.3317139423688,12.5083037280981));
#59228=CARTESIAN_POINT('Ctrl Pts',(-1.71030639118383,97.3338300087006,12.4929086971463));
#59229=CARTESIAN_POINT('Ctrl Pts',(-1.70278389273608,97.3359449280349,12.4776123674558));
#59230=CARTESIAN_POINT('Ctrl Pts',(-1.66031859728433,97.3478838702648,12.3912629764724));
#59231=CARTESIAN_POINT('Ctrl Pts',(-1.61134955003944,97.3597875863096,12.3080614246423));
#59232=CARTESIAN_POINT('Ctrl Pts',(-1.55649372150675,97.3717254570158,12.2290167036105));
#59233=CARTESIAN_POINT('Ctrl Pts',(-1.54588844188208,97.3740334060588,12.2137349843873));
#59234=CARTESIAN_POINT('Ctrl Pts',(-1.53506310234205,97.3763426521225,12.1986084810493));
#59235=CARTESIAN_POINT('Ctrl Pts',(-1.5240220999447,97.3786537257481,12.1836442710473));
#59236=CARTESIAN_POINT('Ctrl Pts',(-1.47226273355685,97.3894878603888,12.1134932104529));
#59237=CARTESIAN_POINT('Ctrl Pts',(-1.41576587561513,97.4003622125247,12.0469156908551));
#59238=CARTESIAN_POINT('Ctrl Pts',(-1.35502721013357,97.4113207002559,11.9846684462004));
#59239=CARTESIAN_POINT('Ctrl Pts',(-1.35501170563695,97.4113234975817,11.9846525566152));
#59240=CARTESIAN_POINT('Ctrl Pts',(-1.35499620086394,97.4113262949131,11.984636667312));
#59241=CARTESIAN_POINT('Ctrl Pts',(-1.35498069581462,97.4113290922499,11.9846207782906));
#59242=CARTESIAN_POINT('Ctrl Pts',(-1.30684848055419,97.4200128451833,11.9352966012336));
#59243=CARTESIAN_POINT('Ctrl Pts',(-1.25605103493076,97.4287735162158,11.8886525756439));
#59244=CARTESIAN_POINT('Ctrl Pts',(-1.20286240990663,97.4375040172174,11.8449521299479));
#59245=CARTESIAN_POINT('Ctrl Pts',(-1.17363121677151,97.4423020912572,11.8209354126959));
#59246=CARTESIAN_POINT('Ctrl Pts',(-1.14367848326735,97.4470909336674,11.7978083966171));
#59247=CARTESIAN_POINT('Ctrl Pts',(-1.11305514292375,97.4518519102943,11.7756186034057));
#59248=CARTESIAN_POINT('Ctrl Pts',(-1.0427806679806,97.4627774046693,11.7246974416535));
#59249=CARTESIAN_POINT('Ctrl Pts',(-0.968948674937127,97.473558584887,11.6786916139904));
#59250=CARTESIAN_POINT('Ctrl Pts',(-0.892307937823509,97.4842721205025,
11.6378968881267));
#59251=CARTESIAN_POINT('Ctrl Pts',(-0.877548503559858,97.486335327755,11.6300406605203));
#59252=CARTESIAN_POINT('Ctrl Pts',(-0.862684747866399,97.4883960428806,
11.6223777104206));
#59253=CARTESIAN_POINT('Ctrl Pts',(-0.847721802037244,97.4904548370641,
11.6149101853474));
#59254=CARTESIAN_POINT('Ctrl Pts',(-0.767217209046669,97.5015316924966,
11.5747329319161));
#59255=CARTESIAN_POINT('Ctrl Pts',(-0.683844767705889,97.5125542163153,
11.5402139510128));
#59256=CARTESIAN_POINT('Ctrl Pts',(-0.598493168821003,97.5236103165967,
11.5117148396435));
#59257=CARTESIAN_POINT('Ctrl Pts',(-0.584963917182092,97.5253628410345,
11.5071973888372));
#59258=CARTESIAN_POINT('Ctrl Pts',(-0.571384857853042,97.5271162232202,
11.5028311238124));
#59259=CARTESIAN_POINT('Ctrl Pts',(-0.557759436969811,97.5288708291123,
11.4986174116286));
#59260=CARTESIAN_POINT('Ctrl Pts',(-0.482749928213787,97.538530136311,11.4754204415196));
#59261=CARTESIAN_POINT('Ctrl Pts',(-0.406348656347312,97.548273372566,11.4568046119093));
#59262=CARTESIAN_POINT('Ctrl Pts',(-0.329170500018915,97.5580590483754,
11.4430879578146));
#59263=CARTESIAN_POINT('Ctrl Pts',(-0.303898273917259,97.5612633981989,
11.438596396988));
#59264=CARTESIAN_POINT('Ctrl Pts',(-0.278542947167168,97.5644722821677,
11.4346297942812));
#59265=CARTESIAN_POINT('Ctrl Pts',(-0.253126614249737,97.5676841957192,
11.4311981944688));
#59266=CARTESIAN_POINT('Ctrl Pts',(-0.253114077490711,97.5676857800149,
11.4311965018116));
#59267=CARTESIAN_POINT('Ctrl Pts',(-0.253101540716823,97.5676873643113,
11.4311948092845));
#59268=CARTESIAN_POINT('Ctrl Pts',(-0.253089003928123,97.5676889486084,
11.4311931168876));
#59269=CARTESIAN_POINT('Ctrl Pts',(-0.18397673825891,97.5764227932723,11.4218633443996));
#59270=CARTESIAN_POINT('Ctrl Pts',(-0.114340807000573,97.5852839143722,
11.4163857723326));
#59271=CARTESIAN_POINT('Ctrl Pts',(-0.0445872863122623,97.5941519362418,
11.4147926072362));
#59272=CARTESIAN_POINT('Ctrl Pts',(-0.00519438737967313,97.5991601005007,
11.4138928764268));
#59273=CARTESIAN_POINT('Ctrl Pts',(0.0342350496797649,97.6041703463226,
11.4142320296684));
#59274=CARTESIAN_POINT('Ctrl Pts',(0.0736206917584265,97.6091600813032,
11.4158147843246));
#59275=CARTESIAN_POINT('Ctrl Pts',(0.177736982277446,97.6223504895189,11.4199988101501));
#59276=CARTESIAN_POINT('Ctrl Pts',(0.281593113412828,97.6354011413811,11.4328737201666));
#59277=CARTESIAN_POINT('Ctrl Pts',(0.383794535932431,97.6483864558369,11.4541011665343));
#59278=CARTESIAN_POINT('Ctrl Pts',(0.393982852748109,97.6496809436666,11.4562173009623));
#59279=CARTESIAN_POINT('Ctrl Pts',(0.404154754370905,97.6509747868019,11.4584164723396));
#59280=CARTESIAN_POINT('Ctrl Pts',(0.414308876944704,97.6522680620147,11.4606983671469));
#59281=CARTESIAN_POINT('Ctrl Pts',(0.51538101755854,97.6651410693294,11.483411899622));
#59282=CARTESIAN_POINT('Ctrl Pts',(0.614688302321226,97.6779592698353,11.5143213288823));
#59283=CARTESIAN_POINT('Ctrl Pts',(0.710802678033256,97.690801715761,11.5530729741079));
#59284=CARTESIAN_POINT('Ctrl Pts',(0.721563481973412,97.6922395344192,11.5574115431674));
#59285=CARTESIAN_POINT('Ctrl Pts',(0.732284315605942,97.6936776633208,11.5618483986565));
#59286=CARTESIAN_POINT('Ctrl Pts',(0.742963214249548,97.695116218159,11.5663830364405));
#59287=CARTESIAN_POINT('Ctrl Pts',(0.816089918146439,97.7049671191933,11.5974352194021));
#59288=CARTESIAN_POINT('Ctrl Pts',(0.887244901022521,97.7148378563862,11.6330726003644));
#59289=CARTESIAN_POINT('Ctrl Pts',(0.955770879025923,97.7247576167201,11.6731072941802));
#59290=CARTESIAN_POINT('Ctrl Pts',(0.955778057190901,97.7247586558249,11.6731114878545));
#59291=CARTESIAN_POINT('Ctrl Pts',(0.95578523532708,97.7247596949303,11.6731156815771));
#59292=CARTESIAN_POINT('Ctrl Pts',(0.955792413434416,97.7247607340362,11.673119875348));
#59293=CARTESIAN_POINT('Ctrl Pts',(0.961320102867578,97.7255609247558,11.676349398341));
#59294=CARTESIAN_POINT('Ctrl Pts',(0.966831261423941,97.7263615109594,11.6796078576718));
#59295=CARTESIAN_POINT('Ctrl Pts',(0.972325610934361,97.7271624022525,11.6828950646503));
#59296=CARTESIAN_POINT('Ctrl Pts',(1.0576495049121,97.7395997551455,11.7339433824157));
#59297=CARTESIAN_POINT('Ctrl Pts',(1.13891370374107,97.7521106981753,11.7919244505447));
#59298=CARTESIAN_POINT('Ctrl Pts',(1.21522114079168,97.7646330653377,11.85591814004));
#59299=CARTESIAN_POINT('Ctrl Pts',(1.22860955846217,97.766830160251,11.8671460658669));
#59300=CARTESIAN_POINT('Ctrl Pts',(1.24184538597427,97.7690275976935,11.8785589546342));
#59301=CARTESIAN_POINT('Ctrl Pts',(1.25492378700352,97.771225030318,11.8901516736471));
#59302=CARTESIAN_POINT('Ctrl Pts',(1.34365338452769,97.7861333751475,11.9688017540295));
#59303=CARTESIAN_POINT('Ctrl Pts',(1.42513893512118,97.8010402883418,12.0557330915253));
#59304=CARTESIAN_POINT('Ctrl Pts',(1.49795370519445,97.8158551547241,12.1494019687695));
#59305=CARTESIAN_POINT('Ctrl Pts',(1.54737741727755,97.8259108850367,12.2129806028214));
#59306=CARTESIAN_POINT('Ctrl Pts',(1.59280836790521,97.8359245255454,12.2796639253639));
#59307=CARTESIAN_POINT('Ctrl Pts',(1.6338115478498,97.8458777775162,12.3489859331239));
#59308=CARTESIAN_POINT('Ctrl Pts',(1.67374319894691,97.8555709229141,12.4164963611191));
#59309=CARTESIAN_POINT('Ctrl Pts',(1.70948069097325,97.8652096736894,12.4865223985512));
#59310=CARTESIAN_POINT('Ctrl Pts',(1.74067678353583,97.8749187713275,12.5585082030784));
#59311=CARTESIAN_POINT('Ctrl Pts',(1.74800334055896,97.8771990010501,12.5754144262109));
#59312=CARTESIAN_POINT('Ctrl Pts',(1.75507959183736,97.879483136023,12.5924288752536));
#59313=CARTESIAN_POINT('Ctrl Pts',(1.7619013630991,97.8817728379105,12.6095446057079));
#59314=CARTESIAN_POINT('Ctrl Pts',(1.76190587693937,97.881774352964,12.6095559308711));
#59315=CARTESIAN_POINT('Ctrl Pts',(1.76191039066822,97.88177586802,12.6095672560787));
#59316=CARTESIAN_POINT('Ctrl Pts',(1.76191490428566,97.8817773830784,12.6095785813307));
#59317=CARTESIAN_POINT('Ctrl Pts',(1.79316542671293,97.8922670550735,12.6879901979561));
#59318=CARTESIAN_POINT('Ctrl Pts',(1.81910715435611,97.9028856558508,12.7686162639768));
#59319=CARTESIAN_POINT('Ctrl Pts',(1.83960776096729,97.9135411552663,12.8506684014478));
#59320=CARTESIAN_POINT('Ctrl Pts',(1.84804109783546,97.9179245092701,12.884422198551));
#59321=CARTESIAN_POINT('Ctrl Pts',(1.85555397315441,97.9223140597097,12.9184167872872));
#59322=CARTESIAN_POINT('Ctrl Pts',(1.86213869323708,97.9267032033215,12.9525952536877));
#59323=CARTESIAN_POINT('Ctrl Pts',(1.88122198474518,97.939423456569,13.0516484601161));
#59324=CARTESIAN_POINT('Ctrl Pts',(1.8925131317968,97.9521388029293,13.1522571128828));
#59325=CARTESIAN_POINT('Ctrl Pts',(1.89585194995449,97.9647097334425,13.2532002880244));
#59326=CARTESIAN_POINT('Ctrl Pts',(1.89908136035533,97.9768687345711,13.3508357159814));
#59327=CARTESIAN_POINT('Ctrl Pts',(1.89487040675864,97.9888961908162,13.4488127390259));
#59328=CARTESIAN_POINT('Ctrl Pts',(1.88321720173359,98.0009377480042,13.5459564284894));
#59329=CARTESIAN_POINT('Ctrl Pts',(1.88062458085643,98.003616769998,13.5675690884268));
#59330=CARTESIAN_POINT('Ctrl Pts',(1.87766353102134,98.0062965178051,13.5891406967765));
#59331=CARTESIAN_POINT('Ctrl Pts',(1.87433391400233,98.0089786424861,13.6106586388472));
#59332=CARTESIAN_POINT('Ctrl Pts',(1.86188033756779,98.0190104402967,13.6911409690258));
#59333=CARTESIAN_POINT('Ctrl Pts',(1.84426925603202,98.0290755093867,13.7708615208926));
#59334=CARTESIAN_POINT('Ctrl Pts',(1.82153079495272,98.0392443933049,13.8490694515221));
#59335=CARTESIAN_POINT('Ctrl Pts',(1.82153060951391,98.0392444762351,13.8490700893307));
#59336=CARTESIAN_POINT('Ctrl Pts',(1.82153042407478,98.0392445591653,13.8490707271391));
#59337=CARTESIAN_POINT('Ctrl Pts',(1.82153023863529,98.0392446420956,13.8490713649475));
#59338=CARTESIAN_POINT('Ctrl Pts',(1.79669839808222,98.0503496690028,13.9344790411315));
#59339=CARTESIAN_POINT('Ctrl Pts',(1.76573754278492,98.061598231716,14.0181644050579));
#59340=CARTESIAN_POINT('Ctrl Pts',(1.72905504094309,98.072828361964,14.0993655503024));
#59341=CARTESIAN_POINT('Ctrl Pts',(1.71735742975068,98.0764095162116,14.1252596245274));
#59342=CARTESIAN_POINT('Ctrl Pts',(1.70507822047769,98.079988746162,14.1509007561787));
#59343=CARTESIAN_POINT('Ctrl Pts',(1.69223134657825,98.0835606620397,14.1762634153602));
#59344=CARTESIAN_POINT('Ctrl Pts',(1.63960277065782,98.0981933927275,14.2801642277076));
#59345=CARTESIAN_POINT('Ctrl Pts',(1.57742320284422,98.112709580116,14.3794469289553));
#59346=CARTESIAN_POINT('Ctrl Pts',(1.50679347614601,98.1271985721253,14.472525352511));
#59347=CARTESIAN_POINT('Ctrl Pts',(1.4994630010331,98.1287023468148,14.4821857193186));
#59348=CARTESIAN_POINT('Ctrl Pts',(1.49204145614255,98.130205832455,14.4917792536687));
#59349=CARTESIAN_POINT('Ctrl Pts',(1.48453004020065,98.1317091316073,14.5013041789783));
#59350=CARTESIAN_POINT('Ctrl Pts',(1.41674058875893,98.1452761908243,14.5872652636464));
#59351=CARTESIAN_POINT('Ctrl Pts',(1.34163048417663,98.1588298766215,14.667634774901));
#59352=CARTESIAN_POINT('Ctrl Pts',(1.26017484902886,98.1724340366167,14.7410255875902));
#59353=CARTESIAN_POINT('Ctrl Pts',(1.24631731984343,98.1747484258401,14.7535110998195));
#59354=CARTESIAN_POINT('Ctrl Pts',(1.23227618425927,98.1770642830045,14.765794746951));
#59355=CARTESIAN_POINT('Ctrl Pts',(1.21805629252046,98.1793819310667,14.7778698418999));
#59356=CARTESIAN_POINT('Ctrl Pts',(1.18028855227559,98.1855375566931,14.8099410459457));
#59357=CARTESIAN_POINT('Ctrl Pts',(1.14126131994144,98.1917053619478,14.8405392166875));
#59358=CARTESIAN_POINT('Ctrl Pts',(1.10107288945578,98.1978892643502,14.8695362388996));
#59359=CARTESIAN_POINT('Ctrl Pts',(1.10107163047069,98.1978894580737,14.8695371472908));
#59360=CARTESIAN_POINT('Ctrl Pts',(1.10107037148441,98.1978896517971,14.8695380556806));
#59361=CARTESIAN_POINT('Ctrl Pts',(1.10106911249695,98.1978898455206,14.8695389640687));
#59362=CARTESIAN_POINT('Ctrl Pts',(1.08999497411366,98.1995938503551,14.877529207575));
#59363=CARTESIAN_POINT('Ctrl Pts',(1.07883106803453,98.2012995077411,14.8853991677259));
#59364=CARTESIAN_POINT('Ctrl Pts',(1.06758025653102,98.2030060995129,14.893147481334));
#59365=CARTESIAN_POINT('Ctrl Pts',(0.966358762533452,98.2183599936496,14.9628576421641));
#59366=CARTESIAN_POINT('Ctrl Pts',(0.8581056922415,98.2337880700468,15.0227161239156));
#59367=CARTESIAN_POINT('Ctrl Pts',(0.745006988691363,98.2492258523374,15.0719571136518));
#59368=CARTESIAN_POINT('Ctrl Pts',(0.631369164669553,98.2647372236631,15.1214328260222));
#59369=CARTESIAN_POINT('Ctrl Pts',(0.512840164194871,98.280257780815,15.1601937414373));
#59370=CARTESIAN_POINT('Ctrl Pts',(0.391584713061079,98.2957470338434,15.1874950289018));
#59371=CARTESIAN_POINT('Ctrl Pts',(0.318389028749424,98.3050970998759,15.2039754130814));
#59372=CARTESIAN_POINT('Ctrl Pts',(0.244198641903657,98.3144362830383,15.2162803197437));
#59373=CARTESIAN_POINT('Ctrl Pts',(0.169480875927792,98.3237613047438,15.2242422448514));
#59374=CARTESIAN_POINT('Ctrl Pts',(0.0861780938318283,98.3341577645554,
15.2331189892728));
#59375=CARTESIAN_POINT('Ctrl Pts',(0.00220769556974054,98.3445394959874,
15.236594405874));
#59376=CARTESIAN_POINT('Ctrl Pts',(-0.0816538360917527,98.3549879395243,
15.2344770340646));
#59377=CARTESIAN_POINT('Ctrl Pts',(-0.0895298655725071,98.355969226745,
15.2342781767046));
#59378=CARTESIAN_POINT('Ctrl Pts',(-0.0974049476914433,98.3569511040135,
15.234030024446));
#59379=CARTESIAN_POINT('Ctrl Pts',(-0.105278447982589,98.3579336397859,
15.2337324409201));
#59380=CARTESIAN_POINT('Ctrl Pts',(-0.105280137831452,98.3579338506625,
15.2337323770513));
#59381=CARTESIAN_POINT('Ctrl Pts',(-0.105281827680237,98.3579340615391,
15.2337323131802));
#59382=CARTESIAN_POINT('Ctrl Pts',(-0.105283517529021,98.3579342724158,
15.2337322493068));
#59383=CARTESIAN_POINT('Ctrl Pts',(-0.196236757805741,98.3692843519231,
15.230294373682));
#59384=CARTESIAN_POINT('Ctrl Pts',(-0.287078604914497,98.380764542737,15.2202640739733));
#59385=CARTESIAN_POINT('Ctrl Pts',(-0.376875246424487,98.3922550241297,
15.2039088174115));
#59386=CARTESIAN_POINT('Ctrl Pts',(-0.387994247358728,98.393677824261,15.2018836401896));
#59387=CARTESIAN_POINT('Ctrl Pts',(-0.399097201379292,98.3951007782829,
15.1997615477108));
#59388=CARTESIAN_POINT('Ctrl Pts',(-0.410182320594743,98.3965236554648,
15.1975431005546));
#59389=CARTESIAN_POINT('Ctrl Pts',(-0.458552898082515,98.4027324647383,
15.1878627743453));
#59390=CARTESIAN_POINT('Ctrl Pts',(-0.50658797540966,98.4089401094051,15.1763470910284));
#59391=CARTESIAN_POINT('Ctrl Pts',(-0.55415873369442,98.4151299300796,15.1630371011503));
#59392=CARTESIAN_POINT('Ctrl Pts',(-0.653347259642252,98.4280361609391,
15.1352847943973));
#59393=CARTESIAN_POINT('Ctrl Pts',(-0.750534462141843,98.4408656260839,
15.0997304289456));
#59394=CARTESIAN_POINT('Ctrl Pts',(-0.844558781017521,98.4536866342342,
15.0567776350573));
#59395=CARTESIAN_POINT('Ctrl Pts',(-0.938273398623484,98.4664654120068,
15.0139663208943));
#59396=CARTESIAN_POINT('Ctrl Pts',(-1.0288433211155,98.4792371418048,14.963798187976));
#59397=CARTESIAN_POINT('Ctrl Pts',(-1.11497562087733,98.4920574584708,14.9067308503489));
#59398=CARTESIAN_POINT('Ctrl Pts',(-1.17676837065842,98.5012549676751,14.865789789627));
#59399=CARTESIAN_POINT('Ctrl Pts',(-1.23627335466819,98.5104772704496,14.8212989097111));
#59400=CARTESIAN_POINT('Ctrl Pts',(-1.29298640342411,98.5197355057998,14.7734746819127));
#59401=CARTESIAN_POINT('Ctrl Pts',(-1.29298818097518,98.5197357959797,14.773473182963));
#59402=CARTESIAN_POINT('Ctrl Pts',(-1.29298995852352,98.5197360861597,14.7734716840101));
#59403=CARTESIAN_POINT('Ctrl Pts',(-1.29299173606918,98.5197363763397,14.7734701850538));
#59404=CARTESIAN_POINT('Ctrl Pts',(-1.38337910074375,98.5344918958645,14.6972489603198));
#59405=CARTESIAN_POINT('Ctrl Pts',(-1.46678149799099,98.5494536768941,14.6125203526301));
#59406=CARTESIAN_POINT('Ctrl Pts',(-1.54211853187568,98.5643546623537,14.5208660303085));
#59407=CARTESIAN_POINT('Ctrl Pts',(-1.5486717060631,98.565650821072,14.5128935006211));
#59408=CARTESIAN_POINT('Ctrl Pts',(-1.55516409110504,98.5669465796977,14.5048682835478));
#59409=CARTESIAN_POINT('Ctrl Pts',(-1.56159508914682,98.5682417993886,14.4967912458765));
#59410=CARTESIAN_POINT('Ctrl Pts',(-1.63616755869191,98.5832608882342,14.4031316549639));
#59411=CARTESIAN_POINT('Ctrl Pts',(-1.70250070767046,98.5982088276308,14.3024918863326));
#59412=CARTESIAN_POINT('Ctrl Pts',(-1.75950459074744,98.6131622539348,14.1964906056999));
#59413=CARTESIAN_POINT('Ctrl Pts',(-1.80886624811544,98.6261109491088,14.1047003869863));
#59414=CARTESIAN_POINT('Ctrl Pts',(-1.85122540847539,98.6390647369957,14.0088871266353));
#59415=CARTESIAN_POINT('Ctrl Pts',(-1.88581619914007,98.6520550379284,13.9102265519788));
#59416=CARTESIAN_POINT('Ctrl Pts',(-1.89079028899205,98.6539230184747,13.8960393491494));
#59417=CARTESIAN_POINT('Ctrl Pts',(-1.89560382633042,98.655791755085,13.8817933042435));
#59418=CARTESIAN_POINT('Ctrl Pts',(-1.90025461792823,98.657661342201,13.8674919433306));
#59419=CARTESIAN_POINT('Ctrl Pts',(-1.92176803375755,98.6663095914743,13.8013373720549));
#59420=CARTESIAN_POINT('Ctrl Pts',(-1.93979592581145,98.6749753880474,13.7340024237611));
#59421=CARTESIAN_POINT('Ctrl Pts',(-1.95412537357618,98.6836614942994,13.6658673102719));
#59422=CARTESIAN_POINT('Ctrl Pts',(-1.95412619333049,98.6836619912113,13.6658634124208));
#59423=CARTESIAN_POINT('Ctrl Pts',(-1.95412701307277,98.6836624881233,13.6658595145669));
#59424=CARTESIAN_POINT('Ctrl Pts',(-1.954127832803,98.6836629850355,13.66585561671));
#59425=CARTESIAN_POINT('Ctrl Pts',(-1.95869657896549,98.6864325124844,13.6441310082917));
#59426=CARTESIAN_POINT('Ctrl Pts',(-1.9628912897172,98.6892056382613,13.6223172263087));
#59427=CARTESIAN_POINT('Ctrl Pts',(-1.96671237321969,98.6919808767534,13.600427835094));
#59428=CARTESIAN_POINT('Ctrl Pts',(-1.98732041921042,98.7069484225933,13.4823729481577));
#59429=CARTESIAN_POINT('Ctrl Pts',(-1.99705812785772,98.7219762330531,13.3621230330987));
#59430=CARTESIAN_POINT('Ctrl Pts',(-1.99607641639472,98.737030524678,13.2416925988717));
#59431=CARTESIAN_POINT('Ctrl Pts',(-1.99508560520575,98.7522243582495,13.1201458652111));
#59432=CARTESIAN_POINT('Ctrl Pts',(-1.98317976262498,98.7674451627657,12.9984139576203));
#59433=CARTESIAN_POINT('Ctrl Pts',(-1.96051531540606,98.7826761714344,12.8784999684021));
#59434=CARTESIAN_POINT('Ctrl Pts',(-1.94328165112652,98.7942575741265,12.7873193888519));
#59435=CARTESIAN_POINT('Ctrl Pts',(-1.91982766407115,98.8058452838051,12.6971879433377));
#59436=CARTESIAN_POINT('Ctrl Pts',(-1.89020449960675,98.817438351822,12.6089713671772));
#59437=CARTESIAN_POINT('Ctrl Pts',(-1.86337948525766,98.8279363597669,12.5290875679911));
#59438=CARTESIAN_POINT('Ctrl Pts',(-1.83148685794366,98.8384408144044,12.4507650277481));
#59439=CARTESIAN_POINT('Ctrl Pts',(-1.79462643332624,98.8489816702695,12.374765893803));
#59440=CARTESIAN_POINT('Ctrl Pts',(-1.79345888505005,98.8493155502565,12.3723586329331));
#59441=CARTESIAN_POINT('Ctrl Pts',(-1.79228636127879,98.8496494649769,12.3699537110507));
#59442=CARTESIAN_POINT('Ctrl Pts',(-1.79110886665425,98.8499834152402,12.3675511530638));
#59443=CARTESIAN_POINT('Ctrl Pts',(-1.79110633219145,98.8499841340413,12.3675459817503));
#59444=CARTESIAN_POINT('Ctrl Pts',(-1.79110379770541,98.8499848528427,12.3675408104473));
#59445=CARTESIAN_POINT('Ctrl Pts',(-1.79110126319609,98.8499855716444,12.3675356391548));
#59446=CARTESIAN_POINT('Ctrl Pts',(-1.74887751576844,98.8619604724573,12.2813843088857));
#59447=CARTESIAN_POINT('Ctrl Pts',(-1.700191678123,98.8739967806476,12.1981396898583));
#59448=CARTESIAN_POINT('Ctrl Pts',(-1.645748687921,98.8860580721743,12.1186180955533));
#59449=CARTESIAN_POINT('Ctrl Pts',(-1.63299796783116,98.888882864707,12.0999938872518));
#59450=CARTESIAN_POINT('Ctrl Pts',(-1.61993166374205,98.8917090258783,12.0815737899685));
#59451=CARTESIAN_POINT('Ctrl Pts',(-1.60655918315871,98.8945360847195,12.0633680814703));
#59452=CARTESIAN_POINT('Ctrl Pts',(-1.53875885600299,98.9088696642773,11.9710626199226));
#59453=CARTESIAN_POINT('Ctrl Pts',(-1.46309077473602,98.9232257701794,11.884264458137));
#59454=CARTESIAN_POINT('Ctrl Pts',(-1.38062901541154,98.9375749952128,11.8041346915348));
#59455=CARTESIAN_POINT('Ctrl Pts',(-1.37606804181495,98.9383686532313,11.7997027008428));
#59456=CARTESIAN_POINT('Ctrl Pts',(-1.37148627429814,98.9391622901798,11.7952911180463));
#59457=CARTESIAN_POINT('Ctrl Pts',(-1.36688389103222,98.9399559010773,11.7909001425279));
#59458=CARTESIAN_POINT('Ctrl Pts',(-1.35817186874008,98.9414581566329,11.7825883018162));
#59459=CARTESIAN_POINT('Ctrl Pts',(-1.34938582819855,98.9429603522622,11.7743501579612));
#59460=CARTESIAN_POINT('Ctrl Pts',(-1.34052686707804,98.9444624762572,11.7661869849063));
#59461=CARTESIAN_POINT('Ctrl Pts',(-1.25172850800733,98.9595191114618,11.6843629016738));
#59462=CARTESIAN_POINT('Ctrl Pts',(-1.1555785484111,98.9745726509216,11.6100489305369));
#59463=CARTESIAN_POINT('Ctrl Pts',(-1.05335786448829,98.9896624341179,11.5447106820709));
#59464=CARTESIAN_POINT('Ctrl Pts',(-0.987469521576181,98.9993888492773,
11.5025956349493));
#59465=CARTESIAN_POINT('Ctrl Pts',(-0.919064266961413,99.0091293501279,
11.4642171790027));
#59466=CARTESIAN_POINT('Ctrl Pts',(-0.848573143922676,99.0188824801348,
11.4299952775465));
#59467=CARTESIAN_POINT('Ctrl Pts',(-0.848567958395836,99.0188831976027,
11.4299927600864));
#59468=CARTESIAN_POINT('Ctrl Pts',(-0.84856277285726,99.0188839150707,11.4299902426485));
#59469=CARTESIAN_POINT('Ctrl Pts',(-0.848557587307047,99.018884632539,11.429987725233));
#59470=CARTESIAN_POINT('Ctrl Pts',(-0.748837726886114,99.0326817855019,
11.3815769847876));
#59471=CARTESIAN_POINT('Ctrl Pts',(-0.644794435651932,99.0465373107453,
11.3414081760795));
#59472=CARTESIAN_POINT('Ctrl Pts',(-0.537965648557116,99.0604173137764,
11.3097658392848));
#59473=CARTESIAN_POINT('Ctrl Pts',(-0.527140572212493,99.0618237894704,
11.3065594871317));
#59474=CARTESIAN_POINT('Ctrl Pts',(-0.516286909372726,99.0632305162845,
11.3034406432814));
#59475=CARTESIAN_POINT('Ctrl Pts',(-0.505406268621373,99.0646374588121,
11.3004095754447));
#59476=CARTESIAN_POINT('Ctrl Pts',(-0.484768089040163,99.0673061189774,
11.2946603072017));
#59477=CARTESIAN_POINT('Ctrl Pts',(-0.464031602062175,99.0699757227276,
11.2892264770465));
#59478=CARTESIAN_POINT('Ctrl Pts',(-0.443206192442698,99.0726462392845,
11.2841096394152));
#59479=CARTESIAN_POINT('Ctrl Pts',(-0.324308376627887,99.0878929302988,
11.25489624917));
#59480=CARTESIAN_POINT('Ctrl Pts',(-0.202497790263523,99.1031711376377,
11.2360127819059));
#59481=CARTESIAN_POINT('Ctrl Pts',(-0.0797155686824385,99.1184889367771,
11.2278125167363));
#59482=CARTESIAN_POINT('Ctrl Pts',(-0.0726784790510279,99.1193668548023,
11.2273425301188));
#59483=CARTESIAN_POINT('Ctrl Pts',(-0.065638240207429,99.1202448976162,
11.2269076377068));
#59484=CARTESIAN_POINT('Ctrl Pts',(-0.0585952329236468,99.1211230648279,
11.2265079049832));
#59485=CARTESIAN_POINT('Ctrl Pts',(0.062732712974499,99.1362510094189,11.2196218194921));
#59486=CARTESIAN_POINT('Ctrl Pts',(0.184890897368926,99.1514171321329,11.2231670003939));
#59487=CARTESIAN_POINT('Ctrl Pts',(0.306055934128646,99.166611611458,11.237487058001));
#59488=CARTESIAN_POINT('Ctrl Pts',(0.314699380078351,99.1676955269529,11.2385085956264));
#59489=CARTESIAN_POINT('Ctrl Pts',(0.32333772377812,99.1687795796955,11.2395849710132));
#59490=CARTESIAN_POINT('Ctrl Pts',(0.33197028002139,99.1698637627013,11.2407163092596));
#59491=CARTESIAN_POINT('Ctrl Pts',(0.386420873240079,99.1767023405413,11.2478523228468));
#59492=CARTESIAN_POINT('Ctrl Pts',(0.440642990526318,99.1835463287813,11.2571762344221));
#59493=CARTESIAN_POINT('Ctrl Pts',(0.494433566894493,99.1903909774577,11.2687102385151));
#59494=CARTESIAN_POINT('Ctrl Pts',(0.494434332164162,99.1903910748354,11.2687104026075));
#59495=CARTESIAN_POINT('Ctrl Pts',(0.494435097433744,99.1903911722131,11.2687105667003));
#59496=CARTESIAN_POINT('Ctrl Pts',(0.494435862703259,99.1903912695907,11.2687107307936));
#59497=CARTESIAN_POINT('Ctrl Pts',(0.583481658251176,99.2017220150766,11.2878044172989));
#59498=CARTESIAN_POINT('Ctrl Pts',(0.671484670266375,99.213075632491,11.3129866647636));
#59499=CARTESIAN_POINT('Ctrl Pts',(0.757644214645959,99.2244520508583,11.3438670371024));
#59500=CARTESIAN_POINT('Ctrl Pts',(0.785045848831569,99.2280701346897,11.3536880345605));
#59501=CARTESIAN_POINT('Ctrl Pts',(0.812261106649497,99.2316905230872,11.364084980821));
#59502=CARTESIAN_POINT('Ctrl Pts',(0.839264541734818,99.2353132089604,11.375044266686));
#59503=CARTESIAN_POINT('Ctrl Pts',(0.920341263355562,99.246190176766,11.4079490792193));
#59504=CARTESIAN_POINT('Ctrl Pts',(0.999515454592334,99.2570889340257,11.445924826957));
#59505=CARTESIAN_POINT('Ctrl Pts',(1.0761967882515,99.2680232652008,11.4886436863882));
#59506=CARTESIAN_POINT('Ctrl Pts',(1.17263218746403,99.2817744161221,11.5423674554799));
#59507=CARTESIAN_POINT('Ctrl Pts',(1.26515178344775,99.2955859302042,11.6036043442725));
#59508=CARTESIAN_POINT('Ctrl Pts',(1.3526095427359,99.3094356944523,11.6717679947235));
#59509=CARTESIAN_POINT('Ctrl Pts',(1.36154320244813,99.3108504240532,11.6787307943976));
#59510=CARTESIAN_POINT('Ctrl Pts',(1.37042401857231,99.3122655531071,11.6857659057565));
#59511=CARTESIAN_POINT('Ctrl Pts',(1.37925074973229,99.313681058288,11.6928727277097));
#59512=CARTESIAN_POINT('Ctrl Pts',(1.45913776652313,99.3264921980074,11.757193572473));
#59513=CARTESIAN_POINT('Ctrl Pts',(1.53459254995152,99.3393338010028,11.8273923622317));
#59514=CARTESIAN_POINT('Ctrl Pts',(1.60458603251227,99.352165974687,11.9029059606615));
#59515=CARTESIAN_POINT('Ctrl Pts',(1.61693751847119,99.3544304199937,11.9162315606544));
#59516=CARTESIAN_POINT('Ctrl Pts',(1.62911902663242,99.3566945718676,11.9297225692549));
#59517=CARTESIAN_POINT('Ctrl Pts',(1.64112502549409,99.3589582113924,11.9433757736953));
#59518=CARTESIAN_POINT('Ctrl Pts',(1.65216477562623,99.3610396720882,11.9559301614861));
#59519=CARTESIAN_POINT('Ctrl Pts',(1.6630558483895,99.3631206503809,11.9686213732987));
#59520=CARTESIAN_POINT('Ctrl Pts',(1.67379374264166,99.365200932442,11.9814465471939));
#59521=CARTESIAN_POINT('Ctrl Pts',(1.67380835861525,99.3652037640351,11.9814640042854));
#59522=CARTESIAN_POINT('Ctrl Pts',(1.67382297430502,99.3652065956269,11.9814814616252));
#59523=CARTESIAN_POINT('Ctrl Pts',(1.67383758971101,99.3652094272175,11.9814989192131));
#59524=CARTESIAN_POINT('Ctrl Pts',(1.67768434523775,99.3659546981063,11.9860937332597));
#59525=CARTESIAN_POINT('Ctrl Pts',(1.68151185425506,99.3666999811197,11.9907062370342));
#59526=CARTESIAN_POINT('Ctrl Pts',(1.68532000044771,99.3674452826907,11.9953362194907));
#59527=CARTESIAN_POINT('Ctrl Pts',(1.74387883110136,99.3789059741336,12.0665326349854));
#59528=CARTESIAN_POINT('Ctrl Pts',(1.79784641496243,99.3903686577716,12.1418534154281));
#59529=CARTESIAN_POINT('Ctrl Pts',(1.84681756557283,99.401863028944,12.2205000922566));
#59530=CARTESIAN_POINT('Ctrl Pts',(1.86205035663532,99.4054384269545,12.24496364643));
#59531=CARTESIAN_POINT('Ctrl Pts',(1.87679999799802,99.4090168869979,12.2697487469405));
#59532=CARTESIAN_POINT('Ctrl Pts',(1.8910551057942,99.4125992916037,12.294830743662));
#59533=CARTESIAN_POINT('Ctrl Pts',(1.95110900255702,99.4276912403589,12.4004961418657));
#59534=CARTESIAN_POINT('Ctrl Pts',(2.00238675861918,99.4428738848819,12.5114282785142));
#59535=CARTESIAN_POINT('Ctrl Pts',(2.04421079468902,99.4580904602187,12.6260585904732));
#59536=CARTESIAN_POINT('Ctrl Pts',(2.05297957054067,99.4612807486484,12.6500918403894));
#59537=CARTESIAN_POINT('Ctrl Pts',(2.06133304005819,99.4644726596183,12.6742887381014));
#59538=CARTESIAN_POINT('Ctrl Pts',(2.06926498832166,99.4676664859055,12.6986365937338));
#59539=CARTESIAN_POINT('Ctrl Pts',(2.10723158690889,99.4829538675894,12.8151786122328));
#59540=CARTESIAN_POINT('Ctrl Pts',(2.13552515695722,99.4984499739216,12.9352164099709));
#59541=CARTESIAN_POINT('Ctrl Pts',(2.15337815930707,99.5139729306774,13.057151698573));
#59542=CARTESIAN_POINT('Ctrl Pts',(2.16485500934828,99.5239519047116,13.1355381231415));
#59543=CARTESIAN_POINT('Ctrl Pts',(2.17201203177395,99.5339359392258,13.2146990788338));
#59544=CARTESIAN_POINT('Ctrl Pts',(2.17465225662852,99.5438758174746,13.2940922511326));
#59545=CARTESIAN_POINT('Ctrl Pts',(2.17465250999375,99.5438767713402,13.2940998699797));
#59546=CARTESIAN_POINT('Ctrl Pts',(2.17465276331743,99.5438777252053,13.2941074888289));
#59547=CARTESIAN_POINT('Ctrl Pts',(2.17465301659955,99.54387867907,13.2941151076802));
#59548=CARTESIAN_POINT('Ctrl Pts',(2.17733544349689,99.5539807441159,13.3748038348931));
#59549=CARTESIAN_POINT('Ctrl Pts',(2.17536218380245,99.5640491175395,13.4559394106849));
#59550=CARTESIAN_POINT('Ctrl Pts',(2.1688311785283,99.5741025981913,13.5369052169983));
#59551=CARTESIAN_POINT('Ctrl Pts',(2.16710917366223,99.5767533604976,13.5582531575687));
#59552=CARTESIAN_POINT('Ctrl Pts',(2.16507059489321,99.5794030846536,13.5795892556402));
#59553=CARTESIAN_POINT('Ctrl Pts',(2.16271783205606,99.5820521090332,13.6009021558878));
#59554=CARTESIAN_POINT('Ctrl Pts',(2.15133149971718,99.5948722163059,13.7040471739456));
#59555=CARTESIAN_POINT('Ctrl Pts',(2.13258283001489,99.607679571714,13.8066505407393));
#59556=CARTESIAN_POINT('Ctrl Pts',(2.10673035469947,99.6206636446915,13.9075658443977));
#59557=CARTESIAN_POINT('Ctrl Pts',(2.08570540303654,99.63122315605,13.9896368784315));
#59558=CARTESIAN_POINT('Ctrl Pts',(2.06000808575108,99.6417930747003,14.0706069478822));
#59559=CARTESIAN_POINT('Ctrl Pts',(2.0297813703537,99.6523784596769,14.1499580976884));
#59560=CARTESIAN_POINT('Ctrl Pts',(2.01097046577524,99.6589660317669,14.199340469791));
#59561=CARTESIAN_POINT('Ctrl Pts',(1.99040590211624,99.6655593707656,14.2480942993227));
#59562=CARTESIAN_POINT('Ctrl Pts',(1.96811302571224,99.6721612472383,14.2961051261221));
#59563=CARTESIAN_POINT('Ctrl Pts',(1.92430869073101,99.6851335888631,14.3904438871565));
#59564=CARTESIAN_POINT('Ctrl Pts',(1.87381620266567,99.6981423334792,14.4819377217618));
#59565=CARTESIAN_POINT('Ctrl Pts',(1.81688138065531,99.7112427268971,14.5695059311583));
#59566=CARTESIAN_POINT('Ctrl Pts',(1.79588465351929,99.7160739598097,14.6017998021772));
#59567=CARTESIAN_POINT('Ctrl Pts',(1.77401026281012,99.7209346584008,14.6335529471061));
#59568=CARTESIAN_POINT('Ctrl Pts',(1.75128585840563,99.7257868596548,14.6647124589427));
#59569=CARTESIAN_POINT('Ctrl Pts',(1.75123939456334,99.7257967807911,14.6647761697718));
#59570=CARTESIAN_POINT('Ctrl Pts',(1.75119292716784,99.725806701892,14.6648398781203));
#59571=CARTESIAN_POINT('Ctrl Pts',(1.75114645621964,99.7258166229571,14.6649035839879));
#59572=CARTESIAN_POINT('Ctrl Pts',(1.69420145669655,99.7379737893328,14.7429680682209));
#59573=CARTESIAN_POINT('Ctrl Pts',(1.63180444131572,99.7500896128888,14.8174668607998));
#59574=CARTESIAN_POINT('Ctrl Pts',(1.56463978125246,99.7621883077862,14.8877746218344));
#59575=CARTESIAN_POINT('Ctrl Pts',(1.52240421213,99.7697964050229,14.9319866866051));
#59576=CARTESIAN_POINT('Ctrl Pts',(1.47828438596298,99.7773977137962,14.97454186018));
#59577=CARTESIAN_POINT('Ctrl Pts',(1.43245938870037,99.784998085906,15.0152901982427));
#59578=CARTESIAN_POINT('Ctrl Pts',(1.31889443393477,99.803833567988,15.1162740159252));
#59579=CARTESIAN_POINT('Ctrl Pts',(1.19483881768242,99.8228290554776,15.2061128570069));
#59580=CARTESIAN_POINT('Ctrl Pts',(1.06279457934823,99.8418819585718,15.2828918450947));
#59581=CARTESIAN_POINT('Ctrl Pts',(1.05466051134674,99.8430556380246,15.2876215138639));
#59582=CARTESIAN_POINT('Ctrl Pts',(1.04649611401815,99.8442295364327,15.2923016312756));
#59583=CARTESIAN_POINT('Ctrl Pts',(1.03830196624621,99.8454036302503,15.2969317521906));
#59584=CARTESIAN_POINT('Ctrl Pts',(0.954433305329069,99.8574207037783,15.3443219203741));
#59585=CARTESIAN_POINT('Ctrl Pts',(0.867441690335356,99.8694593707389,15.3864821264533));
#59586=CARTESIAN_POINT('Ctrl Pts',(0.777865883180836,99.8815301958095,15.4229426509981));
#59587=CARTESIAN_POINT('Ctrl Pts',(0.712348864663079,99.890358968832,15.4496103968734));
#59588=CARTESIAN_POINT('Ctrl Pts',(0.645437412417385,99.899206361356,15.4732296160634));
#59589=CARTESIAN_POINT('Ctrl Pts',(0.577432620505872,99.9080652754043,15.493579863064));
#59590=CARTESIAN_POINT('Ctrl Pts',(0.568105477213835,99.9092803127336,15.4963709850492));
#59591=CARTESIAN_POINT('Ctrl Pts',(0.558757828830809,99.9105007863209,15.4990985496394));
#59592=CARTESIAN_POINT('Ctrl Pts',(0.549390643273964,99.9117205036068,15.5017644278983));
#59593=CARTESIAN_POINT('Ctrl Pts',(0.549303760441458,99.9117318167693,15.5017891545414));
#59594=CARTESIAN_POINT('Ctrl Pts',(0.549216875927361,99.9117431298669,15.5018138758781));
#59595=CARTESIAN_POINT('Ctrl Pts',(0.549129989732626,99.9117544428946,15.5018385919101));
#59596=CARTESIAN_POINT('Ctrl Pts',(0.450557554638052,99.924589078939,15.5298789437017));
#59597=CARTESIAN_POINT('Ctrl Pts',(0.349697811882334,99.937366876107,15.5511163310684));
#59598=CARTESIAN_POINT('Ctrl Pts',(0.247623594733156,99.950198263937,15.5654747265406));
#59599=CARTESIAN_POINT('Ctrl Pts',(0.232582801106788,99.9520889887614,15.5675904583007));
#59600=CARTESIAN_POINT('Ctrl Pts',(0.217515698898134,99.9539808712478,15.5695568993481));
#59601=CARTESIAN_POINT('Ctrl Pts',(0.202425780047518,99.9558742584633,15.5713738805561));
#59602=CARTESIAN_POINT('Ctrl Pts',(0.117124253231252,99.9665773524916,15.5816450604592));
#59603=CARTESIAN_POINT('Ctrl Pts',(0.0310858230689608,99.9772955882342,
15.5871565204135));
#59604=CARTESIAN_POINT('Ctrl Pts',(-0.0551574262171184,99.9880340081795,
15.5879089851066));
#59605=CARTESIAN_POINT('Ctrl Pts',(-0.173253145552197,100.00273847999,15.5889393597729));
#59606=CARTESIAN_POINT('Ctrl Pts',(-0.291755310329019,100.017516805886,
15.5810316528577));
#59607=CARTESIAN_POINT('Ctrl Pts',(-0.409204178600894,100.032500685822,
15.5640881905311));
#59608=CARTESIAN_POINT('Ctrl Pts',(-0.523525503977769,100.047085560403,
15.5475959152274));
#59609=CARTESIAN_POINT('Ctrl Pts',(-0.636861243755178,100.061746925084,
15.5225878453474));
#59610=CARTESIAN_POINT('Ctrl Pts',(-0.747795796437421,100.07638777261,15.4890900970245));
#59611=CARTESIAN_POINT('Ctrl Pts',(-0.799676054300541,100.083234791204,
15.4734243573716));
#59612=CARTESIAN_POINT('Ctrl Pts',(-0.851029851688863,100.090077086273,
15.4559027336504));
#59613=CARTESIAN_POINT('Ctrl Pts',(-0.901706648082814,100.096904017119,
15.4365349514725));
#59614=CARTESIAN_POINT('Ctrl Pts',(-0.916450353441402,100.098890217196,
15.4309001660441));
#59615=CARTESIAN_POINT('Ctrl Pts',(-0.931136742687463,100.100875116686,
15.4251091506041));
#59616=CARTESIAN_POINT('Ctrl Pts',(-0.945762089483852,100.102857986619,
15.4191624762268));
#59617=CARTESIAN_POINT('Ctrl Pts',(-0.945778031059615,100.10286014794,15.4191559943729));
#59618=CARTESIAN_POINT('Ctrl Pts',(-0.945793972562841,100.102862309258,
15.4191495123342));
#59619=CARTESIAN_POINT('Ctrl Pts',(-0.945809913993562,100.102864470575,
15.4191430301105));
#59620=CARTESIAN_POINT('Ctrl Pts',(-1.04799977669469,100.116719225642,15.3775898244658));
#59621=CARTESIAN_POINT('Ctrl Pts',(-1.14738413899489,100.130483380395,15.3283701976069));
#59622=CARTESIAN_POINT('Ctrl Pts',(-1.2430104132479,100.144252397705,15.2721648231545));
#59623=CARTESIAN_POINT('Ctrl Pts',(-1.31364396260535,100.154422767422,15.2306491924186));
#59624=CARTESIAN_POINT('Ctrl Pts',(-1.38222670024172,100.164595719987,15.1853232548914));
#59625=CARTESIAN_POINT('Ctrl Pts',(-1.44837327938249,100.17480840503,15.1364794768139));
#59626=CARTESIAN_POINT('Ctrl Pts',(-1.51548974446611,100.185170835377,15.0869195181815));
#59627=CARTESIAN_POINT('Ctrl Pts',(-1.58011109425372,100.195577744006,15.0337298099532));
#59628=CARTESIAN_POINT('Ctrl Pts',(-1.64187900958763,100.206077098135,14.9771766118642));
#59629=CARTESIAN_POINT('Ctrl Pts',(-1.74258242110682,100.223194735566,14.8849750222672));
#59630=CARTESIAN_POINT('Ctrl Pts',(-1.83573088714695,100.240559926231,14.7838007788656));
#59631=CARTESIAN_POINT('Ctrl Pts',(-1.91975790605777,100.25803654293,14.675008534083));
#59632=CARTESIAN_POINT('Ctrl Pts',(-1.95224816775895,100.264794129448,14.6329424397497));
#59633=CARTESIAN_POINT('Ctrl Pts',(-1.98337523693324,100.271568434829,14.5897373495495));
#59634=CARTESIAN_POINT('Ctrl Pts',(-2.01305060062776,100.278351822717,14.5454711408116));
#59635=CARTESIAN_POINT('Ctrl Pts',(-2.04203376731463,100.284976983705,14.5022374699575));
#59636=CARTESIAN_POINT('Ctrl Pts',(-2.06962877181567,100.291610749388,14.4579956181135));
#59637=CARTESIAN_POINT('Ctrl Pts',(-2.09574884560272,100.298246765759,14.4128279128811));
#59638=CARTESIAN_POINT('Ctrl Pts',(-2.09575697155803,100.298248830224,14.4128138612074));
#59639=CARTESIAN_POINT('Ctrl Pts',(-2.09576509737053,100.298250894689,14.4127998094441));
#59640=CARTESIAN_POINT('Ctrl Pts',(-2.09577322304035,100.298252959155,14.4127857575909));
#59641=CARTESIAN_POINT('Ctrl Pts',(-2.12248343407465,100.305039145696,14.3665953544916));
#59642=CARTESIAN_POINT('Ctrl Pts',(-2.14765135421186,100.311829629413,14.3194351763449));
#59643=CARTESIAN_POINT('Ctrl Pts',(-2.17121629666769,100.31863605248,14.2714235530651));
#59644=CARTESIAN_POINT('Ctrl Pts',(-2.21830681840551,100.332237529079,14.1754805057199));
#59645=CARTESIAN_POINT('Ctrl Pts',(-2.25899867212424,100.345905410451,14.076136946669));
#59646=CARTESIAN_POINT('Ctrl Pts',(-2.2928898276478,100.359606310524,13.9742881567927));
#59647=CARTESIAN_POINT('Ctrl Pts',(-2.30621162432765,100.36499180424,13.9342538513858));
#59648=CARTESIAN_POINT('Ctrl Pts',(-2.3184824575564,100.370382006744,13.893832245958));
#59649=CARTESIAN_POINT('Ctrl Pts',(-2.32967708652519,100.375773321592,13.8530771968934));
#59650=CARTESIAN_POINT('Ctrl Pts',(-2.35437903891379,100.387669741123,13.7631475275495));
#59651=CARTESIAN_POINT('Ctrl Pts',(-2.37384061634741,100.399572478644,13.6715843293427));
#59652=CARTESIAN_POINT('Ctrl Pts',(-2.38782825765813,100.411334417878,13.5790799856954));
#59653=CARTESIAN_POINT('Ctrl Pts',(-2.39001701902716,100.413174905323,13.564605069636));
#59654=CARTESIAN_POINT('Ctrl Pts',(-2.39207182906872,100.415011955553,13.5501070441293));
#59655=CARTESIAN_POINT('Ctrl Pts',(-2.39399187955346,100.416845016453,13.5355884844563));
#59656=CARTESIAN_POINT('Ctrl Pts',(-2.39945831298096,100.42206378828,13.4942537692776));
#59657=CARTESIAN_POINT('Ctrl Pts',(-2.40383189474815,100.427249953131,13.4527549038664));
#59658=CARTESIAN_POINT('Ctrl Pts',(-2.40709471261336,100.432390402776,13.4111586367477));
#59659=CARTESIAN_POINT('Ctrl Pts',(-2.40709787622975,100.432395386937,13.4111183051577));
#59660=CARTESIAN_POINT('Ctrl Pts',(-2.4071010387989,100.43240037107,13.411077973439));
#59661=CARTESIAN_POINT('Ctrl Pts',(-2.40710420032078,100.432405355173,13.4110376415917));
#59662=CARTESIAN_POINT('Ctrl Pts',(-2.41381135753041,100.442979111809,13.3254737737003));
#59663=CARTESIAN_POINT('Ctrl Pts',(-2.41580151253102,100.453422042174,13.2393282676031));
#59664=CARTESIAN_POINT('Ctrl Pts',(-2.41313967918205,100.46382042649,13.1531670804234));
#59665=CARTESIAN_POINT('Ctrl Pts',(-2.41158529906977,100.469892572887,13.1028531733358));
#59666=CARTESIAN_POINT('Ctrl Pts',(-2.40844537421013,100.47594946381,13.0525345450383));
#59667=CARTESIAN_POINT('Ctrl Pts',(-2.40373978080333,100.482007711917,13.002328242712));
#59668=CARTESIAN_POINT('Ctrl Pts',(-2.39438755313016,100.494048300786,12.9025447022761));
#59669=CARTESIAN_POINT('Ctrl Pts',(-2.37885121677452,100.50609867673,12.8032014758413));
#59670=CARTESIAN_POINT('Ctrl Pts',(-2.35727131497552,100.518320450128,12.7050350944655));
#59671=CARTESIAN_POINT('Ctrl Pts',(-2.34872486511952,100.523160730426,12.6661575284882));
#59672=CARTESIAN_POINT('Ctrl Pts',(-2.33923035221702,100.528027818563,12.6274650930927));
#59673=CARTESIAN_POINT('Ctrl Pts',(-2.3287961596825,100.532931452916,12.589005765313));
#59674=CARTESIAN_POINT('Ctrl Pts',(-2.32160408235416,100.536311428639,12.562496530557));
#59675=CARTESIAN_POINT('Ctrl Pts',(-2.31396520449789,100.539708857728,12.536096340056));
#59676=CARTESIAN_POINT('Ctrl Pts',(-2.30588147887959,100.543126929759,12.5098188373672));
#59677=CARTESIAN_POINT('Ctrl Pts',(-2.2760356874277,100.555746737733,12.4128000984639));
#59678=CARTESIAN_POINT('Ctrl Pts',(-2.24012155072084,100.568652301366,12.3174378106301));
#59679=CARTESIAN_POINT('Ctrl Pts',(-2.19841568484051,100.581715205391,12.22440728038));
#59680=CARTESIAN_POINT('Ctrl Pts',(-2.18236550217605,100.586742363833,12.1886051942137));
#59681=CARTESIAN_POINT('Ctrl Pts',(-2.1654570885242,100.591792888321,12.1531481562251));
#59682=CARTESIAN_POINT('Ctrl Pts',(-2.14770437000184,100.59685970141,12.1180737365215));
#59683=CARTESIAN_POINT('Ctrl Pts',(-2.1024118139436,100.609786674572,12.028588280047));
#59684=CARTESIAN_POINT('Ctrl Pts',(-2.05162395767972,100.622816458876,11.9415966638525));
#59685=CARTESIAN_POINT('Ctrl Pts',(-1.99564331342835,100.635812319395,11.8578356081371));
#59686=CARTESIAN_POINT('Ctrl Pts',(-1.97414291619667,100.640803618928,11.8256656323444));
#59687=CARTESIAN_POINT('Ctrl Pts',(-1.95187664614289,100.645789976378,11.7939716615095));
#59688=CARTESIAN_POINT('Ctrl Pts',(-1.92886183642982,100.650763880935,11.76279339908));
#59689=CARTESIAN_POINT('Ctrl Pts',(-1.87960254668455,100.661409678523,11.6960616258473));
#59690=CARTESIAN_POINT('Ctrl Pts',(-1.82691430179624,100.671995963239,11.6316957175191));
#59691=CARTESIAN_POINT('Ctrl Pts',(-1.77102050030755,100.682456431535,11.5701340456267));
#59692=CARTESIAN_POINT('Ctrl Pts',(-1.73631729585265,100.688951101074,11.5319117878921));
#59693=CARTESIAN_POINT('Ctrl Pts',(-1.70037892184861,100.69539731069,11.4947697029924));
#59694=CARTESIAN_POINT('Ctrl Pts',(-1.66326310795707,100.701779597646,11.4588034785056));
#59695=CARTESIAN_POINT('Ctrl Pts',(-1.66323745244004,100.701784009266,11.4587786176178));
#59696=CARTESIAN_POINT('Ctrl Pts',(-1.66321179633677,100.701788420855,11.4587537572618));
#59697=CARTESIAN_POINT('Ctrl Pts',(-1.66318613964721,100.701792832411,11.4587288974377));
#59698=CARTESIAN_POINT('Ctrl Pts',(-1.60430288709543,100.71191755316,11.4016744868032));
#59699=CARTESIAN_POINT('Ctrl Pts',(-1.54232771466886,100.721876200575,11.3474197051733));
#59700=CARTESIAN_POINT('Ctrl Pts',(-1.47759943445463,100.731811060499,11.2962869777295));
#59701=CARTESIAN_POINT('Ctrl Pts',(-1.46304701463237,100.734044647612,11.2847911537411));
#59702=CARTESIAN_POINT('Ctrl Pts',(-1.44835562899329,100.736277008215,11.2734532147885));
#59703=CARTESIAN_POINT('Ctrl Pts',(-1.43352946771426,100.738509716868,11.2622769493372));
#59704=CARTESIAN_POINT('Ctrl Pts',(-1.36685292573567,100.748550703836,11.2120147999848));
#59705=CARTESIAN_POINT('Ctrl Pts',(-1.29744712026998,100.758600719898,11.1650194486941));
#59706=CARTESIAN_POINT('Ctrl Pts',(-1.22562892850108,100.76880321441,11.1215867895098));
#59707=CARTESIAN_POINT('Ctrl Pts',(-1.21074116223448,100.770918170939,11.1125832868826));
#59708=CARTESIAN_POINT('Ctrl Pts',(-1.19574983233038,100.77303965936,11.1037330267289));
#59709=CARTESIAN_POINT('Ctrl Pts',(-1.18065793506841,100.775168925174,11.0950388653619));
#59710=CARTESIAN_POINT('Ctrl Pts',(1.85693809316476,98.5858197253477,11.6266881416021));
#59711=CARTESIAN_POINT('Ctrl Pts',(1.91417673598575,98.5969468569167,11.6949465173591));
#59712=CARTESIAN_POINT('Ctrl Pts',(1.96773903937305,98.6079987826475,11.7661548820132));
#59713=CARTESIAN_POINT('Ctrl Pts',(2.01732925929512,98.6190075301634,11.8398678057961));
#59714=CARTESIAN_POINT('Ctrl Pts',(2.047604010715,98.6257283532412,11.8848694300571));
#59715=CARTESIAN_POINT('Ctrl Pts',(2.07639816329627,98.6324329822682,11.9308035091556));
#59716=CARTESIAN_POINT('Ctrl Pts',(2.10364433161086,98.6391277432176,11.9775591854309));
#59717=CARTESIAN_POINT('Ctrl Pts',(2.14800936196921,98.6500288456896,12.0536916152619));
#59718=CARTESIAN_POINT('Ctrl Pts',(2.1882598999595,98.6609084447206,12.1320088513954));
#59719=CARTESIAN_POINT('Ctrl Pts',(2.22411431958962,98.6718089272195,12.2120820155326));
#59720=CARTESIAN_POINT('Ctrl Pts',(2.24634745585678,98.6785682588522,12.2617349617515));
#59721=CARTESIAN_POINT('Ctrl Pts',(2.26688965691372,98.6853354878269,12.3120622309737));
#59722=CARTESIAN_POINT('Ctrl Pts',(2.2856700677231,98.6921194114877,12.3629522603032));
#59723=CARTESIAN_POINT('Ctrl Pts',(2.31285775264305,98.7019402392045,12.4366238161079));
#59724=CARTESIAN_POINT('Ctrl Pts',(2.33635867160346,98.7117988182997,12.5114924425386));
#59725=CARTESIAN_POINT('Ctrl Pts',(2.35618043222215,98.721649839398,12.5871735365766));
#59726=CARTESIAN_POINT('Ctrl Pts',(2.37113415918653,98.7290815445153,12.6442680822317));
#59727=CARTESIAN_POINT('Ctrl Pts',(2.38399444164648,98.736509079571,12.7018260119645));
#59728=CARTESIAN_POINT('Ctrl Pts',(2.39476779116759,98.7439154465351,12.7597014291137));
#59729=CARTESIAN_POINT('Ctrl Pts',(2.401226103283,98.7483553497799,12.7943960713906));
#59730=CARTESIAN_POINT('Ctrl Pts',(2.40693425238278,98.7527872203904,12.8292022708228));
#59731=CARTESIAN_POINT('Ctrl Pts',(2.41190643219563,98.7572035475463,12.8640867791556));
#59732=CARTESIAN_POINT('Ctrl Pts',(2.41190675506834,98.7572038343243,12.8640890444107));
#59733=CARTESIAN_POINT('Ctrl Pts',(2.41190707793795,98.7572041211021,12.8640913096662));
#59734=CARTESIAN_POINT('Ctrl Pts',(2.41190740080446,98.75720440788,12.864093574922));
#59735=CARTESIAN_POINT('Ctrl Pts',(2.42701541202014,98.7706237078314,12.9700925226681));
#59736=CARTESIAN_POINT('Ctrl Pts',(2.43514073546767,98.783968420195,13.0769193128911));
#59737=CARTESIAN_POINT('Ctrl Pts',(2.43638481590199,98.7972525916792,13.18362664369));
#59738=CARTESIAN_POINT('Ctrl Pts',(2.43700897416945,98.8039172937591,13.2371619786083));
#59739=CARTESIAN_POINT('Ctrl Pts',(2.4359016179274,98.8105666942635,13.2906665995291));
#59740=CARTESIAN_POINT('Ctrl Pts',(2.43307914839644,98.8172021819321,13.3440175316217));
#59741=CARTESIAN_POINT('Ctrl Pts',(2.42789700836977,98.8293851393977,13.4419714679263));
#59742=CARTESIAN_POINT('Ctrl Pts',(2.41690336065044,98.8415293527585,13.5394029421038));
#59743=CARTESIAN_POINT('Ctrl Pts',(2.40014414136372,98.8536652226893,13.6355897984486));
#59744=CARTESIAN_POINT('Ctrl Pts',(2.38876309683304,98.8619065896491,13.7009094816985));
#59745=CARTESIAN_POINT('Ctrl Pts',(2.37472306456667,98.8701439677234,13.7656541013784));
#59746=CARTESIAN_POINT('Ctrl Pts',(2.35804083292173,98.8783850720437,13.8295840832372));
#59747=CARTESIAN_POINT('Ctrl Pts',(2.34750679934094,98.8835889363408,13.8699528174721));
#59748=CARTESIAN_POINT('Ctrl Pts',(2.33591896182167,98.8887945023829,13.9099988567666));
#59749=CARTESIAN_POINT('Ctrl Pts',(2.32328120727427,98.8940038103791,13.9496644746548));
#59750=CARTESIAN_POINT('Ctrl Pts',(2.30140899554917,98.9030195803093,14.018313916247));
#59751=CARTESIAN_POINT('Ctrl Pts',(2.27639112347116,98.9120469498515,14.0858253077428));
#59752=CARTESIAN_POINT('Ctrl Pts',(2.24841602309062,98.9210535394763,14.151975538528));
#59753=CARTESIAN_POINT('Ctrl Pts',(2.24405759988463,98.9224567347711,14.1622815140925));
#59754=CARTESIAN_POINT('Ctrl Pts',(2.23962734738864,98.9238594385837,14.1725545399852));
#59755=CARTESIAN_POINT('Ctrl Pts',(2.23512591934516,98.9252615427703,14.1827938692418));
#59756=CARTESIAN_POINT('Ctrl Pts',(2.23511817777363,98.925263954114,14.1828114788757));
#59757=CARTESIAN_POINT('Ctrl Pts',(2.23511043599147,98.9252663654558,14.1828290884078));
#59758=CARTESIAN_POINT('Ctrl Pts',(2.23510269399866,98.9252687767959,14.1828466978383));
#59759=CARTESIAN_POINT('Ctrl Pts',(2.17794479438478,98.9430713162717,14.312854317855));
#59760=CARTESIAN_POINT('Ctrl Pts',(2.10930175381278,98.9607767910995,14.4373209986211));
#59761=CARTESIAN_POINT('Ctrl Pts',(2.03066171000624,98.9783997225956,14.5545960989096));
#59762=CARTESIAN_POINT('Ctrl Pts',(2.02606260275723,98.9794303648494,14.5614547009367));
#59763=CARTESIAN_POINT('Ctrl Pts',(2.02142931602233,98.9804607232536,14.568288698883));
#59764=CARTESIAN_POINT('Ctrl Pts',(2.01676215236437,98.9814908001412,14.575097760253));
#59765=CARTESIAN_POINT('Ctrl Pts',(1.94416808705626,98.99751283715,14.6810073623154));
#59766=CARTESIAN_POINT('Ctrl Pts',(1.86337509951493,99.0134675800737,14.780885479184));
#59767=CARTESIAN_POINT('Ctrl Pts',(1.77547310145705,99.0293745555827,14.8734835174004));
#59768=CARTESIAN_POINT('Ctrl Pts',(1.76064829300454,99.0320572917001,14.8891003203169));
#59769=CARTESIAN_POINT('Ctrl Pts',(1.74562134434268,99.0347386535236,14.9045099526594));
#59770=CARTESIAN_POINT('Ctrl Pts',(1.73039756958489,99.0374187156741,14.919706308246));
#59771=CARTESIAN_POINT('Ctrl Pts',(1.64769725892055,99.0519776523356,15.0022576693882));
#59772=CARTESIAN_POINT('Ctrl Pts',(1.55918602531543,99.0664990006054,15.0785180605838));
#59773=CARTESIAN_POINT('Ctrl Pts',(1.46568429520091,99.0809991507652,15.1475124088901));
#59774=CARTESIAN_POINT('Ctrl Pts',(1.44599705066954,99.0840522279819,15.1620395048564));
#59775=CARTESIAN_POINT('Ctrl Pts',(1.42608862878947,99.0871043460674,15.1762443027718));
#59776=CARTESIAN_POINT('Ctrl Pts',(1.40596681419401,99.0901556270038,15.1901174339669));
#59777=CARTESIAN_POINT('Ctrl Pts',(1.40594264751216,99.0901592916502,15.1901340958612));
#59778=CARTESIAN_POINT('Ctrl Pts',(1.40591848052765,99.0901629562946,15.1901507572739));
#59779=CARTESIAN_POINT('Ctrl Pts',(1.40589431324056,99.090166620937,15.1901674182049));
#59780=CARTESIAN_POINT('Ctrl Pts',(1.40368185140187,99.0905021108659,15.1916926896963));
#59781=CARTESIAN_POINT('Ctrl Pts',(1.40146685330708,99.0908375839379,15.1932139243866));
#59782=CARTESIAN_POINT('Ctrl Pts',(1.39924932977195,99.0911730415125,15.1947311102363));
#59783=CARTESIAN_POINT('Ctrl Pts',(1.30214891635913,99.1058619810725,15.2611652972421));
#59784=CARTESIAN_POINT('Ctrl Pts',(1.20019985425589,99.1205226743845,15.3198379144593));
#59785=CARTESIAN_POINT('Ctrl Pts',(1.09471441959963,99.1351467647404,15.3704986170229));
#59786=CARTESIAN_POINT('Ctrl Pts',(1.02858782949793,99.1443142979806,15.4022567410103));
#59787=CARTESIAN_POINT('Ctrl Pts',(0.96107047246329,99.1534675576461,15.430866581243));
#59788=CARTESIAN_POINT('Ctrl Pts',(0.892475242895028,99.1626056045417,15.4562660571135));
#59789=CARTESIAN_POINT('Ctrl Pts',(0.781385488346495,99.1774046422166,15.4974004269214));
#59790=CARTESIAN_POINT('Ctrl Pts',(0.667469791677626,99.1921631044739,15.5301183468881));
#59791=CARTESIAN_POINT('Ctrl Pts',(0.552101904503678,99.2068707663012,15.5541397627508));
#59792=CARTESIAN_POINT('Ctrl Pts',(0.466973388836592,99.2177233653299,15.5718648639615));
#59793=CARTESIAN_POINT('Ctrl Pts',(0.381053394821842,99.2285484406278,15.5848557127175));
#59794=CARTESIAN_POINT('Ctrl Pts',(0.294876898577294,99.2393441839979,15.5930062691574));
#59795=CARTESIAN_POINT('Ctrl Pts',(0.261373376392985,99.2435413310538,15.5961750258416));
#59796=CARTESIAN_POINT('Ctrl Pts',(0.22783196433043,99.2477339593837,15.598611776666));
#59797=CARTESIAN_POINT('Ctrl Pts',(0.194284751723588,99.2519219225085,15.6003099778197));
#59798=CARTESIAN_POINT('Ctrl Pts',(0.194274870771869,99.2519231560256,15.6003104780056));
#59799=CARTESIAN_POINT('Ctrl Pts',(0.194264989819291,99.2519243895424,15.6003109781277));
#59800=CARTESIAN_POINT('Ctrl Pts',(0.194255108865836,99.2519256230587,15.600311478186));
#59801=CARTESIAN_POINT('Ctrl Pts',(0.125549408185388,99.2605026907845,15.6037885570454));
#59802=CARTESIAN_POINT('Ctrl Pts',(0.0567974642991696,99.2690620764199,
15.6041793692269));
#59803=CARTESIAN_POINT('Ctrl Pts',(-0.0117206539231109,99.277612972139,
15.6014220862784));
#59804=CARTESIAN_POINT('Ctrl Pts',(-0.0279277522598392,99.2796355788799,
15.6007698857065));
#59805=CARTESIAN_POINT('Ctrl Pts',(-0.0441215422889647,99.2816576821861,
15.599941580274));
#59806=CARTESIAN_POINT('Ctrl Pts',(-0.0602979007831986,99.2836793508579,
15.5989364281172));
#59807=CARTESIAN_POINT('Ctrl Pts',(-0.155189454247767,99.2955385885799,
15.5930401412822));
#59808=CARTESIAN_POINT('Ctrl Pts',(-0.249497472395329,99.3073853048398,
15.5810531959571));
#59809=CARTESIAN_POINT('Ctrl Pts',(-0.342529244294992,99.3192120108426,
15.5633069676301));
#59810=CARTESIAN_POINT('Ctrl Pts',(-0.383655949057396,99.3244402617526,
15.5554618639827));
#59811=CARTESIAN_POINT('Ctrl Pts',(-0.424533895934865,99.3296646860019,
15.546491035537));
#59812=CARTESIAN_POINT('Ctrl Pts',(-0.465106181639773,99.3348850358048,
15.536421804769));
#59813=CARTESIAN_POINT('Ctrl Pts',(-0.552371864455765,99.3461133258105,
15.514764205668));
#59814=CARTESIAN_POINT('Ctrl Pts',(-0.638221444598278,99.3573222854356,
15.4880276545498));
#59815=CARTESIAN_POINT('Ctrl Pts',(-0.72206074077835,99.3685044860839,15.4565129213605));
#59816=CARTESIAN_POINT('Ctrl Pts',(-0.766011985468675,99.3743665538644,
15.4399918887081));
#59817=CARTESIAN_POINT('Ctrl Pts',(-0.809411630058819,99.3802213759304,
15.4221576968483));
#59818=CARTESIAN_POINT('Ctrl Pts',(-0.852179681968102,99.3860685973948,
15.4030527200777));
#59819=CARTESIAN_POINT('Ctrl Pts',(-0.911766896620319,99.3942153243315,
15.3764344314036));
#59820=CARTESIAN_POINT('Ctrl Pts',(-0.970130500379672,99.4023468455704,
15.3473587082573));
#59821=CARTESIAN_POINT('Ctrl Pts',(-1.02701479794973,99.410460877643,15.3159043816065));
#59822=CARTESIAN_POINT('Ctrl Pts',(-1.02702824809226,99.4104627961845,15.3158969443137));
#59823=CARTESIAN_POINT('Ctrl Pts',(-1.02704169815214,99.4104647147251,15.3158895068879));
#59824=CARTESIAN_POINT('Ctrl Pts',(-1.02705514812928,99.4104666332647,15.3158820693293));
#59825=CARTESIAN_POINT('Ctrl Pts',(-1.09439411538887,99.4200720379882,15.278645015782));
#59826=CARTESIAN_POINT('Ctrl Pts',(-1.15975492266891,99.4296619103106,15.2380844448373));
#59827=CARTESIAN_POINT('Ctrl Pts',(-1.22278322196834,99.4392373810056,15.1943637056183));
#59828=CARTESIAN_POINT('Ctrl Pts',(-1.28581152126779,99.4488128517006,15.1506429663993));
#59829=CARTESIAN_POINT('Ctrl Pts',(-1.34650663618581,99.4583739206444,15.1037613526107));
#59830=CARTESIAN_POINT('Ctrl Pts',(-1.40447276324155,99.4679146068899,15.0539221631217));
#59831=CARTESIAN_POINT('Ctrl Pts',(-1.4122049541814,99.4691872537182,15.0472740368971));
#59832=CARTESIAN_POINT('Ctrl Pts',(-1.41988877852004,99.4704595693226,15.0405731177698));
#59833=CARTESIAN_POINT('Ctrl Pts',(-1.42752335664479,99.4717315482021,15.0338198509602));
#59834=CARTESIAN_POINT('Ctrl Pts',(-1.46126734594077,99.4773535538969,15.0039711600158));
#59835=CARTESIAN_POINT('Ctrl Pts',(-1.49404925406796,99.4829689748849,14.9730998278357));
#59836=CARTESIAN_POINT('Ctrl Pts',(-1.52583311760315,99.4885787544094,14.9412808719977));
#59837=CARTESIAN_POINT('Ctrl Pts',(-1.52585068633716,99.488581855251,14.9412632838662));
#59838=CARTESIAN_POINT('Ctrl Pts',(-1.52586825476187,99.4885849560902,14.9412456954474));
#59839=CARTESIAN_POINT('Ctrl Pts',(-1.52588582287745,99.4885880569271,14.9412281067411));
#59840=CARTESIAN_POINT('Ctrl Pts',(-1.58115232099639,99.4983427967564,14.8858968335732));
#59841=CARTESIAN_POINT('Ctrl Pts',(-1.63335593453091,99.508074040194,14.827725076819));
#59842=CARTESIAN_POINT('Ctrl Pts',(-1.68232436251468,99.5177858924878,14.7671431406004));
#59843=CARTESIAN_POINT('Ctrl Pts',(-1.73129279049846,99.5274977447815,14.7065612043818));
#59844=CARTESIAN_POINT('Ctrl Pts',(-1.77702683221379,99.5371902063529,14.6435695394248));
#59845=CARTESIAN_POINT('Ctrl Pts',(-1.81938005116608,99.5468739059855,14.5785523901826));
#59846=CARTESIAN_POINT('Ctrl Pts',(-1.8471358321929,99.5532200268514,14.5359440170295));
#59847=CARTESIAN_POINT('Ctrl Pts',(-1.87339785697294,99.5595593031522,14.4924487952036));
#59848=CARTESIAN_POINT('Ctrl Pts',(-1.89806545832282,99.5658887441428,14.4481683280864));
#59849=CARTESIAN_POINT('Ctrl Pts',(-1.89807927164982,99.5658922884938,14.4481435319758));
#59850=CARTESIAN_POINT('Ctrl Pts',(-1.89809308447688,99.5658958328417,14.4481187356191));
#59851=CARTESIAN_POINT('Ctrl Pts',(-1.89810689680401,99.5658993771865,14.4480939390164));
#59852=CARTESIAN_POINT('Ctrl Pts',(-1.94180310649515,99.5771121462621,14.3696482475861));
#59853=CARTESIAN_POINT('Ctrl Pts',(-1.98072253908252,99.5883221576043,14.2886978400264));
#59854=CARTESIAN_POINT('Ctrl Pts',(-2.01465522212182,99.5995194743399,14.2058796237811));
#59855=CARTESIAN_POINT('Ctrl Pts',(-2.03003793630761,99.60459555756,14.1683356150034));
#59856=CARTESIAN_POINT('Ctrl Pts',(-2.044395998321,99.6096689699237,14.1304084537033));
#59857=CARTESIAN_POINT('Ctrl Pts',(-2.05771101303856,99.6147384764741,14.0921607815144));
#59858=CARTESIAN_POINT('Ctrl Pts',(-2.082980968104,99.6243596601867,14.0195722806323));
#59859=CARTESIAN_POINT('Ctrl Pts',(-2.10442266847298,99.6339607541982,13.9458068879));
#59860=CARTESIAN_POINT('Ctrl Pts',(-2.12184796472555,99.643529007375,13.8712543843034));
#59861=CARTESIAN_POINT('Ctrl Pts',(-2.12915552340198,99.6475415974915,13.8399896765699));
#59862=CARTESIAN_POINT('Ctrl Pts',(-2.1357565710266,99.6515483310469,13.808587147076));
#59863=CARTESIAN_POINT('Ctrl Pts',(-2.14163678817645,99.6555479171719,13.7770782183977));
#59864=CARTESIAN_POINT('Ctrl Pts',(-2.15486319803449,99.664544211697,13.7062049845924));
#59865=CARTESIAN_POINT('Ctrl Pts',(-2.16444389128284,99.6735062092448,13.6347768389589));
#59866=CARTESIAN_POINT('Ctrl Pts',(-2.17045407467893,99.6824452970138,13.5631727727705));
#59867=CARTESIAN_POINT('Ctrl Pts',(-2.17527721457745,99.6896188669423,13.5057108941939));
#59868=CARTESIAN_POINT('Ctrl Pts',(-2.1778013805117,99.6967778078112,13.4481347336066));
#59869=CARTESIAN_POINT('Ctrl Pts',(-2.17806600939497,99.7039310388077,13.3906160471066));
#59870=CARTESIAN_POINT('Ctrl Pts',(-2.17824403641185,99.7087433191592,13.3519207994595));
#59871=CARTESIAN_POINT('Ctrl Pts',(-2.17739989657897,99.7135525531618,13.3132557449292));
#59872=CARTESIAN_POINT('Ctrl Pts',(-2.17559770860353,99.7183686082064,13.2746659401345));
#59873=CARTESIAN_POINT('Ctrl Pts',(-2.17559713642049,99.7183701372728,13.2746536881207));
#59874=CARTESIAN_POINT('Ctrl Pts',(-2.17559656414086,99.7183716663399,13.2746414361144));
#59875=CARTESIAN_POINT('Ctrl Pts',(-2.17559599176465,99.7183731954077,13.2746291841155));
#59876=CARTESIAN_POINT('Ctrl Pts',(-2.17048933018398,99.7320153272009,13.165318540355));
#59877=CARTESIAN_POINT('Ctrl Pts',(-2.15706993053311,99.7456422820892,13.0565812767468));
#59878=CARTESIAN_POINT('Ctrl Pts',(-2.13578190969035,99.7592462060556,12.949678958828));
#59879=CARTESIAN_POINT('Ctrl Pts',(-2.13133578786128,99.7620874614149,12.9273518137737));
#59880=CARTESIAN_POINT('Ctrl Pts',(-2.12654661235941,99.7649277125925,12.9051046916816));
#59881=CARTESIAN_POINT('Ctrl Pts',(-2.12141870851789,99.7677668886852,12.8829490359156));
#59882=CARTESIAN_POINT('Ctrl Pts',(-2.10189348894183,99.7785774534577,12.7985882411245));
#59883=CARTESIAN_POINT('Ctrl Pts',(-2.07746172782855,99.7893739247512,12.7155472879905));
#59884=CARTESIAN_POINT('Ctrl Pts',(-2.04824592303377,99.8001393971766,12.6344516591826));
#59885=CARTESIAN_POINT('Ctrl Pts',(-2.03297415615081,99.8057667549174,12.5920611261446));
#59886=CARTESIAN_POINT('Ctrl Pts',(-2.01639540213309,99.811385530251,12.5502029742387));
#59887=CARTESIAN_POINT('Ctrl Pts',(-1.99852925915575,99.8169925733225,12.5089717602133));
#59888=CARTESIAN_POINT('Ctrl Pts',(-1.97943931953326,99.8229836881272,12.4649162868352));
#59889=CARTESIAN_POINT('Ctrl Pts',(-1.95887915899225,99.828961763856,12.4215742489325));
#59890=CARTESIAN_POINT('Ctrl Pts',(-1.93687541951419,99.8349244125409,12.3790552447253));
#59891=CARTESIAN_POINT('Ctrl Pts',(-1.90744196851941,99.8429003898988,12.3221794110549));
#59892=CARTESIAN_POINT('Ctrl Pts',(-1.87542325629485,99.8508490300377,12.2667734780342));
#59893=CARTESIAN_POINT('Ctrl Pts',(-1.8410372511685,99.8587984234362,12.2130119194893));
#59894=CARTESIAN_POINT('Ctrl Pts',(-1.82781102231123,99.8618560771526,12.1923330801061));
#59895=CARTESIAN_POINT('Ctrl Pts',(-1.81423425731905,99.8649139110618,12.1718970672831));
#59896=CARTESIAN_POINT('Ctrl Pts',(-1.80031811883615,99.8679737811827,12.1517121936808));
#59897=CARTESIAN_POINT('Ctrl Pts',(-1.80030955952059,99.8679756631986,12.151699778692));
#59898=CARTESIAN_POINT('Ctrl Pts',(-1.80030100007656,99.8679775452153,12.1516873637982));
#59899=CARTESIAN_POINT('Ctrl Pts',(-1.80029244050419,99.8679794272327,12.1516749489994));
#59900=CARTESIAN_POINT('Ctrl Pts',(-1.7479410958742,99.8794900658441,12.0757445892562));
#59901=CARTESIAN_POINT('Ctrl Pts',(-1.69066835351395,99.891022885017,12.0033523218074));
#59902=CARTESIAN_POINT('Ctrl Pts',(-1.62911768397407,99.902562860591,11.9349818441119));
#59903=CARTESIAN_POINT('Ctrl Pts',(-1.60195215802481,99.907656054674,11.9048063805485));
#59904=CARTESIAN_POINT('Ctrl Pts',(-1.5739540200414,99.9127506110194,11.875414235167));
#59905=CARTESIAN_POINT('Ctrl Pts',(-1.54518169887168,99.9178450865659,11.8468462498985));
#59906=CARTESIAN_POINT('Ctrl Pts',(-1.4835056390015,99.928765553391,11.7856082024225));
#59907=CARTESIAN_POINT('Ctrl Pts',(-1.41824828233156,99.9396779509967,11.7281826004569));
#59908=CARTESIAN_POINT('Ctrl Pts',(-1.34992072050328,99.9505545328162,11.6749941954782));
#59909=CARTESIAN_POINT('Ctrl Pts',(-1.31243779271239,99.9565211752669,11.6458162606919));
#59910=CARTESIAN_POINT('Ctrl Pts',(-1.27403171113861,99.9624769210925,11.6179139380439));
#59911=CARTESIAN_POINT('Ctrl Pts',(-1.23479297782328,99.968416332379,11.5913598429592));
#59912=CARTESIAN_POINT('Ctrl Pts',(-1.16188419622155,99.9794522452065,11.5420201585306));
#59913=CARTESIAN_POINT('Ctrl Pts',(-1.08609498573667,99.9904318799357,11.4973329907347));
#59914=CARTESIAN_POINT('Ctrl Pts',(-1.00797578322965,100.001327151754,11.4577351239215));
#59915=CARTESIAN_POINT('Ctrl Pts',(-0.984896824454309,100.004545970189,
11.4460366233423));
#59916=CARTESIAN_POINT('Ctrl Pts',(-0.961614757223156,100.007757380463,
11.4347825492624));
#59917=CARTESIAN_POINT('Ctrl Pts',(-0.938144459933422,100.010960545475,
11.4239846976537));
#59918=CARTESIAN_POINT('Ctrl Pts',(-0.87745855544309,100.019242799574,11.3960652647065));
#59919=CARTESIAN_POINT('Ctrl Pts',(-0.815496414881841,100.027472245218,
11.3711882621347));
#59920=CARTESIAN_POINT('Ctrl Pts',(-0.752601331419458,100.035687471341,
11.3493825214119));
#59921=CARTESIAN_POINT('Ctrl Pts',(-0.689706247957076,100.043902697464,
11.3275767806891));
#59922=CARTESIAN_POINT('Ctrl Pts',(-0.625878476001496,100.052103707113,
11.3088414440984));
#59923=CARTESIAN_POINT('Ctrl Pts',(-0.561407853639797,100.060336256543,
11.2931873647555));
#59924=CARTESIAN_POINT('Ctrl Pts',(-0.553617389451351,100.061331056642,
11.2912957660698));
#59925=CARTESIAN_POINT('Ctrl Pts',(-0.545817752823663,100.062326290681,
11.2894492130978));
#59926=CARTESIAN_POINT('Ctrl Pts',(-0.538009509754961,100.063322031072,
11.2876477355394));
#59927=CARTESIAN_POINT('Ctrl Pts',(-0.538006771879202,100.063322380217,
11.2876471038708));
#59928=CARTESIAN_POINT('Ctrl Pts',(-0.538004034002362,100.063322729363,
11.2876464722078));
#59929=CARTESIAN_POINT('Ctrl Pts',(-0.538001296124486,100.063323078509,
11.2876458405503));
#59930=CARTESIAN_POINT('Ctrl Pts',(-0.465603546126105,100.072555543897,
11.270942911166));
#59931=CARTESIAN_POINT('Ctrl Pts',(-0.392351732701438,100.081845544988,
11.258092863964));
#59932=CARTESIAN_POINT('Ctrl Pts',(-0.318688500137045,100.091160594883,
11.2491285684583));
#59933=CARTESIAN_POINT('Ctrl Pts',(-0.2827428207369,100.095706089094,11.2447542329713));
#59934=CARTESIAN_POINT('Ctrl Pts',(-0.246699900062628,100.100257475839,
11.2413048304038));
#59935=CARTESIAN_POINT('Ctrl Pts',(-0.210615032233411,100.104810568345,
11.2387819165222));
#59936=CARTESIAN_POINT('Ctrl Pts',(-0.133382096340926,100.114555614476,
11.2333820894533));
#59937=CARTESIAN_POINT('Ctrl Pts',(-0.0559542955087094,100.124307966008,
11.2322293802618));
#59938=CARTESIAN_POINT('Ctrl Pts',(0.0211658642688437,100.134026105027,
11.2353374696711));
#59939=CARTESIAN_POINT('Ctrl Pts',(0.0555764068329223,100.138362279087,
11.2367242801137));
#59940=CARTESIAN_POINT('Ctrl Pts',(0.0899250234073539,100.142691553371,
11.2389592244015));
#59941=CARTESIAN_POINT('Ctrl Pts',(0.124163920066559,100.147009814598,11.2420424808953));
#59942=CARTESIAN_POINT('Ctrl Pts',(0.20308162759669,100.156963034759,11.249149121528));
#59943=CARTESIAN_POINT('Ctrl Pts',(0.281422458186795,100.166857903795,11.2607641033883));
#59944=CARTESIAN_POINT('Ctrl Pts',(0.358643616091216,100.17665221554,11.2768842354255));
#59945=CARTESIAN_POINT('Ctrl Pts',(0.375094826460005,100.178738797603,11.2803184714628));
#59946=CARTESIAN_POINT('Ctrl Pts',(0.391495032520846,100.180820791012,11.2839571764946));
#59947=CARTESIAN_POINT('Ctrl Pts',(0.407838682318079,100.182897747539,11.2878002992483));
#59948=CARTESIAN_POINT('Ctrl Pts',(0.468585816358258,100.190617513817,11.3020846663235));
#59949=CARTESIAN_POINT('Ctrl Pts',(0.528562118821918,100.198268652909,11.3191960405154));
#59950=CARTESIAN_POINT('Ctrl Pts',(0.587545717563093,100.205904122806,11.3389426777065));
#59951=CARTESIAN_POINT('Ctrl Pts',(0.633794056365937,100.211891004011,11.354425781256));
#59952=CARTESIAN_POINT('Ctrl Pts',(0.679433166441745,100.217868381716,11.3715292065591));
#59953=CARTESIAN_POINT('Ctrl Pts',(0.724375738701851,100.223864581261,11.39017098217));
#59954=CARTESIAN_POINT('Ctrl Pts',(0.779479836473583,100.231216522846,11.4130276673627));
#59955=CARTESIAN_POINT('Ctrl Pts',(0.833582014341551,100.238634172081,11.4381156038251));
#59956=CARTESIAN_POINT('Ctrl Pts',(0.886359497714081,100.246059788204,11.4655029679801));
#59957=CARTESIAN_POINT('Ctrl Pts',(0.905127540089821,100.248700389255,11.4752421063052));
#59958=CARTESIAN_POINT('Ctrl Pts',(0.923727743854149,100.251341943263,11.4852716690271));
#59959=CARTESIAN_POINT('Ctrl Pts',(0.942144614126101,100.253981673654,11.4955934837883));
#59960=CARTESIAN_POINT('Ctrl Pts',(0.942200171877861,100.253989636868,11.495624621371));
#59961=CARTESIAN_POINT('Ctrl Pts',(0.942255727960906,100.253997600066,11.4956557616129));
#59962=CARTESIAN_POINT('Ctrl Pts',(0.942311282374887,100.254005563247,11.4956869045136));
#59963=CARTESIAN_POINT('Ctrl Pts',(1.01163318083879,100.263942178207,11.5345476331031));
#59964=CARTESIAN_POINT('Ctrl Pts',(1.07849560640498,100.273872967035,11.5776313369723));
#59965=CARTESIAN_POINT('Ctrl Pts',(1.14251460414552,100.28380385674,11.6244143374231));
#59966=CARTESIAN_POINT('Ctrl Pts',(1.17092756044083,100.288211391146,11.6451776013617));
#59967=CARTESIAN_POINT('Ctrl Pts',(1.19878098938501,100.29261898177,11.6666691120486));
#59968=CARTESIAN_POINT('Ctrl Pts',(1.22604411207514,100.29702731935,11.6888414174065));
#59969=CARTESIAN_POINT('Ctrl Pts',(1.27456703557271,100.304873281442,11.7283037009047));
#59970=CARTESIAN_POINT('Ctrl Pts',(1.32130430385171,100.3127723134,11.7698414731503));
#59971=CARTESIAN_POINT('Ctrl Pts',(1.36601958771573,100.320664003457,11.8133526078688));
#59972=CARTESIAN_POINT('Ctrl Pts',(1.40490907505444,100.327527513068,11.8511948304045));
#59973=CARTESIAN_POINT('Ctrl Pts',(1.44226820566837,100.334385363039,11.8905294255716));
#59974=CARTESIAN_POINT('Ctrl Pts',(1.47792043455174,100.341193724797,11.9312653626777));
#59975=CARTESIAN_POINT('Ctrl Pts',(1.49582365413962,100.344612630133,11.9517214309228));
#59976=CARTESIAN_POINT('Ctrl Pts',(1.5132973929337,100.348019242088,11.9725317016156));
#59977=CARTESIAN_POINT('Ctrl Pts',(1.53032424456408,100.351410609321,11.9936821046758));
#59978=CARTESIAN_POINT('Ctrl Pts',(1.57351136842727,100.36001251647,12.0473282570325));
#59979=CARTESIAN_POINT('Ctrl Pts',(1.61382641444132,100.368515862212,12.1031700902447));
#59980=CARTESIAN_POINT('Ctrl Pts',(1.65116008545529,100.376979620875,12.160833428752));
#59981=CARTESIAN_POINT('Ctrl Pts',(1.67918990886772,100.383334143596,12.2041266049073));
#59982=CARTESIAN_POINT('Ctrl Pts',(1.70553985327126,100.389666485609,12.2484474471584));
#59983=CARTESIAN_POINT('Ctrl Pts',(1.73017010000186,100.396003992062,12.2936556590329));
#59984=CARTESIAN_POINT('Ctrl Pts',(1.76510427318049,100.404992759018,12.3577764743862));
#59985=CARTESIAN_POINT('Ctrl Pts',(1.79668138150137,100.414047556875,12.423644839922));
#59986=CARTESIAN_POINT('Ctrl Pts',(1.8245316294591,100.423117001667,12.4909006139287));
#59987=CARTESIAN_POINT('Ctrl Pts',(1.84244460797566,100.428950370547,12.5341588009554));
#59988=CARTESIAN_POINT('Ctrl Pts',(1.85881590498794,100.434789699189,12.5779898849672));
#59989=CARTESIAN_POINT('Ctrl Pts',(1.87355074227944,100.440620248091,12.6222872607065));
#59990=CARTESIAN_POINT('Ctrl Pts',(1.87357203853786,100.440628674983,12.6223512836979));
#59991=CARTESIAN_POINT('Ctrl Pts',(1.87359333137863,100.440637101856,12.6224153076619));
#59992=CARTESIAN_POINT('Ctrl Pts',(1.87361462080168,100.44064552871,12.6224793325982));
#59993=CARTESIAN_POINT('Ctrl Pts',(1.90030799893165,100.451211395838,12.7027559013972));
#59994=CARTESIAN_POINT('Ctrl Pts',(1.92167142133264,100.461766833131,12.7847043625893));
#59995=CARTESIAN_POINT('Ctrl Pts',(1.93770069774032,100.47229961058,12.8675332722959));
#59996=CARTESIAN_POINT('Ctrl Pts',(1.94150753778997,100.474801070908,12.8872045539384));
#59997=CARTESIAN_POINT('Ctrl Pts',(1.94501374241068,100.47730125392,12.9069254417717));
#59998=CARTESIAN_POINT('Ctrl Pts',(1.94821967647636,100.479799997206,12.926685261519));
#59999=CARTESIAN_POINT('Ctrl Pts',(1.9590004398596,100.488202652894,12.9931326484044));
#60000=CARTESIAN_POINT('Ctrl Pts',(1.96649001887271,100.496645809469,13.0600178136398));
#60001=CARTESIAN_POINT('Ctrl Pts',(1.97057829127119,100.505060909447,13.1270246813479));
#60002=CARTESIAN_POINT('Ctrl Pts',(1.97240853228865,100.508828188054,13.1570223688249));
#60003=CARTESIAN_POINT('Ctrl Pts',(1.97355695524824,100.512589754712,13.1870437638236));
#60004=CARTESIAN_POINT('Ctrl Pts',(1.97401335744123,100.516339028903,13.2170571680248));
#60005=CARTESIAN_POINT('Ctrl Pts',(1.97499263442704,100.524383639525,13.281455272266));
#60006=CARTESIAN_POINT('Ctrl Pts',(1.97275259966565,100.532353585413,13.345826039755));
#60007=CARTESIAN_POINT('Ctrl Pts',(1.9674374615346,100.54032627025,13.4098672138259));
#60008=CARTESIAN_POINT('Ctrl Pts',(1.96413806745553,100.545275347489,13.4496210387194));
#60009=CARTESIAN_POINT('Ctrl Pts',(1.95965359226287,100.55022560885,13.4892488967257));
#60010=CARTESIAN_POINT('Ctrl Pts',(1.95401557164059,100.555196819791,13.5286880681682));
#60011=CARTESIAN_POINT('Ctrl Pts',(1.94533253058027,100.562852916073,13.5894278149629));
#60012=CARTESIAN_POINT('Ctrl Pts',(1.93382032564991,100.570502383121,13.6496950384495));
#60013=CARTESIAN_POINT('Ctrl Pts',(1.91949667738152,100.578140410089,13.7091766423013));
#60014=CARTESIAN_POINT('Ctrl Pts',(1.91270501795872,100.581762034752,13.7373802666653));
#60015=CARTESIAN_POINT('Ctrl Pts',(1.90527920058936,100.585382323055,13.7654169435566));
#60016=CARTESIAN_POINT('Ctrl Pts',(1.89723411364723,100.589001020792,13.7932606663128));
#60017=CARTESIAN_POINT('Ctrl Pts',(1.86995121684532,100.601272927563,13.8876856762602));
#60018=CARTESIAN_POINT('Ctrl Pts',(1.83554273386024,100.613526474822,13.9798896887639));
#60019=CARTESIAN_POINT('Ctrl Pts',(1.79462375037523,100.625751298097,14.0688641654385));
#60020=CARTESIAN_POINT('Ctrl Pts',(1.77730603659434,100.630925082303,14.1065199034268));
#60021=CARTESIAN_POINT('Ctrl Pts',(1.75882279384373,100.636093723609,14.1435974289194));
#60022=CARTESIAN_POINT('Ctrl Pts',(1.73922308164032,100.641256444873,14.1800216839161));
#60023=CARTESIAN_POINT('Ctrl Pts',(1.70422022775325,100.650476477095,14.2450712551733));
#60024=CARTESIAN_POINT('Ctrl Pts',(1.66570410472337,100.659721350228,14.3080859673018));
#60025=CARTESIAN_POINT('Ctrl Pts',(1.62381459103056,100.668918090935,14.3686340530643));
#60026=CARTESIAN_POINT('Ctrl Pts',(1.60866011209576,100.672245219876,14.3905386924201));
#60027=CARTESIAN_POINT('Ctrl Pts',(1.59306431364288,100.675565986668,14.4121200450159));
#60028=CARTESIAN_POINT('Ctrl Pts',(1.57703457414371,100.678876724653,14.4333561841082));
#60029=CARTESIAN_POINT('Ctrl Pts',(1.52079585687444,100.690492113506,14.5078610269577));
#60030=CARTESIAN_POINT('Ctrl Pts',(1.45935413988508,100.702131699336,14.578282915961));
#60031=CARTESIAN_POINT('Ctrl Pts',(1.39315836180106,100.713758449561,14.643758705858));
#60032=CARTESIAN_POINT('Ctrl Pts',(1.39312957784061,100.713763505229,14.6437871767455));
#60033=CARTESIAN_POINT('Ctrl Pts',(1.39310079298179,100.713768560895,14.6438156466972));
#60034=CARTESIAN_POINT('Ctrl Pts',(1.39307200722447,100.713773616559,14.6438441157133));
#60035=CARTESIAN_POINT('Ctrl Pts',(1.32191845089236,100.726270367787,14.7142147411049));
#60036=CARTESIAN_POINT('Ctrl Pts',(1.24528800902981,100.738749371248,14.7788522261899));
#60037=CARTESIAN_POINT('Ctrl Pts',(1.16430067964347,100.751204384363,14.8371779698929));
#60038=CARTESIAN_POINT('Ctrl Pts',(1.10472621250904,100.760366320867,14.8800825220944));
#60039=CARTESIAN_POINT('Ctrl Pts',(1.04279677413752,100.769515002972,14.9195711277492));
#60040=CARTESIAN_POINT('Ctrl Pts',(0.978957754214814,100.778648905549,14.9554270445908));
#60041=CARTESIAN_POINT('Ctrl Pts',(0.883515326126466,100.792304532483,15.0090333776587));
#60042=CARTESIAN_POINT('Ctrl Pts',(0.783795240018645,100.805928784227,15.0545307252639));
#60043=CARTESIAN_POINT('Ctrl Pts',(0.681176813927582,100.819530429895,15.0912367272569));
#60044=CARTESIAN_POINT('Ctrl Pts',(0.616191545489925,100.828143957003,15.1144815721025));
#60045=CARTESIAN_POINT('Ctrl Pts',(0.550044628400873,100.836748278969,15.1342003360991));
#60046=CARTESIAN_POINT('Ctrl Pts',(0.483067235435529,100.845347664371,15.1502137842078));
#60047=CARTESIAN_POINT('Ctrl Pts',(0.477040302176027,100.846121476543,15.1516547477737));
#60048=CARTESIAN_POINT('Ctrl Pts',(0.471006687997389,100.846895242936,15.1530656880532));
#60049=CARTESIAN_POINT('Ctrl Pts',(0.464966659778986,100.847668963334,15.1544464643299));
#60050=CARTESIAN_POINT('Ctrl Pts',(0.42837216229489,100.852356674741,15.1628121229257));
#60051=CARTESIAN_POINT('Ctrl Pts',(0.3915518982456,100.857041458656,15.1700683324017));
#60052=CARTESIAN_POINT('Ctrl Pts',(0.354569618166892,100.861723385158,15.1762220161701));
#60053=CARTESIAN_POINT('Ctrl Pts',(0.197073679531693,100.881662242566,15.2024286264464));
#60054=CARTESIAN_POINT('Ctrl Pts',(0.0366346791472735,100.901549900725,
15.2086399019479));
#60055=CARTESIAN_POINT('Ctrl Pts',(-0.121807786054843,100.921389366738,
15.1953830408523));
#60056=CARTESIAN_POINT('Ctrl Pts',(-0.141394222126714,100.923841893794,
15.1937442462146));
#60057=CARTESIAN_POINT('Ctrl Pts',(-0.160950110191157,100.92629367905,15.191807954743));
#60058=CARTESIAN_POINT('Ctrl Pts',(-0.180466105457516,100.92874472587,15.1895751716503));
#60059=CARTESIAN_POINT('Ctrl Pts',(-0.285412859949347,100.941925166088,
15.1775684389236));
#60060=CARTESIAN_POINT('Ctrl Pts',(-0.389203408420552,100.955083918522,
15.156988916179));
#60061=CARTESIAN_POINT('Ctrl Pts',(-0.490405259706409,100.968252572555,
15.1280211534391));
#60062=CARTESIAN_POINT('Ctrl Pts',(-0.520850058179763,100.972214130699,
15.1193067110882));
#60063=CARTESIAN_POINT('Ctrl Pts',(-0.551069765750844,100.976200068202,
15.1098567628718));
#60064=CARTESIAN_POINT('Ctrl Pts',(-0.581017382346599,100.980185608747,
15.0996490570147));
#60065=CARTESIAN_POINT('Ctrl Pts',(-0.581025570119883,100.980186698406,
15.0996462661956));
#60066=CARTESIAN_POINT('Ctrl Pts',(-0.581033757872797,100.980187788065,
15.0996434753198));
#60067=CARTESIAN_POINT('Ctrl Pts',(-0.581041945605342,100.980188877725,
15.0996406843875));
#60068=CARTESIAN_POINT('Ctrl Pts',(-0.623812244882491,100.985880936685,
15.0850616769844));
#60069=CARTESIAN_POINT('Ctrl Pts',(-0.666033261975055,100.991572632388,
15.0689345095551));
#60070=CARTESIAN_POINT('Ctrl Pts',(-0.707585192450922,100.997232238504,
15.0512956057487));
#60071=CARTESIAN_POINT('Ctrl Pts',(-0.785530363569268,101.007848808231,
15.018207675542));
#60072=CARTESIAN_POINT('Ctrl Pts',(-0.861125942375691,101.018350906553,
14.9797971836134));
#60073=CARTESIAN_POINT('Ctrl Pts',(-0.933743648892485,101.028803989415,
14.9365513449058));
#60074=CARTESIAN_POINT('Ctrl Pts',(-0.973059126825815,101.034463324697,
14.9131378979798));
#60075=CARTESIAN_POINT('Ctrl Pts',(-1.01150033413506,101.040108544714,14.8883086551989));
#60076=CARTESIAN_POINT('Ctrl Pts',(-1.04899875150532,101.045803082492,14.8621841577998));
#60077=CARTESIAN_POINT('Ctrl Pts',(-1.04901392620711,101.045805386934,14.8621735858481));
#60078=CARTESIAN_POINT('Ctrl Pts',(-1.04902910075475,101.045807691384,14.8621630136841));
#60079=CARTESIAN_POINT('Ctrl Pts',(-1.04904427514814,101.045809995841,14.8621524413079));
#60080=CARTESIAN_POINT('Ctrl Pts',(-1.14780635197162,101.060808489259,14.7933424528808));
#60081=CARTESIAN_POINT('Ctrl Pts',(-1.23983412163089,101.075803762398,14.7152570292142));
#60082=CARTESIAN_POINT('Ctrl Pts',(-1.32352871457936,101.090775856186,14.6293332957179));
#60083=CARTESIAN_POINT('Ctrl Pts',(-1.36158956475337,101.097584547146,14.5902587243294));
#60084=CARTESIAN_POINT('Ctrl Pts',(-1.39792524580788,101.104388121798,14.5495649265683));
#60085=CARTESIAN_POINT('Ctrl Pts',(-1.43240459690608,101.111214025577,14.5074087269095));
#60086=CARTESIAN_POINT('Ctrl Pts',(-1.43241988519781,101.111217052212,14.5073900346702));
#60087=CARTESIAN_POINT('Ctrl Pts',(-1.43243517312469,101.111220078851,14.5073713421434));
#60088=CARTESIAN_POINT('Ctrl Pts',(-1.43245046068667,101.111223105495,14.5073526493289));
#60089=CARTESIAN_POINT('Ctrl Pts',(-1.48051087329716,101.120738144411,14.4485869431873));
#60090=CARTESIAN_POINT('Ctrl Pts',(-1.52502073840214,101.130362355319,14.3870057519655));
#60091=CARTESIAN_POINT('Ctrl Pts',(-1.56565256142995,101.139984095314,14.3230138391529));
#60092=CARTESIAN_POINT('Ctrl Pts',(-1.58484471744172,101.14452885657,14.2927877089262));
#60093=CARTESIAN_POINT('Ctrl Pts',(-1.60317115550466,101.149072972734,14.2620243070821));
#60094=CARTESIAN_POINT('Ctrl Pts',(-1.62059515320848,101.153604182934,14.2307696225186));
#60095=CARTESIAN_POINT('Ctrl Pts',(-1.65094915067705,101.16149791348,14.1763214624438));
#60096=CARTESIAN_POINT('Ctrl Pts',(-1.67856899910062,101.169354671326,14.1203746208637));
#60097=CARTESIAN_POINT('Ctrl Pts',(-1.70332335292387,101.177202871508,14.0632424874143));
#60098=CARTESIAN_POINT('Ctrl Pts',(-1.70334055254959,101.177208324533,14.063202791314));
#60099=CARTESIAN_POINT('Ctrl Pts',(-1.70335775079447,101.177213777555,14.0631630946374));
#60100=CARTESIAN_POINT('Ctrl Pts',(-1.70337494765864,101.177219230573,14.0631233973841));
#60101=CARTESIAN_POINT('Ctrl Pts',(-1.73956596018279,101.188695175205,13.9795800386841));
#60102=CARTESIAN_POINT('Ctrl Pts',(-1.76964128316824,101.200157172918,13.8934831722751));
#60103=CARTESIAN_POINT('Ctrl Pts',(-1.79329485505532,101.211603009127,13.8057429884609));
#60104=CARTESIAN_POINT('Ctrl Pts',(-1.81475047729921,101.221985269326,13.7261558441381));
#60105=CARTESIAN_POINT('Ctrl Pts',(-1.83092241545109,101.23235382455,13.6452166785262));
#60106=CARTESIAN_POINT('Ctrl Pts',(-1.84156944772461,101.242689565247,13.5635931444862));
#60107=CARTESIAN_POINT('Ctrl Pts',(-1.8415803211725,101.242700120783,13.5635097851781));
#60108=CARTESIAN_POINT('Ctrl Pts',(-1.84159118883685,101.242710676261,13.5634264252065));
#60109=CARTESIAN_POINT('Ctrl Pts',(-1.84160205071728,101.242721231681,13.5633430645722));
#60110=CARTESIAN_POINT('Ctrl Pts',(-1.84680043505974,101.247772947181,13.523447521735));
#60111=CARTESIAN_POINT('Ctrl Pts',(-1.85067393068992,101.252811335925,13.4833998267027));
#60112=CARTESIAN_POINT('Ctrl Pts',(-1.85321962496362,101.25781362015,13.4432879472018));
#60113=CARTESIAN_POINT('Ctrl Pts',(-1.85842998682014,101.268051970917,13.3611895549859));
#60114=CARTESIAN_POINT('Ctrl Pts',(-1.85807984797538,101.278136725782,13.2788132899903));
#60115=CARTESIAN_POINT('Ctrl Pts',(-1.85234433187327,101.288149422771,13.1968274547615));
#60116=CARTESIAN_POINT('Ctrl Pts',(-1.8513286980246,101.289922451352,13.1823095651963));
#60117=CARTESIAN_POINT('Ctrl Pts',(-1.85014409132655,101.291693230341,13.1678038394538));
#60118=CARTESIAN_POINT('Ctrl Pts',(-1.84879134307173,101.293462225153,13.1533138959481));
#60119=CARTESIAN_POINT('Ctrl Pts',(-1.84158549322088,101.302885346533,13.0761285387478));
#60120=CARTESIAN_POINT('Ctrl Pts',(-1.82961053303086,101.312258858656,12.9993940513807));
#60121=CARTESIAN_POINT('Ctrl Pts',(-1.81305769334936,101.321733758925,12.9237059904937));
#60122=CARTESIAN_POINT('Ctrl Pts',(-1.80874409929264,101.324202874453,12.903982029174));
#60123=CARTESIAN_POINT('Ctrl Pts',(-1.80411954513465,101.326678912259,12.8843288675909));
#60124=CARTESIAN_POINT('Ctrl Pts',(-1.79918721630898,101.329164621995,12.864756507233));
#60125=CARTESIAN_POINT('Ctrl Pts',(-1.781259516784,101.338199513791,12.7936161984879));
#60126=CARTESIAN_POINT('Ctrl Pts',(-1.75923329448882,101.347322928088,12.7235507049475));
#60127=CARTESIAN_POINT('Ctrl Pts',(-1.73316690681723,101.356455930992,12.6551701085499));
#60128=CARTESIAN_POINT('Ctrl Pts',(-1.72493949639034,101.359338607497,12.633586940261));
#60129=CARTESIAN_POINT('Ctrl Pts',(-1.71630997222543,101.362222217204,12.6121716803674));
#60130=CARTESIAN_POINT('Ctrl Pts',(-1.70728125239787,101.365104217731,12.5909435637318));
#60131=CARTESIAN_POINT('Ctrl Pts',(-1.70175345113774,101.366868712195,12.5779467256274));
#60132=CARTESIAN_POINT('Ctrl Pts',(-1.69607614872213,101.368632562364,12.5650203364091));
#60133=CARTESIAN_POINT('Ctrl Pts',(-1.69025059179796,101.370395644794,12.5521689181993));
#60134=CARTESIAN_POINT('Ctrl Pts',(-1.69023447999782,101.370400520968,12.5521333749054));
#60135=CARTESIAN_POINT('Ctrl Pts',(-1.69021836706369,101.370405397137,12.5520978321849));
#60136=CARTESIAN_POINT('Ctrl Pts',(-1.69020225299568,101.3704102733,12.552062290038));
#60137=CARTESIAN_POINT('Ctrl Pts',(-1.65916228541274,101.379803055533,12.4835986911381));
#60138=CARTESIAN_POINT('Ctrl Pts',(-1.62385625943898,101.38925368914,12.4170512664938));
#60139=CARTESIAN_POINT('Ctrl Pts',(-1.58474965219824,101.398869160746,12.3528580433392));
#60140=CARTESIAN_POINT('Ctrl Pts',(-1.57438738692411,101.401417018373,12.335848457132));
#60141=CARTESIAN_POINT('Ctrl Pts',(-1.56375837782247,101.403976475443,12.3190038975838));
#60142=CARTESIAN_POINT('Ctrl Pts',(-1.5528714606858,101.406549577566,12.3023319367589));
#60143=CARTESIAN_POINT('Ctrl Pts',(-1.50522547062975,101.417810616538,12.2293680233106));
#60144=CARTESIAN_POINT('Ctrl Pts',(-1.45250347161367,101.429092584902,12.1598012467578));
#60145=CARTESIAN_POINT('Ctrl Pts',(-1.39521693588701,101.440235591337,12.0942983431898));
#60146=CARTESIAN_POINT('Ctrl Pts',(-1.39002164922676,101.441246144898,12.0883579183274));
#60147=CARTESIAN_POINT('Ctrl Pts',(-1.38478884617555,101.442255550578,12.082450941634));
#60148=CARTESIAN_POINT('Ctrl Pts',(-1.37951892383719,101.443263686164,12.0765779241854));
#60149=CARTESIAN_POINT('Ctrl Pts',(-1.34495561219293,101.449875644027,12.0380591530657));
#60150=CARTESIAN_POINT('Ctrl Pts',(-1.30879295146384,101.456433750153,12.0009970434627));
#60151=CARTESIAN_POINT('Ctrl Pts',(-1.27112355840083,101.462910739872,11.9655177583786));
#60152=CARTESIAN_POINT('Ctrl Pts',(-1.21153623134443,101.473156365653,11.9093948534913));
#60153=CARTESIAN_POINT('Ctrl Pts',(-1.14816421603574,101.483201663861,11.8572216830367));
#60154=CARTESIAN_POINT('Ctrl Pts',(-1.08158704318588,101.493204938719,11.8094775242596));
#60155=CARTESIAN_POINT('Ctrl Pts',(-1.07093446555862,101.494805497249,11.8018382939371));
#60156=CARTESIAN_POINT('Ctrl Pts',(-1.06019975954228,101.496404994277,11.7943123720928));
#60157=CARTESIAN_POINT('Ctrl Pts',(-1.04938521216415,101.498004094492,11.7869016371136));
#60158=CARTESIAN_POINT('Ctrl Pts',(-1.04408127981267,101.498788363964,11.7832670849099));
#60159=CARTESIAN_POINT('Ctrl Pts',(-1.03875823942205,101.499572522058,11.7796603068044));
#60160=CARTESIAN_POINT('Ctrl Pts',(-1.03341640307116,101.500356639497,11.7760815487043));
#60161=CARTESIAN_POINT('Ctrl Pts',(-1.03336341869387,101.500364416967,11.7760460518719));
#60162=CARTESIAN_POINT('Ctrl Pts',(-1.03331043248073,101.500372194422,11.7760105578119));
#60163=CARTESIAN_POINT('Ctrl Pts',(-1.03325744443199,101.500379971861,11.7759750665246));
#60164=CARTESIAN_POINT('Ctrl Pts',(-0.955872453571939,101.511738326574,
11.7241427568935));
#60165=CARTESIAN_POINT('Ctrl Pts',(-0.874575856573246,101.523063002066,
11.6782231996781));
#60166=CARTESIAN_POINT('Ctrl Pts',(-0.790359710197059,101.534440141483,
11.638646522071));
#60167=CARTESIAN_POINT('Ctrl Pts',(-0.704629111445532,101.546021875109,
11.598358140165));
#60168=CARTESIAN_POINT('Ctrl Pts',(-0.615871254096779,101.557658540445,
11.5646445337412));
#60169=CARTESIAN_POINT('Ctrl Pts',(-0.525157127555539,101.5694273881,11.5379923168064));
#60170=CARTESIAN_POINT('Ctrl Pts',(-0.486104601680084,101.574493889263,
11.5265185096809));
#60171=CARTESIAN_POINT('Ctrl Pts',(-0.44668998168622,101.579584667721,11.5163536479057));
#60172=CARTESIAN_POINT('Ctrl Pts',(-0.407001013407849,101.584704683254,
11.5075368986187));
#60173=CARTESIAN_POINT('Ctrl Pts',(-0.407000476373084,101.584704752534,
11.5075367793186));
#60174=CARTESIAN_POINT('Ctrl Pts',(-0.406999939338346,101.584704821813,
11.5075366600186));
#60175=CARTESIAN_POINT('Ctrl Pts',(-0.406999402303475,101.584704891092,
11.507536540719));
#60176=CARTESIAN_POINT('Ctrl Pts',(-0.329796015306562,101.594664396958,
11.490386184222));
#60177=CARTESIAN_POINT('Ctrl Pts',(-0.251492954156446,101.604714509963,
11.4783421362832));
#60178=CARTESIAN_POINT('Ctrl Pts',(-0.172779497151643,101.614698161061,
11.4713970122687));
#60179=CARTESIAN_POINT('Ctrl Pts',(-0.0732229176585234,101.627325457485,
11.4626128371436));
#60180=CARTESIAN_POINT('Ctrl Pts',(0.0270156898914488,101.639845380572,
11.4619757156826));
#60181=CARTESIAN_POINT('Ctrl Pts',(0.126710271978849,101.652303314665,11.4692731564523));
#60182=CARTESIAN_POINT('Ctrl Pts',(0.144363878509435,101.654509326888,11.4705653645676));
#60183=CARTESIAN_POINT('Ctrl Pts',(0.162000461720921,101.656713399613,11.4721064977722));
#60184=CARTESIAN_POINT('Ctrl Pts',(0.179613246981865,101.658915790235,11.4738955420251));
#60185=CARTESIAN_POINT('Ctrl Pts',(0.299670272934969,101.673928320291,11.4860905088702));
#60186=CARTESIAN_POINT('Ctrl Pts',(0.418621183774718,101.688864860963,11.509803609733));
#60187=CARTESIAN_POINT('Ctrl Pts',(0.534175038594159,101.703818319451,11.5446916778135));
#60188=CARTESIAN_POINT('Ctrl Pts',(0.625510733876132,101.715637782592,11.5722677890575));
#60189=CARTESIAN_POINT('Ctrl Pts',(0.714723094408206,101.727469194262,11.6068287669749));
#60190=CARTESIAN_POINT('Ctrl Pts',(0.800618974009707,101.739347773171,11.6481618141023));
#60191=CARTESIAN_POINT('Ctrl Pts',(0.822690628825449,101.742400072007,11.6587826815166));
#60192=CARTESIAN_POINT('Ctrl Pts',(0.84454346195733,101.745455492811,11.6698504774106));
#60193=CARTESIAN_POINT('Ctrl Pts',(0.866157592691843,101.748514648518,11.6813611589937));
#60194=CARTESIAN_POINT('Ctrl Pts',(0.882327175044809,101.750803210141,11.6899723271264));
#60195=CARTESIAN_POINT('Ctrl Pts',(0.898362881185585,101.753093780665,11.6988312276732));
#60196=CARTESIAN_POINT('Ctrl Pts',(0.914256168507836,101.755386520252,11.7079359260225));
#60197=CARTESIAN_POINT('Ctrl Pts',(0.914257785080811,101.755386753456,11.7079368520996));
#60198=CARTESIAN_POINT('Ctrl Pts',(0.914259401652273,101.75538698666,11.7079377781792));
#60199=CARTESIAN_POINT('Ctrl Pts',(0.914261018222301,101.755387219864,11.7079387042614));
#60200=CARTESIAN_POINT('Ctrl Pts',(0.940937878451754,101.759235587764,11.7232210393108));
#60201=CARTESIAN_POINT('Ctrl Pts',(0.967219185296116,101.763089293198,11.7391999111188));
#60202=CARTESIAN_POINT('Ctrl Pts',(0.993078145908535,101.766939862247,11.7558493116055));
#60203=CARTESIAN_POINT('Ctrl Pts',(1.09706050237409,101.782423517972,11.8227987888986));
#60204=CARTESIAN_POINT('Ctrl Pts',(1.19422509448536,101.797855820889,11.9005944041794));
#60205=CARTESIAN_POINT('Ctrl Pts',(1.28287524634823,101.813292829038,11.9873054502622));
#60206=CARTESIAN_POINT('Ctrl Pts',(1.37094245719128,101.828628327318,12.0734463063953));
#60207=CARTESIAN_POINT('Ctrl Pts',(1.45060397515945,101.843969870604,12.1683902843922));
#60208=CARTESIAN_POINT('Ctrl Pts',(1.52013310260964,101.859376807715,12.2701898116273));
#60209=CARTESIAN_POINT('Ctrl Pts',(1.55646790317967,101.867428224551,12.3233886026356));
#60210=CARTESIAN_POINT('Ctrl Pts',(1.59003475840863,101.875497444833,12.3784582390317));
#60211=CARTESIAN_POINT('Ctrl Pts',(1.6205862173276,101.883591653322,12.4351093933504));
#60212=CARTESIAN_POINT('Ctrl Pts',(1.62059035214418,101.883592748787,12.4351170604845));
#60213=CARTESIAN_POINT('Ctrl Pts',(1.62059448690538,101.883593844252,12.4351247276477));
#60214=CARTESIAN_POINT('Ctrl Pts',(1.62059862161118,101.883594939718,12.4351323948399));
#60215=CARTESIAN_POINT('Ctrl Pts',(1.6664257952741,101.895736572376,12.5201120196885));
#60216=CARTESIAN_POINT('Ctrl Pts',(1.70544966603001,101.907870263664,12.6086609400639));
#60217=CARTESIAN_POINT('Ctrl Pts',(1.73736806302339,101.919867668819,12.6996931149193));
#60218=CARTESIAN_POINT('Ctrl Pts',(1.76962662516437,101.931992934377,12.791695450438));
#60219=CARTESIAN_POINT('Ctrl Pts',(1.79464393036553,101.943983508552,12.8862714787962));
#60220=CARTESIAN_POINT('Ctrl Pts',(1.81216092264036,101.955985694475,12.9823149943274));
#60221=CARTESIAN_POINT('Ctrl Pts',(1.81308726913102,101.956620402913,12.9873940382733));
#60222=CARTESIAN_POINT('Ctrl Pts',(1.8139926307371,101.957255144673,12.9924771935236));
#60223=CARTESIAN_POINT('Ctrl Pts',(1.81487696576785,101.957889941672,12.9975642987641));
#60224=CARTESIAN_POINT('Ctrl Pts',(1.82899891315167,101.968027015858,13.0788002897002));
#60225=CARTESIAN_POINT('Ctrl Pts',(1.83779581543448,101.978310040119,13.1610389512985));
#60226=CARTESIAN_POINT('Ctrl Pts',(1.84103497551246,101.988621501177,13.2435190816003));
#60227=CARTESIAN_POINT('Ctrl Pts',(1.84178424014302,101.991006691435,13.262597930089));
#60228=CARTESIAN_POINT('Ctrl Pts',(1.84223632106058,101.993393393443,13.2816895896245));
#60229=CARTESIAN_POINT('Ctrl Pts',(1.84238869790875,101.995780135486,13.3007844682262));
#60230=CARTESIAN_POINT('Ctrl Pts',(1.84272083135378,102.000982479981,13.3424052780066));
#60231=CARTESIAN_POINT('Ctrl Pts',(1.84162862701176,102.006184700812,13.3840388243844));
#60232=CARTESIAN_POINT('Ctrl Pts',(1.83909409203655,102.011384338421,13.4255758404419));
#60233=CARTESIAN_POINT('Ctrl Pts',(1.83779789651504,102.014043503533,13.4468184331532));
#60234=CARTESIAN_POINT('Ctrl Pts',(1.83612393970882,102.016703302959,13.4680462597766));
#60235=CARTESIAN_POINT('Ctrl Pts',(1.83407633900791,102.019363590456,13.4892456201563));
#60236=CARTESIAN_POINT('Ctrl Pts',(1.82766919708152,102.027687889014,13.5555804825347));
#60237=CARTESIAN_POINT('Ctrl Pts',(1.81760231663384,102.036016924254,13.621636062974));
#60238=CARTESIAN_POINT('Ctrl Pts',(1.8040139429858,102.044345796022,13.6869904507889));
#60239=CARTESIAN_POINT('Ctrl Pts',(1.79101315962279,102.052314509595,13.749518775356));
#60240=CARTESIAN_POINT('Ctrl Pts',(1.77479143474322,102.060282887811,13.8114041897799));
#60241=CARTESIAN_POINT('Ctrl Pts',(1.75545902205749,102.068254622193,13.8723411019657));
#60242=CARTESIAN_POINT('Ctrl Pts',(1.73933737379134,102.074902395539,13.9231574941385));
#60243=CARTESIAN_POINT('Ctrl Pts',(1.72105119034358,102.081552937498,13.9733176567778));
#60244=CARTESIAN_POINT('Ctrl Pts',(1.70065806726025,102.088208317205,14.02264184491));
#60245=CARTESIAN_POINT('Ctrl Pts',(1.6779294041025,102.095625910034,14.0776149283855));
#60246=CARTESIAN_POINT('Ctrl Pts',(1.65258423716673,102.103049168786,14.1315469654491));
#60247=CARTESIAN_POINT('Ctrl Pts',(1.62470540352126,102.110478898782,14.1841714827423));
#60248=CARTESIAN_POINT('Ctrl Pts',(1.587534538446,102.120384962097,14.2543357821828));
#60249=CARTESIAN_POINT('Ctrl Pts',(1.5458600144321,102.130301369684,14.3221648529801));
#60250=CARTESIAN_POINT('Ctrl Pts',(1.49995615465894,102.140215749872,14.3869384221161));
#60251=CARTESIAN_POINT('Ctrl Pts',(1.48734045478903,102.142940506472,14.4047400604044));
#60252=CARTESIAN_POINT('Ctrl Pts',(1.47439954153894,102.145666410903,14.4223195999312));
#60253=CARTESIAN_POINT('Ctrl Pts',(1.46114438841258,102.148393241876,14.4396669702997));
#60254=CARTESIAN_POINT('Ctrl Pts',(1.4160858220106,102.157662625134,14.4986363109174));
#60255=CARTESIAN_POINT('Ctrl Pts',(1.3673941495347,102.166942663326,14.554920683033));
#60256=CARTESIAN_POINT('Ctrl Pts',(1.31552286783466,102.17622408939,14.6081351998545));
#60257=CARTESIAN_POINT('Ctrl Pts',(1.26336195040341,102.185557340521,14.6616468526824));
#60258=CARTESIAN_POINT('Ctrl Pts',(1.20798779172185,102.194892123591,14.712057171807));
#60259=CARTESIAN_POINT('Ctrl Pts',(1.14981223697842,102.204229756255,14.759048787269));
#60260=CARTESIAN_POINT('Ctrl Pts',(1.10365938611782,102.211637650681,14.7963289993731));
#60261=CARTESIAN_POINT('Ctrl Pts',(1.05574721904259,102.219046787273,14.8314554930974));
#60262=CARTESIAN_POINT('Ctrl Pts',(1.00625472402403,102.22646140787,14.8642839688946));
#60263=CARTESIAN_POINT('Ctrl Pts',(0.957401217845584,102.233780299613,14.8966886020533));
#60264=CARTESIAN_POINT('Ctrl Pts',(0.906999077813325,102.24110575819,14.9268587964748));
#60265=CARTESIAN_POINT('Ctrl Pts',(0.855243661351061,102.248437734779,14.9546304809421));
#60266=CARTESIAN_POINT('Ctrl Pts',(0.811904162093474,102.254577463056,14.9778862284681));
#60267=CARTESIAN_POINT('Ctrl Pts',(0.767613285959494,102.260722091471,14.9994610717527));
#60268=CARTESIAN_POINT('Ctrl Pts',(0.722496403019601,102.266870227603,15.0192545554209));
#60269=CARTESIAN_POINT('Ctrl Pts',(0.715359425450396,102.267842792789,15.0223856593392));
#60270=CARTESIAN_POINT('Ctrl Pts',(0.708201875033396,102.26881543306,15.0254721527729));
#60271=CARTESIAN_POINT('Ctrl Pts',(0.701024298372724,102.269788136874,15.0285136309998));
#60272=CARTESIAN_POINT('Ctrl Pts',(0.615939180428338,102.281318855751,15.0645682140294));
#60273=CARTESIAN_POINT('Ctrl Pts',(0.528030250094319,102.292859831511,15.094301342847));
#60274=CARTESIAN_POINT('Ctrl Pts',(0.438327753451193,102.304412015396,15.1174064003212));
#60275=CARTESIAN_POINT('Ctrl Pts',(0.326028892076433,102.318874233787,15.1463317005464));
#60276=CARTESIAN_POINT('Ctrl Pts',(0.2109168522982,102.333354294598,15.1648692645029));
#60277=CARTESIAN_POINT('Ctrl Pts',(0.0950175608262004,102.347853139992,
15.1724149891679));
#60278=CARTESIAN_POINT('Ctrl Pts',(0.0714651087958735,102.350799520046,
15.1739483921417));
#60279=CARTESIAN_POINT('Ctrl Pts',(0.0478803795012013,102.353746645807,
15.1750278648192));
#60280=CARTESIAN_POINT('Ctrl Pts',(0.0242805671923874,102.356694499776,
15.1756483834939));
#60281=CARTESIAN_POINT('Ctrl Pts',(-0.0380995050157335,102.36448639833,
15.1772885660185));
#60282=CARTESIAN_POINT('Ctrl Pts',(-0.100574621710386,102.372282104824,
15.175721745767));
#60283=CARTESIAN_POINT('Ctrl Pts',(-0.162848598268233,102.380081104816,
15.1710433231385));
#60284=CARTESIAN_POINT('Ctrl Pts',(-0.16935289488909,102.380895682784,15.1705546784401));
#60285=CARTESIAN_POINT('Ctrl Pts',(-0.175854998454186,102.381710296692,
15.170032090788));
#60286=CARTESIAN_POINT('Ctrl Pts',(-0.182354572319706,102.382524945955,
15.1694756700676));
#60287=CARTESIAN_POINT('Ctrl Pts',(-0.282839184518071,102.395119574,15.1608733029789));
#60288=CARTESIAN_POINT('Ctrl Pts',(-0.382747780320032,102.407726159361,
15.1441862030543));
#60289=CARTESIAN_POINT('Ctrl Pts',(-0.480937897916016,102.420370641684,
15.119773069128));
#60290=CARTESIAN_POINT('Ctrl Pts',(-0.501012570839243,102.422955767897,
15.1147818776456));
#60291=CARTESIAN_POINT('Ctrl Pts',(-0.521015380460676,102.425542478708,
15.1094675780936));
#60292=CARTESIAN_POINT('Ctrl Pts',(-0.540936493039643,102.428130996603,
15.1038329779157));
#60293=CARTESIAN_POINT('Ctrl Pts',(-0.658381045798903,102.443391556239,
15.0706142962156));
#60294=CARTESIAN_POINT('Ctrl Pts',(-0.772985749299366,102.458653750469,
15.0262582844338));
#60295=CARTESIAN_POINT('Ctrl Pts',(-0.88256931461987,102.473947768897,14.9713889903129));
#60296=CARTESIAN_POINT('Ctrl Pts',(-0.969660333172714,102.486102617472,
14.9277818791709));
#60297=CARTESIAN_POINT('Ctrl Pts',(-1.05357673346733,102.498277424713,14.8775317112844));
#60298=CARTESIAN_POINT('Ctrl Pts',(-1.13316354042019,102.510478295086,14.8210130851769));
#60299=CARTESIAN_POINT('Ctrl Pts',(-1.151776491269,102.513331710234,14.8077950852337));
#60300=CARTESIAN_POINT('Ctrl Pts',(-1.17015275037832,102.51618655043,14.794234422748));
#60301=CARTESIAN_POINT('Ctrl Pts',(-1.18827778456024,102.519042892776,14.7803362314562));
#60302=CARTESIAN_POINT('Ctrl Pts',(-1.21584666837573,102.523387500872,14.7591965405114));
#60303=CARTESIAN_POINT('Ctrl Pts',(-1.24283357738955,102.527735467329,14.7372764277728));
#60304=CARTESIAN_POINT('Ctrl Pts',(-1.26918653405338,102.532086809549,14.7145960189609));
#60305=CARTESIAN_POINT('Ctrl Pts',(-1.26919696311563,102.532088531573,14.7145870432927));
#60306=CARTESIAN_POINT('Ctrl Pts',(-1.26920739207869,102.532090253597,14.7145780675054));
#60307=CARTESIAN_POINT('Ctrl Pts',(-1.26921782094239,102.532091975622,14.714569091599));
#60308=CARTESIAN_POINT('Ctrl Pts',(-1.28456090482882,102.534625441661,14.7013636180524));
#60309=CARTESIAN_POINT('Ctrl Pts',(-1.29969240282331,102.537159012642,14.6878976203342));
#60310=CARTESIAN_POINT('Ctrl Pts',(-1.31460648803677,102.539692695173,14.6741800832161));
#60311=CARTESIAN_POINT('Ctrl Pts',(-1.39473833968511,102.553305911791,14.6004771618771));
#60312=CARTESIAN_POINT('Ctrl Pts',(-1.46859534561534,102.566922618664,14.5195113086034));
#60313=CARTESIAN_POINT('Ctrl Pts',(-1.53520819985887,102.580549113367,14.4327271126073));
#60314=CARTESIAN_POINT('Ctrl Pts',(-1.56437067294813,102.586514662953,14.3947338182342));
#60315=CARTESIAN_POINT('Ctrl Pts',(-1.5921446874049,102.592482079263,14.3556253967641));
#60316=CARTESIAN_POINT('Ctrl Pts',(-1.61844847607299,102.598453269443,14.3155236653087));
#60317=CARTESIAN_POINT('Ctrl Pts',(-1.61845152457497,102.598453961479,14.3155190176814));
#60318=CARTESIAN_POINT('Ctrl Pts',(-1.61845457305721,102.598454653516,14.3155143700407));
#60319=CARTESIAN_POINT('Ctrl Pts',(-1.61845762151969,102.598455345553,14.3155097223866));
#60320=CARTESIAN_POINT('Ctrl Pts',(-1.67094957347155,102.610371634069,14.2354810411373));
#60321=CARTESIAN_POINT('Ctrl Pts',(-1.71758551027082,102.622325341605,14.1514964047542));
#60322=CARTESIAN_POINT('Ctrl Pts',(-1.7577644917214,102.634297942855,14.0644150502798));
#60323=CARTESIAN_POINT('Ctrl Pts',(-1.7795209022467,102.640780955077,14.0172615976874));
#60324=CARTESIAN_POINT('Ctrl Pts',(-1.79938391606633,102.647269470249,13.9692004169408));
#60325=CARTESIAN_POINT('Ctrl Pts',(-1.81725750356379,102.653763399263,13.9203696200825));
#60326=CARTESIAN_POINT('Ctrl Pts',(-1.82773260126707,102.657569268729,13.8917515618392));
#60327=CARTESIAN_POINT('Ctrl Pts',(-1.83752439343444,102.661376997973,13.86286916227));
#60328=CARTESIAN_POINT('Ctrl Pts',(-1.84661362179659,102.665186567981,13.8337502505934));
#60329=CARTESIAN_POINT('Ctrl Pts',(-1.86607209132476,102.673342200006,13.7714116853185));
#60330=CARTESIAN_POINT('Ctrl Pts',(-1.88230101863283,102.681502005255,13.7080220587029));
#60331=CARTESIAN_POINT('Ctrl Pts',(-1.89528967154877,102.689668313321,13.6439064532373));
#60332=CARTESIAN_POINT('Ctrl Pts',(-1.90747059011716,102.697326777536,13.5837780492995));
#60333=CARTESIAN_POINT('Ctrl Pts',(-1.91680197140128,102.704990534476,13.5230145044515));
#60334=CARTESIAN_POINT('Ctrl Pts',(-1.92327094072407,102.712665487171,13.461849798818));
#60335=CARTESIAN_POINT('Ctrl Pts',(-1.93042148727562,102.721149080737,13.3942407171976));
#60336=CARTESIAN_POINT('Ctrl Pts',(-1.93407349653831,102.729645648482,13.3261467485587));
#60337=CARTESIAN_POINT('Ctrl Pts',(-1.93418979043081,102.738159614938,13.257911754622));
#60338=CARTESIAN_POINT('Ctrl Pts',(-1.93434417440255,102.749462185765,13.1673275532573));
#60339=CARTESIAN_POINT('Ctrl Pts',(-1.92825964438706,102.760808710744,13.0764949618271));
#60340=CARTESIAN_POINT('Ctrl Pts',(-1.91585938591349,102.772173558771,12.9863960700822));
#60341=CARTESIAN_POINT('Ctrl Pts',(-1.9138656038006,102.774000861868,12.9719094721507));
#60342=CARTESIAN_POINT('Ctrl Pts',(-1.91170865694649,102.775828638566,12.9574418448425));
#60343=CARTESIAN_POINT('Ctrl Pts',(-1.90938835218873,102.777656782239,12.942997266508));
#60344=CARTESIAN_POINT('Ctrl Pts',(-1.89995256426744,102.785091140129,12.8842567164484));
#60345=CARTESIAN_POINT('Ctrl Pts',(-1.8878157775183,102.792517866429,12.8259022336328));
#60346=CARTESIAN_POINT('Ctrl Pts',(-1.87298374690933,102.799937257785,12.7682421088022));
#60347=CARTESIAN_POINT('Ctrl Pts',(-1.8729798057892,102.799939229242,12.7682267875367));
#60348=CARTESIAN_POINT('Ctrl Pts',(-1.87297586447891,102.799941200699,12.7682114663202));
#60349=CARTESIAN_POINT('Ctrl Pts',(-1.87297192297847,102.799943172155,12.7681961451527));
#60350=CARTESIAN_POINT('Ctrl Pts',(-1.85503528338224,102.808914704184,12.6984739003073));
#60351=CARTESIAN_POINT('Ctrl Pts',(-1.83312581629033,102.817917013102,12.6296507484991));
#60352=CARTESIAN_POINT('Ctrl Pts',(-1.80744518956224,102.826929347774,12.5621627833291));
#60353=CARTESIAN_POINT('Ctrl Pts',(-1.77925088720554,102.836823829377,12.4880689492654));
#60354=CARTESIAN_POINT('Ctrl Pts',(-1.74651361060821,102.846730296013,12.4155844666192));
#60355=CARTESIAN_POINT('Ctrl Pts',(-1.70947907627453,102.856651617251,12.3452247196208));
#60356=CARTESIAN_POINT('Ctrl Pts',(-1.69542614491709,102.860416310094,12.3185263767718));
#60357=CARTESIAN_POINT('Ctrl Pts',(-1.68075401715658,102.864183244747,12.2921332498829));
#60358=CARTESIAN_POINT('Ctrl Pts',(-1.66547438252735,102.86795287411,12.2660717160896));
#60359=CARTESIAN_POINT('Ctrl Pts',(-1.63366447046097,102.875800678163,12.2118155039226));
#60360=CARTESIAN_POINT('Ctrl Pts',(-1.59922589293084,102.883658946406,12.1590052148897));
#60361=CARTESIAN_POINT('Ctrl Pts',(-1.56231253061641,102.89152602577,12.1079052427554));
#60362=CARTESIAN_POINT('Ctrl Pts',(-1.5265805530251,102.899141325106,12.0584406872466));
#60363=CARTESIAN_POINT('Ctrl Pts',(-1.48853265842265,102.906764399259,12.010581333861));
#60364=CARTESIAN_POINT('Ctrl Pts',(-1.44829244275389,102.91439729182,11.9645434850451));
#60365=CARTESIAN_POINT('Ctrl Pts',(-1.40956940665713,102.921742400916,11.9202414043558));
#60366=CARTESIAN_POINT('Ctrl Pts',(-1.36881158033374,102.929097353996,11.8776221213014));
#60367=CARTESIAN_POINT('Ctrl Pts',(-1.32614769321825,102.936461761375,11.8369019475121));
#60368=CARTESIAN_POINT('Ctrl Pts',(-1.32614712479651,102.936461859493,11.8369014049869));
#60369=CARTESIAN_POINT('Ctrl Pts',(-1.32614655637446,102.936461957611,11.8369008624621));
#60370=CARTESIAN_POINT('Ctrl Pts',(-1.32614598795205,102.936462055729,11.8369003199376));
#60371=CARTESIAN_POINT('Ctrl Pts',(-1.26598108840654,102.946847380366,11.7794765976501));
#60372=CARTESIAN_POINT('Ctrl Pts',(-1.20204608060229,102.957302316582,11.725860928667));
#60373=CARTESIAN_POINT('Ctrl Pts',(-1.13488521307142,102.967748055726,11.676348725627));
#60374=CARTESIAN_POINT('Ctrl Pts',(-1.06602794478382,102.978457641369,11.6255859053483));
#60375=CARTESIAN_POINT('Ctrl Pts',(-0.993778276255049,102.989157524831,
11.5791364441837));
#60376=CARTESIAN_POINT('Ctrl Pts',(-0.91872494735699,102.999860013816,11.5373700252457));
#60377=CARTESIAN_POINT('Ctrl Pts',(-0.843891976344137,103.010531080106,
11.4957262332436));
#60378=CARTESIAN_POINT('Ctrl Pts',(-0.766271104913007,103.021204517336,
11.4587392283868));
#60379=CARTESIAN_POINT('Ctrl Pts',(-0.686476193102858,103.031898548805,
11.4267986738155));
#60380=CARTESIAN_POINT('Ctrl Pts',(-0.607735369721644,103.042451312433,
11.395280053027));
#60381=CARTESIAN_POINT('Ctrl Pts',(-0.526875037269166,103.053059105642,
11.3686857904221));
#60382=CARTESIAN_POINT('Ctrl Pts',(-0.444524447119211,103.063682235268,
11.3473774222192));
#60383=CARTESIAN_POINT('Ctrl Pts',(-0.415305104344762,103.067451496245,
11.3398168629889));
#60384=CARTESIAN_POINT('Ctrl Pts',(-0.385898388663963,103.071222664651,
11.3329216111304));
#60385=CARTESIAN_POINT('Ctrl Pts',(-0.356333030015614,103.074995438591,
11.3267075705126));
#60386=CARTESIAN_POINT('Ctrl Pts',(-0.327472646434759,103.078678252128,
11.3206417014004));
#60387=CARTESIAN_POINT('Ctrl Pts',(-0.298451485147569,103.082363820692,
11.3152229434911));
#60388=CARTESIAN_POINT('Ctrl Pts',(-0.26930238812307,103.086051687325,11.3104518308713));
#60389=CARTESIAN_POINT('Ctrl Pts',(-0.20458121217553,103.094240039269,11.2998582945064));
#60390=CARTESIAN_POINT('Ctrl Pts',(-0.139230056703358,103.102439623834,
11.2924587532058));
#60391=CARTESIAN_POINT('Ctrl Pts',(-0.0736083162059315,103.110645640778,
11.2882471963228));
#60392=CARTESIAN_POINT('Ctrl Pts',(-0.00798657570850504,103.118851657722,
11.2840356394398));
#60393=CARTESIAN_POINT('Ctrl Pts',(0.0579131368202692,103.127065048991,
11.2830092363397));
#60394=CARTESIAN_POINT('Ctrl Pts',(0.123805004717542,103.135290075073,11.2851582785366));
#60395=CARTESIAN_POINT('Ctrl Pts',(0.214244652810041,103.146579305265,11.2881079387334));
#60396=CARTESIAN_POINT('Ctrl Pts',(0.304695613052521,103.157893607708,11.2970399445611));
#60397=CARTESIAN_POINT('Ctrl Pts',(0.394391122754232,103.169243831579,11.3119717209192));
#60398=CARTESIAN_POINT('Ctrl Pts',(0.471293148687995,103.178975146039,11.3247737425203));
#60399=CARTESIAN_POINT('Ctrl Pts',(0.547630135722643,103.188856484811,11.3420316864373));
#60400=CARTESIAN_POINT('Ctrl Pts',(0.6228077283068,103.198711670681,11.3636742783697));
#60401=CARTESIAN_POINT('Ctrl Pts',(0.636214023632117,103.200469129622,11.3675337658722));
#60402=CARTESIAN_POINT('Ctrl Pts',(0.649583533381155,103.202225764564,11.371532585887));
#60403=CARTESIAN_POINT('Ctrl Pts',(0.662913004719139,103.2039805866,11.3756702041141));
#60404=CARTESIAN_POINT('Ctrl Pts',(0.693468921848236,103.208003266522,11.3851551053867));
#60405=CARTESIAN_POINT('Ctrl Pts',(0.723812672012547,103.212016229393,11.3953690133007));
#60406=CARTESIAN_POINT('Ctrl Pts',(0.753899777174038,103.216013772683,11.4063046363991));
#60407=CARTESIAN_POINT('Ctrl Pts',(0.753902936989191,103.216014192514,11.4063057848827));
#60408=CARTESIAN_POINT('Ctrl Pts',(0.753906096801517,103.216014612345,11.4063069333743));
#60409=CARTESIAN_POINT('Ctrl Pts',(0.753909256611011,103.216015032176,11.4063080818738));
#60410=CARTESIAN_POINT('Ctrl Pts',(0.831077829019071,103.226268096064,11.4343566304229));
#60411=CARTESIAN_POINT('Ctrl Pts',(0.906727440592672,103.236537191423,11.4672517312917));
#60412=CARTESIAN_POINT('Ctrl Pts',(0.980272721481336,103.246808793055,11.5046490674096));
#60413=CARTESIAN_POINT('Ctrl Pts',(1.05449406478093,103.257174816025,11.542390177226));
#60414=CARTESIAN_POINT('Ctrl Pts',(1.12657224304582,103.267543619923,11.5847147858458));
#60415=CARTESIAN_POINT('Ctrl Pts',(1.195954914188,103.277912779759,11.6312655663058));
#60416=CARTESIAN_POINT('Ctrl Pts',(1.26536731042619,103.288286381977,11.6778362901666));
#60417=CARTESIAN_POINT('Ctrl Pts',(1.33208389772585,103.298660751963,11.7286358289529));
#60418=CARTESIAN_POINT('Ctrl Pts',(1.39557045685016,103.309115263228,11.7833497909187));
#60419=CARTESIAN_POINT('Ctrl Pts',(1.45852793730277,103.319482649611,11.8376077825071));
#60420=CARTESIAN_POINT('Ctrl Pts',(1.51832441931271,103.32987163696,11.8956962147245));
#60421=CARTESIAN_POINT('Ctrl Pts',(1.57448689960039,103.340282729759,11.9573233898565));
#60422=CARTESIAN_POINT('Ctrl Pts',(1.6076778484669,103.346435485958,11.9937438685839));
#60423=CARTESIAN_POINT('Ctrl Pts',(1.63960000505281,103.352596068282,12.031401157824));
#60424=CARTESIAN_POINT('Ctrl Pts',(1.67015586494958,103.358766683304,12.0702437448549));
#60425=CARTESIAN_POINT('Ctrl Pts',(1.68429678126935,103.361622376155,12.088219667467));
#60426=CARTESIAN_POINT('Ctrl Pts',(1.69813887463945,103.364478977697,12.106441678321));
#60427=CARTESIAN_POINT('Ctrl Pts',(1.71167812354762,103.36733676856,12.1248998638413));
#60428=CARTESIAN_POINT('Ctrl Pts',(1.76588854289307,103.378779208398,12.1988054389729));
#60429=CARTESIAN_POINT('Ctrl Pts',(1.81524252832232,103.390240048391,12.2764916368507));
#60430=CARTESIAN_POINT('Ctrl Pts',(1.85941492971959,103.401726965554,12.3572704625853));
#60431=CARTESIAN_POINT('Ctrl Pts',(1.89162372670102,103.410102778757,12.4161712403602));
#60432=CARTESIAN_POINT('Ctrl Pts',(1.92107843238021,103.418492896569,12.4767200850574));
#60433=CARTESIAN_POINT('Ctrl Pts',(1.94763876734934,103.426898617052,12.5386425155357));
#60434=CARTESIAN_POINT('Ctrl Pts',(1.9916465790334,103.440826053001,12.6412417735148));
#60435=CARTESIAN_POINT('Ctrl Pts',(2.02770239861494,103.4547950446,12.7476036022882));
#60436=CARTESIAN_POINT('Ctrl Pts',(2.05514361094351,103.468802788122,12.8564086888768));
#60437=CARTESIAN_POINT('Ctrl Pts',(2.07383108038386,103.478342063424,12.9305049680876));
#60438=CARTESIAN_POINT('Ctrl Pts',(2.08852214736075,103.487899095292,13.0057325280781));
#60439=CARTESIAN_POINT('Ctrl Pts',(2.09901135869357,103.497469170066,13.0816417223927));
#60440=CARTESIAN_POINT('Ctrl Pts',(2.10151813830666,103.499756288476,13.0997829929532));
#60441=CARTESIAN_POINT('Ctrl Pts',(2.10378500003126,103.50204413754,13.1179630708559));
#60442=CARTESIAN_POINT('Ctrl Pts',(2.10580936422368,103.504332751059,13.1361765897923));
#60443=CARTESIAN_POINT('Ctrl Pts',(2.1141529711838,103.51376548641,13.2112453170178));
#60444=CARTESIAN_POINT('Ctrl Pts',(2.11837768012527,103.523211823801,13.2868869077833));
#60445=CARTESIAN_POINT('Ctrl Pts',(2.11854006212329,103.532671927025,13.3626648484844));
#60446=CARTESIAN_POINT('Ctrl Pts',(2.11870409170741,103.542228015856,13.4392116594046));
#60447=CARTESIAN_POINT('Ctrl Pts',(2.11472397092425,103.551799338126,13.5159072693305));
#60448=CARTESIAN_POINT('Ctrl Pts',(2.10664856791811,103.561389659365,13.5923313907327));
#60449=CARTESIAN_POINT('Ctrl Pts',(2.09854131514464,103.57101780528,13.6690569324458));
#60450=CARTESIAN_POINT('Ctrl Pts',(2.08630637981466,103.580664825254,13.7455068118658));
#60451=CARTESIAN_POINT('Ctrl Pts',(2.06998377103888,103.590333688978,13.8212470882111));
#60452=CARTESIAN_POINT('Ctrl Pts',(2.05180076205487,103.601104579733,13.90562000581));
#60453=CARTESIAN_POINT('Ctrl Pts',(2.02854198299513,103.611902775125,13.9891132148051));
#60454=CARTESIAN_POINT('Ctrl Pts',(2.00028426875198,103.622722405094,14.0710475380929));
#60455=CARTESIAN_POINT('Ctrl Pts',(1.98078817873922,103.630187286293,14.1275771967981));
#60456=CARTESIAN_POINT('Ctrl Pts',(1.95891301016525,103.637662366928,14.1833647902223));
#60457=CARTESIAN_POINT('Ctrl Pts',(1.93469031992368,103.645145688019,14.238189090484));
#60458=CARTESIAN_POINT('Ctrl Pts',(1.92670015647016,103.647614156967,14.2562735854739));
#60459=CARTESIAN_POINT('Ctrl Pts',(1.91845496550383,103.65008341462,14.274252500844));
#60460=CARTESIAN_POINT('Ctrl Pts',(1.90995524976028,103.652553614003,14.2921195862409));
#60461=CARTESIAN_POINT('Ctrl Pts',(1.89491267730729,103.656925307634,14.3237402821224));
#60462=CARTESIAN_POINT('Ctrl Pts',(1.87906984952767,103.661300828955,14.3550170548085));
#60463=CARTESIAN_POINT('Ctrl Pts',(1.86245045886573,103.665680166301,14.3859142415477));
#60464=CARTESIAN_POINT('Ctrl Pts',(1.82578231744815,103.675342503772,14.4540841543806));
#60465=CARTESIAN_POINT('Ctrl Pts',(1.78533663347209,103.685022518145,14.5203994452426));
#60466=CARTESIAN_POINT('Ctrl Pts',(1.741384462713,103.69471746067,14.5844623370871));
#60467=CARTESIAN_POINT('Ctrl Pts',(1.69810640721786,103.704263707268,14.6475426660116));
#60468=CARTESIAN_POINT('Ctrl Pts',(1.65142912045016,103.713824666201,14.7084418930771));
#60469=CARTESIAN_POINT('Ctrl Pts',(1.60157737672231,103.723404640978,14.766824779694));
#60470=CARTESIAN_POINT('Ctrl Pts',(1.55049795325477,103.733220538113,14.8266454392288));
#60471=CARTESIAN_POINT('Ctrl Pts',(1.49608623762861,103.743056026327,14.8838207915626));
#60472=CARTESIAN_POINT('Ctrl Pts',(1.43861834771889,103.752908804079,14.9379465120586));
#60473=CARTESIAN_POINT('Ctrl Pts',(1.37072344167981,103.764549277058,15.0018928430121));
#60474=CARTESIAN_POINT('Ctrl Pts',(1.29855742573973,103.776214953096,15.0615893537912));
#60475=CARTESIAN_POINT('Ctrl Pts',(1.22272263305689,103.787907076375,15.1165784625959));
#60476=CARTESIAN_POINT('Ctrl Pts',(1.09926103729112,103.806942246735,15.2061025831557));
#60477=CARTESIAN_POINT('Ctrl Pts',(0.966078309936567,103.826046911828,15.2831457798114));
#60478=CARTESIAN_POINT('Ctrl Pts',(0.825808902011507,103.845220872878,15.3457040765431));
#60479=CARTESIAN_POINT('Ctrl Pts',(0.803092666440182,103.848326041871,15.3558352165152));
#60480=CARTESIAN_POINT('Ctrl Pts',(0.780190517107452,103.85143303692,15.3655865045497));
#60481=CARTESIAN_POINT('Ctrl Pts',(0.757113321523855,103.854541900927,15.3749495554873));
#60482=CARTESIAN_POINT('Ctrl Pts',(0.682328192372906,103.864616643131,15.4052919327091));
#60483=CARTESIAN_POINT('Ctrl Pts',(0.605703386872605,103.874711165779,15.4315568903168));
#60484=CARTESIAN_POINT('Ctrl Pts',(0.527732548759711,103.884823374306,15.4535997137354));
#60485=CARTESIAN_POINT('Ctrl Pts',(0.473764907657852,103.891822555714,15.4688566894447));
#60486=CARTESIAN_POINT('Ctrl Pts',(0.419152414187769,103.89883022874,15.4820914790451));
#60487=CARTESIAN_POINT('Ctrl Pts',(0.364045913284344,103.905847363209,15.4932599819668));
#60488=CARTESIAN_POINT('Ctrl Pts',(0.364027306121928,103.905849732602,15.4932637531035));
#60489=CARTESIAN_POINT('Ctrl Pts',(0.36400869890318,103.905852101996,15.4932675240046));
#60490=CARTESIAN_POINT('Ctrl Pts',(0.363990091628161,103.905854471391,15.49327129467));
#60491=CARTESIAN_POINT('Ctrl Pts',(0.246306748264742,103.920839919279,15.5171191993108));
#60492=CARTESIAN_POINT('Ctrl Pts',(0.126383243509028,103.935866907769,15.531541288314));
#60493=CARTESIAN_POINT('Ctrl Pts',(0.00574208375256261,103.951031871898,
15.5360830723919));
#60494=CARTESIAN_POINT('Ctrl Pts',(-0.0117271028536529,103.953227802281,
15.5367407357776));
#60495=CARTESIAN_POINT('Ctrl Pts',(-0.0292112542072715,103.955426615217,
15.5371911983692));
#60496=CARTESIAN_POINT('Ctrl Pts',(-0.0467056605022778,103.957628592728,
15.5374330531079));
#60497=CARTESIAN_POINT('Ctrl Pts',(-0.046708228653569,103.957628915975,
15.5374330886118));
#60498=CARTESIAN_POINT('Ctrl Pts',(-0.0467107968050665,103.957629239221,
15.5374331241112));
#60499=CARTESIAN_POINT('Ctrl Pts',(-0.0467133649567995,103.957629562468,
15.5374331596061));
#60500=CARTESIAN_POINT('Ctrl Pts',(-0.185025688623094,103.9750385958,15.5393448000133));
#60501=CARTESIAN_POINT('Ctrl Pts',(-0.324007003002818,103.992370846683,
15.5284412546859));
#60502=CARTESIAN_POINT('Ctrl Pts',(-0.46124508751448,104.00969676724,15.5048857075416));
#60503=CARTESIAN_POINT('Ctrl Pts',(-0.589157278613788,104.025845320094,
15.4829308569001));
#60504=CARTESIAN_POINT('Ctrl Pts',(-0.71555758177041,104.041990045687,15.4499886266189));
#60505=CARTESIAN_POINT('Ctrl Pts',(-0.838547870354058,104.058221754719,
15.4061513096145));
#60506=CARTESIAN_POINT('Ctrl Pts',(-0.847508384789385,104.059404323398,
15.4029575215817));
#60507=CARTESIAN_POINT('Ctrl Pts',(-0.856450830115381,104.060587360047,
15.3997058739288));
#60508=CARTESIAN_POINT('Ctrl Pts',(-0.865373302888538,104.06177483061,15.3963930849294));
#60509=CARTESIAN_POINT('Ctrl Pts',(-0.865379805326339,104.061775696004,
15.3963906706654));
#60510=CARTESIAN_POINT('Ctrl Pts',(-0.865386307753549,104.0617765614,15.396388256369));
#60511=CARTESIAN_POINT('Ctrl Pts',(-0.865392810170118,104.061777426799,
15.3963858420401));
#60512=CARTESIAN_POINT('Ctrl Pts',(-0.913587803696001,104.068191639078,
15.3784911771197));
#60513=CARTESIAN_POINT('Ctrl Pts',(-0.961214152223209,104.074614481611,
15.3589195478217));
#60514=CARTESIAN_POINT('Ctrl Pts',(-1.00817362924042,104.081044261839,15.3377268451394));
#60515=CARTESIAN_POINT('Ctrl Pts',(-1.10307424807729,104.094038233693,15.2948984167341));
#60516=CARTESIAN_POINT('Ctrl Pts',(-1.1952221055417,104.107191365773,15.2453345790668));
#60517=CARTESIAN_POINT('Ctrl Pts',(-1.28377358272751,104.120396167781,15.1895659707695));
#60518=CARTESIAN_POINT('Ctrl Pts',(-1.30872560007234,104.124117014222,15.1738515035946));
#60519=CARTESIAN_POINT('Ctrl Pts',(-1.33339232672395,104.12784200427,15.1576442027968));
#60520=CARTESIAN_POINT('Ctrl Pts',(-1.35775547083743,104.13156883061,15.1409554752094));
#60521=CARTESIAN_POINT('Ctrl Pts',(-1.43743384378368,104.143757218843,15.0863758751989));
#60522=CARTESIAN_POINT('Ctrl Pts',(-1.51385936633913,104.155955491083,15.0266568408663));
#60523=CARTESIAN_POINT('Ctrl Pts',(-1.58634113998981,104.168074490316,14.9622567875904));
#60524=CARTESIAN_POINT('Ctrl Pts',(-1.58635458946933,104.168076739078,14.9622448377283));
#60525=CARTESIAN_POINT('Ctrl Pts',(-1.58636803881416,104.168078987838,14.9622328877027));
#60526=CARTESIAN_POINT('Ctrl Pts',(-1.58638148802423,104.168081236597,14.9622209375136));
#60527=CARTESIAN_POINT('Ctrl Pts',(-1.65297955240087,104.179216686535,14.9030457548682));
#60528=CARTESIAN_POINT('Ctrl Pts',(-1.71627492265425,104.190321643138,14.8398596493715));
#60529=CARTESIAN_POINT('Ctrl Pts',(-1.77586158642476,104.201440127394,14.7731028926433));
#60530=CARTESIAN_POINT('Ctrl Pts',(-1.81119809134838,104.20803368959,14.7335143284656));
#60531=CARTESIAN_POINT('Ctrl Pts',(-1.84523090896447,104.21463233714,14.692669492739));
#60532=CARTESIAN_POINT('Ctrl Pts',(-1.87787879786267,104.221247238861,14.650653947854));
#60533=CARTESIAN_POINT('Ctrl Pts',(-1.87788445285372,104.221248384638,14.6506466702768));
#60534=CARTESIAN_POINT('Ctrl Pts',(-1.8778901078031,104.221249530416,14.6506393926647));
#60535=CARTESIAN_POINT('Ctrl Pts',(-1.87789576271087,104.221250676194,14.6506321150175));
#60536=CARTESIAN_POINT('Ctrl Pts',(-1.94309068071361,104.23446024942,14.5667287817711));
#60537=CARTESIAN_POINT('Ctrl Pts',(-2.00274975442905,104.247731816801,14.4781733383104));
#60538=CARTESIAN_POINT('Ctrl Pts',(-2.05600639711968,104.261043873617,14.3856565465746));
#60539=CARTESIAN_POINT('Ctrl Pts',(-2.07052185168252,104.264672163838,14.3604404755102));
#60540=CARTESIAN_POINT('Ctrl Pts',(-2.08456176106021,104.268303308782,14.3349302817011));
#60541=CARTESIAN_POINT('Ctrl Pts',(-2.09810878331213,104.271936536213,14.3091403214694));
#60542=CARTESIAN_POINT('Ctrl Pts',(-2.101723072737,104.272905866243,14.3022596669019));
#60543=CARTESIAN_POINT('Ctrl Pts',(-2.10530227924626,104.273875343736,14.2953590991255));
#60544=CARTESIAN_POINT('Ctrl Pts',(-2.10884618910972,104.274844823265,14.2884389695789));
#60545=CARTESIAN_POINT('Ctrl Pts',(-2.10884833437069,104.274845410127,14.2884347805661));
#60546=CARTESIAN_POINT('Ctrl Pts',(-2.10885047961875,104.27484599699,14.2884305915461));
#60547=CARTESIAN_POINT('Ctrl Pts',(-2.10885262485392,104.274846583852,14.2884264025188));
#60548=CARTESIAN_POINT('Ctrl Pts',(-2.16974195938393,104.291503801379,14.1695270438694));
#60549=CARTESIAN_POINT('Ctrl Pts',(-2.22023732229178,104.308178181703,14.0447781897744));
#60550=CARTESIAN_POINT('Ctrl Pts',(-2.25989936296388,104.324896771998,13.9161976968558));
#60551=CARTESIAN_POINT('Ctrl Pts',(-2.27625468960672,104.331790971102,13.8631753125824));
#60552=CARTESIAN_POINT('Ctrl Pts',(-2.29076816705059,104.338692649523,13.8095019061632));
#60553=CARTESIAN_POINT('Ctrl Pts',(-2.30341055969347,104.345603539293,13.7553209891809));
#60554=CARTESIAN_POINT('Ctrl Pts',(-2.34492074316024,104.368294837562,13.5774227172425));
#60555=CARTESIAN_POINT('Ctrl Pts',(-2.36619407616884,104.39114322775,13.3940410050713));
#60556=CARTESIAN_POINT('Ctrl Pts',(-2.36638569117636,104.414108494208,13.2101467996555));
#60557=CARTESIAN_POINT('Ctrl Pts',(-2.36653130410778,104.431560361956,13.0704010946139));
#60558=CARTESIAN_POINT('Ctrl Pts',(-2.35442107477345,104.449151659613,12.9303487498688));
#60559=CARTESIAN_POINT('Ctrl Pts',(-2.32963645208776,104.466892315332,12.7921344291781));
#60560=CARTESIAN_POINT('Ctrl Pts',(-2.31730459512665,104.475719370377,12.7233643996985));
#60561=CARTESIAN_POINT('Ctrl Pts',(-2.30183392522366,104.484582955546,12.6550465613128));
#60562=CARTESIAN_POINT('Ctrl Pts',(-2.28328232913452,104.493398049182,12.5874422945741));
#60563=CARTESIAN_POINT('Ctrl Pts',(-2.28327721304368,104.493400480176,12.5874236509184));
#60564=CARTESIAN_POINT('Ctrl Pts',(-2.28327209671646,104.493402911168,12.5874050073124));
#60565=CARTESIAN_POINT('Ctrl Pts',(-2.28326698015286,104.493405342157,12.5873863637562));
#60566=CARTESIAN_POINT('Ctrl Pts',(-2.2575264836489,104.505635204904,12.4935940388947));
#60567=CARTESIAN_POINT('Ctrl Pts',(-2.22579953848601,104.517804679907,12.4010580314143));
#60568=CARTESIAN_POINT('Ctrl Pts',(-2.18843650510388,104.529954291053,12.3105092748478));
#60569=CARTESIAN_POINT('Ctrl Pts',(-2.17837609430193,104.533225708498,12.2861280186648));
#60570=CARTESIAN_POINT('Ctrl Pts',(-2.16790732621083,104.536495663971,12.2618909596933));
#60571=CARTESIAN_POINT('Ctrl Pts',(-2.15703763802858,104.539764899956,12.2378125948701));
#60572=CARTESIAN_POINT('Ctrl Pts',(-2.11792783245846,104.551527811789,12.1511771596219));
#60573=CARTESIAN_POINT('Ctrl Pts',(-2.07362431716633,104.563282862789,12.0665933270532));
#60574=CARTESIAN_POINT('Ctrl Pts',(-2.02442105756846,104.575107823939,11.9847268004912));
#60575=CARTESIAN_POINT('Ctrl Pts',(-2.0082166354671,104.579002213526,11.9577651771511));
#60576=CARTESIAN_POINT('Ctrl Pts',(-1.99148103306734,104.582904132789,11.9310986069685));
#60577=CARTESIAN_POINT('Ctrl Pts',(-1.97422558590797,104.586816202795,11.9047517760302));
#60578=CARTESIAN_POINT('Ctrl Pts',(-1.90537055124895,104.602426677178,11.7996190639854));
#60579=CARTESIAN_POINT('Ctrl Pts',(-1.8283375168013,104.618118484337,11.6995233412364));
#60580=CARTESIAN_POINT('Ctrl Pts',(-1.74402731031377,104.633846836001,11.6057135876507));
#60581=CARTESIAN_POINT('Ctrl Pts',(-1.69274105295165,104.643414459245,11.5486487153664));
#60582=CARTESIAN_POINT('Ctrl Pts',(-1.63875720934119,104.652996539739,11.4939035602363));
#60583=CARTESIAN_POINT('Ctrl Pts',(-1.5821558071339,104.662685002477,11.4418579253114));
#60584=CARTESIAN_POINT('Ctrl Pts',(-1.5749876441991,104.663911977018,11.4352667177328));
#60585=CARTESIAN_POINT('Ctrl Pts',(-1.56777753282949,104.665140649707,11.4287188657917));
#60586=CARTESIAN_POINT('Ctrl Pts',(-1.560525666171,104.666371200229,11.4222151919796));
#60587=CARTESIAN_POINT('Ctrl Pts',(-1.5055804555543,104.675694711097,11.3729388133293));
#60588=CARTESIAN_POINT('Ctrl Pts',(-1.44825119977244,104.685105532953,11.3261676546078));
#60589=CARTESIAN_POINT('Ctrl Pts',(-1.38881768833724,104.694505635279,11.2820824080902));
#60590=CARTESIAN_POINT('Ctrl Pts',(-1.34605129191711,104.701269639168,11.2503601173602));
#60591=CARTESIAN_POINT('Ctrl Pts',(-1.30219489123442,104.708028222326,11.2200275463276));
#60592=CARTESIAN_POINT('Ctrl Pts',(-1.25734215753611,104.714746897393,11.1911392063596));
#60593=CARTESIAN_POINT('Ctrl Pts',(-1.25035757338188,104.715793146919,11.1866406390495));
#60594=CARTESIAN_POINT('Ctrl Pts',(-1.24334895990707,104.716838419881,11.1821771946694));
#60595=CARTESIAN_POINT('Ctrl Pts',(-1.23631670261522,104.717882600176,11.177749122534));
#60596=CARTESIAN_POINT('Ctrl Pts',(-1.23628269719713,104.71788764945,11.1777277100006));
#60597=CARTESIAN_POINT('Ctrl Pts',(-1.23624869119803,104.717892698706,11.1777062982871));
#60598=CARTESIAN_POINT('Ctrl Pts',(-1.23621468461808,104.717897747947,11.1776848873937));
#60599=CARTESIAN_POINT('Ctrl Pts',(-1.15935205338826,104.729310183284,11.1292913822398));
#60600=CARTESIAN_POINT('Ctrl Pts',(-1.07951740542718,104.740639255472,11.0850877874245));
#60601=CARTESIAN_POINT('Ctrl Pts',(-0.997264676478942,104.751932187046,
11.045326783786));
#60602=CARTESIAN_POINT('Ctrl Pts',(-0.969483553245763,104.755746410935,
11.0318973771745));
#60603=CARTESIAN_POINT('Ctrl Pts',(-0.941427015877044,104.75955647207,11.0189746984554));
#60604=CARTESIAN_POINT('Ctrl Pts',(-0.913117709667293,104.763364066709,
11.0065681929864));
#60605=CARTESIAN_POINT('Ctrl Pts',(-0.842634762476249,104.772844005563,
10.9756791608313));
#60606=CARTESIAN_POINT('Ctrl Pts',(-0.770581015164748,104.782310004766,
10.9479894287309));
#60607=CARTESIAN_POINT('Ctrl Pts',(-0.69725070595239,104.791845872049,10.9237153410963));
#60608=CARTESIAN_POINT('Ctrl Pts',(-0.652537084713335,104.79766042762,10.9089140621699));
#60609=CARTESIAN_POINT('Ctrl Pts',(-0.607349743046027,104.803500833865,
10.8953831642764));
#60610=CARTESIAN_POINT('Ctrl Pts',(-0.561764445978303,104.809384893613,
10.8831744227458));
#60611=CARTESIAN_POINT('Ctrl Pts',(-0.454886573630109,104.823180477433,
10.854550186363));
#60612=CARTESIAN_POINT('Ctrl Pts',(-0.34593646565383,104.837005124755,10.83285266738));
#60613=CARTESIAN_POINT('Ctrl Pts',(-0.235792247083463,104.850865137857,
10.8182859260231));
#60614=CARTESIAN_POINT('Ctrl Pts',(-0.220693775708796,104.852765056108,
10.8162891300927));
#60615=CARTESIAN_POINT('Ctrl Pts',(-0.20557283729048,104.854665640299,10.8144264009999));
#60616=CARTESIAN_POINT('Ctrl Pts',(-0.190431669900425,104.856566907995,
10.812698336862));
#60617=CARTESIAN_POINT('Ctrl Pts',(-0.152853269521076,104.861285606155,
10.8084095073165));
#60618=CARTESIAN_POINT('Ctrl Pts',(-0.115148932112492,104.866008682015,
10.8049499169657));
#60619=CARTESIAN_POINT('Ctrl Pts',(-0.0773493836361189,104.870737059702,
10.8023297075166));
#60620=CARTESIAN_POINT('Ctrl Pts',(-1.07958803427197,23.125761603439,10.3785207772594));
#60621=CARTESIAN_POINT('Ctrl Pts',(-0.34554065930921,23.2239632414138,10.0948431126673));
#60622=CARTESIAN_POINT('Ctrl Pts',(1.34243986332755,23.420102020386,10.1127125594068));
#60623=CARTESIAN_POINT('Ctrl Pts',(3.18017348682762,23.7162461148519,11.8764837958139));
#60624=CARTESIAN_POINT('Ctrl Pts',(3.32060625935821,24.0131814407576,14.4260813171523));
#60625=CARTESIAN_POINT('Ctrl Pts',(1.67691747945551,24.3117154001464,16.3981628554893));
#60626=CARTESIAN_POINT('Ctrl Pts',(-0.880376510953372,24.6113532051016,
16.7210498975078));
#60627=CARTESIAN_POINT('Ctrl Pts',(-2.97471211665326,24.9115581886552,15.2128811643004));
#60628=CARTESIAN_POINT('Ctrl Pts',(-3.48144100827184,25.211804507667,12.6778104888403));
#60629=CARTESIAN_POINT('Ctrl Pts',(-2.17274142682733,25.5004550944448,10.5709222508267));
#60630=CARTESIAN_POINT('Ctrl Pts',(0.0600344106941335,25.7771166135459,
9.85725397170378));
#60631=CARTESIAN_POINT('Ctrl Pts',(2.15934368744129,26.0415422132396,10.6413269741514));
#60632=CARTESIAN_POINT('Ctrl Pts',(3.22061067469158,26.2825345572412,12.3845222667272));
#60633=CARTESIAN_POINT('Ctrl Pts',(3.15347935583999,26.5002557872507,14.1840957311028));
#60634=CARTESIAN_POINT('Ctrl Pts',(2.33420364046461,26.6950126881386,15.5694145660939));
#60635=CARTESIAN_POINT('Ctrl Pts',(0.958566958400896,26.8884387445348,16.3854549505474));
#60636=CARTESIAN_POINT('Ctrl Pts',(-0.627537293809016,27.0804033115453,
16.4434136719425));
#60637=CARTESIAN_POINT('Ctrl Pts',(-2.03552350511545,27.2707817161207,15.7397540217649));
#60638=CARTESIAN_POINT('Ctrl Pts',(-2.92642873709077,27.4594521092887,14.4589186698802));
#60639=CARTESIAN_POINT('Ctrl Pts',(-3.06476918820841,27.6151620870074,13.1791852448839));
#60640=CARTESIAN_POINT('Ctrl Pts',(-2.80163706893976,27.7387642717718,12.2162436591921));
#60641=CARTESIAN_POINT('Ctrl Pts',(-2.31305221628185,27.8617107211686,11.3516558461287));
#60642=CARTESIAN_POINT('Ctrl Pts',(-1.33339394747703,28.0141249041079,10.5593435278253));
#60643=CARTESIAN_POINT('Ctrl Pts',(0.137466061428836,28.1949063678745,10.2916382306392));
#60644=CARTESIAN_POINT('Ctrl Pts',(1.42221496642251,28.3586060455309,10.7168492274562));
#60645=CARTESIAN_POINT('Ctrl Pts',(2.12004744313203,28.4763323007467,11.3762841986774));
#60646=CARTESIAN_POINT('Ctrl Pts',(2.62396197101089,28.5932856628549,12.168670878928));
#60647=CARTESIAN_POINT('Ctrl Pts',(2.89307483334103,28.7237599241023,13.2130931079621));
#60648=CARTESIAN_POINT('Ctrl Pts',(2.54652333624131,28.8953280039873,14.5887900128546));
#60649=CARTESIAN_POINT('Ctrl Pts',(1.59579795643967,29.0644499469633,15.6142705384307));
#60650=CARTESIAN_POINT('Ctrl Pts',(0.617102208219719,29.1894288450293,15.9444046726897));
#60651=CARTESIAN_POINT('Ctrl Pts',(-0.0456556529442235,29.2719631152849,
15.9535087705334));
#60652=CARTESIAN_POINT('Ctrl Pts',(-0.483011850539022,29.3267759193272,
15.9050013907027));
#60653=CARTESIAN_POINT('Ctrl Pts',(-1.2198054873934,29.4221461631643,15.6794201744828));
#60654=CARTESIAN_POINT('Ctrl Pts',(-2.09014382104258,29.5568075472996,14.9852905198769));
#60655=CARTESIAN_POINT('Ctrl Pts',(-2.59788149289038,29.7158584966411,13.7719095212622));
#60656=CARTESIAN_POINT('Ctrl Pts',(-2.46711739291308,29.8723680883128,12.4845544452712));
#60657=CARTESIAN_POINT('Ctrl Pts',(-1.74601398001167,30.0263461962339,11.4352049138197));
#60658=CARTESIAN_POINT('Ctrl Pts',(-0.629844515312964,30.1778111542655,
10.8670301468742));
#60659=CARTESIAN_POINT('Ctrl Pts',(0.601496364936027,30.3267943685925,10.9037055374241));
#60660=CARTESIAN_POINT('Ctrl Pts',(1.64825284718227,30.4733320948358,11.5144435828851));
#60661=CARTESIAN_POINT('Ctrl Pts',(2.2635440376844,30.6174743670642,12.5350177559086));
#60662=CARTESIAN_POINT('Ctrl Pts',(2.31580800504618,30.7592767886105,13.7065846562522));
#60663=CARTESIAN_POINT('Ctrl Pts',(1.807753632511,30.8988065252971,14.7424093963853));
#60664=CARTESIAN_POINT('Ctrl Pts',(0.881013187737084,31.0361391305485,15.3991007570354));
#60665=CARTESIAN_POINT('Ctrl Pts',(-0.229384030457491,31.1713551305116,
15.5289368437615));
#60666=CARTESIAN_POINT('Ctrl Pts',(-1.25180204175459,31.3045516305373,15.1187939179942));
#60667=CARTESIAN_POINT('Ctrl Pts',(-1.9415893920128,31.4358200365546,14.2806703731829));
#60668=CARTESIAN_POINT('Ctrl Pts',(-2.14468763692602,31.5652759046523,13.2295435090225));
#60669=CARTESIAN_POINT('Ctrl Pts',(-1.82320966062737,31.6930248645021,12.2230522342915));
#60670=CARTESIAN_POINT('Ctrl Pts',(-1.06864419389326,31.8191908990757,11.5022587818521));
#60671=CARTESIAN_POINT('Ctrl Pts',(-0.0727669233574973,31.9438975626322,
11.2346252743258));
#60672=CARTESIAN_POINT('Ctrl Pts',(0.919693554917522,32.0672810695473,11.4726566241412));
#60673=CARTESIAN_POINT('Ctrl Pts',(1.66887056249793,32.1894739538329,12.1506666424005));
#60674=CARTESIAN_POINT('Ctrl Pts',(2.00013058191407,32.3106196673884,13.0969596993241));
#60675=CARTESIAN_POINT('Ctrl Pts',(1.83781539368687,32.4308629546113,14.0774584579158));
#60676=CARTESIAN_POINT('Ctrl Pts',(1.1632926479292,32.5636275136061,14.9453606036313));
#60677=CARTESIAN_POINT('Ctrl Pts',(-0.00197077022069799,32.708812342,15.3383648007732));
#60678=CARTESIAN_POINT('Ctrl Pts',(-1.26239853292309,32.8664892999126,14.8907072077442));
#60679=CARTESIAN_POINT('Ctrl Pts',(-1.8258439893124,32.9910569449221,13.9989784067232));
#60680=CARTESIAN_POINT('Ctrl Pts',(-1.90256425845217,33.0828535369837,13.260933206721));
#60681=CARTESIAN_POINT('Ctrl Pts',(-1.81251203490417,33.1615760274655,12.63147976504));
#60682=CARTESIAN_POINT('Ctrl Pts',(-1.40892388448975,33.2600857890204,11.9236479231083));
#60683=CARTESIAN_POINT('Ctrl Pts',(-0.57432734621905,33.3786362635983,11.4089625889543));
#60684=CARTESIAN_POINT('Ctrl Pts',(0.408902180381898,33.4976766157179,11.3569408514114));
#60685=CARTESIAN_POINT('Ctrl Pts',(1.3016420224292,33.6173620208606,11.7849288978517));
#60686=CARTESIAN_POINT('Ctrl Pts',(1.88421901808678,33.7378433732163,12.5934241275751));
#60687=CARTESIAN_POINT('Ctrl Pts',(2.00841783454731,33.859267715344,13.590321732198));
#60688=CARTESIAN_POINT('Ctrl Pts',(1.67741798856941,33.9681678843717,14.4284141902102));
#60689=CARTESIAN_POINT('Ctrl Pts',(1.12015075491802,34.0642516399516,14.9752972742767));
#60690=CARTESIAN_POINT('Ctrl Pts',(0.30883305425423,34.1748415606842,15.3636707172977));
#60691=CARTESIAN_POINT('Ctrl Pts',(-0.63683898934766,34.2866861183453,15.3112234175934));
#60692=CARTESIAN_POINT('Ctrl Pts',(-1.41733709088844,34.3999293831788,14.8225486779453));
#60693=CARTESIAN_POINT('Ctrl Pts',(-2.04209650955594,34.5212951308744,14.0586970846731));
#60694=CARTESIAN_POINT('Ctrl Pts',(-2.23763665747699,34.6806558523311,12.7030451058781));
#60695=CARTESIAN_POINT('Ctrl Pts',(-1.2527133198986,34.8805161631469,11.2917435621959));
#60696=CARTESIAN_POINT('Ctrl Pts',(0.464977883462776,35.0849872890747,10.9202321885198));
#60697=CARTESIAN_POINT('Ctrl Pts',(2.0130473474812,35.2943670661089,11.8427459642946));
#60698=CARTESIAN_POINT('Ctrl Pts',(2.52660114584721,35.50890654089,13.6144619963185));
#60699=CARTESIAN_POINT('Ctrl Pts',(1.67665102832899,35.7288118669548,15.3040875688965));
#60700=CARTESIAN_POINT('Ctrl Pts',(-0.192116355100357,35.9600384371841,
15.9901518801674));
#60701=CARTESIAN_POINT('Ctrl Pts',(-1.45964153582199,36.120174190932,15.41955795021));
#60702=CARTESIAN_POINT('Ctrl Pts',(-1.91091130723325,36.2043175118729,14.9174925473367));
#60703=CARTESIAN_POINT('Ctrl Pts',(-1.00595942234827,23.4703156359905,10.5694791067139));
#60704=CARTESIAN_POINT('Ctrl Pts',(-0.315877847047438,23.5621480601222,
10.3142801806992));
#60705=CARTESIAN_POINT('Ctrl Pts',(1.25363167841598,23.7446337943067,10.3564313620877));
#60706=CARTESIAN_POINT('Ctrl Pts',(2.92084555199283,24.0175788900516,12.0084073813003));
#60707=CARTESIAN_POINT('Ctrl Pts',(3.01267803575596,24.2888665683142,14.3388519167426));
#60708=CARTESIAN_POINT('Ctrl Pts',(1.49612998604492,24.5594335621326,16.1026512075001));
#60709=CARTESIAN_POINT('Ctrl Pts',(-0.808179728832318,24.8290174145929,
16.3582951621009));
#60710=CARTESIAN_POINT('Ctrl Pts',(-2.65944370200479,25.0973445240907,14.9829489444263));
#60711=CARTESIAN_POINT('Ctrl Pts',(-3.07651190721737,25.3641623643543,12.724296780867));
#60712=CARTESIAN_POINT('Ctrl Pts',(-1.8928067719465,25.6194082319424,10.8786418964801));
#60713=CARTESIAN_POINT('Ctrl Pts',(0.0822095539269653,25.8631059996756,
10.2780969229765));
#60714=CARTESIAN_POINT('Ctrl Pts',(1.91564198504364,26.0953415910853,10.992459371924));
#60715=CARTESIAN_POINT('Ctrl Pts',(2.8239435354046,26.3065275168311,12.5326018159647));
#60716=CARTESIAN_POINT('Ctrl Pts',(2.7433255831973,26.4970749742018,14.1062282815387));
#60717=CARTESIAN_POINT('Ctrl Pts',(2.01014712384195,26.6674096336721,15.3074755501791));
#60718=CARTESIAN_POINT('Ctrl Pts',(0.797707037023478,26.8365425712707,16.0040071039835));
#60719=CARTESIAN_POINT('Ctrl Pts',(-0.589761995396185,27.004435551555,16.0352476373376));
#60720=CARTESIAN_POINT('Ctrl Pts',(-1.81296648289921,27.1710551901992,15.4022578695728));
#60721=CARTESIAN_POINT('Ctrl Pts',(-2.57745246520028,27.336372182225,14.2692880697337));
#60722=CARTESIAN_POINT('Ctrl Pts',(-2.68282409359319,27.473031356267,13.1447629858075));
#60723=CARTESIAN_POINT('Ctrl Pts',(-2.43928761960126,27.5816857231595,12.3019245827255));
#60724=CARTESIAN_POINT('Ctrl Pts',(-1.9983164528988,27.6898899233007,11.5475832051832));
#60725=CARTESIAN_POINT('Ctrl Pts',(-1.12459065098004,27.8242955054052,10.8616462820568));
#60726=CARTESIAN_POINT('Ctrl Pts',(0.17954106387617,27.9842153349351,10.6439457189669));
#60727=CARTESIAN_POINT('Ctrl Pts',(1.31419007004281,28.129552146691,11.0381880889183));
#60728=CARTESIAN_POINT('Ctrl Pts',(1.92687082167423,28.2344536276736,11.6350157508958));
#60729=CARTESIAN_POINT('Ctrl Pts',(2.3656901722259,28.3389005281905,12.3493840235856));
#60730=CARTESIAN_POINT('Ctrl Pts',(2.59246433293698,28.455765405854,13.2881757380847));
#60731=CARTESIAN_POINT('Ctrl Pts',(2.26154052562728,28.6102370497776,14.5214959902665));
#60732=CARTESIAN_POINT('Ctrl Pts',(1.38650323158265,28.7633774443539,15.436319994476));
#60733=CARTESIAN_POINT('Ctrl Pts',(0.490367493818371,28.8772522456174,15.7228478889474));
#60734=CARTESIAN_POINT('Ctrl Pts',(-0.115902755902976,28.9527679590394,
15.720994514257));
#60735=CARTESIAN_POINT('Ctrl Pts',(-0.515823678956967,29.0030064433406,
15.6697851525537));
#60736=CARTESIAN_POINT('Ctrl Pts',(-1.18906392073067,29.0906466047621,15.4512023590902));
#60737=CARTESIAN_POINT('Ctrl Pts',(-1.98232267801215,29.2150670210491,14.7969700130926));
#60738=CARTESIAN_POINT('Ctrl Pts',(-2.43605903789984,29.3631627820738,13.6597517681805));
#60739=CARTESIAN_POINT('Ctrl Pts',(-2.29279814786244,29.5100883241477,12.4539148456178));
#60740=CARTESIAN_POINT('Ctrl Pts',(-1.5930426178182,29.6558949765442,11.4725425950399));
#60741=CARTESIAN_POINT('Ctrl Pts',(-0.517432252664176,29.8006287421963,
10.94878973249));
#60742=CARTESIAN_POINT('Ctrl Pts',(0.669193813981328,29.9443493199384,11.0056188986052));
#60743=CARTESIAN_POINT('Ctrl Pts',(1.67744591647376,30.0871116323955,11.6191187333393));
#60744=CARTESIAN_POINT('Ctrl Pts',(2.26375300252859,30.2289807478686,12.6345032307524));
#60745=CARTESIAN_POINT('Ctrl Pts',(2.293238531032,30.370021008209,13.8000545156108));
#60746=CARTESIAN_POINT('Ctrl Pts',(1.76220071904141,30.510302264146,14.8307970020976));
#60747=CARTESIAN_POINT('Ctrl Pts',(0.80734479632738,30.6498973070903,15.4789104494946));
#60748=CARTESIAN_POINT('Ctrl Pts',(-0.336016774735876,30.7888783301199,
15.5887400642292));
#60749=CARTESIAN_POINT('Ctrl Pts',(-1.3890059475663,30.9273270494787,15.1403607710382));
#60750=CARTESIAN_POINT('Ctrl Pts',(-2.09465588475557,31.065316325783,14.2442944012222));
#60751=CARTESIAN_POINT('Ctrl Pts',(-2.28581823124681,31.202933769985,13.1230263682163));
#60752=CARTESIAN_POINT('Ctrl Pts',(-1.91623167317492,31.3402558750362,12.0496946881804));
#60753=CARTESIAN_POINT('Ctrl Pts',(-1.07890358209417,31.4773688229052,11.2857618737474));
#60754=CARTESIAN_POINT('Ctrl Pts',(0.0210509156088651,31.6143552012013,
11.0175686839098));
#60755=CARTESIAN_POINT('Ctrl Pts',(1.11536038725298,31.7513022871471,11.3077307424644));
#60756=CARTESIAN_POINT('Ctrl Pts',(1.93612871033968,31.8882925319881,12.0875194085925));
#60757=CARTESIAN_POINT('Ctrl Pts',(2.28442129393533,32.0254116397918,13.1668223690244));
#60758=CARTESIAN_POINT('Ctrl Pts',(2.07119455170064,32.1627436409057,14.2810268476482));
#60759=CARTESIAN_POINT('Ctrl Pts',(1.26984743031617,32.3156626735956,15.2600648520212));
#60760=CARTESIAN_POINT('Ctrl Pts',(-0.0947238237671589,32.4844144762023,
15.6826089699051));
#60761=CARTESIAN_POINT('Ctrl Pts',(-1.55853578518989,32.6693698596506,15.1204857695937));
#60762=CARTESIAN_POINT('Ctrl Pts',(-2.19675809292368,32.816625001231,14.0501554524693));
#60763=CARTESIAN_POINT('Ctrl Pts',(-2.26420720501918,32.9256178774175,13.1722540887062));
#60764=CARTESIAN_POINT('Ctrl Pts',(-2.13704607973914,33.0192849787917,12.4269900391733));
#60765=CARTESIAN_POINT('Ctrl Pts',(-1.63346515637257,33.1368424073631,11.5959647067977));
#60766=CARTESIAN_POINT('Ctrl Pts',(-0.619082947445776,33.2787432000681,
11.0071612785401));
#60767=CARTESIAN_POINT('Ctrl Pts',(0.560814397369453,33.4215398351124,10.9762790753619));
#60768=CARTESIAN_POINT('Ctrl Pts',(1.61829684472986,33.5652955286783,11.5183922685832));
#60769=CARTESIAN_POINT('Ctrl Pts',(2.29179274561511,33.7100689358281,12.5075111711697));
#60770=CARTESIAN_POINT('Ctrl Pts',(2.40911494050403,33.8559145947988,13.7076478489104));
#60771=CARTESIAN_POINT('Ctrl Pts',(1.98595485145375,33.9865536897804,14.7015680988501));
#60772=CARTESIAN_POINT('Ctrl Pts',(1.30221394563286,34.1016210722776,15.3384786563256));
#60773=CARTESIAN_POINT('Ctrl Pts',(0.321129855928317,34.2338358770118,15.7772973775983));
#60774=CARTESIAN_POINT('Ctrl Pts',(-0.803167037301693,34.3671404111073,
15.6853838858228));
#60775=CARTESIAN_POINT('Ctrl Pts',(-1.71413544543102,34.5015739164706,15.0824384631522));
#60776=CARTESIAN_POINT('Ctrl Pts',(-2.43039140986002,34.6452224333733,14.1605266697859));
#60777=CARTESIAN_POINT('Ctrl Pts',(-2.61917840501806,34.8328540037758,12.5599786999848));
#60778=CARTESIAN_POINT('Ctrl Pts',(-1.42858408684654,35.0661480293711,10.9435773618336));
#60779=CARTESIAN_POINT('Ctrl Pts',(0.565898564707986,35.3025057604142,10.5642067088703));
#60780=CARTESIAN_POINT('Ctrl Pts',(2.30872173182878,35.5419477791935,11.6617907113252));
#60781=CARTESIAN_POINT('Ctrl Pts',(2.840613788849,35.784466262583,13.6767542672384));
#60782=CARTESIAN_POINT('Ctrl Pts',(1.8478141234025,36.0300290070386,15.5397950856984));
#60783=CARTESIAN_POINT('Ctrl Pts',(-0.228189814937037,36.2849569348317,
16.2481689080808));
#60784=CARTESIAN_POINT('Ctrl Pts',(-1.5918854708806,36.4591229948481,15.5967610939565));
#60785=CARTESIAN_POINT('Ctrl Pts',(-2.0681370687829,36.5499727686619,15.0455429908956));
#60786=CARTESIAN_POINT('Ctrl Pts',(-0.932330810424575,23.8148696685421,
10.7604374361683));
#60787=CARTESIAN_POINT('Ctrl Pts',(-0.286215034785667,23.9003328788305,
10.5337172487311));
#60788=CARTESIAN_POINT('Ctrl Pts',(1.16482349350439,24.0691655682275,10.6001501647687));
#60789=CARTESIAN_POINT('Ctrl Pts',(2.66151761715804,24.3189116652514,12.1403309667867));
#60790=CARTESIAN_POINT('Ctrl Pts',(2.70474981215371,24.5645516958709,14.2516225163327));
#60791=CARTESIAN_POINT('Ctrl Pts',(1.31534249263431,24.8071517241187,15.8071395595109));
#60792=CARTESIAN_POINT('Ctrl Pts',(-0.735982946711268,25.0466816240843,
15.9955404266939));
#60793=CARTESIAN_POINT('Ctrl Pts',(-2.3441752873563,25.2831308595262,14.7530167245522));
#60794=CARTESIAN_POINT('Ctrl Pts',(-2.67158280616291,25.5165202210414,12.7707830728936));
#60795=CARTESIAN_POINT('Ctrl Pts',(-1.61287211706566,25.7383613694401,11.1863615421335));
#60796=CARTESIAN_POINT('Ctrl Pts',(0.1043846971598,25.9490953858052,10.6989398742492));
#60797=CARTESIAN_POINT('Ctrl Pts',(1.67194028264597,26.1491409689308,11.3435917696966));
#60798=CARTESIAN_POINT('Ctrl Pts',(2.42727639611763,26.3305204764211,12.6806813652021));
#60799=CARTESIAN_POINT('Ctrl Pts',(2.33317181055461,26.493894161153,14.0283608319746));
#60800=CARTESIAN_POINT('Ctrl Pts',(1.6860906072193,26.6398065792055,15.0455365342643));
#60801=CARTESIAN_POINT('Ctrl Pts',(0.636847115646059,26.7846463980065,15.6225592574197));
#60802=CARTESIAN_POINT('Ctrl Pts',(-0.551986696983355,26.9284677915647,
15.6270816027327));
#60803=CARTESIAN_POINT('Ctrl Pts',(-1.59040946068298,27.0713286642777,15.0647617173808));
#60804=CARTESIAN_POINT('Ctrl Pts',(-2.22847619330979,27.2132922551612,14.0796574695873));
#60805=CARTESIAN_POINT('Ctrl Pts',(-2.30087899897796,27.3309006255265,13.1103407267311));
#60806=CARTESIAN_POINT('Ctrl Pts',(-2.07693817026276,27.4246071745472,12.3876055062589));
#60807=CARTESIAN_POINT('Ctrl Pts',(-1.68358068951573,27.5180691254328,11.7435105642378));
#60808=CARTESIAN_POINT('Ctrl Pts',(-0.915787354483041,27.6344661067026,
11.1639490362885));
#60809=CARTESIAN_POINT('Ctrl Pts',(0.221616066323505,27.7735243019958,10.9962532072946));
#60810=CARTESIAN_POINT('Ctrl Pts',(1.2061651736631,27.9004982478512,11.3595269503803));
#60811=CARTESIAN_POINT('Ctrl Pts',(1.73369420021643,27.9925749546004,11.8937473031143));
#60812=CARTESIAN_POINT('Ctrl Pts',(2.10741837344092,28.0845153935261,12.5300971682432));
#60813=CARTESIAN_POINT('Ctrl Pts',(2.29185383253292,28.1877708876058,13.3632583682073));
#60814=CARTESIAN_POINT('Ctrl Pts',(1.97655771501325,28.3251460955679,14.4542019676785));
#60815=CARTESIAN_POINT('Ctrl Pts',(1.17720850672562,28.4623049417444,15.2583694505214));
#60816=CARTESIAN_POINT('Ctrl Pts',(0.363632779417019,28.5650756462056,15.501291105205));
#60817=CARTESIAN_POINT('Ctrl Pts',(-0.186149858861731,28.633572802794,15.4884802579808));
#60818=CARTESIAN_POINT('Ctrl Pts',(-0.548635507374914,28.679236967354,15.4345689144049));
#60819=CARTESIAN_POINT('Ctrl Pts',(-1.15832235406793,28.7591470463601,15.2229845436976));
#60820=CARTESIAN_POINT('Ctrl Pts',(-1.8745015349817,28.8733264947987,14.6086495063083));
#60821=CARTESIAN_POINT('Ctrl Pts',(-2.27423658290929,29.0104670675064,13.547594015099));
#60822=CARTESIAN_POINT('Ctrl Pts',(-2.11847890281181,29.1478085599825,12.4232752459646));
#60823=CARTESIAN_POINT('Ctrl Pts',(-1.44007125562472,29.2854437568545,11.50988027626));
#60824=CARTESIAN_POINT('Ctrl Pts',(-0.405019990015385,29.4234463301271,
11.0305493181059));
#60825=CARTESIAN_POINT('Ctrl Pts',(0.736891263026629,29.5619042712843,11.1075322597862));
#60826=CARTESIAN_POINT('Ctrl Pts',(1.70663898576526,29.7008911699554,11.7237938837935));
#60827=CARTESIAN_POINT('Ctrl Pts',(2.26396196737277,29.8404871286729,12.7339887055961));
#60828=CARTESIAN_POINT('Ctrl Pts',(2.27066905701781,29.9807652278076,13.8935243749694));
#60829=CARTESIAN_POINT('Ctrl Pts',(1.71664780557182,30.1217980029948,14.9191846078098));
#60830=CARTESIAN_POINT('Ctrl Pts',(0.733676404917682,30.2636554836321,15.5587201419538));
#60831=CARTESIAN_POINT('Ctrl Pts',(-0.442649519014257,30.4064015297281,
15.6485432846969));
#60832=CARTESIAN_POINT('Ctrl Pts',(-1.52620985337802,30.5501024684201,15.161927624082));
#60833=CARTESIAN_POINT('Ctrl Pts',(-2.24772237749834,30.6948126150113,14.2079184292616));
#60834=CARTESIAN_POINT('Ctrl Pts',(-2.42694882556761,30.8405916353176,13.0165092274103));
#60835=CARTESIAN_POINT('Ctrl Pts',(-2.00925368572246,30.9874868855705,11.8763371420694));
#60836=CARTESIAN_POINT('Ctrl Pts',(-1.08916297029509,31.1355467467346,11.0692649656428));
#60837=CARTESIAN_POINT('Ctrl Pts',(0.114868754575229,31.2848128397704,10.800512093494));
#60838=CARTESIAN_POINT('Ctrl Pts',(1.31102721958845,31.435323504747,11.1428048607877));
#60839=CARTESIAN_POINT('Ctrl Pts',(2.20338685818143,31.5871111101434,12.0243721747846));
#60840=CARTESIAN_POINT('Ctrl Pts',(2.56871200595661,31.7402036121951,13.2366850387248));
#60841=CARTESIAN_POINT('Ctrl Pts',(2.30457370971442,31.8946243272,14.4845952373805));
#60842=CARTESIAN_POINT('Ctrl Pts',(1.37640221270315,32.0676978335851,15.5747691004112));
#60843=CARTESIAN_POINT('Ctrl Pts',(-0.187476877313618,32.2600166104046,
16.0268531390372));
#60844=CARTESIAN_POINT('Ctrl Pts',(-1.85467303745672,32.4722504193886,15.3502643314434));
#60845=CARTESIAN_POINT('Ctrl Pts',(-2.56767219653497,32.6421930575399,14.1013324982155));
#60846=CARTESIAN_POINT('Ctrl Pts',(-2.6258501515862,32.7683822178512,13.0835749706912));
#60847=CARTESIAN_POINT('Ctrl Pts',(-2.46158012457412,32.8769939301179,12.2225003133065));
#60848=CARTESIAN_POINT('Ctrl Pts',(-1.85800642825539,33.0135990257057,11.2682814904871));
#60849=CARTESIAN_POINT('Ctrl Pts',(-0.663838548672504,33.178850136538,10.6053599681259));
#60850=CARTESIAN_POINT('Ctrl Pts',(0.712726614357012,33.3454030545069,10.5956172993124));
#60851=CARTESIAN_POINT('Ctrl Pts',(1.93495166703052,33.5132290364961,11.2518556393147));
#60852=CARTESIAN_POINT('Ctrl Pts',(2.69936647314346,33.6822944984401,12.4215982147645));
#60853=CARTESIAN_POINT('Ctrl Pts',(2.80981204646077,33.8525614742537,13.8249739656226));
#60854=CARTESIAN_POINT('Ctrl Pts',(2.2944917143381,34.004939495189,14.97472200749));
#60855=CARTESIAN_POINT('Ctrl Pts',(1.48427713634769,34.1389905046036,15.7016600383746));
#60856=CARTESIAN_POINT('Ctrl Pts',(0.333426657602405,34.2928301933393,16.1909240378989));
#60857=CARTESIAN_POINT('Ctrl Pts',(-0.969495085255728,34.4475947038694,
16.0595443540521));
#60858=CARTESIAN_POINT('Ctrl Pts',(-2.0109337999736,34.6032184497623,15.3423282483589));
#60859=CARTESIAN_POINT('Ctrl Pts',(-2.81868631016408,34.7691497358721,14.2623562548988));
#60860=CARTESIAN_POINT('Ctrl Pts',(-3.00072015255915,34.9850521552204,12.4169122940916));
#60861=CARTESIAN_POINT('Ctrl Pts',(-1.60445485379447,35.2517798955955,10.5954111614711));
#60862=CARTESIAN_POINT('Ctrl Pts',(0.666819245953194,35.5200242317538,10.2081812292208));
#60863=CARTESIAN_POINT('Ctrl Pts',(2.60439611617634,35.7895284922781,11.4808354583559));
#60864=CARTESIAN_POINT('Ctrl Pts',(3.1546264318508,36.0600259842761,13.7390465381583));
#60865=CARTESIAN_POINT('Ctrl Pts',(2.01897721847602,36.3312461471225,15.7755026025001));
#60866=CARTESIAN_POINT('Ctrl Pts',(-0.264263274773716,36.6098754324793,
16.5061859359941));
#60867=CARTESIAN_POINT('Ctrl Pts',(-1.7241294059392,36.7980717987643,15.7739642377031));
#60868=CARTESIAN_POINT('Ctrl Pts',(-2.22536283033256,36.895628025451,15.1735934344545));
#60869=CARTESIAN_POINT('Ctrl Pts',(-0.858702198500876,24.1594237010936,
10.9513957656227));
#60870=CARTESIAN_POINT('Ctrl Pts',(-0.256552222523894,24.2385176975388,
10.7531543167631));
#60871=CARTESIAN_POINT('Ctrl Pts',(1.07601530859282,24.3936973421483,10.8438689674496));
#60872=CARTESIAN_POINT('Ctrl Pts',(2.40218968232325,24.620244440451,12.2722545522732));
#60873=CARTESIAN_POINT('Ctrl Pts',(2.39682158855147,24.8402368234276,14.1643931159229));
#60874=CARTESIAN_POINT('Ctrl Pts',(1.13455499922372,25.0548698861049,15.5116279115216));
#60875=CARTESIAN_POINT('Ctrl Pts',(-0.66378616459021,25.2643458335756,15.632785691287));
#60876=CARTESIAN_POINT('Ctrl Pts',(-2.02890687270782,25.4689171949617,14.5230845046781));
#60877=CARTESIAN_POINT('Ctrl Pts',(-2.26665370510843,25.6688780777285,12.8172693649202));
#60878=CARTESIAN_POINT('Ctrl Pts',(-1.33293746218483,25.8573145069377,11.4940811877868));
#60879=CARTESIAN_POINT('Ctrl Pts',(0.126559840392635,26.0350847719349,11.1197828255219));
#60880=CARTESIAN_POINT('Ctrl Pts',(1.42823858024832,26.2029403467764,11.6947241674692));
#60881=CARTESIAN_POINT('Ctrl Pts',(2.03060925683066,26.3545134360111,12.8287609144396));
#60882=CARTESIAN_POINT('Ctrl Pts',(1.92301803791192,26.490713348104,13.9504933824104));
#60883=CARTESIAN_POINT('Ctrl Pts',(1.36203409059664,26.612203524739,14.7835975183494));
#60884=CARTESIAN_POINT('Ctrl Pts',(0.475987194268644,26.7327502247424,15.2411114108558));
#60885=CARTESIAN_POINT('Ctrl Pts',(-0.514211398570525,26.8525000315743,
15.2189155681279));
#60886=CARTESIAN_POINT('Ctrl Pts',(-1.36785243846674,26.9716021383562,14.7272655651888));
#60887=CARTESIAN_POINT('Ctrl Pts',(-1.87949992141931,27.0902123280975,13.8900268694409));
#60888=CARTESIAN_POINT('Ctrl Pts',(-1.91893390436274,27.1887698947861,13.0759184676546));
#60889=CARTESIAN_POINT('Ctrl Pts',(-1.71458872092426,27.267528625935,12.4732864297923));
#60890=CARTESIAN_POINT('Ctrl Pts',(-1.36884492613267,27.3462483275648,11.9394379232924));
#60891=CARTESIAN_POINT('Ctrl Pts',(-0.70698405798605,27.4446367079999,11.4662517905201));
#60892=CARTESIAN_POINT('Ctrl Pts',(0.26369106877084,27.5628332690564,11.3485606956223));
#60893=CARTESIAN_POINT('Ctrl Pts',(1.0981402772834,27.6714443490113,11.6808658118425));
#60894=CARTESIAN_POINT('Ctrl Pts',(1.54051757875863,27.7506962815273,12.1524788553328));
#60895=CARTESIAN_POINT('Ctrl Pts',(1.84914657465594,27.8301302588617,12.7108103129009));
#60896=CARTESIAN_POINT('Ctrl Pts',(1.99124333212888,27.9197763693575,13.4383409983297));
#60897=CARTESIAN_POINT('Ctrl Pts',(1.69157490439921,28.0400551413582,14.3869079450905));
#60898=CARTESIAN_POINT('Ctrl Pts',(0.967913781868604,28.161232439135,15.0804189065668));
#60899=CARTESIAN_POINT('Ctrl Pts',(0.236898065015672,28.2528990467938,15.2797343214628));
#60900=CARTESIAN_POINT('Ctrl Pts',(-0.256396961820482,28.3143776465486,
15.2559660017045));
#60901=CARTESIAN_POINT('Ctrl Pts',(-0.581447335792858,28.3554674913674,
15.199352676256));
#60902=CARTESIAN_POINT('Ctrl Pts',(-1.12758078740518,28.427647487958,14.9947667283049));
#60903=CARTESIAN_POINT('Ctrl Pts',(-1.76668039195127,28.5315859685482,14.4203289995239));
#60904=CARTESIAN_POINT('Ctrl Pts',(-2.11241412791876,28.6577713529391,13.4354362620173));
#60905=CARTESIAN_POINT('Ctrl Pts',(-1.94415965776118,28.7855287958173,12.3926356463114));
#60906=CARTESIAN_POINT('Ctrl Pts',(-1.28709989343125,28.9149925371647,11.5472179574802));
#60907=CARTESIAN_POINT('Ctrl Pts',(-0.292607727366596,29.0462639180579,
11.1123089037218));
#60908=CARTESIAN_POINT('Ctrl Pts',(0.804588712071932,29.1794592226303,11.2094456209673));
#60909=CARTESIAN_POINT('Ctrl Pts',(1.73583205505676,29.3146707075153,11.8284690342478));
#60910=CARTESIAN_POINT('Ctrl Pts',(2.26417093221696,29.4519935094771,12.8334741804398));
#60911=CARTESIAN_POINT('Ctrl Pts',(2.24809958300362,29.5915094474061,13.986994234328));
#60912=CARTESIAN_POINT('Ctrl Pts',(1.67109489210224,29.7332937418437,15.0075722135221));
#60913=CARTESIAN_POINT('Ctrl Pts',(0.66000801350798,29.8774136601739,15.638529834413));
#60914=CARTESIAN_POINT('Ctrl Pts',(-0.549282263292639,30.0239247293364,
15.7083465051647));
#60915=CARTESIAN_POINT('Ctrl Pts',(-1.66341375918974,30.1728778873614,15.183494477126));
#60916=CARTESIAN_POINT('Ctrl Pts',(-2.40078887024112,30.3243089042397,14.171542457301));
#60917=CARTESIAN_POINT('Ctrl Pts',(-2.5680794198884,30.4782495006503,12.9099920866041));
#60918=CARTESIAN_POINT('Ctrl Pts',(-2.10227569826999,30.6347178961047,11.7029795959583));
#60919=CARTESIAN_POINT('Ctrl Pts',(-1.099422358496,30.7937246705641,10.8527680575381));
#60920=CARTESIAN_POINT('Ctrl Pts',(0.208686593541593,30.9552704783395,10.583455503078));
#60921=CARTESIAN_POINT('Ctrl Pts',(1.50669405192392,31.1193447223469,10.9778789791109));
#60922=CARTESIAN_POINT('Ctrl Pts',(2.47064500602316,31.2859296882988,11.9612249409767));
#60923=CARTESIAN_POINT('Ctrl Pts',(2.85300271797787,31.4549955845984,13.3065477084251));
#60924=CARTESIAN_POINT('Ctrl Pts',(2.53795286772821,31.6265050134944,14.6881636271129));
#60925=CARTESIAN_POINT('Ctrl Pts',(1.48295699509012,31.8197329935747,15.8894733488012));
#60926=CARTESIAN_POINT('Ctrl Pts',(-0.280229930860079,32.035618744607,16.3710973081691));
#60927=CARTESIAN_POINT('Ctrl Pts',(-2.15081028972353,32.2751309791266,15.580042893293));
#60928=CARTESIAN_POINT('Ctrl Pts',(-2.93858630014624,32.4677611138487,14.1525095439616));
#60929=CARTESIAN_POINT('Ctrl Pts',(-2.98749309815322,32.6111465582849,12.9948958526763));
#60930=CARTESIAN_POINT('Ctrl Pts',(-2.7861141694091,32.734702881444,12.0180105874398));
#60931=CARTESIAN_POINT('Ctrl Pts',(-2.0825477001382,32.8903556440484,10.9405982741765));
#60932=CARTESIAN_POINT('Ctrl Pts',(-0.70859414989923,33.0789570730078,10.2035586577117));
#60933=CARTESIAN_POINT('Ctrl Pts',(0.864638831344568,33.2692662739014,10.2149555232629));
#60934=CARTESIAN_POINT('Ctrl Pts',(2.25160648933118,33.4611625443139,10.9853190100463));
#60935=CARTESIAN_POINT('Ctrl Pts',(3.10694020067178,33.654520061052,12.3356852583592));
#60936=CARTESIAN_POINT('Ctrl Pts',(3.21050915241751,33.8492083537085,13.942300082335));
#60937=CARTESIAN_POINT('Ctrl Pts',(2.60302857722243,34.0233253005977,15.2478759161299));
#60938=CARTESIAN_POINT('Ctrl Pts',(1.66634032706253,34.1763599369296,16.0648414204235));
#60939=CARTESIAN_POINT('Ctrl Pts',(0.345723459276493,34.351824509667,16.6045506981994));
#60940=CARTESIAN_POINT('Ctrl Pts',(-1.13582313320976,34.5280489966315,16.4337048222816));
#60941=CARTESIAN_POINT('Ctrl Pts',(-2.30773215451618,34.7048629830541,15.6022180335656));
#60942=CARTESIAN_POINT('Ctrl Pts',(-3.20698121046816,34.893077038371,14.3641858400115));
#60943=CARTESIAN_POINT('Ctrl Pts',(-3.38226190010022,35.137250306665,12.2738458881984));
#60944=CARTESIAN_POINT('Ctrl Pts',(-1.78032562074241,35.4374117618199,10.2472449611088));
#60945=CARTESIAN_POINT('Ctrl Pts',(0.767739927198404,35.7375427030933,9.85215574957131));
#60946=CARTESIAN_POINT('Ctrl Pts',(2.90007050052391,36.0371092053627,11.2998802053865));
#60947=CARTESIAN_POINT('Ctrl Pts',(3.46863907485259,36.3355857059691,13.8013388090782));
#60948=CARTESIAN_POINT('Ctrl Pts',(2.19014031354954,36.6324632872062,16.011210119302));
#60949=CARTESIAN_POINT('Ctrl Pts',(-0.300336734610397,36.934793930127,16.7642029639074));
#60950=CARTESIAN_POINT('Ctrl Pts',(-1.85637334099781,37.1370206026804,15.9511673814496));
#60951=CARTESIAN_POINT('Ctrl Pts',(-2.38258859188221,37.2412832822401,15.3016438780132));
#60952=CARTESIAN_POINT('Ctrl Pts',(-0.790532179204624,24.1655288633479,
10.9282793432527));
#60953=CARTESIAN_POINT('Ctrl Pts',(-0.705496619700135,24.1767170952653,
10.9031561171223));
#60954=CARTESIAN_POINT('Ctrl Pts',(-0.619144472715279,24.1877826920262,
10.8826943635782));
#60955=CARTESIAN_POINT('Ctrl Pts',(-0.532069686028644,24.1987800959838,
10.8669106881475));
#60956=CARTESIAN_POINT('Ctrl Pts',(-0.483596225465598,24.2049022152254,
10.858124110567));
#60957=CARTESIAN_POINT('Ctrl Pts',(-0.434899379414604,24.2110031686845,
10.8507864916071));
#60958=CARTESIAN_POINT('Ctrl Pts',(-0.386085050814084,24.2170920918391,
10.8448946532159));
#60959=CARTESIAN_POINT('Ctrl Pts',(-0.27235985485341,24.231277762293,10.8311681410461));
#60960=CARTESIAN_POINT('Ctrl Pts',(-0.157995879763926,24.245402739549,10.8252904681307));
#60961=CARTESIAN_POINT('Ctrl Pts',(-0.044133356191355,24.2596412506791,
10.8271840731439));
#60962=CARTESIAN_POINT('Ctrl Pts',(-0.00672289068076599,24.2643194302315,
10.8278062325938));
#60963=CARTESIAN_POINT('Ctrl Pts',(0.0306330371977953,24.2690098023138,
10.8292672357684));
#60964=CARTESIAN_POINT('Ctrl Pts',(0.0678928039773157,24.2737183571399,
10.8315639981628));
#60965=CARTESIAN_POINT('Ctrl Pts',(0.166869893362189,24.2862261931297,10.8376651328842));
#60966=CARTESIAN_POINT('Ctrl Pts',(0.26520479343476,24.2988712150022,10.8496654424747));
#60967=CARTESIAN_POINT('Ctrl Pts',(0.362271568845702,24.3115482937811,10.867392080451));
#60968=CARTESIAN_POINT('Ctrl Pts',(0.410662303838928,24.3178682024943,10.8762293477549));
#60969=CARTESIAN_POINT('Ctrl Pts',(0.458738358994614,24.3241961434368,10.8864904394408));
#60970=CARTESIAN_POINT('Ctrl Pts',(0.506424551980968,24.3305194888752,10.8981581464292));
#60971=CARTESIAN_POINT('Ctrl Pts',(0.603301083544006,24.3433656343858,10.9218615899954));
#60972=CARTESIAN_POINT('Ctrl Pts',(0.698567758984909,24.3561892987608,10.951371162955));
#60973=CARTESIAN_POINT('Ctrl Pts',(0.7914604069988,24.368854727582,10.9864979260627));
#60974=CARTESIAN_POINT('Ctrl Pts',(0.83358748498768,24.3745985352904,11.0024280122491));
#60975=CARTESIAN_POINT('Ctrl Pts',(0.875226967343351,24.3803098774156,11.0195131178887));
#60976=CARTESIAN_POINT('Ctrl Pts',(0.916311035982236,24.3859764877482,11.0377348653186));
#60977=CARTESIAN_POINT('Ctrl Pts',(0.93496960169188,24.3885500113729,11.0460103765576));
#60978=CARTESIAN_POINT('Ctrl Pts',(0.953512771719649,24.3911142427904,11.0545199877682));
#60979=CARTESIAN_POINT('Ctrl Pts',(0.971933515321555,24.3936680138793,11.0632615340076));
#60980=CARTESIAN_POINT('Ctrl Pts',(0.971942242388927,24.3936692237617,11.063265675429));
#60981=CARTESIAN_POINT('Ctrl Pts',(0.971950969430421,24.3936704336419,11.0632698169033));
#60982=CARTESIAN_POINT('Ctrl Pts',(0.971959696446036,24.39367164352,11.0632739584305));
#60983=CARTESIAN_POINT('Ctrl Pts',(1.04914245071372,24.4043719481958,11.0999021122559));
#60984=CARTESIAN_POINT('Ctrl Pts',(1.12430172397661,24.4149077656456,11.1406668535456));
#60985=CARTESIAN_POINT('Ctrl Pts',(1.1970061235826,24.4253721436316,11.1852297915425));
#60986=CARTESIAN_POINT('Ctrl Pts',(1.22895635016355,24.4299707545753,11.2048131451474));
#60987=CARTESIAN_POINT('Ctrl Pts',(1.26043238448574,24.4345555211935,11.2251293302296));
#60988=CARTESIAN_POINT('Ctrl Pts',(1.29139731547581,24.4391341100558,11.2461464799215));
#60989=CARTESIAN_POINT('Ctrl Pts',(1.37098541213915,24.4509022994658,11.3001661366033));
#60990=CARTESIAN_POINT('Ctrl Pts',(1.44720127556825,24.4626330806121,11.3588201391346));
#60991=CARTESIAN_POINT('Ctrl Pts',(1.51953449180492,24.4744791334325,11.4216421310785));
#60992=CARTESIAN_POINT('Ctrl Pts',(1.53478362557048,24.4769764929231,11.4348861289043));
#60993=CARTESIAN_POINT('Ctrl Pts',(1.54986003924515,24.4794789505739,11.4483152792074));
#60994=CARTESIAN_POINT('Ctrl Pts',(1.56475870316925,24.4819878965692,11.4619250513116));
#60995=CARTESIAN_POINT('Ctrl Pts',(1.63920471899428,24.4945246605517,11.5299307003153));
#60996=CARTESIAN_POINT('Ctrl Pts',(1.70923359743602,24.507228457478,11.6024629594918));
#60997=CARTESIAN_POINT('Ctrl Pts',(1.77443543912681,24.520000136623,11.6788891281613));
#60998=CARTESIAN_POINT('Ctrl Pts',(1.78842496438163,24.5227403924703,11.6952869136993));
#60999=CARTESIAN_POINT('Ctrl Pts',(1.8021922749423,24.5254837910698,11.7118641446668));
#61000=CARTESIAN_POINT('Ctrl Pts',(1.8157332990014,24.5282293825457,11.7286148816749));
#61001=CARTESIAN_POINT('Ctrl Pts',(1.86939917563113,24.5391107289475,11.795001514016));
#61002=CARTESIAN_POINT('Ctrl Pts',(1.91952345758861,24.550000412573,11.8640972412425));
#61003=CARTESIAN_POINT('Ctrl Pts',(1.96588294352946,24.5607466336136,11.9354502051949));
#61004=CARTESIAN_POINT('Ctrl Pts',(1.98539079095622,24.5652685914442,11.9654751872667));
#61005=CARTESIAN_POINT('Ctrl Pts',(2.00423247487847,24.5697652275476,11.9959002729666));
#61006=CARTESIAN_POINT('Ctrl Pts',(2.02239321040764,24.5742255895454,12.0266938375357));
#61007=CARTESIAN_POINT('Ctrl Pts',(2.06903817571315,24.5856818122464,12.1057856093777));
#61008=CARTESIAN_POINT('Ctrl Pts',(2.11103045397057,24.5971236620765,12.1874184618897));
#61009=CARTESIAN_POINT('Ctrl Pts',(2.14791722509451,24.6085374701448,12.2710079526033));
#61010=CARTESIAN_POINT('Ctrl Pts',(2.15952133018242,24.6121281077702,12.2973041342676));
#61011=CARTESIAN_POINT('Ctrl Pts',(2.17062051788247,24.6157159717933,12.3237937961603));
#61012=CARTESIAN_POINT('Ctrl Pts',(2.18120170250727,24.6193006409265,12.3504583663367));
#61013=CARTESIAN_POINT('Ctrl Pts',(2.18122393174747,24.6193081716968,12.3505143839904));
#61014=CARTESIAN_POINT('Ctrl Pts',(2.18124615873495,24.6193157024643,12.3505704024998));
#61015=CARTESIAN_POINT('Ctrl Pts',(2.18126838346963,24.6193232332289,12.3506264218648));
#61016=CARTESIAN_POINT('Ctrl Pts',(2.20973609341923,24.6289694056803,12.4223817457815));
#61017=CARTESIAN_POINT('Ctrl Pts',(2.23450332313288,24.6386105247647,12.4955396730197));
#61018=CARTESIAN_POINT('Ctrl Pts',(2.2556350856279,24.6481441236829,12.5696228019282));
#61019=CARTESIAN_POINT('Ctrl Pts',(2.26875201254688,24.654061827912,12.6156077493765));
#61020=CARTESIAN_POINT('Ctrl Pts',(2.28046925525904,24.6599381860582,12.6619494053648));
#61021=CARTESIAN_POINT('Ctrl Pts',(2.29081156324566,24.6657495006055,12.7085376385827));
#61022=CARTESIAN_POINT('Ctrl Pts',(2.30207900199876,24.6720806435982,12.7592932402412));
#61023=CARTESIAN_POINT('Ctrl Pts',(2.3116601899614,24.6783999723304,12.8103653611132));
#61024=CARTESIAN_POINT('Ctrl Pts',(2.31952197262884,24.6847548600815,12.8616437840524));
#61025=CARTESIAN_POINT('Ctrl Pts',(2.33615474600301,24.6981995725917,12.9701309330633));
#61026=CARTESIAN_POINT('Ctrl Pts',(2.34509270969781,24.7118071130983,13.0795481055681));
#61027=CARTESIAN_POINT('Ctrl Pts',(2.34648323516451,24.7255126943041,13.1888535873786));
#61028=CARTESIAN_POINT('Ctrl Pts',(2.34666482489125,24.7273025160697,13.2031278693303));
#61029=CARTESIAN_POINT('Ctrl Pts',(2.34671764919802,24.7290940155374,13.2174002971286));
#61030=CARTESIAN_POINT('Ctrl Pts',(2.34664198787484,24.7308870536076,13.2316685936994));
#61031=CARTESIAN_POINT('Ctrl Pts',(2.3460443552167,24.7450498789838,13.3443708257972));
#61032=CARTESIAN_POINT('Ctrl Pts',(2.33743141035916,24.7593068482667,13.4568121330953));
#61033=CARTESIAN_POINT('Ctrl Pts',(2.3209700712763,24.7735505590859,13.5677977657174));
#61034=CARTESIAN_POINT('Ctrl Pts',(2.31920339452561,24.7750792337958,13.579709052875));
#61035=CARTESIAN_POINT('Ctrl Pts',(2.31734631797717,24.776607762684,13.5916036223843));
#61036=CARTESIAN_POINT('Ctrl Pts',(2.31539904563125,24.7781360179876,13.6034800327375));
#61037=CARTESIAN_POINT('Ctrl Pts',(2.30072012589076,24.7896563053219,13.6930067364601));
#61038=CARTESIAN_POINT('Ctrl Pts',(2.28107548322618,24.8010011828669,13.78152064807));
#61039=CARTESIAN_POINT('Ctrl Pts',(2.25639523308752,24.8122854609448,13.8683633433921));
#61040=CARTESIAN_POINT('Ctrl Pts',(2.24802818244187,24.8161110350637,13.8978045859193));
#61041=CARTESIAN_POINT('Ctrl Pts',(2.23908248514902,24.8199295887774,13.9270533262758));
#61042=CARTESIAN_POINT('Ctrl Pts',(2.22955587438,24.8237454230163,13.9560826342555));
#61043=CARTESIAN_POINT('Ctrl Pts',(2.22060788506496,24.8273294934508,13.9833487778949));
#61044=CARTESIAN_POINT('Ctrl Pts',(2.21114760051682,24.8309110769025,14.0104206574023));
#61045=CARTESIAN_POINT('Ctrl Pts',(2.20117766020254,24.8344898520955,14.0372755869749));
#61046=CARTESIAN_POINT('Ctrl Pts',(2.19666877540559,24.8361083457425,14.0494206730893));
#61047=CARTESIAN_POINT('Ctrl Pts',(2.19205566739131,24.837726261712,14.0615213648026));
#61048=CARTESIAN_POINT('Ctrl Pts',(2.18733850595882,24.8393436033777,14.0735758212477));
#61049=CARTESIAN_POINT('Ctrl Pts',(2.15412366891343,24.8507317529334,14.1584545798452));
#61050=CARTESIAN_POINT('Ctrl Pts',(2.11568162245519,24.8621133654551,14.241203190023));
#61051=CARTESIAN_POINT('Ctrl Pts',(2.07250095223306,24.8734753982924,14.3212727372763));
#61052=CARTESIAN_POINT('Ctrl Pts',(2.05683229597124,24.8775982566466,14.3503269924905));
#61053=CARTESIAN_POINT('Ctrl Pts',(2.04054018211963,24.8817185388973,14.3790286750262));
#61054=CARTESIAN_POINT('Ctrl Pts',(2.02364947288061,24.8858356285032,14.4073522635993));
#61055=CARTESIAN_POINT('Ctrl Pts',(1.97234923286759,24.8983399989205,14.4933762944002));
#61056=CARTESIAN_POINT('Ctrl Pts',(1.91552827492433,24.9108143979704,14.5759077643999));
#61057=CARTESIAN_POINT('Ctrl Pts',(1.85391371717396,24.9231899294079,14.6543719309755));
#61058=CARTESIAN_POINT('Ctrl Pts',(1.83723589444989,24.926539737099,14.6756106042391));
#61059=CARTESIAN_POINT('Ctrl Pts',(1.82020684408341,24.9298823279963,14.696551569122));
#61060=CARTESIAN_POINT('Ctrl Pts',(1.80284091122112,24.9332163962459,14.7171840815965));
#61061=CARTESIAN_POINT('Ctrl Pts',(1.72900519018026,24.9473920431954,14.8049085043222));
#61062=CARTESIAN_POINT('Ctrl Pts',(1.64890821977102,24.9615971674717,14.8869397613431));
#61063=CARTESIAN_POINT('Ctrl Pts',(1.56345082456623,24.9759033631905,14.9623497514021));
#61064=CARTESIAN_POINT('Ctrl Pts',(1.55458349057646,24.9773878200389,14.9701745343412));
#61065=CARTESIAN_POINT('Ctrl Pts',(1.54565845157056,24.9788733594118,14.9779279823833));
#61066=CARTESIAN_POINT('Ctrl Pts',(1.53667672267686,24.9803600573206,14.985609027744));
#61067=CARTESIAN_POINT('Ctrl Pts',(1.46649583481387,24.9919767271689,15.0456267135936));
#61068=CARTESIAN_POINT('Ctrl Pts',(1.39298361824446,25.0034897132474,15.1013960053529));
#61069=CARTESIAN_POINT('Ctrl Pts',(1.31653655629669,25.0149663173393,15.1524299601093));
#61070=CARTESIAN_POINT('Ctrl Pts',(1.28900030227362,25.0191001934825,15.1708124055058));
#61071=CARTESIAN_POINT('Ctrl Pts',(1.2610833151214,25.0232293098059,15.1885799835318));
#61072=CARTESIAN_POINT('Ctrl Pts',(1.2328044127504,25.0273566770993,15.2057083009526));
#61073=CARTESIAN_POINT('Ctrl Pts',(1.19862197354779,25.0323456784304,15.2264123460107));
#61074=CARTESIAN_POINT('Ctrl Pts',(1.1639127149925,25.0373318212796,15.2461809395287));
#61075=CARTESIAN_POINT('Ctrl Pts',(1.12872391769523,25.042314251943,15.2649699507994));
#61076=CARTESIAN_POINT('Ctrl Pts',(1.10539121064818,25.0456179623276,15.2774284185321));
#61077=CARTESIAN_POINT('Ctrl Pts',(1.08184768478996,25.0489200407177,15.2894562228361));
#61078=CARTESIAN_POINT('Ctrl Pts',(1.05810730004401,25.0522202396665,15.3010408104736));
#61079=CARTESIAN_POINT('Ctrl Pts',(1.05381435491867,25.0528170106599,15.3031356374766));
#61080=CARTESIAN_POINT('Ctrl Pts',(1.04951498853502,25.0534137180518,15.3052159649668));
#61081=CARTESIAN_POINT('Ctrl Pts',(1.04520923680936,25.0540103669038,15.3072817422161));
#61082=CARTESIAN_POINT('Ctrl Pts',(0.969805629592131,25.0644590593851,15.3434582489506));
#61083=CARTESIAN_POINT('Ctrl Pts',(0.892341956280082,25.0749036058817,15.3752162655216));
#61084=CARTESIAN_POINT('Ctrl Pts',(0.813439179742434,25.085329857511,15.402490680532));
#61085=CARTESIAN_POINT('Ctrl Pts',(0.76493533764984,25.0917391790183,15.4192570603336));
#61086=CARTESIAN_POINT('Ctrl Pts',(0.715888201301439,25.0981415910813,15.4343300757289));
#61087=CARTESIAN_POINT('Ctrl Pts',(0.666445302518113,25.1045338451292,15.4477037384638));
#61088=CARTESIAN_POINT('Ctrl Pts',(0.614869246181018,25.1112018856974,15.4616543926451));
#61089=CARTESIAN_POINT('Ctrl Pts',(0.562857337859564,25.1178595682796,15.4737578028836));
#61090=CARTESIAN_POINT('Ctrl Pts',(0.510559142633728,25.1244846159198,15.4840465880969));
#61091=CARTESIAN_POINT('Ctrl Pts',(0.400691370382397,25.1384024810037,15.5056612137196));
#61092=CARTESIAN_POINT('Ctrl Pts',(0.289494973989037,25.1523103392757,15.5191035287391));
#61093=CARTESIAN_POINT('Ctrl Pts',(0.178168006039007,25.1662170317109,15.5243958968317));
#61094=CARTESIAN_POINT('Ctrl Pts',(0.154206513136954,25.1692102427739,15.5255350012447));
#61095=CARTESIAN_POINT('Ctrl Pts',(0.130238937104567,25.1722033992284,15.52629636005));
#61096=CARTESIAN_POINT('Ctrl Pts',(0.106277191373282,25.1751965882398,15.5266798849848));
#61097=CARTESIAN_POINT('Ctrl Pts',(-0.0157005557933355,25.1904334769267,
15.528632226357));
#61098=CARTESIAN_POINT('Ctrl Pts',(-0.137518646175449,25.2055947319702,
15.5209039553958));
#61099=CARTESIAN_POINT('Ctrl Pts',(-0.257535222984943,25.2207227529219,
15.5034159658435));
#61100=CARTESIAN_POINT('Ctrl Pts',(-0.32788569056501,25.2295903891752,15.4931649798986));
#61101=CARTESIAN_POINT('Ctrl Pts',(-0.39761384151569,25.2384462211708,15.4795598380239));
#61102=CARTESIAN_POINT('Ctrl Pts',(-0.466367579709816,25.2472885820012,
15.4625996730074));
#61103=CARTESIAN_POINT('Ctrl Pts',(-0.508500016991226,25.2527071995613,
15.4522064477428));
#61104=CARTESIAN_POINT('Ctrl Pts',(-0.55026502310578,25.2581205625057,15.4405538196307));
#61105=CARTESIAN_POINT('Ctrl Pts',(-0.591582755307492,25.2635284025615,
15.4276425302246));
#61106=CARTESIAN_POINT('Ctrl Pts',(-0.64233587687555,25.2701711864015,15.4117827962579));
#61107=CARTESIAN_POINT('Ctrl Pts',(-0.692434795980019,25.276808341162,15.3940173763629));
#61108=CARTESIAN_POINT('Ctrl Pts',(-0.741770597672253,25.2834392934233,
15.3744395748014));
#61109=CARTESIAN_POINT('Ctrl Pts',(-0.857544245502194,25.2989997891597,
15.3284974105817));
#61110=CARTESIAN_POINT('Ctrl Pts',(-0.969110719126935,25.3145257007673,
15.2725724022707));
#61111=CARTESIAN_POINT('Ctrl Pts',(-1.07505557528344,25.3300070899883,15.2079177932711));
#61112=CARTESIAN_POINT('Ctrl Pts',(-1.18911110385875,25.3466736663067,15.1383135116495));
#61113=CARTESIAN_POINT('Ctrl Pts',(-1.29665566949087,25.3632890992371,15.0585942988193));
#61114=CARTESIAN_POINT('Ctrl Pts',(-1.39601903951251,25.3798514631867,14.9703134442671));
#61115=CARTESIAN_POINT('Ctrl Pts',(-1.47922852439741,25.3937212199434,14.8963847476972));
#61116=CARTESIAN_POINT('Ctrl Pts',(-1.55669744124286,25.4075529445037,14.8164578973725));
#61117=CARTESIAN_POINT('Ctrl Pts',(-1.62747830354971,25.4213506382061,14.731414023057));
#61118=CARTESIAN_POINT('Ctrl Pts',(-1.66759405307742,25.429170616751,14.6832145712601));
#61119=CARTESIAN_POINT('Ctrl Pts',(-1.70556177787918,25.4369797441687,14.6333706895916));
#61120=CARTESIAN_POINT('Ctrl Pts',(-1.74120779536032,25.4447788901693,14.5820398672115));
#61121=CARTESIAN_POINT('Ctrl Pts',(-1.76668649433977,25.4503534846762,14.5453501424061));
#61122=CARTESIAN_POINT('Ctrl Pts',(-1.79097852609347,25.4559228466412,14.5079016655005));
#61123=CARTESIAN_POINT('Ctrl Pts',(-1.81402318205396,25.4614881423788,14.4697456290445));
#61124=CARTESIAN_POINT('Ctrl Pts',(-1.82321919151665,25.4637089831826,14.4545193972921));
#61125=CARTESIAN_POINT('Ctrl Pts',(-1.83221652257459,25.4659291714859,14.4391805132043));
#61126=CARTESIAN_POINT('Ctrl Pts',(-1.84101122675499,25.4681487818585,14.4237321791533));
#61127=CARTESIAN_POINT('Ctrl Pts',(-1.88684654114243,25.4797167137817,14.3432201763085));
#61128=CARTESIAN_POINT('Ctrl Pts',(-1.92720831415073,25.4912775260564,14.2596729273911));
#61129=CARTESIAN_POINT('Ctrl Pts',(-1.96195986740268,25.5028194777214,14.1739469541749));
#61130=CARTESIAN_POINT('Ctrl Pts',(-1.97652305852491,25.5076563161441,14.138022121606));
#61131=CARTESIAN_POINT('Ctrl Pts',(-1.99010154975033,25.5124898446114,14.1017150196534));
#61132=CARTESIAN_POINT('Ctrl Pts',(-2.00268767175644,25.5173192087944,14.0650899071979));
#61133=CARTESIAN_POINT('Ctrl Pts',(-2.03305155914572,25.5289699992557,13.9767322073694));
#61134=CARTESIAN_POINT('Ctrl Pts',(-2.05764605012002,25.5405910885114,13.8865324065618));
#61135=CARTESIAN_POINT('Ctrl Pts',(-2.07648640744474,25.5521405012169,13.7953550858352));
#61136=CARTESIAN_POINT('Ctrl Pts',(-2.08463482010811,25.5571355965393,13.7559210972959));
#61137=CARTESIAN_POINT('Ctrl Pts',(-2.09170733081712,25.5621173521082,13.7163037678985));
#61138=CARTESIAN_POINT('Ctrl Pts',(-2.09770689659465,25.5670826828953,13.6765705608211));
#61139=CARTESIAN_POINT('Ctrl Pts',(-2.1132466639355,25.5799436278473,13.5736556472115));
#61140=CARTESIAN_POINT('Ctrl Pts',(-2.1213613048407,25.5928052311059,13.4698990160121));
#61141=CARTESIAN_POINT('Ctrl Pts',(-2.12187461644586,25.6057095945976,13.3664402375084));
#61142=CARTESIAN_POINT('Ctrl Pts',(-2.12200261201119,25.6089273307325,13.3406425257282));
#61143=CARTESIAN_POINT('Ctrl Pts',(-2.12165791636404,25.6121476908188,13.3148635757551));
#61144=CARTESIAN_POINT('Ctrl Pts',(-2.12083770945619,25.6153712581238,13.2891215522233));
#61145=CARTESIAN_POINT('Ctrl Pts',(-2.11938579728351,25.6210775458481,13.243553590094));
#61146=CARTESIAN_POINT('Ctrl Pts',(-2.11644439600435,25.6267938637586,13.1980997598415));
#61147=CARTESIAN_POINT('Ctrl Pts',(-2.11199908667531,25.6325229244125,13.1528573978578));
#61148=CARTESIAN_POINT('Ctrl Pts',(-2.10483338533847,25.641757993234,13.0799281077339));
#61149=CARTESIAN_POINT('Ctrl Pts',(-2.09402822430077,25.6509132713589,13.0075333641132));
#61150=CARTESIAN_POINT('Ctrl Pts',(-2.07943293734265,25.6600407951577,12.9360188309056));
#61151=CARTESIAN_POINT('Ctrl Pts',(-2.0751099749949,25.6627442666156,12.9148370182245));
#61152=CARTESIAN_POINT('Ctrl Pts',(-2.07045436364957,25.665445268338,12.893732736597));
#61153=CARTESIAN_POINT('Ctrl Pts',(-2.06546185421087,25.6681450640045,12.8727157771258));
#61154=CARTESIAN_POINT('Ctrl Pts',(-2.06544940448432,25.668151796434,12.8726633675306));
#61155=CARTESIAN_POINT('Ctrl Pts',(-2.06543695264387,25.6681585288649,12.8726109584431));
#61156=CARTESIAN_POINT('Ctrl Pts',(-2.06542449868951,25.6681652612972,12.8725585498632));
#61157=CARTESIAN_POINT('Ctrl Pts',(-2.04706670352818,25.6780892267127,12.7953054986337));
#61158=CARTESIAN_POINT('Ctrl Pts',(-2.02411173197653,25.6880159792777,12.719157839309));
#61159=CARTESIAN_POINT('Ctrl Pts',(-1.99691841665238,25.6979165175409,12.6446076271924));
#61160=CARTESIAN_POINT('Ctrl Pts',(-1.97815704130777,25.7047471563305,12.5931734973385));
#61161=CARTESIAN_POINT('Ctrl Pts',(-1.95737933574469,25.711565369604,12.5424992703761));
#61162=CARTESIAN_POINT('Ctrl Pts',(-1.93471454859936,25.7183623386049,12.4927378129865));
#61163=CARTESIAN_POINT('Ctrl Pts',(-1.90381859825576,25.727627760574,12.4249045036916));
#61164=CARTESIAN_POINT('Ctrl Pts',(-1.86951402923737,25.736814826264,12.3587326941799));
#61165=CARTESIAN_POINT('Ctrl Pts',(-1.83195605601144,25.7459738178074,12.2945925865526));
#61166=CARTESIAN_POINT('Ctrl Pts',(-1.799712190562,25.7538368962861,12.2395277142336));
#61167=CARTESIAN_POINT('Ctrl Pts',(-1.76507040226176,25.7616791745314,12.1859612746389));
#61168=CARTESIAN_POINT('Ctrl Pts',(-1.72814447768616,25.7695284244644,12.1341536739523));
#61169=CARTESIAN_POINT('Ctrl Pts',(-1.67904171679383,25.7799660735435,12.0652617976308));
#61170=CARTESIAN_POINT('Ctrl Pts',(-1.62589626718616,25.7904174914076,11.9994767187561));
#61171=CARTESIAN_POINT('Ctrl Pts',(-1.56903195918004,25.8009195175335,11.9373505639572));
#61172=CARTESIAN_POINT('Ctrl Pts',(-1.55282802297368,25.8039121532895,11.9196472227155));
#61173=CARTESIAN_POINT('Ctrl Pts',(-1.53632224392474,25.8069088566848,11.902241282607));
#61174=CARTESIAN_POINT('Ctrl Pts',(-1.51952248701259,25.8099103799305,11.8851461970513));
#61175=CARTESIAN_POINT('Ctrl Pts',(-1.47307690973132,25.8182085642789,11.8378841371619));
#61176=CARTESIAN_POINT('Ctrl Pts',(-1.42436848087704,25.8265465474126,11.7929833373008));
#61177=CARTESIAN_POINT('Ctrl Pts',(-1.3736949908021,25.8348777561905,11.7505909960002));
#61178=CARTESIAN_POINT('Ctrl Pts',(-1.32316410291418,25.8431855197984,11.7083179525923));
#61179=CARTESIAN_POINT('Ctrl Pts',(-1.27067975251719,25.8514865453385,11.6685385981701));
#61180=CARTESIAN_POINT('Ctrl Pts',(-1.21649750600729,25.8597412413196,11.6313665775228));
#61181=CARTESIAN_POINT('Ctrl Pts',(-1.20785701892122,25.8610576244269,11.6254387250424));
#61182=CARTESIAN_POINT('Ctrl Pts',(-1.19917326060815,25.862372843015,11.6195771253524));
#61183=CARTESIAN_POINT('Ctrl Pts',(-1.19044715961659,25.8636867521325,11.6137821819781));
#61184=CARTESIAN_POINT('Ctrl Pts',(-1.19043009629525,25.863689321396,11.6137708503443));
#61185=CARTESIAN_POINT('Ctrl Pts',(-1.19041303281199,25.8636918906546,11.6137595189654));
#61186=CARTESIAN_POINT('Ctrl Pts',(-1.19039596916682,25.8636944599082,11.6137481878413));
#61187=CARTESIAN_POINT('Ctrl Pts',(-1.1264798774272,25.8733182328611,11.5713046678307));
#61188=CARTESIAN_POINT('Ctrl Pts',(-1.0602419068925,25.88287799545,11.5324007693119));
#61189=CARTESIAN_POINT('Ctrl Pts',(-0.992127910317745,25.8923960439564,
11.497249014445));
#61190=CARTESIAN_POINT('Ctrl Pts',(-0.954893728848248,25.8975990383944,
11.4780334804064));
#61191=CARTESIAN_POINT('Ctrl Pts',(-0.917099873275302,25.9027894827606,
11.4599391294038));
#61192=CARTESIAN_POINT('Ctrl Pts',(-0.878825649101653,25.9079703957492,
11.4429997173555));
#61193=CARTESIAN_POINT('Ctrl Pts',(-0.806452006496361,25.917767107586,11.4109685794291));
#61194=CARTESIAN_POINT('Ctrl Pts',(-0.732357649991044,25.9275309240989,
11.383069151588));
#61195=CARTESIAN_POINT('Ctrl Pts',(-0.657042265930863,25.9372912720487,
11.3595166165103));
#61196=CARTESIAN_POINT('Ctrl Pts',(-0.617950712547168,25.9423572644442,
11.3472919535971));
#61197=CARTESIAN_POINT('Ctrl Pts',(-0.578531040024393,25.9474222116115,
11.3362385664458));
#61198=CARTESIAN_POINT('Ctrl Pts',(-0.538858577138134,25.9524895090482,
11.3263872119904));
#61199=CARTESIAN_POINT('Ctrl Pts',(-0.461125338555252,25.9624182458083,
11.3070847127117));
#61200=CARTESIAN_POINT('Ctrl Pts',(-0.382413447933152,25.972357367322,11.2923951419602));
#61201=CARTESIAN_POINT('Ctrl Pts',(-0.303259288052649,25.9823332138581,
11.2825335805622));
#61202=CARTESIAN_POINT('Ctrl Pts',(-0.297711178831835,25.9830324454113,
11.2818423595347));
#61203=CARTESIAN_POINT('Ctrl Pts',(-0.292160916532026,25.983731854668,11.2811748657093));
#61204=CARTESIAN_POINT('Ctrl Pts',(-0.286608694963468,25.9844314494653,
11.2805311761697));
#61205=CARTESIAN_POINT('Ctrl Pts',(-0.222577255127463,25.9924995824858,
11.2731077750104));
#61206=CARTESIAN_POINT('Ctrl Pts',(-0.158271073497767,26.0005943248532,
11.2688495367221));
#61207=CARTESIAN_POINT('Ctrl Pts',(-0.094001194438398,26.0086819927456,
11.2676757735204));
#61208=CARTESIAN_POINT('Ctrl Pts',(-0.0387229759484104,26.0156381575833,
11.2666662253515));
#61209=CARTESIAN_POINT('Ctrl Pts',(0.0165292080911561,26.0225891930742,
11.2679379464167));
#61210=CARTESIAN_POINT('Ctrl Pts',(0.0715880859921679,26.0295175830648,
11.2714396645856));
#61211=CARTESIAN_POINT('Ctrl Pts',(0.084378900806373,26.0311271282772,11.2722531542595));
#61212=CARTESIAN_POINT('Ctrl Pts',(0.0971588050985991,26.0327353844242,
11.2731869421992));
#61213=CARTESIAN_POINT('Ctrl Pts',(0.109925490074801,26.0343421056677,11.2742403467456));
#61214=CARTESIAN_POINT('Ctrl Pts',(0.109972769734755,26.0343480559386,11.2742442478843));
#61215=CARTESIAN_POINT('Ctrl Pts',(0.110020049213505,26.0343540061884,11.2742481506635));
#61216=CARTESIAN_POINT('Ctrl Pts',(0.11006732851095,26.0343599564172,11.2742520550831));
#61217=CARTESIAN_POINT('Ctrl Pts',(0.188020361137296,26.0441705586301,11.2806895735294));
#61218=CARTESIAN_POINT('Ctrl Pts',(0.265575905387572,26.0539352675481,11.2915938245673));
#61219=CARTESIAN_POINT('Ctrl Pts',(0.342214902082606,26.063668281761,11.3068339293819));
#61220=CARTESIAN_POINT('Ctrl Pts',(0.390739736116091,26.0698308480744,11.3164833714241));
#61221=CARTESIAN_POINT('Ctrl Pts',(0.438896281133394,26.0759806095347,11.3278703749953));
#61222=CARTESIAN_POINT('Ctrl Pts',(0.486545379588903,26.0821201325041,11.3409539337011));
#61223=CARTESIAN_POINT('Ctrl Pts',(0.563970580707379,26.0920962667036,11.362213457952));
#61224=CARTESIAN_POINT('Ctrl Pts',(0.640056503626392,26.1020463490841,11.3879562301718));
#61225=CARTESIAN_POINT('Ctrl Pts',(0.71424317795541,26.1119894619148,11.4180218755906));
#61226=CARTESIAN_POINT('Ctrl Pts',(0.759084224907484,26.1179994305961,11.4361946138898));
#61227=CARTESIAN_POINT('Ctrl Pts',(0.803230433542023,26.1240067201267,11.4559463527347));
#61228=CARTESIAN_POINT('Ctrl Pts',(0.846550212966073,26.1300143244821,11.4772370783737));
#61229=CARTESIAN_POINT('Ctrl Pts',(0.909556373290494,26.138752044023,11.5082032303457));
#61230=CARTESIAN_POINT('Ctrl Pts',(0.970821095358348,26.1474914138024,11.5424279026674));
#61231=CARTESIAN_POINT('Ctrl Pts',(1.02995902501875,26.156242665362,11.5797922673297));
#61232=CARTESIAN_POINT('Ctrl Pts',(1.08330906414026,26.1641374228509,11.6134997428524));
#61233=CARTESIAN_POINT('Ctrl Pts',(1.13493737523878,26.1720434998679,11.649770328516));
#61234=CARTESIAN_POINT('Ctrl Pts',(1.18465916249167,26.1799398318734,11.6883537635916));
#61235=CARTESIAN_POINT('Ctrl Pts',(1.2319428817391,26.1874489735649,11.7250452908378));
#61236=CARTESIAN_POINT('Ctrl Pts',(1.2775032029302,26.1949493480024,11.7638280765745));
#61237=CARTESIAN_POINT('Ctrl Pts',(1.32121473384328,26.2024283816673,11.8045145043413));
#61238=CARTESIAN_POINT('Ctrl Pts',(1.32122793493449,26.2024306403712,11.8045267918369));
#61239=CARTESIAN_POINT('Ctrl Pts',(1.32124113585729,26.2024328990732,11.8045390795064));
#61240=CARTESIAN_POINT('Ctrl Pts',(1.32125433661169,26.2024351577733,11.8045513673497));
#61241=CARTESIAN_POINT('Ctrl Pts',(1.37801297437162,26.2121467800477,11.8573848060531));
#61242=CARTESIAN_POINT('Ctrl Pts',(1.43169948115193,26.2218308038756,11.9134760130508));
#61243=CARTESIAN_POINT('Ctrl Pts',(1.48198939395346,26.2314938796934,11.9724026782956));
#61244=CARTESIAN_POINT('Ctrl Pts',(1.51313722648761,26.2374788546232,12.0088998165603));
#61245=CARTESIAN_POINT('Ctrl Pts',(1.54298181658575,26.2434556952527,12.0464836545084));
#61246=CARTESIAN_POINT('Ctrl Pts',(1.57144506963523,26.2494250094457,12.0850439326772));
#61247=CARTESIAN_POINT('Ctrl Pts',(1.61873444276281,26.2593425380465,12.1491086894025));
#61248=CARTESIAN_POINT('Ctrl Pts',(1.66220900579363,26.2692399343127,12.2158722020372));
#61249=CARTESIAN_POINT('Ctrl Pts',(1.70152968323113,26.2791263300845,12.2848631692563));
#61250=CARTESIAN_POINT('Ctrl Pts',(1.72475382543219,26.2849655748846,12.3256116033551));
#61251=CARTESIAN_POINT('Ctrl Pts',(1.74652835507116,26.2908008517139,12.367136242237));
#61252=CARTESIAN_POINT('Ctrl Pts',(1.76678028680931,26.2966329134192,12.4093320909615));
#61253=CARTESIAN_POINT('Ctrl Pts',(1.80005920530197,26.3062164291375,12.4786702769966));
#61254=CARTESIAN_POINT('Ctrl Pts',(1.82923081452741,26.3157924156678,12.5498286696334));
#61255=CARTESIAN_POINT('Ctrl Pts',(1.85398895827861,26.3253663094589,12.6223615583329));
#61256=CARTESIAN_POINT('Ctrl Pts',(1.87236010055433,26.33247037052,12.676182718407));
#61257=CARTESIAN_POINT('Ctrl Pts',(1.88830247173791,26.3395741832107,12.7307678714192));
#61258=CARTESIAN_POINT('Ctrl Pts',(1.90188226208757,26.3466673663647,12.7858629420231));
#61259=CARTESIAN_POINT('Ctrl Pts',(1.91546205243723,26.3537605495187,12.840958012627));
#61260=CARTESIAN_POINT('Ctrl Pts',(1.92668008312622,26.3608431015405,12.8965627720862));
#61261=CARTESIAN_POINT('Ctrl Pts',(1.93561630538568,26.367911785215,12.9524780880961));
#61262=CARTESIAN_POINT('Ctrl Pts',(1.93562275162362,26.3679168842843,12.9525184231976));
#61263=CARTESIAN_POINT('Ctrl Pts',(1.93562919656829,26.3679219833525,12.9525587584958));
#61264=CARTESIAN_POINT('Ctrl Pts',(1.93563564021965,26.3679270824197,12.9525990939906));
#61265=CARTESIAN_POINT('Ctrl Pts',(1.95062575478464,26.3797892388983,13.0464331104734));
#61266=CARTESIAN_POINT('Ctrl Pts',(1.95861245256558,26.3916455404621,13.1413327981437));
#61267=CARTESIAN_POINT('Ctrl Pts',(1.95972135279568,26.4034863493552,13.2362255096162));
#61268=CARTESIAN_POINT('Ctrl Pts',(1.96011599306144,26.4077003082321,13.2699963429669));
#61269=CARTESIAN_POINT('Ctrl Pts',(1.95964000198191,26.4119122991106,13.3037661489313));
#61270=CARTESIAN_POINT('Ctrl Pts',(1.95830058261461,26.4161218682396,13.3374862584528));
#61271=CARTESIAN_POINT('Ctrl Pts',(1.95434162975595,26.4285641892513,13.4371535674707));
#61272=CARTESIAN_POINT('Ctrl Pts',(1.94284017687827,26.4409852182778,13.5363853582024));
#61273=CARTESIAN_POINT('Ctrl Pts',(1.92400116712185,26.4533856195568,13.6340279456407));
#61274=CARTESIAN_POINT('Ctrl Pts',(1.91445570397717,26.4596687297053,13.683502081054));
#61275=CARTESIAN_POINT('Ctrl Pts',(1.90302703138298,26.4659463059117,13.7325664537329));
#61276=CARTESIAN_POINT('Ctrl Pts',(1.88973927860849,26.472219504861,13.7810795599549));
#61277=CARTESIAN_POINT('Ctrl Pts',(1.88062909918911,26.476520455438,13.8143404965012));
#61278=CARTESIAN_POINT('Ctrl Pts',(1.87064488666174,26.4808194051564,13.847342746645));
#61279=CARTESIAN_POINT('Ctrl Pts',(1.85979331324087,26.4851168427575,13.8800413709616));
#61280=CARTESIAN_POINT('Ctrl Pts',(1.85523491647467,26.4869220579926,13.8937770107222));
#61281=CARTESIAN_POINT('Ctrl Pts',(1.85052345568052,26.4887270075576,13.9074590790529));
#61282=CARTESIAN_POINT('Ctrl Pts',(1.84565939619719,26.4905317240626,13.9210842015379));
#61283=CARTESIAN_POINT('Ctrl Pts',(1.81614650041742,26.5014819211777,14.0037552340909));
#61284=CARTESIAN_POINT('Ctrl Pts',(1.78105506079411,26.5124100594858,14.0842289057742));
#61285=CARTESIAN_POINT('Ctrl Pts',(1.74082207812923,26.5233253660463,14.1619289386771));
#61286=CARTESIAN_POINT('Ctrl Pts',(1.70864272274104,26.5320557038368,14.2240753868607));
#61287=CARTESIAN_POINT('Ctrl Pts',(1.67317232189177,26.5407780438814,14.2844488396059));
#61288=CARTESIAN_POINT('Ctrl Pts',(1.6346238651926,26.5494960544694,14.3427400123217));
#61289=CARTESIAN_POINT('Ctrl Pts',(1.58845574675654,26.559937306333,14.4125532810273));
#61290=CARTESIAN_POINT('Ctrl Pts',(1.53787552728397,26.5703712878131,14.4793717093387));
#61291=CARTESIAN_POINT('Ctrl Pts',(1.4832791576902,26.5807970301582,14.5426113180809));
#61292=CARTESIAN_POINT('Ctrl Pts',(1.45068725105528,26.5870207923541,14.5803629019149));
#61293=CARTESIAN_POINT('Ctrl Pts',(1.41666303948595,26.5932418291801,14.6168403129119));
#61294=CARTESIAN_POINT('Ctrl Pts',(1.38129613268988,26.5994591668962,14.6519153510326));
#61295=CARTESIAN_POINT('Ctrl Pts',(1.35961950282918,26.6032698176033,14.6734130924969));
#61296=CARTESIAN_POINT('Ctrl Pts',(1.33743898344636,26.6070789961626,14.6943835775831));
#61297=CARTESIAN_POINT('Ctrl Pts',(1.31477635765406,26.6108863604908,14.7147970998005));
#61298=CARTESIAN_POINT('Ctrl Pts',(1.31247484687325,26.6112730186886,14.7168702020918));
#61299=CARTESIAN_POINT('Ctrl Pts',(1.31016836889469,26.611659657391,14.7189375563384));
#61300=CARTESIAN_POINT('Ctrl Pts',(1.30785693242784,26.6120462786337,14.720999144444));
#61301=CARTESIAN_POINT('Ctrl Pts',(1.24754470925209,26.6221343719074,14.7747920839022));
#61302=CARTESIAN_POINT('Ctrl Pts',(1.18380547269851,26.6322186925159,14.8246994538605));
#61303=CARTESIAN_POINT('Ctrl Pts',(1.11728747194782,26.642288086747,14.870392029666));
#61304=CARTESIAN_POINT('Ctrl Pts',(1.08014341960182,26.647910897147,14.8959070392632));
#61305=CARTESIAN_POINT('Ctrl Pts',(1.04213727426503,26.6535285142367,14.9201063881285));
#61306=CARTESIAN_POINT('Ctrl Pts',(1.00336745358979,26.6591415297132,14.9429479129451));
#61307=CARTESIAN_POINT('Ctrl Pts',(0.924298984036139,26.6705889012921,14.9895316829514));
#61308=CARTESIAN_POINT('Ctrl Pts',(0.842044189226941,26.682018815034,15.0304781036758));
#61309=CARTESIAN_POINT('Ctrl Pts',(0.757372202484891,26.6934429055962,15.0654266189583));
#61310=CARTESIAN_POINT('Ctrl Pts',(0.708942119160386,26.6999771760099,15.0854162232221));
#61311=CARTESIAN_POINT('Ctrl Pts',(0.659718569616521,26.7065098058046,15.1034428713422));
#61312=CARTESIAN_POINT('Ctrl Pts',(0.609871030073124,26.7130393843689,15.1194250206855));
#61313=CARTESIAN_POINT('Ctrl Pts',(0.577391561902696,26.7172939020661,15.1298386081092));
#61314=CARTESIAN_POINT('Ctrl Pts',(0.544647299040207,26.7215471137913,15.1393842404181));
#61315=CARTESIAN_POINT('Ctrl Pts',(0.511685614043769,26.72579860937,15.1480401775463));
#61316=CARTESIAN_POINT('Ctrl Pts',(0.494059682036892,26.7280720541895,15.1526688535164));
#61317=CARTESIAN_POINT('Ctrl Pts',(0.476371647943156,26.7303449999217,15.1570431209779));
#61318=CARTESIAN_POINT('Ctrl Pts',(0.45862857818344,26.7326174092138,15.1611597883168));
#61319=CARTESIAN_POINT('Ctrl Pts',(0.38046746716195,26.7426277421139,15.1792943781745));
#61320=CARTESIAN_POINT('Ctrl Pts',(0.301129619201349,26.7526414469723,15.192451208845));
#61321=CARTESIAN_POINT('Ctrl Pts',(0.221333754180482,26.7626470419077,15.2006242822204));
#61322=CARTESIAN_POINT('Ctrl Pts',(0.166144292991359,26.7695672425123,15.2062770502646));
#61323=CARTESIAN_POINT('Ctrl Pts',(0.110738439382832,26.7764832785875,15.2095467921131));
#61324=CARTESIAN_POINT('Ctrl Pts',(0.0553475638220142,26.7833923674015,
15.2104447558368));
#61325=CARTESIAN_POINT('Ctrl Pts',(-0.0390703674654303,26.795169431156,
15.2119754028308));
#61326=CARTESIAN_POINT('Ctrl Pts',(-0.133458536060384,26.8069280922523,
15.2066172944852));
#61327=CARTESIAN_POINT('Ctrl Pts',(-0.22680115270891,26.8186701463211,15.1944388640106));
#61328=CARTESIAN_POINT('Ctrl Pts',(-0.281207451622415,26.8255141981215,
15.1873404629534));
#61329=CARTESIAN_POINT('Ctrl Pts',(-0.335267285992045,26.832353670009,15.1779243281533));
#61330=CARTESIAN_POINT('Ctrl Pts',(-0.388799278321244,26.8391914212386,
15.1661949873908));
#61331=CARTESIAN_POINT('Ctrl Pts',(-0.423252557289703,26.8435922092604,
15.1586459642399));
#61332=CARTESIAN_POINT('Ctrl Pts',(-0.4574866653146,26.847992220101,15.1501386986599));
#61333=CARTESIAN_POINT('Ctrl Pts',(-0.49145180641335,26.852392081566,15.1406732080927));
#61334=CARTESIAN_POINT('Ctrl Pts',(-0.599371058044128,26.8663719957137,
15.1105980008277));
#61335=CARTESIAN_POINT('Ctrl Pts',(-0.704548142392309,26.8803470920764,
15.0708508825517));
#61336=CARTESIAN_POINT('Ctrl Pts',(-0.805424879994097,26.8943094435373,
15.0223366624272));
#61337=CARTESIAN_POINT('Ctrl Pts',(-0.813762095815551,26.8954633977617,
15.018327080702));
#61338=CARTESIAN_POINT('Ctrl Pts',(-0.822069946174581,26.8966172649693,
15.0142576422613));
#61339=CARTESIAN_POINT('Ctrl Pts',(-0.830347556806284,26.8977710407052,
15.0101288725927));
#61340=CARTESIAN_POINT('Ctrl Pts',(-0.91080387239077,26.9089854537587,14.9699982587943));
#61341=CARTESIAN_POINT('Ctrl Pts',(-0.988407123994427,26.9201971235708,
14.9242936222472));
#61342=CARTESIAN_POINT('Ctrl Pts',(-1.06244749711786,26.9314310570154,14.8735557043439));
#61343=CARTESIAN_POINT('Ctrl Pts',(-1.08585840943374,26.9349831275918,14.8575128226428));
#61344=CARTESIAN_POINT('Ctrl Pts',(-1.10891344923103,26.9385374708552,14.8409665277642));
#61345=CARTESIAN_POINT('Ctrl Pts',(-1.13159104930669,26.9420950068572,14.8239332758962));
#61346=CARTESIAN_POINT('Ctrl Pts',(-1.1946640178834,26.9519895440091,14.7765588731266));
#61347=CARTESIAN_POINT('Ctrl Pts',(-1.25476955099053,26.9618813400662,14.7253122557269));
#61348=CARTESIAN_POINT('Ctrl Pts',(-1.31137381328732,26.9717637864018,14.670461066501));
#61349=CARTESIAN_POINT('Ctrl Pts',(-1.31139052214061,26.9717667035734,14.6704448751324));
#61350=CARTESIAN_POINT('Ctrl Pts',(-1.31140723068865,26.9717696207442,14.6704286834497));
#61351=CARTESIAN_POINT('Ctrl Pts',(-1.31142393893143,26.9717725379141,14.6704124914531));
#61352=CARTESIAN_POINT('Ctrl Pts',(-1.33082736807509,26.9751602729854,14.6516085834398));
#61353=CARTESIAN_POINT('Ctrl Pts',(-1.34981315569576,26.9785457490261,14.6323860978909));
#61354=CARTESIAN_POINT('Ctrl Pts',(-1.36836037779142,26.9819253610666,14.6127570761749));
#61355=CARTESIAN_POINT('Ctrl Pts',(-1.42590474410372,26.9924109007471,14.5518563326483));
#61356=CARTESIAN_POINT('Ctrl Pts',(-1.47923450728921,27.0028405712445,14.4870294015218));
#61357=CARTESIAN_POINT('Ctrl Pts',(-1.52804058251419,27.0132426074834,14.4189863742454));
#61358=CARTESIAN_POINT('Ctrl Pts',(-1.57616415976755,27.0234991829656,14.3518948520406));
#61359=CARTESIAN_POINT('Ctrl Pts',(-1.61989074263381,27.0337289117467,14.2816768217104));
#61360=CARTESIAN_POINT('Ctrl Pts',(-1.65894551313848,27.0439651116435,14.2089685605005));
#61361=CARTESIAN_POINT('Ctrl Pts',(-1.6979841396017,27.0541970802099,14.1362903546504));
#61362=CARTESIAN_POINT('Ctrl Pts',(-1.73235238482967,27.0644360409672,14.0611322062671));
#61363=CARTESIAN_POINT('Ctrl Pts',(-1.76175618743411,27.0747075582735,13.9841704423163));
#61364=CARTESIAN_POINT('Ctrl Pts',(-1.77653058095541,27.0798686403549,13.9454998185878));
#61365=CARTESIAN_POINT('Ctrl Pts',(-1.79005226973994,27.0850380317582,13.9063733688481));
#61366=CARTESIAN_POINT('Ctrl Pts',(-1.80228759725112,27.0902195146341,13.8668735420617));
#61367=CARTESIAN_POINT('Ctrl Pts',(-1.80229046233201,27.0902207279541,13.8668642925995));
#61368=CARTESIAN_POINT('Ctrl Pts',(-1.80229332734293,27.0902219412749,13.8668550431156));
#61369=CARTESIAN_POINT('Ctrl Pts',(-1.80229619228388,27.0902231545967,13.8668457936099));
#61370=CARTESIAN_POINT('Ctrl Pts',(-1.82161493453645,27.0984047720284,13.8044749386984));
#61371=CARTESIAN_POINT('Ctrl Pts',(-1.8377521095277,27.106627436244,13.7411106197772));
#61372=CARTESIAN_POINT('Ctrl Pts',(-1.85056980592683,27.114845167761,13.6770854800078));
#61373=CARTESIAN_POINT('Ctrl Pts',(-1.8574351557973,27.1192467076516,13.642792657699));
#61374=CARTESIAN_POINT('Ctrl Pts',(-1.86334817017396,27.1236467259484,13.6083111509094));
#61375=CARTESIAN_POINT('Ctrl Pts',(-1.86828817979346,27.1280374245996,13.5736981560504));
#61376=CARTESIAN_POINT('Ctrl Pts',(-1.87384907442427,27.1329799681239,13.5347348276173));
#61377=CARTESIAN_POINT('Ctrl Pts',(-1.87817738865227,27.1379110306736,13.4956014988121));
#61378=CARTESIAN_POINT('Ctrl Pts',(-1.88124534124361,27.1428204812618,13.4563732323631));
#61379=CARTESIAN_POINT('Ctrl Pts',(-1.88670842728362,27.1515627124969,13.3865196774493));
#61380=CARTESIAN_POINT('Ctrl Pts',(-1.88817352459399,27.160236350819,13.3163590539875));
#61381=CARTESIAN_POINT('Ctrl Pts',(-1.88574467811591,27.168885879747,13.2463477102035));
#61382=CARTESIAN_POINT('Ctrl Pts',(-1.88469445278418,27.1726259079743,13.2160750324473));
#61383=CARTESIAN_POINT('Ctrl Pts',(-1.88291621065804,27.1763615122148,13.1858296027228));
#61384=CARTESIAN_POINT('Ctrl Pts',(-1.88041816319571,27.1800966692258,13.1556453328878));
#61385=CARTESIAN_POINT('Ctrl Pts',(-1.87412761009965,27.1895024967189,13.0796356673686));
#61386=CARTESIAN_POINT('Ctrl Pts',(-1.86336477392588,27.1989397763323,13.004033176327));
#61387=CARTESIAN_POINT('Ctrl Pts',(-1.84820671069898,27.208441770839,12.9293977240039));
#61388=CARTESIAN_POINT('Ctrl Pts',(-1.84820111143111,27.2084452808001,12.929370154262));
#61389=CARTESIAN_POINT('Ctrl Pts',(-1.84819551153823,27.2084487907615,12.929342584645));
#61390=CARTESIAN_POINT('Ctrl Pts',(-1.84818991102035,27.2084523007232,12.9293150151529));
#61391=CARTESIAN_POINT('Ctrl Pts',(-1.83030520988397,27.2196610168163,12.8412745629681));
#61392=CARTESIAN_POINT('Ctrl Pts',(-1.8060448615243,27.2308723673325,12.7545081592047));
#61393=CARTESIAN_POINT('Ctrl Pts',(-1.77577747562567,27.2420816866914,12.6698953588806));
#61394=CARTESIAN_POINT('Ctrl Pts',(-1.75287738960566,27.2505625769276,12.6058779239986));
#61395=CARTESIAN_POINT('Ctrl Pts',(-1.72668954665041,27.2591051415846,12.5430686690698));
#61396=CARTESIAN_POINT('Ctrl Pts',(-1.69724790405521,27.2676669113444,12.4818153629211));
#61397=CARTESIAN_POINT('Ctrl Pts',(-1.69724652292347,27.2676673129841,12.481812489478));
#61398=CARTESIAN_POINT('Ctrl Pts',(-1.69724514178453,27.2676677146238,12.4818096160383));
#61399=CARTESIAN_POINT('Ctrl Pts',(-1.69724376063839,27.2676681162635,12.4818067426021));
#61400=CARTESIAN_POINT('Ctrl Pts',(-1.66430207130025,27.2772476172591,12.4132724725238));
#61401=CARTESIAN_POINT('Ctrl Pts',(-1.62726066159056,27.2868384375968,12.3466995858302));
#61402=CARTESIAN_POINT('Ctrl Pts',(-1.58629098297827,27.2963888487984,12.2826368596186));
#61403=CARTESIAN_POINT('Ctrl Pts',(-1.57662795109612,27.298641390948,12.2675271446585));
#61404=CARTESIAN_POINT('Ctrl Pts',(-1.56674652444052,27.3008916571568,12.2525572529114));
#61405=CARTESIAN_POINT('Ctrl Pts',(-1.55664921499818,27.3031389170245,12.2377347113786));
#61406=CARTESIAN_POINT('Ctrl Pts',(-1.52072433105668,27.3111343687233,12.1849980801679));
#61407=CARTESIAN_POINT('Ctrl Pts',(-1.48206375949998,27.3190928728718,12.134121665641));
#61408=CARTESIAN_POINT('Ctrl Pts',(-1.44091793592416,27.3270608041123,12.0853539206243));
#61409=CARTESIAN_POINT('Ctrl Pts',(-1.44089965093364,27.3270643450196,12.0853322484914));
#61410=CARTESIAN_POINT('Ctrl Pts',(-1.44088136545198,27.3270678859289,12.0853105767744));
#61411=CARTESIAN_POINT('Ctrl Pts',(-1.44086307947923,27.3270714268401,12.0852889054732));
#61412=CARTESIAN_POINT('Ctrl Pts',(-1.37290541594973,27.340230806158,12.0047500678301));
#61413=CARTESIAN_POINT('Ctrl Pts',(-1.29814242898036,27.353423300194,11.9299261142695));
#61414=CARTESIAN_POINT('Ctrl Pts',(-1.2177183305258,27.3666107050185,11.8617505225983));
#61415=CARTESIAN_POINT('Ctrl Pts',(-1.171839339842,27.3741336345224,11.8228588546126));
#61416=CARTESIAN_POINT('Ctrl Pts',(-1.1241189340707,27.3816547985145,11.7861312188262));
#61417=CARTESIAN_POINT('Ctrl Pts',(-1.07477681256499,27.3891662459853,11.7517428934414));
#61418=CARTESIAN_POINT('Ctrl Pts',(-0.99956793163206,27.4006154407348,11.699327079317));
#61419=CARTESIAN_POINT('Ctrl Pts',(-0.920584331624732,27.4120420994908,
11.6523420033146));
#61420=CARTESIAN_POINT('Ctrl Pts',(-0.838579152359779,27.4234222755877,
11.6113921337498));
#61421=CARTESIAN_POINT('Ctrl Pts',(-0.794850714564251,27.4294906401351,
11.5895560272983));
#61422=CARTESIAN_POINT('Ctrl Pts',(-0.750262542867168,27.4355460182717,
11.5694357671497));
#61423=CARTESIAN_POINT('Ctrl Pts',(-0.704959621222531,27.4416147128761,
11.5510781899004));
#61424=CARTESIAN_POINT('Ctrl Pts',(-0.696050783088503,27.4428081241607,
11.5474681648003));
#61425=CARTESIAN_POINT('Ctrl Pts',(-0.687114326100849,27.4440021923229,
11.5439260602436));
#61426=CARTESIAN_POINT('Ctrl Pts',(-0.678150996518129,27.445196938178,11.5404524767586));
#61427=CARTESIAN_POINT('Ctrl Pts',(-0.652873478156679,27.4485662453099,
11.5306566113371));
#61428=CARTESIAN_POINT('Ctrl Pts',(-0.627382253185017,27.4519409421826,
11.5214056561756));
#61429=CARTESIAN_POINT('Ctrl Pts',(-0.601698775311904,27.455321496039,11.5127018755957));
#61430=CARTESIAN_POINT('Ctrl Pts',(-0.512785748786099,27.4670245557332,
11.4825704628098));
#61431=CARTESIAN_POINT('Ctrl Pts',(-0.421596875476661,27.478791232657,11.4590127255446));
#61432=CARTESIAN_POINT('Ctrl Pts',(-0.329148571622093,27.4905698807564,
11.4422447586241));
#61433=CARTESIAN_POINT('Ctrl Pts',(-0.26164332414904,27.4991705853848,11.4300008805929));
#61434=CARTESIAN_POINT('Ctrl Pts',(-0.193467731801849,27.5077775363492,
11.4213775047135));
#61435=CARTESIAN_POINT('Ctrl Pts',(-0.125034808865138,27.5163684720874,
11.416456530407));
#61436=CARTESIAN_POINT('Ctrl Pts',(-0.0519841159098541,27.5255391136717,
11.4112034947674));
#61437=CARTESIAN_POINT('Ctrl Pts',(0.0213678892687439,27.5346915349819,
11.4101692925342));
#61438=CARTESIAN_POINT('Ctrl Pts',(0.0945403155628665,27.5438002147465,
11.4134558015847));
#61439=CARTESIAN_POINT('Ctrl Pts',(0.144374619553393,27.5500037088676,11.4156940885923));
#61440=CARTESIAN_POINT('Ctrl Pts',(0.194126449213719,27.5561869384646,11.4199365452109));
#61441=CARTESIAN_POINT('Ctrl Pts',(0.243651158933981,27.5623809508564,11.4261604084152));
#61442=CARTESIAN_POINT('Ctrl Pts',(0.246929283648362,27.5627909430646,11.4265723764995));
#61443=CARTESIAN_POINT('Ctrl Pts',(0.250206368205759,27.5632009860023,11.4269930074509));
#61444=CARTESIAN_POINT('Ctrl Pts',(0.253482365585964,27.5636110783592,11.4274223086756));
#61445=CARTESIAN_POINT('Ctrl Pts',(0.295019741136255,27.5688107651305,11.4328655505729));
#61446=CARTESIAN_POINT('Ctrl Pts',(0.336382394805737,27.5740184062628,11.4397027942762));
#61447=CARTESIAN_POINT('Ctrl Pts',(0.377479965674802,27.5792312709867,11.4479033776284));
#61448=CARTESIAN_POINT('Ctrl Pts',(0.489172342174389,27.5933984647422,11.4701904039398));
#61449=CARTESIAN_POINT('Ctrl Pts',(0.59891405835899,27.6076025976756,11.5025514309844));
#61450=CARTESIAN_POINT('Ctrl Pts',(0.70498573918653,27.6218081421299,11.5443691488903));
#61451=CARTESIAN_POINT('Ctrl Pts',(0.80981178530218,27.6358468661932,11.5856957875506));
#61452=CARTESIAN_POINT('Ctrl Pts',(0.911053985636797,27.6498861793188,11.6362575654412));
#61453=CARTESIAN_POINT('Ctrl Pts',(1.00707860992282,27.6639253942448,11.6954416207046));
#61454=CARTESIAN_POINT('Ctrl Pts',(1.04156773713381,27.6689678536465,11.7166987349711));
#61455=CARTESIAN_POINT('Ctrl Pts',(1.07538405831602,27.6740108791178,11.73906822974));
#61456=CARTESIAN_POINT('Ctrl Pts',(1.10844854241686,27.6790679276367,11.7624938816867));
#61457=CARTESIAN_POINT('Ctrl Pts',(1.11475462243416,27.6800324112353,11.766961637336));
#61458=CARTESIAN_POINT('Ctrl Pts',(1.12103345404847,27.6809974777904,11.7714677574257));
#61459=CARTESIAN_POINT('Ctrl Pts',(1.1272846856579,27.6819631475066,11.7760121696997));
#61460=CARTESIAN_POINT('Ctrl Pts',(1.14385067003335,27.6845222063337,11.7880550226016));
#61461=CARTESIAN_POINT('Ctrl Pts',(1.16022285215818,27.6870855012016,11.8003667614323));
#61462=CARTESIAN_POINT('Ctrl Pts',(1.17639727375936,27.6896534044628,11.8129421599516));
#61463=CARTESIAN_POINT('Ctrl Pts',(1.24562276956801,27.7006438671096,11.8667640658569));
#61464=CARTESIAN_POINT('Ctrl Pts',(1.31119539583706,27.7117132341387,11.9253968527617));
#61465=CARTESIAN_POINT('Ctrl Pts',(1.3724868230913,27.7227907181938,11.9882690194109));
#61466=CARTESIAN_POINT('Ctrl Pts',(1.37686796078122,27.7235825415381,11.9927631490354));
#61467=CARTESIAN_POINT('Ctrl Pts',(1.38122721400554,27.724374403745,11.9972789200397));
#61468=CARTESIAN_POINT('Ctrl Pts',(1.38556434912975,27.7251662777597,12.0018161145392));
#61469=CARTESIAN_POINT('Ctrl Pts',(1.44325296611283,27.7356990639016,12.0621657389255));
#61470=CARTESIAN_POINT('Ctrl Pts',(1.49703119317074,27.7462334628006,12.1263084875048));
#61471=CARTESIAN_POINT('Ctrl Pts',(1.54636318879888,27.7566942978174,12.1937888134211));
#61472=CARTESIAN_POINT('Ctrl Pts',(1.55035953962408,27.7575417228226,12.1992553479232));
#61473=CARTESIAN_POINT('Ctrl Pts',(1.55432668879006,27.758388661677,12.2047437694752));
#61474=CARTESIAN_POINT('Ctrl Pts',(1.55826433952585,27.759235072631,12.2102538270502));
#61475=CARTESIAN_POINT('Ctrl Pts',(1.57774734208177,27.7634230079982,12.2375169016651));
#61476=CARTESIAN_POINT('Ctrl Pts',(1.59650875485946,27.7675980087701,12.2653106392325));
#61477=CARTESIAN_POINT('Ctrl Pts',(1.61451335491316,27.7717549888583,12.2936076191409));
#61478=CARTESIAN_POINT('Ctrl Pts',(1.61453750474986,27.7717605646772,12.2936455742991));
#61479=CARTESIAN_POINT('Ctrl Pts',(1.61456165322472,27.7717661404638,12.2936835303626));
#61480=CARTESIAN_POINT('Ctrl Pts',(1.61458580033765,27.7717717162178,12.2937214873314));
#61481=CARTESIAN_POINT('Ctrl Pts',(1.63439184598387,27.776345084453,12.3248547104929));
#61482=CARTESIAN_POINT('Ctrl Pts',(1.65327828751371,27.7808958585312,12.3565921302816));
#61483=CARTESIAN_POINT('Ctrl Pts',(1.67119768818825,27.7854193222409,12.3888748756123));
#61484=CARTESIAN_POINT('Ctrl Pts',(1.69193772409766,27.7906548098266,12.4262391440704));
#61485=CARTESIAN_POINT('Ctrl Pts',(1.71138267339757,27.7958536280428,12.4643344982101));
#61486=CARTESIAN_POINT('Ctrl Pts',(1.72950947559644,27.8010521028769,12.5030547640794));
#61487=CARTESIAN_POINT('Ctrl Pts',(1.72951799205781,27.8010545452609,12.5030729559063));
#61488=CARTESIAN_POINT('Ctrl Pts',(1.72952650822833,27.8010569876447,12.5030911478714));
#61489=CARTESIAN_POINT('Ctrl Pts',(1.729535024108,27.8010594300285,12.5031093399746));
#61490=CARTESIAN_POINT('Ctrl Pts',(1.75621161116458,27.8087103677144,12.5600973721866));
#61491=CARTESIAN_POINT('Ctrl Pts',(1.77999496964844,27.8163359500152,12.6184065650703));
#61492=CARTESIAN_POINT('Ctrl Pts',(1.80095447272991,27.8240478620407,12.6777061742592));
#61493=CARTESIAN_POINT('Ctrl Pts',(1.80661497184171,27.8261306056535,12.6937211238426));
#61494=CARTESIAN_POINT('Ctrl Pts',(1.81206954810936,27.8282196798225,12.7098086011334));
#61495=CARTESIAN_POINT('Ctrl Pts',(1.81731962540062,27.8303173594206,12.7259627345639));
#61496=CARTESIAN_POINT('Ctrl Pts',(1.84046907600862,27.839566771868,12.7971920314329));
#61497=CARTESIAN_POINT('Ctrl Pts',(1.85956826403524,27.8489060776057,12.8697755299982));
#61498=CARTESIAN_POINT('Ctrl Pts',(1.87443315079832,27.8582628805153,12.943311013621));
#61499=CARTESIAN_POINT('Ctrl Pts',(1.87540869087311,27.858876940774,12.9481369374464));
#61500=CARTESIAN_POINT('Ctrl Pts',(1.87636598086617,27.8594910744935,12.9529669484949));
#61501=CARTESIAN_POINT('Ctrl Pts',(1.87730496335598,27.8601052604144,12.9578009274768));
#61502=CARTESIAN_POINT('Ctrl Pts',(1.89250598473335,27.8700482076086,13.0360573578578));
#61503=CARTESIAN_POINT('Ctrl Pts',(1.90290822949596,27.8800048478456,13.1153542584566));
#61504=CARTESIAN_POINT('Ctrl Pts',(1.90835950198352,27.8899729257711,13.1950670158045));
#61505=CARTESIAN_POINT('Ctrl Pts',(1.91108513822731,27.8949569647339,13.2349233944784));
#61506=CARTESIAN_POINT('Ctrl Pts',(1.91257301511765,27.8999438549339,13.2748835851175));
#61507=CARTESIAN_POINT('Ctrl Pts',(1.91280547596267,27.9049323592216,13.3148614673998));
#61508=CARTESIAN_POINT('Ctrl Pts',(1.91295913350828,27.9082297804497,13.3412870070188));
#61509=CARTESIAN_POINT('Ctrl Pts',(1.91256431850402,27.9115279068385,13.3677202694795));
#61510=CARTESIAN_POINT('Ctrl Pts',(1.91161655319156,27.9148263801428,13.3941363756395));
#61511=CARTESIAN_POINT('Ctrl Pts',(1.91113049158358,27.9165180027598,13.4076838803519));
#61512=CARTESIAN_POINT('Ctrl Pts',(1.91049900939872,27.918209704164,13.4212267734741));
#61513=CARTESIAN_POINT('Ctrl Pts',(1.90972153695773,27.9199014734697,13.4347620038057));
#61514=CARTESIAN_POINT('Ctrl Pts',(1.90534923235206,27.9294155479715,13.5108806503292));
#61515=CARTESIAN_POINT('Ctrl Pts',(1.89634539771753,27.9389515961825,13.5869155167899));
#61516=CARTESIAN_POINT('Ctrl Pts',(1.88285252040647,27.9484938268728,13.6622095436909));
#61517=CARTESIAN_POINT('Ctrl Pts',(1.86935964309542,27.958036057563,13.7375035705918));
#61518=CARTESIAN_POINT('Ctrl Pts',(1.85138106885504,27.967584453052,13.8120563319306));
#61519=CARTESIAN_POINT('Ctrl Pts',(1.82908775889807,27.977133039192,13.8852948652974));
#61520=CARTESIAN_POINT('Ctrl Pts',(1.80844629276644,27.985974113837,13.9531067204656));
#61521=CARTESIAN_POINT('Ctrl Pts',(1.7842640395328,27.9949641707816,14.0197929648663));
#61522=CARTESIAN_POINT('Ctrl Pts',(1.75653947367986,28.0039968977633,14.0849877155301));
#61523=CARTESIAN_POINT('Ctrl Pts',(1.75454192988809,28.0046477021005,14.0896849710304));
#61524=CARTESIAN_POINT('Ctrl Pts',(1.75252599432901,28.0052987252934,14.0943744619669));
#61525=CARTESIAN_POINT('Ctrl Pts',(1.75049166532415,28.0059499263501,14.0990560412568));
#61526=CARTESIAN_POINT('Ctrl Pts',(1.72659336103571,28.0135999185435,14.1540529498948));
#61527=CARTESIAN_POINT('Ctrl Pts',(1.70009385182191,28.0212128584894,14.2079551069128));
#61528=CARTESIAN_POINT('Ctrl Pts',(1.67102796759327,28.0287744333106,14.2605321315749));
#61529=CARTESIAN_POINT('Ctrl Pts',(1.65532057049091,28.0328607586225,14.288945105298));
#61530=CARTESIAN_POINT('Ctrl Pts',(1.63886325653744,28.0369324130974,14.3169714922753));
#61531=CARTESIAN_POINT('Ctrl Pts',(1.62168131926052,28.0410046404417,14.3445726722918));
#61532=CARTESIAN_POINT('Ctrl Pts',(1.62166911426219,28.0410075331031,14.3445922784835));
#61533=CARTESIAN_POINT('Ctrl Pts',(1.62165690889821,28.0410104257649,14.3446118844608));
#61534=CARTESIAN_POINT('Ctrl Pts',(1.62164470316857,28.041013318427,14.3446314902236));
#61535=CARTESIAN_POINT('Ctrl Pts',(1.57267741401981,28.0526181814509,14.4232864403415));
#61536=CARTESIAN_POINT('Ctrl Pts',(1.51781046943814,28.0641401287839,14.4983839269083));
#61537=CARTESIAN_POINT('Ctrl Pts',(1.45777148584965,28.0756435782486,14.5692788341777));
#61538=CARTESIAN_POINT('Ctrl Pts',(1.39615710929978,28.0874488724854,14.6420339884272));
#61539=CARTESIAN_POINT('Ctrl Pts',(1.32909482450444,28.0992349137366,14.7103624156715));
#61540=CARTESIAN_POINT('Ctrl Pts',(1.25735647030735,28.1110433153804,14.7735405036232));
#61541=CARTESIAN_POINT('Ctrl Pts',(1.18543183367424,28.1228823798105,14.836882645633));
#61542=CARTESIAN_POINT('Ctrl Pts',(1.10880657100335,28.1347440652443,14.8950469721656));
#61543=CARTESIAN_POINT('Ctrl Pts',(1.02825283032043,28.1466399321335,14.9472888127912));
#61544=CARTESIAN_POINT('Ctrl Pts',(1.01730894768943,28.1482560826676,14.9543862929006));
#61545=CARTESIAN_POINT('Ctrl Pts',(1.0062925477142,28.1498728163086,14.9613744448076));
#61546=CARTESIAN_POINT('Ctrl Pts',(0.995205558188219,28.1514901164888,14.9682513895842));
#61547=CARTESIAN_POINT('Ctrl Pts',(0.972475805446326,28.1548057896136,14.9823500097756));
#61548=CARTESIAN_POINT('Ctrl Pts',(0.949449322592214,28.1581238419525,14.9959812758543));
#61549=CARTESIAN_POINT('Ctrl Pts',(0.926143163075408,28.1614500362462,15.0091338425473));
#61550=CARTESIAN_POINT('Ctrl Pts',(0.926131693837206,28.1614516731059,15.0091403150817));
#61551=CARTESIAN_POINT('Ctrl Pts',(0.926120224530382,28.1614533099669,15.0091467874999));
#61552=CARTESIAN_POINT('Ctrl Pts',(0.926108755154938,28.161454946829,15.0091532598019));
#61553=CARTESIAN_POINT('Ctrl Pts',(0.837659685175365,28.1740780344321,15.0590660989367));
#61554=CARTESIAN_POINT('Ctrl Pts',(0.745127032716431,28.186771118259,15.1020652714529));
#61555=CARTESIAN_POINT('Ctrl Pts',(0.649704821666005,28.1994902401537,15.1377317143075));
#61556=CARTESIAN_POINT('Ctrl Pts',(0.553321727077857,28.2123374411895,15.1737573114659));
#61557=CARTESIAN_POINT('Ctrl Pts',(0.453993920957942,28.225215802371,15.2023068048996));
#61558=CARTESIAN_POINT('Ctrl Pts',(0.352925350219839,28.2380928432519,15.2229791730088));
#61559=CARTESIAN_POINT('Ctrl Pts',(0.254602793423587,28.2506200173688,15.2430898767882));
#61560=CARTESIAN_POINT('Ctrl Pts',(0.154632426084098,28.2631457303804,15.2557469701838));
#61561=CARTESIAN_POINT('Ctrl Pts',(0.0541040691992433,28.2756669717454,
15.2605928269564));
#61562=CARTESIAN_POINT('Ctrl Pts',(0.0327897991787413,28.2783217562034,
15.2616202574539));
#61563=CARTESIAN_POINT('Ctrl Pts',(0.0114516579271045,28.2809803578895,
15.2622993252151));
#61564=CARTESIAN_POINT('Ctrl Pts',(-0.00989862692612825,28.2836444589833,
15.2626278963491));
#61565=CARTESIAN_POINT('Ctrl Pts',(-0.00991502536138304,28.2836465051897,
15.2626281487136));
#61566=CARTESIAN_POINT('Ctrl Pts',(-0.00993142380461405,28.2836485513966,
15.2626284008693));
#61567=CARTESIAN_POINT('Ctrl Pts',(-0.00994782225579749,28.2836505976039,
15.2626286528162));
#61568=CARTESIAN_POINT('Ctrl Pts',(-0.0919646539396332,28.2938847010688,
15.263888765243));
#61569=CARTESIAN_POINT('Ctrl Pts',(-0.174180657339046,28.3041311546817,
15.2599274400423));
#61570=CARTESIAN_POINT('Ctrl Pts',(-0.255920339664015,28.3143906605047,
15.2508700293366));
#61571=CARTESIAN_POINT('Ctrl Pts',(-0.33765847038126,28.3246499715787,15.2418127905616));
#61572=CARTESIAN_POINT('Ctrl Pts',(-0.418920429682987,28.3349223484336,
15.2276597501592));
#61573=CARTESIAN_POINT('Ctrl Pts',(-0.499103565974076,28.3452080191226,
15.2084815967412));
#61574=CARTESIAN_POINT('Ctrl Pts',(-0.600206827742772,28.3581772655781,
15.184299780527));
#61575=CARTESIAN_POINT('Ctrl Pts',(-0.699603445862627,28.3711687987847,
15.1521250292407));
#61576=CARTESIAN_POINT('Ctrl Pts',(-0.795994742605581,28.3841800605095,
15.1122879210286));
#61577=CARTESIAN_POINT('Ctrl Pts',(-0.852489506494473,28.3918059373664,
15.0889394642851));
#61578=CARTESIAN_POINT('Ctrl Pts',(-0.907953474039107,28.3994387680334,
15.0629590072487));
#61579=CARTESIAN_POINT('Ctrl Pts',(-0.962136588998806,28.407079578439,15.0344083837009));
#61580=CARTESIAN_POINT('Ctrl Pts',(-1.12646005194889,28.4302521927586,14.9478216798126));
#61581=CARTESIAN_POINT('Ctrl Pts',(-1.27897078824977,28.4534938027453,14.8376104886566));
#61582=CARTESIAN_POINT('Ctrl Pts',(-1.41393887862166,28.4768086286541,14.7083454242204));
#61583=CARTESIAN_POINT('Ctrl Pts',(-1.50240492763019,28.4920905410364,14.6236174748659));
#61584=CARTESIAN_POINT('Ctrl Pts',(-1.58333431865573,28.5074039430096,14.5307032225104));
#61585=CARTESIAN_POINT('Ctrl Pts',(-1.65511262555103,28.5227498647524,14.4308907336903));
#61586=CARTESIAN_POINT('Ctrl Pts',(-1.66926241111438,28.5257750336554,14.4112145198809));
#61587=CARTESIAN_POINT('Ctrl Pts',(-1.68305657838302,28.5288014662315,14.3912702361043));
#61588=CARTESIAN_POINT('Ctrl Pts',(-1.69648276036997,28.5318291698286,14.3710677556957));
#61589=CARTESIAN_POINT('Ctrl Pts',(-1.77787575643723,28.5501838939946,14.2485950817777));
#61590=CARTESIAN_POINT('Ctrl Pts',(-1.84575323579243,28.5685876070242,14.1166170873232));
#61591=CARTESIAN_POINT('Ctrl Pts',(-1.89879251057137,28.587038324042,13.9785079438035));
#61592=CARTESIAN_POINT('Ctrl Pts',(-1.95222788591733,28.6056268321495,13.8393673927035));
#61593=CARTESIAN_POINT('Ctrl Pts',(-1.99060677787332,28.6242664220067,13.6940061019775));
#61594=CARTESIAN_POINT('Ctrl Pts',(-2.01260790568954,28.6429812057999,13.5458408356626));
#61595=CARTESIAN_POINT('Ctrl Pts',(-2.0180160388561,28.647581517374,13.5094200895271));
#61596=CARTESIAN_POINT('Ctrl Pts',(-2.02243389469254,28.6521848475788,13.4728291848583));
#61597=CARTESIAN_POINT('Ctrl Pts',(-2.02584159212891,28.6567913464262,13.4361185882898));
#61598=CARTESIAN_POINT('Ctrl Pts',(-2.02615949296527,28.6572210823002,13.4326938918282));
#61599=CARTESIAN_POINT('Ctrl Pts',(-2.02646860250647,28.6576508458103,13.4292681536581));
#61600=CARTESIAN_POINT('Ctrl Pts',(-2.02676890775793,28.6580806444262,13.4258414188437));
#61601=CARTESIAN_POINT('Ctrl Pts',(-2.02677007512464,28.6580823151682,13.4258280982103));
#61602=CARTESIAN_POINT('Ctrl Pts',(-2.02677124235842,28.658083985911,13.4258147775617));
#61603=CARTESIAN_POINT('Ctrl Pts',(-2.02677240945925,28.6580856566545,13.425801456898));
#61604=CARTESIAN_POINT('Ctrl Pts',(-2.0405316559978,28.677782473794,13.2687607875455));
#61605=CARTESIAN_POINT('Ctrl Pts',(-2.03580963395929,28.6975830887113,13.1096130060237));
#61606=CARTESIAN_POINT('Ctrl Pts',(-2.01300737612442,28.7174335268602,12.9526738600431));
#61607=CARTESIAN_POINT('Ctrl Pts',(-1.98997249743873,28.7374864724032,12.7941336744667));
#61608=CARTESIAN_POINT('Ctrl Pts',(-1.94849435885256,28.7575884801872,12.6378473421967));
#61609=CARTESIAN_POINT('Ctrl Pts',(-1.8889688971964,28.7776882004441,12.488165435839));
#61610=CARTESIAN_POINT('Ctrl Pts',(-1.88062290443526,28.7805063578359,12.4671787173462));
#61611=CARTESIAN_POINT('Ctrl Pts',(-1.87192198593172,28.7833245038566,12.446321690604));
#61612=CARTESIAN_POINT('Ctrl Pts',(-1.86286706311752,28.7861425377394,12.4256062236929));
#61613=CARTESIAN_POINT('Ctrl Pts',(-1.86286080290841,28.7861444860145,12.425591901853));
#61614=CARTESIAN_POINT('Ctrl Pts',(-1.86285454253086,28.7861464342897,12.4255775800823));
#61615=CARTESIAN_POINT('Ctrl Pts',(-1.86284828198488,28.7861483825649,12.4255632583808));
#61616=CARTESIAN_POINT('Ctrl Pts',(-1.86181575438794,28.786469704041,12.4232012356302));
#61617=CARTESIAN_POINT('Ctrl Pts',(-1.86077864520166,28.7867910253279,12.4208410947962));
#61618=CARTESIAN_POINT('Ctrl Pts',(-1.8597369631722,28.7871123432515,12.4184828489633));
#61619=CARTESIAN_POINT('Ctrl Pts',(-1.81231342527778,28.8017406389244,12.3111215261644));
#61620=CARTESIAN_POINT('Ctrl Pts',(-1.75541341869991,28.8163628134929,12.2076790811907));
#61621=CARTESIAN_POINT('Ctrl Pts',(-1.69002467064595,28.831029030168,12.1094970535507));
#61622=CARTESIAN_POINT('Ctrl Pts',(-1.62433393102225,28.8457629813377,12.0108615817705));
#61623=CARTESIAN_POINT('Ctrl Pts',(-1.55007153298118,28.8605420587782,11.9175376889213));
#61624=CARTESIAN_POINT('Ctrl Pts',(-1.46826629077973,28.8754003434675,11.8309726423896));
#61625=CARTESIAN_POINT('Ctrl Pts',(-1.39497406680941,28.8887124088064,11.7534159405492));
#61626=CARTESIAN_POINT('Ctrl Pts',(-1.31562661124625,28.9020881303713,11.6812880245723));
#61627=CARTESIAN_POINT('Ctrl Pts',(-1.23101598506768,28.9155342832238,11.61565552247));
#61628=CARTESIAN_POINT('Ctrl Pts',(-1.23099796339198,28.9155371471927,11.6156415430478));
#61629=CARTESIAN_POINT('Ctrl Pts',(-1.23097994147602,28.9155400111662,11.6156275639185));
#61630=CARTESIAN_POINT('Ctrl Pts',(-1.23096191931979,28.9155428751441,11.6156135850821));
#61631=CARTESIAN_POINT('Ctrl Pts',(-1.14884577065289,28.9285923035583,11.5519204181195));
#61632=CARTESIAN_POINT('Ctrl Pts',(-1.06173893290582,28.9417352560574,11.4943088010887));
#61633=CARTESIAN_POINT('Ctrl Pts',(-0.970673823222862,28.9548248633794,
11.4433545033137));
#61634=CARTESIAN_POINT('Ctrl Pts',(-0.950609266581978,28.9577089225809,
11.4321276415951));
#61635=CARTESIAN_POINT('Ctrl Pts',(-0.9303517397105,28.9605905530007,11.4212233990956));
#61636=CARTESIAN_POINT('Ctrl Pts',(-0.90991081640154,28.9634684850355,11.4106471890954));
#61637=CARTESIAN_POINT('Ctrl Pts',(-0.818131349886293,28.9763903605709,
11.3631601506239));
#61638=CARTESIAN_POINT('Ctrl Pts',(-0.722640356060095,28.9892385982485,
11.322277457506));
#61639=CARTESIAN_POINT('Ctrl Pts',(-0.624423301925256,29.0021044649047,
11.2885101519301));
#61640=CARTESIAN_POINT('Ctrl Pts',(-0.539660016265759,29.0132079656179,
11.2593682906343));
#61641=CARTESIAN_POINT('Ctrl Pts',(-0.452864400020062,29.0243256761542,
11.2355310152117));
#61642=CARTESIAN_POINT('Ctrl Pts',(-0.364792165622707,29.0355025217288,
11.2173494433471));
#61643=CARTESIAN_POINT('Ctrl Pts',(-0.350519914334075,29.0373137480449,
11.2144030895472));
#61644=CARTESIAN_POINT('Ctrl Pts',(-0.336214152551724,29.0391265288975,
11.2116051485266));
#61645=CARTESIAN_POINT('Ctrl Pts',(-0.321878107417712,29.0409410572737,
11.2089569848025));
#61646=CARTESIAN_POINT('Ctrl Pts',(-0.306478186558829,29.0428902415243,
11.2061123012519));
#61647=CARTESIAN_POINT('Ctrl Pts',(-0.291043687766917,29.0448413775742,
11.2034405256956));
#61648=CARTESIAN_POINT('Ctrl Pts',(-0.275579005610156,29.0467946305441,
11.2009433363203));
#61649=CARTESIAN_POINT('Ctrl Pts',(-0.275570523676965,29.0467957018472,
11.2009419666838));
#61650=CARTESIAN_POINT('Ctrl Pts',(-0.275562041733366,29.0467967731509,
11.2009405970996));
#61651=CARTESIAN_POINT('Ctrl Pts',(-0.27555355977936,29.0467978444553,11.2009392275678));
#61652=CARTESIAN_POINT('Ctrl Pts',(-0.174162714297345,29.0596039102395,
11.1845682365639));
#61653=CARTESIAN_POINT('Ctrl Pts',(-0.0712833547055921,29.0725078447394,
11.1756792523032));
#61654=CARTESIAN_POINT('Ctrl Pts',(0.0319050888017752,29.0854479062699,
11.1742525038087));
#61655=CARTESIAN_POINT('Ctrl Pts',(0.0563634941319289,29.0885150449838,
11.1739143264722));
#61656=CARTESIAN_POINT('Ctrl Pts',(0.0808392051649467,29.0915842082012,
11.1739951662006));
#61657=CARTESIAN_POINT('Ctrl Pts',(0.105316439168227,29.0946545643595,11.1744943403296));
#61658=CARTESIAN_POINT('Ctrl Pts',(0.215803238224659,29.1085137211518,11.1767475422921));
#61659=CARTESIAN_POINT('Ctrl Pts',(0.326326071542987,29.1223966823686,11.187520012059));
#61660=CARTESIAN_POINT('Ctrl Pts',(0.4356269082667,29.1362579642596,11.2067721272977));
#61661=CARTESIAN_POINT('Ctrl Pts',(0.44531767414695,29.1374869250034,11.2084790469067));
#61662=CARTESIAN_POINT('Ctrl Pts',(0.454998828002351,29.1387157148839,11.2102526570044));
#61663=CARTESIAN_POINT('Ctrl Pts',(0.464669488559821,29.1399443019515,11.2120929492527));
#61664=CARTESIAN_POINT('Ctrl Pts',(0.472045000348972,29.1408813070657,11.2134964828678));
#61665=CARTESIAN_POINT('Ctrl Pts',(0.479414478883609,29.1418182095507,11.2149388151259));
#61666=CARTESIAN_POINT('Ctrl Pts',(0.486777559710844,29.1427550015008,11.2164199509909));
#61667=CARTESIAN_POINT('Ctrl Pts',(0.584925682586,29.1552422162397,11.2361631411435));
#61668=CARTESIAN_POINT('Ctrl Pts',(0.681953371103919,29.1677125483654,11.2628089358605));
#61669=CARTESIAN_POINT('Ctrl Pts',(0.776769474478284,29.18024255482,11.2962806128029));
#61670=CARTESIAN_POINT('Ctrl Pts',(0.776795505175567,29.1802459947927,11.2962898020762));
#61671=CARTESIAN_POINT('Ctrl Pts',(0.776821535712201,29.18024943477,11.2962989918659));
#61672=CARTESIAN_POINT('Ctrl Pts',(0.776847566088163,29.1802528747521,11.2963081821719));
#61673=CARTESIAN_POINT('Ctrl Pts',(0.880974325285057,29.1940134976104,11.3330712617267));
#61674=CARTESIAN_POINT('Ctrl Pts',(0.982528966870906,29.2078494488345,11.3781009897652));
#61675=CARTESIAN_POINT('Ctrl Pts',(1.08027920797818,29.221732415313,11.4307123916727));
#61676=CARTESIAN_POINT('Ctrl Pts',(1.10566362016273,29.2253376334633,11.444374859371));
#61677=CARTESIAN_POINT('Ctrl Pts',(1.13079156032285,29.2289460195216,11.4585483521387));
#61678=CARTESIAN_POINT('Ctrl Pts',(1.15564167179722,29.2325570721909,11.4732203485793));
#61679=CARTESIAN_POINT('Ctrl Pts',(1.26785552218459,29.248863241457,11.5394736213333));
#61680=CARTESIAN_POINT('Ctrl Pts',(1.37440664919206,29.2652229399408,11.6158899316168));
#61681=CARTESIAN_POINT('Ctrl Pts',(1.47348562479979,29.2816050850296,11.7014171741355));
#61682=CARTESIAN_POINT('Ctrl Pts',(1.54227988610125,29.2929798248571,11.7608019571748));
#61683=CARTESIAN_POINT('Ctrl Pts',(1.60747602190586,29.3043656634369,11.8245805288282));
#61684=CARTESIAN_POINT('Ctrl Pts',(1.6684943777618,29.3157601683119,11.8924550823692));
#61685=CARTESIAN_POINT('Ctrl Pts',(1.66853645781051,29.3157680262969,11.892501890653));
#61686=CARTESIAN_POINT('Ctrl Pts',(1.66857853581567,29.3157758843017,11.8925487008194));
#61687=CARTESIAN_POINT('Ctrl Pts',(1.66862061177711,29.3157837423264,11.8925955128682));
#61688=CARTESIAN_POINT('Ctrl Pts',(1.68689026181752,29.3191957466442,11.9129216021676));
#61689=CARTESIAN_POINT('Ctrl Pts',(1.70477463383708,29.3226115033997,11.9336025645071));
#61690=CARTESIAN_POINT('Ctrl Pts',(1.7222669118597,29.3260292758585,11.9546242986192));
#61691=CARTESIAN_POINT('Ctrl Pts',(1.77994411232085,29.3372986798196,12.023939156916));
#61692=CARTESIAN_POINT('Ctrl Pts',(1.83336850913228,29.3485911700184,12.0969651193588));
#61693=CARTESIAN_POINT('Ctrl Pts',(1.88224583463627,29.3599118637564,12.1731883821223));
#61694=CARTESIAN_POINT('Ctrl Pts',(1.88636797421079,29.3608666107519,12.1796167806629));
#61695=CARTESIAN_POINT('Ctrl Pts',(1.89045774741834,29.3618215584311,12.1860679385147));
#61696=CARTESIAN_POINT('Ctrl Pts',(1.8945149637451,29.3627767099103,12.1925415568821));
#61697=CARTESIAN_POINT('Ctrl Pts',(1.94704272883048,29.3751428172315,12.2763538748526));
#61698=CARTESIAN_POINT('Ctrl Pts',(1.99411367278242,29.3875433734691,12.363931434955));
#61699=CARTESIAN_POINT('Ctrl Pts',(2.03523714538344,29.3999686153529,12.4545081593452));
#61700=CARTESIAN_POINT('Ctrl Pts',(2.07322751764787,29.4114472073779,12.5381840568421));
#61701=CARTESIAN_POINT('Ctrl Pts',(2.10613781564245,29.4229469985678,12.624420666633));
#61702=CARTESIAN_POINT('Ctrl Pts',(2.13355885314394,29.4344446947496,12.7125039212252));
#61703=CARTESIAN_POINT('Ctrl Pts',(2.13583932206719,29.4354008999563,12.7198293597592));
#61704=CARTESIAN_POINT('Ctrl Pts',(2.13808185278511,29.436357090538,12.7271675592712));
#61705=CARTESIAN_POINT('Ctrl Pts',(2.14028622537885,29.4373132530233,12.7345181035168));
#61706=CARTESIAN_POINT('Ctrl Pts',(2.15252451656922,29.4426216999495,12.7753270398734));
#61707=CARTESIAN_POINT('Ctrl Pts',(2.16358586192327,29.4479290261542,12.8165149793703));
#61708=CARTESIAN_POINT('Ctrl Pts',(2.17343309975439,29.4532317761385,12.8580033371832));
#61709=CARTESIAN_POINT('Ctrl Pts',(2.17343821350038,29.4532345298972,12.858024882405));
#61710=CARTESIAN_POINT('Ctrl Pts',(2.17344332691904,29.4532372836546,12.8580464277078));
#61711=CARTESIAN_POINT('Ctrl Pts',(2.17344844001037,29.4532400374108,12.8580679730916));
#61712=CARTESIAN_POINT('Ctrl Pts',(2.19411109386932,29.4643683172111,12.9451356155083));
#61713=CARTESIAN_POINT('Ctrl Pts',(2.20947493606372,29.475510217651,13.0337400666774));
#61714=CARTESIAN_POINT('Ctrl Pts',(2.21947125049892,29.4866669450407,13.1231108473052));
#61715=CARTESIAN_POINT('Ctrl Pts',(2.22148929070966,29.4889192475907,13.1411528797103));
#61716=CARTESIAN_POINT('Ctrl Pts',(2.22328874345907,29.4911721539522,13.1592261051922));
#61717=CARTESIAN_POINT('Ctrl Pts',(2.22486929541162,29.4934256733204,13.1773241399873));
#61718=CARTESIAN_POINT('Ctrl Pts',(2.23428776598476,29.5068543403262,13.2851698883503));
#61719=CARTESIAN_POINT('Ctrl Pts',(2.23593228547602,29.5203046621321,13.3938963078404));
#61720=CARTESIAN_POINT('Ctrl Pts',(2.22976674229424,29.5338006156728,13.5023174068447));
#61721=CARTESIAN_POINT('Ctrl Pts',(2.22414927678059,29.5460968645763,13.6011005580855));
#61722=CARTESIAN_POINT('Ctrl Pts',(2.21205384164696,29.5584310899797,13.6996317595469));
#61723=CARTESIAN_POINT('Ctrl Pts',(2.19342580677518,29.5708383222901,13.7971348227835));
#61724=CARTESIAN_POINT('Ctrl Pts',(2.19206135353893,29.5717471185424,13.80427665879));
#61725=CARTESIAN_POINT('Ctrl Pts',(2.19066182866396,29.572656306571,13.8114129765725));
#61726=CARTESIAN_POINT('Ctrl Pts',(2.18922719967663,29.5735659001798,13.8185434696397));
#61727=CARTESIAN_POINT('Ctrl Pts',(2.179380513441,29.5798089657715,13.8674841564362));
#61728=CARTESIAN_POINT('Ctrl Pts',(2.16788022758423,29.586071426847,13.9161525834398));
#61729=CARTESIAN_POINT('Ctrl Pts',(2.15471003642721,29.5923592074735,13.964458986641));
#61730=CARTESIAN_POINT('Ctrl Pts',(2.15468671042886,29.592370343892,13.9645445431123));
#61731=CARTESIAN_POINT('Ctrl Pts',(2.15466337925621,29.5923814803489,13.9646300982071));
#61732=CARTESIAN_POINT('Ctrl Pts',(2.15464004290921,29.5923926168443,13.964715651925));
#61733=CARTESIAN_POINT('Ctrl Pts',(2.14403590146766,29.5974530906289,14.0035916476497));
#61734=CARTESIAN_POINT('Ctrl Pts',(2.13236371009766,29.6025215008339,14.0421834073582));
#61735=CARTESIAN_POINT('Ctrl Pts',(2.11964678076267,29.6075987803237,14.0804583158383));
#61736=CARTESIAN_POINT('Ctrl Pts',(2.08780168468648,29.6203130487528,14.1763044203301));
#61737=CARTESIAN_POINT('Ctrl Pts',(2.04939393621146,29.6330888116124,14.2702042051983));
#61738=CARTESIAN_POINT('Ctrl Pts',(2.00478346581371,29.6459139074135,14.3614182861861));
#61739=CARTESIAN_POINT('Ctrl Pts',(1.97944178986073,29.6531994038218,14.413233872575));
#61740=CARTESIAN_POINT('Ctrl Pts',(1.95209761230748,29.6605008231038,14.4641824559238));
#61741=CARTESIAN_POINT('Ctrl Pts',(1.92281048669964,29.6678159670389,14.5141246144164));
#61742=CARTESIAN_POINT('Ctrl Pts',(1.87765301719436,29.6790951001842,14.5911298326601));
#61743=CARTESIAN_POINT('Ctrl Pts',(1.82787363930548,29.6904059116434,14.6657363662634));
#61744=CARTESIAN_POINT('Ctrl Pts',(1.7737969730373,29.7017162772042,14.7372854931457));
#61745=CARTESIAN_POINT('Ctrl Pts',(1.73439595654646,29.7099571679753,14.7894171891755));
#61746=CARTESIAN_POINT('Ctrl Pts',(1.69271464849936,29.7181978182467,14.8399260823175));
#61747=CARTESIAN_POINT('Ctrl Pts',(1.64889283119282,29.7264257544821,14.8885675303056));
#61748=CARTESIAN_POINT('Ctrl Pts',(1.63254870314928,29.7294945099932,14.9067092255388));
#61749=CARTESIAN_POINT('Ctrl Pts',(1.61590806306995,29.7325612921836,14.9245899635758));
#61750=CARTESIAN_POINT('Ctrl Pts',(1.59898001760933,29.7356252411689,14.9421962435881));
#61751=CARTESIAN_POINT('Ctrl Pts',(1.59893601614321,29.7356332053634,14.9422420080052));
#61752=CARTESIAN_POINT('Ctrl Pts',(1.59889201273545,29.7356411695389,14.9422877705682));
#61753=CARTESIAN_POINT('Ctrl Pts',(1.59884800738628,29.7356491336951,14.9423335312769));
#61754=CARTESIAN_POINT('Ctrl Pts',(1.53854824913323,29.7465622773449,15.0050386278986));
#61755=CARTESIAN_POINT('Ctrl Pts',(1.47443051445554,29.7573805351958,15.0644453439063));
#61756=CARTESIAN_POINT('Ctrl Pts',(1.40702016816517,29.7681437325686,15.1201383185971));
#61757=CARTESIAN_POINT('Ctrl Pts',(1.33888074946686,29.7790233386331,15.1764336371919));
#61758=CARTESIAN_POINT('Ctrl Pts',(1.2673791377501,29.7898466507777,15.2289354518161));
#61759=CARTESIAN_POINT('Ctrl Pts',(1.19303629151063,29.8006646111447,15.2772718656253));
#61760=CARTESIAN_POINT('Ctrl Pts',(1.11892238419049,29.8114492575847,15.3254594273673));
#61761=CARTESIAN_POINT('Ctrl Pts',(1.04198600371556,29.8222286282337,15.36950892309));
#61762=CARTESIAN_POINT('Ctrl Pts',(0.962697131488878,29.8330627782369,15.4090874366371));
#61763=CARTESIAN_POINT('Ctrl Pts',(0.885176571317848,29.843655303438,15.4477832643711));
#61764=CARTESIAN_POINT('Ctrl Pts',(0.805407622756845,29.8543003069106,15.4822072937904));
#61765=CARTESIAN_POINT('Ctrl Pts',(0.723775978306456,29.8650757003008,15.512051919412));
#61766=CARTESIAN_POINT('Ctrl Pts',(0.69185218421878,29.8692896475037,15.5237232962338));
#61767=CARTESIAN_POINT('Ctrl Pts',(0.65964519270811,29.873535660542,15.5346917884168));
#61768=CARTESIAN_POINT('Ctrl Pts',(0.627169428730706,29.8777866196656,15.5449446896347));
#61769=CARTESIAN_POINT('Ctrl Pts',(0.627104324720616,29.8777951415432,15.5449652435772));
#61770=CARTESIAN_POINT('Ctrl Pts',(0.627039219745971,29.8778036634256,15.5449857946067));
#61771=CARTESIAN_POINT('Ctrl Pts',(0.626974113806956,29.8778121853127,15.5450063427231));
#61772=CARTESIAN_POINT('Ctrl Pts',(0.573993027685789,29.8847470186868,15.5617277285364));
#61773=CARTESIAN_POINT('Ctrl Pts',(0.520373373533641,29.8916850888289,15.5765205850681));
#61774=CARTESIAN_POINT('Ctrl Pts',(0.46624416580409,29.8986948306155,15.5893696321012));
#61775=CARTESIAN_POINT('Ctrl Pts',(0.373543369291603,29.9106995998375,15.6113747000555));
#61776=CARTESIAN_POINT('Ctrl Pts',(0.279317216943743,29.922860064562,15.6276972133245));
#61777=CARTESIAN_POINT('Ctrl Pts',(0.184173410113904,29.9351243913809,15.6382729149402));
#61778=CARTESIAN_POINT('Ctrl Pts',(0.172193152097602,29.9366686831702,15.6396045794834));
#61779=CARTESIAN_POINT('Ctrl Pts',(0.160198331622726,29.938214622535,15.640845060734));
#61780=CARTESIAN_POINT('Ctrl Pts',(0.148190153236795,29.9397621067286,15.6419941724037));
#61781=CARTESIAN_POINT('Ctrl Pts',(0.0353352487810282,29.9543056265862,
15.6527937194724));
#61782=CARTESIAN_POINT('Ctrl Pts',(-0.0787020464481159,29.9689850838153,
15.6555199105086));
#61783=CARTESIAN_POINT('Ctrl Pts',(-0.192666393973396,29.9836868481843,
15.650006965307));
#61784=CARTESIAN_POINT('Ctrl Pts',(-0.275518477501743,29.9943750312519,
15.6459990540062));
#61785=CARTESIAN_POINT('Ctrl Pts',(-0.358329908898737,30.005074367007,15.6376341430243));
#61786=CARTESIAN_POINT('Ctrl Pts',(-0.440525514520615,30.0157305485564,
15.6248862161416));
#61787=CARTESIAN_POINT('Ctrl Pts',(-0.464990701058588,30.0189023175022,
15.6210918477347));
#61788=CARTESIAN_POINT('Ctrl Pts',(-0.48940139016687,30.0220702645024,15.6169095178364));
#61789=CARTESIAN_POINT('Ctrl Pts',(-0.513742625389251,30.0252329608739,
15.6123394160239));
#61790=CARTESIAN_POINT('Ctrl Pts',(-0.519998017753285,30.0260457342007,
15.6111649571388));
#61791=CARTESIAN_POINT('Ctrl Pts',(-0.526248767278081,30.0268581564716,
15.6099649008537));
#61792=CARTESIAN_POINT('Ctrl Pts',(-0.532494600244034,30.0276702019342,
15.6087392602533));
#61793=CARTESIAN_POINT('Ctrl Pts',(-0.532607167216087,30.0276848372118,
15.6087171708616));
#61794=CARTESIAN_POINT('Ctrl Pts',(-0.532719732591162,30.0276994723669,
15.6086950731596));
#61795=CARTESIAN_POINT('Ctrl Pts',(-0.532832296367725,30.0277141073995,
15.6086729671481));
#61796=CARTESIAN_POINT('Ctrl Pts',(-0.629575186013529,30.0402921799077,
15.5896739650215));
#61797=CARTESIAN_POINT('Ctrl Pts',(-0.725421815311289,30.0527048234065,
15.564499656116));
#61798=CARTESIAN_POINT('Ctrl Pts',(-0.819553158172979,30.0650012028476,
15.533430181105));
#61799=CARTESIAN_POINT('Ctrl Pts',(-0.912430194723611,30.0771337322269,
15.5027747088842));
#61800=CARTESIAN_POINT('Ctrl Pts',(-1.00363754468808,30.0891532520328,15.4663824189752));
#61801=CARTESIAN_POINT('Ctrl Pts',(-1.09244306912936,30.101118142086,15.4245300478977));
#61802=CARTESIAN_POINT('Ctrl Pts',(-1.18304757425361,30.1133254112728,15.3818298511069));
#61803=CARTESIAN_POINT('Ctrl Pts',(-1.27115286095415,30.1254759916691,15.3334481546789));
#61804=CARTESIAN_POINT('Ctrl Pts',(-1.35603062313171,30.1376409804006,15.2796540167812));
#61805=CARTESIAN_POINT('Ctrl Pts',(-1.44090489737409,30.1498054692285,15.2258620894798));
#61806=CARTESIAN_POINT('Ctrl Pts',(-1.52255382815821,30.1619846397928,15.1666596796856));
#61807=CARTESIAN_POINT('Ctrl Pts',(-1.60027633593227,30.1742551659115,15.1022643792663));
#61808=CARTESIAN_POINT('Ctrl Pts',(-1.60027952996336,30.1742556701727,15.102261732921));
#61809=CARTESIAN_POINT('Ctrl Pts',(-1.60028272398781,30.174256174434,15.1022590865669));
#61810=CARTESIAN_POINT('Ctrl Pts',(-1.60028591800562,30.1742566786955,15.1022564402041));
#61811=CARTESIAN_POINT('Ctrl Pts',(-1.6556121130327,30.1829914040227,15.0564166251924));
#61812=CARTESIAN_POINT('Ctrl Pts',(-1.7088727262563,30.1917573173011,15.0080094863337));
#61813=CARTESIAN_POINT('Ctrl Pts',(-1.7599234820375,30.2006017288594,14.9572220375249));
#61814=CARTESIAN_POINT('Ctrl Pts',(-1.8738210369486,30.2203341860134,14.8439119375866));
#61815=CARTESIAN_POINT('Ctrl Pts',(-1.9767798244198,30.2404668949515,14.7186852514332));
#61816=CARTESIAN_POINT('Ctrl Pts',(-2.06678104296929,30.2607837065916,14.583998713918));
#61817=CARTESIAN_POINT('Ctrl Pts',(-2.0791973003519,30.2635865437819,14.5654178242066));
#61818=CARTESIAN_POINT('Ctrl Pts',(-2.0913668989552,30.2663928935877,14.5466568306674));
#61819=CARTESIAN_POINT('Ctrl Pts',(-2.10328448339727,30.2692021972246,14.5277221222004));
#61820=CARTESIAN_POINT('Ctrl Pts',(-2.15511224181361,30.2814194305838,14.4453779608576));
#61821=CARTESIAN_POINT('Ctrl Pts',(-2.20216501934561,30.2936897390157,14.3597551774029));
#61822=CARTESIAN_POINT('Ctrl Pts',(-2.24395841450402,30.3059607202294,14.2714967638777));
#61823=CARTESIAN_POINT('Ctrl Pts',(-2.26596138977105,30.3124210256228,14.2250313431445));
#61824=CARTESIAN_POINT('Ctrl Pts',(-2.28650738014192,30.3188815253586,14.1778357860376));
#61825=CARTESIAN_POINT('Ctrl Pts',(-2.30553125367308,30.3253346297916,14.130005746823));
#61826=CARTESIAN_POINT('Ctrl Pts',(-2.30553533391181,30.3253360138529,14.1299954882403));
#61827=CARTESIAN_POINT('Ctrl Pts',(-2.30553941408055,30.3253373979138,14.1299852296285));
#61828=CARTESIAN_POINT('Ctrl Pts',(-2.30554349417927,30.3253387819744,14.1299749709875));
#61829=CARTESIAN_POINT('Ctrl Pts',(-2.33525917090889,30.335419003064,14.0552604897481));
#61830=CARTESIAN_POINT('Ctrl Pts',(-2.36130148626115,30.3454845543004,13.9789016837452));
#61831=CARTESIAN_POINT('Ctrl Pts',(-2.38355823401219,30.3555699324038,13.9013347181094));
#61832=CARTESIAN_POINT('Ctrl Pts',(-2.42000205154344,30.3720840108957,13.7743244121248));
#61833=CARTESIAN_POINT('Ctrl Pts',(-2.44630586152763,30.3886555642733,13.6440648978829));
#61834=CARTESIAN_POINT('Ctrl Pts',(-2.46214628409733,30.4052617673184,13.5122063580512));
#61835=CARTESIAN_POINT('Ctrl Pts',(-2.47815337947532,30.4220427007082,13.3789604036455));
#61836=CARTESIAN_POINT('Ctrl Pts',(-2.48347301960662,30.4388587794074,13.2440793313919));
#61837=CARTESIAN_POINT('Ctrl Pts',(-2.477753291159,30.4556599230741,13.109316033593));
#61838=CARTESIAN_POINT('Ctrl Pts',(-2.4750610064385,30.4635682464841,13.045882748102));
#61839=CARTESIAN_POINT('Ctrl Pts',(-2.46992283116894,30.471472902046,12.9824764931707));
#61840=CARTESIAN_POINT('Ctrl Pts',(-2.46230396877764,30.4793669670259,12.919285459566));
#61841=CARTESIAN_POINT('Ctrl Pts',(-2.46230212926615,30.4793688729828,12.9192702026121));
#61842=CARTESIAN_POINT('Ctrl Pts',(-2.46230028961007,30.479370778939,12.9192549456707));
#61843=CARTESIAN_POINT('Ctrl Pts',(-2.46229844980938,30.4793726848947,12.9192396887419));
#61844=CARTESIAN_POINT('Ctrl Pts',(-2.45230851230945,30.4897218373576,12.8363960599049));
#61845=CARTESIAN_POINT('Ctrl Pts',(-2.43805598787451,30.5000467733648,12.7539095196764));
#61846=CARTESIAN_POINT('Ctrl Pts',(-2.41964302419575,30.510435508637,12.6722284099323));
#61847=CARTESIAN_POINT('Ctrl Pts',(-2.41850888848298,30.5110753967011,12.6671973098207));
#61848=CARTESIAN_POINT('Ctrl Pts',(-2.41735896832571,30.5117155262703,12.6621692480524));
#61849=CARTESIAN_POINT('Ctrl Pts',(-2.41619328710392,30.5123559175791,12.6571443227054));
#61850=CARTESIAN_POINT('Ctrl Pts',(0.312594521684916,39.2687268985923,10.2006318123981));
#61851=CARTESIAN_POINT('Ctrl Pts',(1.10278451631874,39.367686684378,10.2682228699795));
#61852=CARTESIAN_POINT('Ctrl Pts',(2.61633807062915,39.5646092557192,11.0339471882628));
#61853=CARTESIAN_POINT('Ctrl Pts',(3.48447994224266,39.8615963196975,13.4364945624193));
#61854=CARTESIAN_POINT('Ctrl Pts',(2.4737037416439,40.1586230481117,15.7850298071184));
#61855=CARTESIAN_POINT('Ctrl Pts',(0.519194218473144,40.407493993742,16.6463753640912));
#61856=CARTESIAN_POINT('Ctrl Pts',(-1.09278868638896,40.6071406712818,16.4018153614845));
#61857=CARTESIAN_POINT('Ctrl Pts',(-2.15309749265246,40.7570895673928,15.7935618381816));
#61858=CARTESIAN_POINT('Ctrl Pts',(-2.91471385951109,40.9071784817713,14.8368183188706));
#61859=CARTESIAN_POINT('Ctrl Pts',(-3.4010545907453,41.1074039103802,13.27518106621));
#61860=CARTESIAN_POINT('Ctrl Pts',(-2.95389395785344,41.3076508602556,11.6180538648701));
#61861=CARTESIAN_POINT('Ctrl Pts',(-1.74978220776,41.507656939418,10.5138956535236));
#61862=CARTESIAN_POINT('Ctrl Pts',(-0.485944985235109,41.6741175145073,
10.0214181492683));
#61863=CARTESIAN_POINT('Ctrl Pts',(1.02219499728983,41.8568649670751,10.1224423359238));
#61864=CARTESIAN_POINT('Ctrl Pts',(2.4080714216259,42.055620188501,11.0053265175813));
#61865=CARTESIAN_POINT('Ctrl Pts',(3.19871761650152,42.2536196929027,12.4385646110554));
#61866=CARTESIAN_POINT('Ctrl Pts',(3.20534904741162,42.4507122354209,14.0681869289385));
#61867=CARTESIAN_POINT('Ctrl Pts',(2.43477412422895,42.6467536737798,15.4938098236939));
#61868=CARTESIAN_POINT('Ctrl Pts',(1.0830399884291,42.841601180305,16.371133498718));
#61869=CARTESIAN_POINT('Ctrl Pts',(-0.24597312730138,43.0028674028311,16.4710263452315));
#61870=CARTESIAN_POINT('Ctrl Pts',(-1.17424515823741,43.1231290597125,16.1845758479658));
#61871=CARTESIAN_POINT('Ctrl Pts',(-1.62147454355865,43.1870491201526,15.930571493716));
#61872=CARTESIAN_POINT('Ctrl Pts',(-2.23622373822675,43.2827275887014,15.4716413166819));
#61873=CARTESIAN_POINT('Ctrl Pts',(-2.90863938487666,43.4176422979667,14.5818001747071));
#61874=CARTESIAN_POINT('Ctrl Pts',(-3.13855465666707,43.6064005807676,13.0381770779871));
#61875=CARTESIAN_POINT('Ctrl Pts',(-2.60415871522266,43.7933389117483,11.5873361511012));
#61876=CARTESIAN_POINT('Ctrl Pts',(-1.45426483026413,43.9783463662533,10.5801220890633));
#61877=CARTESIAN_POINT('Ctrl Pts',(0.0244694520634532,44.1613257418401,
10.2498340654442));
#61878=CARTESIAN_POINT('Ctrl Pts',(1.29887252139762,44.3220911833599,10.6192174467748));
#61879=CARTESIAN_POINT('Ctrl Pts',(2.41856206199899,44.5011143240446,11.5510825760216));
#61880=CARTESIAN_POINT('Ctrl Pts',(2.84250102970257,44.6386014173983,12.6326702660212));
#61881=CARTESIAN_POINT('Ctrl Pts',(2.80370202652921,44.7551453055736,13.5697356758772));
#61882=CARTESIAN_POINT('Ctrl Pts',(2.67642885900552,44.8324899718607,14.1780930409513));
#61883=CARTESIAN_POINT('Ctrl Pts',(2.19691057886715,44.9669190865462,15.1608829794906));
#61884=CARTESIAN_POINT('Ctrl Pts',(0.884633708880359,45.1562704903835,16.0821444896688));
#61885=CARTESIAN_POINT('Ctrl Pts',(-0.84304439264534,45.3605213244521,15.9901433791172));
#61886=CARTESIAN_POINT('Ctrl Pts',(-2.05603092570168,45.5429387474247,15.0919397400054));
#61887=CARTESIAN_POINT('Ctrl Pts',(-2.62182065763438,45.704578250735,13.8823526995957));
#61888=CARTESIAN_POINT('Ctrl Pts',(-2.53890823740617,45.8636701656143,12.5686554366777));
#61889=CARTESIAN_POINT('Ctrl Pts',(-1.84908359161403,46.0202157746922,11.4739637874368));
#61890=CARTESIAN_POINT('Ctrl Pts',(-0.737127953307188,46.1742234772143,
10.8524676464036));
#61891=CARTESIAN_POINT('Ctrl Pts',(0.515346184392654,46.3257139419959,10.8400377663191));
#61892=CARTESIAN_POINT('Ctrl Pts',(1.60285677681394,46.4747159390649,11.4192206339482));
#61893=CARTESIAN_POINT('Ctrl Pts',(2.26941428252578,46.621267325306,12.4315435743272));
#61894=CARTESIAN_POINT('Ctrl Pts',(2.36785255272078,46.765417671326,13.6189966756103));
#61895=CARTESIAN_POINT('Ctrl Pts',(1.89419027637734,46.9072227042509,14.6926655000575));
#61896=CARTESIAN_POINT('Ctrl Pts',(0.979655970614668,47.0467488710647,15.3945169326622));
#61897=CARTESIAN_POINT('Ctrl Pts',(-0.267888938204166,47.1993308203444,
15.5934545697946));
#61898=CARTESIAN_POINT('Ctrl Pts',(-1.53802286151021,47.3641460563792,15.0145962937778));
#61899=CARTESIAN_POINT('Ctrl Pts',(-2.22386857489773,47.5403959173155,13.6869883557155));
#61900=CARTESIAN_POINT('Ctrl Pts',(-1.99472867839811,47.6845135743016,12.4883514392389));
#61901=CARTESIAN_POINT('Ctrl Pts',(-1.40787042894492,47.7982904443204,11.7737414854899));
#61902=CARTESIAN_POINT('Ctrl Pts',(-0.628592239028725,47.9110997303948,
11.2898598022948));
#61903=CARTESIAN_POINT('Ctrl Pts',(0.549891817357097,48.0503941761843,11.2289545937645));
#61904=CARTESIAN_POINT('Ctrl Pts',(1.59591722050374,48.2013738551115,11.9659967128779));
#61905=CARTESIAN_POINT('Ctrl Pts',(2.00471040208874,48.3370802711296,13.0108431266425));
#61906=CARTESIAN_POINT('Ctrl Pts',(1.86296813475303,48.4783457746698,14.1718151081312));
#61907=CARTESIAN_POINT('Ctrl Pts',(1.16286679576134,48.5982957390209,14.9262017757273));
#61908=CARTESIAN_POINT('Ctrl Pts',(0.246695609337611,48.717566789975,15.2299109611891));
#61909=CARTESIAN_POINT('Ctrl Pts',(-0.569930120220827,48.8165778583093,
15.1898375551156));
#61910=CARTESIAN_POINT('Ctrl Pts',(-1.40496458666125,48.934940168389,14.6767864237024));
#61911=CARTESIAN_POINT('Ctrl Pts',(-1.89013333564764,49.0530095875852,13.8297344728053));
#61912=CARTESIAN_POINT('Ctrl Pts',(-1.91089170362233,49.1709390025344,12.8543916068453));
#61913=CARTESIAN_POINT('Ctrl Pts',(-1.46115125975772,49.2888886784375,11.9883720090566));
#61914=CARTESIAN_POINT('Ctrl Pts',(-0.785669968721914,49.3873285392625,
11.5338753755548));
#61915=CARTESIAN_POINT('Ctrl Pts',(-0.162780906843137,49.4662449068257,
11.3969697014267));
#61916=CARTESIAN_POINT('Ctrl Pts',(0.31613138970614,49.5255377704516,11.412316051461));
#61917=CARTESIAN_POINT('Ctrl Pts',(0.776867431823825,49.5849509789929,11.5464608590512));
#61918=CARTESIAN_POINT('Ctrl Pts',(1.40001179816061,49.6742843891679,11.9120303973004));
#61919=CARTESIAN_POINT('Ctrl Pts',(1.87317942742205,49.7740147394822,12.6037507980505));
#61920=CARTESIAN_POINT('Ctrl Pts',(1.97191227059097,49.8945205239042,13.5833072938098));
#61921=CARTESIAN_POINT('Ctrl Pts',(1.66936919957167,50.00574156926,14.4507596289108));
#61922=CARTESIAN_POINT('Ctrl Pts',(0.835340557919474,50.1417629552019,15.2072538991447));
#61923=CARTESIAN_POINT('Ctrl Pts',(-0.43261694699927,50.2931364853892,15.4022044191531));
#61924=CARTESIAN_POINT('Ctrl Pts',(-1.35934397586363,50.418870004698,14.8771965133792));
#61925=CARTESIAN_POINT('Ctrl Pts',(-1.89864355168201,50.5317973556908,14.1456434479416));
#61926=CARTESIAN_POINT('Ctrl Pts',(-2.08194393077751,50.604760573542,13.5721200297017));
#61927=CARTESIAN_POINT('Ctrl Pts',(-2.05671808092609,50.6801976316638,12.9645461728789));
#61928=CARTESIAN_POINT('Ctrl Pts',(-1.93870659718733,50.7451915351799,12.4553172529021));
#61929=CARTESIAN_POINT('Ctrl Pts',(-1.48562870557272,50.8598274622143,11.6353297371026));
#61930=CARTESIAN_POINT('Ctrl Pts',(-0.484014005491188,50.992982147934,11.085134484943));
#61931=CARTESIAN_POINT('Ctrl Pts',(0.620094294898221,51.1284453465146,11.1583829405731));
#61932=CARTESIAN_POINT('Ctrl Pts',(1.63397002672975,51.2654986273511,11.6292366243552));
#61933=CARTESIAN_POINT('Ctrl Pts',(2.4487093254446,51.4398837730822,12.887573924851));
#61934=CARTESIAN_POINT('Ctrl Pts',(2.12339578027333,51.6543187474332,14.7042901983831));
#61935=CARTESIAN_POINT('Ctrl Pts',(0.611026275306804,51.8741245979643,15.8381715292352));
#61936=CARTESIAN_POINT('Ctrl Pts',(-1.40546246703902,52.1098521447515,15.6203703325987));
#61937=CARTESIAN_POINT('Ctrl Pts',(-2.29978083208262,52.2747671286668,14.4865823778754));
#61938=CARTESIAN_POINT('Ctrl Pts',(-2.45785835496615,52.3637908706225,13.7890755589211));
#61939=CARTESIAN_POINT('Ctrl Pts',(0.294903861775253,39.6139115644023,10.4045779384392));
#61940=CARTESIAN_POINT('Ctrl Pts',(1.03268206896656,39.7064516885537,10.4785410543229));
#61941=CARTESIAN_POINT('Ctrl Pts',(2.42857112035405,39.8896587319756,11.2135222039816));
#61942=CARTESIAN_POINT('Ctrl Pts',(3.19296975732018,40.1633527535325,13.4396418953121));
#61943=CARTESIAN_POINT('Ctrl Pts',(2.23642221120207,40.4346975246274,15.5696280850306));
#61944=CARTESIAN_POINT('Ctrl Pts',(0.453975309221201,40.6602273892792,16.3228441371572));
#61945=CARTESIAN_POINT('Ctrl Pts',(-0.995070086503688,40.8401590193753,
16.0819104233793));
#61946=CARTESIAN_POINT('Ctrl Pts',(-1.93938070844708,40.9748303090262,15.5223972612286));
#61947=CARTESIAN_POINT('Ctrl Pts',(-2.60894671018738,41.1091870901098,14.6566847282954));
#61948=CARTESIAN_POINT('Ctrl Pts',(-3.02329663478697,41.2878712464816,13.2573491380613));
#61949=CARTESIAN_POINT('Ctrl Pts',(-2.60463724926944,41.4658015589571,11.7911606651713));
#61950=CARTESIAN_POINT('Ctrl Pts',(-1.52552555387745,41.6428577046171,10.8288627721415));
#61951=CARTESIAN_POINT('Ctrl Pts',(-0.403553397693664,41.7898852789765,
10.4094234971742));
#61952=CARTESIAN_POINT('Ctrl Pts',(0.923675528652629,41.9509113858405,10.5169608454263));
#61953=CARTESIAN_POINT('Ctrl Pts',(2.13077972830358,42.1256332856869,11.3097879483148));
#61954=CARTESIAN_POINT('Ctrl Pts',(2.80677821778962,42.299353081632,12.5765216609874));
#61955=CARTESIAN_POINT('Ctrl Pts',(2.79274880982071,42.4720138755312,14.0037583001608));
#61956=CARTESIAN_POINT('Ctrl Pts',(2.10130782698956,42.6435641932168,15.2415086413168));
#61957=CARTESIAN_POINT('Ctrl Pts',(0.908928431243241,42.8139558890705,15.9920026155197));
#61958=CARTESIAN_POINT('Ctrl Pts',(-0.253854780111174,42.9549481130077,
16.0630860323738));
#61959=CARTESIAN_POINT('Ctrl Pts',(-1.06179228515288,43.0601100424265,15.8012973910613));
#61960=CARTESIAN_POINT('Ctrl Pts',(-1.44967403461439,43.1160138685282,15.5737088269141));
#61961=CARTESIAN_POINT('Ctrl Pts',(-1.98157874533087,43.1997094802458,15.1647965689675));
#61962=CARTESIAN_POINT('Ctrl Pts',(-2.5588383120568,43.3177713855586,14.3780726568003));
#61963=CARTESIAN_POINT('Ctrl Pts',(-2.74104930113207,43.483143195421,13.0233004846037));
#61964=CARTESIAN_POINT('Ctrl Pts',(-2.25410072239219,43.647188172129,11.7572301414462));
#61965=CARTESIAN_POINT('Ctrl Pts',(-1.23048329990724,43.8098860070457,10.8863164624582));
#61966=CARTESIAN_POINT('Ctrl Pts',(0.0771158868406177,43.9712239212822,
10.6140519303021));
#61967=CARTESIAN_POINT('Ctrl Pts',(1.19916525789307,44.1134181689073,10.9572039819767));
#61968=CARTESIAN_POINT('Ctrl Pts',(2.1797215331002,44.2722435626865,11.7984904045362));
#61969=CARTESIAN_POINT('Ctrl Pts',(2.54314510409658,44.394707072148,12.7670995874116));
#61970=CARTESIAN_POINT('Ctrl Pts',(2.49539793108867,44.4989185614651,13.604153393425));
#61971=CARTESIAN_POINT('Ctrl Pts',(2.37287581901333,44.568191507612,14.1470080965811));
#61972=CARTESIAN_POINT('Ctrl Pts',(1.92877687281838,44.6888918452501,15.0222703355227));
#61973=CARTESIAN_POINT('Ctrl Pts',(0.732108445051806,44.8598258348619,15.8359448411065));
#61974=CARTESIAN_POINT('Ctrl Pts',(-0.838250425788402,45.0457028640936,
15.7283431435459));
#61975=CARTESIAN_POINT('Ctrl Pts',(-1.93723819221189,45.2130184634799,14.8869161384525));
#61976=CARTESIAN_POINT('Ctrl Pts',(-2.44132651224387,45.3623520315815,13.7613265784781));
#61977=CARTESIAN_POINT('Ctrl Pts',(-2.34379149512239,45.5104721996345,12.5400740554247));
#61978=CARTESIAN_POINT('Ctrl Pts',(-1.67903175903387,45.6574216643582,11.5239844507756));
#61979=CARTESIAN_POINT('Ctrl Pts',(-0.616494263126933,45.8032455001699,
10.9540765507697));
#61980=CARTESIAN_POINT('Ctrl Pts',(0.579876890742993,45.9479958855824,10.9634172020583));
#61981=CARTESIAN_POINT('Ctrl Pts',(1.61826918658412,46.0917277688557,11.5408030474182));
#61982=CARTESIAN_POINT('Ctrl Pts',(2.24906033510871,46.2344985697371,12.5384885873925));
#61983=CARTESIAN_POINT('Ctrl Pts',(2.32378436557046,46.37637271732,13.7083777135971));
#61984=CARTESIAN_POINT('Ctrl Pts',(1.83239123279297,46.5174147356513,14.7665437342237));
#61985=CARTESIAN_POINT('Ctrl Pts',(0.899464032953714,46.657693670538,15.4535636835773));
#61986=CARTESIAN_POINT('Ctrl Pts',(-0.371763906289662,46.8127931156224,
15.630157515452));
#61987=CARTESIAN_POINT('Ctrl Pts',(-1.66726587814456,46.9825231239923,15.0086744544976));
#61988=CARTESIAN_POINT('Ctrl Pts',(-2.35580384867077,47.1667730292082,13.6071446302206));
#61989=CARTESIAN_POINT('Ctrl Pts',(-2.08617697257812,47.3197112981773,12.34100074822));
#61990=CARTESIAN_POINT('Ctrl Pts',(-1.43906379959527,47.4418000516265,11.5892918254582));
#61991=CARTESIAN_POINT('Ctrl Pts',(-0.58526695271636,47.5637444470721,11.0864992112));
#61992=CARTESIAN_POINT('Ctrl Pts',(0.703174222752905,47.7159712607203,11.0485248694669));
#61993=CARTESIAN_POINT('Ctrl Pts',(1.8429732534516,47.8833013930449,11.8911301665703));
#61994=CARTESIAN_POINT('Ctrl Pts',(2.27259405105886,48.0354730745259,13.0729978551617));
#61995=CARTESIAN_POINT('Ctrl Pts',(2.07998644589785,48.1954006594234,14.3821003864233));
#61996=CARTESIAN_POINT('Ctrl Pts',(1.25848223006792,48.3327436550993,15.225877237191));
#61997=CARTESIAN_POINT('Ctrl Pts',(0.192592484505567,48.4704234645487,15.5485749946903));
#61998=CARTESIAN_POINT('Ctrl Pts',(-0.753401380942494,48.5853899109762,
15.4776711893897));
#61999=CARTESIAN_POINT('Ctrl Pts',(-1.71342552510336,48.7238069063804,14.8530008472574));
#62000=CARTESIAN_POINT('Ctrl Pts',(-2.25772039498446,48.8627612021184,13.8421264947207));
#62001=CARTESIAN_POINT('Ctrl Pts',(-2.25181468353777,49.0023278556759,12.6883745865887));
#62002=CARTESIAN_POINT('Ctrl Pts',(-1.69023381425614,49.142582938478,11.6738167015065));
#62003=CARTESIAN_POINT('Ctrl Pts',(-0.870245654444321,49.2600959933723,
11.1533123062566));
#62004=CARTESIAN_POINT('Ctrl Pts',(-0.121299859616587,49.3545201124099,
11.0097786824479));
#62005=CARTESIAN_POINT('Ctrl Pts',(0.451358189684015,49.4255548502409,11.04360042071));
#62006=CARTESIAN_POINT('Ctrl Pts',(0.999038222241836,49.4968126879922,11.2192031733343));
#62007=CARTESIAN_POINT('Ctrl Pts',(1.73449309711661,49.604047323927,11.6776627570674));
#62008=CARTESIAN_POINT('Ctrl Pts',(2.28033102004061,49.723896475789,12.523210973049));
#62009=CARTESIAN_POINT('Ctrl Pts',(2.36751628288518,49.8687455361102,13.7026302524268));
#62010=CARTESIAN_POINT('Ctrl Pts',(1.97671262830022,50.0023841240909,14.7341871695187));
#62011=CARTESIAN_POINT('Ctrl Pts',(0.952834108900274,50.1656178959293,15.614728141144));
#62012=CARTESIAN_POINT('Ctrl Pts',(-0.569770782102248,50.3468428570876,
15.8077195842284));
#62013=CARTESIAN_POINT('Ctrl Pts',(-1.65715677486589,50.496752779469,15.1534589049772));
#62014=CARTESIAN_POINT('Ctrl Pts',(-2.27546471621605,50.6309468937531,14.2688059616163));
#62015=CARTESIAN_POINT('Ctrl Pts',(-2.47523622476083,50.7174027252289,13.5842958454368));
#62016=CARTESIAN_POINT('Ctrl Pts',(-2.42770164858311,50.8064919076948,12.8681568966158));
#62017=CARTESIAN_POINT('Ctrl Pts',(-2.27399740751639,50.8831013712292,12.2718655454637));
#62018=CARTESIAN_POINT('Ctrl Pts',(-1.7181195707613,51.0178208654781,11.3221134951395));
#62019=CARTESIAN_POINT('Ctrl Pts',(-0.533448887883877,51.1732967383133,
10.7100836543821));
#62020=CARTESIAN_POINT('Ctrl Pts',(0.743053321251822,51.3303063206415,10.8254204432482));
#62021=CARTESIAN_POINT('Ctrl Pts',(1.89861213344509,51.4883421473996,11.3954710536808));
#62022=CARTESIAN_POINT('Ctrl Pts',(2.79438771635136,51.6878173191196,12.8565507493252));
#62023=CARTESIAN_POINT('Ctrl Pts',(2.37731698119797,51.9302681611678,14.9000235374981));
#62024=CARTESIAN_POINT('Ctrl Pts',(0.659697208520961,52.1757699545507,16.1255851353615));
#62025=CARTESIAN_POINT('Ctrl Pts',(-1.55650206655295,52.4357027514075,15.8344584184493));
#62026=CARTESIAN_POINT('Ctrl Pts',(-2.50012270616443,52.6150222833368,14.5799293707503));
#62027=CARTESIAN_POINT('Ctrl Pts',(-2.65572307264903,52.7110742858936,13.8247094991072));
#62028=CARTESIAN_POINT('Ctrl Pts',(0.27721320186559,39.9590962302123,10.6085240644802));
#62029=CARTESIAN_POINT('Ctrl Pts',(0.96257962161438,40.0452166927294,10.6888592386662));
#62030=CARTESIAN_POINT('Ctrl Pts',(2.24080417007896,40.2147082082319,11.3930972197004));
#62031=CARTESIAN_POINT('Ctrl Pts',(2.9014595723977,40.4651091873673,13.442789228205));
#62032=CARTESIAN_POINT('Ctrl Pts',(1.99914068076025,40.7107720011432,15.3542263629428));
#62033=CARTESIAN_POINT('Ctrl Pts',(0.388756399969259,40.9129607848164,15.9993129102233));
#62034=CARTESIAN_POINT('Ctrl Pts',(-0.897351486618409,41.0731773674687,
15.7620054852741));
#62035=CARTESIAN_POINT('Ctrl Pts',(-1.7256639242417,41.1925710506597,15.2512326842756));
#62036=CARTESIAN_POINT('Ctrl Pts',(-2.30317956086367,41.3111956984482,14.4765511377203));
#62037=CARTESIAN_POINT('Ctrl Pts',(-2.64553867882863,41.468338582583,13.2395172099127));
#62038=CARTESIAN_POINT('Ctrl Pts',(-2.25538054068543,41.6239522576586,11.9642674654724));
#62039=CARTESIAN_POINT('Ctrl Pts',(-1.30126889999489,41.7780584698162,11.1438298907594));
#62040=CARTESIAN_POINT('Ctrl Pts',(-0.321161810152211,41.9056530434457,
10.7974288450802));
#62041=CARTESIAN_POINT('Ctrl Pts',(0.82515606001542,42.0449578046059,10.9114793549288));
#62042=CARTESIAN_POINT('Ctrl Pts',(1.85348803498126,42.1956463828727,11.6142493790484));
#62043=CARTESIAN_POINT('Ctrl Pts',(2.41483881907772,42.3450864703612,12.7144787109194));
#62044=CARTESIAN_POINT('Ctrl Pts',(2.38014857222981,42.4933155156414,13.9393296713829));
#62045=CARTESIAN_POINT('Ctrl Pts',(1.76784152975018,42.6403747126539,14.9892074589397));
#62046=CARTESIAN_POINT('Ctrl Pts',(0.734816874057389,42.786310597836,15.6128717323214));
#62047=CARTESIAN_POINT('Ctrl Pts',(-0.261736432920961,42.9070288231842,
15.6551457195162));
#62048=CARTESIAN_POINT('Ctrl Pts',(-0.949339412068327,42.9970910251405,
15.4180189341568));
#62049=CARTESIAN_POINT('Ctrl Pts',(-1.27787352567013,43.0449786169039,15.2168461601121));
#62050=CARTESIAN_POINT('Ctrl Pts',(-1.726933752435,43.1166913717903,14.857951821253));
#62051=CARTESIAN_POINT('Ctrl Pts',(-2.20903723923693,43.2179004731506,14.1743451388937));
#62052=CARTESIAN_POINT('Ctrl Pts',(-2.34354394559704,43.3598858100745,13.0084238912205));
#62053=CARTESIAN_POINT('Ctrl Pts',(-1.90404272956172,43.5010374325095,11.9271241317911));
#62054=CARTESIAN_POINT('Ctrl Pts',(-1.00670176955033,43.6414256478381,11.192510835853));
#62055=CARTESIAN_POINT('Ctrl Pts',(0.129762321617784,43.7811221007244,10.9782697951601));
#62056=CARTESIAN_POINT('Ctrl Pts',(1.09945799438853,43.9047451544546,11.2951905171787));
#62057=CARTESIAN_POINT('Ctrl Pts',(1.94088100420141,44.0433728013285,12.0458982330509));
#62058=CARTESIAN_POINT('Ctrl Pts',(2.24378917849061,44.1508127268978,12.9015289088021));
#62059=CARTESIAN_POINT('Ctrl Pts',(2.18709383564812,44.2426918173567,13.6385711109727));
#62060=CARTESIAN_POINT('Ctrl Pts',(2.06932277902114,44.3038930433633,14.115923152211));
#62061=CARTESIAN_POINT('Ctrl Pts',(1.66064316676961,44.410864603954,14.8836576915548));
#62062=CARTESIAN_POINT('Ctrl Pts',(0.579583181223254,44.5633811793401,15.5897451925441));
#62063=CARTESIAN_POINT('Ctrl Pts',(-0.833456458931463,44.7308844037353,
15.4665429079745));
#62064=CARTESIAN_POINT('Ctrl Pts',(-1.81844545872208,44.8830981795351,14.6818925368995));
#62065=CARTESIAN_POINT('Ctrl Pts',(-2.26083236685335,45.020125812428,13.6403004573605));
#62066=CARTESIAN_POINT('Ctrl Pts',(-2.14867475283861,45.1572742336549,12.5114926741716));
#62067=CARTESIAN_POINT('Ctrl Pts',(-1.5089799264537,45.2946275540243,11.5740051141142));
#62068=CARTESIAN_POINT('Ctrl Pts',(-0.495860572946676,45.4322675231254,
11.0556854551358));
#62069=CARTESIAN_POINT('Ctrl Pts',(0.644407597093334,45.5702778291688,11.0867966377975));
#62070=CARTESIAN_POINT('Ctrl Pts',(1.6336815963543,45.7087395986466,11.662385460888));
#62071=CARTESIAN_POINT('Ctrl Pts',(2.22870638769164,45.8477298141681,12.6454336004577));
#62072=CARTESIAN_POINT('Ctrl Pts',(2.27971617842012,45.9873277633141,13.797758751584));
#62073=CARTESIAN_POINT('Ctrl Pts',(1.77059218920859,46.1276067670516,14.84042196839));
#62074=CARTESIAN_POINT('Ctrl Pts',(0.819272095292761,46.2686384700114,15.5126104344925));
#62075=CARTESIAN_POINT('Ctrl Pts',(-0.47563887437516,46.4262554109004,15.6668604611094));
#62076=CARTESIAN_POINT('Ctrl Pts',(-1.79650889477891,46.6009001916055,15.0027526152174));
#62077=CARTESIAN_POINT('Ctrl Pts',(-2.4877391224438,46.7931501411008,13.5273009047258));
#62078=CARTESIAN_POINT('Ctrl Pts',(-2.17762526675814,46.9549090220529,12.1936500572011));
#62079=CARTESIAN_POINT('Ctrl Pts',(-1.47025717024561,47.0853096589328,11.4048421654265));
#62080=CARTESIAN_POINT('Ctrl Pts',(-0.541941666403998,47.2163891637494,
10.8831386201051));
#62081=CARTESIAN_POINT('Ctrl Pts',(0.85645662814871,47.3815483452563,10.8680951451692));
#62082=CARTESIAN_POINT('Ctrl Pts',(2.09002928639948,47.5652289309781,11.8162636202629));
#62083=CARTESIAN_POINT('Ctrl Pts',(2.54047770002897,47.7338658779222,13.1351525836811));
#62084=CARTESIAN_POINT('Ctrl Pts',(2.29700475704268,47.9124555441771,14.5923856647155));
#62085=CARTESIAN_POINT('Ctrl Pts',(1.35409766437449,48.0671915711777,15.5255526986548));
#62086=CARTESIAN_POINT('Ctrl Pts',(0.138489359673523,48.2232801391222,15.8672390281914));
#62087=CARTESIAN_POINT('Ctrl Pts',(-0.936872641664163,48.3542019636433,
15.7655048236637));
#62088=CARTESIAN_POINT('Ctrl Pts',(-2.02188646354548,48.5126736443718,15.0292152708126));
#62089=CARTESIAN_POINT('Ctrl Pts',(-2.62530745432128,48.6725128166516,13.8545185166361));
#62090=CARTESIAN_POINT('Ctrl Pts',(-2.59273766345323,48.8337167088173,12.522357566332));
#62091=CARTESIAN_POINT('Ctrl Pts',(-1.91931636875457,48.9962771985184,11.3592613939564));
#62092=CARTESIAN_POINT('Ctrl Pts',(-0.954821340166725,49.1328634474821,
10.7727492369583));
#62093=CARTESIAN_POINT('Ctrl Pts',(-0.0798188123900331,49.242795317994,
10.6225876634692));
#62094=CARTESIAN_POINT('Ctrl Pts',(0.586584989661894,49.3255719300301,10.6748847899589));
#62095=CARTESIAN_POINT('Ctrl Pts',(1.22120901265984,49.4086743969914,10.8919454876174));
#62096=CARTESIAN_POINT('Ctrl Pts',(2.0689743960726,49.5338102586861,11.4432951168345));
#62097=CARTESIAN_POINT('Ctrl Pts',(2.68748261265918,49.6737782120957,12.4426711480475));
#62098=CARTESIAN_POINT('Ctrl Pts',(2.7631202951794,49.842970548316,13.8219532110439));
#62099=CARTESIAN_POINT('Ctrl Pts',(2.28405605702878,49.999026678922,15.0176147101266));
#62100=CARTESIAN_POINT('Ctrl Pts',(1.07032765988108,50.1894728366565,16.0222023831432));
#62101=CARTESIAN_POINT('Ctrl Pts',(-0.706924617205229,50.400549228786,16.2132347493037));
#62102=CARTESIAN_POINT('Ctrl Pts',(-1.95496957386815,50.5746355542401,15.4297212965753));
#62103=CARTESIAN_POINT('Ctrl Pts',(-2.65228588075009,50.7300964318154,14.3919684752911));
#62104=CARTESIAN_POINT('Ctrl Pts',(-2.86852851874415,50.8300448769158,13.5964716611719));
#62105=CARTESIAN_POINT('Ctrl Pts',(-2.79868521624013,50.9327861837258,12.7717676203526));
#62106=CARTESIAN_POINT('Ctrl Pts',(-2.60928821784544,51.0210112072784,12.0884138380253));
#62107=CARTESIAN_POINT('Ctrl Pts',(-1.9506104359499,51.1758142687417,11.0088972531764));
#62108=CARTESIAN_POINT('Ctrl Pts',(-0.582883770276567,51.3536113286928,
10.3350328238214));
#62109=CARTESIAN_POINT('Ctrl Pts',(0.866012347605427,51.5321672947683,10.4924579459233));
#62110=CARTESIAN_POINT('Ctrl Pts',(2.16325424016043,51.7111856674481,11.1617054830065));
#62111=CARTESIAN_POINT('Ctrl Pts',(3.14006610725811,51.935750865157,12.8255275737996));
#62112=CARTESIAN_POINT('Ctrl Pts',(2.63123818212263,52.2062175749024,15.0957568766131));
#62113=CARTESIAN_POINT('Ctrl Pts',(0.708368141735119,52.4774153111372,16.4129987414879));
#62114=CARTESIAN_POINT('Ctrl Pts',(-1.70754166606687,52.7615533580634,16.0485465042998));
#62115=CARTESIAN_POINT('Ctrl Pts',(-2.70046458024624,52.9552774380068,14.6732763636255));
#62116=CARTESIAN_POINT('Ctrl Pts',(-2.85358779033189,53.0583577011648,13.8603434392933));
#62117=CARTESIAN_POINT('Ctrl Pts',(0.259522541955927,40.3042808960223,10.8124701905213));
#62118=CARTESIAN_POINT('Ctrl Pts',(0.8924771742622,40.3839816969049,10.8991774230097));
#62119=CARTESIAN_POINT('Ctrl Pts',(2.05303721980387,40.5397576844882,11.5726722354191));
#62120=CARTESIAN_POINT('Ctrl Pts',(2.60994938747521,40.7668656212022,13.4459365610979));
#62121=CARTESIAN_POINT('Ctrl Pts',(1.76185915031841,40.9868464776589,15.1388246408551));
#62122=CARTESIAN_POINT('Ctrl Pts',(0.323537490717318,41.1656941803536,15.6757816832893));
#62123=CARTESIAN_POINT('Ctrl Pts',(-0.799632886733132,41.3061957155623,
15.4421005471689));
#62124=CARTESIAN_POINT('Ctrl Pts',(-1.51194714003632,41.4103117922932,14.9800681073227));
#62125=CARTESIAN_POINT('Ctrl Pts',(-1.99741241153996,41.5132043067865,14.2964175471451));
#62126=CARTESIAN_POINT('Ctrl Pts',(-2.2677807228703,41.6488059186844,13.221685281764));
#62127=CARTESIAN_POINT('Ctrl Pts',(-1.90612383210144,41.78210295636,12.1373742657736));
#62128=CARTESIAN_POINT('Ctrl Pts',(-1.07701224611235,41.9132592350153,11.4587970093773));
#62129=CARTESIAN_POINT('Ctrl Pts',(-0.238770222610763,42.0214208079148,
11.185434192986));
#62130=CARTESIAN_POINT('Ctrl Pts',(0.726636591378214,42.1390042233713,11.3059978644313));
#62131=CARTESIAN_POINT('Ctrl Pts',(1.57619634165895,42.2656594800585,11.9187108097819));
#62132=CARTESIAN_POINT('Ctrl Pts',(2.02289942036582,42.3908198590905,12.8524357608515));
#62133=CARTESIAN_POINT('Ctrl Pts',(1.9675483346389,42.5146171557516,13.8749010426051));
#62134=CARTESIAN_POINT('Ctrl Pts',(1.43437523251079,42.637185232091,14.7369062765628));
#62135=CARTESIAN_POINT('Ctrl Pts',(0.56070531687153,42.7586653066015,15.2337408491231));
#62136=CARTESIAN_POINT('Ctrl Pts',(-0.269618085730753,42.8591095333607,
15.2472054066585));
#62137=CARTESIAN_POINT('Ctrl Pts',(-0.83688653898379,42.9340720078546,15.0347404772521));
#62138=CARTESIAN_POINT('Ctrl Pts',(-1.10607301672588,42.9739433652795,14.8599834933103));
#62139=CARTESIAN_POINT('Ctrl Pts',(-1.47228875953913,43.0336732633348,14.5511070735386));
#62140=CARTESIAN_POINT('Ctrl Pts',(-1.85923616641706,43.1180295607426,13.9706176209871));
#62141=CARTESIAN_POINT('Ctrl Pts',(-1.94603859006203,43.2366284247279,12.9935472978372));
#62142=CARTESIAN_POINT('Ctrl Pts',(-1.55398473673125,43.3548866928901,12.097018122136));
#62143=CARTESIAN_POINT('Ctrl Pts',(-0.782920239193443,43.4729652886305,
11.4987052092478));
#62144=CARTESIAN_POINT('Ctrl Pts',(0.182408756394949,43.5910202801664,11.342487660018));
#62145=CARTESIAN_POINT('Ctrl Pts',(0.999750730883996,43.6960721400019,11.6331770523806));
#62146=CARTESIAN_POINT('Ctrl Pts',(1.70204047530261,43.8145020399705,12.2933060615655));
#62147=CARTESIAN_POINT('Ctrl Pts',(1.94443325288464,43.9069183816476,13.0359582301927));
#62148=CARTESIAN_POINT('Ctrl Pts',(1.87878974020758,43.9864650732482,13.6729888285206));
#62149=CARTESIAN_POINT('Ctrl Pts',(1.76576973902895,44.0395945791145,14.0848382078407));
#62150=CARTESIAN_POINT('Ctrl Pts',(1.39250946072084,44.1328373626579,14.7450450475868));
#62151=CARTESIAN_POINT('Ctrl Pts',(0.427057917394702,44.2669365238183,15.3435455439818));
#62152=CARTESIAN_POINT('Ctrl Pts',(-0.828662492074526,44.4160659433769,
15.2047426724031));
#62153=CARTESIAN_POINT('Ctrl Pts',(-1.69965272523227,44.5531778955905,14.4768689353467));
#62154=CARTESIAN_POINT('Ctrl Pts',(-2.08033822146284,44.6778995932745,13.519274336243));
#62155=CARTESIAN_POINT('Ctrl Pts',(-1.95355801055484,44.8040762676752,12.4829112929186));
#62156=CARTESIAN_POINT('Ctrl Pts',(-1.33892809387352,44.9318334436903,11.6240257774529));
#62157=CARTESIAN_POINT('Ctrl Pts',(-0.375226882766422,45.061289546081,11.1572943595019));
#62158=CARTESIAN_POINT('Ctrl Pts',(0.708938303443674,45.1925597727553,11.2101760735367));
#62159=CARTESIAN_POINT('Ctrl Pts',(1.64909400612448,45.3257514284375,11.7839678743579));
#62160=CARTESIAN_POINT('Ctrl Pts',(2.20835244027458,45.4609610585992,12.752378613523));
#62161=CARTESIAN_POINT('Ctrl Pts',(2.2356479912698,45.598282809308,13.8871397895708));
#62162=CARTESIAN_POINT('Ctrl Pts',(1.70879314562423,45.737798798452,14.9143002025562));
#62163=CARTESIAN_POINT('Ctrl Pts',(0.739080157631811,45.8795832694846,15.5716571854076));
#62164=CARTESIAN_POINT('Ctrl Pts',(-0.579513842460654,46.0397177061783,
15.7035634067668));
#62165=CARTESIAN_POINT('Ctrl Pts',(-1.92575191141326,46.2192772592186,14.9968307759372));
#62166=CARTESIAN_POINT('Ctrl Pts',(-2.61967439621684,46.4195272529936,13.447457179231));
#62167=CARTESIAN_POINT('Ctrl Pts',(-2.26907356093815,46.5901067459285,12.0462993661822));
#62168=CARTESIAN_POINT('Ctrl Pts',(-1.50145054089596,46.728819266239,11.2203925053949));
#62169=CARTESIAN_POINT('Ctrl Pts',(-0.498616380091633,46.8690338804268,
10.6797780290102));
#62170=CARTESIAN_POINT('Ctrl Pts',(1.00973903354452,47.0471254297924,10.6876654208715));
#62171=CARTESIAN_POINT('Ctrl Pts',(2.33708531934735,47.2471564689115,11.7413970739553));
#62172=CARTESIAN_POINT('Ctrl Pts',(2.80836134899909,47.4322586813186,13.1973073122003));
#62173=CARTESIAN_POINT('Ctrl Pts',(2.51402306818751,47.6295104289307,14.8026709430076));
#62174=CARTESIAN_POINT('Ctrl Pts',(1.44971309868106,47.8016394872561,15.8252281601187));
#62175=CARTESIAN_POINT('Ctrl Pts',(0.084386234841479,47.9761368136959,16.1859030616927));
#62176=CARTESIAN_POINT('Ctrl Pts',(-1.12034390238583,48.1230140163103,16.0533384579378));
#62177=CARTESIAN_POINT('Ctrl Pts',(-2.3303474019876,48.3015403823632,15.2054296943677));
#62178=CARTESIAN_POINT('Ctrl Pts',(-2.99289451365811,48.4822644311848,13.8669105385515));
#62179=CARTESIAN_POINT('Ctrl Pts',(-2.93366064336868,48.6651055619588,12.3563405460754));
#62180=CARTESIAN_POINT('Ctrl Pts',(-2.14839892325299,48.8499714585589,11.0447060864063));
#62181=CARTESIAN_POINT('Ctrl Pts',(-1.03939702588914,49.005630901592,10.3921861676601));
#62182=CARTESIAN_POINT('Ctrl Pts',(-0.0383377651634865,49.1310705235782,
10.2353966444905));
#62183=CARTESIAN_POINT('Ctrl Pts',(0.721811789639765,49.2255890098193,10.3061691592078));
#62184=CARTESIAN_POINT('Ctrl Pts',(1.44337980307785,49.3205361059907,10.5646878019004));
#62185=CARTESIAN_POINT('Ctrl Pts',(2.4034556950286,49.4635731934453,11.2089274766015));
#62186=CARTESIAN_POINT('Ctrl Pts',(3.09463420527775,49.6236599484025,12.362131323046));
#62187=CARTESIAN_POINT('Ctrl Pts',(3.15872430747361,49.817195560522,13.9412761696611));
#62188=CARTESIAN_POINT('Ctrl Pts',(2.59139948575733,49.995669233753,15.3010422507346));
#62189=CARTESIAN_POINT('Ctrl Pts',(1.18782121086188,50.2133277773838,16.4296766251425));
#62190=CARTESIAN_POINT('Ctrl Pts',(-0.844078452308207,50.4542556004844,
16.6187499143789));
#62191=CARTESIAN_POINT('Ctrl Pts',(-2.25278237287041,50.6525183290112,15.7059836881734));
#62192=CARTESIAN_POINT('Ctrl Pts',(-3.02910704528412,50.8292459698778,14.5151309889659));
#62193=CARTESIAN_POINT('Ctrl Pts',(-3.26182081272746,50.9426870286026,13.608647476907));
#62194=CARTESIAN_POINT('Ctrl Pts',(-3.16966878389714,51.0590804597567,12.6753783440895));
#62195=CARTESIAN_POINT('Ctrl Pts',(-2.94457902817449,51.1589210433276,11.904962130587));
#62196=CARTESIAN_POINT('Ctrl Pts',(-2.18310130113848,51.3338076720054,10.6956810112131));
#62197=CARTESIAN_POINT('Ctrl Pts',(-0.632318652669253,51.5339259190722,
9.95998199326065));
#62198=CARTESIAN_POINT('Ctrl Pts',(0.988971373959032,51.7340282688952,10.1594954485985));
#62199=CARTESIAN_POINT('Ctrl Pts',(2.42789634687579,51.9340291874966,10.9279399123321));
#62200=CARTESIAN_POINT('Ctrl Pts',(3.48574449816487,52.1836844111943,12.7945043982738));
#62201=CARTESIAN_POINT('Ctrl Pts',(2.88515938304727,52.482166988637,15.2914902157282));
#62202=CARTESIAN_POINT('Ctrl Pts',(0.757039074949276,52.7790606677237,16.7004123476143));
#62203=CARTESIAN_POINT('Ctrl Pts',(-1.8585812655808,53.0874039647193,16.2626345901503));
#62204=CARTESIAN_POINT('Ctrl Pts',(-2.90080645432805,53.2955325926767,14.7666233565004));
#62205=CARTESIAN_POINT('Ctrl Pts',(-3.05145250801475,53.4056411164359,13.8959773794795));
#62206=CARTESIAN_POINT('Ctrl Pts',(0.29921364472731,40.3086929042607,10.8178945405685));
#62207=CARTESIAN_POINT('Ctrl Pts',(0.389708924283056,40.3200412428889,10.8317964718351));
#62208=CARTESIAN_POINT('Ctrl Pts',(0.479307970878857,40.3312307169892,10.8507982196188));
#62209=CARTESIAN_POINT('Ctrl Pts',(0.567442862048113,40.3423697335524,10.874654633906));
#62210=CARTESIAN_POINT('Ctrl Pts',(0.61829069060576,40.3487961873324,10.8884181598784));
#62211=CARTESIAN_POINT('Ctrl Pts',(0.668650725446275,40.3552057799045,10.9037966870897));
#62212=CARTESIAN_POINT('Ctrl Pts',(0.71841105546202,40.3616187646839,10.9207358224377));
#62213=CARTESIAN_POINT('Ctrl Pts',(0.768295778232184,40.3680477808852,10.9377173028767));
#62214=CARTESIAN_POINT('Ctrl Pts',(0.817584154307734,40.3744817266285,10.9562693482308));
#62215=CARTESIAN_POINT('Ctrl Pts',(0.866182167778944,40.3809444554227,10.9763435938198));
#62216=CARTESIAN_POINT('Ctrl Pts',(0.992812167616661,40.3977841426384,11.028650293911));
#62217=CARTESIAN_POINT('Ctrl Pts',(1.11477083880608,40.4148213759188,11.0912994771739));
#62218=CARTESIAN_POINT('Ctrl Pts',(1.23052443055251,40.4319181993909,11.1631211590004));
#62219=CARTESIAN_POINT('Ctrl Pts',(1.32825415279444,40.4463528945389,11.2237595626123));
#62220=CARTESIAN_POINT('Ctrl Pts',(1.42155667767204,40.4608333153926,11.2909313605061));
#62221=CARTESIAN_POINT('Ctrl Pts',(1.50958454153687,40.4753200946979,11.3640247833597));
#62222=CARTESIAN_POINT('Ctrl Pts',(1.52586217991162,40.4779989118859,11.3775408253554));
#62223=CARTESIAN_POINT('Ctrl Pts',(1.54195940664155,40.4806779520352,11.3912594810224));
#62224=CARTESIAN_POINT('Ctrl Pts',(1.55787077915975,40.4833569738712,11.4051770599222));
#62225=CARTESIAN_POINT('Ctrl Pts',(1.63095701633537,40.4956626140715,11.4691051384844));
#62226=CARTESIAN_POINT('Ctrl Pts',(1.70012936350538,40.5079651183981,11.5372375066277));
#62227=CARTESIAN_POINT('Ctrl Pts',(1.76480372628695,40.5201590532169,11.6090886428941));
#62228=CARTESIAN_POINT('Ctrl Pts',(1.79231321248755,40.5253457897722,11.6396507969936));
#62229=CARTESIAN_POINT('Ctrl Pts',(1.8190095269056,40.5305129350236,11.6708856794057));
#62230=CARTESIAN_POINT('Ctrl Pts',(1.84485058684559,40.5356526085924,11.7027558137197));
#62231=CARTESIAN_POINT('Ctrl Pts',(1.85147263365616,40.5369697046806,11.7109228750467));
#62232=CARTESIAN_POINT('Ctrl Pts',(1.85803839042547,40.5382849988255,11.7191315174064));
#62233=CARTESIAN_POINT('Ctrl Pts',(1.86454710629466,40.5395983634004,11.7273810383168));
#62234=CARTESIAN_POINT('Ctrl Pts',(1.86456047911591,40.5396010618421,11.7273979877997));
#62235=CARTESIAN_POINT('Ctrl Pts',(1.86457385169639,40.5396037602755,11.7274149374552));
#62236=CARTESIAN_POINT('Ctrl Pts',(1.86458722403605,40.5396064587008,11.7274318872833));
#62237=CARTESIAN_POINT('Ctrl Pts',(1.91920647481157,40.5506281626434,11.7966633704424));
#62238=CARTESIAN_POINT('Ctrl Pts',(1.96988117462805,40.5615262747318,11.868867246658));
#62239=CARTESIAN_POINT('Ctrl Pts',(2.01635880546304,40.5724223878967,11.9435176162419));
#62240=CARTESIAN_POINT('Ctrl Pts',(2.03391176247672,40.5765374643875,11.9717104200664));
#62241=CARTESIAN_POINT('Ctrl Pts',(2.05086612770534,40.580652204766,12.0002516398698));
#62242=CARTESIAN_POINT('Ctrl Pts',(2.06720854888125,40.5847729704798,12.0291110379928));
#62243=CARTESIAN_POINT('Ctrl Pts',(2.1251107751972,40.5993731026384,12.1313617010662));
#62244=CARTESIAN_POINT('Ctrl Pts',(2.17534849306533,40.6140595297461,12.2376372192857));
#62245=CARTESIAN_POINT('Ctrl Pts',(2.21770338471842,40.6287898647364,12.3467457412031));
#62246=CARTESIAN_POINT('Ctrl Pts',(2.22676037647349,40.6319397375693,12.3700770482811));
#62247=CARTESIAN_POINT('Ctrl Pts',(2.23545679903343,40.635091626804,12.3935380428671));
#62248=CARTESIAN_POINT('Ctrl Pts',(2.24379030937884,40.6382451323147,12.4171172937197));
#62249=CARTESIAN_POINT('Ctrl Pts',(2.28177739974992,40.6526199268315,12.5245998665965));
#62250=CARTESIAN_POINT('Ctrl Pts',(2.31222379200685,40.6670266825246,12.6345367851813));
#62251=CARTESIAN_POINT('Ctrl Pts',(2.33494566400176,40.6813420419667,12.7457804166104));
#62252=CARTESIAN_POINT('Ctrl Pts',(2.34093686488405,40.6851166514768,12.7751126363728));
#62253=CARTESIAN_POINT('Ctrl Pts',(2.3463910825083,40.6888849446716,12.8045359763344));
#62254=CARTESIAN_POINT('Ctrl Pts',(2.35130503246029,40.6926447427818,12.8340299954686));
#62255=CARTESIAN_POINT('Ctrl Pts',(2.3708251816471,40.7075801452054,12.951191883409));
#62256=CARTESIAN_POINT('Ctrl Pts',(2.3818237226639,40.7223757699855,13.0694732144141));
#62257=CARTESIAN_POINT('Ctrl Pts',(2.38389473371903,40.7371193386535,13.1875244947628));
#62258=CARTESIAN_POINT('Ctrl Pts',(2.38425800952661,40.7397055063136,13.2082318560773));
#62259=CARTESIAN_POINT('Ctrl Pts',(2.38434665072993,40.7422900586909,13.2289320216384));
#62260=CARTESIAN_POINT('Ctrl Pts',(2.3841585449045,40.7448734517146,13.2496175621632));
#62261=CARTESIAN_POINT('Ctrl Pts',(2.38380342397982,40.7497505836018,13.2886693473047));
#62262=CARTESIAN_POINT('Ctrl Pts',(2.38246187836942,40.7546234616989,13.3276680242106));
#62263=CARTESIAN_POINT('Ctrl Pts',(2.38012342299583,40.7594914216212,13.3665605088907));
#62264=CARTESIAN_POINT('Ctrl Pts',(2.37908962600529,40.7616434756543,13.3837543087259));
#62265=CARTESIAN_POINT('Ctrl Pts',(2.37786100980895,40.7637945658517,13.4009273349506));
#62266=CARTESIAN_POINT('Ctrl Pts',(2.37643673308905,40.7659446431555,13.4180750779064));
#62267=CARTESIAN_POINT('Ctrl Pts',(2.37233988670818,40.7721292112929,13.4673995298806));
#62268=CARTESIAN_POINT('Ctrl Pts',(2.36662142988896,40.778308975065,13.5165432850552));
#62269=CARTESIAN_POINT('Ctrl Pts',(2.35933309034131,40.7844817243333,13.5654036434861));
#62270=CARTESIAN_POINT('Ctrl Pts',(2.33704875590962,40.8033551053219,13.7147957732856));
#62271=CARTESIAN_POINT('Ctrl Pts',(2.30014819488779,40.8221023500989,13.8615581024037));
#62272=CARTESIAN_POINT('Ctrl Pts',(2.25003614297448,40.8407735714396,14.0033046981994));
#62273=CARTESIAN_POINT('Ctrl Pts',(2.19888350058474,40.8598325058027,14.1479947008606));
#62274=CARTESIAN_POINT('Ctrl Pts',(2.13389124211246,40.878890914239,14.287436632662));
#62275=CARTESIAN_POINT('Ctrl Pts',(2.0566055062284,40.8979317948094,14.4190419642919));
#62276=CARTESIAN_POINT('Ctrl Pts',(1.98146478693575,40.9164442078138,14.5469946733954));
#62277=CARTESIAN_POINT('Ctrl Pts',(1.89470320260612,40.9349397372278,14.6675387394565));
#62278=CARTESIAN_POINT('Ctrl Pts',(1.79776587934872,40.9533860059923,14.7783012426381));
#62279=CARTESIAN_POINT('Ctrl Pts',(1.75293375851325,40.961917140569,14.8295273107799));
#62280=CARTESIAN_POINT('Ctrl Pts',(1.70594716370153,40.9704109181371,14.8786784377205));
#62281=CARTESIAN_POINT('Ctrl Pts',(1.65693321099782,40.9788826648687,14.9255125539089));
#62282=CARTESIAN_POINT('Ctrl Pts',(1.64331612303024,40.9812362910123,14.9385240382893));
#62283=CARTESIAN_POINT('Ctrl Pts',(1.62954199423124,40.9835889418671,14.9513561644984));
#62284=CARTESIAN_POINT('Ctrl Pts',(1.61561341902634,40.9859406848803,14.9640042671608));
#62285=CARTESIAN_POINT('Ctrl Pts',(1.61559001021275,40.9859446372956,14.9640255239709));
#62286=CARTESIAN_POINT('Ctrl Pts',(1.61556660095658,40.9859485897094,14.9640467802669));
#62287=CARTESIAN_POINT('Ctrl Pts',(1.61554319125781,40.9859525421217,14.9640680360489));
#62288=CARTESIAN_POINT('Ctrl Pts',(1.53699799424492,40.9992138406697,15.0353863217062));
#62289=CARTESIAN_POINT('Ctrl Pts',(1.45346874200654,41.0124580741077,15.100913361394));
#62290=CARTESIAN_POINT('Ctrl Pts',(1.36598276713797,41.0256372990086,15.1603283697664));
#62291=CARTESIAN_POINT('Ctrl Pts',(1.30906834718812,41.0342111068876,15.1989810880212));
#62292=CARTESIAN_POINT('Ctrl Pts',(1.25047987467762,41.042757462791,15.2350481158454));
#62293=CARTESIAN_POINT('Ctrl Pts',(1.1905023459014,41.0512638657709,15.26845268478));
#62294=CARTESIAN_POINT('Ctrl Pts',(1.08122052341071,41.0667629241591,15.329317349383));
#62295=CARTESIAN_POINT('Ctrl Pts',(0.967285307371829,41.0821959395283,15.3812831031045));
#62296=CARTESIAN_POINT('Ctrl Pts',(0.850290169753213,41.0976389120642,15.4238000634698));
#62297=CARTESIAN_POINT('Ctrl Pts',(0.795820561512864,41.1048287208136,15.4435947508544));
#62298=CARTESIAN_POINT('Ctrl Pts',(0.740688400621284,41.1120205844328,15.4613411633113));
#62299=CARTESIAN_POINT('Ctrl Pts',(0.68505833144481,41.1192216234386,15.4769835331194));
#62300=CARTESIAN_POINT('Ctrl Pts',(0.571552703550573,41.1339143690336,15.5088996718751));
#62301=CARTESIAN_POINT('Ctrl Pts',(0.455966207734481,41.1486479005713,15.5320595644014));
#62302=CARTESIAN_POINT('Ctrl Pts',(0.339637431692946,41.1634826568834,15.5460020514382));
#62303=CARTESIAN_POINT('Ctrl Pts',(0.325257843037984,41.1653164051684,15.5477255048711));
#62304=CARTESIAN_POINT('Ctrl Pts',(0.310866960743178,41.1671516927431,15.5493080740837));
#62305=CARTESIAN_POINT('Ctrl Pts',(0.296467356775281,41.1689886274585,15.5507488532967));
#62306=CARTESIAN_POINT('Ctrl Pts',(0.226273338322151,41.1779431674308,15.5577722466407));
#62307=CARTESIAN_POINT('Ctrl Pts',(0.155897904900614,41.1867591053219,15.5616485894261));
#62308=CARTESIAN_POINT('Ctrl Pts',(0.0855691817809186,41.1955437231765,
15.5621662701891));
#62309=CARTESIAN_POINT('Ctrl Pts',(0.0721177742732594,41.197223911147,15.5622652842846));
#62310=CARTESIAN_POINT('Ctrl Pts',(0.058668207975929,41.1989029364518,15.5622413560316));
#62311=CARTESIAN_POINT('Ctrl Pts',(0.0452222715730123,41.2005815256376,
15.562092905444));
#62312=CARTESIAN_POINT('Ctrl Pts',(0.0451600061366055,41.2005892988477,
15.5620922179991));
#62313=CARTESIAN_POINT('Ctrl Pts',(0.0450977407922936,41.2005970720496,
15.5620915278801));
#62314=CARTESIAN_POINT('Ctrl Pts',(0.0450354755402967,41.2006048452436,
15.5620908350869));
#62315=CARTESIAN_POINT('Ctrl Pts',(-0.081427957730793,41.2163925399532,
15.5606837419627));
#62316=CARTESIAN_POINT('Ctrl Pts',(-0.207510800809204,41.2321468958339,
15.548240943279));
#62317=CARTESIAN_POINT('Ctrl Pts',(-0.331408562526946,41.2478592715305,
15.525416196154));
#62318=CARTESIAN_POINT('Ctrl Pts',(-0.446691773100654,41.2624791733829,
15.5041784426013));
#62319=CARTESIAN_POINT('Ctrl Pts',(-0.560079211735611,41.277062186552,15.4739576326248));
#62320=CARTESIAN_POINT('Ctrl Pts',(-0.670192647273795,41.2916109840416,
15.4352831102998));
#62321=CARTESIAN_POINT('Ctrl Pts',(-0.706446075772782,41.2964009879767,
15.4225500226162));
#62322=CARTESIAN_POINT('Ctrl Pts',(-0.742344255168313,41.3011872392498,
15.4089006313629));
#62323=CARTESIAN_POINT('Ctrl Pts',(-0.777839298886074,41.3059700276314,
15.394352965456));
#62324=CARTESIAN_POINT('Ctrl Pts',(-0.777878076994723,41.3059752527971,
15.3943370722239));
#62325=CARTESIAN_POINT('Ctrl Pts',(-0.777916854633722,41.3059804779314,
15.3943211779562));
#62326=CARTESIAN_POINT('Ctrl Pts',(-0.777955631802971,41.3059857030343,
15.394305282653));
#62327=CARTESIAN_POINT('Ctrl Pts',(-0.845785815731969,41.3151256091237,
15.3665007429917));
#62328=CARTESIAN_POINT('Ctrl Pts',(-0.912182599394111,41.3241697766217,
15.3355258587009));
#62329=CARTESIAN_POINT('Ctrl Pts',(-0.976793529516771,41.3332125956318,
15.3014564402282));
#62330=CARTESIAN_POINT('Ctrl Pts',(-1.00835275007618,41.3376295622205,15.2848152265841));
#62331=CARTESIAN_POINT('Ctrl Pts',(-1.03948518449441,41.3420461083214,15.2674360359707));
#62332=CARTESIAN_POINT('Ctrl Pts',(-1.07014589413268,41.3464726629492,15.2493300025927));
#62333=CARTESIAN_POINT('Ctrl Pts',(-1.09008732209048,41.3493516511152,15.2375540142197));
#62334=CARTESIAN_POINT('Ctrl Pts',(-1.10982934471936,41.3522356210233,15.2254693704854));
#62335=CARTESIAN_POINT('Ctrl Pts',(-1.12936096218729,41.3551260565641,15.213080737006));
#62336=CARTESIAN_POINT('Ctrl Pts',(-1.18740847623011,41.3637163639424,15.1762620056825));
#62337=CARTESIAN_POINT('Ctrl Pts',(-1.24360031778782,41.3723650434639,15.1367548615641));
#62338=CARTESIAN_POINT('Ctrl Pts',(-1.29777160212577,41.3809771605696,15.0948428402832));
#62339=CARTESIAN_POINT('Ctrl Pts',(-1.3297139369798,41.3860553331061,15.0701292335352));
#62340=CARTESIAN_POINT('Ctrl Pts',(-1.36095461147447,41.3911209143976,15.044579025209));
#62341=CARTESIAN_POINT('Ctrl Pts',(-1.39146671510647,41.3961554986744,15.0182454627002));
#62342=CARTESIAN_POINT('Ctrl Pts',(-1.41900663030876,41.4006996633684,14.9944770563257));
#62343=CARTESIAN_POINT('Ctrl Pts',(-1.44593358249322,41.4052387725666,14.9700461351532));
#62344=CARTESIAN_POINT('Ctrl Pts',(-1.47220672066735,41.4097741167282,14.944977687754));
#62345=CARTESIAN_POINT('Ctrl Pts',(-1.47285119576385,41.4098853678603,14.9443627634937));
#62346=CARTESIAN_POINT('Ctrl Pts',(-1.47349528119897,41.4099966173698,14.9437474520967));
#62347=CARTESIAN_POINT('Ctrl Pts',(-1.4741389764032,41.4101078652536,14.943131753934));
#62348=CARTESIAN_POINT('Ctrl Pts',(-1.55503558920578,41.4240889807296,14.8657536788142));
#62349=CARTESIAN_POINT('Ctrl Pts',(-1.62976666435367,41.4380444185006,14.7822644022364));
#62350=CARTESIAN_POINT('Ctrl Pts',(-1.69765987755627,41.45196673785,14.6938022668145));
#62351=CARTESIAN_POINT('Ctrl Pts',(-1.71610060763517,41.4557482311847,14.6697747346862));
#62352=CARTESIAN_POINT('Ctrl Pts',(-1.73403715537414,41.4595273060083,14.6453803408061));
#62353=CARTESIAN_POINT('Ctrl Pts',(-1.75145650730607,41.4633038406332,14.6206420253425));
#62354=CARTESIAN_POINT('Ctrl Pts',(-1.79941698135957,41.4737017240676,14.552530344635));
#62355=CARTESIAN_POINT('Ctrl Pts',(-1.84345465993251,41.4840795024122,14.4818155892012));
#62356=CARTESIAN_POINT('Ctrl Pts',(-1.88341683573492,41.4943720001996,14.4090078495041));
#62357=CARTESIAN_POINT('Ctrl Pts',(-1.89134100977552,41.4964129186967,14.394570667612));
#62358=CARTESIAN_POINT('Ctrl Pts',(-1.89910502357148,41.498450504055,14.3800510525844));
#62359=CARTESIAN_POINT('Ctrl Pts',(-1.90670780596449,41.5004842780006,14.3654527697682));
#62360=CARTESIAN_POINT('Ctrl Pts',(-1.92203075343397,41.5045832262176,14.3360308148611));
#62361=CARTESIAN_POINT('Ctrl Pts',(-1.93667848735068,41.5086818513199,14.3062737320976));
#62362=CARTESIAN_POINT('Ctrl Pts',(-1.95062893794502,41.5127822756707,14.2762114621491));
#62363=CARTESIAN_POINT('Ctrl Pts',(-1.95303105473353,41.5134883244185,14.271035064236));
#62364=CARTESIAN_POINT('Ctrl Pts',(-1.95541249773989,41.5141944262844,14.2658496199283));
#62365=CARTESIAN_POINT('Ctrl Pts',(-1.95777318849794,41.5149005918288,14.2606553125988));
#62366=CARTESIAN_POINT('Ctrl Pts',(-1.98281014357756,41.522390024722,14.2055656576594));
#62367=CARTESIAN_POINT('Ctrl Pts',(-2.00550484535097,41.5298867889419,14.1494891022725));
#62368=CARTESIAN_POINT('Ctrl Pts',(-2.02573738634781,41.5374229399387,14.0926310802962));
#62369=CARTESIAN_POINT('Ctrl Pts',(-2.04854357092303,41.5459177133163,14.0285405370482));
#62370=CARTESIAN_POINT('Ctrl Pts',(-2.06822067624309,41.5544637764423,13.9634546675661));
#62371=CARTESIAN_POINT('Ctrl Pts',(-2.08482135703504,41.5629839304559,13.8977113934608));
#62372=CARTESIAN_POINT('Ctrl Pts',(-2.09159121163654,41.566458499034,13.8709009022348));
#62373=CARTESIAN_POINT('Ctrl Pts',(-2.09784959854094,41.5699288335508,13.8439805042489));
#62374=CARTESIAN_POINT('Ctrl Pts',(-2.10360055620429,41.5733900089782,13.8169706884938));
#62375=CARTESIAN_POINT('Ctrl Pts',(-2.1236059163137,41.5854301012344,13.723013973404));
#62376=CARTESIAN_POINT('Ctrl Pts',(-2.13742420412686,41.5973875232401,13.6279516650221));
#62377=CARTESIAN_POINT('Ctrl Pts',(-2.14468551498309,41.6093217191047,13.5326515650383));
#62378=CARTESIAN_POINT('Ctrl Pts',(-2.1457745351032,41.6111115583873,13.5183588666006));
#62379=CARTESIAN_POINT('Ctrl Pts',(-2.14671605313871,41.6129008236976,13.5040612353341));
#62380=CARTESIAN_POINT('Ctrl Pts',(-2.14750923793178,41.6146894540213,13.4897620970082));
#62381=CARTESIAN_POINT('Ctrl Pts',(-2.14751278765176,41.6146974586337,13.4896981044337));
#62382=CARTESIAN_POINT('Ctrl Pts',(-2.14751633446029,41.6147054632175,13.4896341117367));
#62383=CARTESIAN_POINT('Ctrl Pts',(-2.14751987835732,41.6147134677728,13.4895701189175));
#62384=CARTESIAN_POINT('Ctrl Pts',(-2.15201532684852,41.6248672803339,13.4083949548605));
#62385=CARTESIAN_POINT('Ctrl Pts',(-2.15182151215461,41.6349749615117,13.327024578324));
#62386=CARTESIAN_POINT('Ctrl Pts',(-2.147149080938,41.6450029527301,13.246018671873));
#62387=CARTESIAN_POINT('Ctrl Pts',(-2.14333727732236,41.6531838614287,13.1799334599599));
#62388=CARTESIAN_POINT('Ctrl Pts',(-2.13654599047871,41.6613117860843,13.1140907826608));
#62389=CARTESIAN_POINT('Ctrl Pts',(-2.12691228998368,41.6693699018129,13.0487826967084));
#62390=CARTESIAN_POINT('Ctrl Pts',(-2.11564878821672,41.6787912659911,12.9724259797956));
#62391=CARTESIAN_POINT('Ctrl Pts',(-2.10033681376959,41.6881990268741,12.8967983660334));
#62392=CARTESIAN_POINT('Ctrl Pts',(-2.08102619939381,41.6976521858791,12.8223395356854));
#62393=CARTESIAN_POINT('Ctrl Pts',(-2.06921096952788,41.7034361161275,12.7767817828873));
#62394=CARTESIAN_POINT('Ctrl Pts',(-2.05589880879169,41.7092369106262,12.7316625943557));
#62395=CARTESIAN_POINT('Ctrl Pts',(-2.04110298493506,41.7150668347247,12.6870920669858));
#62396=CARTESIAN_POINT('Ctrl Pts',(-2.01561930883787,41.7251080395158,12.6103257514374));
#62397=CARTESIAN_POINT('Ctrl Pts',(-1.9857256496552,41.7352391333325,12.5351627453933));
#62398=CARTESIAN_POINT('Ctrl Pts',(-1.9517297894167,41.7454027323094,12.4620609055182));
#62399=CARTESIAN_POINT('Ctrl Pts',(-1.92355032332468,41.7538274284557,12.4014661506399));
#62400=CARTESIAN_POINT('Ctrl Pts',(-1.89255229461433,41.7622745755602,12.3422865252118));
#62401=CARTESIAN_POINT('Ctrl Pts',(-1.85889837851605,41.7707149892952,12.2847589717646));
#62402=CARTESIAN_POINT('Ctrl Pts',(-1.81950911849044,41.7805938292602,12.2174274982222));
#62403=CARTESIAN_POINT('Ctrl Pts',(-1.77648736441405,41.7904611540848,12.1523692608652));
#62404=CARTESIAN_POINT('Ctrl Pts',(-1.73011822727339,41.8002681947985,12.0899959420359));
#62405=CARTESIAN_POINT('Ctrl Pts',(-1.72435025841091,41.8014881162582,12.0822371743934));
#62406=CARTESIAN_POINT('Ctrl Pts',(-1.71853048361876,41.8027071123791,12.0745198867226));
#62407=CARTESIAN_POINT('Ctrl Pts',(-1.71265944073235,41.8039250956661,12.0668448162017));
#62408=CARTESIAN_POINT('Ctrl Pts',(-1.69565312410084,41.807453158709,12.0446128751355));
#62409=CARTESIAN_POINT('Ctrl Pts',(-1.6782168963213,41.8109727231298,12.0227358723218));
#62410=CARTESIAN_POINT('Ctrl Pts',(-1.66036526887978,41.8144806926752,12.0012284753065));
#62411=CARTESIAN_POINT('Ctrl Pts',(-1.6603632194742,41.8144810953977,12.0012260062107));
#62412=CARTESIAN_POINT('Ctrl Pts',(-1.66036117006314,41.8144814981201,12.0012235371197));
#62413=CARTESIAN_POINT('Ctrl Pts',(-1.66035912064661,41.8144819008423,12.0012210680335));
#62414=CARTESIAN_POINT('Ctrl Pts',(-1.60821266638108,41.8247289809986,11.9383963154232));
#62415=CARTESIAN_POINT('Ctrl Pts',(-1.55247647132068,41.83488619402,11.8786714244548));
#62416=CARTESIAN_POINT('Ctrl Pts',(-1.49354549202297,41.8450014026924,11.822404207685));
#62417=CARTESIAN_POINT('Ctrl Pts',(-1.4883815886577,41.8458877609495,11.8174737199603));
#62418=CARTESIAN_POINT('Ctrl Pts',(-1.48319317620903,41.8467737926257,11.8125698063066));
#62419=CARTESIAN_POINT('Ctrl Pts',(-1.47798053339602,41.8476595275812,11.8076927213209));
#62420=CARTESIAN_POINT('Ctrl Pts',(-1.42309820539036,41.8569851610647,11.7563433794429));
#62421=CARTESIAN_POINT('Ctrl Pts',(-1.36553232159843,41.8662768706289,11.7079683961237));
#62422=CARTESIAN_POINT('Ctrl Pts',(-1.30561140899485,41.875578475886,11.6629071708844));
#62423=CARTESIAN_POINT('Ctrl Pts',(-1.27274558510597,41.8806802827007,11.6381916879489));
#62424=CARTESIAN_POINT('Ctrl Pts',(-1.23917201965742,41.8857849530133,11.6144736420939));
#62425=CARTESIAN_POINT('Ctrl Pts',(-1.20495077659448,41.890898885685,11.5918121276779));
#62426=CARTESIAN_POINT('Ctrl Pts',(-1.15638684658384,41.8981561518192,11.5596527990992));
#62427=CARTESIAN_POINT('Ctrl Pts',(-1.10651335019658,41.905433193919,11.5296178064519));
#62428=CARTESIAN_POINT('Ctrl Pts',(-1.0555248004714,41.9127118485166,11.5017548784269));
#62429=CARTESIAN_POINT('Ctrl Pts',(-1.05549913535242,41.912715512232,11.5017408536043));
#62430=CARTESIAN_POINT('Ctrl Pts',(-1.0554734699505,41.9127191759479,11.5017268293321));
#62431=CARTESIAN_POINT('Ctrl Pts',(-1.05544780426564,41.9127228396642,11.5017128056101));
#62432=CARTESIAN_POINT('Ctrl Pts',(-0.974974870225346,41.9242101623427,
11.4577424201886));
#62433=CARTESIAN_POINT('Ctrl Pts',(-0.89180778368217,41.9356890569172,11.4192251624486));
#62434=CARTESIAN_POINT('Ctrl Pts',(-0.806686485525665,41.9471334535082,
11.386287900019));
#62435=CARTESIAN_POINT('Ctrl Pts',(-0.789077040580342,41.9495010098786,
11.37947401299));
#62436=CARTESIAN_POINT('Ctrl Pts',(-0.771383784061609,41.9518671099596,
11.372898926669));
#62437=CARTESIAN_POINT('Ctrl Pts',(-0.753612990007207,41.9542315545212,
11.3665637686692));
#62438=CARTESIAN_POINT('Ctrl Pts',(-0.66263533706061,41.9663363381385,11.3341309013419));
#62439=CARTESIAN_POINT('Ctrl Pts',(-0.569629829803022,41.9783966846349,
11.3079860838203));
#62440=CARTESIAN_POINT('Ctrl Pts',(-0.475465072600727,41.9903866688685,
11.2883103668133));
#62441=CARTESIAN_POINT('Ctrl Pts',(-0.459458822915358,41.99242474221,11.2849658624731));
#62442=CARTESIAN_POINT('Ctrl Pts',(-0.443418960303733,41.9944607979775,
11.2818082466664));
#62443=CARTESIAN_POINT('Ctrl Pts',(-0.427349602979368,41.9964947278661,
11.2788383836326));
#62444=CARTESIAN_POINT('Ctrl Pts',(-0.390917916437925,42.0011059574662,
11.2721052506931));
#62445=CARTESIAN_POINT('Ctrl Pts',(-0.354335452180833,42.0057062529319,
11.2663376977822));
#62446=CARTESIAN_POINT('Ctrl Pts',(-0.317651724132881,42.0102945165577,
11.2615471228867));
#62447=CARTESIAN_POINT('Ctrl Pts',(-0.317649527816609,42.0102947912647,
11.2615468360669));
#62448=CARTESIAN_POINT('Ctrl Pts',(-0.317647331499938,42.0102950659717,
11.2615465492507));
#62449=CARTESIAN_POINT('Ctrl Pts',(-0.317645135182867,42.0102953406786,
11.2615462624379));
#62450=CARTESIAN_POINT('Ctrl Pts',(-0.249506701873501,42.0188178357928,
11.252648197594));
#62451=CARTESIAN_POINT('Ctrl Pts',(-0.180978975914568,42.0273035867772,
11.2471157665343));
#62452=CARTESIAN_POINT('Ctrl Pts',(-0.112414609941067,42.0357869027238,
11.2450258022412));
#62453=CARTESIAN_POINT('Ctrl Pts',(-0.0766654418275343,42.0402100674921,
11.2439361037687));
#62454=CARTESIAN_POINT('Ctrl Pts',(-0.040907166826984,42.0446324668788,
11.2437821724988));
#62455=CARTESIAN_POINT('Ctrl Pts',(-0.00519524463400642,42.0490582852264,
11.2445737716325));
#62456=CARTESIAN_POINT('Ctrl Pts',(0.031375385536169,42.0535905242114,11.2453844050956));
#62457=CARTESIAN_POINT('Ctrl Pts',(0.0678999347651532,42.0581266875243,
11.2471866328337));
#62458=CARTESIAN_POINT('Ctrl Pts',(0.104323051734636,42.0626716287559,11.2499903668977));
#62459=CARTESIAN_POINT('Ctrl Pts',(0.178549888398028,42.0719337852793,11.2557041093705));
#62460=CARTESIAN_POINT('Ctrl Pts',(0.252359763212599,42.0812335714815,11.2655798042766));
#62461=CARTESIAN_POINT('Ctrl Pts',(0.325315592533385,42.0905367642454,11.2794198507996));
#62462=CARTESIAN_POINT('Ctrl Pts',(0.354711087375632,42.094285223518,11.2849963074031));
#62463=CARTESIAN_POINT('Ctrl Pts',(0.383968515541066,42.0980343105421,11.2912164383134));
#62464=CARTESIAN_POINT('Ctrl Pts',(0.413061600809365,42.1017820899529,11.2980678380498));
#62465=CARTESIAN_POINT('Ctrl Pts',(0.482481934639655,42.1107248368437,11.3144162745432));
#62466=CARTESIAN_POINT('Ctrl Pts',(0.550962843439977,42.1196590721596,11.3343571753581));
#62467=CARTESIAN_POINT('Ctrl Pts',(0.618117926916335,42.1285530190561,11.3577013517488));
#62468=CARTESIAN_POINT('Ctrl Pts',(0.643243679210771,42.1318806466172,11.3664354633476));
#62469=CARTESIAN_POINT('Ctrl Pts',(0.668184354966428,42.1352026955231,11.3756459489252));
#62470=CARTESIAN_POINT('Ctrl Pts',(0.692921584537619,42.1385177210261,11.3853229296319));
#62471=CARTESIAN_POINT('Ctrl Pts',(0.692939560513565,42.1385201299789,11.3853299616713));
#62472=CARTESIAN_POINT('Ctrl Pts',(0.69295753638213,42.138522538928,11.385336993957));
#62473=CARTESIAN_POINT('Ctrl Pts',(0.692975512143297,42.1385249478734,11.3853440264891));
#62474=CARTESIAN_POINT('Ctrl Pts',(0.763650395731234,42.1479961426866,11.4129936697879));
#62475=CARTESIAN_POINT('Ctrl Pts',(0.83277045242766,42.1574232662154,11.4444904798113));
#62476=CARTESIAN_POINT('Ctrl Pts',(0.899894377043377,42.1668266383785,11.4796363913641));
#62477=CARTESIAN_POINT('Ctrl Pts',(0.947822006023835,42.1735408067585,11.5047311726768));
#62478=CARTESIAN_POINT('Ctrl Pts',(0.994731099116168,42.1802427486524,11.53168562757));
#62479=CARTESIAN_POINT('Ctrl Pts',(1.04045131454124,42.1869380742162,11.5604147064339));
#62480=CARTESIAN_POINT('Ctrl Pts',(1.10548782309154,42.1964621019189,11.601281508259));
#62481=CARTESIAN_POINT('Ctrl Pts',(1.16811995715933,42.2059740216997,11.6457435079751));
#62482=CARTESIAN_POINT('Ctrl Pts',(1.22789007894113,42.2154964115977,11.693577895516));
#62483=CARTESIAN_POINT('Ctrl Pts',(1.26131603094944,42.2208217303062,11.7203288857202));
#62484=CARTESIAN_POINT('Ctrl Pts',(1.29384607028539,42.2261502030454,11.7481341423429));
#62485=CARTESIAN_POINT('Ctrl Pts',(1.3253946185824,42.2314848597499,11.7769503010397));
#62486=CARTESIAN_POINT('Ctrl Pts',(1.37375156243058,42.239661708088,11.8211190962217));
#62487=CARTESIAN_POINT('Ctrl Pts',(1.41981048771004,42.2478544794227,11.8676700248371));
#62488=CARTESIAN_POINT('Ctrl Pts',(1.46342795372799,42.2560397529707,11.9163149769343));
#62489=CARTESIAN_POINT('Ctrl Pts',(1.47943059990831,42.2590428168448,11.934162138357));
#62490=CARTESIAN_POINT('Ctrl Pts',(1.49510493384772,42.2620449351324,11.9522915536643));
#62491=CARTESIAN_POINT('Ctrl Pts',(1.51044488246768,42.2650451729185,11.9706904195566));
#62492=CARTESIAN_POINT('Ctrl Pts',(1.51049483357141,42.2650549425203,11.9707503313387));
#62493=CARTESIAN_POINT('Ctrl Pts',(1.51054478112997,42.2650647121022,11.9708102459786));
#62494=CARTESIAN_POINT('Ctrl Pts',(1.51059472514333,42.2650744816642,11.9708701634757));
#62495=CARTESIAN_POINT('Ctrl Pts',(1.59683622386887,42.2819442047123,12.074333509788));
#62496=CARTESIAN_POINT('Ctrl Pts',(1.67243490577711,42.2987396556532,12.1862255054654));
#62497=CARTESIAN_POINT('Ctrl Pts',(1.73631215842149,42.3154757047293,12.3041221328013));
#62498=CARTESIAN_POINT('Ctrl Pts',(1.79428034222021,42.3306635584449,12.4111125414325));
#62499=CARTESIAN_POINT('Ctrl Pts',(1.84259533597738,42.3458027937175,12.5230481751928));
#62500=CARTESIAN_POINT('Ctrl Pts',(1.88042817925358,42.3609092433609,12.6381457050623));
#62501=CARTESIAN_POINT('Ctrl Pts',(1.88540868050647,42.3628979305665,12.6532977090376));
#62502=CARTESIAN_POINT('Ctrl Pts',(1.89020746677454,42.3648860410024,12.6685044613407));
#62503=CARTESIAN_POINT('Ctrl Pts',(1.89482259963009,42.3668736029749,12.6837618462973));
#62504=CARTESIAN_POINT('Ctrl Pts',(1.91305124808663,42.3747239877019,12.7440247933123));
#62505=CARTESIAN_POINT('Ctrl Pts',(1.92841526796983,42.3825660203068,12.8050790443732));
#62506=CARTESIAN_POINT('Ctrl Pts',(1.94079431330655,42.3904018914181,12.8666749392279));
#62507=CARTESIAN_POINT('Ctrl Pts',(1.94080538279298,42.3904088983452,12.866730018994));
#62508=CARTESIAN_POINT('Ctrl Pts',(1.9408164498923,42.3904159052674,12.866785099193));
#62509=CARTESIAN_POINT('Ctrl Pts',(1.94082751460454,42.3904229121846,12.8668401798248));
#62510=CARTESIAN_POINT('Ctrl Pts',(1.94475934098526,42.3929128081224,12.8864129871634));
#62511=CARTESIAN_POINT('Ctrl Pts',(1.94838922236558,42.39540175289,12.9060378691002));
#62512=CARTESIAN_POINT('Ctrl Pts',(1.95171349888433,42.3978902143845,12.9257067365807));
#62513=CARTESIAN_POINT('Ctrl Pts',(1.96761896503129,42.4097966065981,13.0198151851698));
#62514=CARTESIAN_POINT('Ctrl Pts',(1.97652941610515,42.4216924760102,13.1149342117459));
#62515=CARTESIAN_POINT('Ctrl Pts',(1.97863244733539,42.4335719581307,13.2100822071488));
#62516=CARTESIAN_POINT('Ctrl Pts',(1.97948496302688,42.438387599843,13.2486527989349));
#62517=CARTESIAN_POINT('Ctrl Pts',(1.97921872054168,42.4432006194967,13.2872287404352));
#62518=CARTESIAN_POINT('Ctrl Pts',(1.97784553494189,42.4480109165588,13.3257469651751));
#62519=CARTESIAN_POINT('Ctrl Pts',(1.97429488067168,42.4604489306242,13.4253437707157));
#62520=CARTESIAN_POINT('Ctrl Pts',(1.96334565529604,42.4728680349482,13.5245510557992));
#62521=CARTESIAN_POINT('Ctrl Pts',(1.94519022359318,42.4852628635351,13.622239251103));
#62522=CARTESIAN_POINT('Ctrl Pts',(1.93863348315691,42.4897391918939,13.6575188385442));
#62523=CARTESIAN_POINT('Ctrl Pts',(1.93113692151219,42.4942124162428,13.6926007850153));
#62524=CARTESIAN_POINT('Ctrl Pts',(1.922709587364,42.4986824947968,13.7274335506639));
#62525=CARTESIAN_POINT('Ctrl Pts',(1.91286572512561,42.5039039369167,13.7681212628631));
#62526=CARTESIAN_POINT('Ctrl Pts',(1.90175154041046,42.5091209489411,13.8084675312016));
#62527=CARTESIAN_POINT('Ctrl Pts',(1.88938058275007,42.5143332820113,13.8483877905191));
#62528=CARTESIAN_POINT('Ctrl Pts',(1.88936713991042,42.5143389459671,13.8484311696705));
#62529=CARTESIAN_POINT('Ctrl Pts',(1.88935369558682,42.5143446099174,13.848474548319));
#62530=CARTESIAN_POINT('Ctrl Pts',(1.88934024977934,42.5143502738622,13.8485179264645));
#62531=CARTESIAN_POINT('Ctrl Pts',(1.87077278763808,42.5221716769888,13.9084192805149));
#62532=CARTESIAN_POINT('Ctrl Pts',(1.8493691554294,42.5299879209432,13.9674068716725));
#62533=CARTESIAN_POINT('Ctrl Pts',(1.82517111605764,42.5377988314389,14.0251660285722));
#62534=CARTESIAN_POINT('Ctrl Pts',(1.81388311926842,42.5414424957557,14.0521097477561));
#62535=CARTESIAN_POINT('Ctrl Pts',(1.80198745247787,42.5450849110612,14.0787855396012));
#62536=CARTESIAN_POINT('Ctrl Pts',(1.78949078968044,42.54872559605,14.1051584724611));
#62537=CARTESIAN_POINT('Ctrl Pts',(1.77448006045558,42.5530987104923,14.1368370862194));
#62538=CARTESIAN_POINT('Ctrl Pts',(1.75860107719396,42.5574696300421,14.1680808381114));
#62539=CARTESIAN_POINT('Ctrl Pts',(1.7418644439805,42.5618380058926,14.1988332167171));
#62540=CARTESIAN_POINT('Ctrl Pts',(1.71247101624427,42.5695098917641,14.2528415591798));
#62541=CARTESIAN_POINT('Ctrl Pts',(1.68042916372249,42.5771742446803,14.3053352714451));
#62542=CARTESIAN_POINT('Ctrl Pts',(1.6460207588783,42.5848284344902,14.3561499430919));
#62543=CARTESIAN_POINT('Ctrl Pts',(1.62916427312265,42.5885781794169,14.3810437675127));
#62544=CARTESIAN_POINT('Ctrl Pts',(1.61173942472271,42.592325583695,14.405535313502));
#62545=CARTESIAN_POINT('Ctrl Pts',(1.59377670300584,42.5960709051086,14.4296089222223));
#62546=CARTESIAN_POINT('Ctrl Pts',(1.55914873649875,42.6032910172114,14.4760172633198));
#62547=CARTESIAN_POINT('Ctrl Pts',(1.52271985975815,42.6105013040806,14.5209829604909));
#62548=CARTESIAN_POINT('Ctrl Pts',(1.48447273530543,42.617706601848,14.5642671857303));
#62549=CARTESIAN_POINT('Ctrl Pts',(1.46168436591892,42.6219996562779,14.5900567562531));
#62550=CARTESIAN_POINT('Ctrl Pts',(1.4382509215297,42.626290816224,14.6152484881778));
#62551=CARTESIAN_POINT('Ctrl Pts',(1.41417332299015,42.6305800124311,14.6397844353151));
#62552=CARTESIAN_POINT('Ctrl Pts',(1.40214956548563,42.6327219309865,14.6520370807788));
#62553=CARTESIAN_POINT('Ctrl Pts',(1.38996570285484,42.634863262063,14.6641256142807));
#62554=CARTESIAN_POINT('Ctrl Pts',(1.37762576359211,42.6370038984529,14.6760444996634));
#62555=CARTESIAN_POINT('Ctrl Pts',(1.31200813933492,42.6483867319751,14.7394231700081));
#62556=CARTESIAN_POINT('Ctrl Pts',(1.2418649492262,42.6597688584519,14.7981076923313));
#62557=CARTESIAN_POINT('Ctrl Pts',(1.16804459840713,42.6711396652326,14.8515972801294));
#62558=CARTESIAN_POINT('Ctrl Pts',(1.09738226872308,42.6820240309745,14.902798593124));
#62559=CARTESIAN_POINT('Ctrl Pts',(1.02335923147554,42.6928970547553,14.9492371895748));
#62560=CARTESIAN_POINT('Ctrl Pts',(0.946697171476419,42.7037561622759,14.9905293134562));
#62561=CARTESIAN_POINT('Ctrl Pts',(0.913311298611611,42.7084852392549,15.008511788728));
#62562=CARTESIAN_POINT('Ctrl Pts',(0.879424674105818,42.7132117248894,15.0255185420544));
#62563=CARTESIAN_POINT('Ctrl Pts',(0.84509668278392,42.7179354752911,15.0415187184684));
#62564=CARTESIAN_POINT('Ctrl Pts',(0.774769865368988,42.7276128936084,15.0742978424994));
#62565=CARTESIAN_POINT('Ctrl Pts',(0.702716449912161,42.7372903507808,15.1030452829988));
#62566=CARTESIAN_POINT('Ctrl Pts',(0.629302381291837,42.7469761521853,15.1274709114355));
#62567=CARTESIAN_POINT('Ctrl Pts',(0.608107942487717,42.7497724162937,15.1345225228894));
#62568=CARTESIAN_POINT('Ctrl Pts',(0.586800226012909,42.7525693460874,15.1412136224501));
#62569=CARTESIAN_POINT('Ctrl Pts',(0.565388389919398,42.7553670690054,15.1475365058111));
#62570=CARTESIAN_POINT('Ctrl Pts',(0.55718087964312,42.7564394823892,15.1499601713919));
#62571=CARTESIAN_POINT('Ctrl Pts',(0.548957102893311,42.7575118763432,15.1523278304504));
#62572=CARTESIAN_POINT('Ctrl Pts',(0.540717629607357,42.7585842514268,15.1546390187087));
#62573=CARTESIAN_POINT('Ctrl Pts',(0.540695318249796,42.7585871552707,15.1546452770878));
#62574=CARTESIAN_POINT('Ctrl Pts',(0.540673006777153,42.7585900591144,15.1546515350528));
#62575=CARTESIAN_POINT('Ctrl Pts',(0.54065069518942,42.758592962958,15.1546577926038));
#62576=CARTESIAN_POINT('Ctrl Pts',(0.49246290568457,42.7648645831174,15.1681726330802));
#62577=CARTESIAN_POINT('Ctrl Pts',(0.443780012972278,42.7711302171204,15.1797449878543));
#62578=CARTESIAN_POINT('Ctrl Pts',(0.394732848316695,42.7773801057318,15.1892846520821));
#62579=CARTESIAN_POINT('Ctrl Pts',(0.323682173577829,42.7864338156862,15.20310399485));
#62580=CARTESIAN_POINT('Ctrl Pts',(0.251860925182453,42.7954548674434,15.2126560886557));
#62581=CARTESIAN_POINT('Ctrl Pts',(0.179759012530397,42.8044535753376,15.218064782161));
#62582=CARTESIAN_POINT('Ctrl Pts',(0.142098641767993,42.8091537928937,15.2208898584351));
#62583=CARTESIAN_POINT('Ctrl Pts',(0.104360829440141,42.8138480236583,15.2225845865189));
#62584=CARTESIAN_POINT('Ctrl Pts',(0.0666098022250313,42.8185384501019,
15.2231662273549));
#62585=CARTESIAN_POINT('Ctrl Pts',(0.00168799995770721,42.826604745527,
15.2241664960661));
#62586=CARTESIAN_POINT('Ctrl Pts',(-0.0632696613322676,42.8346597279797,
15.2218763741639));
#62587=CARTESIAN_POINT('Ctrl Pts',(-0.127904922426963,42.8427160306386,
15.2164300042142));
#62588=CARTESIAN_POINT('Ctrl Pts',(-0.172040947023254,42.8482172565373,
15.2127109642663));
#62589=CARTESIAN_POINT('Ctrl Pts',(-0.216027677298764,42.8537192316855,
15.20752059654));
#62590=CARTESIAN_POINT('Ctrl Pts',(-0.259764820855651,42.8592277004498,
15.2009032833102));
#62591=CARTESIAN_POINT('Ctrl Pts',(-0.312212838029759,42.8658332590405,
15.1929680381227));
#62592=CARTESIAN_POINT('Ctrl Pts',(-0.364301538169402,42.8724449833506,
15.182955242973));
#62593=CARTESIAN_POINT('Ctrl Pts',(-0.415828148376253,42.879049848528,15.1707954835916));
#62594=CARTESIAN_POINT('Ctrl Pts',(-0.41587164670824,42.8790554242997,15.1707852184247));
#62595=CARTESIAN_POINT('Ctrl Pts',(-0.415915144672645,42.8790610000708,
15.1707749517203));
#62596=CARTESIAN_POINT('Ctrl Pts',(-0.415958642269399,42.8790665758413,
15.1707646834784));
#62597=CARTESIAN_POINT('Ctrl Pts',(-0.473867314471872,42.8864896402445,
15.157094497067));
#62598=CARTESIAN_POINT('Ctrl Pts',(-0.5311200159653,42.8939109955232,15.1406994155213));
#62599=CARTESIAN_POINT('Ctrl Pts',(-0.587498039973528,42.9013502931383,
15.1218310232062));
#62600=CARTESIAN_POINT('Ctrl Pts',(-0.614661409572605,42.9049346044765,
15.1127400853238));
#62601=CARTESIAN_POINT('Ctrl Pts',(-0.641622503810247,42.9085231761516,
15.1030749623491));
#62602=CARTESIAN_POINT('Ctrl Pts',(-0.668361108099995,42.9121187362383,
15.0928631758522));
#62603=CARTESIAN_POINT('Ctrl Pts',(-0.735732438505744,42.9211782093495,
15.0671332748199));
#62604=CARTESIAN_POINT('Ctrl Pts',(-0.801662743307208,42.930256284252,15.0377558250763));
#62605=CARTESIAN_POINT('Ctrl Pts',(-0.865742422457812,42.9393440302551,
15.0048247434824));
#62606=CARTESIAN_POINT('Ctrl Pts',(-0.865793964183904,42.9393513398753,
15.0047982557594));
#62607=CARTESIAN_POINT('Ctrl Pts',(-0.865845504710373,42.9393586495015,
15.0047717657375));
#62608=CARTESIAN_POINT('Ctrl Pts',(-0.865897044036977,42.9393659591336,
15.0047452734168));
#62609=CARTESIAN_POINT('Ctrl Pts',(-0.926015645569417,42.9478923581244,
14.9738430210856));
#62610=CARTESIAN_POINT('Ctrl Pts',(-0.984497013294306,42.9564230042295,
14.9397834670354));
#62611=CARTESIAN_POINT('Ctrl Pts',(-1.04094057269787,42.9649284253592,14.9026580519905));
#62612=CARTESIAN_POINT('Ctrl Pts',(-1.08152164931343,42.9710435454927,14.8759660905295));
#62613=CARTESIAN_POINT('Ctrl Pts',(-1.1210493387345,42.9771455625012,14.8476894911776));
#62614=CARTESIAN_POINT('Ctrl Pts',(-1.15937493671053,42.9832234671643,14.8178640118327));
#62615=CARTESIAN_POINT('Ctrl Pts',(-1.16231162737626,42.9836891852961,14.8155786409209));
#62616=CARTESIAN_POINT('Ctrl Pts',(-1.16524125182036,42.9841547599697,14.8132841750208));
#62617=CARTESIAN_POINT('Ctrl Pts',(-1.16816373353031,42.9846201857316,14.8109806493365));
#62618=CARTESIAN_POINT('Ctrl Pts',(-1.18014962096974,42.9865290225858,14.801533267862));
#62619=CARTESIAN_POINT('Ctrl Pts',(-1.19201536446151,42.9884353555117,14.7919334860694));
#62620=CARTESIAN_POINT('Ctrl Pts',(-1.2037547431206,42.9903387901022,14.7821837380565));
#62621=CARTESIAN_POINT('Ctrl Pts',(-1.22277701629086,42.9934230804889,14.7663854257755));
#62622=CARTESIAN_POINT('Ctrl Pts',(-1.24146787534786,42.996499826126,14.7501930759828));
#62623=CARTESIAN_POINT('Ctrl Pts',(-1.25981365272742,42.9995712552817,14.7336289146085));
#62624=CARTESIAN_POINT('Ctrl Pts',(-1.25992537907663,42.9995899603799,14.7335280383556));
#62625=CARTESIAN_POINT('Ctrl Pts',(-1.26003709263278,42.9996086652816,14.7334271483098));
#62626=CARTESIAN_POINT('Ctrl Pts',(-1.26014879339496,42.9996273699875,14.7333262444771));
#62627=CARTESIAN_POINT('Ctrl Pts',(-1.31609084749496,43.0089950739053,14.6827915162186));
#62628=CARTESIAN_POINT('Ctrl Pts',(-1.36878818457866,43.0183093018439,14.628856664969));
#62629=CARTESIAN_POINT('Ctrl Pts',(-1.41805397503608,43.0275946032795,14.5720258357116));
#62630=CARTESIAN_POINT('Ctrl Pts',(-1.43876420354246,43.0314979348346,14.54813543531));
#62631=CARTESIAN_POINT('Ctrl Pts',(-1.45886824080916,43.0353962218378,14.5237326689404));
#62632=CARTESIAN_POINT('Ctrl Pts',(-1.47835292496802,43.0392915793856,14.4988523605217));
#62633=CARTESIAN_POINT('Ctrl Pts',(-1.5252709700236,43.0486713855679,14.4389419497667));
#62634=CARTESIAN_POINT('Ctrl Pts',(-1.56859813794963,43.0580345049384,14.3762657123884));
#62635=CARTESIAN_POINT('Ctrl Pts',(-1.6081341418334,43.067409278086,14.3113441550447));
#62636=CARTESIAN_POINT('Ctrl Pts',(-1.62926440674908,43.0724196843151,14.276646422076));
#62637=CARTESIAN_POINT('Ctrl Pts',(-1.64931230767255,43.0774335321756,14.2413066347036));
#62638=CARTESIAN_POINT('Ctrl Pts',(-1.6682503056147,43.0824559227731,14.2053990062672));
#62639=CARTESIAN_POINT('Ctrl Pts',(-1.69949928782609,43.0907432082041,14.146148981756));
#62640=CARTESIAN_POINT('Ctrl Pts',(-1.72778401534493,43.0990713486404,14.0853959924843));
#62641=CARTESIAN_POINT('Ctrl Pts',(-1.75280261215093,43.1074088827253,14.0233804035923));
#62642=CARTESIAN_POINT('Ctrl Pts',(-1.76332832940544,43.1109166144761,13.9972894697517));
#62643=CARTESIAN_POINT('Ctrl Pts',(-1.77327566205206,43.1144259286465,13.9709756242431));
#62644=CARTESIAN_POINT('Ctrl Pts',(-1.78262119037841,43.1179341333482,13.944459332879));
#62645=CARTESIAN_POINT('Ctrl Pts',(-1.78263305732695,43.1179385880653,13.9444256625017));
#62646=CARTESIAN_POINT('Ctrl Pts',(-1.78264492337347,43.1179430428018,13.9443919917987));
#62647=CARTESIAN_POINT('Ctrl Pts',(-1.78265678851792,43.1179474975577,13.9443583207702));
#62648=CARTESIAN_POINT('Ctrl Pts',(-1.80401722676052,43.1259672515009,13.8837414501733));
#62649=CARTESIAN_POINT('Ctrl Pts',(-1.82245389414707,43.1340504487419,13.8220649991582));
#62650=CARTESIAN_POINT('Ctrl Pts',(-1.83781262195428,43.142160944959,13.7596376484174));
#62651=CARTESIAN_POINT('Ctrl Pts',(-1.8453470093919,43.1461396352241,13.7290132468987));
#62652=CARTESIAN_POINT('Ctrl Pts',(-1.85214072866539,43.1501248052658,13.6982089385095));
#62653=CARTESIAN_POINT('Ctrl Pts',(-1.85817623987287,43.1541116697546,13.6672656690419));
#62654=CARTESIAN_POINT('Ctrl Pts',(-1.87103315614179,43.1626045349232,13.60134995603));
#62655=CARTESIAN_POINT('Ctrl Pts',(-1.88042368888652,43.1710975472846,13.5347904585874));
#62656=CARTESIAN_POINT('Ctrl Pts',(-1.88619439323734,43.179549508963,13.4679553974391));
#62657=CARTESIAN_POINT('Ctrl Pts',(-1.88869853933062,43.1832171629495,13.4389529140169));
#62658=CARTESIAN_POINT('Ctrl Pts',(-1.89052098216898,43.1868770013553,13.4098991996398));
#62659=CARTESIAN_POINT('Ctrl Pts',(-1.89164915444521,43.190525266468,13.3808273721726));
#62660=CARTESIAN_POINT('Ctrl Pts',(-1.89269316585455,43.1939013735414,13.353924282808));
#62661=CARTESIAN_POINT('Ctrl Pts',(-1.89314293463907,43.1972678116781,13.3270043227245));
#62662=CARTESIAN_POINT('Ctrl Pts',(-1.89298914402905,43.2006220825191,13.3000918639857));
#62663=CARTESIAN_POINT('Ctrl Pts',(-1.89264191636583,43.2081953382971,13.2393290504546));
#62664=CARTESIAN_POINT('Ctrl Pts',(-1.88921587375014,43.2157069487255,13.1785964328137));
#62665=CARTESIAN_POINT('Ctrl Pts',(-1.88282612266878,43.2232009630549,13.1181934879298));
#62666=CARTESIAN_POINT('Ctrl Pts',(-1.87889104701324,43.2278160901506,13.0809948310636));
#62667=CARTESIAN_POINT('Ctrl Pts',(-1.87383201706931,43.2324246738829,13.0439201696221));
#62668=CARTESIAN_POINT('Ctrl Pts',(-1.86767488783895,43.2370382462145,13.0070297509779));
#62669=CARTESIAN_POINT('Ctrl Pts',(-1.86766817257427,43.2370432780009,13.0069895164927));
#62670=CARTESIAN_POINT('Ctrl Pts',(-1.86766145600323,43.2370483097934,13.0069492822259));
#62671=CARTESIAN_POINT('Ctrl Pts',(-1.86765473812588,43.2370533415919,13.0069090481776));
#62672=CARTESIAN_POINT('Ctrl Pts',(-1.85150139867034,43.2491524534186,12.9101650610084));
#62673=CARTESIAN_POINT('Ctrl Pts',(-1.82779225177506,43.2612687901266,12.8147726777807));
#62674=CARTESIAN_POINT('Ctrl Pts',(-1.79706272814456,43.2734283523782,12.7217319802806));
#62675=CARTESIAN_POINT('Ctrl Pts',(-1.76578946767481,43.2858030693463,12.6270449944947));
#62676=CARTESIAN_POINT('Ctrl Pts',(-1.72724459925867,43.2982226939109,12.534792539745));
#62677=CARTESIAN_POINT('Ctrl Pts',(-1.68194441752588,43.3107058267891,12.446038338779));
#62678=CARTESIAN_POINT('Ctrl Pts',(-1.63731684090383,43.3230036134137,12.3586019367024));
#62679=CARTESIAN_POINT('Ctrl Pts',(-1.58613233761101,43.3353632126334,12.2745597643092));
#62680=CARTESIAN_POINT('Ctrl Pts',(-1.52884857878348,43.3477916956768,12.1949531992576));
#62681=CARTESIAN_POINT('Ctrl Pts',(-1.51695804136936,43.3503715079246,12.1784290594398));
#62682=CARTESIAN_POINT('Ctrl Pts',(-1.5048046046168,43.3529542449554,12.1620961448403));
#62683=CARTESIAN_POINT('Ctrl Pts',(-1.49239220489772,43.355539897961,12.145963956135));
#62684=CARTESIAN_POINT('Ctrl Pts',(-1.49236250936106,43.3555460839005,12.1459253613418));
#62685=CARTESIAN_POINT('Ctrl Pts',(-1.49233281234219,43.3555522698567,12.1458867676974));
#62686=CARTESIAN_POINT('Ctrl Pts',(-1.49230311384122,43.3555584558296,12.145848175202));
#62687=CARTESIAN_POINT('Ctrl Pts',(-1.4545347737477,43.3634253150821,12.0967691158786));
#62688=CARTESIAN_POINT('Ctrl Pts',(-1.41435409216997,43.3713267067413,12.0495178634875));
#62689=CARTESIAN_POINT('Ctrl Pts',(-1.37191233999428,43.3792042996883,12.004384183538));
#62690=CARTESIAN_POINT('Ctrl Pts',(-1.35676188097806,43.3820163690062,11.9882727853682));
#62691=CARTESIAN_POINT('Ctrl Pts',(-1.34132370425351,43.3848253487554,11.9724314847919));
#62692=CARTESIAN_POINT('Ctrl Pts',(-1.32560608944061,43.3876283966831,11.9568742317137));
#62693=CARTESIAN_POINT('Ctrl Pts',(-1.282771636548,43.395267407172,11.9144768048746));
#62694=CARTESIAN_POINT('Ctrl Pts',(-1.23785644605668,43.4028629014454,11.8741844741578));
#62695=CARTESIAN_POINT('Ctrl Pts',(-1.19101162640978,43.4103642763285,11.8362520488016));
#62696=CARTESIAN_POINT('Ctrl Pts',(-1.14129719018095,43.418325169893,11.7959959616699));
#62697=CARTESIAN_POINT('Ctrl Pts',(-1.08940463871221,43.4261804547596,11.7583952441686));
#62698=CARTESIAN_POINT('Ctrl Pts',(-1.03570065855932,43.4339861919705,11.7235726644063));
#62699=CARTESIAN_POINT('Ctrl Pts',(-1.01736716360115,43.436650918931,11.7116849125361));
#62700=CARTESIAN_POINT('Ctrl Pts',(-0.998822227914527,43.4393099284136,
11.7001206320748));
#62701=CARTESIAN_POINT('Ctrl Pts',(-0.980079346897465,43.4419656268008,
11.6888838730866));
#62702=CARTESIAN_POINT('Ctrl Pts',(-0.927109714832717,43.4494709492919,
11.6571274430767));
#62703=CARTESIAN_POINT('Ctrl Pts',(-0.872562133097849,43.4569503499513,
11.6279886360763));
#62704=CARTESIAN_POINT('Ctrl Pts',(-0.816783143296509,43.4644537234662,
11.6015690506751));
#62705=CARTESIAN_POINT('Ctrl Pts',(-0.795010087872118,43.467382628561,11.5912562949354));
#62706=CARTESIAN_POINT('Ctrl Pts',(-0.773049086495344,43.4703152480498,
11.5813574036137));
#62707=CARTESIAN_POINT('Ctrl Pts',(-0.750919415419833,43.473254785114,11.5718767440723));
#62708=CARTESIAN_POINT('Ctrl Pts',(-0.685059041735581,43.4820031758537,
11.5436612419964));
#62709=CARTESIAN_POINT('Ctrl Pts',(-0.617659340501183,43.4908538709827,
11.5190612043455));
#62710=CARTESIAN_POINT('Ctrl Pts',(-0.549098729605882,43.4997554578476,
11.498242316879));
#62711=CARTESIAN_POINT('Ctrl Pts',(-0.524316113045828,43.5029731160797,
11.4907169098188));
#62712=CARTESIAN_POINT('Ctrl Pts',(-0.499382239716299,43.5061973623746,
11.4836857953846));
#62713=CARTESIAN_POINT('Ctrl Pts',(-0.474316482522037,43.5094255604747,
11.4771575059488));
#62714=CARTESIAN_POINT('Ctrl Pts',(-0.379305501034998,43.521661946056,11.4524122256878));
#62715=CARTESIAN_POINT('Ctrl Pts',(-0.282348593018896,43.5339000509646,
11.4349928797521));
#62716=CARTESIAN_POINT('Ctrl Pts',(-0.184667622219309,43.5461382098195,
11.4251095300764));
#62717=CARTESIAN_POINT('Ctrl Pts',(-0.090103312372126,43.5579858914758,
11.4155415238065));
#62718=CARTESIAN_POINT('Ctrl Pts',(0.00509447066960697,43.5699008208718,
11.4129073060295));
#62719=CARTESIAN_POINT('Ctrl Pts',(0.0999221662935547,43.5819092658192,
11.4173630715372));
#62720=CARTESIAN_POINT('Ctrl Pts',(0.124869565019585,43.5850684637963,11.4185353003678));
#62721=CARTESIAN_POINT('Ctrl Pts',(0.149793319885776,43.5882296589615,11.420206805125));
#62722=CARTESIAN_POINT('Ctrl Pts',(0.174675120256322,43.5913923188329,11.4223828576123));
#62723=CARTESIAN_POINT('Ctrl Pts',(0.174677432364299,43.5913926127188,11.4223830598191));
#62724=CARTESIAN_POINT('Ctrl Pts',(0.174679744471885,43.5913929066048,11.4223832620302));
#62725=CARTESIAN_POINT('Ctrl Pts',(0.174682056579137,43.5913932004907,11.4223834642457));
#62726=CARTESIAN_POINT('Ctrl Pts',(0.234958923058415,43.5990548367109,11.4276552418788));
#62727=CARTESIAN_POINT('Ctrl Pts',(0.29495787247848,43.6067330495829,11.4358646026484));
#62728=CARTESIAN_POINT('Ctrl Pts',(0.354406667102056,43.6143454706655,11.447047761332));
#62729=CARTESIAN_POINT('Ctrl Pts',(0.365055960100978,43.615709113159,11.4490510438919));
#62730=CARTESIAN_POINT('Ctrl Pts',(0.375687467747781,43.6170706274019,11.4511497267115));
#62731=CARTESIAN_POINT('Ctrl Pts',(0.386299455019993,43.6184295176617,11.453343977426));
#62732=CARTESIAN_POINT('Ctrl Pts',(0.461063654739058,43.6280032516072,11.4688030422023));
#62733=CARTESIAN_POINT('Ctrl Pts',(0.534875685874753,43.6374476583003,11.4890101183549));
#62734=CARTESIAN_POINT('Ctrl Pts',(0.607241015825486,43.646826890073,11.5136655931181));
#62735=CARTESIAN_POINT('Ctrl Pts',(0.622938784997419,43.648861469553,11.519013954715));
#62736=CARTESIAN_POINT('Ctrl Pts',(0.638568648006123,43.6508930066079,11.52457173361));
#62737=CARTESIAN_POINT('Ctrl Pts',(0.654125826897278,43.6529221965091,11.5303360412774));
#62738=CARTESIAN_POINT('Ctrl Pts',(0.731711944031748,43.6630420881976,11.5590835573286));
#62739=CARTESIAN_POINT('Ctrl Pts',(0.807507317384714,43.673216934486,11.5927719803986));
#62740=CARTESIAN_POINT('Ctrl Pts',(0.880908242422253,43.683511395425,11.6310579954211));
#62741=CARTESIAN_POINT('Ctrl Pts',(0.890693352786457,43.6848837546477,11.6361619213214));
#62742=CARTESIAN_POINT('Ctrl Pts',(0.90043598292481,43.6862582489024,11.641347572303));
#62743=CARTESIAN_POINT('Ctrl Pts',(0.910134769176067,43.6876350399056,11.6466141550489));
#62744=CARTESIAN_POINT('Ctrl Pts',(0.942442438941816,43.6922212745041,11.6641576921204));
#62745=CARTESIAN_POINT('Ctrl Pts',(0.974252312453001,43.6968083379815,11.6826381668839));
#62746=CARTESIAN_POINT('Ctrl Pts',(1.00549856845552,43.7013948596203,11.7020274023685));
#62747=CARTESIAN_POINT('Ctrl Pts',(1.02334506020761,43.7040144797307,11.7131016837521));
#62748=CARTESIAN_POINT('Ctrl Pts',(1.04100765718223,43.7066339147091,11.7244723415158));
#62749=CARTESIAN_POINT('Ctrl Pts',(1.05847448231885,43.7092529340121,11.7361339149813));
#62750=CARTESIAN_POINT('Ctrl Pts',(1.1713629347562,43.7261797099836,11.8115029056946));
#62751=CARTESIAN_POINT('Ctrl Pts',(1.27630931051256,43.7431244522926,11.899183329826));
#62752=CARTESIAN_POINT('Ctrl Pts',(1.37069057407131,43.7600840387654,11.9970973873642));
#62753=CARTESIAN_POINT('Ctrl Pts',(1.42280016977232,43.7694477319502,12.0511575022575));
#62754=CARTESIAN_POINT('Ctrl Pts',(1.47169109919433,43.7788162229859,12.1083378898411));
#62755=CARTESIAN_POINT('Ctrl Pts',(1.51692754710015,43.7881900239829,12.1682924647015));
#62756=CARTESIAN_POINT('Ctrl Pts',(1.51696491775492,43.7881977678509,12.1683419942694));
#62757=CARTESIAN_POINT('Ctrl Pts',(1.51700228604121,43.7882055118733,12.168391525532));
#62758=CARTESIAN_POINT('Ctrl Pts',(1.5170396519587,43.7882132560502,12.1684410584893));
#62759=CARTESIAN_POINT('Ctrl Pts',(1.5515881248574,43.7953735106584,12.2142391586534));
#62760=CARTESIAN_POINT('Ctrl Pts',(1.58411479558681,43.8026662744911,12.261488956581));
#62761=CARTESIAN_POINT('Ctrl Pts',(1.61446369987685,43.8099901329818,12.3100982262894));
#62762=CARTESIAN_POINT('Ctrl Pts',(1.63930499134918,43.815984883294,12.3498860560424));
#62763=CARTESIAN_POINT('Ctrl Pts',(1.66268627178357,43.8220003399112,12.3905842036694));
#62764=CARTESIAN_POINT('Ctrl Pts',(1.68450524095631,43.8279775950811,12.4321225050557));
#62765=CARTESIAN_POINT('Ctrl Pts',(1.72480715082951,43.839018208285,12.50884807653));
#62766=CARTESIAN_POINT('Ctrl Pts',(1.75976124537238,43.8499005705538,12.5884996251357));
#62767=CARTESIAN_POINT('Ctrl Pts',(1.78917403748305,43.8606990979938,12.670275591883));
#62768=CARTESIAN_POINT('Ctrl Pts',(1.79842290822096,43.8640947016508,12.6959900953912));
#62769=CARTESIAN_POINT('Ctrl Pts',(1.80712391329608,43.8674820671572,12.7219150440391));
#62770=CARTESIAN_POINT('Ctrl Pts',(1.81527108401148,43.8708636484753,12.7480265615633));
#62771=CARTESIAN_POINT('Ctrl Pts',(1.84067427841761,43.8814075502329,12.8294432863479));
#62772=CARTESIAN_POINT('Ctrl Pts',(1.86069177781362,43.8918966301114,12.9126701156961));
#62773=CARTESIAN_POINT('Ctrl Pts',(1.87513134105699,43.902396414511,12.9969077356303));
#62774=CARTESIAN_POINT('Ctrl Pts',(1.88005393093667,43.9059758948286,13.0256251731586));
#62775=CARTESIAN_POINT('Ctrl Pts',(1.88432858222577,43.9095566713819,13.0544603891218));
#62776=CARTESIAN_POINT('Ctrl Pts',(1.88794859519248,43.9131415008686,13.0833827340923));
#62777=CARTESIAN_POINT('Ctrl Pts',(1.8944580868007,43.9195877256957,13.1353907693138));
#62778=CARTESIAN_POINT('Ctrl Pts',(1.89884935747155,43.9260462734384,13.1876769477747));
#62779=CARTESIAN_POINT('Ctrl Pts',(1.90108421850662,43.9325286885601,13.2400514451286));
#62780=CARTESIAN_POINT('Ctrl Pts',(1.9027099019481,43.9372441293677,13.2781497213826));
#62781=CARTESIAN_POINT('Ctrl Pts',(1.90319460241082,43.9419721741924,13.3162947414601));
#62782=CARTESIAN_POINT('Ctrl Pts',(1.90253324894795,43.9467224113686,13.3544102360176));
#62783=CARTESIAN_POINT('Ctrl Pts',(1.90253284706,43.9467252979689,13.3544333978501));
#62784=CARTESIAN_POINT('Ctrl Pts',(1.90253244474574,43.9467281845762,13.3544565596831));
#62785=CARTESIAN_POINT('Ctrl Pts',(1.90253204200516,43.9467310711905,13.3544797215166));
#62786=CARTESIAN_POINT('Ctrl Pts',(1.9012587208505,43.9558575096353,13.4277091264005));
#62787=CARTESIAN_POINT('Ctrl Pts',(1.8957235974073,43.9650542157224,13.5009454342743));
#62788=CARTESIAN_POINT('Ctrl Pts',(1.88602216453062,43.9742750416705,13.5736597120378));
#62789=CARTESIAN_POINT('Ctrl Pts',(1.88166260850638,43.9784186262132,13.6063355004188));
#62790=CARTESIAN_POINT('Ctrl Pts',(1.87646184173778,43.9825672206978,13.6389063657602));
#62791=CARTESIAN_POINT('Ctrl Pts',(1.87042863065913,43.9867175295375,13.671326662048));
#62792=CARTESIAN_POINT('Ctrl Pts',(1.87042710275171,43.986718580601,13.6713348724704));
#62793=CARTESIAN_POINT('Ctrl Pts',(1.87042557479108,43.9867196316647,13.671343082883));
#62794=CARTESIAN_POINT('Ctrl Pts',(1.87042404677724,43.9867206827286,13.6713512932859));
#62795=CARTESIAN_POINT('Ctrl Pts',(1.85566478271274,43.9968730320419,13.7506565333898));
#62796=CARTESIAN_POINT('Ctrl Pts',(1.83594055493716,44.0070483275033,13.8290544476903));
#62797=CARTESIAN_POINT('Ctrl Pts',(1.81128975971261,44.0171601272258,13.9059652444678));
#62798=CARTESIAN_POINT('Ctrl Pts',(1.80343449962244,44.0203823687834,13.9304737565432));
#62799=CARTESIAN_POINT('Ctrl Pts',(1.79507882153093,44.0235980767071,13.954831397821));
#62800=CARTESIAN_POINT('Ctrl Pts',(1.78622345395315,44.026804267668,13.9790197714345));
#62801=CARTESIAN_POINT('Ctrl Pts',(1.78622218841255,44.026804725872,13.9790232282497));
#62802=CARTESIAN_POINT('Ctrl Pts',(1.78622092286174,44.0268051840758,13.9790266850614));
#62803=CARTESIAN_POINT('Ctrl Pts',(1.78621965730073,44.0268056422794,13.9790301418696));
#62804=CARTESIAN_POINT('Ctrl Pts',(1.77544514018287,44.030706617887,14.008460125274));
#62805=CARTESIAN_POINT('Ctrl Pts',(1.76394558147227,44.0346018285825,14.0376304480357));
#62806=CARTESIAN_POINT('Ctrl Pts',(1.75172504237321,44.0384820425673,14.066506010278));
#62807=CARTESIAN_POINT('Ctrl Pts',(1.72456897088087,44.0471045237461,14.1306723147493));
#62808=CARTESIAN_POINT('Ctrl Pts',(1.69385165573129,44.0556523962681,14.1933854221277));
#62809=CARTESIAN_POINT('Ctrl Pts',(1.65982723199645,44.0642355969814,14.2543086369607));
#62810=CARTESIAN_POINT('Ctrl Pts',(1.62591803131924,44.0727897308504,14.3150255364965));
#62811=CARTESIAN_POINT('Ctrl Pts',(1.58881380009087,44.0814663514857,14.3739910087394));
#62812=CARTESIAN_POINT('Ctrl Pts',(1.54854748895314,44.0901513341039,14.4307802087173));
#62813=CARTESIAN_POINT('Ctrl Pts',(1.53320531004564,44.0934604665615,14.4524179014052));
#62814=CARTESIAN_POINT('Ctrl Pts',(1.51740463455968,44.0967706625248,14.4737385701792));
#62815=CARTESIAN_POINT('Ctrl Pts',(1.50115693587717,44.1000813952048,14.4947169239003));
#62816=CARTESIAN_POINT('Ctrl Pts',(1.49105654617142,44.1021395137687,14.5077581275876));
#62817=CARTESIAN_POINT('Ctrl Pts',(1.48078346323126,44.1041978305208,14.5206669950275));
#62818=CARTESIAN_POINT('Ctrl Pts',(1.4703404162355,44.1062562463378,14.5334377131575));
#62819=CARTESIAN_POINT('Ctrl Pts',(1.4232052948658,44.115546990639,14.5910788737574));
#62820=CARTESIAN_POINT('Ctrl Pts',(1.37249259276042,44.1248617293685,14.6460396110216));
#62821=CARTESIAN_POINT('Ctrl Pts',(1.31867707979036,44.1341873629787,14.6979414591855));
#62822=CARTESIAN_POINT('Ctrl Pts',(1.30299549290356,44.1369048086679,14.7130654131654));
#62823=CARTESIAN_POINT('Ctrl Pts',(1.28705071957,44.1396231789241,14.7279298312709));
#62824=CARTESIAN_POINT('Ctrl Pts',(1.2708551448673,44.1423421482867,14.742525868927));
#62825=CARTESIAN_POINT('Ctrl Pts',(1.21862685325978,44.1511104153811,14.7895958942277));
#62826=CARTESIAN_POINT('Ctrl Pts',(1.16379442317349,44.1598865918041,14.8338720179614));
#62827=CARTESIAN_POINT('Ctrl Pts',(1.10682778192858,44.1687765663926,14.8751740368781));
#62828=CARTESIAN_POINT('Ctrl Pts',(1.08652577629236,44.1719448120581,14.8898934200559));
#62829=CARTESIAN_POINT('Ctrl Pts',(1.06595249883986,44.1751275627198,14.9042354981446));
#62830=CARTESIAN_POINT('Ctrl Pts',(1.04512843756418,44.1783297805026,14.9181934971272));
#62831=CARTESIAN_POINT('Ctrl Pts',(0.964219328541589,44.1907715700402,14.9724254380762));
#62832=CARTESIAN_POINT('Ctrl Pts',(0.879289177392871,44.2032149235223,15.0206870131516));
#62833=CARTESIAN_POINT('Ctrl Pts',(0.791202840516241,44.2155622228643,15.0623301371084));
#62834=CARTESIAN_POINT('Ctrl Pts',(0.71580631198331,44.2261307575559,15.0979741097713));
#62835=CARTESIAN_POINT('Ctrl Pts',(0.638098070836109,44.2366277067109,15.1287706175789));
#62836=CARTESIAN_POINT('Ctrl Pts',(0.558565667470021,44.2470165405819,15.1543230267766));
#62837=CARTESIAN_POINT('Ctrl Pts',(0.545179759982402,44.2487650602194,15.1586236912999));
#62838=CARTESIAN_POINT('Ctrl Pts',(0.531742184172616,44.2505105119025,15.1627756845355));
#62839=CARTESIAN_POINT('Ctrl Pts',(0.518255278193969,44.2522527150447,15.1667769694065));
#62840=CARTESIAN_POINT('Ctrl Pts',(0.476730225248576,44.2576168124762,15.1790965901101));
#62841=CARTESIAN_POINT('Ctrl Pts',(0.434735080639449,44.2629511539096,15.1899888909904));
#62842=CARTESIAN_POINT('Ctrl Pts',(0.392363468462353,44.2682944556014,15.1994255958125));
#62843=CARTESIAN_POINT('Ctrl Pts',(0.392348669898505,44.2682963217846,15.1994288916437));
#62844=CARTESIAN_POINT('Ctrl Pts',(0.392333871288648,44.2682981879689,15.1994321872973));
#62845=CARTESIAN_POINT('Ctrl Pts',(0.3923190726328,44.2683000541543,15.1994354827733));
#62846=CARTESIAN_POINT('Ctrl Pts',(0.303463056846925,44.2795052475772,15.2192226091348));
#62847=CARTESIAN_POINT('Ctrl Pts',(0.213098743752062,44.2907005039032,15.2325524353331));
#62848=CARTESIAN_POINT('Ctrl Pts',(0.122100826373289,44.3019309442477,15.2395437326749));
#62849=CARTESIAN_POINT('Ctrl Pts',(0.0267244225314325,44.3137017522449,
15.246871425636));
#62850=CARTESIAN_POINT('Ctrl Pts',(-0.0693486369463793,44.3255114195325,
15.2472350622581));
#62851=CARTESIAN_POINT('Ctrl Pts',(-0.165101310109247,44.337394572606,15.240737448503));
#62852=CARTESIAN_POINT('Ctrl Pts',(-0.260764325483668,44.3492665989174,
15.234245918773));
#62853=CARTESIAN_POINT('Ctrl Pts',(-0.356107800931346,44.3612121177935,
15.2209050722059));
#62854=CARTESIAN_POINT('Ctrl Pts',(-0.450101264067399,44.3732463862623,
15.2007983539383));
#62855=CARTESIAN_POINT('Ctrl Pts',(-0.541034403506556,44.3848888321964,
15.181346288285));
#62856=CARTESIAN_POINT('Ctrl Pts',(-0.630703688762427,44.396614449005,15.1555612094307));
#62857=CARTESIAN_POINT('Ctrl Pts',(-0.718161474242711,44.4084172748796,
15.1235116420653));
#62858=CARTESIAN_POINT('Ctrl Pts',(-0.773397886299599,44.4158716798804,
15.1032698408406));
#62859=CARTESIAN_POINT('Ctrl Pts',(-0.827751833483358,44.423356480698,15.0805291321155));
#62860=CARTESIAN_POINT('Ctrl Pts',(-0.880982903069709,44.4308655889996,
15.0553060862276));
#62861=CARTESIAN_POINT('Ctrl Pts',(-0.880991504927449,44.4308668024315,
15.0553020103176));
#62862=CARTESIAN_POINT('Ctrl Pts',(-0.881000106756236,44.4308680158645,
15.0552979343428));
#62863=CARTESIAN_POINT('Ctrl Pts',(-0.881008708556081,44.4308692292984,
15.0552938583032));
#62864=CARTESIAN_POINT('Ctrl Pts',(-0.949777952894382,44.4405703311217,
15.022706938637));
#62865=CARTESIAN_POINT('Ctrl Pts',(-1.01670018024658,44.4503355641457,14.9859787929044));
#62866=CARTESIAN_POINT('Ctrl Pts',(-1.08130811717254,44.460002951837,14.9453570067032));
#62867=CARTESIAN_POINT('Ctrl Pts',(-1.08881927634195,44.4611268584522,14.9406344181728));
#62868=CARTESIAN_POINT('Ctrl Pts',(-1.09629911536165,44.4622494355331,14.935859244514));
#62869=CARTESIAN_POINT('Ctrl Pts',(-1.10374686948965,44.463370423022,14.9310319078346));
#62870=CARTESIAN_POINT('Ctrl Pts',(-1.11576672495049,44.4651795734527,14.923241117732));
#62871=CARTESIAN_POINT('Ctrl Pts',(-1.12770346753595,44.4669846854585,14.9153141979155));
#62872=CARTESIAN_POINT('Ctrl Pts',(-1.13955436632537,44.4687847978907,14.9072526043425));
#62873=CARTESIAN_POINT('Ctrl Pts',(-1.20881460051703,44.4793051989881,14.8601382150673));
#62874=CARTESIAN_POINT('Ctrl Pts',(-1.27514891107262,44.489653444563,14.8084199677914));
#62875=CARTESIAN_POINT('Ctrl Pts',(-1.33806632362854,44.4999383822885,14.752580101493));
#62876=CARTESIAN_POINT('Ctrl Pts',(-1.40200047511709,44.5103895235527,14.6958378686834));
#62877=CARTESIAN_POINT('Ctrl Pts',(-1.46240423535586,44.5207766906942,14.6348368848923));
#62878=CARTESIAN_POINT('Ctrl Pts',(-1.51870614782633,44.5312202034947,14.5701558030753));
#62879=CARTESIAN_POINT('Ctrl Pts',(-1.55879377509555,44.5386561080699,14.5241021081745));
#62880=CARTESIAN_POINT('Ctrl Pts',(-1.59680043494514,44.5461207607961,14.4761843015882));
#62881=CARTESIAN_POINT('Ctrl Pts',(-1.63251480183106,44.5536534130216,14.4266441099927));
#62882=CARTESIAN_POINT('Ctrl Pts',(-1.63252331082678,44.5536552076861,14.4266323069757));
#62883=CARTESIAN_POINT('Ctrl Pts',(-1.63253181969435,44.5536570023525,14.4266205038614));
#62884=CARTESIAN_POINT('Ctrl Pts',(-1.63254032843374,44.5536587970208,14.4266087006498));
#62885=CARTESIAN_POINT('Ctrl Pts',(-1.68445643326028,44.564608972198,14.3545913611944));
#62886=CARTESIAN_POINT('Ctrl Pts',(-1.73159885214559,44.5756300349953,14.2789488134197));
#62887=CARTESIAN_POINT('Ctrl Pts',(-1.77359830303046,44.5867104940924,14.2004365969182));
#62888=CARTESIAN_POINT('Ctrl Pts',(-1.81582089846807,44.5978498240565,14.1215072422621));
#62889=CARTESIAN_POINT('Ctrl Pts',(-1.852846965609,44.609048601566,14.0396788990061));
#62890=CARTESIAN_POINT('Ctrl Pts',(-1.88433431500624,44.6202898644539,13.9556864859498));
#62891=CARTESIAN_POINT('Ctrl Pts',(-1.91569856854481,44.6314871810289,13.8720224307389));
#62892=CARTESIAN_POINT('Ctrl Pts',(-1.94156907374052,44.6427262186232,13.7862116512348));
#62893=CARTESIAN_POINT('Ctrl Pts',(-1.96161764693458,44.6539925222584,13.69893534269));
#62894=CARTESIAN_POINT('Ctrl Pts',(-1.97620527972793,44.6621900482758,13.6354318340719));
#62895=CARTESIAN_POINT('Ctrl Pts',(-1.98771101076676,44.6704020473443,13.5711513935466));
#62896=CARTESIAN_POINT('Ctrl Pts',(-1.99600309484505,44.6786255226448,13.5063407137072));
#62897=CARTESIAN_POINT('Ctrl Pts',(-1.99600413073181,44.6786265499607,13.5063326172474));
#62898=CARTESIAN_POINT('Ctrl Pts',(-1.99600516656828,44.6786275772765,13.5063245207802));
#62899=CARTESIAN_POINT('Ctrl Pts',(-1.99600620235445,44.6786286045924,13.5063164243057));
#62900=CARTESIAN_POINT('Ctrl Pts',(-1.9989524566471,44.6815507655481,13.4832863110676));
#62901=CARTESIAN_POINT('Ctrl Pts',(-2.0014917701668,44.6844732366445,13.4601968132775));
#62902=CARTESIAN_POINT('Ctrl Pts',(-2.00362382472207,44.6873925139984,13.4370592699312));
#62903=CARTESIAN_POINT('Ctrl Pts',(-2.0138298820748,44.7013669744684,13.3263008027942));
#62904=CARTESIAN_POINT('Ctrl Pts',(-2.0147077970061,44.7152691479107,13.2144301717847));
#62905=CARTESIAN_POINT('Ctrl Pts',(-2.00640344852531,44.7291692282355,13.1029507560109));
#62906=CARTESIAN_POINT('Ctrl Pts',(-2.00589556393409,44.730019341478,13.096132800618));
#62907=CARTESIAN_POINT('Ctrl Pts',(-2.00535331908657,44.7308694478072,13.0893163022739));
#62908=CARTESIAN_POINT('Ctrl Pts',(-2.00477674144566,44.7317195636347,13.0825016027861));
#62909=CARTESIAN_POINT('Ctrl Pts',(-1.99472189986248,44.7465445921599,12.963661191844));
#62910=CARTESIAN_POINT('Ctrl Pts',(-1.97422402633385,44.7613736991323,12.8453705757279));
#62911=CARTESIAN_POINT('Ctrl Pts',(-1.94345486610982,44.776271931547,12.729580488958));
#62912=CARTESIAN_POINT('Ctrl Pts',(-1.92391562895981,44.7857327063665,12.6560506965118));
#62913=CARTESIAN_POINT('Ctrl Pts',(-1.90023477131147,44.7952208737969,12.583532124005));
#62914=CARTESIAN_POINT('Ctrl Pts',(-1.87247430467957,44.8047448794644,12.5125442365009));
#62915=CARTESIAN_POINT('Ctrl Pts',(-1.87247199884922,44.8047456705441,12.5125383401294));
#62916=CARTESIAN_POINT('Ctrl Pts',(-1.87246969299075,44.8047464616243,12.5125324437682));
#62917=CARTESIAN_POINT('Ctrl Pts',(-1.87246738710414,44.8047472527049,12.5125265474173));
#62918=CARTESIAN_POINT('Ctrl Pts',(-1.8417656413995,44.8152801017681,12.4340195367457));
#62919=CARTESIAN_POINT('Ctrl Pts',(-1.80607587860346,44.8258945414302,12.3573440782967));
#62920=CARTESIAN_POINT('Ctrl Pts',(-1.76571080889466,44.836476728865,12.2830640674007));
#62921=CARTESIAN_POINT('Ctrl Pts',(-1.71646942493366,44.8493859486034,12.1924498169226));
#62922=CARTESIAN_POINT('Ctrl Pts',(-1.66026211689408,44.8622489307279,12.1053787678795));
#62923=CARTESIAN_POINT('Ctrl Pts',(-1.59771604579451,44.8751219231574,12.022801987044));
#62924=CARTESIAN_POINT('Ctrl Pts',(-1.53522822528026,44.8879829266749,11.9403021118515));
#62925=CARTESIAN_POINT('Ctrl Pts',(-1.46640908545805,44.9008550726673,11.8622913408099));
#62926=CARTESIAN_POINT('Ctrl Pts',(-1.39195572467721,44.9137854253946,11.7898077068253));
#62927=CARTESIAN_POINT('Ctrl Pts',(-1.35621175803568,44.9199930981135,11.7550093771323));
#62928=CARTESIAN_POINT('Ctrl Pts',(-1.31917068762716,44.9262139460458,11.7214859910814));
#62929=CARTESIAN_POINT('Ctrl Pts',(-1.28091943577779,44.9324512723062,11.6893554841697));
#62930=CARTESIAN_POINT('Ctrl Pts',(-1.28091426683009,44.9324521151652,11.6893511423272));
#62931=CARTESIAN_POINT('Ctrl Pts',(-1.28090909786018,44.9324529580248,11.68934680051));
#62932=CARTESIAN_POINT('Ctrl Pts',(-1.28090392886803,44.9324538008848,11.689342458718));
#62933=CARTESIAN_POINT('Ctrl Pts',(-1.18903365872423,44.94743424159,11.6121743003787));
#62934=CARTESIAN_POINT('Ctrl Pts',(-1.09014141607981,44.9625752668603,11.5429731154381));
#62935=CARTESIAN_POINT('Ctrl Pts',(-0.985766402849624,44.9776815456083,
11.4826592838517));
#62936=CARTESIAN_POINT('Ctrl Pts',(-0.97325193505438,44.9794927744939,11.475427711087));
#62937=CARTESIAN_POINT('Ctrl Pts',(-0.960658680559212,44.9813034961629,
11.4683239524804));
#62938=CARTESIAN_POINT('Ctrl Pts',(-0.947989320712283,44.9831133677631,
11.4613496339711));
#62939=CARTESIAN_POINT('Ctrl Pts',(-0.937102327850855,44.9846686207064,
11.4553564854031));
#62940=CARTESIAN_POINT('Ctrl Pts',(-0.926158772207229,44.9862233275243,
11.4494587047961));
#62941=CARTESIAN_POINT('Ctrl Pts',(-0.915160127495719,44.9877773234709,
11.443657227826));
#62942=CARTESIAN_POINT('Ctrl Pts',(-0.803195994864283,45.0035967096614,
11.3845992844179));
#62943=CARTESIAN_POINT('Ctrl Pts',(-0.685498295157008,45.0193461150921,
11.3355123919204));
#62944=CARTESIAN_POINT('Ctrl Pts',(-0.564026643895891,45.0351569854134,
11.2974601095493));
#62945=CARTESIAN_POINT('Ctrl Pts',(-0.557153255633243,45.0360516324307,
11.2953069478173));
#62946=CARTESIAN_POINT('Ctrl Pts',(-0.550267782542978,45.0369464774048,
11.2931891028702));
#62947=CARTESIAN_POINT('Ctrl Pts',(-0.543370578909281,45.0378415445592,
11.2911067625676));
#62948=CARTESIAN_POINT('Ctrl Pts',(-0.481520058743433,45.0458680393563,
11.2724334222236));
#62949=CARTESIAN_POINT('Ctrl Pts',(-0.418731397380921,45.053911575045,11.2566180320663));
#62950=CARTESIAN_POINT('Ctrl Pts',(-0.355289380165877,45.0619836125773,
11.2437966393052));
#62951=CARTESIAN_POINT('Ctrl Pts',(-0.355285043067044,45.0619841644075,
11.2437957627938));
#62952=CARTESIAN_POINT('Ctrl Pts',(-0.355280705964929,45.0619847162379,
11.2437948862964));
#62953=CARTESIAN_POINT('Ctrl Pts',(-0.355276368859519,45.0619852680685,
11.243794009813));
#62954=CARTESIAN_POINT('Ctrl Pts',(-0.349648787210502,45.0627012920588,
11.242656734663));
#62955=CARTESIAN_POINT('Ctrl Pts',(-0.344015669854361,45.0634175707409,
11.2415429346111));
#62956=CARTESIAN_POINT('Ctrl Pts',(-0.338377233770639,45.0641340836512,
11.2404526226096));
#62957=CARTESIAN_POINT('Ctrl Pts',(-0.212337755202137,45.0801507436369,
11.2160801983943));
#62958=CARTESIAN_POINT('Ctrl Pts',(-0.083657625338293,45.0962819756428,
11.203452144954));
#62959=CARTESIAN_POINT('Ctrl Pts',(0.0454031143779827,45.1124275059506,
11.2026060087752));
#62960=CARTESIAN_POINT('Ctrl Pts',(0.122713040983513,45.1220989967994,11.2020991565285));
#62961=CARTESIAN_POINT('Ctrl Pts',(0.200163706613968,45.1317761380361,11.2058176283785));
#62962=CARTESIAN_POINT('Ctrl Pts',(0.277304443770296,45.141444268965,11.2137694907024));
#62963=CARTESIAN_POINT('Ctrl Pts',(0.392755226298408,45.1559138387731,11.2256704494137));
#62964=CARTESIAN_POINT('Ctrl Pts',(0.507541491897695,45.1703677451665,11.2470625359803));
#62965=CARTESIAN_POINT('Ctrl Pts',(0.619988601592955,45.1849028038661,11.2779180352251));
#62966=CARTESIAN_POINT('Ctrl Pts',(0.632706684454347,45.1865467596906,11.2814078785584));
#62967=CARTESIAN_POINT('Ctrl Pts',(0.645394870547359,45.1881917558853,11.2850187320195));
#62968=CARTESIAN_POINT('Ctrl Pts',(0.658050758780454,45.1898379341977,11.2887505194805));
#62969=CARTESIAN_POINT('Ctrl Pts',(0.666998222341376,45.191001749822,11.2913888196701));
#62970=CARTESIAN_POINT('Ctrl Pts',(0.675929375511245,45.1921661297048,11.2940875173707));
#62971=CARTESIAN_POINT('Ctrl Pts',(0.684843296158863,45.1933311104401,11.2968465526485));
#62972=CARTESIAN_POINT('Ctrl Pts',(0.684848158254035,45.1933317458784,11.2968480575634));
#62973=CARTESIAN_POINT('Ctrl Pts',(0.684853020344242,45.193332381317,11.2968495624963));
#62974=CARTESIAN_POINT('Ctrl Pts',(0.684857882429488,45.1933330167558,11.2968510674472));
#62975=CARTESIAN_POINT('Ctrl Pts',(0.775542254410143,45.2051847966284,11.3249204085195));
#62976=CARTESIAN_POINT('Ctrl Pts',(0.864500574667007,45.2171028831587,11.3592540114329));
#62977=CARTESIAN_POINT('Ctrl Pts',(0.950951991990921,45.2290358758107,11.3994507400536));
#62978=CARTESIAN_POINT('Ctrl Pts',(1.11212620474213,45.2512829453903,11.4743908195936));
#62979=CARTESIAN_POINT('Ctrl Pts',(1.26460168681221,45.2735846116156,11.5697127495115));
#62980=CARTESIAN_POINT('Ctrl Pts',(1.40341572670576,45.2959102457559,11.6827721945687));
#62981=CARTESIAN_POINT('Ctrl Pts',(1.44821014969757,45.3031145883427,11.7192557707905));
#62982=CARTESIAN_POINT('Ctrl Pts',(1.49158325573292,45.3103216000242,11.7575872908086));
#62983=CARTESIAN_POINT('Ctrl Pts',(1.53337112977183,45.3175309541919,11.7976817952021));
#62984=CARTESIAN_POINT('Ctrl Pts',(1.55105511791145,45.3205818424346,11.8146491752487));
#62985=CARTESIAN_POINT('Ctrl Pts',(1.56845528293424,45.3236331684876,11.8319323814174));
#62986=CARTESIAN_POINT('Ctrl Pts',(1.58555880455248,45.3266863052577,11.849524300512));
#62987=CARTESIAN_POINT('Ctrl Pts',(1.58556698423901,45.3266877654074,11.8495327137725));
#62988=CARTESIAN_POINT('Ctrl Pts',(1.58557516385734,45.3266892255575,11.8495411271033));
#62989=CARTESIAN_POINT('Ctrl Pts',(1.58558334340749,45.3266906857082,11.8495495405043));
#62990=CARTESIAN_POINT('Ctrl Pts',(1.67599372359701,45.3428300542994,11.9425447258912));
#62991=CARTESIAN_POINT('Ctrl Pts',(1.75807542442181,45.3590280166517,12.0441179598847));
#62992=CARTESIAN_POINT('Ctrl Pts',(1.8306691593267,45.3752881408786,12.1525001696805));
#62993=CARTESIAN_POINT('Ctrl Pts',(1.9033168266553,45.3915603453203,12.2609629004092));
#62994=CARTESIAN_POINT('Ctrl Pts',(1.96646025163579,45.4078950327212,12.3762469632662));
#62995=CARTESIAN_POINT('Ctrl Pts',(2.01889794999029,45.4242878521849,12.4965442673756));
#62996=CARTESIAN_POINT('Ctrl Pts',(2.05891676953857,45.436798341863,12.5883514262778));
#62997=CARTESIAN_POINT('Ctrl Pts',(2.09269894674285,45.4493425300974,12.6830775196885));
#62998=CARTESIAN_POINT('Ctrl Pts',(2.11970969578712,45.4619143413547,12.7798970723477));
#62999=CARTESIAN_POINT('Ctrl Pts',(2.11971337779344,45.4619160550979,12.7799102704343));
#63000=CARTESIAN_POINT('Ctrl Pts',(2.11971705967376,45.4619177688419,12.7799234685589));
#63001=CARTESIAN_POINT('Ctrl Pts',(2.1197207414281,45.4619194825866,12.7799366667217));
#63002=CARTESIAN_POINT('Ctrl Pts',(2.14488606212673,45.473633174392,12.8701480085141));
#63003=CARTESIAN_POINT('Ctrl Pts',(2.16416769647576,45.4853817456121,12.9621390488384));
#63004=CARTESIAN_POINT('Ctrl Pts',(2.17752086339295,45.4971268278867,13.0551903597028));
#63005=CARTESIAN_POINT('Ctrl Pts',(2.19789478370435,45.5150471738089,13.1971656681956));
#63006=CARTESIAN_POINT('Ctrl Pts',(2.20447572595291,45.5329691475165,13.3416848784884));
#63007=CARTESIAN_POINT('Ctrl Pts',(2.19698946825817,45.5509580385708,13.4860284921698));
#63008=CARTESIAN_POINT('Ctrl Pts',(2.1921617577059,45.5625586490103,13.5791122751943));
#63009=CARTESIAN_POINT('Ctrl Pts',(2.18147855175247,45.5741869045399,13.6721180984126));
#63010=CARTESIAN_POINT('Ctrl Pts',(2.16489369591591,45.5858440596454,13.7642000865692));
#63011=CARTESIAN_POINT('Ctrl Pts',(2.15857076358717,45.5902883191315,13.7993061004862));
#63012=CARTESIAN_POINT('Ctrl Pts',(2.1513905601623,45.5947367776815,13.8342778892848));
#63013=CARTESIAN_POINT('Ctrl Pts',(2.1433525037659,45.599189498898,13.8690689663171));
#63014=CARTESIAN_POINT('Ctrl Pts',(2.14335156752272,45.5991900175345,13.8690730186535));
#63015=CARTESIAN_POINT('Ctrl Pts',(2.14335063126784,45.5991905361712,13.8690770709878));
#63016=CARTESIAN_POINT('Ctrl Pts',(2.14334969500126,45.5991910548079,13.8690811233198));
#63017=CARTESIAN_POINT('Ctrl Pts',(2.12029927780217,45.6119596331554,13.9688475214958));
#63018=CARTESIAN_POINT('Ctrl Pts',(2.09015480355828,45.6247828779577,14.0672843773186));
#63019=CARTESIAN_POINT('Ctrl Pts',(2.05333535530513,45.6376364238151,14.1633752639895));
#63020=CARTESIAN_POINT('Ctrl Pts',(2.05017992087395,45.6387379753887,14.171610273114));
#63021=CARTESIAN_POINT('Ctrl Pts',(2.04697549230673,45.6398397493399,14.1798280608758));
#63022=CARTESIAN_POINT('Ctrl Pts',(2.04372235015577,45.6409417302387,14.1880279931464));
#63023=CARTESIAN_POINT('Ctrl Pts',(2.00503673649245,45.6540462320831,14.2855396901957));
#63024=CARTESIAN_POINT('Ctrl Pts',(1.95946432547649,45.667180363089,14.3805303543247));
#63025=CARTESIAN_POINT('Ctrl Pts',(1.90739615061957,45.6803410718172,14.4720865331734));
#63026=CARTESIAN_POINT('Ctrl Pts',(1.85220623644864,45.6942908287874,14.5691319484652));
#63027=CARTESIAN_POINT('Ctrl Pts',(1.7896938670021,45.7082755242419,14.6623505984215));
#63028=CARTESIAN_POINT('Ctrl Pts',(1.72036142470787,45.7223009067304,14.75053057276));
#63029=CARTESIAN_POINT('Ctrl Pts',(1.69298913966996,45.7278380947269,14.7853438190898));
#63030=CARTESIAN_POINT('Ctrl Pts',(1.66455587907725,45.7333812079543,14.8193690720306));
#63031=CARTESIAN_POINT('Ctrl Pts',(1.63510297141474,45.7389289160858,14.8525234594651));
#63032=CARTESIAN_POINT('Ctrl Pts',(1.63510159445506,45.738929175448,14.8525250094735));
#63033=CARTESIAN_POINT('Ctrl Pts',(1.63510021749315,45.7389294348102,14.85252655948));
#63034=CARTESIAN_POINT('Ctrl Pts',(1.63509884052901,45.7389296941724,14.8525281094847));
#63035=CARTESIAN_POINT('Ctrl Pts',(1.56613403134531,45.7519197672924,14.9301595954892));
#63036=CARTESIAN_POINT('Ctrl Pts',(1.49147302194478,45.7649111277806,15.0031318085196));
#63037=CARTESIAN_POINT('Ctrl Pts',(1.41197344679732,45.7779126670361,15.0707752935465));
#63038=CARTESIAN_POINT('Ctrl Pts',(1.39514738493469,45.7806644390225,15.0850920173977));
#63039=CARTESIAN_POINT('Ctrl Pts',(1.37810471388298,45.7834166663575,15.0991701635101));
#63040=CARTESIAN_POINT('Ctrl Pts',(1.36085377109113,45.7861694322808,15.1130035985599));
#63041=CARTESIAN_POINT('Ctrl Pts',(1.26113857677847,45.8020811764825,15.1929646581178));
#63042=CARTESIAN_POINT('Ctrl Pts',(1.15446609125249,45.8180109660089,15.2647499446223));
#63043=CARTESIAN_POINT('Ctrl Pts',(1.04229941144345,45.8340003826846,15.3272985880928));
#63044=CARTESIAN_POINT('Ctrl Pts',(0.964178247229751,45.8451365939724,15.3708620853473));
#63045=CARTESIAN_POINT('Ctrl Pts',(0.883389045608882,45.8563023000698,15.4099489244777));
#63046=CARTESIAN_POINT('Ctrl Pts',(0.800370417838151,45.8675181404225,15.4442127136742));
#63047=CARTESIAN_POINT('Ctrl Pts',(0.768259093867673,45.8718563894738,15.4574658312562));
#63048=CARTESIAN_POINT('Ctrl Pts',(0.735813330122108,45.8762022324817,15.4699973713265));
#63049=CARTESIAN_POINT('Ctrl Pts',(0.703060616133092,45.8805553092923,15.4817854332903));
#63050=CARTESIAN_POINT('Ctrl Pts',(0.703050939619478,45.8805565953722,15.481788915974));
#63051=CARTESIAN_POINT('Ctrl Pts',(0.703041263080088,45.8805578814527,15.4817923985924));
#63052=CARTESIAN_POINT('Ctrl Pts',(0.703031586514911,45.8805591675338,15.4817958811455));
#63053=CARTESIAN_POINT('Ctrl Pts',(0.598913190449675,45.8943972085069,15.5192676326809));
#63054=CARTESIAN_POINT('Ctrl Pts',(0.491811322180734,45.9083071390249,15.5491856344644));
#63055=CARTESIAN_POINT('Ctrl Pts',(0.382840015976741,45.922258918402,15.5713404404648));
#63056=CARTESIAN_POINT('Ctrl Pts',(0.273289653390351,45.9362848353404,15.5936129736198));
#63057=CARTESIAN_POINT('Ctrl Pts',(0.16184872763076,45.9503529969648,15.6080373508393));
#63058=CARTESIAN_POINT('Ctrl Pts',(0.0496935301666531,45.9644259055572,
15.6143695599238));
#63059=CARTESIAN_POINT('Ctrl Pts',(-0.0623519980788118,45.9784850531745,
15.6206955771559));
#63060=CARTESIAN_POINT('Ctrl Pts',(-0.175110226864188,45.9925487458726,
15.6189427438539));
#63061=CARTESIAN_POINT('Ctrl Pts',(-0.28735619715166,46.0065744352014,15.6088725393529));
#63062=CARTESIAN_POINT('Ctrl Pts',(-0.336779260054703,46.0127500914337,
15.604438524045));
#63063=CARTESIAN_POINT('Ctrl Pts',(-0.386102348209196,46.0189183298531,
15.5983922846779));
#63064=CARTESIAN_POINT('Ctrl Pts',(-0.435218281183437,46.0250754033888,
15.5907156564064));
#63065=CARTESIAN_POINT('Ctrl Pts',(-0.435230082382689,46.0250768827632,
15.5907138119251));
#63066=CARTESIAN_POINT('Ctrl Pts',(-0.435241883569989,46.0250783621369,
15.5907119673496));
#63067=CARTESIAN_POINT('Ctrl Pts',(-0.435253684745325,46.0250798415099,
15.5907101226801));
#63068=CARTESIAN_POINT('Ctrl Pts',(-0.525371743418507,46.0363768712413,
15.5766235565477));
#63069=CARTESIAN_POINT('Ctrl Pts',(-0.614753314310338,46.0476966561241,
15.5570477433176));
#63070=CARTESIAN_POINT('Ctrl Pts',(-0.702841229104749,46.0590791391817,
15.5322464666312));
#63071=CARTESIAN_POINT('Ctrl Pts',(-0.815299827109943,46.0736107362738,
15.5005835897042));
#63072=CARTESIAN_POINT('Ctrl Pts',(-0.925682269708267,46.0882487675148,
15.4603969024718));
#63073=CARTESIAN_POINT('Ctrl Pts',(-1.03285245568836,46.102958952506,15.4121867479535));
#63074=CARTESIAN_POINT('Ctrl Pts',(-1.0452004310303,46.1046538362079,15.4066320519923));
#63075=CARTESIAN_POINT('Ctrl Pts',(-1.05750574276826,46.1063496784497,15.4009707890295));
#63076=CARTESIAN_POINT('Ctrl Pts',(-1.06976663537864,46.1080464273473,15.3952036835102));
#63077=CARTESIAN_POINT('Ctrl Pts',(-1.18897462636356,46.1245432709069,15.3391323121512));
#63078=CARTESIAN_POINT('Ctrl Pts',(-1.30398312889218,46.1411250683823,15.2730541157071));
#63079=CARTESIAN_POINT('Ctrl Pts',(-1.41303318927676,46.1577210886726,15.1977111356521));
#63080=CARTESIAN_POINT('Ctrl Pts',(-1.50084466817589,46.1710848693105,15.1370419486754));
#63081=CARTESIAN_POINT('Ctrl Pts',(-1.58478982824556,46.1844572504357,15.0703635161614));
#63082=CARTESIAN_POINT('Ctrl Pts',(-1.66390124624768,46.1977957708119,14.9981333392991));
#63083=CARTESIAN_POINT('Ctrl Pts',(-1.68290645862786,46.2010001301698,14.9807812315226));
#63084=CARTESIAN_POINT('Ctrl Pts',(-1.70163286462932,46.2042025364822,14.9631088938852));
#63085=CARTESIAN_POINT('Ctrl Pts',(-1.7200673811099,46.2074024033346,14.9451229832622));
#63086=CARTESIAN_POINT('Ctrl Pts',(-1.7460829147076,46.2119181845699,14.9197405403546));
#63087=CARTESIAN_POINT('Ctrl Pts',(-1.77151646079242,46.2164288955996,14.8937341201424));
#63088=CARTESIAN_POINT('Ctrl Pts',(-1.79633063772826,46.2209329275884,14.867124224798));
#63089=CARTESIAN_POINT('Ctrl Pts',(-1.7963377999747,46.2209342276108,14.8671165442439));
#63090=CARTESIAN_POINT('Ctrl Pts',(-1.79634496216954,46.2209355276327,14.8671088636395));
#63091=CARTESIAN_POINT('Ctrl Pts',(-1.7963521243128,46.2209368276541,14.8671011829849));
#63092=CARTESIAN_POINT('Ctrl Pts',(-1.8580267719732,46.2321315713293,14.8009615301429));
#63093=CARTESIAN_POINT('Ctrl Pts',(-1.91588801512161,46.243332586979,14.7310686861218));
#63094=CARTESIAN_POINT('Ctrl Pts',(-1.96966602037887,46.2546052295084,14.6579467026471));
#63095=CARTESIAN_POINT('Ctrl Pts',(-2.04086980476799,46.2695305656995,14.5611308776545));
#63096=CARTESIAN_POINT('Ctrl Pts',(-2.10493619863944,46.2845858219809,14.458629663659));
#63097=CARTESIAN_POINT('Ctrl Pts',(-2.16125877011487,46.2997260694423,14.3516151544837));
#63098=CARTESIAN_POINT('Ctrl Pts',(-2.16793241666151,46.301520033346,14.3389350336922));
#63099=CARTESIAN_POINT('Ctrl Pts',(-2.17449729258174,46.3033151917321,14.3261915119305));
#63100=CARTESIAN_POINT('Ctrl Pts',(-2.18095234819548,46.3051114708695,14.3133865127906));
#63101=CARTESIAN_POINT('Ctrl Pts',(-2.2423176437236,46.3221878845696,14.1916551748319));
#63102=CARTESIAN_POINT('Ctrl Pts',(-2.29375669115427,46.3393645221848,14.0643671729683));
#63103=CARTESIAN_POINT('Ctrl Pts',(-2.3343019945624,46.3565508938873,13.9333222913705));
#63104=CARTESIAN_POINT('Ctrl Pts',(-2.36673028871117,46.3702966220006,13.8285120763779));
#63105=CARTESIAN_POINT('Ctrl Pts',(-2.3921868447487,46.3840478092587,13.7212985838361));
#63106=CARTESIAN_POINT('Ctrl Pts',(-2.41018104824501,46.3977527520996,13.6126860575908));
#63107=CARTESIAN_POINT('Ctrl Pts',(-2.41458682489408,46.401108328086,13.5860929087456));
#63108=CARTESIAN_POINT('Ctrl Pts',(-2.4185454856787,46.4044611347154,13.5594159140209));
#63109=CARTESIAN_POINT('Ctrl Pts',(-2.42205031287158,46.4078104189869,13.5326698291747));
#63110=CARTESIAN_POINT('Ctrl Pts',(-2.42671081461347,46.4122640894027,13.4971045450237));
#63111=CARTESIAN_POINT('Ctrl Pts',(-2.4305686623175,46.4167115284011,13.4614179034804));
#63112=CARTESIAN_POINT('Ctrl Pts',(-2.43360857407939,46.4211510309047,13.4256462336321));
#63113=CARTESIAN_POINT('Ctrl Pts',(-2.43360923252887,46.4211519925077,13.4256384854344));
#63114=CARTESIAN_POINT('Ctrl Pts',(-2.43360989093997,46.4211529541102,13.4256307372327));
#63115=CARTESIAN_POINT('Ctrl Pts',(-2.43361054931271,46.4211539157124,13.425622989027));
#63116=CARTESIAN_POINT('Ctrl Pts',(-2.44118605491686,46.4322185033857,13.3364689698517));
#63117=CARTESIAN_POINT('Ctrl Pts',(-2.44367563763571,46.4432709808867,13.2467458408072));
#63118=CARTESIAN_POINT('Ctrl Pts',(-2.44116990612555,46.4543970479552,13.1569972656756));
#63119=CARTESIAN_POINT('Ctrl Pts',(-2.43756619939952,46.4703983962905,13.0279221662322));
#63120=CARTESIAN_POINT('Ctrl Pts',(-2.42363224404003,46.4865569668884,12.898760902024));
#63121=CARTESIAN_POINT('Ctrl Pts',(-2.39968396120161,46.502820237758,12.7710505777282));
#63122=CARTESIAN_POINT('Ctrl Pts',(-2.39583844700153,46.5054317251657,12.7505433927709));
#63123=CARTESIAN_POINT('Ctrl Pts',(-2.39173460861502,46.5080459155969,12.730073614735));
#63124=CARTESIAN_POINT('Ctrl Pts',(-2.38737362867296,46.510662595552,12.7096476098486));
#63125=CARTESIAN_POINT('Ctrl Pts',(-2.35555178287611,46.529756374276,12.560600105302));
#63126=CARTESIAN_POINT('Ctrl Pts',(-2.31003584733003,46.5489807973168,12.4138849447933));
#63127=CARTESIAN_POINT('Ctrl Pts',(-2.25134135194109,46.5682193411139,12.2721586464856));
#63128=CARTESIAN_POINT('Ctrl Pts',(-2.20846714539796,46.5822724017097,12.1686327102632));
#63129=CARTESIAN_POINT('Ctrl Pts',(-2.1585595379306,46.5963319308722,12.0677701985499));
#63130=CARTESIAN_POINT('Ctrl Pts',(-2.10187305059963,46.6103505794577,11.9706580098738));
#63131=CARTESIAN_POINT('Ctrl Pts',(-2.08096405430936,46.6155214038476,11.934837861398));
#63132=CARTESIAN_POINT('Ctrl Pts',(-2.05913317880697,46.6206866739007,11.899527659463));
#63133=CARTESIAN_POINT('Ctrl Pts',(-2.03639456038824,46.6258440409837,11.8647807478773));
#63134=CARTESIAN_POINT('Ctrl Pts',(-2.03638593685606,46.625845996895,11.8647675702468));
#63135=CARTESIAN_POINT('Ctrl Pts',(-2.03637731319332,46.6258479528052,11.8647543926974));
#63136=CARTESIAN_POINT('Ctrl Pts',(-2.03636868940005,46.6258499087143,11.864741215229));
#63137=CARTESIAN_POINT('Ctrl Pts',(-1.99141350257691,46.6360459156751,11.7960480618037));
#63138=CARTESIAN_POINT('Ctrl Pts',(-1.94288302261679,46.6462057173813,11.7295064414119));
#63139=CARTESIAN_POINT('Ctrl Pts',(-1.89105741220381,46.6564390616992,11.6654615457098));
#63140=CARTESIAN_POINT('Ctrl Pts',(-1.88709149184184,46.6572221615658,11.6605605526694));
#63141=CARTESIAN_POINT('Ctrl Pts',(-1.88310626025049,46.6580056935545,11.6556741540323));
#63142=CARTESIAN_POINT('Ctrl Pts',(-1.87910183479348,46.6587897073237,11.6508024920328));
#63143=CARTESIAN_POINT('Ctrl Pts',(1.6569451353564,55.4128966646337,10.6605449173006));
#63144=CARTESIAN_POINT('Ctrl Pts',(2.33530670602075,55.5119034702439,11.0720924681345));
#63145=CARTESIAN_POINT('Ctrl Pts',(3.35287144550745,55.7089215617343,12.4309775396479));
#63146=CARTESIAN_POINT('Ctrl Pts',(3.06131862396214,56.0060657212896,14.970206851602));
#63147=CARTESIAN_POINT('Ctrl Pts',(1.11674766776748,56.3032657896637,16.6277723342266));
#63148=CARTESIAN_POINT('Ctrl Pts',(-1.45201060496089,56.602088525808,16.5144825668909));
#63149=CARTESIAN_POINT('Ctrl Pts',(-2.9552727303039,56.8520507440691,14.979981386742));
#63150=CARTESIAN_POINT('Ctrl Pts',(-3.29622519867115,57.052306151596,13.3826435061434));
#63151=CARTESIAN_POINT('Ctrl Pts',(-3.03946287691416,57.252676609567,11.7672071495042));
#63152=CARTESIAN_POINT('Ctrl Pts',(-1.90135817724995,57.4530663770427,10.4790510860224));
#63153=CARTESIAN_POINT('Ctrl Pts',(-0.331321547087517,57.653223522874,10.0240350930701));
#63154=CARTESIAN_POINT('Ctrl Pts',(1.02092307270453,57.8198122673918,10.1438419603152));
#63155=CARTESIAN_POINT('Ctrl Pts',(2.32847716926071,58.002702432299,10.9045066475814));
#63156=CARTESIAN_POINT('Ctrl Pts',(3.17902663186017,58.2016159780822,12.3119941431888));
#63157=CARTESIAN_POINT('Ctrl Pts',(3.25111765677419,58.3997743068538,13.9484260261249));
#63158=CARTESIAN_POINT('Ctrl Pts',(2.53332529252753,58.5970285722796,15.4132580743736));
#63159=CARTESIAN_POINT('Ctrl Pts',(1.20880262079472,58.7932309276008,16.349001183064));
#63160=CARTESIAN_POINT('Ctrl Pts',(-0.392972327268547,58.9882406659482,
16.5356913377198));
#63161=CARTESIAN_POINT('Ctrl Pts',(-1.87723242415658,59.1819184781718,15.9349461681502));
#63162=CARTESIAN_POINT('Ctrl Pts',(-2.71710555490916,59.3420967355076,14.9109753802198));
#63163=CARTESIAN_POINT('Ctrl Pts',(-3.03243667131599,59.4694445491574,13.9321695038961));
#63164=CARTESIAN_POINT('Ctrl Pts',(-3.09841455447119,59.5962431685408,12.9100621162179));
#63165=CARTESIAN_POINT('Ctrl Pts',(-2.69924485240655,59.7536690381048,11.6714562710649));
#63166=CARTESIAN_POINT('Ctrl Pts',(-1.57613832723902,59.9407574424593,10.6072778298864));
#63167=CARTESIAN_POINT('Ctrl Pts',(-0.096551163052406,60.1259118027667,
10.2150729201606));
#63168=CARTESIAN_POINT('Ctrl Pts',(1.37396628627166,60.3090339467634,10.5757102953909));
#63169=CARTESIAN_POINT('Ctrl Pts',(2.47908226284073,60.4900310898842,11.5848804741311));
#63170=CARTESIAN_POINT('Ctrl Pts',(2.95980408366685,60.6688191325761,12.9826417343107));
#63171=CARTESIAN_POINT('Ctrl Pts',(2.74235929646795,60.8257126597751,14.2617726150318));
#63172=CARTESIAN_POINT('Ctrl Pts',(2.13344390025228,60.9614695210831,15.1810775758813));
#63173=CARTESIAN_POINT('Ctrl Pts',(1.14324694123969,61.1152052069727,15.9444605983494));
#63174=CARTESIAN_POINT('Ctrl Pts',(-0.442597201666302,61.3046784881151,
16.1881055945206));
#63175=CARTESIAN_POINT('Ctrl Pts',(-1.95016975236964,61.5090501034515,15.3377070645724));
#63176=CARTESIAN_POINT('Ctrl Pts',(-2.63888887238414,61.6915669650262,13.9936833394969));
#63177=CARTESIAN_POINT('Ctrl Pts',(-2.60879331776602,61.8532873127061,12.6578979527681));
#63178=CARTESIAN_POINT('Ctrl Pts',(-1.95119277387709,62.0124516622465,11.5172602409941));
#63179=CARTESIAN_POINT('Ctrl Pts',(-0.846601874313005,62.1690601894784,
10.8418271444237));
#63180=CARTESIAN_POINT('Ctrl Pts',(0.425857363513597,62.3231222193529,10.7795975324474));
#63181=CARTESIAN_POINT('Ctrl Pts',(1.36594609467601,62.4494013640976,11.2333728797989));
#63182=CARTESIAN_POINT('Ctrl Pts',(1.91361895881445,62.5491746001873,11.8247167504303));
#63183=CARTESIAN_POINT('Ctrl Pts',(2.20031261426614,62.623386180769,12.351148983469));
#63184=CARTESIAN_POINT('Ctrl Pts',(2.34638492720226,62.6969812241368,12.927312881863));
#63185=CARTESIAN_POINT('Ctrl Pts',(2.34622867202676,62.794297702193,13.7136951888079));
#63186=CARTESIAN_POINT('Ctrl Pts',(1.98055868552105,62.9144348967284,14.6366736894937));
#63187=CARTESIAN_POINT('Ctrl Pts',(1.07943680968674,63.0562449888743,15.3885632620892));
#63188=CARTESIAN_POINT('Ctrl Pts',(-0.0517025031410053,63.1957665233168,
15.611357253593));
#63189=CARTESIAN_POINT('Ctrl Pts',(-1.25748872761872,63.3483316662509,15.2359395671154));
#63190=CARTESIAN_POINT('Ctrl Pts',(-2.13867141013038,63.5131145797047,14.153379855809));
#63191=CARTESIAN_POINT('Ctrl Pts',(-2.16335040768803,63.6893115604284,12.660199850989));
#63192=CARTESIAN_POINT('Ctrl Pts',(-1.2796523659689,63.8621839816488,11.4927639172216));
#63193=CARTESIAN_POINT('Ctrl Pts',(0.113042382290236,64.0320007008191,11.1257732842045));
#63194=CARTESIAN_POINT('Ctrl Pts',(1.19376322125476,64.1712099717327,11.5955981161));
#63195=CARTESIAN_POINT('Ctrl Pts',(1.74482084921513,64.2813450206176,12.3015104532762));
#63196=CARTESIAN_POINT('Ctrl Pts',(1.99967883271567,64.3770450715635,13.0361210359255));
#63197=CARTESIAN_POINT('Ctrl Pts',(1.92373662025134,64.4855227576122,13.9302995954116));
#63198=CARTESIAN_POINT('Ctrl Pts',(1.37247448803971,64.6065013765781,14.7653662718488));
#63199=CARTESIAN_POINT('Ctrl Pts',(0.494716294691718,64.7265690605065,15.2299530497279));
#63200=CARTESIAN_POINT('Ctrl Pts',(-0.491871158051163,64.8458671269723,
15.2191438616901));
#63201=CARTESIAN_POINT('Ctrl Pts',(-1.34795918795173,64.96455763081,14.7381624934));
#63202=CARTESIAN_POINT('Ctrl Pts',(-1.737771459396,65.0532306509411,14.1172205890816));
#63203=CARTESIAN_POINT('Ctrl Pts',(-1.89283496250823,65.1319236578043,13.5043914212779));
#63204=CARTESIAN_POINT('Ctrl Pts',(-1.89254479014124,65.2105336050236,12.8629868281662));
#63205=CARTESIAN_POINT('Ctrl Pts',(-1.5131484507725,65.3185043266858,12.0544839835084));
#63206=CARTESIAN_POINT('Ctrl Pts',(-0.726972137876947,65.436307457049,11.4786714103702));
#63207=CARTESIAN_POINT('Ctrl Pts',(0.240309264892923,65.554283263124,11.3496940189649));
#63208=CARTESIAN_POINT('Ctrl Pts',(1.15372183914517,65.6725903488457,11.7010113985837));
#63209=CARTESIAN_POINT('Ctrl Pts',(1.78960549170489,65.7913838071524,12.4501752820213));
#63210=CARTESIAN_POINT('Ctrl Pts',(1.98978935163561,65.9108195532194,13.4176318348034));
#63211=CARTESIAN_POINT('Ctrl Pts',(1.70010179189264,66.031048010758,14.3690921123399));
#63212=CARTESIAN_POINT('Ctrl Pts',(0.983696228421434,66.1522187579812,15.0698078200568));
#63213=CARTESIAN_POINT('Ctrl Pts',(-0.0976755268654362,66.2880612365788,
15.3766078480273));
#63214=CARTESIAN_POINT('Ctrl Pts',(-1.31878244840489,66.4392396164331,14.9904843787632));
#63215=CARTESIAN_POINT('Ctrl Pts',(-2.11559642723716,66.6066695529819,13.8144955958308));
#63216=CARTESIAN_POINT('Ctrl Pts',(-2.02851560781646,66.75208241469,12.5861000530642));
#63217=CARTESIAN_POINT('Ctrl Pts',(-1.46871591953313,66.8743804483054,11.7598210561588));
#63218=CARTESIAN_POINT('Ctrl Pts',(-0.590976964864925,67.0052427017216,
11.1517409461587));
#63219=CARTESIAN_POINT('Ctrl Pts',(0.836486125966097,67.1715005769598,11.088655253674));
#63220=CARTESIAN_POINT('Ctrl Pts',(2.17249609611971,67.3756418705779,12.2305198194672));
#63221=CARTESIAN_POINT('Ctrl Pts',(2.37549715084904,67.5847068153988,14.0174281878148));
#63222=CARTESIAN_POINT('Ctrl Pts',(1.27924295687799,67.7989571326317,15.4990495841261));
#63223=CARTESIAN_POINT('Ctrl Pts',(-0.578620920351347,68.0185939823309,
15.8438079846843));
#63224=CARTESIAN_POINT('Ctrl Pts',(-2.29959856019092,68.2557971598705,14.7465525063924));
#63225=CARTESIAN_POINT('Ctrl Pts',(-2.59210142572018,68.4223406725752,13.3131908810002));
#63226=CARTESIAN_POINT('Ctrl Pts',(-2.40813948819331,68.5130695044136,12.607364467103));
#63227=CARTESIAN_POINT('Ctrl Pts',(1.55030632904987,55.7588406051485,10.8358132077334));
#63228=CARTESIAN_POINT('Ctrl Pts',(2.17876663993083,55.8514133669438,11.2297589453932));
#63229=CARTESIAN_POINT('Ctrl Pts',(3.10425265743942,56.0346852578565,12.5086978226667));
#63230=CARTESIAN_POINT('Ctrl Pts',(2.7983392353447,56.3084852816261,14.8432409534713));
#63231=CARTESIAN_POINT('Ctrl Pts',(0.999166163143576,56.5799450362436,16.3288210786526));
#63232=CARTESIAN_POINT('Ctrl Pts',(-1.32580643434958,56.8507000918492,16.1904044489405));
#63233=CARTESIAN_POINT('Ctrl Pts',(-2.65653224227183,57.0755242670608,14.7903593192062));
#63234=CARTESIAN_POINT('Ctrl Pts',(-2.94151465380921,57.2547579143383,13.3570145845722));
#63235=CARTESIAN_POINT('Ctrl Pts',(-2.69226601616852,57.4335381145205,11.9192191403096));
#63236=CARTESIAN_POINT('Ctrl Pts',(-1.66478551166155,57.6115643239159,10.7899644198409));
#63237=CARTESIAN_POINT('Ctrl Pts',(-0.270097413097286,57.788721156688,10.40668375296));
#63238=CARTESIAN_POINT('Ctrl Pts',(0.922243286047465,57.9358340402107,10.5289617109777));
#63239=CARTESIAN_POINT('Ctrl Pts',(2.06444297016673,58.0969552999316,11.2149702554646));
#63240=CARTESIAN_POINT('Ctrl Pts',(2.79453271510212,58.2717826325117,12.462035133664));
#63241=CARTESIAN_POINT('Ctrl Pts',(2.8377849285338,58.4456085398852,13.897952306082));
#63242=CARTESIAN_POINT('Ctrl Pts',(2.19145453480309,58.6183767694301,15.1717938539383));
#63243=CARTESIAN_POINT('Ctrl Pts',(1.02160522451961,58.7900344295843,15.9740909181386));
#63244=CARTESIAN_POINT('Ctrl Pts',(-0.380669222056866,58.9605337467761,
16.1177395446806));
#63245=CARTESIAN_POINT('Ctrl Pts',(-1.67032812037787,59.1298305650957,15.574657980914));
#63246=CARTESIAN_POINT('Ctrl Pts',(-2.39184175344818,59.2698766903008,14.6693785233005));
#63247=CARTESIAN_POINT('Ctrl Pts',(-2.65547925022823,59.3812757961609,13.8095358651761));
#63248=CARTESIAN_POINT('Ctrl Pts',(-2.70048215198635,59.4922450908539,12.9145183722852));
#63249=CARTESIAN_POINT('Ctrl Pts',(-2.33557323358447,59.6301401972359,11.8349012228523));
#63250=CARTESIAN_POINT('Ctrl Pts',(-1.33720550047092,59.794285375669,10.915598661706));
#63251=CARTESIAN_POINT('Ctrl Pts',(-0.0317735574344565,59.9570811821498,
10.5895801462829));
#63252=CARTESIAN_POINT('Ctrl Pts',(1.25950858227736,60.1185138351077,10.9261995573682));
#63253=CARTESIAN_POINT('Ctrl Pts',(2.2233718578003,60.2785742015327,11.8326346868727));
#63254=CARTESIAN_POINT('Ctrl Pts',(2.63150737695493,60.4372585851517,13.0790938708883));
#63255=CARTESIAN_POINT('Ctrl Pts',(2.42070552945755,60.5770896003784,14.2157979806749));
#63256=CARTESIAN_POINT('Ctrl Pts',(1.86333929704872,60.6985554821939,15.0295958228732));
#63257=CARTESIAN_POINT('Ctrl Pts',(0.964146758236579,60.8365676763953,15.7006770391375));
#63258=CARTESIAN_POINT('Ctrl Pts',(-0.469990621989699,61.0075823543855,
15.8990905951955));
#63259=CARTESIAN_POINT('Ctrl Pts',(-1.82942006965859,61.1935399322503,15.1047258503496));
#63260=CARTESIAN_POINT('Ctrl Pts',(-2.44101035487483,61.3609220053499,13.8624175643746));
#63261=CARTESIAN_POINT('Ctrl Pts',(-2.39290165806376,61.5103093723956,12.6295218273013));
#63262=CARTESIAN_POINT('Ctrl Pts',(-1.76327705757714,61.6584778781679,11.5783996321574));
#63263=CARTESIAN_POINT('Ctrl Pts',(-0.716199583790733,61.8054689868533,
10.9624222170237));
#63264=CARTESIAN_POINT('Ctrl Pts',(0.488992325435071,61.9513295435539,10.9244754634972));
#63265=CARTESIAN_POINT('Ctrl Pts',(1.37900585512795,62.0719795781345,11.3737626521626));
#63266=CARTESIAN_POINT('Ctrl Pts',(1.89495908614165,62.1679858723417,11.952452288719));
#63267=CARTESIAN_POINT('Ctrl Pts',(2.16225961813357,62.2397432439528,12.4664773515498));
#63268=CARTESIAN_POINT('Ctrl Pts',(2.29327778325782,62.3112572030224,13.0287746925004));
#63269=CARTESIAN_POINT('Ctrl Pts',(2.27811114094167,62.4062990558202,13.7962768006778));
#63270=CARTESIAN_POINT('Ctrl Pts',(1.90119161550483,62.5245351899349,14.69731375192));
#63271=CARTESIAN_POINT('Ctrl Pts',(0.991059706471317,62.6655805612644,15.4273887252442));
#63272=CARTESIAN_POINT('Ctrl Pts',(-0.150004376109035,62.8058564957149,
15.6286856953522));
#63273=CARTESIAN_POINT('Ctrl Pts',(-1.36709509943824,62.9609447222707,15.222648270889));
#63274=CARTESIAN_POINT('Ctrl Pts',(-2.25211611298564,63.130653191994,14.0905190910481));
#63275=CARTESIAN_POINT('Ctrl Pts',(-2.24624586275741,63.3148678618416,12.5297620164941));
#63276=CARTESIAN_POINT('Ctrl Pts',(-1.28301168864727,63.4983480200434,11.311171244946));
#63277=CARTESIAN_POINT('Ctrl Pts',(0.224770595741629,63.6812901487001,10.9483526840942));
#63278=CARTESIAN_POINT('Ctrl Pts',(1.39390275914629,63.8334601868623,11.4879250790583));
#63279=CARTESIAN_POINT('Ctrl Pts',(1.98317789908194,63.9551256179044,12.2820193030557));
#63280=CARTESIAN_POINT('Ctrl Pts',(2.24617475003574,64.0615735288727,13.1053181121864));
#63281=CARTESIAN_POINT('Ctrl Pts',(2.13668022844515,64.1832525517915,14.105364041827));
#63282=CARTESIAN_POINT('Ctrl Pts',(1.48954809134978,64.3202627986689,15.034777364303));
#63283=CARTESIAN_POINT('Ctrl Pts',(0.473982051015632,64.4574800889518,15.5400576078666));
#63284=CARTESIAN_POINT('Ctrl Pts',(-0.66171351991401,64.594983404464,15.4986622727337));
#63285=CARTESIAN_POINT('Ctrl Pts',(-1.64085117064997,64.7328610307015,14.914831237791));
#63286=CARTESIAN_POINT('Ctrl Pts',(-2.07753209225151,64.8366078315501,14.1771813960306));
#63287=CARTESIAN_POINT('Ctrl Pts',(-2.24009694071431,64.929048128958,13.4531318429259));
#63288=CARTESIAN_POINT('Ctrl Pts',(-2.21963294989472,65.0216743325075,12.6981819858978));
#63289=CARTESIAN_POINT('Ctrl Pts',(-1.74549286459253,65.1495231060764,11.7537198628781));
#63290=CARTESIAN_POINT('Ctrl Pts',(-0.79283887697972,65.2896804488173,11.0942726574537));
#63291=CARTESIAN_POINT('Ctrl Pts',(0.365435937342801,65.4305951420548,10.9712986683346));
#63292=CARTESIAN_POINT('Ctrl Pts',(1.4473487981291,65.5723372986805,11.4211295951556));
#63293=CARTESIAN_POINT('Ctrl Pts',(2.18589654308168,65.714972902499,12.340214248751));
#63294=CARTESIAN_POINT('Ctrl Pts',(2.39511056864538,65.8585655679861,13.508592320582));
#63295=CARTESIAN_POINT('Ctrl Pts',(2.01640605087595,66.0031741366381,14.6424709362779));
#63296=CARTESIAN_POINT('Ctrl Pts',(1.13352498395727,66.1488542435468,15.4610899116906));
#63297=CARTESIAN_POINT('Ctrl Pts',(-0.173417136522122,66.3119687801929,
15.7946856755799));
#63298=CARTESIAN_POINT('Ctrl Pts',(-1.62240671165605,66.4930630885744,15.293817234782));
#63299=CARTESIAN_POINT('Ctrl Pts',(-2.53500320867109,66.6928009644741,13.8672779219842));
#63300=CARTESIAN_POINT('Ctrl Pts',(-2.39383160202435,66.8653436855591,12.4138986555751));
#63301=CARTESIAN_POINT('Ctrl Pts',(-1.709215002913,67.0097186748878,11.4559652991775));
#63302=CARTESIAN_POINT('Ctrl Pts',(-0.660294050672969,67.1635832522325,
10.7671026808167));
#63303=CARTESIAN_POINT('Ctrl Pts',(1.00756509210864,67.3578056337846,10.7361814279581));
#63304=CARTESIAN_POINT('Ctrl Pts',(2.5182626185487,67.59394679212,12.0948221133186));
#63305=CARTESIAN_POINT('Ctrl Pts',(2.69974491017161,67.8331851043461,14.1434923407273));
#63306=CARTESIAN_POINT('Ctrl Pts',(1.42035678851664,68.0755129907451,15.7878664622788));
#63307=CARTESIAN_POINT('Ctrl Pts',(-0.662768296243718,68.3209020968419,
16.1235997088386));
#63308=CARTESIAN_POINT('Ctrl Pts',(-2.53145414382765,68.5825321030457,14.8705287716948));
#63309=CARTESIAN_POINT('Ctrl Pts',(-2.81335053070336,68.7636377248232,13.3051962830399));
#63310=CARTESIAN_POINT('Ctrl Pts',(-2.60004493251108,68.8615196046778,12.5484192313165));
#63311=CARTESIAN_POINT('Ctrl Pts',(1.44366752274332,56.1047845456634,11.0110814981665));
#63312=CARTESIAN_POINT('Ctrl Pts',(2.02222657384092,56.1909232636435,11.387425422652));
#63313=CARTESIAN_POINT('Ctrl Pts',(2.85563386937139,56.3604489539787,12.5864181056853));
#63314=CARTESIAN_POINT('Ctrl Pts',(2.53535984672727,56.6109048419626,14.7162750553406));
#63315=CARTESIAN_POINT('Ctrl Pts',(0.881584658519683,56.8566242828234,16.0298698230785));
#63316=CARTESIAN_POINT('Ctrl Pts',(-1.19960226373825,57.0993116578905,15.8663263309902));
#63317=CARTESIAN_POINT('Ctrl Pts',(-2.35779175423974,57.2989977900524,14.6007372516703));
#63318=CARTESIAN_POINT('Ctrl Pts',(-2.58680410894727,57.4572096770807,13.3313856630009));
#63319=CARTESIAN_POINT('Ctrl Pts',(-2.34506915542287,57.6143996194741,12.0712311311148));
#63320=CARTESIAN_POINT('Ctrl Pts',(-1.42821284607315,57.7700622707892,11.1008777536595));
#63321=CARTESIAN_POINT('Ctrl Pts',(-0.208873279107056,57.9242187905022,
10.78933241285));
#63322=CARTESIAN_POINT('Ctrl Pts',(0.823563499390395,58.0518558130299,10.9140814616404));
#63323=CARTESIAN_POINT('Ctrl Pts',(1.80040877107275,58.191208167564,11.5254338633479));
#63324=CARTESIAN_POINT('Ctrl Pts',(2.41003879834408,58.3419492869412,12.6120761241389));
#63325=CARTESIAN_POINT('Ctrl Pts',(2.42445220029341,58.4914427729167,13.8474785860391));
#63326=CARTESIAN_POINT('Ctrl Pts',(1.84958377707867,58.6397249665805,14.930329633503));
#63327=CARTESIAN_POINT('Ctrl Pts',(0.834407828244496,58.7868379315678,15.5991806532132));
#63328=CARTESIAN_POINT('Ctrl Pts',(-0.368366116845181,58.9328268276039,
15.6997877516412));
#63329=CARTESIAN_POINT('Ctrl Pts',(-1.46342381659914,59.0777426520196,15.214369793678));
#63330=CARTESIAN_POINT('Ctrl Pts',(-2.06657795198719,59.1976566450941,14.4277816663813));
#63331=CARTESIAN_POINT('Ctrl Pts',(-2.27852182914047,59.2931070431642,13.6869022264562));
#63332=CARTESIAN_POINT('Ctrl Pts',(-2.30254974950152,59.388247013167,12.9189746283525));
#63333=CARTESIAN_POINT('Ctrl Pts',(-1.97190161476237,59.5066113563671,11.9983461746398));
#63334=CARTESIAN_POINT('Ctrl Pts',(-1.09827267370282,59.6478133088788,11.2239194935258));
#63335=CARTESIAN_POINT('Ctrl Pts',(0.0330040481834923,59.7882505615329,
10.9640873724053));
#63336=CARTESIAN_POINT('Ctrl Pts',(1.14505087828308,59.9279937234519,11.2766888193456));
#63337=CARTESIAN_POINT('Ctrl Pts',(1.96766145275984,60.0671173131813,12.0803888996145));
#63338=CARTESIAN_POINT('Ctrl Pts',(2.30321067024301,60.2056980377275,13.175546007466));
#63339=CARTESIAN_POINT('Ctrl Pts',(2.09905176244713,60.3284665409815,14.1698233463179));
#63340=CARTESIAN_POINT('Ctrl Pts',(1.59323469384517,60.4356414433047,14.8781140698653));
#63341=CARTESIAN_POINT('Ctrl Pts',(0.785046575233456,60.5579301458178,15.4568934799259));
#63342=CARTESIAN_POINT('Ctrl Pts',(-0.497384042313105,60.710486220656,15.6100755958704));
#63343=CARTESIAN_POINT('Ctrl Pts',(-1.70867038694753,60.8780297610492,14.8717446361267));
#63344=CARTESIAN_POINT('Ctrl Pts',(-2.24313183736552,61.0302770456738,13.7311517892522));
#63345=CARTESIAN_POINT('Ctrl Pts',(-2.17700999836153,61.1673314320849,12.6011457018345));
#63346=CARTESIAN_POINT('Ctrl Pts',(-1.5753613412772,61.3045040940893,11.6395390233208));
#63347=CARTESIAN_POINT('Ctrl Pts',(-0.585797293268466,61.4418777842281,
11.0830172896236));
#63348=CARTESIAN_POINT('Ctrl Pts',(0.552127287356539,61.579536867755,11.069353394547));
#63349=CARTESIAN_POINT('Ctrl Pts',(1.39206561557985,61.6945577921715,11.5141524245262));
#63350=CARTESIAN_POINT('Ctrl Pts',(1.87629921346887,61.7867971444959,12.0801878270077));
#63351=CARTESIAN_POINT('Ctrl Pts',(2.12420662200097,61.8561003071363,12.5818057196306));
#63352=CARTESIAN_POINT('Ctrl Pts',(2.24017063931338,61.9255331819081,13.1302365031378));
#63353=CARTESIAN_POINT('Ctrl Pts',(2.20999360985659,62.0183004094474,13.8788584125477));
#63354=CARTESIAN_POINT('Ctrl Pts',(1.82182454548863,62.1346354831413,14.7579538143466));
#63355=CARTESIAN_POINT('Ctrl Pts',(0.902682603255894,62.2749161336543,15.4662141883991));
#63356=CARTESIAN_POINT('Ctrl Pts',(-0.248306249077079,62.4159464681129,
15.6460141371113));
#63357=CARTESIAN_POINT('Ctrl Pts',(-1.47670147125775,62.5735577782905,15.2093569746626));
#63358=CARTESIAN_POINT('Ctrl Pts',(-2.36556081584091,62.7481918042831,14.0276583262871));
#63359=CARTESIAN_POINT('Ctrl Pts',(-2.3291413178268,62.9404241632548,12.3993241819992));
#63360=CARTESIAN_POINT('Ctrl Pts',(-1.28637101132565,63.1345120584382,11.1295785726704));
#63361=CARTESIAN_POINT('Ctrl Pts',(0.336498809193019,63.3305795965811,10.7709320839836));
#63362=CARTESIAN_POINT('Ctrl Pts',(1.5940422970378,63.495710401992,11.3802520420165));
#63363=CARTESIAN_POINT('Ctrl Pts',(2.22153494894874,63.6289062151912,12.2625281528353));
#63364=CARTESIAN_POINT('Ctrl Pts',(2.49267066735581,63.7461019861821,13.1745151884475));
#63365=CARTESIAN_POINT('Ctrl Pts',(2.34962383663894,63.8809823459707,14.2804284882425));
#63366=CARTESIAN_POINT('Ctrl Pts',(1.60662169465985,64.0340242207596,15.304188456757));
#63367=CARTESIAN_POINT('Ctrl Pts',(0.453247807339546,64.1883911173971,15.8501621660054));
#63368=CARTESIAN_POINT('Ctrl Pts',(-0.831555881776861,64.3440996819558,
15.7781806837776));
#63369=CARTESIAN_POINT('Ctrl Pts',(-1.93374315334822,64.501164430593,15.091499982182));
#63370=CARTESIAN_POINT('Ctrl Pts',(-2.41729272510702,64.6199850121592,14.2371422029794));
#63371=CARTESIAN_POINT('Ctrl Pts',(-2.58735891892037,64.7261726001119,13.401872264574));
#63372=CARTESIAN_POINT('Ctrl Pts',(-2.54672110964819,64.8328150599913,12.5333771436294));
#63373=CARTESIAN_POINT('Ctrl Pts',(-1.97783727841256,64.9805418854671,11.4529557422479));
#63374=CARTESIAN_POINT('Ctrl Pts',(-0.858705616082495,65.1430534405857,
10.7098739045374));
#63375=CARTESIAN_POINT('Ctrl Pts',(0.490562609792683,65.3069070209856,10.5929033177043));
#63376=CARTESIAN_POINT('Ctrl Pts',(1.74097575711306,65.4720842485154,11.1412477917274));
#63377=CARTESIAN_POINT('Ctrl Pts',(2.58218759445846,65.6385619978454,12.2302532154808));
#63378=CARTESIAN_POINT('Ctrl Pts',(2.80043178565517,65.8063115827527,13.5995528063605));
#63379=CARTESIAN_POINT('Ctrl Pts',(2.33271030985925,65.9753002625182,14.915849760216));
#63380=CARTESIAN_POINT('Ctrl Pts',(1.28335373949313,66.1454897291123,15.8523720033243));
#63381=CARTESIAN_POINT('Ctrl Pts',(-0.249158746178807,66.3358763238071,
16.2127635031324));
#63382=CARTESIAN_POINT('Ctrl Pts',(-1.92603097490719,66.5468865607158,15.5971500908009));
#63383=CARTESIAN_POINT('Ctrl Pts',(-2.95440999010503,66.7789323759663,13.9200602481374));
#63384=CARTESIAN_POINT('Ctrl Pts',(-2.75914759623228,66.9786049564283,12.2416972580859));
#63385=CARTESIAN_POINT('Ctrl Pts',(-1.94971408629286,67.14505690147,11.1521095421962));
#63386=CARTESIAN_POINT('Ctrl Pts',(-0.729611136481014,67.3219238027436,
10.3824644154745));
#63387=CARTESIAN_POINT('Ctrl Pts',(1.17864405825117,67.5441106906095,10.383707602242));
#63388=CARTESIAN_POINT('Ctrl Pts',(2.8640291409777,67.8122517136621,11.9591244071702));
#63389=CARTESIAN_POINT('Ctrl Pts',(3.02399266949419,68.0816633932933,14.2695564936399));
#63390=CARTESIAN_POINT('Ctrl Pts',(1.56147062015531,68.3520688488585,16.0766833404313));
#63391=CARTESIAN_POINT('Ctrl Pts',(-0.746915672136096,68.6232102113529,
16.4033914329926));
#63392=CARTESIAN_POINT('Ctrl Pts',(-2.76330972746438,68.909267046221,14.9945050369972));
#63393=CARTESIAN_POINT('Ctrl Pts',(-3.03459963568654,69.1049347770713,13.2972016850794));
#63394=CARTESIAN_POINT('Ctrl Pts',(-2.79195037682888,69.2099697049419,12.4894739955298));
#63395=CARTESIAN_POINT('Ctrl Pts',(1.33702871643679,56.4507284861783,11.1863497885993));
#63396=CARTESIAN_POINT('Ctrl Pts',(1.865686507751,56.5304331603432,11.5450918999109));
#63397=CARTESIAN_POINT('Ctrl Pts',(2.60701508130335,56.6862126501008,12.664138388704));
#63398=CARTESIAN_POINT('Ctrl Pts',(2.27238045810983,56.9133244022991,14.5893091572099));
#63399=CARTESIAN_POINT('Ctrl Pts',(0.764003153895783,57.1333035294033,15.7309185675046));
#63400=CARTESIAN_POINT('Ctrl Pts',(-1.07339809312691,57.3479232239317,15.5422482130399));
#63401=CARTESIAN_POINT('Ctrl Pts',(-2.05905126620767,57.5224713130439,14.4111151841345));
#63402=CARTESIAN_POINT('Ctrl Pts',(-2.23209356408533,57.659661439823,13.3057567414297));
#63403=CARTESIAN_POINT('Ctrl Pts',(-1.99787229467723,57.7952611244277,12.2232431219201));
#63404=CARTESIAN_POINT('Ctrl Pts',(-1.19164018048475,57.9285602176624,11.4117910874779));
#63405=CARTESIAN_POINT('Ctrl Pts',(-0.147649145116826,58.0597164243163,
11.1719810727399));
#63406=CARTESIAN_POINT('Ctrl Pts',(0.724883712733328,58.1678775858489,11.2992012123028));
#63407=CARTESIAN_POINT('Ctrl Pts',(1.53637457197876,58.2854610351965,11.8358974712311));
#63408=CARTESIAN_POINT('Ctrl Pts',(2.02554488158604,58.4121159413706,12.7621171146141));
#63409=CARTESIAN_POINT('Ctrl Pts',(2.01111947205303,58.5372770059481,13.7970048659963));
#63410=CARTESIAN_POINT('Ctrl Pts',(1.50771301935423,58.6610731637311,14.6888654130677));
#63411=CARTESIAN_POINT('Ctrl Pts',(0.647210431969383,58.7836414335513,15.2242703882877));
#63412=CARTESIAN_POINT('Ctrl Pts',(-0.3560630116335,58.9051199084318,15.2818359586019));
#63413=CARTESIAN_POINT('Ctrl Pts',(-1.25651951282042,59.0256547389435,14.8540816064417));
#63414=CARTESIAN_POINT('Ctrl Pts',(-1.74131415052621,59.1254365998873,14.1861848094619));
#63415=CARTESIAN_POINT('Ctrl Pts',(-1.9015644080527,59.2049382901675,13.5642685877362));
#63416=CARTESIAN_POINT('Ctrl Pts',(-1.90461734701668,59.28424893548,12.9234308844198));
#63417=CARTESIAN_POINT('Ctrl Pts',(-1.60822999594029,59.3830825154982,12.161791126427));
#63418=CARTESIAN_POINT('Ctrl Pts',(-0.859339846934732,59.5013412420884,
11.5322403253455));
#63419=CARTESIAN_POINT('Ctrl Pts',(0.0977816538014409,59.6194199409159,
11.3385945985277));
#63420=CARTESIAN_POINT('Ctrl Pts',(1.0305931742888,59.7374736117961,11.6271780813229));
#63421=CARTESIAN_POINT('Ctrl Pts',(1.71195104771939,59.8556604248299,12.3281431123561));
#63422=CARTESIAN_POINT('Ctrl Pts',(1.9749139635311,59.9741374903032,13.2719981440439));
#63423=CARTESIAN_POINT('Ctrl Pts',(1.77739799543672,60.0798434815848,14.1238487119609));
#63424=CARTESIAN_POINT('Ctrl Pts',(1.32313009064161,60.1727274044155,14.7266323168573));
#63425=CARTESIAN_POINT('Ctrl Pts',(0.605946392230338,60.2792926152404,15.213109920714));
#63426=CARTESIAN_POINT('Ctrl Pts',(-0.524777462636502,60.4133900869263,
15.3210605965453));
#63427=CARTESIAN_POINT('Ctrl Pts',(-1.58792070423647,60.5625195898481,14.638763421904));
#63428=CARTESIAN_POINT('Ctrl Pts',(-2.04525331985621,60.6996320859974,13.5998860141298));
#63429=CARTESIAN_POINT('Ctrl Pts',(-1.96111833865927,60.8243534917744,12.5727695763677));
#63430=CARTESIAN_POINT('Ctrl Pts',(-1.38744562497725,60.9505303100106,11.7006784144841));
#63431=CARTESIAN_POINT('Ctrl Pts',(-0.455395002746195,61.078286581603,11.2036123622235));
#63432=CARTESIAN_POINT('Ctrl Pts',(0.61526224927801,61.207744191956,11.2142313255967));
#63433=CARTESIAN_POINT('Ctrl Pts',(1.40512537603178,61.3171360062083,11.6545421968898));
#63434=CARTESIAN_POINT('Ctrl Pts',(1.85763934079607,61.4056084166502,12.2079233652964));
#63435=CARTESIAN_POINT('Ctrl Pts',(2.0861536258684,61.47245737032,12.6971340877114));
#63436=CARTESIAN_POINT('Ctrl Pts',(2.18706349536892,61.5398091607938,13.2316983137753));
#63437=CARTESIAN_POINT('Ctrl Pts',(2.1418760787715,61.6303017630745,13.9614400244176));
#63438=CARTESIAN_POINT('Ctrl Pts',(1.74245747547242,61.7447357763476,14.8185938767729));
#63439=CARTESIAN_POINT('Ctrl Pts',(0.81430550004047,61.8842517060443,15.505039651554));
#63440=CARTESIAN_POINT('Ctrl Pts',(-0.346608122045112,62.0260364405109,
15.6633425788705));
#63441=CARTESIAN_POINT('Ctrl Pts',(-1.58630784307727,62.1861708343101,15.1960656784363));
#63442=CARTESIAN_POINT('Ctrl Pts',(-2.47900551869618,62.3657304165722,13.9647975615262));
#63443=CARTESIAN_POINT('Ctrl Pts',(-2.41203677289619,62.5659804646678,12.2688863475043));
#63444=CARTESIAN_POINT('Ctrl Pts',(-1.28973033400403,62.7706760968329,10.9479859003946));
#63445=CARTESIAN_POINT('Ctrl Pts',(0.448227022644404,62.9798690444623,10.5935114838732));
#63446=CARTESIAN_POINT('Ctrl Pts',(1.7941818349293,63.1579606171217,11.2725790049749));
#63447=CARTESIAN_POINT('Ctrl Pts',(2.45989199881554,63.302686812478,12.2430370026149));
#63448=CARTESIAN_POINT('Ctrl Pts',(2.73916658467588,63.4306304434913,13.2437122647084));
#63449=CARTESIAN_POINT('Ctrl Pts',(2.56256744483272,63.5787121401499,14.4554929346579));
#63450=CARTESIAN_POINT('Ctrl Pts',(1.7236952979699,63.7477856428504,15.5735995492112));
#63451=CARTESIAN_POINT('Ctrl Pts',(0.432513563663454,63.9193021458423,16.1602667241441));
#63452=CARTESIAN_POINT('Ctrl Pts',(-1.00139824363972,64.0932159594475,16.0576990948213));
#63453=CARTESIAN_POINT('Ctrl Pts',(-2.22663513604646,64.2694678304844,15.2681687265729));
#63454=CARTESIAN_POINT('Ctrl Pts',(-2.75705335796253,64.4033621927682,14.2971030099283));
#63455=CARTESIAN_POINT('Ctrl Pts',(-2.93462089712645,64.5232970712658,13.3506126862221));
#63456=CARTESIAN_POINT('Ctrl Pts',(-2.87380926940167,64.6439557874752,12.3685723013612));
#63457=CARTESIAN_POINT('Ctrl Pts',(-2.21018169223259,64.8115606648577,11.1521916216177));
#63458=CARTESIAN_POINT('Ctrl Pts',(-0.924572355185274,64.9964264323541,
10.325475151621));
#63459=CARTESIAN_POINT('Ctrl Pts',(0.615689282242555,65.1832188999163,10.2145079670741));
#63460=CARTESIAN_POINT('Ctrl Pts',(2.03460271609701,65.3718311983502,10.8613659882994));
#63461=CARTESIAN_POINT('Ctrl Pts',(2.97847864583523,65.5621510931919,12.1202921822106));
#63462=CARTESIAN_POINT('Ctrl Pts',(3.20575300266493,65.7540575975192,13.6905132921389));
#63463=CARTESIAN_POINT('Ctrl Pts',(2.64901456884257,65.9474263883983,15.1892285841541));
#63464=CARTESIAN_POINT('Ctrl Pts',(1.43318249502898,66.1421252146777,16.2436540949582));
#63465=CARTESIAN_POINT('Ctrl Pts',(-0.324900355835495,66.3597838674212,
16.630841330685));
#63466=CARTESIAN_POINT('Ctrl Pts',(-2.22965523815834,66.6007100328571,15.9004829468197));
#63467=CARTESIAN_POINT('Ctrl Pts',(-3.37381677153895,66.8650637874584,13.9728425742908));
#63468=CARTESIAN_POINT('Ctrl Pts',(-3.12446359044018,67.0918662272974,12.0694958605968));
#63469=CARTESIAN_POINT('Ctrl Pts',(-2.19021316967273,67.2803951280524,10.8482537852148));
#63470=CARTESIAN_POINT('Ctrl Pts',(-0.798928222289059,67.4802643532546,
9.99782615013244));
#63471=CARTESIAN_POINT('Ctrl Pts',(1.34972302439372,67.7304157474343,10.0312337765259));
#63472=CARTESIAN_POINT('Ctrl Pts',(3.20979566340669,68.0305566352042,11.8234267010217));
#63473=CARTESIAN_POINT('Ctrl Pts',(3.34824042881676,68.3301416822406,14.3956206465524));
#63474=CARTESIAN_POINT('Ctrl Pts',(1.70258445179397,68.6286247069719,16.3655002185839));
#63475=CARTESIAN_POINT('Ctrl Pts',(-0.831063048028466,68.925518325864,16.6831831571466));
#63476=CARTESIAN_POINT('Ctrl Pts',(-2.9951653111011,69.2360019893962,15.1184813022997));
#63477=CARTESIAN_POINT('Ctrl Pts',(-3.25584874066971,69.4462318293195,13.2892070871188));
#63478=CARTESIAN_POINT('Ctrl Pts',(-2.98385582114668,69.5584198052059,12.4305287597433));
#63479=CARTESIAN_POINT('Ctrl Pts',(1.36952200671963,56.456522023403,11.210153809184));
#63480=CARTESIAN_POINT('Ctrl Pts',(1.46915479225293,56.4711352014148,11.2795181510653));
#63481=CARTESIAN_POINT('Ctrl Pts',(1.56373629895278,56.485870845212,11.3557719878152));
#63482=CARTESIAN_POINT('Ctrl Pts',(1.65197830956387,56.5006895712442,11.4383671401521));
#63483=CARTESIAN_POINT('Ctrl Pts',(1.70737706113225,56.5099928375267,11.4902207673913));
#63484=CARTESIAN_POINT('Ctrl Pts',(1.76027691285286,56.5193288095134,11.5445726741234));
#63485=CARTESIAN_POINT('Ctrl Pts',(1.81035947915606,56.5286873433543,11.601276770048));
#63486=CARTESIAN_POINT('Ctrl Pts',(1.88979050117883,56.543529991455,11.6912095475521));
#63487=CARTESIAN_POINT('Ctrl Pts',(1.96213299726991,56.558429483682,11.7870613695224));
#63488=CARTESIAN_POINT('Ctrl Pts',(2.02695886821799,56.5733438778432,11.8875325464049));
#63489=CARTESIAN_POINT('Ctrl Pts',(2.09252685586196,56.5884290097169,11.9891539020159));
#63490=CARTESIAN_POINT('Ctrl Pts',(2.15040431437628,56.6035293837288,12.095499941867));
#63491=CARTESIAN_POINT('Ctrl Pts',(2.20018409192502,56.6185997150804,12.2051859417651));
#63492=CARTESIAN_POINT('Ctrl Pts',(2.24899952968614,56.6333781021757,12.3127470913916));
#63493=CARTESIAN_POINT('Ctrl Pts',(2.29002742551468,56.6481275864915,12.4235187978667));
#63494=CARTESIAN_POINT('Ctrl Pts',(2.32292804780908,56.6628037938509,12.5361744777578));
#63495=CARTESIAN_POINT('Ctrl Pts',(2.34058678061769,56.6706809465104,12.5966400985223));
#63496=CARTESIAN_POINT('Ctrl Pts',(2.35590503222919,56.6785369620146,12.6576482027778));
#63497=CARTESIAN_POINT('Ctrl Pts',(2.36883652287042,56.6863647942985,12.7189930735352));
#63498=CARTESIAN_POINT('Ctrl Pts',(2.39398426951609,56.7015875051616,12.8382898592361));
#63499=CARTESIAN_POINT('Ctrl Pts',(2.41022684587955,56.7168011823224,12.9592973300442));
#63500=CARTESIAN_POINT('Ctrl Pts',(2.41708988396143,56.73199278412,13.0805678610677));
#63501=CARTESIAN_POINT('Ctrl Pts',(2.42441418136815,56.7482054013782,13.2099888879205));
#63502=CARTESIAN_POINT('Ctrl Pts',(2.4210541734813,56.7643928764075,13.3397084907732));
#63503=CARTESIAN_POINT('Ctrl Pts',(2.40748602314114,56.7805392535346,13.4680953009946));
#63504=CARTESIAN_POINT('Ctrl Pts',(2.39363959749359,56.7970167839836,13.5991152541414));
#63505=CARTESIAN_POINT('Ctrl Pts',(2.36916218100632,56.8134515121532,13.7287459024911));
#63506=CARTESIAN_POINT('Ctrl Pts',(2.33461478926672,56.8298263323069,13.8552462620182));
#63507=CARTESIAN_POINT('Ctrl Pts',(2.30038099907859,56.8460525111668,13.9805983233087));
#63508=CARTESIAN_POINT('Ctrl Pts',(2.25625968067984,56.8622198625916,14.1028753579633));
#63509=CARTESIAN_POINT('Ctrl Pts',(2.20284497159892,56.8783116252546,14.2203959349855));
#63510=CARTESIAN_POINT('Ctrl Pts',(2.16523804021797,56.8896411227784,14.3031369692805));
#63511=CARTESIAN_POINT('Ctrl Pts',(2.12302543917162,56.9009331488864,14.383520485037));
#63512=CARTESIAN_POINT('Ctrl Pts',(2.07642721540174,56.9121818271769,14.4609687618267));
#63513=CARTESIAN_POINT('Ctrl Pts',(2.05084753377501,56.9183566893522,14.5034833064283));
#63514=CARTESIAN_POINT('Ctrl Pts',(2.02393973676091,56.9245292662071,14.5451342256592));
#63515=CARTESIAN_POINT('Ctrl Pts',(1.99573526534201,56.9306991957531,14.5858283392573));
#63516=CARTESIAN_POINT('Ctrl Pts',(1.87461643961411,56.9571948038551,14.760581596634));
#63517=CARTESIAN_POINT('Ctrl Pts',(1.72958135983153,56.9836417604212,14.9176889956811));
#63518=CARTESIAN_POINT('Ctrl Pts',(1.56726157064771,57.0100104770603,15.0528795939312));
#63519=CARTESIAN_POINT('Ctrl Pts',(1.41029786293072,57.0355091026574,15.1836092951987));
#63520=CARTESIAN_POINT('Ctrl Pts',(1.23717304322571,57.0609345399046,15.2938430214388));
#63521=CARTESIAN_POINT('Ctrl Pts',(1.05391732366964,57.0862582787262,15.3797486128614));
#63522=CARTESIAN_POINT('Ctrl Pts',(0.959359416725181,57.0993250454541,15.4240749396982));
#63523=CARTESIAN_POINT('Ctrl Pts',(0.862104619060483,57.1123647089386,15.4619246795065));
#63524=CARTESIAN_POINT('Ctrl Pts',(0.762982644582906,57.1253731946399,15.4927768488092));
#63525=CARTESIAN_POINT('Ctrl Pts',(0.745090725751282,57.1277212791239,15.4983457906292));
#63526=CARTESIAN_POINT('Ctrl Pts',(0.727137971166554,57.1300683475208,15.5036867518304));
#63527=CARTESIAN_POINT('Ctrl Pts',(0.709129923407988,57.1324143756952,15.5088003294947));
#63528=CARTESIAN_POINT('Ctrl Pts',(0.576167781695582,57.1497362383857,15.5465563509793));
#63529=CARTESIAN_POINT('Ctrl Pts',(0.440014625634233,57.166977374934,15.5719390453827));
#63530=CARTESIAN_POINT('Ctrl Pts',(0.30295689367336,57.1841542470737,15.5851230291766));
#63531=CARTESIAN_POINT('Ctrl Pts',(0.162785739243805,57.2017213114258,15.5986065021769));
#63532=CARTESIAN_POINT('Ctrl Pts',(0.0216699639080719,57.2192211623843,
15.5993309988529));
#63533=CARTESIAN_POINT('Ctrl Pts',(-0.117938738247654,57.2366727970848,
15.5875382594333));
#63534=CARTESIAN_POINT('Ctrl Pts',(-0.255122987319975,57.2538213656518,
15.5759503134328));
#63535=CARTESIAN_POINT('Ctrl Pts',(-0.390850693548286,57.2709233908915,
15.5522766269456));
#63536=CARTESIAN_POINT('Ctrl Pts',(-0.522811632813748,57.2879980833134,
15.5167927491621));
#63537=CARTESIAN_POINT('Ctrl Pts',(-0.594243683425765,57.2972408205965,
15.4975848974458));
#63538=CARTESIAN_POINT('Ctrl Pts',(-0.664572399923294,57.3064755683326,
15.4749171931375));
#63539=CARTESIAN_POINT('Ctrl Pts',(-0.73343539588025,57.315705502545,15.4488383768472));
#63540=CARTESIAN_POINT('Ctrl Pts',(-0.812199921677987,57.3262625714219,
15.4190097937318));
#63541=CARTESIAN_POINT('Ctrl Pts',(-0.889046791608116,57.3368133410116,
15.3847187452103));
#63542=CARTESIAN_POINT('Ctrl Pts',(-0.963590004270745,57.3473627169651,
15.3463487943232));
#63543=CARTESIAN_POINT('Ctrl Pts',(-1.08193195564432,57.3641105024645,15.2854341288574));
#63544=CARTESIAN_POINT('Ctrl Pts',(-1.19471796432954,57.3807339436101,15.214041258376));
#63545=CARTESIAN_POINT('Ctrl Pts',(-1.3003244675683,57.3972693450953,15.1336235297956));
#63546=CARTESIAN_POINT('Ctrl Pts',(-1.41254409492565,57.4148402004495,15.0481700088717));
#63547=CARTESIAN_POINT('Ctrl Pts',(-1.51665560727272,57.4323116416365,14.9525269778875));
#63548=CARTESIAN_POINT('Ctrl Pts',(-1.61074790517429,57.4497293507773,14.848487847841));
#63549=CARTESIAN_POINT('Ctrl Pts',(-1.70484020307585,57.4671470599181,14.7444487177944));
#63550=CARTESIAN_POINT('Ctrl Pts',(-1.78891233014478,57.4845110575209,14.6320149368002));
#63551=CARTESIAN_POINT('Ctrl Pts',(-1.8611057861045,57.5018689170491,14.5130081981115));
#63552=CARTESIAN_POINT('Ctrl Pts',(-1.9315731818671,57.5188117706735,14.3968467698753));
#63553=CARTESIAN_POINT('Ctrl Pts',(-1.99072369019082,57.5357488018311,14.2744246847192));
#63554=CARTESIAN_POINT('Ctrl Pts',(-2.03825416039261,57.5527258161985,14.1481060172276));
#63555=CARTESIAN_POINT('Ctrl Pts',(-2.04206738360015,57.5540878297639,14.1379718596571));
#63556=CARTESIAN_POINT('Ctrl Pts',(-2.04580584336057,57.5554501013471,14.1278126166248));
#63557=CARTESIAN_POINT('Ctrl Pts',(-2.04946939738334,57.5568126549421,14.1176295051128));
#63558=CARTESIAN_POINT('Ctrl Pts',(-2.08629397670067,57.5705084985468,14.015272942267));
#63559=CARTESIAN_POINT('Ctrl Pts',(-2.11552985890596,57.584067304602,13.9104423303983));
#63560=CARTESIAN_POINT('Ctrl Pts',(-2.13703900698149,57.5975463105243,13.8042550242954));
#63561=CARTESIAN_POINT('Ctrl Pts',(-2.15823222694189,57.610827335712,13.6996274059752));
#63562=CARTESIAN_POINT('Ctrl Pts',(-2.17192429643729,57.624030899012,13.5936813263486));
#63563=CARTESIAN_POINT('Ctrl Pts',(-2.17793518415767,57.6372124451921,13.4874740432984));
#63564=CARTESIAN_POINT('Ctrl Pts',(-2.18130687263158,57.6446063725771,13.4278991703739));
#63565=CARTESIAN_POINT('Ctrl Pts',(-2.18226084418098,57.6519933839862,13.3682420118614));
#63566=CARTESIAN_POINT('Ctrl Pts',(-2.18075809699843,57.6593833431459,13.3086899191046));
#63567=CARTESIAN_POINT('Ctrl Pts',(-2.17908779112742,57.667597294444,13.2424976737842));
#63568=CARTESIAN_POINT('Ctrl Pts',(-2.17438685459266,57.6758318257226,13.1764779016195));
#63569=CARTESIAN_POINT('Ctrl Pts',(-2.16660982827104,57.6840728077332,13.1109318190068));
#63570=CARTESIAN_POINT('Ctrl Pts',(-2.15443325449219,57.6969758019257,13.0083056122999));
#63571=CARTESIAN_POINT('Ctrl Pts',(-2.13471323311804,57.7098946288363,12.9068415882772));
#63572=CARTESIAN_POINT('Ctrl Pts',(-2.10799407319067,57.7227746974414,12.8075421459927));
#63573=CARTESIAN_POINT('Ctrl Pts',(-2.0812749132633,57.7356547660465,12.7082427037083));
#63574=CARTESIAN_POINT('Ctrl Pts',(-2.0475571847817,57.748496067773,12.6111090901458));
#63575=CARTESIAN_POINT('Ctrl Pts',(-2.00743360751768,57.7612436457027,12.5171219278902));
#63576=CARTESIAN_POINT('Ctrl Pts',(-1.95960297560244,57.7764398158685,12.4050814352636));
#63577=CARTESIAN_POINT('Ctrl Pts',(-1.90250269344863,57.7916004469951,12.297099083334));
#63578=CARTESIAN_POINT('Ctrl Pts',(-1.83697618143483,57.8067259564533,12.1948146325061));
#63579=CARTESIAN_POINT('Ctrl Pts',(-1.76997508043438,57.8221918458428,12.0902284030536));
#63580=CARTESIAN_POINT('Ctrl Pts',(-1.69416479782066,57.8376210170525,11.9916007489786));
#63581=CARTESIAN_POINT('Ctrl Pts',(-1.61049800291813,57.8530142661307,11.9006699114393));
#63582=CARTESIAN_POINT('Ctrl Pts',(-1.59288421178826,57.8562549002961,11.8815268716999));
#63583=CARTESIAN_POINT('Ctrl Pts',(-1.57492237912845,57.8594939435387,11.8627248618025));
#63584=CARTESIAN_POINT('Ctrl Pts',(-1.55662163580077,57.8627314050621,11.844279930786));
#63585=CARTESIAN_POINT('Ctrl Pts',(-1.46954820889466,57.8781349798938,11.756520470752));
#63586=CARTESIAN_POINT('Ctrl Pts',(-1.37480023118978,57.8935027266487,11.6768479525723));
#63587=CARTESIAN_POINT('Ctrl Pts',(-1.27418433883334,57.90883586577,11.606036012281));
#63588=CARTESIAN_POINT('Ctrl Pts',(-1.17428500528259,57.9240598064775,11.5357283752183));
#63589=CARTESIAN_POINT('Ctrl Pts',(-1.06860244194075,57.9392496346171,11.4741560655824));
#63590=CARTESIAN_POINT('Ctrl Pts',(-0.958921897657103,57.9544067765099,
11.4220290587066));
#63591=CARTESIAN_POINT('Ctrl Pts',(-0.942941105331535,57.9566152186581,
11.4144339936303));
#63592=CARTESIAN_POINT('Ctrl Pts',(-0.926875446568214,57.9588229672423,
11.4070393564504));
#63593=CARTESIAN_POINT('Ctrl Pts',(-0.91073044638101,57.9610300270125,11.3998472488055));
#63594=CARTESIAN_POINT('Ctrl Pts',(-0.802078772554052,57.9758829682009,
11.3514462252752));
#63595=CARTESIAN_POINT('Ctrl Pts',(-0.68951124289933,57.9906778732759,11.3120840084787));
#63596=CARTESIAN_POINT('Ctrl Pts',(-0.57468075747263,58.0054375483017,11.2825376714842));
#63597=CARTESIAN_POINT('Ctrl Pts',(-0.490862048121693,58.0162111412767,
11.2609707868392));
#63598=CARTESIAN_POINT('Ctrl Pts',(-0.405838698862453,58.0269659749054,
11.2446331488682));
#63599=CARTESIAN_POINT('Ctrl Pts',(-0.320263597472245,58.0377110484851,
11.2338127230293));
#63600=CARTESIAN_POINT('Ctrl Pts',(-0.262819530238262,58.0449239026813,
11.2265492870615));
#63601=CARTESIAN_POINT('Ctrl Pts',(-0.205127001097988,58.0521323611149,
11.2217716976632));
#63602=CARTESIAN_POINT('Ctrl Pts',(-0.147388309001223,58.0593391764746,
11.2194302960943));
#63603=CARTESIAN_POINT('Ctrl Pts',(-0.0354529472583231,58.0733106998155,
11.2148911279545));
#63604=CARTESIAN_POINT('Ctrl Pts',(0.0764822901895972,58.0872450371051,
11.2195100301769));
#63605=CARTESIAN_POINT('Ctrl Pts',(0.187089969165227,58.1011471073447,11.2328499431645));
#63606=CARTESIAN_POINT('Ctrl Pts',(0.301642484454331,58.1155449966091,11.2466656257701));
#63607=CARTESIAN_POINT('Ctrl Pts',(0.414772366645668,58.1299082752455,11.2698355625883));
#63608=CARTESIAN_POINT('Ctrl Pts',(0.525011184291908,58.1442421967197,11.3019287802839));
#63609=CARTESIAN_POINT('Ctrl Pts',(0.557083914043899,58.1484124880884,11.3112659368318));
#63610=CARTESIAN_POINT('Ctrl Pts',(0.588911895013926,58.1525802932436,11.3213587438726));
#63611=CARTESIAN_POINT('Ctrl Pts',(0.620458802335199,58.1567457385606,11.3321973951995));
#63612=CARTESIAN_POINT('Ctrl Pts',(0.720698748189065,58.169981394556,11.3666370887985));
#63613=CARTESIAN_POINT('Ctrl Pts',(0.818219758215847,58.1831868276257,11.4086523751259));
#63614=CARTESIAN_POINT('Ctrl Pts',(0.911694682471907,58.196363142706,11.4579120813134));
#63615=CARTESIAN_POINT('Ctrl Pts',(0.942996064161856,58.2007754155254,11.4744073807489));
#63616=CARTESIAN_POINT('Ctrl Pts',(0.973843827233434,58.2051844247905,11.491714600034));
#63617=CARTESIAN_POINT('Ctrl Pts',(1.00418852593819,58.2095902163625,11.5098200550111));
#63618=CARTESIAN_POINT('Ctrl Pts',(1.0952104818817,58.2228058284293,11.5641291763935));
#63619=CARTESIAN_POINT('Ctrl Pts',(1.18170356584887,58.2359924796513,11.6256236394623));
#63620=CARTESIAN_POINT('Ctrl Pts',(1.26282540655847,58.2491515207159,11.6932280698124));
#63621=CARTESIAN_POINT('Ctrl Pts',(1.33673971272878,58.2611414038553,11.7548259640374));
#63622=CARTESIAN_POINT('Ctrl Pts',(1.40619469115228,58.273108368793,11.8214951503265));
#63623=CARTESIAN_POINT('Ctrl Pts',(1.47058191229359,58.2850535092159,11.8923978684573));
#63624=CARTESIAN_POINT('Ctrl Pts',(1.55934551451336,58.3015209646234,11.990143672002));
#63625=CARTESIAN_POINT('Ctrl Pts',(1.63872811823348,58.3179912427726,12.0962091899425));
#63626=CARTESIAN_POINT('Ctrl Pts',(1.70711030016581,58.3344279546954,12.208568079396));
#63627=CARTESIAN_POINT('Ctrl Pts',(1.76850836920012,58.3491859273839,12.3094513600452));
#63628=CARTESIAN_POINT('Ctrl Pts',(1.82103804330843,58.363916839067,12.4154066166125));
#63629=CARTESIAN_POINT('Ctrl Pts',(1.86355177000897,58.3785946681204,12.5249412106564));
#63630=CARTESIAN_POINT('Ctrl Pts',(1.8958257431273,58.3897372307012,12.6080935668025));
#63631=CARTESIAN_POINT('Ctrl Pts',(1.9223280224056,58.400849207458,12.6933080865615));
#63632=CARTESIAN_POINT('Ctrl Pts',(1.94306795259562,58.4119193850068,12.7797880655436));
#63633=CARTESIAN_POINT('Ctrl Pts',(1.97369195728146,58.4282653016044,12.9074819997715));
#63634=CARTESIAN_POINT('Ctrl Pts',(1.99172875240901,58.4446042581234,13.0378664290804));
#63635=CARTESIAN_POINT('Ctrl Pts',(1.99726345184883,58.4609280668734,13.1685019735049));
#63636=CARTESIAN_POINT('Ctrl Pts',(2.00285136787762,58.4774088303831,13.3003935894014));
#63637=CARTESIAN_POINT('Ctrl Pts',(1.99569569652062,58.493874145555,13.4325428006213));
#63638=CARTESIAN_POINT('Ctrl Pts',(1.97583337247747,58.5103156295835,13.5624486156509));
#63639=CARTESIAN_POINT('Ctrl Pts',(1.96494735116715,58.5193267777814,13.6336466017313));
#63640=CARTESIAN_POINT('Ctrl Pts',(1.95024355218929,58.5283307689126,13.7041707270376));
#63641=CARTESIAN_POINT('Ctrl Pts',(1.93172152819956,58.5373262414551,13.7736076911243));
#63642=CARTESIAN_POINT('Ctrl Pts',(1.92646290178778,58.5398801648019,13.7933216842334));
#63643=CARTESIAN_POINT('Ctrl Pts',(1.92089668302801,58.5424317495683,13.8129486176893));
#63644=CARTESIAN_POINT('Ctrl Pts',(1.91502289079323,58.5449811871001,13.8324784185738));
#63645=CARTESIAN_POINT('Ctrl Pts',(1.88328902704021,58.5587548277138,13.9379904992913));
#63646=CARTESIAN_POINT('Ctrl Pts',(1.84257471791898,58.5724658315662,14.040667129551));
#63647=CARTESIAN_POINT('Ctrl Pts',(1.79383537303964,58.5861443504739,14.1390694208639));
#63648=CARTESIAN_POINT('Ctrl Pts',(1.74509660439038,58.5998227076647,14.2374705487971));
#63649=CARTESIAN_POINT('Ctrl Pts',(1.68833337657972,58.6134685911499,14.3315967117396));
#63650=CARTESIAN_POINT('Ctrl Pts',(1.6243790725386,58.6271113319548,14.4204004062708));
#63651=CARTESIAN_POINT('Ctrl Pts',(1.57100352011599,58.6384974120308,14.4945149842313));
#63652=CARTESIAN_POINT('Ctrl Pts',(1.51261982577684,58.6498812961438,14.5649221359379));
#63653=CARTESIAN_POINT('Ctrl Pts',(1.44983275270448,58.6612796689561,14.6308315551199));
#63654=CARTESIAN_POINT('Ctrl Pts',(1.38345085869734,58.6733306459941,14.7005145625308));
#63655=CARTESIAN_POINT('Ctrl Pts',(1.31201748268334,58.685294084935,14.7653544008138));
#63656=CARTESIAN_POINT('Ctrl Pts',(1.23624186293984,58.6971928215782,14.8243406496));
#63657=CARTESIAN_POINT('Ctrl Pts',(1.21186318343082,58.7010209062335,14.8433178200865));
#63658=CARTESIAN_POINT('Ctrl Pts',(1.18703539965888,58.7048422908144,14.8616893301434));
#63659=CARTESIAN_POINT('Ctrl Pts',(1.16178303325293,58.7086577263161,14.8794222478575));
#63660=CARTESIAN_POINT('Ctrl Pts',(1.07934652366972,58.7211132396032,14.9373114697061));
#63661=CARTESIAN_POINT('Ctrl Pts',(0.992382662271615,58.7335054044598,14.9883910564383));
#63662=CARTESIAN_POINT('Ctrl Pts',(0.902162503100363,58.7458600482291,15.0324453600377));
#63663=CARTESIAN_POINT('Ctrl Pts',(0.811942343929102,58.7582146919983,15.0764996636372));
#63664=CARTESIAN_POINT('Ctrl Pts',(0.718467402301991,58.7705318247608,15.1135283473514));
#63665=CARTESIAN_POINT('Ctrl Pts',(0.623030282885385,58.7828365159479,15.143373103638));
#63666=CARTESIAN_POINT('Ctrl Pts',(0.517947159259993,58.7963848647779,15.1762343240269));
#63667=CARTESIAN_POINT('Ctrl Pts',(0.410297161681419,58.8100682620767,15.2004102053103));
#63668=CARTESIAN_POINT('Ctrl Pts',(0.301564826465718,58.8238266280958,15.2157189812137));
#63669=CARTESIAN_POINT('Ctrl Pts',(0.195041967533067,58.8373054196594,15.2307166778303));
#63670=CARTESIAN_POINT('Ctrl Pts',(0.0874789688953521,58.8508561503634,
15.2372043414448));
#63671=CARTESIAN_POINT('Ctrl Pts',(-0.0197408061838438,58.8644239434151,
15.2349638258398));
#63672=CARTESIAN_POINT('Ctrl Pts',(-0.12696058126305,58.8779917364668,15.2327233102347));
#63673=CARTESIAN_POINT('Ctrl Pts',(-0.233838514980572,58.8915765723245,
15.2217552850595));
#63674=CARTESIAN_POINT('Ctrl Pts',(-0.33898369743854,58.9051254605321,15.2017859192415));
#63675=CARTESIAN_POINT('Ctrl Pts',(-0.388101430627564,58.911454715572,15.1924573893053));
#63676=CARTESIAN_POINT('Ctrl Pts',(-0.436804588784485,58.9177326978257,
15.181186213811));
#63677=CARTESIAN_POINT('Ctrl Pts',(-0.48493597423247,58.9239726430724,15.1679472005774));
#63678=CARTESIAN_POINT('Ctrl Pts',(-0.590618795069899,58.9376737865031,
15.1388780962786));
#63679=CARTESIAN_POINT('Ctrl Pts',(-0.693545745303446,58.9511918737145,
15.1003183673063));
#63680=CARTESIAN_POINT('Ctrl Pts',(-0.792416488328475,58.964663578416,15.0533507465721));
#63681=CARTESIAN_POINT('Ctrl Pts',(-0.88980790192202,58.9779337160143,15.0070858674332));
#63682=CARTESIAN_POINT('Ctrl Pts',(-0.983262368726927,58.9911588756171,
14.9526627861704));
#63683=CARTESIAN_POINT('Ctrl Pts',(-1.07153430160592,59.0044647352171,14.8911656444755));
#63684=CARTESIAN_POINT('Ctrl Pts',(-1.11674862865751,59.0112802140226,14.859665803171));
#63685=CARTESIAN_POINT('Ctrl Pts',(-1.16060329803473,59.0181167827722,14.8263107762819));
#63686=CARTESIAN_POINT('Ctrl Pts',(-1.20293243047534,59.024990783203,14.7912513816117));
#63687=CARTESIAN_POINT('Ctrl Pts',(-1.29308763872583,59.0396314551145,14.7165797111713));
#63688=CARTESIAN_POINT('Ctrl Pts',(-1.3766548618386,59.0545307734405,14.6338784592106));
#63689=CARTESIAN_POINT('Ctrl Pts',(-1.4521181887582,59.0694624048309,14.5445224940884));
#63690=CARTESIAN_POINT('Ctrl Pts',(-1.52508091871205,59.0838992529447,14.458127480522));
#63691=CARTESIAN_POINT('Ctrl Pts',(-1.59046897631651,59.0983662889856,14.3655135371929));
#63692=CARTESIAN_POINT('Ctrl Pts',(-1.64695323383549,59.1126678517981,14.2679037639584));
#63693=CARTESIAN_POINT('Ctrl Pts',(-1.67968449607391,59.1209552618376,14.2113412591986));
#63694=CARTESIAN_POINT('Ctrl Pts',(-1.70942665510631,59.1291872755138,14.1531006644654));
#63695=CARTESIAN_POINT('Ctrl Pts',(-1.73592496734939,59.1373273010696,14.0934128830763));
#63696=CARTESIAN_POINT('Ctrl Pts',(-1.74601632931443,59.1404272699859,14.0706819634101));
#63697=CARTESIAN_POINT('Ctrl Pts',(-1.75563724386547,59.1435139094074,14.0477410856583));
#63698=CARTESIAN_POINT('Ctrl Pts',(-1.76478956866252,59.1465852431225,14.0246091300138));
#63699=CARTESIAN_POINT('Ctrl Pts',(-1.80536798654199,59.1602025333413,13.922049596417));
#63700=CARTESIAN_POINT('Ctrl Pts',(-1.83657035143438,59.1736094947579,13.8159541542144));
#63701=CARTESIAN_POINT('Ctrl Pts',(-1.8584594990833,59.1869805087201,13.708080846563));
#63702=CARTESIAN_POINT('Ctrl Pts',(-1.86827580838667,59.192976813869,13.6597044652407));
#63703=CARTESIAN_POINT('Ctrl Pts',(-1.8762193674693,59.1989657744317,13.6109711615938));
#63704=CARTESIAN_POINT('Ctrl Pts',(-1.88229770380362,59.2049625373459,13.5620423520191));
#63705=CARTESIAN_POINT('Ctrl Pts',(-1.89325814455268,59.2157758851095,13.4738140459876));
#63706=CARTESIAN_POINT('Ctrl Pts',(-1.89815786692028,59.2266198901948,13.3849386548247));
#63707=CARTESIAN_POINT('Ctrl Pts',(-1.89705304640125,59.2375636303809,13.2962222606873));
#63708=CARTESIAN_POINT('Ctrl Pts',(-1.89617891964835,59.2462222458833,13.2260304311549));
#63709=CARTESIAN_POINT('Ctrl Pts',(-1.89154479315468,59.2549432457717,13.1559378089459));
#63710=CARTESIAN_POINT('Ctrl Pts',(-1.88315639628323,59.2637596239283,13.0863502148045));
#63711=CARTESIAN_POINT('Ctrl Pts',(-1.87190005597408,59.2755902698008,12.9929710324704));
#63712=CARTESIAN_POINT('Ctrl Pts',(-1.85392161476602,59.2875105766096,12.9003063603965));
#63713=CARTESIAN_POINT('Ctrl Pts',(-1.82927755571808,59.2994348418841,12.8095092266655));
#63714=CARTESIAN_POINT('Ctrl Pts',(-1.80470413682341,59.3113249272402,12.718972355395));
#63715=CARTESIAN_POINT('Ctrl Pts',(-1.77350406515564,59.3232189330005,12.6302935786374));
#63716=CARTESIAN_POINT('Ctrl Pts',(-1.73577654944931,59.33503556681,12.544589431288));
#63717=CARTESIAN_POINT('Ctrl Pts',(-1.72310881099013,59.3390032287078,12.5158126167228));
#63718=CARTESIAN_POINT('Ctrl Pts',(-1.70970546851552,59.342962199326,12.4873708617542));
#63719=CARTESIAN_POINT('Ctrl Pts',(-1.69557111796058,59.3469094990656,12.459305403527));
#63720=CARTESIAN_POINT('Ctrl Pts',(-1.65390985097694,59.3585442400944,12.3765819318206));
#63721=CARTESIAN_POINT('Ctrl Pts',(-1.60589658641429,59.3700772980045,12.2971313838428));
#63722=CARTESIAN_POINT('Ctrl Pts',(-1.55240337212546,59.3814349689118,12.2215710200243));
#63723=CARTESIAN_POINT('Ctrl Pts',(-1.54939948336779,59.3820727541039,12.2173279598452));
#63724=CARTESIAN_POINT('Ctrl Pts',(-1.54637831753911,59.3827099872707,12.2130971534733));
#63725=CARTESIAN_POINT('Ctrl Pts',(-1.5433400298968,59.38334665573,12.2088787054353));
#63726=CARTESIAN_POINT('Ctrl Pts',(-1.48531316216982,59.3955060957916,12.1283124934336));
#63727=CARTESIAN_POINT('Ctrl Pts',(-1.42093213095254,59.4077161778422,12.0524321900086));
#63728=CARTESIAN_POINT('Ctrl Pts',(-1.35115712210107,59.4199965915774,11.9819264213592));
#63729=CARTESIAN_POINT('Ctrl Pts',(-1.28018237202813,59.432488159977,11.9102083464931));
#63730=CARTESIAN_POINT('Ctrl Pts',(-1.20362531570199,59.4450525045962,11.8440503158963));
#63731=CARTESIAN_POINT('Ctrl Pts',(-1.12245738108134,59.4577094768668,11.7842139500287));
#63732=CARTESIAN_POINT('Ctrl Pts',(-1.04285713935044,59.4701219899734,11.7255332750846));
#63733=CARTESIAN_POINT('Ctrl Pts',(-0.958821080636736,59.4826235875242,
11.6729318434965));
#63734=CARTESIAN_POINT('Ctrl Pts',(-0.871247569242309,59.4952321297453,
11.627173841781));
#63735=CARTESIAN_POINT('Ctrl Pts',(-0.856026546876538,59.4974236018022,
11.619220711246));
#63736=CARTESIAN_POINT('Ctrl Pts',(-0.840698643668718,59.4996183024387,
11.61147444279));
#63737=CARTESIAN_POINT('Ctrl Pts',(-0.825268565222567,59.5018163226858,
11.6039392134727));
#63738=CARTESIAN_POINT('Ctrl Pts',(-0.749854981388678,59.5125590149383,
11.5671112316964));
#63739=CARTESIAN_POINT('Ctrl Pts',(-0.671975232143976,59.5232278785692,
11.5351623712557));
#63740=CARTESIAN_POINT('Ctrl Pts',(-0.592288075088419,59.5338228938777,
11.5086453437354));
#63741=CARTESIAN_POINT('Ctrl Pts',(-0.534497448341847,59.5415065984757,
11.4894146960817));
#63742=CARTESIAN_POINT('Ctrl Pts',(-0.475757099452308,59.5491514566829,
11.4730402248142));
#63743=CARTESIAN_POINT('Ctrl Pts',(-0.416327025131937,59.5567573322003,
11.4597179131493));
#63744=CARTESIAN_POINT('Ctrl Pts',(-0.332861466849647,59.5674392748622,
11.4410076188507));
#63745=CARTESIAN_POINT('Ctrl Pts',(-0.248035654363545,59.5780443502871,
11.4283199523734));
#63746=CARTESIAN_POINT('Ctrl Pts',(-0.162744825157152,59.5885717398189,
11.4214702052937));
#63747=CARTESIAN_POINT('Ctrl Pts',(-0.0774539959507597,59.5990991293507,
11.414620458214));
#63748=CARTESIAN_POINT('Ctrl Pts',(0.00830053247729802,59.609548837757,
11.4136083750919));
#63749=CARTESIAN_POINT('Ctrl Pts',(0.0936270681948237,59.6199194861507,
11.4181939671387));
#63750=CARTESIAN_POINT('Ctrl Pts',(0.186566867222982,59.6312154560315,11.4231887088057));
#63751=CARTESIAN_POINT('Ctrl Pts',(0.279136406833507,59.6426668287692,11.4350438175505));
#63752=CARTESIAN_POINT('Ctrl Pts',(0.370372628682501,59.654224037212,11.4534565807964));
#63753=CARTESIAN_POINT('Ctrl Pts',(0.462195851790772,59.6658556031389,11.4719878092199));
#63754=CARTESIAN_POINT('Ctrl Pts',(0.552669731572818,59.6775943565418,11.4971608886472));
#63755=CARTESIAN_POINT('Ctrl Pts',(0.640837575008383,59.6893935521328,11.5287134846517));
#63756=CARTESIAN_POINT('Ctrl Pts',(0.726403413497647,59.700844530459,11.5593349020351));
#63757=CARTESIAN_POINT('Ctrl Pts',(0.809798661279672,59.7123524427399,11.5959646870322));
#63758=CARTESIAN_POINT('Ctrl Pts',(0.890153554389046,59.7238781358003,11.6384105630698));
#63759=CARTESIAN_POINT('Ctrl Pts',(0.92372720212957,59.7286937673543,11.6561451755493));
#63760=CARTESIAN_POINT('Ctrl Pts',(0.956770035111332,59.7335125461735,11.6748957055525));
#63761=CARTESIAN_POINT('Ctrl Pts',(0.989217984613843,59.7383318061232,11.6946508071429));
#63762=CARTESIAN_POINT('Ctrl Pts',(1.0505133797862,59.7474355691525,11.7319689359375));
#63763=CARTESIAN_POINT('Ctrl Pts',(1.10970588496588,59.7564248801717,11.7727467116865));
#63764=CARTESIAN_POINT('Ctrl Pts',(1.16628383133372,59.7653417868353,11.8169196632499));
#63765=CARTESIAN_POINT('Ctrl Pts',(1.23412840109227,59.7760343576161,11.8698889752554));
#63766=CARTESIAN_POINT('Ctrl Pts',(1.29821302930044,59.7866229642167,11.9277420092064));
#63767=CARTESIAN_POINT('Ctrl Pts',(1.35807742641337,59.7971752733908,11.989773943096));
#63768=CARTESIAN_POINT('Ctrl Pts',(1.41801592431191,59.8077406443252,12.0518826607712));
#63769=CARTESIAN_POINT('Ctrl Pts',(1.47372275725937,59.8182696433691,12.1181806836443));
#63770=CARTESIAN_POINT('Ctrl Pts',(1.52473198283119,59.828824653008,12.1879088572466));
#63771=CARTESIAN_POINT('Ctrl Pts',(1.5671879292086,59.8376097878188,12.2459449392742));
#63772=CARTESIAN_POINT('Ctrl Pts',(1.60638916190907,59.8464128458041,12.3063562701437));
#63773=CARTESIAN_POINT('Ctrl Pts',(1.64207304820684,59.8552667761938,12.3686783630951));
#63774=CARTESIAN_POINT('Ctrl Pts',(1.68474217136199,59.8658538922679,12.4432002085365));
#63775=CARTESIAN_POINT('Ctrl Pts',(1.72240275794083,59.8766262430058,12.5206967959212));
#63776=CARTESIAN_POINT('Ctrl Pts',(1.75474908250705,59.8874898709194,12.6003740149981));
#63777=CARTESIAN_POINT('Ctrl Pts',(1.78696605902631,59.8983100568324,12.6797326169582));
#63778=CARTESIAN_POINT('Ctrl Pts',(1.81391228100278,59.9092207784099,12.761253861667));
#63779=CARTESIAN_POINT('Ctrl Pts',(1.83531021566769,59.9201363585182,12.8441978620612));
#63780=CARTESIAN_POINT('Ctrl Pts',(1.85629914264622,59.9308432943701,12.9255564415149));
#63781=CARTESIAN_POINT('Ctrl Pts',(1.87195111963573,59.9415549103696,13.0082837455269));
#63782=CARTESIAN_POINT('Ctrl Pts',(1.88201041978646,59.9521972755145,13.0917298756377));
#63783=CARTESIAN_POINT('Ctrl Pts',(1.88913208181775,59.9597317288702,13.1508070606866));
#63784=CARTESIAN_POINT('Ctrl Pts',(1.89345078665872,59.9672316148274,13.210245563423));
#63785=CARTESIAN_POINT('Ctrl Pts',(1.89487217930387,59.9746728473432,13.2698301275761));
#63786=CARTESIAN_POINT('Ctrl Pts',(1.89490682209874,59.9748542082729,13.2712823482843));
#63787=CARTESIAN_POINT('Ctrl Pts',(1.89493974355676,59.9750355344513,13.2727346563888));
#63788=CARTESIAN_POINT('Ctrl Pts',(1.89497094555377,59.9752168255432,13.2741870487142));
#63789=CARTESIAN_POINT('Ctrl Pts',(1.89677829811965,59.9857179777607,13.3583157983999));
#63790=CARTESIAN_POINT('Ctrl Pts',(1.89280614713868,59.9960846861283,13.4425444573657));
#63791=CARTESIAN_POINT('Ctrl Pts',(1.88326890729464,60.0064013269797,13.5262189405871));
#63792=CARTESIAN_POINT('Ctrl Pts',(1.87373988880451,60.0167090746129,13.609821294183));
#63793=CARTESIAN_POINT('Ctrl Pts',(1.85865402480473,60.0269668514144,13.6928706812733));
#63794=CARTESIAN_POINT('Ctrl Pts',(1.83821308355048,60.0372517759125,13.7746646005829));
#63795=CARTESIAN_POINT('Ctrl Pts',(1.81795152205156,60.0474464449171,13.8557407362518));
#63796=CARTESIAN_POINT('Ctrl Pts',(1.79242724450045,60.0576677876008,13.9355831774851));
#63797=CARTESIAN_POINT('Ctrl Pts',(1.76184393626309,60.0679839244412,14.0134579846426));
#63798=CARTESIAN_POINT('Ctrl Pts',(1.73773376718324,60.0761165895389,14.0748501255142));
#63799=CARTESIAN_POINT('Ctrl Pts',(1.71047943775938,60.0843080332466,14.1350183263249));
#63800=CARTESIAN_POINT('Ctrl Pts',(1.68019112349398,60.0925885199882,14.1935827800625));
#63801=CARTESIAN_POINT('Ctrl Pts',(1.64617234989821,60.1018888726343,14.2593603230119));
#63802=CARTESIAN_POINT('Ctrl Pts',(1.60827967828574,60.1113122103187,14.3232153087731));
#63803=CARTESIAN_POINT('Ctrl Pts',(1.56681116476779,60.1207766078547,14.3847055551712));
#63804=CARTESIAN_POINT('Ctrl Pts',(1.52570925077873,60.1301573360381,14.4456522012942));
#63805=CARTESIAN_POINT('Ctrl Pts',(1.48109535301017,60.1395783988457,14.5042762946321));
#63806=CARTESIAN_POINT('Ctrl Pts',(1.43323386744353,60.1489670428787,14.5601903354092));
#63807=CARTESIAN_POINT('Ctrl Pts',(1.3909742468693,60.157256809271,14.6095600137641));
#63808=CARTESIAN_POINT('Ctrl Pts',(1.34618279641613,60.1655213958391,14.6568178708656));
#63809=CARTESIAN_POINT('Ctrl Pts',(1.29901616765672,60.1737153708029,14.7017191651865));
#63810=CARTESIAN_POINT('Ctrl Pts',(1.27653538709293,60.1776208217108,14.7231202313896));
#63811=CARTESIAN_POINT('Ctrl Pts',(1.25354142483049,60.1814968462128,14.743987430385));
#63812=CARTESIAN_POINT('Ctrl Pts',(1.23003893721349,60.1853508455441,14.7642795404087));
#63813=CARTESIAN_POINT('Ctrl Pts',(1.17850318108619,60.1938018134966,14.8087756486729));
#63814=CARTESIAN_POINT('Ctrl Pts',(1.1245194032915,60.202147329404,14.8505083976961));
#63815=CARTESIAN_POINT('Ctrl Pts',(1.06840191913485,60.2104604779086,14.8892670571694));
#63816=CARTESIAN_POINT('Ctrl Pts',(1.01245611748207,60.2187481936596,14.9279071406979));
#63817=CARTESIAN_POINT('Ctrl Pts',(0.954389243181839,60.2270037432293,14.9635904930496));
#63818=CARTESIAN_POINT('Ctrl Pts',(0.894559103236365,60.2352927338508,14.9960864424661));
#63819=CARTESIAN_POINT('Ctrl Pts',(0.853701766196935,60.2409531933424,15.0182775648491));
#63820=CARTESIAN_POINT('Ctrl Pts',(0.812023143287833,60.2466291062208,15.0389818208246));
#63821=CARTESIAN_POINT('Ctrl Pts',(0.769650774154881,60.2523395235873,15.0581229548416));
#63822=CARTESIAN_POINT('Ctrl Pts',(0.689645595206691,60.2631216198597,15.0942641922478));
#63823=CARTESIAN_POINT('Ctrl Pts',(0.606941476645531,60.2740524261799,15.1249449266891));
#63824=CARTESIAN_POINT('Ctrl Pts',(0.522444982365712,60.285071073973,15.149965228729));
#63825=CARTESIAN_POINT('Ctrl Pts',(0.437621342071081,60.2961323827871,15.1750824021499));
#63826=CARTESIAN_POINT('Ctrl Pts',(0.350992113414438,60.307282198988,15.1944962313341));
#63827=CARTESIAN_POINT('Ctrl Pts',(0.263432036152865,60.3184657956524,15.2080342251105));
#63828=CARTESIAN_POINT('Ctrl Pts',(0.176159419448295,60.3296126764638,15.2215277735259));
#63829=CARTESIAN_POINT('Ctrl Pts',(0.0879623625203319,60.3407931092736,
15.2291851981355));
#63830=CARTESIAN_POINT('Ctrl Pts',(-0.000342428140762663,60.35195985489,
15.2308486929397));
#63831=CARTESIAN_POINT('Ctrl Pts',(-0.0873515597100696,60.3629627555396,
15.2324877799835));
#63832=CARTESIAN_POINT('Ctrl Pts',(-0.174465405949206,60.3739523744458,
15.2283088106122));
#63833=CARTESIAN_POINT('Ctrl Pts',(-0.260951948886756,60.3848902619989,
15.2181551593732));
#63834=CARTESIAN_POINT('Ctrl Pts',(-0.295577040787573,60.3892692711356,
15.2140901210986));
#63835=CARTESIAN_POINT('Ctrl Pts',(-0.330102133728782,60.3936400645258,
15.2090672793448));
#63836=CARTESIAN_POINT('Ctrl Pts',(-0.364482390228697,60.3980004808765,
15.2030755991657));
#63837=CARTESIAN_POINT('Ctrl Pts',(-0.407226977467079,60.4034217376114,
15.195626210412));
#63838=CARTESIAN_POINT('Ctrl Pts',(-0.449747605612096,60.4088269411944,
15.1866792819153));
#63839=CARTESIAN_POINT('Ctrl Pts',(-0.491974712434599,60.414212316012,15.176297632117));
#63840=CARTESIAN_POINT('Ctrl Pts',(-0.588087657829569,60.4264699456419,
15.1526680014071));
#63841=CARTESIAN_POINT('Ctrl Pts',(-0.682389832285348,60.4387055858607,
15.1214097839479));
#63842=CARTESIAN_POINT('Ctrl Pts',(-0.773961605253539,60.4509579910253,
15.0831399777681));
#63843=CARTESIAN_POINT('Ctrl Pts',(-0.868104331035284,60.4635543925384,
15.0437957153156));
#63844=CARTESIAN_POINT('Ctrl Pts',(-0.959361818712132,60.4761685462156,
14.9970390198292));
#63845=CARTESIAN_POINT('Ctrl Pts',(-1.04668730101127,60.4888365227693,14.9435163114177));
#63846=CARTESIAN_POINT('Ctrl Pts',(-1.13321362150058,60.5013885679499,14.8904834177017));
#63847=CARTESIAN_POINT('Ctrl Pts',(-1.2158795732269,60.5139934528858,14.8308062486209));
#63848=CARTESIAN_POINT('Ctrl Pts',(-1.29361658023214,60.5266802484715,14.7651142565974));
#63849=CARTESIAN_POINT('Ctrl Pts',(-1.36959167559692,60.5390794974474,14.7009111755816));
#63850=CARTESIAN_POINT('Ctrl Pts',(-1.44085830285566,60.5515569720563,14.6309616720683));
#63851=CARTESIAN_POINT('Ctrl Pts',(-1.50637402923232,60.5641341783868,14.5558736210541));
#63852=CARTESIAN_POINT('Ctrl Pts',(-1.52762443586511,60.5682136683599,14.53151837529));
#63853=CARTESIAN_POINT('Ctrl Pts',(-1.54826947951281,60.5723036066061,14.5066227524367));
#63854=CARTESIAN_POINT('Ctrl Pts',(-1.56827268040012,60.5764045990175,14.4812082615031));
#63855=CARTESIAN_POINT('Ctrl Pts',(-1.62937100982656,60.5889307835386,14.4035815382592));
#63856=CARTESIAN_POINT('Ctrl Pts',(-1.68486113862731,60.6014260076282,14.3213353076629));
#63857=CARTESIAN_POINT('Ctrl Pts',(-1.73373650575351,60.6139032535682,14.2350744823463));
#63858=CARTESIAN_POINT('Ctrl Pts',(-1.78382192982385,60.6266894113177,14.146678010449));
#63859=CARTESIAN_POINT('Ctrl Pts',(-1.8269594190976,60.6394567134822,14.0540656621294));
#63860=CARTESIAN_POINT('Ctrl Pts',(-1.86279055072064,60.652215379453,13.9584928980425));
#63861=CARTESIAN_POINT('Ctrl Pts',(-1.89878988776966,60.6650339396205,13.8624714778077));
#63862=CARTESIAN_POINT('Ctrl Pts',(-1.92741307745339,60.6778437918713,13.7634626856993));
#63863=CARTESIAN_POINT('Ctrl Pts',(-1.9483285077907,60.6906513214101,13.6627802207895));
#63864=CARTESIAN_POINT('Ctrl Pts',(-1.95371074865907,60.6939471277977,13.6368712498228));
#63865=CARTESIAN_POINT('Ctrl Pts',(-1.95858278705612,60.6972427595641,13.6108516132584));
#63866=CARTESIAN_POINT('Ctrl Pts',(-1.96293944415645,60.7005382821062,13.5847440033346));
#63867=CARTESIAN_POINT('Ctrl Pts',(-1.97300581117807,60.7081528220328,13.5244205081643));
#63868=CARTESIAN_POINT('Ctrl Pts',(-1.98031066061398,60.7157785521554,13.463570155228));
#63869=CARTESIAN_POINT('Ctrl Pts',(-1.98479348719843,60.7234144908285,13.4024573530112));
#63870=CARTESIAN_POINT('Ctrl Pts',(-1.99657422568646,60.7434815166044,13.2418546779747));
#63871=CARTESIAN_POINT('Ctrl Pts',(-1.98886620028509,60.7636184653362,13.07944306302));
#63872=CARTESIAN_POINT('Ctrl Pts',(-1.96190927563821,60.7838131630534,12.9199097467551));
#63873=CARTESIAN_POINT('Ctrl Pts',(-1.94350514443476,60.7976005617004,12.8109925715832));
#63874=CARTESIAN_POINT('Ctrl Pts',(-1.91612902463564,60.8114150450154,12.7034157944574));
#63875=CARTESIAN_POINT('Ctrl Pts',(-1.87984993124581,60.8252549333523,12.5986590852905));
#63876=CARTESIAN_POINT('Ctrl Pts',(-1.87237181125249,60.8281077153821,12.5770658433416));
#63877=CARTESIAN_POINT('Ctrl Pts',(-1.86452114578359,60.8309602703639,12.5555931375228));
#63878=CARTESIAN_POINT('Ctrl Pts',(-1.85629745446083,60.8338128756041,12.5342537835132));
#63879=CARTESIAN_POINT('Ctrl Pts',(-1.81970534913029,60.8465058169271,12.4393022758562));
#63880=CARTESIAN_POINT('Ctrl Pts',(-1.77572703052217,60.8592002794464,12.3469869163756));
#63881=CARTESIAN_POINT('Ctrl Pts',(-1.72496264541799,60.8719164694528,12.2582888657482));
#63882=CARTESIAN_POINT('Ctrl Pts',(-1.6724160717148,60.8850790875761,12.166476886837));
#63883=CARTESIAN_POINT('Ctrl Pts',(-1.61259705340655,60.898265031652,12.0785409582365));
#63884=CARTESIAN_POINT('Ctrl Pts',(-1.54619418402695,60.9114891754909,11.9956227499056));
#63885=CARTESIAN_POINT('Ctrl Pts',(-1.47979131464733,60.9247133193299,11.9127045415747));
#63886=CARTESIAN_POINT('Ctrl Pts',(-1.40680339243252,60.9379756658135,11.8348051182777));
#63887=CARTESIAN_POINT('Ctrl Pts',(-1.32796230537848,60.9512833737372,11.7631079740704));
#63888=CARTESIAN_POINT('Ctrl Pts',(-1.26598629827422,60.961744398967,11.7067477324149));
#63889=CARTESIAN_POINT('Ctrl Pts',(-1.20049286612118,60.9722144435424,11.6540711597815));
#63890=CARTESIAN_POINT('Ctrl Pts',(-1.13182440260108,60.9826983981754,11.6056255448801));
#63891=CARTESIAN_POINT('Ctrl Pts',(-1.09084918772005,60.9889542872963,11.5767175224945));
#63892=CARTESIAN_POINT('Ctrl Pts',(-1.04874369202499,60.9952150927196,11.5493162091802));
#63893=CARTESIAN_POINT('Ctrl Pts',(-1.00566818612401,61.0014816988447,11.5234423362574));
#63894=CARTESIAN_POINT('Ctrl Pts',(-0.962594463826959,61.0077480454919,
11.49756953468));
#63895=CARTESIAN_POINT('Ctrl Pts',(-0.91855080808143,61.0140201924027,11.4732240671337));
#63896=CARTESIAN_POINT('Ctrl Pts',(-0.87361793905202,61.0202985106828,11.450524928987));
#63897=CARTESIAN_POINT('Ctrl Pts',(-0.773152929515877,61.0343361477069,
11.3997721241999));
#63898=CARTESIAN_POINT('Ctrl Pts',(-0.668239101491088,61.0484050465533,
11.3572500207284));
#63899=CARTESIAN_POINT('Ctrl Pts',(-0.560352649403341,61.0625060042088,
11.3235457214749));
#63900=CARTESIAN_POINT('Ctrl Pts',(-0.518148271713797,61.0680221939728,
11.3103608502707));
#63901=CARTESIAN_POINT('Ctrl Pts',(-0.475489546815452,61.0735432233592,
11.2985253351017));
#63902=CARTESIAN_POINT('Ctrl Pts',(-0.432466963195663,61.0790688840395,
11.2880738510178));
#63903=CARTESIAN_POINT('Ctrl Pts',(-0.320866162986129,61.0934024758821,
11.2609626482726));
#63904=CARTESIAN_POINT('Ctrl Pts',(-0.206749271624201,61.107768758523,11.2429306468698));
#63905=CARTESIAN_POINT('Ctrl Pts',(-0.091645956239233,61.1221689807695,
11.2345907989729));
#63906=CARTESIAN_POINT('Ctrl Pts',(-0.0601010265759873,61.126115470029,
11.2323052009046));
#63907=CARTESIAN_POINT('Ctrl Pts',(-0.028482293873111,61.1300644798337,
11.2307474565802));
#63908=CARTESIAN_POINT('Ctrl Pts',(0.00317813948409761,61.1340159710391,
11.2299298964506));
#63909=CARTESIAN_POINT('Ctrl Pts',(0.118796983769572,61.1484461855977,11.2269442974773));
#63910=CARTESIAN_POINT('Ctrl Pts',(0.23497465217744,61.1629098763671,11.2338327438001));
#63911=CARTESIAN_POINT('Ctrl Pts',(0.350030063026787,61.1774019927302,11.2503173834763));
#63912=CARTESIAN_POINT('Ctrl Pts',(0.432372184468717,61.1877736179908,11.2621150050928));
#63913=CARTESIAN_POINT('Ctrl Pts',(0.514138539597379,61.1981596985619,11.2788270263037));
#63914=CARTESIAN_POINT('Ctrl Pts',(0.594704550095013,61.2085568151962,11.3003375309651));
#63915=CARTESIAN_POINT('Ctrl Pts',(0.701692939563703,61.2223637637711,11.3289026074305));
#63916=CARTESIAN_POINT('Ctrl Pts',(0.806767964229992,61.2362149107861,11.3659430373292));
#63917=CARTESIAN_POINT('Ctrl Pts',(0.908473479897716,61.2501016666349,11.4111383449384));
#63918=CARTESIAN_POINT('Ctrl Pts',(1.00021889379422,61.2626284814755,11.451907640247));
#63919=CARTESIAN_POINT('Ctrl Pts',(1.08922237606095,61.2751843254157,11.4993116533713));
#63920=CARTESIAN_POINT('Ctrl Pts',(1.17444482557351,61.287765803511,11.5530942618712));
#63921=CARTESIAN_POINT('Ctrl Pts',(1.26814532044362,61.3015989041841,11.612227237521));
#63922=CARTESIAN_POINT('Ctrl Pts',(1.35727408503484,61.3154629378033,11.6790699682437));
#63923=CARTESIAN_POINT('Ctrl Pts',(1.44090431072691,61.3293571514557,11.7525023543434));
#63924=CARTESIAN_POINT('Ctrl Pts',(1.46205543896261,61.3328711715635,11.771074321622));
#63925=CARTESIAN_POINT('Ctrl Pts',(1.48285511373977,61.3363871419884,11.7900677939993));
#63926=CARTESIAN_POINT('Ctrl Pts',(1.50328887112793,61.339905090742,11.8094646946219));
#63927=CARTESIAN_POINT('Ctrl Pts',(1.5794445722949,61.3530163286269,11.8817560769321));
#63928=CARTESIAN_POINT('Ctrl Pts',(1.65032057243723,61.3661424004616,11.9599808167139));
#63929=CARTESIAN_POINT('Ctrl Pts',(1.71516743938303,61.3792867600178,12.0431980663506));
#63930=CARTESIAN_POINT('Ctrl Pts',(1.75938636176628,61.3882498671403,12.0999437084448));
#63931=CARTESIAN_POINT('Ctrl Pts',(1.80080259418761,61.3972216164688,12.159011698473));
#63932=CARTESIAN_POINT('Ctrl Pts',(1.83918332776035,61.406204877657,12.2201166228578));
#63933=CARTESIAN_POINT('Ctrl Pts',(1.88406660745716,61.4167101022051,12.2915740744675));
#63934=CARTESIAN_POINT('Ctrl Pts',(1.92481866657411,61.4272340928429,12.3658161772094));
#63935=CARTESIAN_POINT('Ctrl Pts',(1.96110251039936,61.4377829526498,12.4423180005748));
#63936=CARTESIAN_POINT('Ctrl Pts',(1.99085484123667,61.4464328952646,12.5050486078773));
#63937=CARTESIAN_POINT('Ctrl Pts',(2.01760384199706,61.4550996769869,12.5692989446145));
#63938=CARTESIAN_POINT('Ctrl Pts',(2.04118161774851,61.463789852119,12.6347984710244));
#63939=CARTESIAN_POINT('Ctrl Pts',(2.0494963355269,61.4668544479668,12.6578969211266));
#63940=CARTESIAN_POINT('Ctrl Pts',(2.05741679693751,61.4699219790975,12.6811508977909));
#63941=CARTESIAN_POINT('Ctrl Pts',(2.06494465670457,61.4729928172606,12.7045450077392));
#63942=CARTESIAN_POINT('Ctrl Pts',(2.09243054740177,61.4842051305491,12.7899621075384));
#63943=CARTESIAN_POINT('Ctrl Pts',(2.11458011981301,61.4954464062451,12.877260276532));
#63944=CARTESIAN_POINT('Ctrl Pts',(2.13125540857689,61.5067073051811,12.9657828175091));
#63945=CARTESIAN_POINT('Ctrl Pts',(2.14789143364656,61.5179416891645,13.0540969229964));
#63946=CARTESIAN_POINT('Ctrl Pts',(2.15907783747761,61.5291955981566,13.1436300129846));
#63947=CARTESIAN_POINT('Ctrl Pts',(2.16465876667325,61.5404530657803,13.2336822050908));
#63948=CARTESIAN_POINT('Ctrl Pts',(2.17398320685921,61.5592616870373,13.3841385627104));
#63949=CARTESIAN_POINT('Ctrl Pts',(2.16767126813817,61.5780856248973,13.5360794717045));
#63950=CARTESIAN_POINT('Ctrl Pts',(2.14549595895314,61.5969303796965,13.6861414620898));
#63951=CARTESIAN_POINT('Ctrl Pts',(2.14109490036659,61.6006704344226,13.7159237576056));
#63952=CARTESIAN_POINT('Ctrl Pts',(2.13606886954778,61.6044113291931,13.7456321435509));
#63953=CARTESIAN_POINT('Ctrl Pts',(2.13041587611228,61.6081531367628,13.7752404432675));
#63954=CARTESIAN_POINT('Ctrl Pts',(2.11280862816456,61.6198076582838,13.8674607298055));
#63955=CARTESIAN_POINT('Ctrl Pts',(2.08941019597058,61.6315190928153,13.9587167983496));
#63956=CARTESIAN_POINT('Ctrl Pts',(2.0600668219164,61.6432768391579,14.0482459937675));
#63957=CARTESIAN_POINT('Ctrl Pts',(2.02936375310375,61.6555794085343,14.1419237365717));
#63958=CARTESIAN_POINT('Ctrl Pts',(1.9921508370218,61.6679327262336,14.233710857238));
#63959=CARTESIAN_POINT('Ctrl Pts',(1.94883949167143,61.6803182038231,14.3228166045752));
#63960=CARTESIAN_POINT('Ctrl Pts',(1.90537869029098,61.6927464204292,14.4122298323462));
#63961=CARTESIAN_POINT('Ctrl Pts',(1.85577632749744,61.7052070191149,14.4989425067665));
#63962=CARTESIAN_POINT('Ctrl Pts',(1.8004760420889,61.7176746273994,14.5821118430939));
#63963=CARTESIAN_POINT('Ctrl Pts',(1.75932809814522,61.7269515496252,14.6439966446596));
#63964=CARTESIAN_POINT('Ctrl Pts',(1.71502599467862,61.7362322161595,14.703918634141));
#63965=CARTESIAN_POINT('Ctrl Pts',(1.66776687229128,61.7455038255094,14.7615187689036));
#63966=CARTESIAN_POINT('Ctrl Pts',(1.59763392570811,61.7592629740172,14.8469978673384));
#63967=CARTESIAN_POINT('Ctrl Pts',(1.52100707003437,61.7730735779605,14.9276302297976));
#63968=CARTESIAN_POINT('Ctrl Pts',(1.43862385219125,61.7869320574814,15.0022941683172));
#63969=CARTESIAN_POINT('Ctrl Pts',(1.36031021816126,61.8001059528671,15.0732698416344));
#63970=CARTESIAN_POINT('Ctrl Pts',(1.27679594274065,61.8133231251821,15.1388517715873));
#63971=CARTESIAN_POINT('Ctrl Pts',(1.18873969579851,61.8265819222932,15.1981121666516));
#63972=CARTESIAN_POINT('Ctrl Pts',(1.09666770856855,61.8404453770813,15.2600750883871));
#63973=CARTESIAN_POINT('Ctrl Pts',(0.99963118253683,61.8543543316727,15.3151261617681));
#63974=CARTESIAN_POINT('Ctrl Pts',(0.898912823232068,61.8683084208655,15.3628784602649));
#63975=CARTESIAN_POINT('Ctrl Pts',(0.858386533620023,61.873923161453,15.3820926680011));
#63976=CARTESIAN_POINT('Ctrl Pts',(0.817264179198787,61.8795452274309,15.4001257646514));
#63977=CARTESIAN_POINT('Ctrl Pts',(0.775629168390384,61.8851746664602,15.4169549299689));
#63978=CARTESIAN_POINT('Ctrl Pts',(0.685817155271583,61.897318082353,15.4532575797562));
#63979=CARTESIAN_POINT('Ctrl Pts',(0.593362597818468,61.9094279499761,15.4837639692001));
#63980=CARTESIAN_POINT('Ctrl Pts',(0.499132047757716,61.9215309125639,15.5082773603599));
#63981=CARTESIAN_POINT('Ctrl Pts',(0.404521099924699,61.933682733404,15.532889709229));
#63982=CARTESIAN_POINT('Ctrl Pts',(0.308120225844149,61.9458275940093,15.551461626621));
#63983=CARTESIAN_POINT('Ctrl Pts',(0.21075956535082,61.9579992118371,15.5638169852688));
#63984=CARTESIAN_POINT('Ctrl Pts',(0.113205540709764,61.9701950032326,15.5761968824044));
#63985=CARTESIAN_POINT('Ctrl Pts',(0.0146880365663079,61.9824176616428,
15.582336657944));
#63986=CARTESIAN_POINT('Ctrl Pts',(-0.0840090766511814,61.9947078352595,
15.5820655802065));
#63987=CARTESIAN_POINT('Ctrl Pts',(-0.13444640871128,62.0009885008998,15.5819270509485));
#63988=CARTESIAN_POINT('Ctrl Pts',(-0.184931484660247,62.0072869061431,
15.5801143038734));
#63989=CARTESIAN_POINT('Ctrl Pts',(-0.235364843567225,62.0136091475188,
15.5766036679292));
#63990=CARTESIAN_POINT('Ctrl Pts',(-0.26994468556806,62.0179440185763,15.5741965858132));
#63991=CARTESIAN_POINT('Ctrl Pts',(-0.304500286908054,62.0222901049293,
15.5709912696112));
#63992=CARTESIAN_POINT('Ctrl Pts',(-0.338999847063386,62.0266494928043,
15.5670034814));
#63993=CARTESIAN_POINT('Ctrl Pts',(-0.451703931082599,62.0408908574803,
15.5539760684249));
#63994=CARTESIAN_POINT('Ctrl Pts',(-0.563680880569419,62.0551893687934,
15.5324319507017));
#63995=CARTESIAN_POINT('Ctrl Pts',(-0.673761042537445,62.0695164405951,
15.5027165105806));
#63996=CARTESIAN_POINT('Ctrl Pts',(-0.784111718606247,62.0838787201479,
15.4729280468973));
#63997=CARTESIAN_POINT('Ctrl Pts',(-0.892556452373441,62.0982696942304,
15.4349266344889));
#63998=CARTESIAN_POINT('Ctrl Pts',(-0.997865993481773,62.1126540724659,
15.3890504899903));
#63999=CARTESIAN_POINT('Ctrl Pts',(-1.10268296977809,62.1269711705815,15.3433889221982));
#64000=CARTESIAN_POINT('Ctrl Pts',(-1.2043937851748,62.1412817210782,15.2899248919537));
#64001=CARTESIAN_POINT('Ctrl Pts',(-1.30173641567575,62.1555446619255,15.2290020161442));
#64002=CARTESIAN_POINT('Ctrl Pts',(-1.33746396564815,62.1607795721519,15.2066415654481));
#64003=CARTESIAN_POINT('Ctrl Pts',(-1.37260261002422,62.1660080087906,15.1832765211277));
#64004=CARTESIAN_POINT('Ctrl Pts',(-1.40708839617374,62.171227733778,15.1589246924533));
#64005=CARTESIAN_POINT('Ctrl Pts',(-1.4815991685812,62.1825055900773,15.1063095786149));
#64006=CARTESIAN_POINT('Ctrl Pts',(-1.55318222100573,62.1938572267572,15.0493158946748));
#64007=CARTESIAN_POINT('Ctrl Pts',(-1.62123624053169,62.2052677199323,14.9881020864936));
#64008=CARTESIAN_POINT('Ctrl Pts',(-1.70919033190374,62.2200148218128,14.9089883924679));
#64009=CARTESIAN_POINT('Ctrl Pts',(-1.79125060481977,62.2348604481774,14.8228239298759));
#64010=CARTESIAN_POINT('Ctrl Pts',(-1.86660942439318,62.2497664850856,14.730702390601));
#64011=CARTESIAN_POINT('Ctrl Pts',(-1.94228821598917,62.2647358127247,14.638189705135));
#64012=CARTESIAN_POINT('Ctrl Pts',(-2.01120743413818,62.2797660598917,14.5396685205953));
#64013=CARTESIAN_POINT('Ctrl Pts',(-2.07251726871229,62.2948120763592,14.4362881380417));
#64014=CARTESIAN_POINT('Ctrl Pts',(-2.13388727297309,62.30987285904,14.332806297618));
#64015=CARTESIAN_POINT('Ctrl Pts',(-2.18763165103999,62.3249494318462,14.2244553837266));
#64016=CARTESIAN_POINT('Ctrl Pts',(-2.23288424985752,62.3399900837948,14.1124376546826));
#64017=CARTESIAN_POINT('Ctrl Pts',(-2.26016929432925,62.3490588415684,14.044896589673));
#64018=CARTESIAN_POINT('Ctrl Pts',(-2.28436697702911,62.3581144170538,13.9760234597122));
#64019=CARTESIAN_POINT('Ctrl Pts',(-2.30528819609144,62.3671443726308,13.906090902458));
#64020=CARTESIAN_POINT('Ctrl Pts',(-2.33117525897419,62.3783176712398,13.8195592093574));
#64021=CARTESIAN_POINT('Ctrl Pts',(-2.3522325795562,62.389560868264,13.7314261277675));
#64022=CARTESIAN_POINT('Ctrl Pts',(-2.36810889832169,62.4008599357382,13.6421621895604));
#64023=CARTESIAN_POINT('Ctrl Pts',(-2.39025521020944,62.4166213144319,13.5176454772758));
#64024=CARTESIAN_POINT('Ctrl Pts',(-2.40231955223421,62.4324916509277,13.3909260949408));
#64025=CARTESIAN_POINT('Ctrl Pts',(-2.40436278109046,62.4484275093813,13.2636193065498));
#64026=CARTESIAN_POINT('Ctrl Pts',(-2.40641819902219,62.4644584347096,13.1355530574407));
#64027=CARTESIAN_POINT('Ctrl Pts',(-2.39833131619744,62.4805556608201,13.0068926973835));
#64028=CARTESIAN_POINT('Ctrl Pts',(-2.38017332370241,62.4966688169118,12.879334371197));
#64029=CARTESIAN_POINT('Ctrl Pts',(-2.36199507708613,62.5127999462358,12.7516337615612));
#64030=CARTESIAN_POINT('Ctrl Pts',(-2.33372206985597,62.5289470290862,12.6250384379951));
#64031=CARTESIAN_POINT('Ctrl Pts',(-2.29545331523554,62.5450535149947,12.5012935366798));
#64032=CARTESIAN_POINT('Ctrl Pts',(-2.2777550052266,62.5525023484776,12.4440647178372));
#64033=CARTESIAN_POINT('Ctrl Pts',(-2.25791927630086,62.5599424159396,12.3874460872777));
#64034=CARTESIAN_POINT('Ctrl Pts',(-2.23595894097234,62.5673677011894,12.3316125240405));
#64035=CARTESIAN_POINT('Ctrl Pts',(-2.20325929085431,62.5784241912685,12.248474541155));
#64036=CARTESIAN_POINT('Ctrl Pts',(-2.16597892862786,62.5895536077964,12.1669980756594));
#64037=CARTESIAN_POINT('Ctrl Pts',(-2.12413456271561,62.6007408015926,12.0877263643258));
#64038=CARTESIAN_POINT('Ctrl Pts',(-2.06280503129239,62.6171374021505,11.9715411430849));
#64039=CARTESIAN_POINT('Ctrl Pts',(-1.99166944133828,62.6336583962586,11.8600904636704));
#64040=CARTESIAN_POINT('Ctrl Pts',(-1.91183578353717,62.6502506069489,11.7546857033027));
#64041=CARTESIAN_POINT('Ctrl Pts',(-1.83147654432938,62.6669520517351,11.6485870152891));
#64042=CARTESIAN_POINT('Ctrl Pts',(-1.74230347665068,62.6837256461713,11.5486152012365));
#64043=CARTESIAN_POINT('Ctrl Pts',(-1.64548519487996,62.7005107585213,11.4561434919834));
#64044=CARTESIAN_POINT('Ctrl Pts',(-1.54866258252202,62.7172966216531,11.363667646561));
#64045=CARTESIAN_POINT('Ctrl Pts',(-1.44419361983878,62.7340939872039,11.2786939854489));
#64046=CARTESIAN_POINT('Ctrl Pts',(-1.33329535227736,62.7508360309726,11.2026127655733));
#64047=CARTESIAN_POINT('Ctrl Pts',(-1.28567692813959,62.7580248695238,11.1699443760969));
#64048=CARTESIAN_POINT('Ctrl Pts',(-1.23687374844507,62.7652034321293,11.1389156099597));
#64049=CARTESIAN_POINT('Ctrl Pts',(-1.18698511474629,62.7723660906114,11.1096364226772));
#64050=CARTESIAN_POINT('Ctrl Pts',(-1.1169662830485,62.7824189010732,11.0685430045058));
#64051=CARTESIAN_POINT('Ctrl Pts',(-1.04473989886747,62.7924325160741,11.0308791404912));
#64052=CARTESIAN_POINT('Ctrl Pts',(-0.970669154241979,62.802513573085,10.9968390349676));
#64053=CARTESIAN_POINT('Ctrl Pts',(-0.96417153747111,62.8033979012422,10.9938529766844));
#64054=CARTESIAN_POINT('Ctrl Pts',(-0.957659702528321,62.8042827525257,
10.9908947829975));
#64055=CARTESIAN_POINT('Ctrl Pts',(-0.95113387948199,62.8051682013071,10.9879645736141));
#64056=CARTESIAN_POINT('Ctrl Pts',(2.62606127725066,71.5535446069272,11.6247283617098));
#64057=CARTESIAN_POINT('Ctrl Pts',(3.07369675274833,71.6548048472623,12.3017885911471));
#64058=CARTESIAN_POINT('Ctrl Pts',(3.39947547686869,71.8540694654572,13.9926794859483));
#64059=CARTESIAN_POINT('Ctrl Pts',(2.00035370322902,72.1534741441049,16.1563562104496));
#64060=CARTESIAN_POINT('Ctrl Pts',(-0.479193598718106,72.4505896841945,
16.7743438931863));
#64061=CARTESIAN_POINT('Ctrl Pts',(-2.72820677080343,72.749329075019,15.5345476487549));
#64062=CARTESIAN_POINT('Ctrl Pts',(-3.53053655760175,73.0491815267796,13.0830348300015));
#64063=CARTESIAN_POINT('Ctrl Pts',(-2.44583127626423,73.3496165328875,10.73926097503));
#64064=CARTESIAN_POINT('Ctrl Pts',(-0.0515057170124552,73.6501034404386,
9.76262003450415));
#64065=CARTESIAN_POINT('Ctrl Pts',(2.08813716621235,73.9167737645113,10.5786304219304));
#64066=CARTESIAN_POINT('Ctrl Pts',(3.14505930727665,74.1494556326765,12.1881664149021));
#64067=CARTESIAN_POINT('Ctrl Pts',(3.28302856381622,74.3482934483014,13.8249014301578));
#64068=CARTESIAN_POINT('Ctrl Pts',(2.62022018676624,74.5463751228733,15.3232742760889));
#64069=CARTESIAN_POINT('Ctrl Pts',(1.32704205219576,74.7435517804002,16.3159859655964));
#64070=CARTESIAN_POINT('Ctrl Pts',(-0.00839796692879819,74.9069885873292,
16.5242436918362));
#64071=CARTESIAN_POINT('Ctrl Pts',(-1.03406743711528,75.0371432170061,16.2943148716111));
#64072=CARTESIAN_POINT('Ctrl Pts',(-1.96986838717684,75.1668758709914,15.8219854723893));
#64073=CARTESIAN_POINT('Ctrl Pts',(-2.67823089801238,75.2959450476796,15.024243908725));
#64074=CARTESIAN_POINT('Ctrl Pts',(-2.99017889307188,75.4082368997061,14.1724204800879));
#64075=CARTESIAN_POINT('Ctrl Pts',(-3.06457943071697,75.4642187845407,13.7291125469622));
#64076=CARTESIAN_POINT('Ctrl Pts',(-3.08233538140113,75.4961587160299,13.4737488921684));
#64077=CARTESIAN_POINT('Ctrl Pts',(-3.0984392379095,75.6397395192991,12.3218754758916));
#64078=CARTESIAN_POINT('Ctrl Pts',(-1.89880363741605,75.9006508147323,10.2819015113804));
#64079=CARTESIAN_POINT('Ctrl Pts',(0.905612844857268,76.2108186357633,10.1560618488092));
#64080=CARTESIAN_POINT('Ctrl Pts',(2.4356553389957,76.4548900770423,11.4712451450617));
#64081=CARTESIAN_POINT('Ctrl Pts',(3.17219985054598,76.6961315682435,13.3281170575199));
#64082=CARTESIAN_POINT('Ctrl Pts',(2.56238501016055,76.8811530474602,14.8814311629097));
#64083=CARTESIAN_POINT('Ctrl Pts',(1.72783980301917,77.0124960583169,15.5266153278474));
#64084=CARTESIAN_POINT('Ctrl Pts',(1.53551862751901,77.0416343818686,15.6589169268593));
#64085=CARTESIAN_POINT('Ctrl Pts',(1.17818387297515,77.0924962062513,15.8569804874213));
#64086=CARTESIAN_POINT('Ctrl Pts',(0.623815753643446,77.1647861338154,16.0404402005033));
#64087=CARTESIAN_POINT('Ctrl Pts',(-0.0702939325535233,77.250932262354,
16.0883675706203));
#64088=CARTESIAN_POINT('Ctrl Pts',(-0.97706182894233,77.3649831053848,15.9240026281399));
#64089=CARTESIAN_POINT('Ctrl Pts',(-1.96791083657319,77.5060145445082,15.3088785584671));
#64090=CARTESIAN_POINT('Ctrl Pts',(-2.64752139679713,77.672758908484,14.1087106115944));
#64091=CARTESIAN_POINT('Ctrl Pts',(-2.66935132912839,77.8369818342363,12.7510168963697));
#64092=CARTESIAN_POINT('Ctrl Pts',(-2.04802128466415,77.9986630811314,11.5672470590297));
#64093=CARTESIAN_POINT('Ctrl Pts',(-0.953406375685504,78.1577929882928,
10.8374874366033));
#64094=CARTESIAN_POINT('Ctrl Pts',(0.336148931890551,78.3143710867681,10.7228295007321));
#64095=CARTESIAN_POINT('Ctrl Pts',(1.50307999575334,78.4684077961839,11.2321414818918));
#64096=CARTESIAN_POINT('Ctrl Pts',(2.27244152083141,78.6199207500098,12.2206815704071));
#64097=CARTESIAN_POINT('Ctrl Pts',(2.47025450075222,78.7689406968174,13.4369060696769));
#64098=CARTESIAN_POINT('Ctrl Pts',(2.06838453699815,78.9155054863287,14.580422079702));
#64099=CARTESIAN_POINT('Ctrl Pts',(1.18267230002556,79.0596632019735,15.3776880766993));
#64100=CARTESIAN_POINT('Ctrl Pts',(0.0417367172907162,79.2014711616318,
15.651091689114));
#64101=CARTESIAN_POINT('Ctrl Pts',(-1.07091431074263,79.3409947472366,15.348470280034));
#64102=CARTESIAN_POINT('Ctrl Pts',(-1.98410802505723,79.4935674136222,14.4759887843483));
#64103=CARTESIAN_POINT('Ctrl Pts',(-2.29250453277775,79.6583660808514,13.1152303337474));
#64104=CARTESIAN_POINT('Ctrl Pts',(-1.65329344570907,79.8345871894848,11.7642469664184));
#64105=CARTESIAN_POINT('Ctrl Pts',(-0.561194871313656,79.9786744458678,
11.2211155923112));
#64106=CARTESIAN_POINT('Ctrl Pts',(0.248468418157764,80.078205765166,11.2502761671321));
#64107=CARTESIAN_POINT('Ctrl Pts',(0.683379628434247,80.134714093272,11.3779527164502));
#64108=CARTESIAN_POINT('Ctrl Pts',(1.50537944865847,80.247265487895,11.7682049163228));
#64109=CARTESIAN_POINT('Ctrl Pts',(2.06939217422075,80.3720681591741,12.736646766933));
#64110=CARTESIAN_POINT('Ctrl Pts',(1.90567271165315,80.5225053556114,13.9535241790153));
#64111=CARTESIAN_POINT('Ctrl Pts',(1.44391453743883,80.6310252212425,14.7196833195633));
#64112=CARTESIAN_POINT('Ctrl Pts',(0.57711443901227,80.7520545863008,15.2239016882313));
#64113=CARTESIAN_POINT('Ctrl Pts',(-0.415289947510754,80.8721738215391,
15.2506488494656));
#64114=CARTESIAN_POINT('Ctrl Pts',(-1.29478405254176,80.9915321525424,14.801994928262));
#64115=CARTESIAN_POINT('Ctrl Pts',(-1.84882892486789,81.1102808484601,13.9907678349858));
#64116=CARTESIAN_POINT('Ctrl Pts',(-1.92183367763277,81.1990029414579,13.2607435842994));
#64117=CARTESIAN_POINT('Ctrl Pts',(-1.8217052798405,81.2580564159435,12.7970006616204));
#64118=CARTESIAN_POINT('Ctrl Pts',(-1.71726172276848,81.2974025519046,12.4987499564163));
#64119=CARTESIAN_POINT('Ctrl Pts',(-1.43925958278793,81.366216398273,12.0170756654402));
#64120=CARTESIAN_POINT('Ctrl Pts',(-0.803691837170658,81.4644268389926,
11.5113131401901));
#64121=CARTESIAN_POINT('Ctrl Pts',(0.157310001461349,81.5823031737216,11.3451440479436));
#64122=CARTESIAN_POINT('Ctrl Pts',(1.08175881202912,81.7003494145943,11.6587285348207));
#64123=CARTESIAN_POINT('Ctrl Pts',(1.74459855235824,81.8187309164738,12.3798675479581));
#64124=CARTESIAN_POINT('Ctrl Pts',(1.98175103862329,81.9375991758226,13.3341054677106));
#64125=CARTESIAN_POINT('Ctrl Pts',(1.73131320698376,82.0571102816978,14.2902754504896));
#64126=CARTESIAN_POINT('Ctrl Pts',(1.04838542790616,82.1774164300365,15.0148406760434));
#64127=CARTESIAN_POINT('Ctrl Pts',(0.0950356967664279,82.2986627179121,
15.3241799164539));
#64128=CARTESIAN_POINT('Ctrl Pts',(-1.01123848225145,82.4345915545847,15.1190339956634));
#64129=CARTESIAN_POINT('Ctrl Pts',(-1.93343043195045,82.5858630943909,14.2288726578984));
#64130=CARTESIAN_POINT('Ctrl Pts',(-2.1256356945421,82.7533957188934,12.8212136757709));
#64131=CARTESIAN_POINT('Ctrl Pts',(-1.50138332796606,82.8988937003856,11.7583081310997));
#64132=CARTESIAN_POINT('Ctrl Pts',(-0.632429912249052,83.0212610196965,
11.2664585694225));
#64133=CARTESIAN_POINT('Ctrl Pts',(0.424674872888512,83.1521963337219,11.1113494661316));
#64134=CARTESIAN_POINT('Ctrl Pts',(1.73233529621671,83.3185416832946,11.6891669232624));
#64135=CARTESIAN_POINT('Ctrl Pts',(2.42258940526503,83.5227848964116,13.3064020986805));
#64136=CARTESIAN_POINT('Ctrl Pts',(1.81060149541817,83.7319444375417,14.9983668615199));
#64137=CARTESIAN_POINT('Ctrl Pts',(0.169716220670518,83.9462835131092,15.8393531505486));
#64138=CARTESIAN_POINT('Ctrl Pts',(-1.64864304635011,84.1660018217439,15.3229733594306));
#64139=CARTESIAN_POINT('Ctrl Pts',(-2.69270309708095,84.4008278320615,13.5930908615205));
#64140=CARTESIAN_POINT('Ctrl Pts',(-2.34009646860672,84.5648308878988,12.2032471101965));
#64141=CARTESIAN_POINT('Ctrl Pts',(-1.89038667730081,84.6529546621916,11.6566997621504));
#64142=CARTESIAN_POINT('Ctrl Pts',(2.45537460810738,71.8997412275771,11.7369673410428));
#64143=CARTESIAN_POINT('Ctrl Pts',(2.86465514317376,71.9944459875631,12.3761438649969));
#64144=CARTESIAN_POINT('Ctrl Pts',(3.14183581063553,72.1798336583578,13.9534707954349));
#64145=CARTESIAN_POINT('Ctrl Pts',(1.82121553961701,72.4557236515511,15.9258509314207));
#64146=CARTESIAN_POINT('Ctrl Pts',(-0.451459878047153,72.7271148628889,
16.454626209561));
#64147=CARTESIAN_POINT('Ctrl Pts',(-2.47125649787517,72.9978001233845,15.3003831479765));
#64148=CARTESIAN_POINT('Ctrl Pts',(-3.15929694060047,73.267507381235,13.0852384125598));
#64149=CARTESIAN_POINT('Ctrl Pts',(-2.15920493547541,73.535967111269,11.0060938504777));
#64150=CARTESIAN_POINT('Ctrl Pts',(-0.0200714085127461,73.8029233628205,
10.1699982444172));
#64151=CARTESIAN_POINT('Ctrl Pts',(1.86030659853292,74.0386635562282,10.9184680604956));
#64152=CARTESIAN_POINT('Ctrl Pts',(2.77130128735905,74.2436551756362,12.3489582116326));
#64153=CARTESIAN_POINT('Ctrl Pts',(2.87251295759163,74.4184202620592,13.7887881944876));
#64154=CARTESIAN_POINT('Ctrl Pts',(2.27296651564915,74.5921831870885,15.0946922490105));
#64155=CARTESIAN_POINT('Ctrl Pts',(1.12856013061699,74.7648878883527,15.9481703025818));
#64156=CARTESIAN_POINT('Ctrl Pts',(-0.0420118937118654,74.9078827780563,
16.1140624242939));
#64157=CARTESIAN_POINT('Ctrl Pts',(-0.935852251025538,75.0216999964023,
15.9006181548314));
#64158=CARTESIAN_POINT('Ctrl Pts',(-1.74799302734623,75.1351234789987,15.4764072161691));
#64159=CARTESIAN_POINT('Ctrl Pts',(-2.35725039846603,75.247946473202,14.7706510349632));
#64160=CARTESIAN_POINT('Ctrl Pts',(-2.61943865821339,75.3461227134966,14.0223232072198));
#64161=CARTESIAN_POINT('Ctrl Pts',(-2.67900504266786,75.3950740424631,13.6339039044037));
#64162=CARTESIAN_POINT('Ctrl Pts',(-2.69137681403548,75.4230063808888,13.4104334520196));
#64163=CARTESIAN_POINT('Ctrl Pts',(-2.69118459524818,75.5485825065238,12.4031854715294));
#64164=CARTESIAN_POINT('Ctrl Pts',(-1.61715338616522,75.7769418229487,10.6324544464939));
#64165=CARTESIAN_POINT('Ctrl Pts',(0.846315643470564,76.0493083690221,10.5555177734551));
#64166=CARTESIAN_POINT('Ctrl Pts',(2.17807352495375,76.2644764381485,11.7341625679922));
#64167=CARTESIAN_POINT('Ctrl Pts',(2.8051524329496,76.4778185988283,13.3850640198186));
#64168=CARTESIAN_POINT('Ctrl Pts',(2.24430249048783,76.642344041271,14.7582423366972));
#64169=CARTESIAN_POINT('Ctrl Pts',(1.48979469934905,76.7597131591705,15.3229864188903));
#64170=CARTESIAN_POINT('Ctrl Pts',(1.31604755489563,76.7857668522089,15.4385204013053));
#64171=CARTESIAN_POINT('Ctrl Pts',(0.9935887065671,76.8312864599085,15.610685427541));
#64172=CARTESIAN_POINT('Ctrl Pts',(0.494170705343874,76.8961015211196,15.7672982479309));
#64173=CARTESIAN_POINT('Ctrl Pts',(-0.130228120937696,76.9735420130962,
15.8004817055351));
#64174=CARTESIAN_POINT('Ctrl Pts',(-0.944846658431455,77.0763476093393,
15.6393426684008));
#64175=CARTESIAN_POINT('Ctrl Pts',(-1.83275135211394,77.2040199705238,15.0686965094999));
#64176=CARTESIAN_POINT('Ctrl Pts',(-2.43422897081155,77.3559138629566,13.9660529667295));
#64177=CARTESIAN_POINT('Ctrl Pts',(-2.43412964201641,77.5065223841571,12.7211217363066));
#64178=CARTESIAN_POINT('Ctrl Pts',(-1.84244736467127,77.6558779466535,11.6375025646228));
#64179=CARTESIAN_POINT('Ctrl Pts',(-0.812508634489196,77.8040179721768,
10.9754960366569));
#64180=CARTESIAN_POINT('Ctrl Pts',(0.399169147060676,77.9509840951834,10.888554482799));
#64181=CARTESIAN_POINT('Ctrl Pts',(1.49515333246982,78.0968241859332,11.3897674493044));
#64182=CARTESIAN_POINT('Ctrl Pts',(2.21309666412229,78.2415857024887,12.346800944208));
#64183=CARTESIAN_POINT('Ctrl Pts',(2.38257715684069,78.3853267723206,13.5227887118762));
#64184=CARTESIAN_POINT('Ctrl Pts',(1.97070979036788,78.5281048583051,14.6289215533792));
#64185=CARTESIAN_POINT('Ctrl Pts',(1.0846356356463,78.6699825164188,15.3966558175012));
#64186=CARTESIAN_POINT('Ctrl Pts',(-0.0546578360320794,78.8110261821086,
15.6465003144658));
#64187=CARTESIAN_POINT('Ctrl Pts',(-1.16663794159566,78.9513037625806,15.320240485781));
#64188=CARTESIAN_POINT('Ctrl Pts',(-2.07635850104646,79.106398067496,14.4152732562341));
#64189=CARTESIAN_POINT('Ctrl Pts',(-2.36611662039193,79.2761195563421,13.0084404449859));
#64190=CARTESIAN_POINT('Ctrl Pts',(-1.66972195348897,79.4603539256571,11.6104800674147));
#64191=CARTESIAN_POINT('Ctrl Pts',(-0.499241727900942,79.6132764154737,
11.0587123014677));
#64192=CARTESIAN_POINT('Ctrl Pts',(0.368381431253317,79.7200919455142,11.1100688932815));
#64193=CARTESIAN_POINT('Ctrl Pts',(0.834024390540476,79.7810729395003,11.2590830141615));
#64194=CARTESIAN_POINT('Ctrl Pts',(1.71327073675581,79.9029752811733,11.7022803019732));
#64195=CARTESIAN_POINT('Ctrl Pts',(2.31023027030925,80.039893650478,12.7769722273746));
#64196=CARTESIAN_POINT('Ctrl Pts',(2.0952937696238,80.2072118206172,14.1251984017593));
#64197=CARTESIAN_POINT('Ctrl Pts',(1.55681308005668,80.3289253095954,14.9709562403181));
#64198=CARTESIAN_POINT('Ctrl Pts',(0.562156846133121,80.4659772183401,15.5172494438125));
#64199=CARTESIAN_POINT('Ctrl Pts',(-0.571635535172935,80.6032374513939,
15.5193058729101));
#64200=CARTESIAN_POINT('Ctrl Pts',(-1.57105590216914,80.7407895484418,14.9769995665407));
#64201=CARTESIAN_POINT('Ctrl Pts',(-2.18972564985028,80.8787156023155,14.0191108554115));
#64202=CARTESIAN_POINT('Ctrl Pts',(-2.25281448620538,80.9825022603659,13.1637487406573));
#64203=CARTESIAN_POINT('Ctrl Pts',(-2.12068431526726,81.0518598050773,12.6228061624787));
#64204=CARTESIAN_POINT('Ctrl Pts',(-1.98850067502905,81.0981436402853,12.2756453504514));
#64205=CARTESIAN_POINT('Ctrl Pts',(-1.64588283908225,81.1792688423294,11.7171923425473));
#64206=CARTESIAN_POINT('Ctrl Pts',(-0.878376654572089,81.2955409216237,
11.1389422271489));
#64207=CARTESIAN_POINT('Ctrl Pts',(0.268860592398065,81.4357574199077,10.9718961823663));
#64208=CARTESIAN_POINT('Ctrl Pts',(1.36168464727168,81.5767306353953,11.3754866253281));
#64209=CARTESIAN_POINT('Ctrl Pts',(2.13170024959015,81.7185337285348,12.2596742591993));
#64210=CARTESIAN_POINT('Ctrl Pts',(2.38537574225421,81.861230869759,13.411638936312));
#64211=CARTESIAN_POINT('Ctrl Pts',(2.0538618627471,82.0048858136013,14.5517127600868));
#64212=CARTESIAN_POINT('Ctrl Pts',(1.21016878839885,82.1495577534274,15.4001780362731));
#64213=CARTESIAN_POINT('Ctrl Pts',(0.0554960675800941,82.2953007614427,
15.7411221116997));
#64214=CARTESIAN_POINT('Ctrl Pts',(-1.26478769570871,82.4584859871312,15.4599241062122));
#64215=CARTESIAN_POINT('Ctrl Pts',(-2.33986872524533,82.6396574319745,14.3656368632881));
#64216=CARTESIAN_POINT('Ctrl Pts',(-2.52469843952306,82.8394791673108,12.6823557101889));
#64217=CARTESIAN_POINT('Ctrl Pts',(-1.75208427106857,83.0120920363884,11.441919509068));
#64218=CARTESIAN_POINT('Ctrl Pts',(-0.712950690786717,83.1565241170819,
10.8875878228662));
#64219=CARTESIAN_POINT('Ctrl Pts',(0.533306351324057,83.3104483484253,10.7361019540252));
#64220=CARTESIAN_POINT('Ctrl Pts',(2.04196476140802,83.5047430421028,11.4494235183952));
#64221=CARTESIAN_POINT('Ctrl Pts',(2.79244898421244,83.7409671959345,13.3383065741216));
#64222=CARTESIAN_POINT('Ctrl Pts',(2.0450220032682,83.9802835859361,15.2551413117453));
#64223=CARTESIAN_POINT('Ctrl Pts',(0.167912320780133,84.2226842947316,16.1606000614443));
#64224=CARTESIAN_POINT('Ctrl Pts',(-1.84816591142016,84.4681399480701,15.5361778286278));
#64225=CARTESIAN_POINT('Ctrl Pts',(-2.95469492563506,84.7271265431151,13.6033326154612));
#64226=CARTESIAN_POINT('Ctrl Pts',(-2.53671169284916,84.9054952968908,12.1013400726277));
#64227=CARTESIAN_POINT('Ctrl Pts',(-2.04018169331035,85.000602884221,11.5215710376628));
#64228=CARTESIAN_POINT('Ctrl Pts',(2.28468793896408,72.245937848227,11.8492063203758));
#64229=CARTESIAN_POINT('Ctrl Pts',(2.65561353359917,72.334087127864,12.4504991388465));
#64230=CARTESIAN_POINT('Ctrl Pts',(2.88419614440235,72.5055978512584,13.9142621049215));
#64231=CARTESIAN_POINT('Ctrl Pts',(1.64207737600503,72.7579731589971,15.695345652392));
#64232=CARTESIAN_POINT('Ctrl Pts',(-0.423726157376209,73.0036400415831,
16.1349085259356));
#64233=CARTESIAN_POINT('Ctrl Pts',(-2.21430622494689,73.24627117175,15.0662186471979));
#64234=CARTESIAN_POINT('Ctrl Pts',(-2.78805732359919,73.4858332356904,13.0874419951179));
#64235=CARTESIAN_POINT('Ctrl Pts',(-1.87257859468661,73.7223176896503,11.2729267259256));
#64236=CARTESIAN_POINT('Ctrl Pts',(0.0113628999869613,73.9557432852023,
10.5773764543301));
#64237=CARTESIAN_POINT('Ctrl Pts',(1.63247603085348,74.1605533479452,11.2583056990608));
#64238=CARTESIAN_POINT('Ctrl Pts',(2.39754326744144,74.3378547185957,12.5097500083632));
#64239=CARTESIAN_POINT('Ctrl Pts',(2.46199735136702,74.488547075817,13.7526749588175));
#64240=CARTESIAN_POINT('Ctrl Pts',(1.92571284453205,74.6379912513037,14.8661102219322));
#64241=CARTESIAN_POINT('Ctrl Pts',(0.930078209038217,74.7862239963053,15.5803546395671));
#64242=CARTESIAN_POINT('Ctrl Pts',(-0.0756258204949394,74.9087769687833,
15.7038811567516));
#64243=CARTESIAN_POINT('Ctrl Pts',(-0.837637064935803,75.0062567757983,
15.5069214380518));
#64244=CARTESIAN_POINT('Ctrl Pts',(-1.52611766751561,75.1033710870057,15.1308289599487));
#64245=CARTESIAN_POINT('Ctrl Pts',(-2.03626989891968,75.1999478987245,14.5170581612014));
#64246=CARTESIAN_POINT('Ctrl Pts',(-2.2486984233549,75.2840085272871,13.8722259343517));
#64247=CARTESIAN_POINT('Ctrl Pts',(-2.29343065461876,75.3259293003855,13.5386952618452));
#64248=CARTESIAN_POINT('Ctrl Pts',(-2.30041824666983,75.3498540457475,13.3471180118707));
#64249=CARTESIAN_POINT('Ctrl Pts',(-2.28392995258685,75.4574254937484,12.4844954671671));
#64250=CARTESIAN_POINT('Ctrl Pts',(-1.33550313491438,75.6532328311649,10.9830073816075));
#64251=CARTESIAN_POINT('Ctrl Pts',(0.787018442083865,75.8877981022809,10.9549736981013));
#64252=CARTESIAN_POINT('Ctrl Pts',(1.92049171091181,76.0740627992544,11.9970799909228));
#64253=CARTESIAN_POINT('Ctrl Pts',(2.43810501535319,76.2595056294131,13.4420109821172));
#64254=CARTESIAN_POINT('Ctrl Pts',(1.92621997081512,76.4035350350817,14.6350535104845));
#64255=CARTESIAN_POINT('Ctrl Pts',(1.25174959567892,76.5069302600241,15.1193575099331));
#64256=CARTESIAN_POINT('Ctrl Pts',(1.09657648227224,76.5298993225489,15.2181238757514));
#64257=CARTESIAN_POINT('Ctrl Pts',(0.808993540159056,76.5700767135657,15.3643903676609));
#64258=CARTESIAN_POINT('Ctrl Pts',(0.364525657044304,76.6274169084238,15.4941562953586));
#64259=CARTESIAN_POINT('Ctrl Pts',(-0.190162309321864,76.6961517638386,
15.5125958404498));
#64260=CARTESIAN_POINT('Ctrl Pts',(-0.912631487920573,76.7877121132939,
15.3546827086616));
#64261=CARTESIAN_POINT('Ctrl Pts',(-1.69759186765469,76.9020253965394,14.8285144605326));
#64262=CARTESIAN_POINT('Ctrl Pts',(-2.22093654482596,77.039068817429,13.8233953218645));
#64263=CARTESIAN_POINT('Ctrl Pts',(-2.19890795490443,77.1760629340776,12.6912265762433));
#64264=CARTESIAN_POINT('Ctrl Pts',(-1.63687344467838,77.3130928121755,11.7077580702161));
#64265=CARTESIAN_POINT('Ctrl Pts',(-0.671610893292886,77.4502429560611,
11.1135046367102));
#64266=CARTESIAN_POINT('Ctrl Pts',(0.462189362230805,77.5875971035986,11.0542794648659));
#64267=CARTESIAN_POINT('Ctrl Pts',(1.4872266691863,77.7252405756827,11.5473934167169));
#64268=CARTESIAN_POINT('Ctrl Pts',(2.15375180741318,77.8632506549678,12.4729203180088));
#64269=CARTESIAN_POINT('Ctrl Pts',(2.29489981292916,78.0017128478238,13.6086713540756));
#64270=CARTESIAN_POINT('Ctrl Pts',(1.87303504373762,78.1407042302814,14.6774210270564));
#64271=CARTESIAN_POINT('Ctrl Pts',(0.986598971267029,78.2803018308642,15.4156235583032));
#64272=CARTESIAN_POINT('Ctrl Pts',(-0.151052389354876,78.4205812025852,
15.6419089398177));
#64273=CARTESIAN_POINT('Ctrl Pts',(-1.2623615724487,78.5616127779246,15.2920106915281));
#64274=CARTESIAN_POINT('Ctrl Pts',(-2.1686089770357,78.7192287213697,14.3545577281199));
#64275=CARTESIAN_POINT('Ctrl Pts',(-2.43972870800612,78.8938730318327,12.9016505562244));
#64276=CARTESIAN_POINT('Ctrl Pts',(-1.68615046126887,79.0861206618293,11.4567131684111));
#64277=CARTESIAN_POINT('Ctrl Pts',(-0.43728858448823,79.2478783850796,10.8963090106243));
#64278=CARTESIAN_POINT('Ctrl Pts',(0.488294444348867,79.3619781258626,10.9698616194307));
#64279=CARTESIAN_POINT('Ctrl Pts',(0.984669152646702,79.4274317857285,11.140213311873));
#64280=CARTESIAN_POINT('Ctrl Pts',(1.92116202485315,79.5586850744516,11.6363556876237));
#64281=CARTESIAN_POINT('Ctrl Pts',(2.55106836639776,79.7077191417819,12.8172976878161));
#64282=CARTESIAN_POINT('Ctrl Pts',(2.28491482759442,79.8919182856231,14.2968726245033));
#64283=CARTESIAN_POINT('Ctrl Pts',(1.66971162267453,80.0268253979483,15.2222291610727));
#64284=CARTESIAN_POINT('Ctrl Pts',(0.547199253253971,80.1798998503795,15.8105971993939));
#64285=CARTESIAN_POINT('Ctrl Pts',(-0.727981122835118,80.3343010812489,
15.7879628963548));
#64286=CARTESIAN_POINT('Ctrl Pts',(-1.84732775179652,80.4900469443413,15.1520042048194));
#64287=CARTESIAN_POINT('Ctrl Pts',(-2.53062237483268,80.6471503561707,14.0474538758371));
#64288=CARTESIAN_POINT('Ctrl Pts',(-2.583795294778,80.7660015792739,13.0667538970152));
#64289=CARTESIAN_POINT('Ctrl Pts',(-2.419663350694,80.8456631942111,12.4486116633369));
#64290=CARTESIAN_POINT('Ctrl Pts',(-2.25973962728962,80.8988847286658,12.0525407444864));
#64291=CARTESIAN_POINT('Ctrl Pts',(-1.85250609537659,80.9923212863861,11.4173090196543));
#64292=CARTESIAN_POINT('Ctrl Pts',(-0.953061471973522,81.1266550042549,
10.7665713141076));
#64293=CARTESIAN_POINT('Ctrl Pts',(0.380411183334777,81.2892116660939,10.598648316789));
#64294=CARTESIAN_POINT('Ctrl Pts',(1.64161048251426,81.4531118561961,11.0922447158354));
#64295=CARTESIAN_POINT('Ctrl Pts',(2.51880194682208,81.6183365405957,12.1394809704407));
#64296=CARTESIAN_POINT('Ctrl Pts',(2.78900044588513,81.7848625636954,13.4891724049134));
#64297=CARTESIAN_POINT('Ctrl Pts',(2.37641051851043,81.9526613455049,14.8131500696841));
#64298=CARTESIAN_POINT('Ctrl Pts',(1.37195214889153,82.1216990768183,15.785515396503));
#64299=CARTESIAN_POINT('Ctrl Pts',(0.0159564383937635,82.2919388049734,
16.1580643069455));
#64300=CARTESIAN_POINT('Ctrl Pts',(-1.51833690916597,82.4823804196777,15.800814216761));
#64301=CARTESIAN_POINT('Ctrl Pts',(-2.7463070185402,82.6934517695579,14.502401068678));
#64302=CARTESIAN_POINT('Ctrl Pts',(-2.92376118450403,82.9255626157282,12.5434977446069));
#64303=CARTESIAN_POINT('Ctrl Pts',(-2.00278521417108,83.1252903723912,11.1255308870361));
#64304=CARTESIAN_POINT('Ctrl Pts',(-0.793471469324382,83.2917872144671,
10.5087170763097));
#64305=CARTESIAN_POINT('Ctrl Pts',(0.641937829759612,83.4687003631288,10.3608544419188));
#64306=CARTESIAN_POINT('Ctrl Pts',(2.35159422659933,83.6909444009111,11.2096801135279));
#64307=CARTESIAN_POINT('Ctrl Pts',(3.16230856315989,83.9591494954575,13.3702110495627));
#64308=CARTESIAN_POINT('Ctrl Pts',(2.27944251111824,84.2286227343307,15.5119157619708));
#64309=CARTESIAN_POINT('Ctrl Pts',(0.166108420889751,84.4990850763539,16.48184697234));
#64310=CARTESIAN_POINT('Ctrl Pts',(-2.04768877649022,84.7702780743964,15.7493822978251));
#64311=CARTESIAN_POINT('Ctrl Pts',(-3.21668675418916,85.0534252541687,13.6135743694018));
#64312=CARTESIAN_POINT('Ctrl Pts',(-2.7333269170916,85.246159705883,11.999433035059));
#64313=CARTESIAN_POINT('Ctrl Pts',(-2.18997670931989,85.3482511062504,11.3864423131751));
#64314=CARTESIAN_POINT('Ctrl Pts',(2.11400126982079,72.5921344688769,11.9614452997087));
#64315=CARTESIAN_POINT('Ctrl Pts',(2.44657192402459,72.6737282681649,12.5248544126962));
#64316=CARTESIAN_POINT('Ctrl Pts',(2.62655647816917,72.8313620441591,13.8750534144082));
#64317=CARTESIAN_POINT('Ctrl Pts',(1.46293921239302,73.0602226664433,15.464840373363));
#64318=CARTESIAN_POINT('Ctrl Pts',(-0.395992436705256,73.2801652202774,
15.8151908423103));
#64319=CARTESIAN_POINT('Ctrl Pts',(-1.95735595201862,73.4947422201155,14.8320541464193));
#64320=CARTESIAN_POINT('Ctrl Pts',(-2.4168177065979,73.7041590901459,13.0896455776762));
#64321=CARTESIAN_POINT('Ctrl Pts',(-1.5859522538978,73.9086682680316,11.5397596013732));
#64322=CARTESIAN_POINT('Ctrl Pts',(0.0427972084866695,74.1085632075843,
10.9847546642431));
#64323=CARTESIAN_POINT('Ctrl Pts',(1.40464546317404,74.282443139662,11.598143337626));
#64324=CARTESIAN_POINT('Ctrl Pts',(2.02378524752384,74.4320542615553,12.6705418050936));
#64325=CARTESIAN_POINT('Ctrl Pts',(2.05148174514243,74.5586738895749,13.7165617231474));
#64326=CARTESIAN_POINT('Ctrl Pts',(1.57845917341493,74.6837993155188,14.6375281948537));
#64327=CARTESIAN_POINT('Ctrl Pts',(0.731596287459446,74.8075601042579,15.2125389765525));
#64328=CARTESIAN_POINT('Ctrl Pts',(-0.109239747278009,74.9096711595105,
15.2936998892093));
#64329=CARTESIAN_POINT('Ctrl Pts',(-0.739421878846066,74.9908135551944,
15.1132247212721));
#64330=CARTESIAN_POINT('Ctrl Pts',(-1.30424230768499,75.0716186950129,14.7852507037284));
#64331=CARTESIAN_POINT('Ctrl Pts',(-1.71528939937333,75.1519493242468,14.2634652874395));
#64332=CARTESIAN_POINT('Ctrl Pts',(-1.87795818849642,75.2218943410776,13.7221286614836));
#64333=CARTESIAN_POINT('Ctrl Pts',(-1.90785626656966,75.2567845583079,13.4434866192867));
#64334=CARTESIAN_POINT('Ctrl Pts',(-1.90945967930417,75.2767017106063,13.2838025717218));
#64335=CARTESIAN_POINT('Ctrl Pts',(-1.87667530992554,75.3662684809731,12.5658054628048));
#64336=CARTESIAN_POINT('Ctrl Pts',(-1.05385288366353,75.5295238393814,11.333560316721));
#64337=CARTESIAN_POINT('Ctrl Pts',(0.727721240697154,75.7262878355396,11.3544296227473));
#64338=CARTESIAN_POINT('Ctrl Pts',(1.66290989686987,75.8836491603605,12.2599974138533));
#64339=CARTESIAN_POINT('Ctrl Pts',(2.07105759775679,76.0411926599979,13.4989579444158));
#64340=CARTESIAN_POINT('Ctrl Pts',(1.60813745114241,76.1647260288924,14.5118646842719));
#64341=CARTESIAN_POINT('Ctrl Pts',(1.01370449200879,76.2541473608778,14.9157286009759));
#64342=CARTESIAN_POINT('Ctrl Pts',(0.877105409648848,76.2740317928892,14.9977273501975));
#64343=CARTESIAN_POINT('Ctrl Pts',(0.624398373750998,76.3088669672229,15.1180953077808));
#64344=CARTESIAN_POINT('Ctrl Pts',(0.234880608744721,76.3587322957282,15.2210143427862));
#64345=CARTESIAN_POINT('Ctrl Pts',(-0.250096497706049,76.4187615145809,
15.2247099753646));
#64346=CARTESIAN_POINT('Ctrl Pts',(-0.880416317409708,76.4990766172484,
15.0700227489227));
#64347=CARTESIAN_POINT('Ctrl Pts',(-1.56243238319545,76.6000308225549,14.5883324115654));
#64348=CARTESIAN_POINT('Ctrl Pts',(-2.00764411884039,76.7222237719016,13.6807376769993));
#64349=CARTESIAN_POINT('Ctrl Pts',(-1.96368626779247,76.8456034839983,12.6613314161801));
#64350=CARTESIAN_POINT('Ctrl Pts',(-1.43129952468551,76.9703076776975,11.7780135758093));
#64351=CARTESIAN_POINT('Ctrl Pts',(-0.530713152096587,77.0964679399452,
11.2515132367637));
#64352=CARTESIAN_POINT('Ctrl Pts',(0.525209577400925,77.2242101120139,11.2200044469327));
#64353=CARTESIAN_POINT('Ctrl Pts',(1.47930000590277,77.3536569654321,11.7050193841296));
#64354=CARTESIAN_POINT('Ctrl Pts',(2.09440695070407,77.4849156074468,12.5990396918098));
#64355=CARTESIAN_POINT('Ctrl Pts',(2.20722246901762,77.6180989233271,13.6945539962748));
#64356=CARTESIAN_POINT('Ctrl Pts',(1.77536029710735,77.7533036022579,14.7259205007336));
#64357=CARTESIAN_POINT('Ctrl Pts',(0.88856230688776,77.8906211453096,15.4345912991052));
#64358=CARTESIAN_POINT('Ctrl Pts',(-0.247446942677673,78.030136223062,15.6373175651695));
#64359=CARTESIAN_POINT('Ctrl Pts',(-1.35808520330174,78.1719217932686,15.263780897275));
#64360=CARTESIAN_POINT('Ctrl Pts',(-2.26085945302493,78.3320593752434,14.2938422000058));
#64361=CARTESIAN_POINT('Ctrl Pts',(-2.51334079562032,78.5116265073234,12.7948606674629));
#64362=CARTESIAN_POINT('Ctrl Pts',(-1.70257896904877,78.7118873980016,11.3029462694074));
#64363=CARTESIAN_POINT('Ctrl Pts',(-0.375335441075516,78.8824803546856,
10.7339057197809));
#64364=CARTESIAN_POINT('Ctrl Pts',(0.608207457444419,79.0038643062108,10.8296543455799));
#64365=CARTESIAN_POINT('Ctrl Pts',(1.13531391475293,79.0737906319567,11.0213436095844));
#64366=CARTESIAN_POINT('Ctrl Pts',(2.12905331295049,79.2143948677298,11.5704310732741));
#64367=CARTESIAN_POINT('Ctrl Pts',(2.79190646248625,79.3755446330857,12.8576231482577));
#64368=CARTESIAN_POINT('Ctrl Pts',(2.47453588556505,79.5766247506289,14.4685468472474));
#64369=CARTESIAN_POINT('Ctrl Pts',(1.78261016529238,79.7247254863011,15.4735020818274));
#64370=CARTESIAN_POINT('Ctrl Pts',(0.53224166037482,79.8938224824188,16.1039449549752));
#64371=CARTESIAN_POINT('Ctrl Pts',(-0.884326710497297,80.0653647111037,
16.0566199197993));
#64372=CARTESIAN_POINT('Ctrl Pts',(-2.12359960142391,80.2393043402407,15.3270088430981));
#64373=CARTESIAN_POINT('Ctrl Pts',(-2.87151909981507,80.415585110026,14.0757968962628));
#64374=CARTESIAN_POINT('Ctrl Pts',(-2.91477610335063,80.5495008981822,12.9697590533731));
#64375=CARTESIAN_POINT('Ctrl Pts',(-2.71864238612076,80.6394665833449,12.2744171641952));
#64376=CARTESIAN_POINT('Ctrl Pts',(-2.53097857955019,80.6996258170464,11.8294361385213));
#64377=CARTESIAN_POINT('Ctrl Pts',(-2.05912935167091,80.8053737304426,11.1174256967615));
#64378=CARTESIAN_POINT('Ctrl Pts',(-1.02774628937495,80.957769086886,10.3942004010663));
#64379=CARTESIAN_POINT('Ctrl Pts',(0.491961774271491,81.14266591228,10.2254004512117));
#64380=CARTESIAN_POINT('Ctrl Pts',(1.92153631775683,81.3294930769971,10.8090028063427));
#64381=CARTESIAN_POINT('Ctrl Pts',(2.90590364405399,81.5181393526567,12.0192876816821));
#64382=CARTESIAN_POINT('Ctrl Pts',(3.19262514951605,81.708494257632,13.5667058735148));
#64383=CARTESIAN_POINT('Ctrl Pts',(2.69895917427376,81.9004368774085,15.0745873792813));
#64384=CARTESIAN_POINT('Ctrl Pts',(1.5337355093842,82.0938404002092,16.1708527567328));
#64385=CARTESIAN_POINT('Ctrl Pts',(-0.0235831907925716,82.2885768485042,
16.5750065021912));
#64386=CARTESIAN_POINT('Ctrl Pts',(-1.77188612262323,82.5062748522241,16.1417043273099));
#64387=CARTESIAN_POINT('Ctrl Pts',(-3.15274531183509,82.7472461071415,14.6391652740677));
#64388=CARTESIAN_POINT('Ctrl Pts',(-3.32282392948499,83.0116460641456,12.4046397790249));
#64389=CARTESIAN_POINT('Ctrl Pts',(-2.25348615727359,83.238488708394,10.8091422650043));
#64390=CARTESIAN_POINT('Ctrl Pts',(-0.873992247862047,83.4270503118526,
10.1298463297532));
#64391=CARTESIAN_POINT('Ctrl Pts',(0.750569308195157,83.6269523778323,9.98560692981242));
#64392=CARTESIAN_POINT('Ctrl Pts',(2.66122369179064,83.8771457597194,10.9699367086606));
#64393=CARTESIAN_POINT('Ctrl Pts',(3.53216814210731,84.1773317949803,13.4021155250038));
#64394=CARTESIAN_POINT('Ctrl Pts',(2.51386301896827,84.4769618827252,15.7686902121962));
#64395=CARTESIAN_POINT('Ctrl Pts',(0.164304520999366,84.7754858579762,16.8030938832357));
#64396=CARTESIAN_POINT('Ctrl Pts',(-2.24721164156027,85.0724162007226,15.9625867670223));
#64397=CARTESIAN_POINT('Ctrl Pts',(-3.47867858274328,85.3797239652224,13.6238161233426));
#64398=CARTESIAN_POINT('Ctrl Pts',(-2.92994214133404,85.5868241148751,11.8975259974901));
#64399=CARTESIAN_POINT('Ctrl Pts',(-2.33977172532943,85.6958993282798,11.2513135886875));
#64400=CARTESIAN_POINT('Ctrl Pts',(2.15580107008468,72.6023598638413,12.0348501216199));
#64401=CARTESIAN_POINT('Ctrl Pts',(2.16192017837505,72.6039627934161,12.0461164217861));
#64402=CARTESIAN_POINT('Ctrl Pts',(2.16794896383192,72.6055628651636,12.0574294127845));
#64403=CARTESIAN_POINT('Ctrl Pts',(2.1738869405785,72.6071602218535,12.0687872536258));
#64404=CARTESIAN_POINT('Ctrl Pts',(2.21802819426934,72.6190345234706,12.1532182568705));
#64405=CARTESIAN_POINT('Ctrl Pts',(2.2571383557657,72.6307519284214,12.2401050802808));
#64406=CARTESIAN_POINT('Ctrl Pts',(2.29106954971183,72.6424358407151,12.3287779317616));
#64407=CARTESIAN_POINT('Ctrl Pts',(2.31366187768963,72.6502153128735,12.3878187703058));
#64408=CARTESIAN_POINT('Ctrl Pts',(2.33395858787518,72.6579798501987,12.4476503642754));
#64409=CARTESIAN_POINT('Ctrl Pts',(2.35192204040781,72.6657647884643,12.5080637449848));
#64410=CARTESIAN_POINT('Ctrl Pts',(2.35913568189839,72.6688910111975,12.5323241408569));
#64411=CARTESIAN_POINT('Ctrl Pts',(2.36597362167121,72.672020934687,12.5566802346146));
#64412=CARTESIAN_POINT('Ctrl Pts',(2.37243396813088,72.6751572074983,12.5811204503354));
#64413=CARTESIAN_POINT('Ctrl Pts',(2.40069571426959,72.6888772992249,12.6880378078779));
#64414=CARTESIAN_POINT('Ctrl Pts',(2.42173598994609,72.7027242333294,12.7965775482791));
#64415=CARTESIAN_POINT('Ctrl Pts',(2.43557776633446,72.7166225538976,12.9058136538946));
#64416=CARTESIAN_POINT('Ctrl Pts',(2.44159629602123,72.7226656695056,12.9533105015584));
#64417=CARTESIAN_POINT('Ctrl Pts',(2.44625339444013,72.7287185409955,13.0009394630651));
#64418=CARTESIAN_POINT('Ctrl Pts',(2.44954849542459,72.7347751585101,13.0486262392927));
#64419=CARTESIAN_POINT('Ctrl Pts',(2.45898976623568,72.7521288500734,13.1852605247354));
#64420=CARTESIAN_POINT('Ctrl Pts',(2.45732387889671,72.7693965007803,13.3223587491889));
#64421=CARTESIAN_POINT('Ctrl Pts',(2.44450040696102,72.7864518110501,13.4579925334706));
#64422=CARTESIAN_POINT('Ctrl Pts',(2.44275221189448,72.7887769231119,13.4764831820038));
#64423=CARTESIAN_POINT('Ctrl Pts',(2.44079668027458,72.7910981002317,13.4949466863257));
#64424=CARTESIAN_POINT('Ctrl Pts',(2.43863370702352,72.7934150333741,13.5133782324569));
#64425=CARTESIAN_POINT('Ctrl Pts',(2.43101421930226,72.8015768743126,13.578306885348));
#64426=CARTESIAN_POINT('Ctrl Pts',(2.42078933591859,72.8097296752927,13.6428321004225));
#64427=CARTESIAN_POINT('Ctrl Pts',(2.4079517140088,72.8178702372941,13.7067146591538));
#64428=CARTESIAN_POINT('Ctrl Pts',(2.40049642993096,72.8225977641444,13.7438136348291));
#64429=CARTESIAN_POINT('Ctrl Pts',(2.39216034593699,72.827321030583,13.7806948458528));
#64430=CARTESIAN_POINT('Ctrl Pts',(2.38294349257466,72.8320393982253,13.8173116957368));
#64431=CARTESIAN_POINT('Ctrl Pts',(2.38179041241278,72.8326296925385,13.8218926694739));
#64432=CARTESIAN_POINT('Ctrl Pts',(2.38062353024195,72.8332199194457,13.8264695779706));
#64433=CARTESIAN_POINT('Ctrl Pts',(2.37944282951223,72.8338100856936,13.8310423918975));
#64434=CARTESIAN_POINT('Ctrl Pts',(2.37505304890306,72.8360042914612,13.8480438634816));
#64435=CARTESIAN_POINT('Ctrl Pts',(2.3704722711849,72.8381976588027,13.8649887411019));
#64436=CARTESIAN_POINT('Ctrl Pts',(2.36570237798596,72.8403905339749,13.8818764406027));
#64437=CARTESIAN_POINT('Ctrl Pts',(2.34233269716483,72.8511343369738,13.9646162694997));
#64438=CARTESIAN_POINT('Ctrl Pts',(2.31455794741775,72.8616876594999,14.045967816978));
#64439=CARTESIAN_POINT('Ctrl Pts',(2.28258923074345,72.8722215415317,14.1254793035469));
#64440=CARTESIAN_POINT('Ctrl Pts',(2.27581984726379,72.874452093597,14.1423158800385));
#64441=CARTESIAN_POINT('Ctrl Pts',(2.26886250892418,72.8766817502705,14.1590697932812));
#64442=CARTESIAN_POINT('Ctrl Pts',(2.26171938489829,72.8789120969552,14.1757365035937));
#64443=CARTESIAN_POINT('Ctrl Pts',(2.21603499722703,72.8931764471494,14.2823297046028));
#64444=CARTESIAN_POINT('Ctrl Pts',(2.16268031957557,72.9075604542274,14.3853643597476));
#64445=CARTESIAN_POINT('Ctrl Pts',(2.10244343550131,72.9220139605729,14.4839797541313));
#64446=CARTESIAN_POINT('Ctrl Pts',(2.09215488785125,72.9244826405359,14.5008234073139));
#64447=CARTESIAN_POINT('Ctrl Pts',(2.08166544187366,72.9269533544155,14.5175381318809));
#64448=CARTESIAN_POINT('Ctrl Pts',(2.07097887523531,72.9294258602769,14.5341196249307));
#64449=CARTESIAN_POINT('Ctrl Pts',(2.0074454631808,72.9441253179249,14.632699352739));
#64450=CARTESIAN_POINT('Ctrl Pts',(1.93694733610837,72.9588863338002,14.7265680673354));
#64451=CARTESIAN_POINT('Ctrl Pts',(1.86035589125161,72.97358065531,14.8147952427477));
#64452=CARTESIAN_POINT('Ctrl Pts',(1.84758283533787,72.9760312082486,14.8295087743537));
#64453=CARTESIAN_POINT('Ctrl Pts',(1.83464024041615,72.9784799230308,14.8440654955037));
#64454=CARTESIAN_POINT('Ctrl Pts',(1.82153205289834,72.9809262250919,14.8584611940775));
#64455=CARTESIAN_POINT('Ctrl Pts',(1.74342569442705,72.9955027441918,14.9442393073152));
#64456=CARTESIAN_POINT('Ctrl Pts',(1.65946718255774,73.0099450409698,15.0243272921312));
#64457=CARTESIAN_POINT('Ctrl Pts',(1.57042581740269,73.0243423290664,15.0976555791592));
#64458=CARTESIAN_POINT('Ctrl Pts',(1.55938921075379,73.0261268615166,15.1067445622263));
#64459=CARTESIAN_POINT('Ctrl Pts',(1.54827457741663,73.0279106956431,15.1157296765225));
#64460=CARTESIAN_POINT('Ctrl Pts',(1.53708343697713,73.0296939954808,15.1246088739482));
#64461=CARTESIAN_POINT('Ctrl Pts',(1.49923675511284,73.0357248358578,15.1546369271208));
#64462=CARTESIAN_POINT('Ctrl Pts',(1.46051578423071,73.0417494318799,15.1834527654948));
#64463=CARTESIAN_POINT('Ctrl Pts',(1.42098929437649,73.0477663904587,15.2109790637862));
#64464=CARTESIAN_POINT('Ctrl Pts',(1.39571046045946,73.0516144856769,15.2285832761871));
#64465=CARTESIAN_POINT('Ctrl Pts',(1.37010340299785,73.0554592777747,15.2456593263385));
#64466=CARTESIAN_POINT('Ctrl Pts',(1.34418259454164,73.0593009687491,15.2621899621411));
#64467=CARTESIAN_POINT('Ctrl Pts',(1.32300331453945,73.0624399236534,15.2756967539863));
#64468=CARTESIAN_POINT('Ctrl Pts',(1.30161062933687,73.0655773917466,15.2888419327909));
#64469=CARTESIAN_POINT('Ctrl Pts',(1.28001612212571,73.068713528788,15.3016244983358));
#64470=CARTESIAN_POINT('Ctrl Pts',(1.25855902645133,73.0718297097634,15.3143257250496));
#64471=CARTESIAN_POINT('Ctrl Pts',(1.23690409112748,73.074944365242,15.3266680187035));
#64472=CARTESIAN_POINT('Ctrl Pts',(1.21507475280123,73.0780375247887,15.3386641411617));
#64473=CARTESIAN_POINT('Ctrl Pts',(1.10130146538182,73.0941588989175,15.4011872588099));
#64474=CARTESIAN_POINT('Ctrl Pts',(0.98254969375926,73.1101790706159,15.453953177252));
#64475=CARTESIAN_POINT('Ctrl Pts',(0.860533429664269,73.1261844231029,15.4967042795224));
#64476=CARTESIAN_POINT('Ctrl Pts',(0.840874461480389,73.1287631671551,15.5035922347109));
#64477=CARTESIAN_POINT('Ctrl Pts',(0.821130823890476,73.1313415135199,15.5102201352121));
#64478=CARTESIAN_POINT('Ctrl Pts',(0.801309776798585,73.1339198083819,15.5165868159723));
#64479=CARTESIAN_POINT('Ctrl Pts',(0.653862888784499,73.1530994991431,15.5639479498577));
#64480=CARTESIAN_POINT('Ctrl Pts',(0.502131670630755,73.1722760403049,15.596854524438));
#64481=CARTESIAN_POINT('Ctrl Pts',(0.349169946951665,73.191436916284,15.6149530377744));
#64482=CARTESIAN_POINT('Ctrl Pts',(0.197225453902707,73.2104703680325,15.632931191836));
#64483=CARTESIAN_POINT('Ctrl Pts',(0.0440672956689506,73.2294879697,15.6362965414167));
#64484=CARTESIAN_POINT('Ctrl Pts',(-0.107296279315945,73.2484596733022,
15.6247246061563));
#64485=CARTESIAN_POINT('Ctrl Pts',(-0.169382485558562,73.2562414735321,
15.6199780377743));
#64486=CARTESIAN_POINT('Ctrl Pts',(-0.231166633660567,73.2640153744315,
15.6127186623935));
#64487=CARTESIAN_POINT('Ctrl Pts',(-0.292440818079412,73.2717786369157,
15.6029258396425));
#64488=CARTESIAN_POINT('Ctrl Pts',(-0.310486323983427,73.2740649504802,
15.6000418120141));
#64489=CARTESIAN_POINT('Ctrl Pts',(-0.328487611692874,73.2763503415797,
15.5969380586081));
#64490=CARTESIAN_POINT('Ctrl Pts',(-0.346440106727422,73.2786330779197,
15.5936157835197));
#64491=CARTESIAN_POINT('Ctrl Pts',(-0.346450065622348,73.2786343442357,
15.5936139405341));
#64492=CARTESIAN_POINT('Ctrl Pts',(-0.346460024503054,73.2786356105509,
15.5936120974813));
#64493=CARTESIAN_POINT('Ctrl Pts',(-0.346469983369502,73.2786368768654,
15.593610254361));
#64494=CARTESIAN_POINT('Ctrl Pts',(-0.457116323583858,73.2927060544194,
15.5731325717345));
#64495=CARTESIAN_POINT('Ctrl Pts',(-0.566006383550437,73.306681464898,15.5443376672788));
#64496=CARTESIAN_POINT('Ctrl Pts',(-0.672080024035714,73.3205943231013,
15.5078791483193));
#64497=CARTESIAN_POINT('Ctrl Pts',(-0.710542744613808,73.3256391803822,
15.494659145489));
#64498=CARTESIAN_POINT('Ctrl Pts',(-0.748635013790737,73.3306757873652,
15.4804320013116));
#64499=CARTESIAN_POINT('Ctrl Pts',(-0.786305931834455,73.3357055426912,
15.4652305097075));
#64500=CARTESIAN_POINT('Ctrl Pts',(-0.906109752180169,73.351701539995,15.4168856096176));
#64501=CARTESIAN_POINT('Ctrl Pts',(-1.02165254345175,73.3676303883617,15.3586820909752));
#64502=CARTESIAN_POINT('Ctrl Pts',(-1.13135734234018,73.3835579983143,15.2916599425043));
#64503=CARTESIAN_POINT('Ctrl Pts',(-1.15422573328892,73.386878170403,15.2776889156305));
#64504=CARTESIAN_POINT('Ctrl Pts',(-1.17684034207221,73.3901982654702,15.2633348389487));
#64505=CARTESIAN_POINT('Ctrl Pts',(-1.19918673917259,73.3935188435732,15.2486073777911));
#64506=CARTESIAN_POINT('Ctrl Pts',(-1.30762698986721,73.4096325965118,15.1771394998663));
#64507=CARTESIAN_POINT('Ctrl Pts',(-1.40975438516136,73.4257600997185,15.0968766406711));
#64508=CARTESIAN_POINT('Ctrl Pts',(-1.50398226142444,73.4419645783231,15.0088841574503));
#64509=CARTESIAN_POINT('Ctrl Pts',(-1.51950548048396,73.4446341245456,14.9943881648969));
#64510=CARTESIAN_POINT('Ctrl Pts',(-1.53481419809293,73.447305745063,14.9796824189891));
#64511=CARTESIAN_POINT('Ctrl Pts',(-1.54990119041512,73.4499797049384,14.9647717256329));
#64512=CARTESIAN_POINT('Ctrl Pts',(-1.57165429876864,73.4538351413076,14.9432728131076));
#64513=CARTESIAN_POINT('Ctrl Pts',(-1.59294695284777,73.4576953883003,14.9213475693769));
#64514=CARTESIAN_POINT('Ctrl Pts',(-1.61375807842776,73.4615611018664,14.8990099929552));
#64515=CARTESIAN_POINT('Ctrl Pts',(-1.66414575427112,73.470920726425,14.8449264905739));
#64516=CARTESIAN_POINT('Ctrl Pts',(-1.71171359747127,73.480313309835,14.7884222347898));
#64517=CARTESIAN_POINT('Ctrl Pts',(-1.7562799676571,73.4896314192762,14.7297818120333));
#64518=CARTESIAN_POINT('Ctrl Pts',(-1.76228567573715,73.4908871160028,14.7218795023029));
#64519=CARTESIAN_POINT('Ctrl Pts',(-1.76823692368156,73.4921414701709,14.7139383385766));
#64520=CARTESIAN_POINT('Ctrl Pts',(-1.77413330815155,73.4933942281411,14.7059589578865));
#64521=CARTESIAN_POINT('Ctrl Pts',(-1.77414438921039,73.4933965824456,14.7059439622587));
#64522=CARTESIAN_POINT('Ctrl Pts',(-1.77415547007825,73.4933989367447,14.7059289664928));
#64523=CARTESIAN_POINT('Ctrl Pts',(-1.77416655075512,73.4934012910384,14.705913970589));
#64524=CARTESIAN_POINT('Ctrl Pts',(-1.82681983952755,73.5045884508566,14.6346562609334));
#64525=CARTESIAN_POINT('Ctrl Pts',(-1.87515911625464,73.5156527416839,14.5602781537274));
#64526=CARTESIAN_POINT('Ctrl Pts',(-1.91895260074508,73.5266327185297,14.4833995315359));
#64527=CARTESIAN_POINT('Ctrl Pts',(-1.93911324416827,73.531687429306,14.4480079086289));
#64528=CARTESIAN_POINT('Ctrl Pts',(-1.9583107599767,73.5367242273436,14.4120870492267));
#64529=CARTESIAN_POINT('Ctrl Pts',(-1.97652406882038,73.5417466436806,14.3757007775802));
#64530=CARTESIAN_POINT('Ctrl Pts',(-2.02030622038373,73.553819803762,14.2882334604812));
#64531=CARTESIAN_POINT('Ctrl Pts',(-2.05839898090737,73.5658119149367,14.1980736548514));
#64532=CARTESIAN_POINT('Ctrl Pts',(-2.09053924690994,73.5777931504987,14.1060587105315));
#64533=CARTESIAN_POINT('Ctrl Pts',(-2.10172875730914,73.5819643717296,14.0740240604056));
#64534=CARTESIAN_POINT('Ctrl Pts',(-2.1121967939929,73.5861342171208,14.0417650171957));
#64535=CARTESIAN_POINT('Ctrl Pts',(-2.12193239364035,73.5903054616774,14.0093183825834));
#64536=CARTESIAN_POINT('Ctrl Pts',(-2.1505626523661,73.6025721750993,13.9138999618008));
#64537=CARTESIAN_POINT('Ctrl Pts',(-2.17285889501759,73.6148532268291,13.8168552171571));
#64538=CARTESIAN_POINT('Ctrl Pts',(-2.18856600348633,73.6272217037332,13.7190552747927));
#64539=CARTESIAN_POINT('Ctrl Pts',(-2.19327238703961,73.6309277197957,13.6897510880182));
#64540=CARTESIAN_POINT('Ctrl Pts',(-2.19738702241765,73.6346415366831,13.6603794056819));
#64541=CARTESIAN_POINT('Ctrl Pts',(-2.20090267875922,73.6383649959301,13.6309644939029));
#64542=CARTESIAN_POINT('Ctrl Pts',(-2.20373076100735,73.6413602400537,13.6073024001856));
#64543=CARTESIAN_POINT('Ctrl Pts',(-2.20617146824096,73.6443616997158,13.5836117511436));
#64544=CARTESIAN_POINT('Ctrl Pts',(-2.20822122713813,73.6473702483784,13.5599045428459));
#64545=CARTESIAN_POINT('Ctrl Pts',(-2.21452692848637,73.656625487804,13.4869737335044));
#64546=CARTESIAN_POINT('Ctrl Pts',(-2.21713216075013,73.665950917194,13.4138715163576));
#64547=CARTESIAN_POINT('Ctrl Pts',(-2.21609970788283,73.6752549137358,13.340961115631));
#64548=CARTESIAN_POINT('Ctrl Pts',(-2.21529108434837,73.6825418619409,13.2838572343777));
#64549=CARTESIAN_POINT('Ctrl Pts',(-2.21225139475122,73.6898157910752,13.2268700014323));
#64550=CARTESIAN_POINT('Ctrl Pts',(-2.20700918463086,73.6970355538379,13.1701517901074));
#64551=CARTESIAN_POINT('Ctrl Pts',(-2.20551912316951,73.6990877207686,13.1540300363218));
#64552=CARTESIAN_POINT('Ctrl Pts',(-2.20385120819904,73.7011353779884,13.1379308463664));
#64553=CARTESIAN_POINT('Ctrl Pts',(-2.20200878525503,73.7031758546802,13.1218581211112));
#64554=CARTESIAN_POINT('Ctrl Pts',(-2.2020038117226,73.7031813628492,13.1218147335597));
#64555=CARTESIAN_POINT('Ctrl Pts',(-2.20199883689239,73.7031868709847,13.1217713461652));
#64556=CARTESIAN_POINT('Ctrl Pts',(-2.20199386076437,73.7031923790868,13.1217279589276));
#64557=CARTESIAN_POINT('Ctrl Pts',(-2.19276919631323,73.7134032081921,13.0412974100706));
#64558=CARTESIAN_POINT('Ctrl Pts',(-2.17908064415196,73.723499157845,12.9614044145176));
#64559=CARTESIAN_POINT('Ctrl Pts',(-2.16110800790781,73.7335132188269,12.8825566075815));
#64560=CARTESIAN_POINT('Ctrl Pts',(-2.15188713482429,73.7386509395324,12.8421036873312));
#64561=CARTESIAN_POINT('Ctrl Pts',(-2.1415393667158,73.74376705314,12.8019262799138));
#64562=CARTESIAN_POINT('Ctrl Pts',(-2.13009387019467,73.7488656773271,12.7620949609708));
#64563=CARTESIAN_POINT('Ctrl Pts',(-2.10664860637749,73.7593098366477,12.6805034127946));
#64564=CARTESIAN_POINT('Ctrl Pts',(-2.07858308300931,73.7696893584977,12.6003650885137));
#64565=CARTESIAN_POINT('Ctrl Pts',(-2.04611071225278,73.7800714069487,12.5222386907462));
#64566=CARTESIAN_POINT('Ctrl Pts',(-2.03095970140821,73.7849154797713,12.485786350734));
#64567=CARTESIAN_POINT('Ctrl Pts',(-2.01484971883731,73.7897600075159,12.4497726276748));
#64568=CARTESIAN_POINT('Ctrl Pts',(-1.9978048528833,73.794611309703,12.4142572843166));
#64569=CARTESIAN_POINT('Ctrl Pts',(-1.96095408042119,73.8050997602148,12.3374735864842));
#64570=CARTESIAN_POINT('Ctrl Pts',(-1.91972962868822,73.8156218527174,12.263011969038));
#64571=CARTESIAN_POINT('Ctrl Pts',(-1.87435580531654,73.8262430152286,12.1914288817111));
#64572=CARTESIAN_POINT('Ctrl Pts',(-1.86946470236314,73.8273879308533,12.1837125328601));
#64573=CARTESIAN_POINT('Ctrl Pts',(-1.86452539796778,73.8285339911167,12.1760296798575));
#64574=CARTESIAN_POINT('Ctrl Pts',(-1.85953818476383,73.8296812732155,12.1683810538582));
#64575=CARTESIAN_POINT('Ctrl Pts',(-1.81930052417095,73.8389377348526,12.1066706748604));
#64576=CARTESIAN_POINT('Ctrl Pts',(-1.77593483395429,73.8482765385491,12.0471757256674));
#64577=CARTESIAN_POINT('Ctrl Pts',(-1.72974674754801,73.8576244811704,11.990142400919));
#64578=CARTESIAN_POINT('Ctrl Pts',(-1.69842882972124,73.8639628710377,11.9514708490789));
#64579=CARTESIAN_POINT('Ctrl Pts',(-1.66581268519627,73.8703055972869,11.9139301370438));
#64580=CARTESIAN_POINT('Ctrl Pts',(-1.63198357026612,73.8766315687028,11.8775879042256));
#64581=CARTESIAN_POINT('Ctrl Pts',(-1.58621468770642,73.8851902508736,11.8284189150501));
#64582=CARTESIAN_POINT('Ctrl Pts',(-1.53837185948978,73.8936192613437,11.7813332420409));
#64583=CARTESIAN_POINT('Ctrl Pts',(-1.48849343993653,73.901996996571,11.736671370713));
#64584=CARTESIAN_POINT('Ctrl Pts',(-1.47682194376587,73.9039573775433,11.726220541179));
#64585=CARTESIAN_POINT('Ctrl Pts',(-1.4650391333866,73.9059149229783,11.7159025973676));
#64586=CARTESIAN_POINT('Ctrl Pts',(-1.45314578222703,73.9078705859488,11.7057221988261));
#64587=CARTESIAN_POINT('Ctrl Pts',(-1.45308771947485,73.9078801333987,11.7056724986239));
#64588=CARTESIAN_POINT('Ctrl Pts',(-1.45302965393809,73.9078896808523,11.705622801649));
#64589=CARTESIAN_POINT('Ctrl Pts',(-1.45297158561719,73.9078992283094,11.7055731079019));
#64590=CARTESIAN_POINT('Ctrl Pts',(-1.40195888298438,73.9162866172158,11.6619174226086));
#64591=CARTESIAN_POINT('Ctrl Pts',(-1.34879776939936,73.924676340523,11.6207571729945));
#64592=CARTESIAN_POINT('Ctrl Pts',(-1.29389435594591,73.9330056935469,11.5821578726855));
#64593=CARTESIAN_POINT('Ctrl Pts',(-1.25845225271705,73.9383825867333,11.557240653517));
#64594=CARTESIAN_POINT('Ctrl Pts',(-1.22228411112995,73.9437344221045,11.5333895253827));
#64595=CARTESIAN_POINT('Ctrl Pts',(-1.18549692114481,73.9490454273909,11.5106108692279));
#64596=CARTESIAN_POINT('Ctrl Pts',(-1.12270205757729,73.95811118785,11.4717282417135));
#64597=CARTESIAN_POINT('Ctrl Pts',(-1.05801534278977,73.9671275808998,11.4360770145799));
#64598=CARTESIAN_POINT('Ctrl Pts',(-0.991780224657834,73.9761565253841,
11.4038822871771));
#64599=CARTESIAN_POINT('Ctrl Pts',(-0.957465927451193,73.9808341328714,
11.3872032281561));
#64600=CARTESIAN_POINT('Ctrl Pts',(-0.922736814478702,73.9855149989163,
11.3714522399752));
#64601=CARTESIAN_POINT('Ctrl Pts',(-0.887645822571864,73.9902070189536,
11.3566623625175));
#64602=CARTESIAN_POINT('Ctrl Pts',(-0.842566350883857,73.9962345996214,
11.3376626185407));
#64603=CARTESIAN_POINT('Ctrl Pts',(-0.796885996201166,74.0022810870724,
11.3202472120307));
#64604=CARTESIAN_POINT('Ctrl Pts',(-0.750710375381237,74.0083616693734,
11.3044781595841));
#64605=CARTESIAN_POINT('Ctrl Pts',(-0.679517172795227,74.0177366624956,
11.280165560739));
#64606=CARTESIAN_POINT('Ctrl Pts',(-0.607139682664314,74.0271948678836,
11.2597667286002));
#64607=CARTESIAN_POINT('Ctrl Pts',(-0.534019870815996,74.0366803874199,
11.243273778465));
#64608=CARTESIAN_POINT('Ctrl Pts',(-0.498490175439331,74.0412895023929,
11.2352596783278));
#64609=CARTESIAN_POINT('Ctrl Pts',(-0.462784429619876,74.0459051630657,
11.2281677067626));
#64610=CARTESIAN_POINT('Ctrl Pts',(-0.426948933582017,74.05052150681,11.221996981732));
#64611=CARTESIAN_POINT('Ctrl Pts',(-0.355656275019391,74.0597054572156,
11.2097206791457));
#64612=CARTESIAN_POINT('Ctrl Pts',(-0.283869348663841,74.0688646074762,
11.2010327111927));
#64613=CARTESIAN_POINT('Ctrl Pts',(-0.211981529695926,74.0779444575951,
11.1959149698796));
#64614=CARTESIAN_POINT('Ctrl Pts',(-0.17470091938458,74.0826532157524,11.1932609386083));
#64615=CARTESIAN_POINT('Ctrl Pts',(-0.137392377266259,74.0873407536378,
11.1915668031196));
#64616=CARTESIAN_POINT('Ctrl Pts',(-0.100105390170106,74.0920001644583,
11.1908289012013));
#64617=CARTESIAN_POINT('Ctrl Pts',(-0.0578756745461771,74.0972772224683,
11.1899931836871));
#64618=CARTESIAN_POINT('Ctrl Pts',(-0.0156664371984247,74.102550467867,
11.1904616056632));
#64619=CARTESIAN_POINT('Ctrl Pts',(0.0264309564992198,74.1078180194713,
11.1922550027768));
#64620=CARTESIAN_POINT('Ctrl Pts',(0.0265158087497896,74.1078286368414,
11.1922586175798));
#64621=CARTESIAN_POINT('Ctrl Pts',(0.0266006607436696,74.1078392541547,
11.192262237628));
#64622=CARTESIAN_POINT('Ctrl Pts',(0.0266855124800557,74.107849871411,11.1922658629217));
#64623=CARTESIAN_POINT('Ctrl Pts',(0.101313419299133,74.1171878490496,11.1954543431238));
#64624=CARTESIAN_POINT('Ctrl Pts',(0.175740356384215,74.1264815954097,11.2027045332465));
#64625=CARTESIAN_POINT('Ctrl Pts',(0.249507613526737,74.1357024290768,11.2137816289139));
#64626=CARTESIAN_POINT('Ctrl Pts',(0.291954329481528,74.1410082262921,11.2201555453589));
#64627=CARTESIAN_POINT('Ctrl Pts',(0.334183004514007,74.1462899310993,11.2277956156468));
#64628=CARTESIAN_POINT('Ctrl Pts',(0.376110260413564,74.151542474569,11.2366504666802));
#64629=CARTESIAN_POINT('Ctrl Pts',(0.443050390905403,74.159928569431,11.2507879262144));
#64630=CARTESIAN_POINT('Ctrl Pts',(0.5092165201533,74.1683035555664,11.2681827010546));
#64631=CARTESIAN_POINT('Ctrl Pts',(0.574267704063896,74.1767163627487,11.2888025522495));
#64632=CARTESIAN_POINT('Ctrl Pts',(0.592177927910872,74.1790326197445,11.2944797148835));
#64633=CARTESIAN_POINT('Ctrl Pts',(0.610003344532317,74.1813517045966,11.3004012665055));
#64634=CARTESIAN_POINT('Ctrl Pts',(0.627736187584336,74.1836745492012,11.3065663057738));
#64635=CARTESIAN_POINT('Ctrl Pts',(0.704214690597216,74.1936925523816,11.3331549905588));
#64636=CARTESIAN_POINT('Ctrl Pts',(0.778985410996104,74.203783708351,11.3642799566572));
#64637=CARTESIAN_POINT('Ctrl Pts',(0.851609159976651,74.2139085837343,11.3995796397699));
#64638=CARTESIAN_POINT('Ctrl Pts',(0.884238568050055,74.2184576285744,11.4154395723858));
#64639=CARTESIAN_POINT('Ctrl Pts',(0.916435142903122,74.2230135643075,11.4321426550204));
#64640=CARTESIAN_POINT('Ctrl Pts',(0.948161545368537,74.2275732271854,11.4496583945888));
#64641=CARTESIAN_POINT('Ctrl Pts',(1.01668234420536,74.2374209161302,11.4874878481095));
#64642=CARTESIAN_POINT('Ctrl Pts',(1.08300862473964,74.2472846895342,11.5291051564584));
#64643=CARTESIAN_POINT('Ctrl Pts',(1.14673563186435,74.2571223825849,11.574167656761));
#64644=CARTESIAN_POINT('Ctrl Pts',(1.17864519414785,74.262048339307,11.5967314758532));
#64645=CARTESIAN_POINT('Ctrl Pts',(1.20990383371369,74.2669678611424,11.6201593300922));
#64646=CARTESIAN_POINT('Ctrl Pts',(1.24046515772503,74.2718762846754,11.6444102687014));
#64647=CARTESIAN_POINT('Ctrl Pts',(1.2990789038412,74.2812901795278,11.690921288911));
#64648=CARTESIAN_POINT('Ctrl Pts',(1.35512147007713,74.2906619910334,11.7404559421409));
#64649=CARTESIAN_POINT('Ctrl Pts',(1.40824761554792,74.299957959209,11.7927028910783));
#64650=CARTESIAN_POINT('Ctrl Pts',(1.41481470112055,74.3011070623097,11.7991612964744));
#64651=CARTESIAN_POINT('Ctrl Pts',(1.42133728667879,74.3022550132775,11.8056611609397));
#64652=CARTESIAN_POINT('Ctrl Pts',(1.42781477355712,74.3034017540735,11.8122019108332));
#64653=CARTESIAN_POINT('Ctrl Pts',(1.42784095932973,74.3034063898673,11.8122283523517));
#64654=CARTESIAN_POINT('Ctrl Pts',(1.42786714438612,74.303411025645,11.8122547945592));
#64655=CARTESIAN_POINT('Ctrl Pts',(1.4278933287262,74.3034156614065,11.8122812374555));
#64656=CARTESIAN_POINT('Ctrl Pts',(1.47479074149944,74.3117185332416,11.8596417368433));
#64657=CARTESIAN_POINT('Ctrl Pts',(1.51939244327982,74.3199700398038,11.9092158068034));
#64658=CARTESIAN_POINT('Ctrl Pts',(1.56144817870571,74.3282053919733,11.9607895161716));
#64659=CARTESIAN_POINT('Ctrl Pts',(1.58736784102869,74.3332809790527,11.9925752671049));
#64660=CARTESIAN_POINT('Ctrl Pts',(1.61231989656539,74.3383503093373,12.0251196975741));
#64661=CARTESIAN_POINT('Ctrl Pts',(1.63624194944416,74.3434204545349,12.0583636868686));
#64662=CARTESIAN_POINT('Ctrl Pts',(1.65582144490069,74.3475702189954,12.0855729126256));
#64663=CARTESIAN_POINT('Ctrl Pts',(1.67471225449499,74.3517209114023,12.113252850473));
#64664=CARTESIAN_POINT('Ctrl Pts',(1.69288239112283,74.3558768547122,12.1413737924115));
#64665=CARTESIAN_POINT('Ctrl Pts',(1.73572447055419,74.365675859367,12.2076781715634));
#64666=CARTESIAN_POINT('Ctrl Pts',(1.77455982308679,74.3755054254738,12.2764389500244));
#64667=CARTESIAN_POINT('Ctrl Pts',(1.80926351293272,74.385335506677,12.3471105565211));
#64668=CARTESIAN_POINT('Ctrl Pts',(1.82146603669404,74.3887919633244,12.3719601319223));
#64669=CARTESIAN_POINT('Ctrl Pts',(1.83315791100867,74.392248542058,12.3970463909998));
#64670=CARTESIAN_POINT('Ctrl Pts',(1.84433416221169,74.3957041270959,12.4223470642232));
#64671=CARTESIAN_POINT('Ctrl Pts',(1.87484008529833,74.4051362532598,12.4914060337626));
#64672=CARTESIAN_POINT('Ctrl Pts',(1.90150357679853,74.4145597466018,12.5620571447373));
#64673=CARTESIAN_POINT('Ctrl Pts',(1.92422782173927,74.4239450681702,12.6338132953026));
#64674=CARTESIAN_POINT('Ctrl Pts',(1.92908398492622,74.4259507081031,12.649147559553));
#64675=CARTESIAN_POINT('Ctrl Pts',(1.93376035428528,74.427954627965,12.6645324463498));
#64676=CARTESIAN_POINT('Ctrl Pts',(1.93825613759087,74.4299565772684,12.6799634688133));
#64677=CARTESIAN_POINT('Ctrl Pts',(1.9393309096904,74.4304351677853,12.6836524438559));
#64678=CARTESIAN_POINT('Ctrl Pts',(1.9403954060336,74.4309136531687,12.6873441413251));
#64679=CARTESIAN_POINT('Ctrl Pts',(1.94144959634439,74.4313920380659,12.6910385265463));
#64680=CARTESIAN_POINT('Ctrl Pts',(1.94753699656449,74.4341544617941,12.7123716778554));
#64681=CARTESIAN_POINT('Ctrl Pts',(1.95328078631335,74.4369135371217,12.7337944611126));
#64682=CARTESIAN_POINT('Ctrl Pts',(1.95868003122727,74.4396701426473,12.7552996071111));
#64683=CARTESIAN_POINT('Ctrl Pts',(1.97787033392747,74.4494678264541,12.8317344175158));
#64684=CARTESIAN_POINT('Ctrl Pts',(1.9927007065785,74.45923013598,12.9091803746465));
#64685=CARTESIAN_POINT('Ctrl Pts',(2.00305822928529,74.4689777601459,12.9871152481655));
#64686=CARTESIAN_POINT('Ctrl Pts',(2.01052114765116,74.4760012275784,13.0432697568634));
#64687=CARTESIAN_POINT('Ctrl Pts',(2.01566185350558,74.4830169451425,13.0996769724923));
#64688=CARTESIAN_POINT('Ctrl Pts',(2.01844171971378,74.4900306880044,13.1561252536584));
#64689=CARTESIAN_POINT('Ctrl Pts',(2.0223428691589,74.4998734851121,13.2353424404779));
#64690=CARTESIAN_POINT('Ctrl Pts',(2.02159300613646,74.5097140822882,13.3146491714498));
#64691=CARTESIAN_POINT('Ctrl Pts',(2.01608782135885,74.5195725971845,13.3934914521823));
#64692=CARTESIAN_POINT('Ctrl Pts',(2.01518934110372,74.5211815678798,13.4063590007513));
#64693=CARTESIAN_POINT('Ctrl Pts',(2.01416419210897,74.5227910014299,13.4192140663617));
#64694=CARTESIAN_POINT('Ctrl Pts',(2.01301192188643,74.5244009684201,13.4320541093707));
#64695=CARTESIAN_POINT('Ctrl Pts',(2.00708142438712,74.5326871369099,13.4981391660412));
#64696=CARTESIAN_POINT('Ctrl Pts',(1.99778796228407,74.5409879174046,13.5638386790392));
#64697=CARTESIAN_POINT('Ctrl Pts',(1.9852685667007,74.5492782813175,13.6288398715573));
#64698=CARTESIAN_POINT('Ctrl Pts',(1.98094021513431,74.5521445226938,13.6513128425229));
#64699=CARTESIAN_POINT('Ctrl Pts',(1.97622622120035,74.5550095766191,13.6737027951074));
#64700=CARTESIAN_POINT('Ctrl Pts',(1.9711320027107,74.5578725918486,13.6959982219969));
#64701=CARTESIAN_POINT('Ctrl Pts',(1.96718807432242,74.5600891294907,13.7132592733665));
#64702=CARTESIAN_POINT('Ctrl Pts',(1.9630162436556,74.5623044470594,13.7304636824044));
#64703=CARTESIAN_POINT('Ctrl Pts',(1.95862195803157,74.5645181885269,13.747607152374));
#64704=CARTESIAN_POINT('Ctrl Pts',(1.93049173004795,74.5786895596001,13.857351889047));
#64705=CARTESIAN_POINT('Ctrl Pts',(1.89317217966602,74.5928057813007,13.9645512450797));
#64706=CARTESIAN_POINT('Ctrl Pts',(1.8473907998134,74.6068822020894,14.0677907233878));
#64707=CARTESIAN_POINT('Ctrl Pts',(1.83888623714562,74.6094971036743,14.0869689704369));
#64708=CARTESIAN_POINT('Ctrl Pts',(1.83008973864687,74.6121106136852,14.1060104417081));
#64709=CARTESIAN_POINT('Ctrl Pts',(1.82100607332705,74.6147228056702,14.1249059048358));
#64710=CARTESIAN_POINT('Ctrl Pts',(1.77579474554523,74.6277242388917,14.218952630136));
#64711=CARTESIAN_POINT('Ctrl Pts',(1.72346712437599,74.6406937697442,14.3093851165373));
#64712=CARTESIAN_POINT('Ctrl Pts',(1.66457756792296,74.6536459079467,14.3950771829617));
#64713=CARTESIAN_POINT('Ctrl Pts',(1.64931634734291,74.6570024528079,14.4172842703712));
#64714=CARTESIAN_POINT('Ctrl Pts',(1.63361449454355,74.6603577968262,14.4391727328735));
#64715=CARTESIAN_POINT('Ctrl Pts',(1.61748182560175,74.6637121236636,14.4607224276072));
#64716=CARTESIAN_POINT('Ctrl Pts',(1.58627959143489,74.6701997353432,14.5024017445093));
#64717=CARTESIAN_POINT('Ctrl Pts',(1.55346490905361,74.6766837372837,14.5428150216422));
#64718=CARTESIAN_POINT('Ctrl Pts',(1.51910631662569,74.683165766496,14.5818178250006));
#64719=CARTESIAN_POINT('Ctrl Pts',(1.519028822493,74.6831803863973,14.581905793925));
#64720=CARTESIAN_POINT('Ctrl Pts',(1.51895132050671,74.6831950062885,14.5819937556725));
#64721=CARTESIAN_POINT('Ctrl Pts',(1.51887381066809,74.6832096261694,14.5820817102422));
#64722=CARTESIAN_POINT('Ctrl Pts',(1.50558108259855,74.6857168962855,14.5971656814981));
#64723=CARTESIAN_POINT('Ctrl Pts',(1.4920601355563,74.6882233561188,14.6120355654605));
#64724=CARTESIAN_POINT('Ctrl Pts',(1.47831532366195,74.6907294675882,14.6266831059059));
#64725=CARTESIAN_POINT('Ctrl Pts',(1.41866624898481,74.7016053698074,14.6902497986028));
#64726=CARTESIAN_POINT('Ctrl Pts',(1.35479218909004,74.7124763142226,14.7496347287381));
#64727=CARTESIAN_POINT('Ctrl Pts',(1.28740183232951,74.7233337414734,14.8045175217916));
#64728=CARTESIAN_POINT('Ctrl Pts',(1.22693477957409,74.7330757380724,14.8537619671761));
#64729=CARTESIAN_POINT('Ctrl Pts',(1.16363647191518,74.7428069340349,14.8993827722767));
#64730=CARTESIAN_POINT('Ctrl Pts',(1.09798669092278,74.7525254754109,14.9411636149424));
#64731=CARTESIAN_POINT('Ctrl Pts',(1.02420938336678,74.7634471845964,14.9881169791836));
#64732=CARTESIAN_POINT('Ctrl Pts',(0.947467312276564,74.7743520707771,15.0302211078564));
#64733=CARTESIAN_POINT('Ctrl Pts',(0.868473044750292,74.7852330922427,15.067141180662));
#64734=CARTESIAN_POINT('Ctrl Pts',(0.815124851004688,74.7925815095327,15.0920748784961));
#64735=CARTESIAN_POINT('Ctrl Pts',(0.760748902071486,74.7999191685314,15.1146451328699));
#64736=CARTESIAN_POINT('Ctrl Pts',(0.705554870479162,74.8072454720367,15.1347579546826));
#64737=CARTESIAN_POINT('Ctrl Pts',(0.705512057820929,74.8072511548709,15.1347735557058));
#64738=CARTESIAN_POINT('Ctrl Pts',(0.705469244669996,74.8072568376982,15.1347891552507));
#64739=CARTESIAN_POINT('Ctrl Pts',(0.705426431026517,74.8072625205189,15.1348047533174));
#64740=CARTESIAN_POINT('Ctrl Pts',(0.645100516539383,74.8152698126569,15.156782972391));
#64741=CARTESIAN_POINT('Ctrl Pts',(0.583741977736648,74.8232708914926,15.1758472221042));
#64742=CARTESIAN_POINT('Ctrl Pts',(0.521641228908294,74.8312665354659,15.1918447534929));
#64743=CARTESIAN_POINT('Ctrl Pts',(0.488248291436797,74.8355659689555,15.2004469777082));
#64744=CARTESIAN_POINT('Ctrl Pts',(0.45464163788152,74.8398637245999,15.2081623978426));
#64745=CARTESIAN_POINT('Ctrl Pts',(0.420872611953215,74.8441591806084,15.2149674285766));
#64746=CARTESIAN_POINT('Ctrl Pts',(0.393277639352099,74.8476692904681,15.2205282829836));
#64747=CARTESIAN_POINT('Ctrl Pts',(0.365572672690947,74.8511780646081,15.2254814472713));
#64748=CARTESIAN_POINT('Ctrl Pts',(0.337783856362672,74.8546854022102,15.2298146768192));
#64749=CARTESIAN_POINT('Ctrl Pts',(0.265257556785499,74.8638392364234,15.2411240143821));
#64750=CARTESIAN_POINT('Ctrl Pts',(0.192156085109537,74.8729837677774,15.2482080863385));
#64751=CARTESIAN_POINT('Ctrl Pts',(0.118967764499052,74.8821167241471,15.2511597356922));
#64752=CARTESIAN_POINT('Ctrl Pts',(0.0915763247955409,74.8855348217565,
15.2522644191256));
#64753=CARTESIAN_POINT('Ctrl Pts',(0.0641721975875338,74.8889513631873,
15.2527902925941));
#64754=CARTESIAN_POINT('Ctrl Pts',(0.0367791242492394,74.892366462911,15.252742140314));
#64755=CARTESIAN_POINT('Ctrl Pts',(-0.0333491909333243,74.901109373458,
15.2526188668781));
#64756=CARTESIAN_POINT('Ctrl Pts',(-0.103401965497628,74.9098424726392,
15.2487346624949));
#64757=CARTESIAN_POINT('Ctrl Pts',(-0.172949517403085,74.9185639227761,
15.2411882329299));
#64758=CARTESIAN_POINT('Ctrl Pts',(-0.203152651108026,74.9223514770087,
15.2379109670176));
#64759=CARTESIAN_POINT('Ctrl Pts',(-0.233261142036416,74.9261369134886,
15.2339431705582));
#64760=CARTESIAN_POINT('Ctrl Pts',(-0.263242806676454,74.9299204465575,
15.2292933908425));
#64761=CARTESIAN_POINT('Ctrl Pts',(-0.26324487004777,74.9299207069445,15.2292930708395));
#64762=CARTESIAN_POINT('Ctrl Pts',(-0.263246933418519,74.9299209673314,
15.2292927508333));
#64763=CARTESIAN_POINT('Ctrl Pts',(-0.263248996788635,74.9299212277183,
15.2292924308239));
#64764=CARTESIAN_POINT('Ctrl Pts',(-0.343335449250516,74.9400277344896,
15.216871769703));
#64765=CARTESIAN_POINT('Ctrl Pts',(-0.422566406385879,74.9501267421625,
15.1995584594227));
#64766=CARTESIAN_POINT('Ctrl Pts',(-0.500372848947576,74.9602178008868,
15.1774906759502));
#64767=CARTESIAN_POINT('Ctrl Pts',(-0.533467373120428,74.9645099748493,
15.168104270795));
#64768=CARTESIAN_POINT('Ctrl Pts',(-0.566303544687431,74.968800630062,15.1578578177866));
#64769=CARTESIAN_POINT('Ctrl Pts',(-0.598834860827465,74.9730893735596,
15.1467627706444));
#64770=CARTESIAN_POINT('Ctrl Pts',(-0.643694027475191,74.9790033506775,
15.1314632184661));
#64771=CARTESIAN_POINT('Ctrl Pts',(-0.68797634563979,74.9849140526127,15.1145487039482));
#64772=CARTESIAN_POINT('Ctrl Pts',(-0.731565348541546,74.9908212280144,
15.0960452135253));
#64773=CARTESIAN_POINT('Ctrl Pts',(-0.731573386736688,74.9908223173495,
15.0960418013191));
#64774=CARTESIAN_POINT('Ctrl Pts',(-0.731581424908254,74.9908234066844,
15.0960383890588));
#64775=CARTESIAN_POINT('Ctrl Pts',(-0.731589463056202,74.9908244960192,
15.0960349767445));
#64776=CARTESIAN_POINT('Ctrl Pts',(-0.79445314485466,74.9993438212396,15.0693484015454));
#64777=CARTESIAN_POINT('Ctrl Pts',(-0.855855254470442,75.0078532350169,
15.0393737720039));
#64778=CARTESIAN_POINT('Ctrl Pts',(-0.915407830563247,75.0163465056109,
15.0062009476611));
#64779=CARTESIAN_POINT('Ctrl Pts',(-0.971425808638196,75.0243356788278,
14.9749970154614));
#64780=CARTESIAN_POINT('Ctrl Pts',(-1.02581131808626,75.0323112182964,14.9409608397735));
#64781=CARTESIAN_POINT('Ctrl Pts',(-1.07831624700676,75.0402791188551,14.9043633413764));
#64782=CARTESIAN_POINT('Ctrl Pts',(-1.1027578997126,75.0439882688769,14.8873267818741));
#64783=CARTESIAN_POINT('Ctrl Pts',(-1.12679272620587,75.047695853712,14.8697349449566));
#64784=CARTESIAN_POINT('Ctrl Pts',(-1.15039918302486,75.0514029488734,14.8516135820113));
#64785=CARTESIAN_POINT('Ctrl Pts',(-1.15042313215987,75.0514067097818,14.8515951975934));
#64786=CARTESIAN_POINT('Ctrl Pts',(-1.15044708086044,75.0514104706908,14.8515768126246));
#64787=CARTESIAN_POINT('Ctrl Pts',(-1.15047102912656,75.0514142316002,14.8515584271049));
#64788=CARTESIAN_POINT('Ctrl Pts',(-1.23163381332312,75.0641602851648,14.7892482807145));
#64789=CARTESIAN_POINT('Ctrl Pts',(-1.30780791253006,75.0769127374865,14.7206058432401));
#64790=CARTESIAN_POINT('Ctrl Pts',(-1.37817228584358,75.089663154856,14.646599244424));
#64791=CARTESIAN_POINT('Ctrl Pts',(-1.43987402621517,75.100843854763,14.5817036768106));
#64792=CARTESIAN_POINT('Ctrl Pts',(-1.49710857111955,75.1120228402846,14.5126836757894));
#64793=CARTESIAN_POINT('Ctrl Pts',(-1.54930332365839,75.1231904560488,14.4401619423412));
#64794=CARTESIAN_POINT('Ctrl Pts',(-1.55608174661695,75.1246407708679,14.430743697037));
#64795=CARTESIAN_POINT('Ctrl Pts',(-1.56277512510347,75.1260908846029,14.4212664482243));
#64796=CARTESIAN_POINT('Ctrl Pts',(-1.56938216741063,75.1275407677611,14.4117316114416));
#64797=CARTESIAN_POINT('Ctrl Pts',(-1.61630638655644,75.1378380584229,14.3440137507241));
#64798=CARTESIAN_POINT('Ctrl Pts',(-1.65887797582533,75.1481240462068,14.2733878730649));
#64799=CARTESIAN_POINT('Ctrl Pts',(-1.69662379552537,75.1583882525853,14.2003271148885));
#64800=CARTESIAN_POINT('Ctrl Pts',(-1.70283559236494,75.1600774241347,14.1883035692259));
#64801=CARTESIAN_POINT('Ctrl Pts',(-1.70891660919459,75.1617659922579,14.1762141568186));
#64802=CARTESIAN_POINT('Ctrl Pts',(-1.71486464298032,75.1634538942864,14.1640610826852));
#64803=CARTESIAN_POINT('Ctrl Pts',(-1.72499159849874,75.166327668945,14.1433695994836));
#64804=CARTESIAN_POINT('Ctrl Pts',(-1.73473317330876,75.1691995488222,14.1224931836789));
#64805=CARTESIAN_POINT('Ctrl Pts',(-1.74407844997948,75.1720692639313,14.1014421786624));
#64806=CARTESIAN_POINT('Ctrl Pts',(-1.74408173925696,75.1720702739912,14.1014347692941));
#64807=CARTESIAN_POINT('Ctrl Pts',(-1.74408502848537,75.1720712840509,14.1014273599041));
#64808=CARTESIAN_POINT('Ctrl Pts',(-1.74408831766465,75.1720722941103,14.1014199504926));
#64809=CARTESIAN_POINT('Ctrl Pts',(-1.74912296447396,75.1736183613032,14.0900785893136));
#64810=CARTESIAN_POINT('Ctrl Pts',(-1.75404253371793,75.1751637110891,14.0786881199489));
#64811=CARTESIAN_POINT('Ctrl Pts',(-1.7588451242202,75.1767080631392,14.067250592328));
#64812=CARTESIAN_POINT('Ctrl Pts',(-1.79041612375115,75.1868602378511,13.99206321606));
#64813=CARTESIAN_POINT('Ctrl Pts',(-1.81692814272135,75.1969686342519,13.9148403841097));
#64814=CARTESIAN_POINT('Ctrl Pts',(-1.83838148126977,75.2070493575475,13.8363131439182));
#64815=CARTESIAN_POINT('Ctrl Pts',(-1.85206261976672,75.2134779966726,13.7862350618324));
#64816=CARTESIAN_POINT('Ctrl Pts',(-1.86390894119643,75.2199323255159,13.7357262251899));
#64817=CARTESIAN_POINT('Ctrl Pts',(-1.87375377347736,75.2263904479145,13.6848691987371));
#64818=CARTESIAN_POINT('Ctrl Pts',(-1.87651059499211,75.2281988983041,13.6706278444204));
#64819=CARTESIAN_POINT('Ctrl Pts',(-1.87911033479588,75.230007607253,13.6563594683737));
#64820=CARTESIAN_POINT('Ctrl Pts',(-1.88154905044117,75.2318160032327,13.642066552674));
#64821=CARTESIAN_POINT('Ctrl Pts',(-1.88156664190423,75.2318290479397,13.6419634519705));
#64822=CARTESIAN_POINT('Ctrl Pts',(-1.88158422499357,75.2318420926342,13.6418603499602));
#64823=CARTESIAN_POINT('Ctrl Pts',(-1.88160179970896,75.2318551373163,13.6417572466445));
#64824=CARTESIAN_POINT('Ctrl Pts',(-1.89503969316487,75.2418292986761,13.562922890464));
#64825=CARTESIAN_POINT('Ctrl Pts',(-1.90358372662692,75.2517961590833,13.4833253137894));
#64826=CARTESIAN_POINT('Ctrl Pts',(-1.90696701947769,75.2617621701583,13.4035272721076));
#64827=CARTESIAN_POINT('Ctrl Pts',(-1.90865777948337,75.2667425646099,13.3636491582821));
#64828=CARTESIAN_POINT('Ctrl Pts',(-1.90905877377697,75.2717227893684,13.3237206427298));
#64829=CARTESIAN_POINT('Ctrl Pts',(-1.90834857578517,75.2767000324125,13.2838187135308));
#64830=CARTESIAN_POINT('Ctrl Pts',(-1.90764161704859,75.2816545739556,13.2440987794006));
#64831=CARTESIAN_POINT('Ctrl Pts',(-1.90583467804834,75.2866060300103,13.2044062106991));
#64832=CARTESIAN_POINT('Ctrl Pts',(-1.90268039003633,75.2915583348428,13.1648413210216));
#64833=CARTESIAN_POINT('Ctrl Pts',(-1.90266563946863,75.2915814935738,13.1646563015873));
#64834=CARTESIAN_POINT('Ctrl Pts',(-1.90265085931897,75.2916046524839,13.1644712836647));
#64835=CARTESIAN_POINT('Ctrl Pts',(-1.9026360495646,75.2916278115732,13.1642862672715));
#64836=CARTESIAN_POINT('Ctrl Pts',(-1.8981808083416,75.2985947960977,13.1086275006487));
#64837=CARTESIAN_POINT('Ctrl Pts',(-1.89104293007554,75.3055776417841,13.0531101156009));
#64838=CARTESIAN_POINT('Ctrl Pts',(-1.8814359156998,75.3125852593552,12.9980115027018));
#64839=CARTESIAN_POINT('Ctrl Pts',(-1.87338588903486,75.318457167744,12.9518426009295));
#64840=CARTESIAN_POINT('Ctrl Pts',(-1.8636032509819,75.3243465465202,12.9059672560355));
#64841=CARTESIAN_POINT('Ctrl Pts',(-1.85223213673048,75.3302609830586,12.8605276268862));
#64842=CARTESIAN_POINT('Ctrl Pts',(-1.83959362228345,75.336834630107,12.810023393372));
#64843=CARTESIAN_POINT('Ctrl Pts',(-1.82513037668464,75.3434690387466,12.7600435140782));
#64844=CARTESIAN_POINT('Ctrl Pts',(-1.80875091426492,75.3501234806354,12.7107244307332));
#64845=CARTESIAN_POINT('Ctrl Pts',(-1.79237145184519,75.3567779225242,12.6614053473882));
#64846=CARTESIAN_POINT('Ctrl Pts',(-1.77407495138808,75.3634523924017,12.6127472908621));
#64847=CARTESIAN_POINT('Ctrl Pts',(-1.75378330692145,75.3700981471543,12.564947614224));
#64848=CARTESIAN_POINT('Ctrl Pts',(-1.73423929954464,75.3764990418734,12.5189090965297));
#64849=CARTESIAN_POINT('Ctrl Pts',(-1.71284271627196,75.3828739576428,12.4736621112999));
#64850=CARTESIAN_POINT('Ctrl Pts',(-1.68961024576259,75.3892021479551,12.4293618498602));
#64851=CARTESIAN_POINT('Ctrl Pts',(-1.65465228155192,75.3987241938506,12.3627031209357));
#64852=CARTESIAN_POINT('Ctrl Pts',(-1.61553399868203,75.4081406901443,12.2981852149581));
#64853=CARTESIAN_POINT('Ctrl Pts',(-1.57268896769164,75.4174769600211,12.2362421749446));
#64854=CARTESIAN_POINT('Ctrl Pts',(-1.55687507894415,75.4209229309945,12.2133793056501));
#64855=CARTESIAN_POINT('Ctrl Pts',(-1.54055321361141,75.4243580404324,12.1908667787775));
#64856=CARTESIAN_POINT('Ctrl Pts',(-1.52374410223504,75.4277837981028,12.1687250189737));
#64857=CARTESIAN_POINT('Ctrl Pts',(-1.47900264321441,75.4369022692104,12.1097894442891));
#64858=CARTESIAN_POINT('Ctrl Pts',(-1.43081223803484,75.445954538049,12.0534836353524));
#64859=CARTESIAN_POINT('Ctrl Pts',(-1.37959434194762,75.4549673385587,12.0002103269436));
#64860=CARTESIAN_POINT('Ctrl Pts',(-1.36112325376369,75.458217691379,11.980997980232));
#64861=CARTESIAN_POINT('Ctrl Pts',(-1.3422582300322,75.4614629743166,11.9621795815972));
#64862=CARTESIAN_POINT('Ctrl Pts',(-1.32301830800744,75.4647046552193,11.9437725482982));
#64863=CARTESIAN_POINT('Ctrl Pts',(-1.27098277329551,75.4734719776088,11.8939896116033));
#64864=CARTESIAN_POINT('Ctrl Pts',(-1.21620842607349,75.4822123776369,11.8472210800521));
#64865=CARTESIAN_POINT('Ctrl Pts',(-1.15909057545261,75.490949156467,11.8038212767092));
#64866=CARTESIAN_POINT('Ctrl Pts',(-1.15473759094654,75.4916149914462,11.8005137525383));
#64867=CARTESIAN_POINT('Ctrl Pts',(-1.15037098756579,75.4922808080305,11.7972257703682));
#64868=CARTESIAN_POINT('Ctrl Pts',(-1.14599093612188,75.4929466178375,11.7939574754032));
#64869=CARTESIAN_POINT('Ctrl Pts',(-1.09923734883009,75.500053611289,11.7590710098211));
#64870=CARTESIAN_POINT('Ctrl Pts',(-1.05097004323201,75.5071704646145,11.7264028158223));
#64871=CARTESIAN_POINT('Ctrl Pts',(-1.00143818770449,75.5143409295118,11.696049786287));
#64872=CARTESIAN_POINT('Ctrl Pts',(-0.9672702277746,75.5192872444575,11.6751117235824));
#64873=CARTESIAN_POINT('Ctrl Pts',(-0.932499888278065,75.524259199438,11.6552744312169));
#64874=CARTESIAN_POINT('Ctrl Pts',(-0.897198351310015,75.5292728555587,
11.6365600239425));
#64875=CARTESIAN_POINT('Ctrl Pts',(-0.897135623778236,75.529281764357,11.6365267701899));
#64876=CARTESIAN_POINT('Ctrl Pts',(-0.897072894089373,75.5292906732001,
11.6364935201442));
#64877=CARTESIAN_POINT('Ctrl Pts',(-0.897010162243998,75.5292995820881,
11.6364602738058));
#64878=CARTESIAN_POINT('Ctrl Pts',(-0.848793065296281,75.5361471522735,
11.6109063957864));
#64879=CARTESIAN_POINT('Ctrl Pts',(-0.799303600639264,75.543020762987,11.5875467945996));
#64880=CARTESIAN_POINT('Ctrl Pts',(-0.748872763198369,75.5499555577861,
11.5663189927731));
#64881=CARTESIAN_POINT('Ctrl Pts',(-0.714420144622406,75.5546931717589,
11.5518168865887));
#64882=CARTESIAN_POINT('Ctrl Pts',(-0.679527838667414,75.559459454955,11.5383086274129));
#64883=CARTESIAN_POINT('Ctrl Pts',(-0.644294595743942,75.5642670645859,
11.5257621898246));
#64884=CARTESIAN_POINT('Ctrl Pts',(-0.583888688816627,75.5725095082502,
11.5042518524744));
#64885=CARTESIAN_POINT('Ctrl Pts',(-0.522372346675663,75.5808060797152,
11.4857360608543));
#64886=CARTESIAN_POINT('Ctrl Pts',(-0.460057431799019,75.589105955884,11.4703277296083));
#64887=CARTESIAN_POINT('Ctrl Pts',(-0.430652191081433,75.5930225119308,
11.4630568268037));
#64888=CARTESIAN_POINT('Ctrl Pts',(-0.401069881618514,75.5969397081773,
11.4564779380468));
#64889=CARTESIAN_POINT('Ctrl Pts',(-0.371347266997866,75.6008516946164,
11.4506029146664));
#64890=CARTESIAN_POINT('Ctrl Pts',(-0.305962402846651,75.6094574214392,
11.4376788294027));
#64891=CARTESIAN_POINT('Ctrl Pts',(-0.239894421453448,75.6180374864646,
11.4281615585366));
#64892=CARTESIAN_POINT('Ctrl Pts',(-0.173491447715413,75.6265396084448,
11.4221589217094));
#64893=CARTESIAN_POINT('Ctrl Pts',(-0.144978066637523,75.6301904124728,
11.419581394504));
#64894=CARTESIAN_POINT('Ctrl Pts',(-0.116403531130909,75.6338267590699,
11.4176521294849));
#64895=CARTESIAN_POINT('Ctrl Pts',(-0.0877982390560473,75.6374441231734,
11.4163803841385));
#64896=CARTESIAN_POINT('Ctrl Pts',(-0.0489006230125617,75.6423630325703,
11.4146510585975));
#64897=CARTESIAN_POINT('Ctrl Pts',(-0.00994327625232608,75.6472475382857,
11.414136431099));
#64898=CARTESIAN_POINT('Ctrl Pts',(0.0290034066344337,75.6520888411402,
11.4148571492207));
#64899=CARTESIAN_POINT('Ctrl Pts',(0.0966315685909427,75.6604954213481,
11.4161086252966));
#64900=CARTESIAN_POINT('Ctrl Pts',(0.16423318315411,75.6687716473232,11.4210869881037));
#64901=CARTESIAN_POINT('Ctrl Pts',(0.231391873384125,75.6769704240339,11.429666307699));
#64902=CARTESIAN_POINT('Ctrl Pts',(0.258994454213436,75.6803401651066,11.4331924539324));
#64903=CARTESIAN_POINT('Ctrl Pts',(0.286522821661356,75.6836969046949,11.4373269787138));
#64904=CARTESIAN_POINT('Ctrl Pts',(0.313950515650403,75.6870446558327,11.4420617230722));
#64905=CARTESIAN_POINT('Ctrl Pts',(0.379256533066087,75.69501573405,11.453335266435));
#64906=CARTESIAN_POINT('Ctrl Pts',(0.44398850254222,75.7029363581561,11.4680103200387));
#64907=CARTESIAN_POINT('Ctrl Pts',(0.507747595471506,75.710858621323,11.4859568730678));
#64908=CARTESIAN_POINT('Ctrl Pts',(0.53513379017223,75.714261440146,11.4936653860482));
#64909=CARTESIAN_POINT('Ctrl Pts',(0.562341145438018,75.7176646451403,11.5019773913128));
#64910=CARTESIAN_POINT('Ctrl Pts',(0.589340981957953,75.721072741656,11.5108825196477));
#64911=CARTESIAN_POINT('Ctrl Pts',(0.65865362053499,75.7298218376683,11.5337433225751));
#64912=CARTESIAN_POINT('Ctrl Pts',(0.726614803478868,75.7386900862247,11.5603150939239));
#64913=CARTESIAN_POINT('Ctrl Pts',(0.792731839442396,75.7477073109522,11.5904922109949));
#64914=CARTESIAN_POINT('Ctrl Pts',(0.809092813106204,75.7499386659145,11.5979596815258));
#64915=CARTESIAN_POINT('Ctrl Pts',(0.825341087495351,75.7521791616775,11.6056478154616));
#64916=CARTESIAN_POINT('Ctrl Pts',(0.841469654748839,75.7544292860038,11.6135548221577));
#64917=CARTESIAN_POINT('Ctrl Pts',(0.859238357464154,75.7569082284666,11.6222659028844));
#64918=CARTESIAN_POINT('Ctrl Pts',(0.87685468981896,75.7593864049395,11.6312687689277));
#64919=CARTESIAN_POINT('Ctrl Pts',(0.894305628425393,75.7618633458217,11.6405607880959));
#64920=CARTESIAN_POINT('Ctrl Pts',(0.903139747007031,75.7631172376591,11.6452646496501));
#64921=CARTESIAN_POINT('Ctrl Pts',(0.911931388265836,75.7643707989428,11.6500425499173));
#64922=CARTESIAN_POINT('Ctrl Pts',(0.920679184464007,75.765624010736,11.6548942660476));
#64923=CARTESIAN_POINT('Ctrl Pts',(0.976183407168826,75.7735755616055,11.6856781030844));
#64924=CARTESIAN_POINT('Ctrl Pts',(1.03009096683839,75.7815373641079,11.719530489887));
#64925=CARTESIAN_POINT('Ctrl Pts',(1.08211815751369,75.7894993738068,11.7561513401554));
#64926=CARTESIAN_POINT('Ctrl Pts',(1.11865528182004,75.7950908526916,11.7818690570088));
#64927=CARTESIAN_POINT('Ctrl Pts',(1.15426350246226,75.8006821379589,11.8089498719097));
#64928=CARTESIAN_POINT('Ctrl Pts',(1.18885608630365,75.8062707195369,11.8372861931718));
#64929=CARTESIAN_POINT('Ctrl Pts',(1.26095224823748,75.817918166408,11.8963433603292));
#64930=CARTESIAN_POINT('Ctrl Pts',(1.32866192715258,75.8295574124541,11.9608676517253));
#64931=CARTESIAN_POINT('Ctrl Pts',(1.39143020206034,75.8412258672627,12.0300131362008));
#64932=CARTESIAN_POINT('Ctrl Pts',(1.39819263057232,75.8424829846776,12.0374626223684));
#64933=CARTESIAN_POINT('Ctrl Pts',(1.4048977027914,75.8437404447991,12.0449657969394));
#64934=CARTESIAN_POINT('Ctrl Pts',(1.41154472262835,75.8449982970642,12.0525216376492));
#64935=CARTESIAN_POINT('Ctrl Pts',(1.47519562629064,75.8570433090111,12.1248752789662));
#64936=CARTESIAN_POINT('Ctrl Pts',(1.53345912753552,75.869068147836,12.2021451994932));
#64937=CARTESIAN_POINT('Ctrl Pts',(1.58568533590138,75.8811243127768,12.2833577550705));
#64938=CARTESIAN_POINT('Ctrl Pts',(1.58953613559223,75.8820132510643,12.2893458076919));
#64939=CARTESIAN_POINT('Ctrl Pts',(1.5933541260633,75.8829023627213,12.2953553140732));
#64940=CARTESIAN_POINT('Ctrl Pts',(1.59713905249284,75.8837916698498,12.3013858934346));
#64941=CARTESIAN_POINT('Ctrl Pts',(1.59716100967478,75.883796828914,12.3014208781379));
#64942=CARTESIAN_POINT('Ctrl Pts',(1.59718296574323,75.8838019879847,12.3014558635489));
#64943=CARTESIAN_POINT('Ctrl Pts',(1.59720492069803,75.8838071470618,12.3014908496674));
#64944=CARTESIAN_POINT('Ctrl Pts',(1.64421070095242,75.8948527833314,12.3763964830218));
#64945=CARTESIAN_POINT('Ctrl Pts',(1.68611306586749,75.9059285477027,12.454549496737));
#64946=CARTESIAN_POINT('Ctrl Pts',(1.7224412023541,75.9169784004475,12.5351730844704));
#64947=CARTESIAN_POINT('Ctrl Pts',(1.7258457009239,75.9180139396054,12.5427287401047));
#64948=CARTESIAN_POINT('Ctrl Pts',(1.72920123537447,75.9190492465905,12.5503060570557));
#64949=CARTESIAN_POINT('Ctrl Pts',(1.73250741417377,75.9200842724326,12.557904373156));
#64950=CARTESIAN_POINT('Ctrl Pts',(1.77029251842462,75.9319132029662,12.6447427395626));
#64951=CARTESIAN_POINT('Ctrl Pts',(1.80163260646769,75.9437053249773,12.7343288544185));
#64952=CARTESIAN_POINT('Ctrl Pts',(1.82597858705125,75.9554081493042,12.8256992037765));
#64953=CARTESIAN_POINT('Ctrl Pts',(1.83126185966317,75.9579477558333,12.8455273007656));
#64954=CARTESIAN_POINT('Ctrl Pts',(1.83621586635653,75.9604832474547,12.8654394204659));
#64955=CARTESIAN_POINT('Ctrl Pts',(1.84083516476731,75.9630142551579,12.8854257223643));
#64956=CARTESIAN_POINT('Ctrl Pts',(1.86238082771495,75.9748195628131,12.9786472651136));
#64957=CARTESIAN_POINT('Ctrl Pts',(1.87693370588993,75.9867185332742,13.0733722423359));
#64958=CARTESIAN_POINT('Ctrl Pts',(1.88394226763736,75.9986685723865,13.168608630988));
#64959=CARTESIAN_POINT('Ctrl Pts',(1.88455932889628,75.9997207006896,13.1769936160954));
#64960=CARTESIAN_POINT('Ctrl Pts',(1.88511733747509,76.0007728324774,13.1853824812178));
#64961=CARTESIAN_POINT('Ctrl Pts',(1.88561596325121,76.0018249466931,13.1937743533224));
#64962=CARTESIAN_POINT('Ctrl Pts',(1.88562071927659,76.0018349820386,13.1938543972323));
#64963=CARTESIAN_POINT('Ctrl Pts',(1.88562546992771,76.0018450174184,13.1939344416131));
#64964=CARTESIAN_POINT('Ctrl Pts',(1.88563021520441,76.0018550528325,13.1940144864636));
#64965=CARTESIAN_POINT('Ctrl Pts',(1.88934921213212,76.0097200682497,13.2567477203733));
#64966=CARTESIAN_POINT('Ctrl Pts',(1.88976376963936,76.01760579953,13.3197665736573));
#64967=CARTESIAN_POINT('Ctrl Pts',(1.88707397236113,76.0255711291619,13.3826907579127));
#64968=CARTESIAN_POINT('Ctrl Pts',(1.88495763313559,76.0318382704371,13.4321996634546));
#64969=CARTESIAN_POINT('Ctrl Pts',(1.88092054514117,76.0381547895768,13.481650542398));
#64970=CARTESIAN_POINT('Ctrl Pts',(1.87507453210503,76.0445515341352,13.5308755365519));
#64971=CARTESIAN_POINT('Ctrl Pts',(1.86621950738515,76.0542407583709,13.6054372142926));
#64972=CARTESIAN_POINT('Ctrl Pts',(1.8530094099864,76.0639800127981,13.679516890321));
#64973=CARTESIAN_POINT('Ctrl Pts',(1.83553504488097,76.0736838726472,13.7526145805329));
#64974=CARTESIAN_POINT('Ctrl Pts',(1.8264729764718,76.0787162181003,13.7905224681876));
#64975=CARTESIAN_POINT('Ctrl Pts',(1.81626422543518,76.0837389263354,13.8281654089272));
#64976=CARTESIAN_POINT('Ctrl Pts',(1.80492310978648,76.0887393302903,13.8654684660956));
#64977=CARTESIAN_POINT('Ctrl Pts',(1.78342243897396,76.0982191771322,13.9361882063155));
#64978=CARTESIAN_POINT('Ctrl Pts',(1.75785031253306,76.1076189232886,14.0056947908024));
#64979=CARTESIAN_POINT('Ctrl Pts',(1.72828352214613,76.1168660130861,14.0735310977614));
#64980=CARTESIAN_POINT('Ctrl Pts',(1.72219223376294,76.1187710792067,14.0875065919943));
#64981=CARTESIAN_POINT('Ctrl Pts',(1.7159313692519,76.120669646444,14.1014110208233));
#64982=CARTESIAN_POINT('Ctrl Pts',(1.70950156945226,76.1225610499344,14.1152401152146));
#64983=CARTESIAN_POINT('Ctrl Pts',(1.67857438950661,76.1316586545134,14.1817577213696));
#64984=CARTESIAN_POINT('Ctrl Pts',(1.64373119636544,76.1405928160376,14.2465505915588));
#64985=CARTESIAN_POINT('Ctrl Pts',(1.60524457886279,76.1494565148589,14.3092026896844));
#64986=CARTESIAN_POINT('Ctrl Pts',(1.58471620064246,76.1541843234751,14.3426206944371));
#64987=CARTESIAN_POINT('Ctrl Pts',(1.56315070554684,76.1588922065802,14.3754303553122));
#64988=CARTESIAN_POINT('Ctrl Pts',(1.54058507095701,76.1635950968011,14.4075726254229));
#64989=CARTESIAN_POINT('Ctrl Pts',(1.50468300191011,76.17107742524,14.4587111828717));
#64990=CARTESIAN_POINT('Ctrl Pts',(1.46625175666687,76.1785485603453,14.5081577299275));
#64991=CARTESIAN_POINT('Ctrl Pts',(1.42553043846439,76.1861085972088,14.5556602595519));
#64992=CARTESIAN_POINT('Ctrl Pts',(1.39344501459786,76.1920653539622,14.5930887826207));
#64993=CARTESIAN_POINT('Ctrl Pts',(1.35993781077964,76.1980774328039,14.6293115024797));
#64994=CARTESIAN_POINT('Ctrl Pts',(1.3251174969929,76.2041965854019,14.6642262173261));
#64995=CARTESIAN_POINT('Ctrl Pts',(1.27871197201487,76.2123516666705,14.7107575519323));
#64996=CARTESIAN_POINT('Ctrl Pts',(1.22980912458991,76.2205534344995,14.7548720734239));
#64997=CARTESIAN_POINT('Ctrl Pts',(1.17859700383456,76.2287601237931,14.7961622794986));
#64998=CARTESIAN_POINT('Ctrl Pts',(1.15685510209923,76.2322442410209,14.8136918719049));
#64999=CARTESIAN_POINT('Ctrl Pts',(1.13469750425527,76.2357292223335,14.8307127456576));
#65000=CARTESIAN_POINT('Ctrl Pts',(1.11214088953549,76.2392117709786,14.8471954707205));
#65001=CARTESIAN_POINT('Ctrl Pts',(1.1120683588603,76.2392229690953,14.8472484708357));
#65002=CARTESIAN_POINT('Ctrl Pts',(1.11199582380467,76.2392341672263,14.8473014655748));
#65003=CARTESIAN_POINT('Ctrl Pts',(1.11192328436901,76.2392453653717,14.8473544549371));
#65004=CARTESIAN_POINT('Ctrl Pts',(1.07975507531341,76.2442112749825,14.8708530232226));
#65005=CARTESIAN_POINT('Ctrl Pts',(1.04672524814866,76.2491799969426,14.8932938242039));
#65006=CARTESIAN_POINT('Ctrl Pts',(1.01314163335639,76.2541489889907,14.9147600024979));
#65007=CARTESIAN_POINT('Ctrl Pts',(0.979548542731243,76.259119383072,14.9362322376122));
#65008=CARTESIAN_POINT('Ctrl Pts',(0.945401876828864,76.2640900161531,14.9567296890912));
#65009=CARTESIAN_POINT('Ctrl Pts',(0.910604768726041,76.2690624667108,14.9761262412943));
#65010=CARTESIAN_POINT('Ctrl Pts',(0.889373533642221,76.2720963759202,14.987960924752));
#65011=CARTESIAN_POINT('Ctrl Pts',(0.867899895825725,76.275130992031,14.9993858049844));
#65012=CARTESIAN_POINT('Ctrl Pts',(0.846204859160859,76.2781661497328,15.0103947483936));
#65013=CARTESIAN_POINT('Ctrl Pts',(0.796822753343998,76.2850747565776,15.0354532360449));
#65014=CARTESIAN_POINT('Ctrl Pts',(0.746295197571573,76.2919894181333,15.0583600802408));
#65015=CARTESIAN_POINT('Ctrl Pts',(0.694854334359175,76.2989088701488,15.0790498124819));
#65016=CARTESIAN_POINT('Ctrl Pts',(0.694804855660447,76.2989155256647,15.0790697130233));
#65017=CARTESIAN_POINT('Ctrl Pts',(0.694755376114044,76.2989221811735,15.0790896115014));
#65018=CARTESIAN_POINT('Ctrl Pts',(0.694705895720112,76.2989288366753,15.0791095079162));
#65019=CARTESIAN_POINT('Ctrl Pts',(0.616257700799937,76.3094807352923,15.1106540794923));
#65020=CARTESIAN_POINT('Ctrl Pts',(0.535681447237287,76.3200146847492,15.1370128233276));
#65021=CARTESIAN_POINT('Ctrl Pts',(0.453661557581416,76.3305748587873,15.1580026317918));
#65022=CARTESIAN_POINT('Ctrl Pts',(0.380788019203144,76.3399574274701,15.1766517865162));
#65023=CARTESIAN_POINT('Ctrl Pts',(0.306771473373925,76.3493533885477,15.1910536728427));
#65024=CARTESIAN_POINT('Ctrl Pts',(0.232129202297214,76.3588065019626,15.201088110003));
#65025=CARTESIAN_POINT('Ctrl Pts',(0.232080751365556,76.3588126380588,15.2010946234413));
#65026=CARTESIAN_POINT('Ctrl Pts',(0.232032300165493,76.3588187741885,15.2011011350494));
#65027=CARTESIAN_POINT('Ctrl Pts',(0.231983848697136,76.3588249103517,15.2011076448271));
#65028=CARTESIAN_POINT('Ctrl Pts',(0.137991589429435,76.3707286123759,15.2137361314379));
#65029=CARTESIAN_POINT('Ctrl Pts',(0.0429853382493918,76.3827589998507,
15.2194764706094));
#65030=CARTESIAN_POINT('Ctrl Pts',(-0.0520240868000823,76.3948323315213,
15.2182468575097));
#65031=CARTESIAN_POINT('Ctrl Pts',(-0.0577682407686029,76.3955622704299,
15.2181725166013));
#65032=CARTESIAN_POINT('Ctrl Pts',(-0.0635123907735374,76.3962923643382,
15.2180727002637));
#65033=CARTESIAN_POINT('Ctrl Pts',(-0.0692563074998502,76.3970225939822,
15.2179473912935));
#65034=CARTESIAN_POINT('Ctrl Pts',(-0.128876426799208,76.4046021569473,
15.2166467220632));
#65035=CARTESIAN_POINT('Ctrl Pts',(-0.188474756072447,76.4121963263439,
15.2125994948107));
#65036=CARTESIAN_POINT('Ctrl Pts',(-0.247812949518697,76.4197844676737,
15.2057811438586));
#65037=CARTESIAN_POINT('Ctrl Pts',(-0.247822696909592,76.4197857141657,
15.2057800238189));
#65038=CARTESIAN_POINT('Ctrl Pts',(-0.247832444293133,76.4197869606571,
15.2057789037042));
#65039=CARTESIAN_POINT('Ctrl Pts',(-0.247842191669441,76.4197882071481,
15.2057777835145));
#65040=CARTESIAN_POINT('Ctrl Pts',(-0.296768621773948,76.4260449015995,
15.2001550515277));
#65041=CARTESIAN_POINT('Ctrl Pts',(-0.345511860507362,76.4322899800438,
15.1926421540169));
#65042=CARTESIAN_POINT('Ctrl Pts',(-0.393923595077852,76.4384991181169,
15.1832364327955));
#65043=CARTESIAN_POINT('Ctrl Pts',(-0.472724647314597,76.4486058952854,
15.1679264932556));
#65044=CARTESIAN_POINT('Ctrl Pts',(-0.55065561839925,76.4586178271985,15.1475983375985));
#65045=CARTESIAN_POINT('Ctrl Pts',(-0.627072151467601,76.4686417005575,
15.1224496752263));
#65046=CARTESIAN_POINT('Ctrl Pts',(-0.63608060953238,76.4698233773384,15.119484993877));
#65047=CARTESIAN_POINT('Ctrl Pts',(-0.64506808015541,76.471005227474,15.116453318266));
#65048=CARTESIAN_POINT('Ctrl Pts',(-0.654033554488171,76.4721874318132,
15.1133549679532));
#65049=CARTESIAN_POINT('Ctrl Pts',(-0.674750719656962,76.4749192362498,
15.1061953874561));
#65050=CARTESIAN_POINT('Ctrl Pts',(-0.69534887222477,76.4776536452001,15.0986812613525));
#65051=CARTESIAN_POINT('Ctrl Pts',(-0.715817134101095,76.4803915333587,
15.0908145306932));
#65052=CARTESIAN_POINT('Ctrl Pts',(-0.743519894557304,76.4840971269393,
15.0801673073802));
#65053=CARTESIAN_POINT('Ctrl Pts',(-0.770984721891046,76.4878090925378,
15.06887420287));
#65054=CARTESIAN_POINT('Ctrl Pts',(-0.798189458128453,76.4915296306858,
15.056951901387));
#65055=CARTESIAN_POINT('Ctrl Pts',(-0.911084414566109,76.5069692213686,
15.0074764095161));
#65056=CARTESIAN_POINT('Ctrl Pts',(-1.01943964134501,76.5225282019892,14.9471703884302));
#65057=CARTESIAN_POINT('Ctrl Pts',(-1.12135445929174,76.5381286396529,14.877182845032));
#65058=CARTESIAN_POINT('Ctrl Pts',(-1.2017001135926,76.5504274142247,14.8220074045953));
#65059=CARTESIAN_POINT('Ctrl Pts',(-1.27804160555201,76.5627518078509,14.7608149186131));
#65060=CARTESIAN_POINT('Ctrl Pts',(-1.34943037510579,76.57506064616,14.6941830749454));
#65061=CARTESIAN_POINT('Ctrl Pts',(-1.39751624084463,76.5833516021469,14.6493013672404));
#65062=CARTESIAN_POINT('Ctrl Pts',(-1.44336147044613,76.5916368827775,14.6019471847877));
#65063=CARTESIAN_POINT('Ctrl Pts',(-1.48668558555809,76.5999089266508,14.5522850350241));
#65064=CARTESIAN_POINT('Ctrl Pts',(-1.49158704091489,76.60084478082,14.5466665288097));
#65065=CARTESIAN_POINT('Ctrl Pts',(-1.49645619035975,76.6017805347959,14.5410186158649));
#65066=CARTESIAN_POINT('Ctrl Pts',(-1.50129260439728,76.6027162098982,14.5353416113803));
#65067=CARTESIAN_POINT('Ctrl Pts',(-1.52167244313396,76.6066589880696,14.5114196652845));
#65068=CARTESIAN_POINT('Ctrl Pts',(-1.54147096485587,76.6106003627238,14.486981144753));
#65069=CARTESIAN_POINT('Ctrl Pts',(-1.56066967448821,76.6145419509358,14.462062680762));
#65070=CARTESIAN_POINT('Ctrl Pts',(-1.62763578885548,76.6282904190389,14.3751457607483));
#65071=CARTESIAN_POINT('Ctrl Pts',(-1.68731612124307,76.6420412457091,14.2823730686698));
#65072=CARTESIAN_POINT('Ctrl Pts',(-1.73899513408363,76.6558316937168,14.185139277798));
#65073=CARTESIAN_POINT('Ctrl Pts',(-1.78985545719773,76.6694036759008,14.0894458473409));
#65074=CARTESIAN_POINT('Ctrl Pts',(-1.83296499614123,76.6830141672576,13.9894312397797));
#65075=CARTESIAN_POINT('Ctrl Pts',(-1.86762072967996,76.6966756005143,13.8864282818764));
#65076=CARTESIAN_POINT('Ctrl Pts',(-1.89216199676877,76.7063498693332,13.8134873037834));
#65077=CARTESIAN_POINT('Ctrl Pts',(-1.91246355224693,76.7160492137621,13.7390479787698));
#65078=CARTESIAN_POINT('Ctrl Pts',(-1.92827250707106,76.7257702474795,13.6635842692239));
#65079=CARTESIAN_POINT('Ctrl Pts',(-1.92827968198353,76.7257746593819,13.6635500199319));
#65080=CARTESIAN_POINT('Ctrl Pts',(-1.92828685597066,76.7257790712888,13.6635157704289));
#65081=CARTESIAN_POINT('Ctrl Pts',(-1.92829402903243,76.7257834832001,13.6634815207149));
#65082=CARTESIAN_POINT('Ctrl Pts',(-1.94524041126691,76.7362066383932,13.5825664579412));
#65083=CARTESIAN_POINT('Ctrl Pts',(-1.95702124385381,76.746654153287,13.5004726711336));
#65084=CARTESIAN_POINT('Ctrl Pts',(-1.96353759162479,76.756969596949,13.4178452341049));
#65085=CARTESIAN_POINT('Ctrl Pts',(-1.96430620794729,76.758186324271,13.4080991617622));
#65086=CARTESIAN_POINT('Ctrl Pts',(-1.96500158041824,76.7594012065497,13.3983457239801));
#65087=CARTESIAN_POINT('Ctrl Pts',(-1.96562354819451,76.7606139810479,13.3885860263595));
#65088=CARTESIAN_POINT('Ctrl Pts',(-1.96602724284844,76.7614011449493,13.3822513931138));
#65089=CARTESIAN_POINT('Ctrl Pts',(-1.96640002443412,76.7621874395988,13.3759140270023));
#65090=CARTESIAN_POINT('Ctrl Pts',(-1.96674185096452,76.762972801968,13.369574190282));
#65091=CARTESIAN_POINT('Ctrl Pts',(-1.97173157861374,76.7744369335669,13.2770300026252));
#65092=CARTESIAN_POINT('Ctrl Pts',(-1.97012670401495,76.7857014028749,13.1839488204329));
#65093=CARTESIAN_POINT('Ctrl Pts',(-1.96201561172285,76.7969266255661,13.0912432452857));
#65094=CARTESIAN_POINT('Ctrl Pts',(-1.95484308074262,76.8068529406188,13.0092649388088));
#65095=CARTESIAN_POINT('Ctrl Pts',(-1.94257920657521,76.8167502917483,12.9275798932984));
#65096=CARTESIAN_POINT('Ctrl Pts',(-1.92530718457434,76.8267249305343,12.8469077778324));
#65097=CARTESIAN_POINT('Ctrl Pts',(-1.92300670533757,76.8280534634311,12.8361629717751));
#65098=CARTESIAN_POINT('Ctrl Pts',(-1.92061742967071,76.8293833739384,12.8254360763024));
#65099=CARTESIAN_POINT('Ctrl Pts',(-1.91813959563186,76.8307149190786,12.8147287361971));
#65100=CARTESIAN_POINT('Ctrl Pts',(-1.9079801459258,76.8361744315682,12.7708272151185));
#65101=CARTESIAN_POINT('Ctrl Pts',(-1.89633200080765,76.8416609959429,12.7272575490495));
#65102=CARTESIAN_POINT('Ctrl Pts',(-1.88321815517742,76.8471892187894,12.6841450721228));
#65103=CARTESIAN_POINT('Ctrl Pts',(-1.88321681362367,76.8471897843297,12.6841406616923));
#65104=CARTESIAN_POINT('Ctrl Pts',(-1.88321547205458,76.8471903498704,12.6841362512665));
#65105=CARTESIAN_POINT('Ctrl Pts',(-1.88321413047017,76.8471909154116,12.6841318408456));
#65106=CARTESIAN_POINT('Ctrl Pts',(-1.85561868320266,76.8588236991485,12.5934125855832));
#65107=CARTESIAN_POINT('Ctrl Pts',(-1.82141417942789,76.8706001098608,12.5044844413145));
#65108=CARTESIAN_POINT('Ctrl Pts',(-1.7810669786483,76.8824653213828,12.4182971120898));
#65109=CARTESIAN_POINT('Ctrl Pts',(-1.74067621942913,76.8943433424699,12.3320167358754));
#65110=CARTESIAN_POINT('Ctrl Pts',(-1.69413295237097,76.906309356748,12.2484822131731));
#65111=CARTESIAN_POINT('Ctrl Pts',(-1.64189620607594,76.9183086184102,12.1685643294944));
#65112=CARTESIAN_POINT('Ctrl Pts',(-1.59030313053314,76.9301600229733,12.0896312086111));
#65113=CARTESIAN_POINT('Ctrl Pts',(-1.53315848344633,76.9420431346575,12.0142237961768));
#65114=CARTESIAN_POINT('Ctrl Pts',(-1.47085200607609,76.9539180294252,11.9431258890206));
#65115=CARTESIAN_POINT('Ctrl Pts',(-1.43887697541807,76.9600121008651,11.9066391888092));
#65116=CARTESIAN_POINT('Ctrl Pts',(-1.40554141244029,76.9661042828369,11.871286756175));
#65117=CARTESIAN_POINT('Ctrl Pts',(-1.37088976906968,76.9721914266629,11.8371724623512));
#65118=CARTESIAN_POINT('Ctrl Pts',(-1.3708804480234,76.9721930640614,11.8371632858481));
#65119=CARTESIAN_POINT('Ctrl Pts',(-1.37087112688185,76.9721947014595,11.8371541094346));
#65120=CARTESIAN_POINT('Ctrl Pts',(-1.37086180564508,76.9721963388573,11.8371449331108));
#65121=CARTESIAN_POINT('Ctrl Pts',(-1.35497785140035,76.9749865642426,11.8215079193249));
#65122=CARTESIAN_POINT('Ctrl Pts',(-1.33882684784642,76.9777759223102,11.8061391757218));
#65123=CARTESIAN_POINT('Ctrl Pts',(-1.32241583834212,76.9805609549376,11.7910442661207));
#65124=CARTESIAN_POINT('Ctrl Pts',(-1.26061011048626,76.9910497044928,11.734195120151));
#65125=CARTESIAN_POINT('Ctrl Pts',(-1.19511367713146,77.0014774844399,11.6812232869333));
#65126=CARTESIAN_POINT('Ctrl Pts',(-1.12643793634185,77.0118924418064,11.6324249051649));
#65127=CARTESIAN_POINT('Ctrl Pts',(-1.05763810402149,77.0223262181618,11.5835383486522));
#65128=CARTESIAN_POINT('Ctrl Pts',(-0.985645517210265,77.032747692906,11.5388423265716));
#65129=CARTESIAN_POINT('Ctrl Pts',(-0.911016984403536,77.0431983409845,
11.4986938705813));
#65130=CARTESIAN_POINT('Ctrl Pts',(-0.836716025017025,77.0536031171371,
11.4587216416525));
#65131=CARTESIAN_POINT('Ctrl Pts',(-0.759801326271844,77.064037300583,11.4232596668721));
#65132=CARTESIAN_POINT('Ctrl Pts',(-0.680885783738669,77.0745271496242,
11.3926851118145));
#65133=CARTESIAN_POINT('Ctrl Pts',(-0.623293559583517,77.0821825964214,
11.3703719327904));
#65134=CARTESIAN_POINT('Ctrl Pts',(-0.564637168277213,77.0898674127886,
11.3506625403562));
#65135=CARTESIAN_POINT('Ctrl Pts',(-0.505178035093774,77.0975846091653,
11.3336993763504));
#65136=CARTESIAN_POINT('Ctrl Pts',(-0.505171807848367,77.097585417399,11.3336975997725));
#65137=CARTESIAN_POINT('Ctrl Pts',(-0.505165580593133,77.0975862256336,
11.3336958232242));
#65138=CARTESIAN_POINT('Ctrl Pts',(-0.505159353328048,77.097587033869,11.3336940467055));
#65139=CARTESIAN_POINT('Ctrl Pts',(-0.427970794669812,77.1076053200649,
11.3116736393542));
#65140=CARTESIAN_POINT('Ctrl Pts',(-0.349268028875698,77.1177520080522,
11.2942127955183));
#65141=CARTESIAN_POINT('Ctrl Pts',(-0.269698011573538,77.1279543471805,
11.2814182132585));
#65142=CARTESIAN_POINT('Ctrl Pts',(-0.249182504980679,77.1305848123073,
11.278119391094));
#65143=CARTESIAN_POINT('Ctrl Pts',(-0.228609489462926,77.1332189671837,
11.2751305338261));
#65144=CARTESIAN_POINT('Ctrl Pts',(-0.207990316034561,77.1358555448891,
11.2724529787815));
#65145=CARTESIAN_POINT('Ctrl Pts',(-0.10725594034829,77.1487364690456,11.259371861019));
#65146=CARTESIAN_POINT('Ctrl Pts',(-0.00541727235168708,77.1616738252754,
11.2537213749054));
#65147=CARTESIAN_POINT('Ctrl Pts',(0.0963934601931026,77.1745429068827,
11.2556178907869));
#65148=CARTESIAN_POINT('Ctrl Pts',(0.17795911434822,77.1848529698145,11.2571372842204));
#65149=CARTESIAN_POINT('Ctrl Pts',(0.259510820212742,77.1951193141316,11.2634973388782));
#65150=CARTESIAN_POINT('Ctrl Pts',(0.340547509078918,77.2052984574678,11.2747743781765));
#65151=CARTESIAN_POINT('Ctrl Pts',(0.39663827639075,77.2123441051651,11.2825799511348));
#65152=CARTESIAN_POINT('Ctrl Pts',(0.452487902306173,77.2193491360449,11.2927430994818));
#65153=CARTESIAN_POINT('Ctrl Pts',(0.50790757268455,77.2263613506863,11.3052703577388));
#65154=CARTESIAN_POINT('Ctrl Pts',(0.507914707147799,77.2263622534053,11.3052719704381));
#65155=CARTESIAN_POINT('Ctrl Pts',(0.507921841603943,77.2263631561244,11.3052735831766));
#65156=CARTESIAN_POINT('Ctrl Pts',(0.507928976052952,77.2263640588436,11.3052751959543));
#65157=CARTESIAN_POINT('Ctrl Pts',(0.587522134718372,77.2364349519282,11.3232676252247));
#65158=CARTESIAN_POINT('Ctrl Pts',(0.666100435522896,77.2465264961178,11.3460970025154));
#65159=CARTESIAN_POINT('Ctrl Pts',(0.743194502175447,77.2566484730819,11.3735298284475));
#65160=CARTESIAN_POINT('Ctrl Pts',(0.821686836697399,77.2669540340206,11.401460208092));
#65161=CARTESIAN_POINT('Ctrl Pts',(0.898640612120766,77.2772913354049,11.4341640505644));
#65162=CARTESIAN_POINT('Ctrl Pts',(0.973518518869272,77.2876640329312,11.4714023624243));
#65163=CARTESIAN_POINT('Ctrl Pts',(1.04830534795594,77.298024113638,11.5085953795034));
#65164=CARTESIAN_POINT('Ctrl Pts',(1.12102068657583,77.3084196510644,11.5503131175396));
#65165=CARTESIAN_POINT('Ctrl Pts',(1.19109289573764,77.3188451736256,11.5963036137688));
#65166=CARTESIAN_POINT('Ctrl Pts',(1.26064147502899,77.3291927891949,11.6419504359812));
#65167=CARTESIAN_POINT('Ctrl Pts',(1.32758505909059,77.3395700470451,11.69180718385));
#65168=CARTESIAN_POINT('Ctrl Pts',(1.39134313883558,77.3499607493381,11.7455983626169));
#65169=CARTESIAN_POINT('Ctrl Pts',(1.40192323838504,77.351684996133,11.7545245415187));
#65170=CARTESIAN_POINT('Ctrl Pts',(1.41241559772089,77.3534095869227,11.7635589824088));
#65171=CARTESIAN_POINT('Ctrl Pts',(1.42281754746619,77.3551344158924,11.7727003302305));
#65172=CARTESIAN_POINT('Ctrl Pts',(1.42282233205405,77.3551352092624,11.772704534979));
#65173=CARTESIAN_POINT('Ctrl Pts',(1.42282711662277,77.3551360026326,11.77270873975));
#65174=CARTESIAN_POINT('Ctrl Pts',(1.42283190117237,77.3551367960028,11.7727129445437));
#65175=CARTESIAN_POINT('Ctrl Pts',(1.49178772355645,77.3665709952717,11.83331321602));
#65176=CARTESIAN_POINT('Ctrl Pts',(1.55686292742098,77.3781202132658,11.8986606409092));
#65177=CARTESIAN_POINT('Ctrl Pts',(1.61748310439179,77.3896949852914,11.9680812937928));
#65178=CARTESIAN_POINT('Ctrl Pts',(1.62634461250205,77.3913869951354,11.9782292628237));
#65179=CARTESIAN_POINT('Ctrl Pts',(1.63511096716908,77.3930795478172,11.9884641933827));
#65180=CARTESIAN_POINT('Ctrl Pts',(1.64378042463416,77.3947723606193,11.9987839027811));
#65181=CARTESIAN_POINT('Ctrl Pts',(1.70831329689349,77.4073731574692,12.0756007613956));
#65182=CARTESIAN_POINT('Ctrl Pts',(1.76748340896777,77.4199876766516,12.1571160574602));
#65183=CARTESIAN_POINT('Ctrl Pts',(1.82069415277911,77.4325363819662,12.2426072139777));
#65184=CARTESIAN_POINT('Ctrl Pts',(1.82353306578513,77.4332058836528,12.2471683596929));
#65185=CARTESIAN_POINT('Ctrl Pts',(1.82635503030065,77.4338752086482,12.2517408672331));
#65186=CARTESIAN_POINT('Ctrl Pts',(1.82915995940703,77.4345443486145,12.2563246423749));
#65187=CARTESIAN_POINT('Ctrl Pts',(1.88152687236951,77.4470369261602,12.3419019046812));
#65188=CARTESIAN_POINT('Ctrl Pts',(1.92796415656752,77.4594676719648,12.4314258227001));
#65189=CARTESIAN_POINT('Ctrl Pts',(1.96781410106725,77.4719740172061,12.5240025913411));
#65190=CARTESIAN_POINT('Ctrl Pts',(1.98315658591846,77.4767890405347,12.5596452424985));
#65191=CARTESIAN_POINT('Ctrl Pts',(1.9975217601537,77.4816149068815,12.5957378830938));
#65192=CARTESIAN_POINT('Ctrl Pts',(2.01087099221024,77.4864577737665,12.6322193067018));
#65193=CARTESIAN_POINT('Ctrl Pts',(2.0108720939687,77.4864581734651,12.6322223176403));
#65194=CARTESIAN_POINT('Ctrl Pts',(2.01087319572024,77.4864585731638,12.6322253285815));
#65195=CARTESIAN_POINT('Ctrl Pts',(2.01087429746486,77.4864589728627,12.6322283395253));
#65196=CARTESIAN_POINT('Ctrl Pts',(2.04106169996882,77.4974105760809,12.7147271066467));
#65197=CARTESIAN_POINT('Ctrl Pts',(2.06608403955404,77.5084003137361,12.7993526711409));
#65198=CARTESIAN_POINT('Ctrl Pts',(2.08580312643331,77.5194164056155,12.8853238092665));
#65199=CARTESIAN_POINT('Ctrl Pts',(2.08730391839802,77.5202548248728,12.8918669516587));
#65200=CARTESIAN_POINT('Ctrl Pts',(2.08877401506984,77.5210933966942,12.8984178811239));
#65201=CARTESIAN_POINT('Ctrl Pts',(2.09021336741114,77.5219321158401,12.9049762501793));
#65202=CARTESIAN_POINT('Ctrl Pts',(2.10996961694659,77.5334441996157,12.9949950536975));
#65203=CARTESIAN_POINT('Ctrl Pts',(2.12393616280023,77.5449809014144,13.0864086301881));
#65204=CARTESIAN_POINT('Ctrl Pts',(2.13200609891081,77.556523293635,13.1785445195497));
#65205=CARTESIAN_POINT('Ctrl Pts',(2.13423662267569,77.559713601439,13.2040108042889));
#65206=CARTESIAN_POINT('Ctrl Pts',(2.13601636211932,77.5629043424034,13.2295323125144));
#65207=CARTESIAN_POINT('Ctrl Pts',(2.13734235872415,77.5660951135256,13.2550948890815));
#65208=CARTESIAN_POINT('Ctrl Pts',(2.14232969036316,77.5780962255288,13.3512407211473));
#65209=CARTESIAN_POINT('Ctrl Pts',(2.14089489791625,77.5901027681026,13.4479841449771));
#65210=CARTESIAN_POINT('Ctrl Pts',(2.13289656690917,77.6021470596629,13.5443487324733));
#65211=CARTESIAN_POINT('Ctrl Pts',(2.13107517228774,77.6048898078497,13.5662930532581));
#65212=CARTESIAN_POINT('Ctrl Pts',(2.12891362379868,77.6076345153341,13.5882177374866));
#65213=CARTESIAN_POINT('Ctrl Pts',(2.12641063000288,77.6103815666591,13.6101112935434));
#65214=CARTESIAN_POINT('Ctrl Pts',(2.1236052103067,77.6134605322987,13.6346501531619));
#65215=CARTESIAN_POINT('Ctrl Pts',(2.12037088223282,77.6165423238692,13.6591495531585));
#65216=CARTESIAN_POINT('Ctrl Pts',(2.11670601944608,77.6196280495591,13.6835941296998));
#65217=CARTESIAN_POINT('Ctrl Pts',(2.11670524046315,77.6196287054439,13.6835993255035));
#65218=CARTESIAN_POINT('Ctrl Pts',(2.11670446146078,77.6196293613288,13.6836045213047));
#65219=CARTESIAN_POINT('Ctrl Pts',(2.11670368243896,77.6196300172139,13.6836097171035));
#65220=CARTESIAN_POINT('Ctrl Pts',(2.09538566729208,77.6375783829701,13.8257933032405));
#65221=CARTESIAN_POINT('Ctrl Pts',(2.05947832160496,77.655611188779,13.9662187126111));
#65222=CARTESIAN_POINT('Ctrl Pts',(2.0099402891869,77.673671542634,14.1021424064051));
#65223=CARTESIAN_POINT('Ctrl Pts',(1.98606321552611,77.6823765391444,14.1676569190038));
#65224=CARTESIAN_POINT('Ctrl Pts',(1.95901852711184,77.6910885492128,14.2321287723318));
#65225=CARTESIAN_POINT('Ctrl Pts',(1.9289030818708,77.6998046301978,14.2952632597381));
#65226=CARTESIAN_POINT('Ctrl Pts',(1.88358371898808,77.7129210637724,14.3902714763619));
#65227=CARTESIAN_POINT('Ctrl Pts',(1.83129880201968,77.7260495789763,14.4822625088632));
#65228=CARTESIAN_POINT('Ctrl Pts',(1.7724595102298,77.7392058631395,14.5700920668984));
#65229=CARTESIAN_POINT('Ctrl Pts',(1.7492554525336,77.744394218871,14.604728821864));
#65230=CARTESIAN_POINT('Ctrl Pts',(1.72503253993325,77.7495868944068,14.6387186414649));
#65231=CARTESIAN_POINT('Ctrl Pts',(1.69981784227148,77.7547848549544,14.6719926195448));
#65232=CARTESIAN_POINT('Ctrl Pts',(1.69981660386776,77.7547851102489,14.671994253775));
#65233=CARTESIAN_POINT('Ctrl Pts',(1.69981536546164,77.7547853655434,14.6719958880034));
#65234=CARTESIAN_POINT('Ctrl Pts',(1.69981412705314,77.7547856208379,14.67199752223));
#65235=CARTESIAN_POINT('Ctrl Pts',(1.64313040410961,77.7664708153475,14.7467984065401));
#65236=CARTESIAN_POINT('Ctrl Pts',(1.58143200068949,77.7782306262676,14.8179957495507));
#65237=CARTESIAN_POINT('Ctrl Pts',(1.51529722136469,77.7900116645491,14.8850828315672));
#65238=CARTESIAN_POINT('Ctrl Pts',(1.44377162948131,77.8027530049556,14.957638350735));
#65239=CARTESIAN_POINT('Ctrl Pts',(1.36704130178963,77.8155220989792,15.0254047507615));
#65240=CARTESIAN_POINT('Ctrl Pts',(1.28579953138186,77.8283149763608,15.0877474472356));
#65241=CARTESIAN_POINT('Ctrl Pts',(1.20448669408966,77.8411190444136,15.150144678479));
#65242=CARTESIAN_POINT('Ctrl Pts',(1.11865162134025,77.8539471269003,15.207104864544));
#65243=CARTESIAN_POINT('Ctrl Pts',(1.02907503919655,77.8667820022936,15.2579246110916));
#65244=CARTESIAN_POINT('Ctrl Pts',(0.970030639997629,77.875242109704,15.2914224442365));
#65245=CARTESIAN_POINT('Ctrl Pts',(0.909362676786896,77.8837048759993,15.3222509845227));
#65246=CARTESIAN_POINT('Ctrl Pts',(0.847321744242881,77.8921618205561,15.3502070063442));
#65247=CARTESIAN_POINT('Ctrl Pts',(0.847318445389668,77.8921622702304,15.3502084928275));
#65248=CARTESIAN_POINT('Ctrl Pts',(0.847315146532601,77.8921627199048,15.3502099793027));
#65249=CARTESIAN_POINT('Ctrl Pts',(0.847311847671628,77.8921631695792,15.3502114657698));
#65250=CARTESIAN_POINT('Ctrl Pts',(0.751839703651021,77.9051771691595,15.3932312238575));
#65251=CARTESIAN_POINT('Ctrl Pts',(0.653001772150457,77.9182546770568,15.4295023368545));
#65252=CARTESIAN_POINT('Ctrl Pts',(0.551921930566669,77.9313687437658,15.4587289085861));
#65253=CARTESIAN_POINT('Ctrl Pts',(0.546319225166615,77.9320956369941,15.4603488940224));
#65254=CARTESIAN_POINT('Ctrl Pts',(0.540709636524094,77.9328226424649,15.4619472488097));
#65255=CARTESIAN_POINT('Ctrl Pts',(0.535093357459425,77.9335497555618,15.4635239269901));
#65256=CARTESIAN_POINT('Ctrl Pts',(0.433033464499162,77.9467629673682,15.4921755670641));
#65257=CARTESIAN_POINT('Ctrl Pts',(0.328762471159584,77.9600120971272,15.5136736717721));
#65258=CARTESIAN_POINT('Ctrl Pts',(0.223256850228694,77.9732939102643,15.5277683984637));
#65259=CARTESIAN_POINT('Ctrl Pts',(0.113355082324048,77.987129142282,15.5424504160459));
#65260=CARTESIAN_POINT('Ctrl Pts',(0.0020733120532726,78.0010049627816,
15.549097396372));
#65261=CARTESIAN_POINT('Ctrl Pts',(-0.109329002057391,78.0149269846661,
15.5473790722238));
#65262=CARTESIAN_POINT('Ctrl Pts',(-0.153880271922976,78.0204945867308,
15.5466918915001));
#65263=CARTESIAN_POINT('Ctrl Pts',(-0.198447432834363,78.0260691514268,
15.5446669978625));
#65264=CARTESIAN_POINT('Ctrl Pts',(-0.242936648274478,78.0316492858954,
15.5412872090875));
#65265=CARTESIAN_POINT('Ctrl Pts',(-0.347325188771049,78.0447423936787,
15.5333569452266));
#65266=CARTESIAN_POINT('Ctrl Pts',(-0.451458589162047,78.0578354273157,
15.5179519585374));
#65267=CARTESIAN_POINT('Ctrl Pts',(-0.554255689722849,78.0709375224221,
15.4953540740277));
#65268=CARTESIAN_POINT('Ctrl Pts',(-0.577203339882884,78.0738623354103,
15.4903094925632));
#65269=CARTESIAN_POINT('Ctrl Pts',(-0.600084417394092,78.0767875992885,
15.4849066746044));
#65270=CARTESIAN_POINT('Ctrl Pts',(-0.62288694974159,78.079713414447,15.4791491029078));
#65271=CARTESIAN_POINT('Ctrl Pts',(-0.748692098686231,78.0958555957712,
15.4473836764269));
#65272=CARTESIAN_POINT('Ctrl Pts',(-0.872105958835944,78.1120145928236,
15.4048215640543));
#65273=CARTESIAN_POINT('Ctrl Pts',(-0.991312055030119,78.1282337846007,
15.3520022596885));
#65274=CARTESIAN_POINT('Ctrl Pts',(-1.06979246515111,78.1389118360018,15.3172281935855));
#65275=CARTESIAN_POINT('Ctrl Pts',(-1.14645373737088,78.1496165478377,15.2780078421207));
#65276=CARTESIAN_POINT('Ctrl Pts',(-1.22081454342312,78.1603660617898,15.2344625968421));
#65277=CARTESIAN_POINT('Ctrl Pts',(-1.25027921111984,78.1646254408003,15.217208262872));
#65278=CARTESIAN_POINT('Ctrl Pts',(-1.2793831890253,78.1688919399429,15.1992742662859));
#65279=CARTESIAN_POINT('Ctrl Pts',(-1.30809417781881,78.1731652012549,15.1806685500313));
#65280=CARTESIAN_POINT('Ctrl Pts',(-1.30812371705732,78.1731695977905,15.1806494075805));
#65281=CARTESIAN_POINT('Ctrl Pts',(-1.30815325587059,78.1731739943298,15.1806302644248));
#65282=CARTESIAN_POINT('Ctrl Pts',(-1.30818279425854,78.1731783908727,15.1806111205643));
#65283=CARTESIAN_POINT('Ctrl Pts',(-1.41737792056874,78.189431175567,15.109841643521));
#65284=CARTESIAN_POINT('Ctrl Pts',(-1.5207631788598,78.2057337640861,15.0294435545618));
#65285=CARTESIAN_POINT('Ctrl Pts',(-1.61694821230293,78.2220782538494,14.9406692825966));
#65286=CARTESIAN_POINT('Ctrl Pts',(-1.62982206252277,78.2242658760355,14.9287873230054));
#65287=CARTESIAN_POINT('Ctrl Pts',(-1.64256688192539,78.2264542493202,14.916755246334));
#65288=CARTESIAN_POINT('Ctrl Pts',(-1.65517929332439,78.2286433552017,14.9045760001642));
#65289=CARTESIAN_POINT('Ctrl Pts',(-1.76407406223872,78.2475439580723,14.7994211526694));
#65290=CARTESIAN_POINT('Ctrl Pts',(-1.86309701647429,78.2664987986576,14.6832927316156));
#65291=CARTESIAN_POINT('Ctrl Pts',(-1.94996231045361,78.285474771462,14.5582134121645));
#65292=CARTESIAN_POINT('Ctrl Pts',(-1.99849692699484,78.2960772977573,14.4883273100322));
#65293=CARTESIAN_POINT('Ctrl Pts',(-2.04323398820215,78.3066860509469,14.415649484336));
#65294=CARTESIAN_POINT('Ctrl Pts',(-2.08377078159536,78.3172933926086,14.3405580188543));
#65295=CARTESIAN_POINT('Ctrl Pts',(-2.08378709230659,78.3172976606642,14.3405278044464));
#65296=CARTESIAN_POINT('Ctrl Pts',(-2.0838034023366,78.3173019287196,14.3404975896503));
#65297=CARTESIAN_POINT('Ctrl Pts',(-2.08381971168551,78.3173061967748,14.3404673744656));
#65298=CARTESIAN_POINT('Ctrl Pts',(-2.12724565660621,78.3286704967171,14.260015178002));
#65299=CARTESIAN_POINT('Ctrl Pts',(-2.16584353660947,78.3400337477527,14.1768104245508));
#65300=CARTESIAN_POINT('Ctrl Pts',(-2.19948308923245,78.3514450876868,14.0914575837564));
#65301=CARTESIAN_POINT('Ctrl Pts',(-2.2475372827229,78.3677462181841,13.9695308158096));
#65302=CARTESIAN_POINT('Ctrl Pts',(-2.28549512559791,78.3841529438893,13.8431691311632));
#65303=CARTESIAN_POINT('Ctrl Pts',(-2.31292841914167,78.4006375907827,13.7141136233115));
#65304=CARTESIAN_POINT('Ctrl Pts',(-2.32514673585844,78.4079795687478,13.656634521633));
#65305=CARTESIAN_POINT('Ctrl Pts',(-2.33527668108419,78.4153370111229,13.5986208868508));
#65306=CARTESIAN_POINT('Ctrl Pts',(-2.3432770851121,78.4227075131537,13.5402262096473));
#65307=CARTESIAN_POINT('Ctrl Pts',(-2.35893393412833,78.437131639369,13.4259474005852));
#65308=CARTESIAN_POINT('Ctrl Pts',(-2.36643003500849,78.451603907741,13.3102103371841));
#65309=CARTESIAN_POINT('Ctrl Pts',(-2.36545462636837,78.4660907289047,13.1943147466042));
#65310=CARTESIAN_POINT('Ctrl Pts',(-2.3648207581295,78.4755049738069,13.1190001237149));
#65311=CARTESIAN_POINT('Ctrl Pts',(-2.36061034689751,78.4849253656596,13.0436188684554));
#65312=CARTESIAN_POINT('Ctrl Pts',(-2.35274996603477,78.4943427127835,12.968527724849));
#65313=CARTESIAN_POINT('Ctrl Pts',(-2.34751826938446,78.5006106919392,12.9185487109394));
#65314=CARTESIAN_POINT('Ctrl Pts',(-2.3406699929971,78.5068771835314,12.868701506355));
#65315=CARTESIAN_POINT('Ctrl Pts',(-2.33218792754542,78.5131394588166,12.819097278665));
#65316=CARTESIAN_POINT('Ctrl Pts',(-2.33218084850186,78.5131446852463,12.8190558794928));
#65317=CARTESIAN_POINT('Ctrl Pts',(-2.33217376831915,78.5131499116753,12.8190144804834));
#65318=CARTESIAN_POINT('Ctrl Pts',(-2.33216668699728,78.5131551381034,12.8189730816368));
#65319=CARTESIAN_POINT('Ctrl Pts',(-2.31698524176577,78.5243599291308,12.7302192680173));
#65320=CARTESIAN_POINT('Ctrl Pts',(-2.29656927625846,78.5355608981172,12.6422135313059));
#65321=CARTESIAN_POINT('Ctrl Pts',(-2.27116370661245,78.5468272037072,12.5554795194696));
#65322=CARTESIAN_POINT('Ctrl Pts',(-2.2368150186937,78.5620594075152,12.4382139140918));
#65323=CARTESIAN_POINT('Ctrl Pts',(-2.19333698767226,78.5774162578449,12.3232372644642));
#65324=CARTESIAN_POINT('Ctrl Pts',(-2.14131353447015,78.5928567706968,12.2118170719353));
#65325=CARTESIAN_POINT('Ctrl Pts',(-2.12842492193079,78.5966820989921,12.1842131432805));
#65326=CARTESIAN_POINT('Ctrl Pts',(-2.11501156929086,78.6005125671688,12.1568275809929));
#65327=CARTESIAN_POINT('Ctrl Pts',(-2.10108189738572,78.6043475619254,12.1296798495071));
#65328=CARTESIAN_POINT('Ctrl Pts',(-2.0357411851411,78.6223365921446,12.0023364258291));
#65329=CARTESIAN_POINT('Ctrl Pts',(-1.95903634319664,78.6404233998862,11.8802289007183));
#65330=CARTESIAN_POINT('Ctrl Pts',(-1.87195445874316,78.6585095289508,11.7655542465218));
#65331=CARTESIAN_POINT('Ctrl Pts',(-1.86692715734923,78.6595536545164,11.7589339941867));
#65332=CARTESIAN_POINT('Ctrl Pts',(-1.86186528308215,78.6605977783431,11.7523385067422));
#65333=CARTESIAN_POINT('Ctrl Pts',(-1.85676903010409,78.6616418816847,11.7457682038198));
#65334=CARTESIAN_POINT('Ctrl Pts',(-1.79446025389726,78.67440749629,11.6654371181837));
#65335=CARTESIAN_POINT('Ctrl Pts',(-1.72701058074564,78.6871690082607,11.5888748317974));
#65336=CARTESIAN_POINT('Ctrl Pts',(-1.65483746441543,78.6998883415336,11.5168887899053));
#65337=CARTESIAN_POINT('Ctrl Pts',(-1.6279452206241,78.7046276603912,11.4900662514509));
#65338=CARTESIAN_POINT('Ctrl Pts',(-1.60039753415085,78.7093611264458,11.4638786844688));
#65339=CARTESIAN_POINT('Ctrl Pts',(-1.57221713776477,78.7140867817196,11.4383663647336));
#65340=CARTESIAN_POINT('Ctrl Pts',(-1.57220858679433,78.7140882156575,11.4383586233559));
#65341=CARTESIAN_POINT('Ctrl Pts',(-1.57220003576561,78.7140896495947,11.4383508820403));
#65342=CARTESIAN_POINT('Ctrl Pts',(-1.57219148467867,78.7140910835312,11.438343140787));
#65343=CARTESIAN_POINT('Ctrl Pts',(-1.50634963536783,78.7251321394107,11.3787368660992));
#65344=CARTESIAN_POINT('Ctrl Pts',(-1.43701291110985,78.7361571730373,11.3227866844017));
#65345=CARTESIAN_POINT('Ctrl Pts',(-1.3646606564299,78.7472508903118,11.2707448125877));
#65346=CARTESIAN_POINT('Ctrl Pts',(-1.25704704269546,78.7637512054844,11.193339983724));
#65347=CARTESIAN_POINT('Ctrl Pts',(-1.14273590660334,78.780408671037,11.1245581429311));
#65348=CARTESIAN_POINT('Ctrl Pts',(-1.02326272375693,78.7971727676276,11.0651276515219));
#65349=CARTESIAN_POINT('Ctrl Pts',(-1.00348002954322,78.7999486122877,11.055286989287));
#65350=CARTESIAN_POINT('Ctrl Pts',(-0.983555729790525,78.8027273840396,
11.0457028076324));
#65351=CARTESIAN_POINT('Ctrl Pts',(-0.963496713582175,78.8055088578284,
11.0363785244326));
#65352=CARTESIAN_POINT('Ctrl Pts',(-0.820137989090681,78.8253876260803,
10.9697392968433));
#65353=CARTESIAN_POINT('Ctrl Pts',(-0.669897993251188,78.8454022618114,
10.9163786242148));
#65354=CARTESIAN_POINT('Ctrl Pts',(-0.515481627642138,78.8654394717011,
10.8776113001209));
#65355=CARTESIAN_POINT('Ctrl Pts',(-0.40414780216269,78.8798862514849,10.8496601533759));
#65356=CARTESIAN_POINT('Ctrl Pts',(-0.290644999770457,78.8943437228425,
10.8292975903655));
#65357=CARTESIAN_POINT('Ctrl Pts',(-0.176056080459361,78.9087697597579,
10.8170014127815));
#65358=CARTESIAN_POINT('Ctrl Pts',(-0.147309435278708,78.9123887847654,
10.8139167004357));
#65359=CARTESIAN_POINT('Ctrl Pts',(-0.118494434526164,78.9160058347536,
10.8113393877997));
#65360=CARTESIAN_POINT('Ctrl Pts',(-0.0896281377141354,78.9196202514175,
10.809276495863));
#65361=CARTESIAN_POINT('Ctrl Pts',(-0.0895780721078092,78.9196265202494,
10.8092729179903));
#65362=CARTESIAN_POINT('Ctrl Pts',(-0.0895280063471258,78.9196327890733,
10.809269341665));
#65363=CARTESIAN_POINT('Ctrl Pts',(-0.0894779404322766,78.9196390578894,
10.8092657668871));
#65364=CARTESIAN_POINT('Ctrl Pts',(-0.0189960371881366,78.9284641854592,
10.8042332581691));
#65365=CARTESIAN_POINT('Ctrl Pts',(0.0518292881978163,78.9372714066356,
10.8022646760837));
#65366=CARTESIAN_POINT('Ctrl Pts',(0.122616109482706,78.9461112930357,10.8033530299608));
#65367=CARTESIAN_POINT('Ctrl Pts',(0.139060825042286,78.9481649156563,10.8036058689725));
#65368=CARTESIAN_POINT('Ctrl Pts',(0.155503594876505,78.9502202956633,10.8040235450871));
#65369=CARTESIAN_POINT('Ctrl Pts',(0.171939877407273,78.952278049441,10.8046057292954));
#65370=CARTESIAN_POINT('Ctrl Pts',(3.10725610873535,87.7143427064635,13.0695248188307));
#65371=CARTESIAN_POINT('Ctrl Pts',(3.1757813234749,87.8112593268296,13.8431174629201));
#65372=CARTESIAN_POINT('Ctrl Pts',(2.70607125735979,88.0061219845433,15.451413371914));
#65373=CARTESIAN_POINT('Ctrl Pts',(0.523695573931209,88.3010140160292,16.7441283328975));
#65374=CARTESIAN_POINT('Ctrl Pts',(-1.97106212602582,88.5980351971415,16.2018249379459));
#65375=CARTESIAN_POINT('Ctrl Pts',(-3.43495695755572,88.8966756526658,14.0914727997129));
#65376=CARTESIAN_POINT('Ctrl Pts',(-3.06482110497942,89.196419298767,11.5400069829436));
#65377=CARTESIAN_POINT('Ctrl Pts',(-1.05291748826742,89.4967419819177,9.92398169476627));
#65378=CARTESIAN_POINT('Ctrl Pts',(1.52616256504467,89.7971047842489,10.1087303766691));
#65379=CARTESIAN_POINT('Ctrl Pts',(3.21140767063859,90.0858783146224,11.9293218383111));
#65380=CARTESIAN_POINT('Ctrl Pts',(3.30323743242567,90.3626559668299,14.276240933303));
#65381=CARTESIAN_POINT('Ctrl Pts',(1.98789207577699,90.627200204105,16.0898027557638));
#65382=CARTESIAN_POINT('Ctrl Pts',(0.0241974623197764,90.86830082554,16.6489912297625));
#65383=CARTESIAN_POINT('Ctrl Pts',(-1.69368084010089,91.0861200642671,16.1049922105906));
#65384=CARTESIAN_POINT('Ctrl Pts',(-2.81033338844852,91.2809643968551,14.9452095342079));
#65385=CARTESIAN_POINT('Ctrl Pts',(-3.23146979160152,91.4744780596263,13.4011379073283));
#65386=CARTESIAN_POINT('Ctrl Pts',(-2.86407265519059,91.6665312140481,11.8566330885878));
#65387=CARTESIAN_POINT('Ctrl Pts',(-1.80990108569908,91.8569947753109,10.6866444426581));
#65388=CARTESIAN_POINT('Ctrl Pts',(-0.337754813899104,92.0457495597246,
10.1687628870289));
#65389=CARTESIAN_POINT('Ctrl Pts',(1.18763110189629,92.2326830579912,10.4178406020297));
#65390=CARTESIAN_POINT('Ctrl Pts',(2.39508588402732,92.4176866578788,11.3569396665519));
#65391=CARTESIAN_POINT('Ctrl Pts',(2.99846077048866,92.6006617408029,12.7442190178643));
#65392=CARTESIAN_POINT('Ctrl Pts',(2.86406492662596,92.7815187653892,14.2338326625746));
#65393=CARTESIAN_POINT('Ctrl Pts',(2.04358132087385,92.9601718455146,15.4619408054085));
#65394=CARTESIAN_POINT('Ctrl Pts',(0.751296929799555,93.1365472418599,16.1382458662903));
#65395=CARTESIAN_POINT('Ctrl Pts',(-0.687290894650869,93.3105782793599,
16.1133154333185));
#65396=CARTESIAN_POINT('Ctrl Pts',(-1.92137415892804,93.4822078008889,15.4121948543585));
#65397=CARTESIAN_POINT('Ctrl Pts',(-2.65731745584422,93.6513873028849,14.2229713817855));
#65398=CARTESIAN_POINT('Ctrl Pts',(-2.72467523247443,93.7995574197688,12.9993478101219));
#65399=CARTESIAN_POINT('Ctrl Pts',(-2.35680632127026,93.9275748885119,12.0272037600701));
#65400=CARTESIAN_POINT('Ctrl Pts',(-1.60700565797264,94.072380504393,11.1189899717487));
#65401=CARTESIAN_POINT('Ctrl Pts',(-0.203446123334107,94.2505639771652,
10.5658090747328));
#65402=CARTESIAN_POINT('Ctrl Pts',(1.49575309669785,94.4598530632153,11.0726893252092));
#65403=CARTESIAN_POINT('Ctrl Pts',(2.49678227792913,94.6646318210984,12.4902982018984));
#65404=CARTESIAN_POINT('Ctrl Pts',(2.42399981467692,94.831561367221,13.9024753634234));
#65405=CARTESIAN_POINT('Ctrl Pts',(1.93577122333525,94.9464973222074,14.6988423857405));
#65406=CARTESIAN_POINT('Ctrl Pts',(1.60855744696839,95.003490707163,15.0199806827984));
#65407=CARTESIAN_POINT('Ctrl Pts',(1.40135621667452,95.0359246481305,15.1765886648261));
#65408=CARTESIAN_POINT('Ctrl Pts',(0.635078339402144,95.1491319775694,15.6724562054475));
#65409=CARTESIAN_POINT('Ctrl Pts',(-0.720559162425314,95.3000177856171,
15.6863625542683));
#65410=CARTESIAN_POINT('Ctrl Pts',(-1.8708747810453,95.4860536506094,14.6538899840269));
#65411=CARTESIAN_POINT('Ctrl Pts',(-2.16058008250562,95.5890455651222,13.8568424348098));
#65412=CARTESIAN_POINT('Ctrl Pts',(-2.17993256337463,95.6570456913322,13.3104242948812));
#65413=CARTESIAN_POINT('Ctrl Pts',(-2.1480847252082,95.702204137361,12.9493357867975));
#65414=CARTESIAN_POINT('Ctrl Pts',(-2.02450479564091,95.7583256112684,12.5130496666982));
#65415=CARTESIAN_POINT('Ctrl Pts',(-1.75360435091691,95.8251694120019,12.0460412039888));
#65416=CARTESIAN_POINT('Ctrl Pts',(-1.37849074783188,95.8915126624859,11.6632242622581));
#65417=CARTESIAN_POINT('Ctrl Pts',(-0.923748479397676,95.9573798229221,
11.387018956129));
#65418=CARTESIAN_POINT('Ctrl Pts',(-0.418445576848205,96.0227717513124,
11.2327055835173));
#65419=CARTESIAN_POINT('Ctrl Pts',(0.105520528106774,96.0877139012382,11.2084459531777));
#65420=CARTESIAN_POINT('Ctrl Pts',(0.786338536997495,96.1737086069401,11.3479552873821));
#65421=CARTESIAN_POINT('Ctrl Pts',(1.52303500717221,96.2801377489088,11.8291464763594));
#65422=CARTESIAN_POINT('Ctrl Pts',(2.01715667209892,96.4062625436115,12.7482521021039));
#65423=CARTESIAN_POINT('Ctrl Pts',(2.01045790345397,96.5309261038632,13.7793624143205));
#65424=CARTESIAN_POINT('Ctrl Pts',(1.51637800664929,96.6542580992801,14.6719798136283));
#65425=CARTESIAN_POINT('Ctrl Pts',(0.663888543978092,96.7763970615423,15.2136124389558));
#65426=CARTESIAN_POINT('Ctrl Pts',(-0.336049672007484,96.8974833143649,
15.2806088470557));
#65427=CARTESIAN_POINT('Ctrl Pts',(-1.23702901529549,97.0176655564635,14.8631858266175));
#65428=CARTESIAN_POINT('Ctrl Pts',(-1.89420479903932,97.1503580247946,13.982436534616));
#65429=CARTESIAN_POINT('Ctrl Pts',(-1.96193864187616,97.2954556790466,12.7556076580179));
#65430=CARTESIAN_POINT('Ctrl Pts',(-1.19721912475719,97.4530355758608,11.6597400684424));
#65431=CARTESIAN_POINT('Ctrl Pts',(-0.0281587723358688,97.5971720203736,
11.306636794884));
#65432=CARTESIAN_POINT('Ctrl Pts',(1.01129169438915,97.7282311720686,11.6161391384085));
#65433=CARTESIAN_POINT('Ctrl Pts',(1.70064661125628,97.8463613303911,12.3082123810528));
#65434=CARTESIAN_POINT('Ctrl Pts',(1.97428043926036,97.9648262448885,13.249425353759));
#65435=CARTESIAN_POINT('Ctrl Pts',(1.76313138826258,98.0837817071748,14.2102217464921));
#65436=CARTESIAN_POINT('Ctrl Pts',(1.11322929763875,98.203378013067,14.956581570516));
#65437=CARTESIAN_POINT('Ctrl Pts',(0.257678298166416,98.3137402058402,15.2727661476035));
#65438=CARTESIAN_POINT('Ctrl Pts',(-0.728874592332793,98.4349564865196,
15.191430874777));
#65439=CARTESIAN_POINT('Ctrl Pts',(-1.58805687481121,98.5572254947863,14.6275712205838));
#65440=CARTESIAN_POINT('Ctrl Pts',(-2.044720159798,98.6911826223687,13.6163889972621));
#65441=CARTESIAN_POINT('Ctrl Pts',(-1.98673559372465,98.7849432279802,12.8437627048067));
#65442=CARTESIAN_POINT('Ctrl Pts',(-1.73073495584116,98.8689105869503,12.2196452596691));
#65443=CARTESIAN_POINT('Ctrl Pts',(-1.32097441252665,98.9533854474619,11.6654502341919));
#65444=CARTESIAN_POINT('Ctrl Pts',(-0.660793794475513,99.0441439765671,
11.3083813226462));
#65445=CARTESIAN_POINT('Ctrl Pts',(-0.0598969890390443,99.1195820525141,
11.218007253297));
#65446=CARTESIAN_POINT('Ctrl Pts',(0.462847266033453,99.1845785155341,11.2370733537587));
#65447=CARTESIAN_POINT('Ctrl Pts',(1.09828510826303,99.2664639660505,11.4455188681155));
#65448=CARTESIAN_POINT('Ctrl Pts',(1.72023525244675,99.3657958818357,11.9636756035441));
#65449=CARTESIAN_POINT('Ctrl Pts',(2.25134488151769,99.4997248277813,12.9196203077091));
#65450=CARTESIAN_POINT('Ctrl Pts',(2.16906732596622,99.6700195549317,14.380884605866));
#65451=CARTESIAN_POINT('Ctrl Pts',(1.2485647484992,99.818254361804,15.2625087202804));
#65452=CARTESIAN_POINT('Ctrl Pts',(0.444576618744897,99.9243407315245,15.5426355963576));
#65453=CARTESIAN_POINT('Ctrl Pts',(-0.124650265136175,99.9954998612222,
15.6294832306231));
#65454=CARTESIAN_POINT('Ctrl Pts',(-0.918737021005253,100.094399188943,
15.4865591877427));
#65455=CARTESIAN_POINT('Ctrl Pts',(-1.67679364799143,100.203632794597,15.0184860900645));
#65456=CARTESIAN_POINT('Ctrl Pts',(-2.12728633876912,100.295798559161,14.4164680057849));
#65457=CARTESIAN_POINT('Ctrl Pts',(-2.44385567388375,100.407434629731,13.5761810060226));
#65458=CARTESIAN_POINT('Ctrl Pts',(-2.43349609112601,100.558140077718,12.3181762302894));
#65459=CARTESIAN_POINT('Ctrl Pts',(-1.71815741033316,100.692891281568,11.40887510621));
#65460=CARTESIAN_POINT('Ctrl Pts',(-1.17713165256918,100.770845395039,11.0964290332353));
#65461=CARTESIAN_POINT('Ctrl Pts',(2.90276395212938,88.0589545760158,13.0875997250314));
#65462=CARTESIAN_POINT('Ctrl Pts',(2.95627977768387,88.1495677453682,13.8115623287023));
#65463=CARTESIAN_POINT('Ctrl Pts',(2.49516168027059,88.330846998084,15.3000193606636));
#65464=CARTESIAN_POINT('Ctrl Pts',(0.465788387492445,88.6026204963471,16.4588062976629));
#65465=CARTESIAN_POINT('Ctrl Pts',(-1.80476146413435,88.8739729860722,15.9279676833003));
#65466=CARTESIAN_POINT('Ctrl Pts',(-3.10155536278043,89.1446181204072,13.9957909307606));
#65467=CARTESIAN_POINT('Ctrl Pts',(-2.73404191397397,89.4142810240402,11.7062879228243));
#65468=CARTESIAN_POINT('Ctrl Pts',(-0.915092544492909,89.682695115903,10.2891619118715));
#65469=CARTESIAN_POINT('Ctrl Pts',(1.37353687594359,89.949600710797,10.486936929915));
#65470=CARTESIAN_POINT('Ctrl Pts',(2.83987558909873,90.2049373800204,12.1177004430502));
#65471=CARTESIAN_POINT('Ctrl Pts',(2.89136847089987,90.4487224978189,14.1852973727042));
#65472=CARTESIAN_POINT('Ctrl Pts',(1.71420211019153,90.6810455124534,15.7611841780058));
#65473=CARTESIAN_POINT('Ctrl Pts',(-0.0128299371654484,90.8923117455707,
16.2269021591063));
#65474=CARTESIAN_POINT('Ctrl Pts',(-1.5090788482888,91.0829321788154,15.7301039900146));
#65475=CARTESIAN_POINT('Ctrl Pts',(-2.4712190066523,91.2533322525557,14.7025505955179));
#65476=CARTESIAN_POINT('Ctrl Pts',(-2.82047005478047,91.4225304385253,13.347796228399));
#65477=CARTESIAN_POINT('Ctrl Pts',(-2.48034860101448,91.590488555968,12.0020035560574));
#65478=CARTESIAN_POINT('Ctrl Pts',(-1.54368559506711,91.7571719060457,10.9914121456071));
#65479=CARTESIAN_POINT('Ctrl Pts',(-0.247851535959068,91.9225516418578,
10.5560764938838));
#65480=CARTESIAN_POINT('Ctrl Pts',(1.08726220401839,92.0866038825379,10.793671671954));
#65481=CARTESIAN_POINT('Ctrl Pts',(2.13696021870783,92.2493092899283,11.6345510627664));
#65482=CARTESIAN_POINT('Ctrl Pts',(2.65109720927979,92.4106541005746,12.8651154167332));
#65483=CARTESIAN_POINT('Ctrl Pts',(2.51299220078441,92.5706298715948,14.1805581643091));
#65484=CARTESIAN_POINT('Ctrl Pts',(1.76873005652531,92.7292329498877,15.2596809574676));
#65485=CARTESIAN_POINT('Ctrl Pts',(0.60811066872096,92.8864652975645,15.845136786697));
#65486=CARTESIAN_POINT('Ctrl Pts',(-0.679516057648502,93.042333919981,15.8032945622656));
#65487=CARTESIAN_POINT('Ctrl Pts',(-1.78042322221891,93.1968512659859,15.1552720996806));
#65488=CARTESIAN_POINT('Ctrl Pts',(-2.42972444918458,93.3500347148581,14.0685141712926));
#65489=CARTESIAN_POINT('Ctrl Pts',(-2.47342502433508,93.485032308027,12.9531599654245));
#65490=CARTESIAN_POINT('Ctrl Pts',(-2.12173691667042,93.6023232400316,12.0683988477808));
#65491=CARTESIAN_POINT('Ctrl Pts',(-1.41794563352187,93.7356222147801,11.2443833855659));
#65492=CARTESIAN_POINT('Ctrl Pts',(-0.108651400054405,93.900868814998,10.7521591008224));
#65493=CARTESIAN_POINT('Ctrl Pts',(1.47580000963189,94.0970547503915,11.2528212630621));
#65494=CARTESIAN_POINT('Ctrl Pts',(2.40245789704906,94.291241610282,12.6122252108601));
#65495=CARTESIAN_POINT('Ctrl Pts',(2.30958675223246,94.451495797935,13.9661845313665));
#65496=CARTESIAN_POINT('Ctrl Pts',(1.82188265588916,94.5629134950966,14.7288928580851));
#65497=CARTESIAN_POINT('Ctrl Pts',(1.49719096913084,94.6184378224292,15.0352973716418));
#65498=CARTESIAN_POINT('Ctrl Pts',(1.29186658376209,94.6501156878609,15.1841493917124));
#65499=CARTESIAN_POINT('Ctrl Pts',(0.533511913404019,94.7608712055693,15.654143026697));
#65500=CARTESIAN_POINT('Ctrl Pts',(-0.808074592779245,94.9101512303414,
15.6464877011121));
#65501=CARTESIAN_POINT('Ctrl Pts',(-1.94420320187033,95.0971904649237,14.5863988238769));
#65502=CARTESIAN_POINT('Ctrl Pts',(-2.22188224409465,95.2018810288088,13.7706870299644));
#65503=CARTESIAN_POINT('Ctrl Pts',(-2.22955039463141,95.2714832059397,13.2113581250775));
#65504=CARTESIAN_POINT('Ctrl Pts',(-2.18876276415898,95.3178348388426,12.8417215097046));
#65505=CARTESIAN_POINT('Ctrl Pts',(-2.05167672673761,95.375681883697,12.3951255440082));
#65506=CARTESIAN_POINT('Ctrl Pts',(-1.76041900544877,95.4449678022735,11.9175965276771));
#65507=CARTESIAN_POINT('Ctrl Pts',(-1.36080955808199,95.5141241472378,11.5275545479325));
#65508=CARTESIAN_POINT('Ctrl Pts',(-0.877970487401089,95.5831702281511,
11.2489614525707));
#65509=CARTESIAN_POINT('Ctrl Pts',(-0.342000986324222,95.6521067193162,
11.0985126748453));
#65510=CARTESIAN_POINT('Ctrl Pts',(0.213623207064906,95.720952651231,11.0855717915074));
#65511=CARTESIAN_POINT('Ctrl Pts',(0.93535872538529,95.812630073061,11.2509739490936));
#65512=CARTESIAN_POINT('Ctrl Pts',(1.71507243567299,95.9270440274078,11.7856963334004));
#65513=CARTESIAN_POINT('Ctrl Pts',(2.22879898544115,96.064126183288,12.7961234832359));
#65514=CARTESIAN_POINT('Ctrl Pts',(2.19496889611997,96.201080189433,13.927792625613));
#65515=CARTESIAN_POINT('Ctrl Pts',(1.62336777189102,96.3379891415667,14.9047555231163));
#65516=CARTESIAN_POINT('Ctrl Pts',(0.653637378996546,96.4749390978704,15.4883450793425));
#65517=CARTESIAN_POINT('Ctrl Pts',(-0.479183597507465,96.6120140716515,
15.5362569140024));
#65518=CARTESIAN_POINT('Ctrl Pts',(-1.49550380827525,96.7493002509423,15.0340431944611));
#65519=CARTESIAN_POINT('Ctrl Pts',(-2.22617634409563,96.902165163245,14.001312148663));
#65520=CARTESIAN_POINT('Ctrl Pts',(-2.26912391360259,97.0708521378234,12.5743617552715));
#65521=CARTESIAN_POINT('Ctrl Pts',(-1.34012118721779,97.2557343745632,11.3126762919694));
#65522=CARTESIAN_POINT('Ctrl Pts',(0.0517192767727834,97.4261669198471,
10.9312737951385));
#65523=CARTESIAN_POINT('Ctrl Pts',(1.27666129064818,97.5819976087186,11.331693969795));
#65524=CARTESIAN_POINT('Ctrl Pts',(2.07664831716534,97.7230050544256,12.178854656779));
#65525=CARTESIAN_POINT('Ctrl Pts',(2.3738396568357,97.8648420439373,13.3133439150153));
#65526=CARTESIAN_POINT('Ctrl Pts',(2.08993730325257,98.0075746833811,14.4582197611074));
#65527=CARTESIAN_POINT('Ctrl Pts',(1.28596236049746,98.1512642776317,15.3331498015845));
#65528=CARTESIAN_POINT('Ctrl Pts',(0.248580457378911,98.2839133694417,15.6853991648919));
#65529=CARTESIAN_POINT('Ctrl Pts',(-0.933019279072089,98.4295580310931,
15.5563383436846));
#65530=CARTESIAN_POINT('Ctrl Pts',(-1.94528147010697,98.5763136628078,14.8529360099437));
#65531=CARTESIAN_POINT('Ctrl Pts',(-2.45982197643258,98.7367255305564,13.6289096816955));
#65532=CARTESIAN_POINT('Ctrl Pts',(-2.36668773663634,98.848688246541,12.7090141811426));
#65533=CARTESIAN_POINT('Ctrl Pts',(-2.04306609875493,98.9487318029496,11.9738450868454));
#65534=CARTESIAN_POINT('Ctrl Pts',(-1.53940292542878,99.0491943457798,11.3277821125564));
#65535=CARTESIAN_POINT('Ctrl Pts',(-0.747158491221365,99.1567306174659,
10.9250034101893));
#65536=CARTESIAN_POINT('Ctrl Pts',(-0.0355768373076844,99.2458149990659,
10.8359274483637));
#65537=CARTESIAN_POINT('Ctrl Pts',(0.579456403249374,99.322420701784,10.8735010914224));
#65538=CARTESIAN_POINT('Ctrl Pts',(1.31947344673593,99.4186441904899,11.1366691296655));
#65539=CARTESIAN_POINT('Ctrl Pts',(2.03176253387087,99.5348675172455,11.7600543420649));
#65540=CARTESIAN_POINT('Ctrl Pts',(2.62304119418394,99.6908473899985,12.8875930599719));
#65541=CARTESIAN_POINT('Ctrl Pts',(2.48567427465143,99.8877397945851,14.5730938352413));
#65542=CARTESIAN_POINT('Ctrl Pts',(1.40893999897151,100.057286246309,15.5547480034218));
#65543=CARTESIAN_POINT('Ctrl Pts',(0.489040922673266,100.177833295425,15.8525318981432));
#65544=CARTESIAN_POINT('Ctrl Pts',(-0.157644488075177,100.258454146333,
15.9365107147818));
#65545=CARTESIAN_POINT('Ctrl Pts',(-1.04840784317475,100.369923284926,15.7556200306154));
#65546=CARTESIAN_POINT('Ctrl Pts',(-1.88548202700648,100.492288158336,15.2130321561939));
#65547=CARTESIAN_POINT('Ctrl Pts',(-2.37213571326726,100.594888104147,14.5324827913111));
#65548=CARTESIAN_POINT('Ctrl Pts',(-2.70319266626553,100.718569100259,13.5947914370014));
#65549=CARTESIAN_POINT('Ctrl Pts',(-2.66142717358176,100.88446549619,12.2109455348121));
#65550=CARTESIAN_POINT('Ctrl Pts',(-1.86143294901679,101.0311095758,11.2394258266373));
#65551=CARTESIAN_POINT('Ctrl Pts',(-1.27034543602034,101.115370990615,10.9133596760187));
#65552=CARTESIAN_POINT('Ctrl Pts',(2.6982717955234,88.403566445568,13.1056746312321));
#65553=CARTESIAN_POINT('Ctrl Pts',(2.73677823189285,88.4878761639066,13.7800071944845));
#65554=CARTESIAN_POINT('Ctrl Pts',(2.28425210318142,88.6555720116245,15.1486253494134));
#65555=CARTESIAN_POINT('Ctrl Pts',(0.407881201053683,88.904226976665,16.1734842624281));
#65556=CARTESIAN_POINT('Ctrl Pts',(-1.63846080224287,89.1499107750029,15.654110428655));
#65557=CARTESIAN_POINT('Ctrl Pts',(-2.76815376800513,89.3925605881487,13.9001090618085));
#65558=CARTESIAN_POINT('Ctrl Pts',(-2.40326272296852,89.6321427493135,11.8725688627051));
#65559=CARTESIAN_POINT('Ctrl Pts',(-0.777267600718407,89.8686482498881,
10.6543421289767));
#65560=CARTESIAN_POINT('Ctrl Pts',(1.2209111868425,90.1020966373451,10.8651434831607));
#65561=CARTESIAN_POINT('Ctrl Pts',(2.46834350755888,90.3239964454185,12.3060790477895));
#65562=CARTESIAN_POINT('Ctrl Pts',(2.47949950937406,90.534789028808,14.0943538121054));
#65563=CARTESIAN_POINT('Ctrl Pts',(1.44051214460606,90.7348908208017,15.4325656002478));
#65564=CARTESIAN_POINT('Ctrl Pts',(-0.0498573366506787,90.9163226656018,
15.8048130884501));
#65565=CARTESIAN_POINT('Ctrl Pts',(-1.32447685647671,91.0797442933639,15.3552157694385));
#65566=CARTESIAN_POINT('Ctrl Pts',(-2.13210462485608,91.2257001082563,14.4598916568282));
#65567=CARTESIAN_POINT('Ctrl Pts',(-2.40947031795943,91.3705828174244,13.2944545494697));
#65568=CARTESIAN_POINT('Ctrl Pts',(-2.09662454683838,91.514445897888,12.1473740235271));
#65569=CARTESIAN_POINT('Ctrl Pts',(-1.27747010443514,91.6573490367806,11.2961798485563));
#65570=CARTESIAN_POINT('Ctrl Pts',(-0.15794825801904,91.7993537239909,10.9433901007385));
#65571=CARTESIAN_POINT('Ctrl Pts',(0.986893306140469,91.9405247070845,11.1695027418782));
#65572=CARTESIAN_POINT('Ctrl Pts',(1.87883455338834,92.080931921978,11.9121624589809));
#65573=CARTESIAN_POINT('Ctrl Pts',(2.30373364807092,92.2206464603464,12.986011815602));
#65574=CARTESIAN_POINT('Ctrl Pts',(2.16191947494285,92.3597409778006,14.1272836660435));
#65575=CARTESIAN_POINT('Ctrl Pts',(1.49387879217675,92.4982940542609,15.0574211095268));
#65576=CARTESIAN_POINT('Ctrl Pts',(0.464924407642362,92.6363833532689,15.5520277071038));
#65577=CARTESIAN_POINT('Ctrl Pts',(-0.671741220646141,92.7740895606021,
15.4932736912129));
#65578=CARTESIAN_POINT('Ctrl Pts',(-1.63947228550976,92.9114947310828,14.898349345003));
#65579=CARTESIAN_POINT('Ctrl Pts',(-2.20213144252492,93.0486821268315,13.9140569607997));
#65580=CARTESIAN_POINT('Ctrl Pts',(-2.22217481619574,93.170507196285,12.906972120727));
#65581=CARTESIAN_POINT('Ctrl Pts',(-1.88666751207057,93.2770715915512,12.1095939354917));
#65582=CARTESIAN_POINT('Ctrl Pts',(-1.22888560907111,93.3988639251671,11.3697767993831));
#65583=CARTESIAN_POINT('Ctrl Pts',(-0.0138566767747093,93.5511736528308,
10.938509126912));
#65584=CARTESIAN_POINT('Ctrl Pts',(1.45584692256595,93.7342564375675,11.432953200915));
#65585=CARTESIAN_POINT('Ctrl Pts',(2.30813351616898,93.9178513994656,12.7341522198219));
#65586=CARTESIAN_POINT('Ctrl Pts',(2.19517368978801,94.0714302286491,14.0298936993096));
#65587=CARTESIAN_POINT('Ctrl Pts',(1.70799408844307,94.1793296679858,14.7589433304297));
#65588=CARTESIAN_POINT('Ctrl Pts',(1.38582449129328,94.2333849376954,15.050614060485));
#65589=CARTESIAN_POINT('Ctrl Pts',(1.18237695084966,94.2643067275912,15.1917101185989));
#65590=CARTESIAN_POINT('Ctrl Pts',(0.431945487405895,94.3726104335691,15.6358298479467));
#65591=CARTESIAN_POINT('Ctrl Pts',(-0.895590023133178,94.5202846750657,
15.6066128479558));
#65592=CARTESIAN_POINT('Ctrl Pts',(-2.01753162269537,94.7083272792382,14.5189076637268));
#65593=CARTESIAN_POINT('Ctrl Pts',(-2.28318440568369,94.8147164924953,13.6845316251193));
#65594=CARTESIAN_POINT('Ctrl Pts',(-2.27916822588818,94.8859207205472,13.1122919552739));
#65595=CARTESIAN_POINT('Ctrl Pts',(-2.22944080310975,94.9334655403241,12.7341072326119));
#65596=CARTESIAN_POINT('Ctrl Pts',(-2.07884865783431,94.9930381561256,12.2772014213181));
#65597=CARTESIAN_POINT('Ctrl Pts',(-1.76723365998065,95.0647661925447,11.7891518513653));
#65598=CARTESIAN_POINT('Ctrl Pts',(-1.34312836833211,95.1367356319896,11.3918848336069));
#65599=CARTESIAN_POINT('Ctrl Pts',(-0.832192495404496,95.2089606333801,
11.1109039490121));
#65600=CARTESIAN_POINT('Ctrl Pts',(-0.265556395800235,95.2814416873198,
10.9643197661734));
#65601=CARTESIAN_POINT('Ctrl Pts',(0.321725886023046,95.3541914012238,10.9626976298369));
#65602=CARTESIAN_POINT('Ctrl Pts',(1.08437891377309,95.4515515391821,11.1539926108051));
#65603=CARTESIAN_POINT('Ctrl Pts',(1.90710986417378,95.5739503059066,11.7422461904413));
#65604=CARTESIAN_POINT('Ctrl Pts',(2.4404412987834,95.7219898229644,12.843994864368));
#65605=CARTESIAN_POINT('Ctrl Pts',(2.379479888786,95.8712342750027,14.0762228369055));
#65606=CARTESIAN_POINT('Ctrl Pts',(1.73035753713278,96.0217201838532,15.1375312326044));
#65607=CARTESIAN_POINT('Ctrl Pts',(0.643386214015007,96.1734811341986,15.7630777197292));
#65608=CARTESIAN_POINT('Ctrl Pts',(-0.622317523007441,96.3265448289381,
15.7919049809492));
#65609=CARTESIAN_POINT('Ctrl Pts',(-1.75397860125501,96.480934945421,15.2049005623045));
#65610=CARTESIAN_POINT('Ctrl Pts',(-2.55814788915194,96.6539723016953,14.02018776271));
#65611=CARTESIAN_POINT('Ctrl Pts',(-2.57630918532901,96.8462485966002,12.393115852525));
#65612=CARTESIAN_POINT('Ctrl Pts',(-1.48302324967836,97.0584331732658,10.9656125154963));
#65613=CARTESIAN_POINT('Ctrl Pts',(0.131597325881443,97.2551618193207,10.555910795393));
#65614=CARTESIAN_POINT('Ctrl Pts',(1.54203088690724,97.4357640453685,11.0472488011817));
#65615=CARTESIAN_POINT('Ctrl Pts',(2.45265002307442,97.5996487784601,12.0494969325054));
#65616=CARTESIAN_POINT('Ctrl Pts',(2.77339887441105,97.764857842986,13.3772624762716));
#65617=CARTESIAN_POINT('Ctrl Pts',(2.41674321824258,97.9313676595873,14.7062177757228));
#65618=CARTESIAN_POINT('Ctrl Pts',(1.45869542335619,98.0991505421964,15.7097180326528));
#65619=CARTESIAN_POINT('Ctrl Pts',(0.239482616591414,98.2540865330431,16.0980321821802));
#65620=CARTESIAN_POINT('Ctrl Pts',(-1.13716396581138,98.4241595756667,15.9212458125922));
#65621=CARTESIAN_POINT('Ctrl Pts',(-2.30250606540272,98.5954018308291,15.0783007993036));
#65622=CARTESIAN_POINT('Ctrl Pts',(-2.87492379306717,98.7822684387443,13.641430366129));
#65623=CARTESIAN_POINT('Ctrl Pts',(-2.74663987954804,98.9124332651019,12.5742656574783));
#65624=CARTESIAN_POINT('Ctrl Pts',(-2.35539724166868,99.0285530189489,11.7280449140218));
#65625=CARTESIAN_POINT('Ctrl Pts',(-1.75783143833091,99.1450032440976,10.9901139909209));
#65626=CARTESIAN_POINT('Ctrl Pts',(-0.833523187967213,99.2693172583649,
10.5416254977322));
#65627=CARTESIAN_POINT('Ctrl Pts',(-0.0112566855763176,99.3720479456177,
10.4538476434305));
#65628=CARTESIAN_POINT('Ctrl Pts',(0.696065540465303,99.4602628880338,10.5099288290863));
#65629=CARTESIAN_POINT('Ctrl Pts',(1.54066178520884,99.5708244149292,10.8278193912155));
#65630=CARTESIAN_POINT('Ctrl Pts',(2.34328981529501,99.7039391526554,11.5564330805856));
#65631=CARTESIAN_POINT('Ctrl Pts',(2.99473750685021,99.8819699522155,12.8555658122346));
#65632=CARTESIAN_POINT('Ctrl Pts',(2.80228122333666,100.105460034239,14.7653030646166));
#65633=CARTESIAN_POINT('Ctrl Pts',(1.56931524944386,100.296318130813,15.8469872865633));
#65634=CARTESIAN_POINT('Ctrl Pts',(0.533505226601642,100.431325859326,16.1624281999286));
#65635=CARTESIAN_POINT('Ctrl Pts',(-0.190638711014172,100.521408431442,
16.2435381989408));
#65636=CARTESIAN_POINT('Ctrl Pts',(-1.17807866534425,100.645447380912,16.024680873488));
#65637=CARTESIAN_POINT('Ctrl Pts',(-2.09417040602153,100.780943522073,15.4075782223232));
#65638=CARTESIAN_POINT('Ctrl Pts',(-2.6169850877654,100.893977649135,14.6484975768373));
#65639=CARTESIAN_POINT('Ctrl Pts',(-2.96252965864728,101.029703570786,13.6134018679802));
#65640=CARTESIAN_POINT('Ctrl Pts',(-2.8893582560375,101.210790914664,12.1037148393349));
#65641=CARTESIAN_POINT('Ctrl Pts',(-2.00470848770043,101.369327870032,11.0699765470644));
#65642=CARTESIAN_POINT('Ctrl Pts',(-1.3635592194715,101.45989658619,10.730290318802));
#65643=CARTESIAN_POINT('Ctrl Pts',(2.49377963891743,88.7481783151202,13.1237495374328));
#65644=CARTESIAN_POINT('Ctrl Pts',(2.51727668610183,88.826184582445,13.7484520602668));
#65645=CARTESIAN_POINT('Ctrl Pts',(2.07334252609224,88.9802970251652,14.9972313381631));
#65646=CARTESIAN_POINT('Ctrl Pts',(0.349974014614918,89.2058334569828,15.8881622271935));
#65647=CARTESIAN_POINT('Ctrl Pts',(-1.4721601403514,89.4258485639336,15.3802531740095));
#65648=CARTESIAN_POINT('Ctrl Pts',(-2.43475217322985,89.6405030558901,13.8044271928562));
#65649=CARTESIAN_POINT('Ctrl Pts',(-2.07248353196307,89.8500044745869,12.0388498025858));
#65650=CARTESIAN_POINT('Ctrl Pts',(-0.639442656943906,90.0546013838731,
11.0195223460819));
#65651=CARTESIAN_POINT('Ctrl Pts',(1.06828549774142,90.2545925638933,11.2433500364064));
#65652=CARTESIAN_POINT('Ctrl Pts',(2.09681142601901,90.4430555108166,12.4944576525287));
#65653=CARTESIAN_POINT('Ctrl Pts',(2.06763054784826,90.6208555597969,14.0034102515066));
#65654=CARTESIAN_POINT('Ctrl Pts',(1.1668221790206,90.78873612915,15.1039470224899));
#65655=CARTESIAN_POINT('Ctrl Pts',(-0.0868847361359067,90.9403335856326,
15.3827240177938));
#65656=CARTESIAN_POINT('Ctrl Pts',(-1.13987486466463,91.0765564079124,14.9803275488623));
#65657=CARTESIAN_POINT('Ctrl Pts',(-1.79299024305986,91.1980679639569,14.2172327181384));
#65658=CARTESIAN_POINT('Ctrl Pts',(-1.99847058113838,91.3186351963235,13.2411128705403));
#65659=CARTESIAN_POINT('Ctrl Pts',(-1.71290049266228,91.438403239808,12.2927444909967));
#65660=CARTESIAN_POINT('Ctrl Pts',(-1.01125461380317,91.5575261675155,11.6009475515055));
#65661=CARTESIAN_POINT('Ctrl Pts',(-0.0680449800790074,91.6761558061239,
11.3307037075934));
#65662=CARTESIAN_POINT('Ctrl Pts',(0.886524408262558,91.7944455316312,11.5453338118024));
#65663=CARTESIAN_POINT('Ctrl Pts',(1.62070888806884,91.9125545540277,12.1897738551953));
#65664=CARTESIAN_POINT('Ctrl Pts',(1.95637008686205,92.0306388201183,13.1069082144709));
#65665=CARTESIAN_POINT('Ctrl Pts',(1.81084674910129,92.1488520840062,14.0740091677779));
#65666=CARTESIAN_POINT('Ctrl Pts',(1.21902752782821,92.2673551586341,14.855161261586));
#65667=CARTESIAN_POINT('Ctrl Pts',(0.321738146563767,92.3863014089734,15.2589186275106));
#65668=CARTESIAN_POINT('Ctrl Pts',(-0.663966383643774,92.5058452012233,
15.1832528201601));
#65669=CARTESIAN_POINT('Ctrl Pts',(-1.49852134880062,92.6261381961799,14.6414265903252));
#65670=CARTESIAN_POINT('Ctrl Pts',(-1.97453843586526,92.7473295388048,13.7595997503068));
#65671=CARTESIAN_POINT('Ctrl Pts',(-1.97092460805639,92.8559820845432,12.8607842760296));
#65672=CARTESIAN_POINT('Ctrl Pts',(-1.65159810747073,92.9518199430708,12.1507890232025));
#65673=CARTESIAN_POINT('Ctrl Pts',(-1.03982558462033,93.0621056355542,11.4951702132003));
#65674=CARTESIAN_POINT('Ctrl Pts',(0.0809380465049925,93.2014784906635,
11.1248591530016));
#65675=CARTESIAN_POINT('Ctrl Pts',(1.4358938355,93.3714581247436,11.6130851387679));
#65676=CARTESIAN_POINT('Ctrl Pts',(2.21380913528891,93.5444611886493,12.8560792287835));
#65677=CARTESIAN_POINT('Ctrl Pts',(2.08076062734356,93.6913646593632,14.0936028672527));
#65678=CARTESIAN_POINT('Ctrl Pts',(1.59410552099699,93.7957458408751,14.7889938027743));
#65679=CARTESIAN_POINT('Ctrl Pts',(1.27445801345573,93.8483320529615,15.0659307493282));
#65680=CARTESIAN_POINT('Ctrl Pts',(1.07288731793725,93.8784977673215,15.1992708454853));
#65681=CARTESIAN_POINT('Ctrl Pts',(0.330379061407773,93.9843496615688,15.6175166691962));
#65682=CARTESIAN_POINT('Ctrl Pts',(-0.983105453487106,94.1304181197899,
15.5667379947997));
#65683=CARTESIAN_POINT('Ctrl Pts',(-2.09086004352039,94.3194640935526,14.4514165035768));
#65684=CARTESIAN_POINT('Ctrl Pts',(-2.34448656727271,94.4275519561817,13.598376220274));
#65685=CARTESIAN_POINT('Ctrl Pts',(-2.32878605714495,94.5003582351546,13.0132257854703));
#65686=CARTESIAN_POINT('Ctrl Pts',(-2.27011884206053,94.5490962418056,12.6264929555191));
#65687=CARTESIAN_POINT('Ctrl Pts',(-2.106020588931,94.6103944285541,12.1592772986281));
#65688=CARTESIAN_POINT('Ctrl Pts',(-1.77404831451251,94.6845645828161,11.6607071750535));
#65689=CARTESIAN_POINT('Ctrl Pts',(-1.32544717858223,94.7593471167414,11.2562151192812));
#65690=CARTESIAN_POINT('Ctrl Pts',(-0.786414503407905,94.8347510386092,
10.9728464454538));
#65691=CARTESIAN_POINT('Ctrl Pts',(-0.189111805276248,94.9107766553234,
10.8301268575013));
#65692=CARTESIAN_POINT('Ctrl Pts',(0.429828564981183,94.9874301512166,10.8398234681666));
#65693=CARTESIAN_POINT('Ctrl Pts',(1.23339910216089,95.090473005303,11.0570112725166));
#65694=CARTESIAN_POINT('Ctrl Pts',(2.09914729267456,95.2208565844055,11.6987960474823));
#65695=CARTESIAN_POINT('Ctrl Pts',(2.65208361212563,95.3798534626408,12.8918662454998));
#65696=CARTESIAN_POINT('Ctrl Pts',(2.56399088145202,95.5413883605725,14.224653048198));
#65697=CARTESIAN_POINT('Ctrl Pts',(1.83734730237453,95.7054512261398,15.3703069420924));
#65698=CARTESIAN_POINT('Ctrl Pts',(0.633135049033465,95.8720231705268,16.0378103601158));
#65699=CARTESIAN_POINT('Ctrl Pts',(-0.76545144850742,96.0410755862248,16.0475530478959));
#65700=CARTESIAN_POINT('Ctrl Pts',(-2.01245339423477,96.2125696398999,15.375757930148));
#65701=CARTESIAN_POINT('Ctrl Pts',(-2.89011943420824,96.4057794401457,14.0390633767572));
#65702=CARTESIAN_POINT('Ctrl Pts',(-2.88349445705544,96.6216450553769,12.2118699497786));
#65703=CARTESIAN_POINT('Ctrl Pts',(-1.62592531213895,96.8611319719683,10.6185487390233));
#65704=CARTESIAN_POINT('Ctrl Pts',(0.211475374990095,97.0841567187942,10.1805477956475));
#65705=CARTESIAN_POINT('Ctrl Pts',(1.80740048316628,97.2895304820185,10.7628036325681));
#65706=CARTESIAN_POINT('Ctrl Pts',(2.82865172898348,97.4762925024945,11.9201392082317));
#65707=CARTESIAN_POINT('Ctrl Pts',(3.17295809198639,97.6648736420349,13.4411810375279));
#65708=CARTESIAN_POINT('Ctrl Pts',(2.74354913323257,97.8551606357935,14.9542157903382));
#65709=CARTESIAN_POINT('Ctrl Pts',(1.63142848621491,98.0470368067611,16.0862862637212));
#65710=CARTESIAN_POINT('Ctrl Pts',(0.230384775803907,98.2242596966446,16.5106651994685));
#65711=CARTESIAN_POINT('Ctrl Pts',(-1.34130865255068,98.4187611202403,16.2861532814996));
#65712=CARTESIAN_POINT('Ctrl Pts',(-2.65973066069848,98.6144899988505,15.3036655886634));
#65713=CARTESIAN_POINT('Ctrl Pts',(-3.29002560970176,98.8278113469321,13.6539510505623));
#65714=CARTESIAN_POINT('Ctrl Pts',(-3.12659202245975,98.9761782836627,12.4395171338142));
#65715=CARTESIAN_POINT('Ctrl Pts',(-2.66772838458244,99.1083742349483,11.482244741198));
#65716=CARTESIAN_POINT('Ctrl Pts',(-1.97625995123304,99.2408121424155,10.6524458692854));
#65717=CARTESIAN_POINT('Ctrl Pts',(-0.919887884713065,99.3819038992638,
10.1582475852753));
#65718=CARTESIAN_POINT('Ctrl Pts',(0.0130634661550411,99.4982808921694,
10.0717678384972));
#65719=CARTESIAN_POINT('Ctrl Pts',(0.812674677681222,99.5981050742835,10.14635656675));
#65720=CARTESIAN_POINT('Ctrl Pts',(1.76185012368174,99.7230046393686,10.5189696527654));
#65721=CARTESIAN_POINT('Ctrl Pts',(2.65481709671915,99.8730107880652,11.3528118191064));
#65722=CARTESIAN_POINT('Ctrl Pts',(3.36643381951645,100.073092514433,12.8235385644975));
#65723=CARTESIAN_POINT('Ctrl Pts',(3.11888817202187,100.323180273892,14.9575122939919));
#65724=CARTESIAN_POINT('Ctrl Pts',(1.72969049991617,100.535350015318,16.1392265697048));
#65725=CARTESIAN_POINT('Ctrl Pts',(0.57796953053001,100.684818423227,16.4723245017141));
#65726=CARTESIAN_POINT('Ctrl Pts',(-0.223632933953175,100.784362716553,
16.5505656830996));
#65727=CARTESIAN_POINT('Ctrl Pts',(-1.30774948751375,100.920971476897,16.2937417163607));
#65728=CARTESIAN_POINT('Ctrl Pts',(-2.30285878503657,101.069598885813,15.6021242884526));
#65729=CARTESIAN_POINT('Ctrl Pts',(-2.86183446226353,101.193067194121,14.7645123623634));
#65730=CARTESIAN_POINT('Ctrl Pts',(-3.22186665102905,101.340838041313,13.632012298959));
#65731=CARTESIAN_POINT('Ctrl Pts',(-3.11728933849324,101.537116333136,11.9964841438576));
#65732=CARTESIAN_POINT('Ctrl Pts',(-2.14798402638407,101.707546164264,10.9005272674917));
#65733=CARTESIAN_POINT('Ctrl Pts',(-1.45677300292266,101.804422181766,10.5472209615853));
#65734=CARTESIAN_POINT('Ctrl Pts',(2.49380022861477,88.7482468790765,13.1242986243742));
#65735=CARTESIAN_POINT('Ctrl Pts',(2.51714660453923,88.8262297351317,13.7488179208904));
#65736=CARTESIAN_POINT('Ctrl Pts',(2.07317421855453,88.980319051494,14.9973183482153));
#65737=CARTESIAN_POINT('Ctrl Pts',(0.349974014614918,89.2058334569828,15.8881622271935));
#65738=CARTESIAN_POINT('Ctrl Pts',(-1.4721601403514,89.4258485639336,15.3802531740095));
#65739=CARTESIAN_POINT('Ctrl Pts',(-2.43475217322985,89.6405030558901,13.8044271928562));
#65740=CARTESIAN_POINT('Ctrl Pts',(-2.07248353196307,89.8500044745869,12.0388498025858));
#65741=CARTESIAN_POINT('Ctrl Pts',(-0.639442656943906,90.0546013838731,
11.0195223460819));
#65742=CARTESIAN_POINT('Ctrl Pts',(1.06828549774142,90.2545925638933,11.2433500364064));
#65743=CARTESIAN_POINT('Ctrl Pts',(2.09681142601901,90.4430555108166,12.4944576525287));
#65744=CARTESIAN_POINT('Ctrl Pts',(2.06763054784826,90.6208555597969,14.0034102515066));
#65745=CARTESIAN_POINT('Ctrl Pts',(1.1668221790206,90.78873612915,15.1039470224899));
#65746=CARTESIAN_POINT('Ctrl Pts',(-0.0868847361359067,90.9403335856326,
15.3827240177938));
#65747=CARTESIAN_POINT('Ctrl Pts',(-1.13987486466463,91.0765564079124,14.9803275488623));
#65748=CARTESIAN_POINT('Ctrl Pts',(-1.79299024305986,91.1980679639569,14.2172327181384));
#65749=CARTESIAN_POINT('Ctrl Pts',(-1.99847058113838,91.3186351963235,13.2411128705403));
#65750=CARTESIAN_POINT('Ctrl Pts',(-1.71290049266228,91.438403239808,12.2927444909967));
#65751=CARTESIAN_POINT('Ctrl Pts',(-1.01125461380317,91.5575261675155,11.6009475515055));
#65752=CARTESIAN_POINT('Ctrl Pts',(-0.0680449800790074,91.6761558061239,
11.3307037075934));
#65753=CARTESIAN_POINT('Ctrl Pts',(0.886524408262558,91.7944455316312,11.5453338118024));
#65754=CARTESIAN_POINT('Ctrl Pts',(1.62070888806884,91.9125545540277,12.1897738551953));
#65755=CARTESIAN_POINT('Ctrl Pts',(1.95637008686205,92.0306388201183,13.1069082144709));
#65756=CARTESIAN_POINT('Ctrl Pts',(1.81084674910129,92.1488520840062,14.0740091677779));
#65757=CARTESIAN_POINT('Ctrl Pts',(1.21902752782821,92.2673551586341,14.855161261586));
#65758=CARTESIAN_POINT('Ctrl Pts',(0.321738146563767,92.3863014089734,15.2589186275106));
#65759=CARTESIAN_POINT('Ctrl Pts',(-0.663966383643774,92.5058452012233,
15.1832528201601));
#65760=CARTESIAN_POINT('Ctrl Pts',(-1.49852134880062,92.6261381961799,14.6414265903252));
#65761=CARTESIAN_POINT('Ctrl Pts',(-1.97453843586526,92.7473295388048,13.7595997503068));
#65762=CARTESIAN_POINT('Ctrl Pts',(-1.97092460805639,92.8559820845432,12.8607842760296));
#65763=CARTESIAN_POINT('Ctrl Pts',(-1.65159810747073,92.9518199430708,12.1507890232025));
#65764=CARTESIAN_POINT('Ctrl Pts',(-1.03982558462033,93.0621056355542,11.4951702132003));
#65765=CARTESIAN_POINT('Ctrl Pts',(0.0809380465049925,93.2014784906635,
11.1248591530016));
#65766=CARTESIAN_POINT('Ctrl Pts',(1.4358938355,93.3714581247436,11.6130851387679));
#65767=CARTESIAN_POINT('Ctrl Pts',(2.21380913528891,93.5444611886493,12.8560792287835));
#65768=CARTESIAN_POINT('Ctrl Pts',(2.08076062734356,93.6913646593632,14.0936028672527));
#65769=CARTESIAN_POINT('Ctrl Pts',(1.59410552099699,93.7957458408751,14.7889938027743));
#65770=CARTESIAN_POINT('Ctrl Pts',(1.27445801345573,93.8483320529615,15.0659307493282));
#65771=CARTESIAN_POINT('Ctrl Pts',(1.07288731793725,93.8784977673215,15.1992708454853));
#65772=CARTESIAN_POINT('Ctrl Pts',(0.330379061407773,93.9843496615688,15.6175166691962));
#65773=CARTESIAN_POINT('Ctrl Pts',(-0.983105453487106,94.1304181197899,
15.5667379947997));
#65774=CARTESIAN_POINT('Ctrl Pts',(-2.09086004352039,94.3194640935526,14.4514165035768));
#65775=CARTESIAN_POINT('Ctrl Pts',(-2.34448656727271,94.4275519561817,13.598376220274));
#65776=CARTESIAN_POINT('Ctrl Pts',(-2.32878605714495,94.5003582351546,13.0132257854703));
#65777=CARTESIAN_POINT('Ctrl Pts',(-2.27011884206053,94.5490962418056,12.6264929555191));
#65778=CARTESIAN_POINT('Ctrl Pts',(-2.106020588931,94.6103944285541,12.1592772986281));
#65779=CARTESIAN_POINT('Ctrl Pts',(-1.77404831451251,94.6845645828161,11.6607071750535));
#65780=CARTESIAN_POINT('Ctrl Pts',(-1.32544717858223,94.7593471167414,11.2562151192812));
#65781=CARTESIAN_POINT('Ctrl Pts',(-0.786414503407905,94.8347510386092,
10.9728464454538));
#65782=CARTESIAN_POINT('Ctrl Pts',(-0.189111805276248,94.9107766553234,
10.8301268575013));
#65783=CARTESIAN_POINT('Ctrl Pts',(0.429828564981183,94.9874301512166,10.8398234681666));
#65784=CARTESIAN_POINT('Ctrl Pts',(0.91716227398176,95.049921561671,10.9715392707581));
#65785=CARTESIAN_POINT('Ctrl Pts',(1.18480262056273,95.0868664053839,11.0991467172034));
#65786=CARTESIAN_POINT('Ctrl Pts',(1.26263430499969,95.0979194610116,11.1414618660017));
#65787=CARTESIAN_POINT('Ctrl Pts',(2.60841185759868,116.632148017263,14.370680154362));
#65788=CARTESIAN_POINT('Ctrl Pts',(2.30778866091531,116.727031067497,15.0690888853187));
#65789=CARTESIAN_POINT('Ctrl Pts',(1.12445764834896,116.913723744564,16.1810188066154));
#65790=CARTESIAN_POINT('Ctrl Pts',(-1.25555818790042,117.188688965645,16.0635810015158));
#65791=CARTESIAN_POINT('Ctrl Pts',(-2.81220088569084,117.457618540921,14.3232511812366));
#65792=CARTESIAN_POINT('Ctrl Pts',(-2.64998973991795,117.722051177067,12.0374368167346));
#65793=CARTESIAN_POINT('Ctrl Pts',(-0.941586509937382,117.981899992631,
10.5634534644126));
#65794=CARTESIAN_POINT('Ctrl Pts',(0.899999153910539,118.194538963125,10.741903484399));
#65795=CARTESIAN_POINT('Ctrl Pts',(1.96699814475253,118.36389001071,11.6130329988365));
#65796=CARTESIAN_POINT('Ctrl Pts',(2.28309757924212,118.448491912406,12.2112327280851));
#65797=CARTESIAN_POINT('Ctrl Pts',(2.38806140485046,118.491549366035,12.5616587240347));
#65798=CARTESIAN_POINT('Ctrl Pts',(2.51630021877766,116.733680406233,14.3148119822871));
#65799=CARTESIAN_POINT('Ctrl Pts',(2.22738125818649,116.825032510427,14.9874533144481));
#65800=CARTESIAN_POINT('Ctrl Pts',(1.09057470294181,117.004399481502,16.0555743277148));
#65801=CARTESIAN_POINT('Ctrl Pts',(-1.18668210243013,117.267494666309,15.9429969544623));
#65802=CARTESIAN_POINT('Ctrl Pts',(-2.67031536555362,117.523876159038,14.2838674933955));
#65803=CARTESIAN_POINT('Ctrl Pts',(-2.51623040664612,117.77508338085,12.1121781733781));
#65804=CARTESIAN_POINT('Ctrl Pts',(-0.897653230639775,118.021236678474,
10.7165287022644));
#65805=CARTESIAN_POINT('Ctrl Pts',(0.841225402353136,118.221999068804,10.8845158308112));
#65806=CARTESIAN_POINT('Ctrl Pts',(1.84905875074838,118.381935657463,11.7068661177474));
#65807=CARTESIAN_POINT('Ctrl Pts',(2.1458150030417,118.461333441716,12.2682356637141));
#65808=CARTESIAN_POINT('Ctrl Pts',(2.245862133833,118.502288008538,12.6013801594841));
#65809=CARTESIAN_POINT('Ctrl Pts',(2.42418857995666,116.835212795203,14.2589438102121));
#65810=CARTESIAN_POINT('Ctrl Pts',(2.14697385545769,116.923033953355,14.9058177435774));
#65811=CARTESIAN_POINT('Ctrl Pts',(1.05669175753469,117.095075218441,15.9301298488143));
#65812=CARTESIAN_POINT('Ctrl Pts',(-1.11780601695983,117.346300366974,15.8224129074088));
#65813=CARTESIAN_POINT('Ctrl Pts',(-2.52842984541641,117.590133777157,14.2444838055542));
#65814=CARTESIAN_POINT('Ctrl Pts',(-2.38247107337429,117.828115584635,12.1869195300215));
#65815=CARTESIAN_POINT('Ctrl Pts',(-0.853719951342167,118.06057336432,10.869603940116));
#65816=CARTESIAN_POINT('Ctrl Pts',(0.782451650795737,118.249459174483,11.0271281772233));
#65817=CARTESIAN_POINT('Ctrl Pts',(1.73111935674423,118.399981304216,11.8006992366585));
#65818=CARTESIAN_POINT('Ctrl Pts',(2.00853242684129,118.474174971026,12.3252385993429));
#65819=CARTESIAN_POINT('Ctrl Pts',(2.10366286281553,118.513026651041,12.6411015949336));
#65820=CARTESIAN_POINT('Ctrl Pts',(2.33207694113565,116.936745184174,14.2030756381372));
#65821=CARTESIAN_POINT('Ctrl Pts',(2.06656645272888,117.021035396283,14.8241821727068));
#65822=CARTESIAN_POINT('Ctrl Pts',(1.02280881212754,117.185750955378,15.8046853699137));
#65823=CARTESIAN_POINT('Ctrl Pts',(-1.04892993148955,117.425106067638,15.7018288603554));
#65824=CARTESIAN_POINT('Ctrl Pts',(-2.38654432527919,117.656391395274,14.2051001177131));
#65825=CARTESIAN_POINT('Ctrl Pts',(-2.24871174010246,117.881147788418,12.2616608866649));
#65826=CARTESIAN_POINT('Ctrl Pts',(-0.809786672044562,118.099910050163,
11.0226791779678));
#65827=CARTESIAN_POINT('Ctrl Pts',(0.723677899238335,118.276919280162,11.1697405236356));
#65828=CARTESIAN_POINT('Ctrl Pts',(1.61317996274009,118.418026950969,11.8945323555693));
#65829=CARTESIAN_POINT('Ctrl Pts',(1.87124985064086,118.487016500336,12.3822415349717));
#65830=CARTESIAN_POINT('Ctrl Pts',(1.96146359179807,118.523765293543,12.680823030383));
#65831=CARTESIAN_POINT('Ctrl Pts',(2.85508310539628,22.7016051911778,13.3));
#65832=CARTESIAN_POINT('Ctrl Pts',(2.84040985303552,22.7610702599433,13.7953362626623));
#65833=CARTESIAN_POINT('Ctrl Pts',(2.57005469369539,22.8818105286997,14.7182643754022));
#65834=CARTESIAN_POINT('Ctrl Pts',(1.18387003193848,23.1175816758084,16.1251408416108));
#65835=CARTESIAN_POINT('Ctrl Pts',(-1.44635846823727,23.4073653880304,16.1636979204723));
#65836=CARTESIAN_POINT('Ctrl Pts',(-3.10207688975974,23.7441121923493,13.5585336200215));
#65837=CARTESIAN_POINT('Ctrl Pts',(-1.93931411699474,24.0343451755729,11.1893587933123));
#65838=CARTESIAN_POINT('Ctrl Pts',(0.0883386693549116,24.2813382692206,
10.6296561281468));
#65839=CARTESIAN_POINT('Ctrl Pts',(1.70144742269104,24.4884076529068,11.3202189090701));
#65840=CARTESIAN_POINT('Ctrl Pts',(2.44259794298568,24.6739869579023,12.7117540199086));
#65841=CARTESIAN_POINT('Ctrl Pts',(2.29730552460407,24.8394118737477,14.0742850221851));
#65842=CARTESIAN_POINT('Ctrl Pts',(1.60135946438255,24.9858059086488,15.065894901695));
#65843=CARTESIAN_POINT('Ctrl Pts',(0.527454597690121,25.1297760483933,15.5827695470996));
#65844=CARTESIAN_POINT('Ctrl Pts',(-0.773691505026583,25.2871272558827,
15.5063423998538));
#65845=CARTESIAN_POINT('Ctrl Pts',(-1.91735749878862,25.4569723948024,14.6292447253925));
#65846=CARTESIAN_POINT('Ctrl Pts',(-2.2807995761954,25.6384274211836,13.1312382095964));
#65847=CARTESIAN_POINT('Ctrl Pts',(-1.63447911169001,25.8163001873567,11.7658051165269));
#65848=CARTESIAN_POINT('Ctrl Pts',(-0.30166668820052,25.9908519237952,11.118090048511));
#65849=CARTESIAN_POINT('Ctrl Pts',(1.11827404154826,26.1623781939067,11.4471128168816));
#65850=CARTESIAN_POINT('Ctrl Pts',(2.00298722537565,26.3311895429685,12.5747319143883));
#65851=CARTESIAN_POINT('Ctrl Pts',(1.98502979276238,26.4976150162961,13.9880823206758));
#65852=CARTESIAN_POINT('Ctrl Pts',(1.09529607704403,26.6620054275366,15.0639864439094));
#65853=CARTESIAN_POINT('Ctrl Pts',(-0.258208853904818,26.8247233802242,
15.3408406941205));
#65854=CARTESIAN_POINT('Ctrl Pts',(-1.47752555552934,26.9861415626953,14.7145503488409));
#65855=CARTESIAN_POINT('Ctrl Pts',(-2.02847081070307,27.1466444125973,13.4669408700617));
#65856=CARTESIAN_POINT('Ctrl Pts',(-1.7064364111904,27.2932881153463,12.2648907963243));
#65857=CARTESIAN_POINT('Ctrl Pts',(-0.874436327135088,27.4265029451041,
11.54040839076));
#65858=CARTESIAN_POINT('Ctrl Pts',(0.0984990014798181,27.5464882437543,
11.3336290315483));
#65859=CARTESIAN_POINT('Ctrl Pts',(1.0464095846472,27.6667307527874,11.627693502193));
#65860=CARTESIAN_POINT('Ctrl Pts',(1.97802584892726,27.8276185888103,12.5894195007116));
#65861=CARTESIAN_POINT('Ctrl Pts',(1.9827636101529,27.9896718678958,14.052696341479));
#65862=CARTESIAN_POINT('Ctrl Pts',(1.0366379049331,28.1535448779212,15.0355576473949));
#65863=CARTESIAN_POINT('Ctrl Pts',(0.0602149397180628,28.2775076356642,
15.3404992503449));
#65864=CARTESIAN_POINT('Ctrl Pts',(-0.955566674000275,28.4026811174227,
15.128424970176));
#65865=CARTESIAN_POINT('Ctrl Pts',(-1.74698128488437,28.5292091514289,14.4420850463022));
#65866=CARTESIAN_POINT('Ctrl Pts',(-2.1084540663241,28.657232610625,13.4461169760093));
#65867=CARTESIAN_POINT('Ctrl Pts',(-1.92196705962975,28.8012916705864,12.2675635904411));
#65868=CARTESIAN_POINT('Ctrl Pts',(-0.988491269521039,28.962263576584,11.2671245863818));
#65869=CARTESIAN_POINT('Ctrl Pts',(0.51289185285495,29.1412742662328,11.0539213646967));
#65870=CARTESIAN_POINT('Ctrl Pts',(2.07965481981169,29.3543978617751,11.967943201084));
#65871=CARTESIAN_POINT('Ctrl Pts',(2.52905815177238,29.6044782263651,14.196116432258));
#65872=CARTESIAN_POINT('Ctrl Pts',(0.579839355331495,29.8952708304772,16.0125676359185));
#65873=CARTESIAN_POINT('Ctrl Pts',(-1.6163097135127,30.1459120270744,15.4054900459629));
#65874=CARTESIAN_POINT('Ctrl Pts',(-2.48042034327965,30.3515915572706,13.9303609021762));
#65875=CARTESIAN_POINT('Ctrl Pts',(-2.50691056537359,30.4561722031845,13.068345948761));
#65876=CARTESIAN_POINT('Ctrl Pts',(-2.41159217086306,30.5089016104533,12.65665943316));
#65877=CARTESIAN_POINT('Ctrl Pts',(2.53672207026418,22.6010701274518,13.3));
#65878=CARTESIAN_POINT('Ctrl Pts',(2.52386596814846,22.6547808871083,13.7475472389172));
#65879=CARTESIAN_POINT('Ctrl Pts',(2.28516242108258,22.7614097926142,14.5627020551058));
#65880=CARTESIAN_POINT('Ctrl Pts',(1.04821201701013,22.9723630473711,15.8230970362253));
#65881=CARTESIAN_POINT('Ctrl Pts',(-1.30163826043596,23.2309895404828,15.8589868213865));
#65882=CARTESIAN_POINT('Ctrl Pts',(-2.79650367489345,23.533893960578,13.5229554773338));
#65883=CARTESIAN_POINT('Ctrl Pts',(-1.75020632631818,23.7966890553668,11.3727757526931));
#65884=CARTESIAN_POINT('Ctrl Pts',(0.100026788420263,24.0222658657341,10.8566282676066));
#65885=CARTESIAN_POINT('Ctrl Pts',(1.58596911863261,24.2127607413429,11.4874877813099));
#65886=CARTESIAN_POINT('Ctrl Pts',(2.27784118097466,24.3849371468287,12.7759298186652));
#65887=CARTESIAN_POINT('Ctrl Pts',(2.14599261285379,24.5396549455458,14.0506824690678));
#65888=CARTESIAN_POINT('Ctrl Pts',(1.49342098412511,24.6776008543935,14.9871469796318));
#65889=CARTESIAN_POINT('Ctrl Pts',(0.475385173604076,24.814339074427,15.4817553369712));
#65890=CARTESIAN_POINT('Ctrl Pts',(-0.770842812967098,24.9650411471909,
15.413615855556));
#65891=CARTESIAN_POINT('Ctrl Pts',(-1.8816802076409,25.1293818886154,14.570924124473));
#65892=CARTESIAN_POINT('Ctrl Pts',(-2.24621461637246,25.3071361639334,13.1059467520125));
#65893=CARTESIAN_POINT('Ctrl Pts',(-1.61366325932767,25.4836327911446,11.747168499655));
#65894=CARTESIAN_POINT('Ctrl Pts',(-0.278378180266116,25.6591480325535,
11.0868932263985));
#65895=CARTESIAN_POINT('Ctrl Pts',(1.17095166640344,25.8339657612004,11.4113524729003));
#65896=CARTESIAN_POINT('Ctrl Pts',(2.09391508043506,26.0083762241633,12.5688636664693));
#65897=CARTESIAN_POINT('Ctrl Pts',(2.0874158269108,26.1826680912139,14.0486955369498));
#65898=CARTESIAN_POINT('Ctrl Pts',(1.15336459345638,26.3571369042277,15.1984251330648));
#65899=CARTESIAN_POINT('Ctrl Pts',(-0.298634256840866,26.5320736766806,
15.5091115507522));
#65900=CARTESIAN_POINT('Ctrl Pts',(-1.63160944640033,26.7077658150152,14.8401215472852));
#65901=CARTESIAN_POINT('Ctrl Pts',(-2.25131622058411,26.8844963732798,13.4725419062569));
#65902=CARTESIAN_POINT('Ctrl Pts',(-1.9059670914065,27.0477020505508,12.1316352867466));
#65903=CARTESIAN_POINT('Ctrl Pts',(-0.979854205581052,27.1972220957301,
11.3101474584682));
#65904=CARTESIAN_POINT('Ctrl Pts',(0.116931174873669,27.3327865136187,11.0664240469857));
#65905=CARTESIAN_POINT('Ctrl Pts',(1.19700060462999,27.4694517064889,11.3906384812928));
#65906=CARTESIAN_POINT('Ctrl Pts',(2.27146199137299,27.6532725125067,12.4789085973207));
#65907=CARTESIAN_POINT('Ctrl Pts',(2.2944534071564,27.8396822715647,14.1613568274049));
#65908=CARTESIAN_POINT('Ctrl Pts',(1.21188254212424,28.0290394905166,15.3070004216219));
#65909=CARTESIAN_POINT('Ctrl Pts',(0.0845872396768884,28.1726048993493,
15.6701949854082));
#65910=CARTESIAN_POINT('Ctrl Pts',(-1.09545910495886,28.3177922830621,15.4348199567659));
#65911=CARTESIAN_POINT('Ctrl Pts',(-2.02084877192932,28.4646665841871,14.6463384527996));
#65912=CARTESIAN_POINT('Ctrl Pts',(-2.45024610790034,28.6132878065287,13.494059057564));
#65913=CARTESIAN_POINT('Ctrl Pts',(-2.24537056320646,28.7804215714648,12.1252219559702));
#65914=CARTESIAN_POINT('Ctrl Pts',(-1.17335673448093,28.966899793215,10.9580237712631));
#65915=CARTESIAN_POINT('Ctrl Pts',(0.558777587586121,29.1736969761794,10.6986804799736));
#65916=CARTESIAN_POINT('Ctrl Pts',(2.36919813842405,29.418962526061,11.7378175469893));
#65917=CARTESIAN_POINT('Ctrl Pts',(2.89725560020412,29.7050532180518,14.2840477585018));
#65918=CARTESIAN_POINT('Ctrl Pts',(0.696448044363527,30.0347471463454,16.3532177295756));
#65919=CARTESIAN_POINT('Ctrl Pts',(-1.76982090953937,30.3159478043037,15.6816271858541));
#65920=CARTESIAN_POINT('Ctrl Pts',(-2.73900717504778,30.5446729887148,14.046826392024));
#65921=CARTESIAN_POINT('Ctrl Pts',(-2.77339105257539,30.6602644219914,13.0943059059134));
#65922=CARTESIAN_POINT('Ctrl Pts',(-2.6710485091933,30.7183585763046,12.640190198649));
#65923=CARTESIAN_POINT('Ctrl Pts',(2.2183610351321,22.5005350637259,13.3));
#65924=CARTESIAN_POINT('Ctrl Pts',(2.20732208326138,22.5484915142731,13.699758215172));
#65925=CARTESIAN_POINT('Ctrl Pts',(2.00027014846976,22.6410090565288,14.4071397348093));
#65926=CARTESIAN_POINT('Ctrl Pts',(0.912554002081777,22.8271444189337,15.5210532308397));
#65927=CARTESIAN_POINT('Ctrl Pts',(-1.15691805263464,23.0546136929354,15.5542757223008));
#65928=CARTESIAN_POINT('Ctrl Pts',(-2.49093046002719,23.3236757288067,13.4873773346461));
#65929=CARTESIAN_POINT('Ctrl Pts',(-1.56109853564162,23.5590329351607,11.5561927120739));
#65930=CARTESIAN_POINT('Ctrl Pts',(0.111714907485613,23.7631934622475,11.0836004070663));
#65931=CARTESIAN_POINT('Ctrl Pts',(1.47049081457418,23.937113829779,11.6547566535498));
#65932=CARTESIAN_POINT('Ctrl Pts',(2.11308441896366,24.0958873357551,12.8401056174219));
#65933=CARTESIAN_POINT('Ctrl Pts',(1.99467970110352,24.239898017344,14.0270799159506));
#65934=CARTESIAN_POINT('Ctrl Pts',(1.38548250386768,24.3693958001383,14.9083990575687));
#65935=CARTESIAN_POINT('Ctrl Pts',(0.423315749518031,24.4989021004607,15.3807411268428));
#65936=CARTESIAN_POINT('Ctrl Pts',(-0.76799412090761,24.6429550384991,15.3208893112581));
#65937=CARTESIAN_POINT('Ctrl Pts',(-1.84600291649318,24.8017913824285,14.5126035235537));
#65938=CARTESIAN_POINT('Ctrl Pts',(-2.21162965654954,24.9758449066832,13.0806552944285));
#65939=CARTESIAN_POINT('Ctrl Pts',(-1.59284740696533,25.1509653949324,11.7285318827829));
#65940=CARTESIAN_POINT('Ctrl Pts',(-0.255089672331717,25.3274441413117,
11.055696404286));
#65941=CARTESIAN_POINT('Ctrl Pts',(1.22362929125862,25.5055533284942,11.375592128919));
#65942=CARTESIAN_POINT('Ctrl Pts',(2.18484293549448,25.685562905358,12.5629954185504));
#65943=CARTESIAN_POINT('Ctrl Pts',(2.18980186105923,25.8677211661319,14.1093087532237));
#65944=CARTESIAN_POINT('Ctrl Pts',(1.21143310986873,26.0522683809189,15.3328638222202));
#65945=CARTESIAN_POINT('Ctrl Pts',(-0.339059659776909,26.239423973137,15.6773824073839));
#65946=CARTESIAN_POINT('Ctrl Pts',(-1.78569333727131,26.4293900673351,14.9656927457296));
#65947=CARTESIAN_POINT('Ctrl Pts',(-2.47416163046515,26.6223483339623,13.4781429424522));
#65948=CARTESIAN_POINT('Ctrl Pts',(-2.10549777162261,26.8021159857552,11.9983797771691));
#65949=CARTESIAN_POINT('Ctrl Pts',(-1.08527208402701,26.9679412463559,11.0798865261764));
#65950=CARTESIAN_POINT('Ctrl Pts',(0.13536334826752,27.1190847834831,10.7992190624231));
#65951=CARTESIAN_POINT('Ctrl Pts',(1.34759162461277,27.2721726601904,11.1535834603927));
#65952=CARTESIAN_POINT('Ctrl Pts',(2.56489813381872,27.4789264362032,12.3683976939296));
#65953=CARTESIAN_POINT('Ctrl Pts',(2.6061432041599,27.6896926752336,14.2700173133308));
#65954=CARTESIAN_POINT('Ctrl Pts',(1.38712717931538,27.904534103112,15.5784431958487));
#65955=CARTESIAN_POINT('Ctrl Pts',(0.10895953963572,28.0677021630343,15.9998907204716));
#65956=CARTESIAN_POINT('Ctrl Pts',(-1.23535153591744,28.2329034487015,15.7412149433557));
#65957=CARTESIAN_POINT('Ctrl Pts',(-2.29471625897426,28.4001240169453,14.8505918592972));
#65958=CARTESIAN_POINT('Ctrl Pts',(-2.79203814947656,28.5693430024324,13.5420011391188));
#65959=CARTESIAN_POINT('Ctrl Pts',(-2.56877406678316,28.7595514723432,11.9828803214993));
#65960=CARTESIAN_POINT('Ctrl Pts',(-1.35822219944082,28.9715360098461,10.6489229561444));
#65961=CARTESIAN_POINT('Ctrl Pts',(0.604663322317292,29.2061196861259,10.3434395952506));
#65962=CARTESIAN_POINT('Ctrl Pts',(2.65874145703642,29.483527190347,11.5076918928945));
#65963=CARTESIAN_POINT('Ctrl Pts',(3.26545304863587,29.8056282097385,14.3719790847457));
#65964=CARTESIAN_POINT('Ctrl Pts',(0.813056733395563,30.1742234622136,16.6938678232326));
#65965=CARTESIAN_POINT('Ctrl Pts',(-1.92333210556604,30.4859835815331,15.9577643257455));
#65966=CARTESIAN_POINT('Ctrl Pts',(-2.9975940068159,30.737754420159,14.1632918818718));
#65967=CARTESIAN_POINT('Ctrl Pts',(-3.0398715397772,30.8643566407983,13.1202658630658));
#65968=CARTESIAN_POINT('Ctrl Pts',(-2.93050484752353,30.9278155421559,12.623720964138));
#65969=CARTESIAN_POINT('Ctrl Pts',(1.9,22.4,13.3));
#65970=CARTESIAN_POINT('Ctrl Pts',(1.89077819837431,22.4422021414379,13.6519691914269));
#65971=CARTESIAN_POINT('Ctrl Pts',(1.71537787585695,22.5206083204434,14.2515774145128));
#65972=CARTESIAN_POINT('Ctrl Pts',(0.776895987153429,22.6819257904964,15.2190094254541));
#65973=CARTESIAN_POINT('Ctrl Pts',(-1.01219784483332,22.8782378453878,15.2495646232149));
#65974=CARTESIAN_POINT('Ctrl Pts',(-2.18535724516091,23.1134574970354,13.4517991919584));
#65975=CARTESIAN_POINT('Ctrl Pts',(-1.37199074496505,23.3213768149546,11.7396096714547));
#65976=CARTESIAN_POINT('Ctrl Pts',(0.123403026550972,23.504121058761,11.3105725465261));
#65977=CARTESIAN_POINT('Ctrl Pts',(1.35501251051576,23.661466918215,11.8220255257895));
#65978=CARTESIAN_POINT('Ctrl Pts',(1.94832765695265,23.8068375246815,12.9042814161785));
#65979=CARTESIAN_POINT('Ctrl Pts',(1.84336678935325,23.9401410891422,14.0034773628334));
#65980=CARTESIAN_POINT('Ctrl Pts',(1.27754402361024,24.0611907458831,14.8296511355055));
#65981=CARTESIAN_POINT('Ctrl Pts',(0.371246325431991,24.1834651264945,15.2797269167144));
#65982=CARTESIAN_POINT('Ctrl Pts',(-0.765145428848119,24.3208689298072,
15.2281627669602));
#65983=CARTESIAN_POINT('Ctrl Pts',(-1.81032562534546,24.4742008762416,14.4542829226342));
#65984=CARTESIAN_POINT('Ctrl Pts',(-2.17704469672661,24.6445536494329,13.0553638368446));
#65985=CARTESIAN_POINT('Ctrl Pts',(-1.57203155460298,24.8182979987203,11.709895265911));
#65986=CARTESIAN_POINT('Ctrl Pts',(-0.23180116439731,24.99574025007,11.0244995821736));
#65987=CARTESIAN_POINT('Ctrl Pts',(1.27630691611381,25.1771408957878,11.3398317849377));
#65988=CARTESIAN_POINT('Ctrl Pts',(2.27577079055389,25.3627495865527,12.5571271706314));
#65989=CARTESIAN_POINT('Ctrl Pts',(2.29218789520766,25.5527742410498,14.1699219694977));
#65990=CARTESIAN_POINT('Ctrl Pts',(1.26950162628108,25.74739985761,15.4673025113756));
#65991=CARTESIAN_POINT('Ctrl Pts',(-0.379485062712953,25.9467742695935,
15.8456532640155));
#65992=CARTESIAN_POINT('Ctrl Pts',(-1.93977722814229,26.1510143196549,15.0912639441738));
#65993=CARTESIAN_POINT('Ctrl Pts',(-2.69700704034618,26.3602002946448,13.4837439786473));
#65994=CARTESIAN_POINT('Ctrl Pts',(-2.30502845183871,26.5565299209596,11.8651242675914));
#65995=CARTESIAN_POINT('Ctrl Pts',(-1.19068996247298,26.7386603969818,10.8496255938845));
#65996=CARTESIAN_POINT('Ctrl Pts',(0.153795521661376,26.9053830533475,10.5320140778605));
#65997=CARTESIAN_POINT('Ctrl Pts',(1.49818264459556,27.0748936138919,10.9165284394926));
#65998=CARTESIAN_POINT('Ctrl Pts',(2.85833427626445,27.3045803598996,12.2578867905387));
#65999=CARTESIAN_POINT('Ctrl Pts',(2.9178330011634,27.5397030789025,14.3786777992568));
#66000=CARTESIAN_POINT('Ctrl Pts',(1.56237181650653,27.7800287157075,15.8498859700755));
#66001=CARTESIAN_POINT('Ctrl Pts',(0.13333183959455,27.9627994267194,16.3295864555349));
#66002=CARTESIAN_POINT('Ctrl Pts',(-1.37524396687603,28.148014614341,16.0476099299455));
#66003=CARTESIAN_POINT('Ctrl Pts',(-2.5685837460192,28.3355814497034,15.0548452657946));
#66004=CARTESIAN_POINT('Ctrl Pts',(-3.13383019105279,28.5253981983361,13.5899432206735));
#66005=CARTESIAN_POINT('Ctrl Pts',(-2.89217757035986,28.7386813732216,11.8405386870284));
#66006=CARTESIAN_POINT('Ctrl Pts',(-1.54308766440071,28.9761722264772,10.3398221410258));
#66007=CARTESIAN_POINT('Ctrl Pts',(0.650549057048467,29.2385423960724,9.98819871052755));
#66008=CARTESIAN_POINT('Ctrl Pts',(2.94828477564879,29.548091854633,11.2775662387998));
#66009=CARTESIAN_POINT('Ctrl Pts',(3.63365049706761,29.9062032014252,14.4599104109895));
#66010=CARTESIAN_POINT('Ctrl Pts',(0.929665422427599,30.3136997780818,17.0345179168896));
#66011=CARTESIAN_POINT('Ctrl Pts',(-2.07684330159272,30.6560193587624,16.2339014656368));
#66012=CARTESIAN_POINT('Ctrl Pts',(-3.25618083858403,30.9308358516032,14.2797573717195));
#66013=CARTESIAN_POINT('Ctrl Pts',(-3.306352026979,31.0684488596052,13.1462258202182));
#66014=CARTESIAN_POINT('Ctrl Pts',(-3.18996118585377,31.1372725080072,12.6072517296268));
#66015=CARTESIAN_POINT('',(2.85,22.7,13.3));
#66016=CARTESIAN_POINT('Ctrl Pts',(-0.969619743608971,35.5250590498763,
10.2301745864681));
#66017=CARTESIAN_POINT('Ctrl Pts',(-0.293405597888406,35.6135359928547,
10.017227865461));
#66018=CARTESIAN_POINT('Ctrl Pts',(1.20310012018456,35.7904514013391,10.0572891405987));
#66019=CARTESIAN_POINT('Ctrl Pts',(2.93390863505459,36.0553071829586,11.48394067231));
#66020=CARTESIAN_POINT('Ctrl Pts',(3.41758282565779,36.319305470682,13.6665663047758));
#66021=CARTESIAN_POINT('Ctrl Pts',(2.45975719166707,36.5820762567064,15.6749533869058));
#66022=CARTESIAN_POINT('Ctrl Pts',(0.481163202010952,36.8432697896237,16.6627535697665));
#66023=CARTESIAN_POINT('Ctrl Pts',(-1.67190062807935,37.1025582194331,16.2252409039492));
#66024=CARTESIAN_POINT('Ctrl Pts',(-3.08306248478425,37.359605173675,14.572269215861));
#66025=CARTESIAN_POINT('Ctrl Pts',(-3.19643759372744,37.6423848448201,12.1766162167722));
#66026=CARTESIAN_POINT('Ctrl Pts',(-1.38811732008393,37.9493821651013,10.154502174276));
#66027=CARTESIAN_POINT('Ctrl Pts',(1.03278567716216,38.2237370964296,10.2682868731901));
#66028=CARTESIAN_POINT('Ctrl Pts',(2.3809218660535,38.4400825676405,11.4276672457298));
#66029=CARTESIAN_POINT('Ctrl Pts',(2.92531221614793,38.6007121886329,12.628817144057));
#66030=CARTESIAN_POINT('Ctrl Pts',(2.89919394194952,38.7596516023286,13.9328342740706));
#66031=CARTESIAN_POINT('Ctrl Pts',(2.1402434917003,38.9692434239079,15.4825527531054));
#66032=CARTESIAN_POINT('Ctrl Pts',(0.0844388902172162,39.2267424133018,
16.4533543876597));
#66033=CARTESIAN_POINT('Ctrl Pts',(-2.12137754341091,39.5031047174653,15.4071077046148));
#66034=CARTESIAN_POINT('Ctrl Pts',(-2.84263724025941,39.7486842815273,13.4542134019695));
#66035=CARTESIAN_POINT('Ctrl Pts',(-2.29285373611436,39.9652776471272,11.7066022813769));
#66036=CARTESIAN_POINT('Ctrl Pts',(-0.809367529129827,40.177402665634,10.6913151614677));
#66037=CARTESIAN_POINT('Ctrl Pts',(0.505559239349309,40.333140300507,10.7738392885579));
#66038=CARTESIAN_POINT('Ctrl Pts',(1.23843792453526,40.4355732287232,11.1503985996136));
#66039=CARTESIAN_POINT('Ctrl Pts',(1.67669838949815,40.5034925168063,11.475947565662));
#66040=CARTESIAN_POINT('Ctrl Pts',(2.28287603261652,40.6213815738627,12.2188580969849));
#66041=CARTESIAN_POINT('Ctrl Pts',(2.53798439367783,40.7870458540183,13.5975998584707));
#66042=CARTESIAN_POINT('Ctrl Pts',(1.77492212034956,40.9815214196383,15.0584075661407));
#66043=CARTESIAN_POINT('Ctrl Pts',(0.307669421971351,41.1717923357691,15.7241021006855));
#66044=CARTESIAN_POINT('Ctrl Pts',(-1.22506403825479,41.3579933663104,15.3538045685215));
#66045=CARTESIAN_POINT('Ctrl Pts',(-2.18442835856201,41.540291349872,14.1430778842092));
#66046=CARTESIAN_POINT('Ctrl Pts',(-2.19211575387567,41.6891193359005,12.8837149285007));
#66047=CARTESIAN_POINT('Ctrl Pts',(-1.79903872344835,41.7917680008934,12.1474870326954));
#66048=CARTESIAN_POINT('Ctrl Pts',(-1.48461936224863,41.8500065969429,11.8006059047461));
#66049=CARTESIAN_POINT('Ctrl Pts',(-0.936263451520069,41.9369461449212,
11.3661693008175));
#66050=CARTESIAN_POINT('Ctrl Pts',(0.120072761527529,42.0658359418734,11.0942972486871));
#66051=CARTESIAN_POINT('Ctrl Pts',(1.43243517464226,42.234704644183,11.6660157935677));
#66052=CARTESIAN_POINT('Ctrl Pts',(2.10042667241831,42.4008672345781,12.9032804607227));
#66053=CARTESIAN_POINT('Ctrl Pts',(1.84785783997348,42.5828304210762,14.4264829178442));
#66054=CARTESIAN_POINT('Ctrl Pts',(0.44228534019957,42.7800073483584,15.4529020688146));
#66055=CARTESIAN_POINT('Ctrl Pts',(-1.37655749427508,42.9922179535626,14.9849431781379));
#66056=CARTESIAN_POINT('Ctrl Pts',(-2.15418937753764,43.2023326687039,13.295902856596));
#66057=CARTESIAN_POINT('Ctrl Pts',(-1.3568352207939,43.4112150248688,11.6324213557684));
#66058=CARTESIAN_POINT('Ctrl Pts',(0.440098590354474,43.6197411074281,11.197323805629));
#66059=CARTESIAN_POINT('Ctrl Pts',(1.6666239589875,43.7939276913608,12.1238487379755));
#66060=CARTESIAN_POINT('Ctrl Pts',(1.96028188226055,43.9339647282883,13.2369884585598));
#66061=CARTESIAN_POINT('Ctrl Pts',(1.76057565116699,44.0745948763178,14.3753735947725));
#66062=CARTESIAN_POINT('Ctrl Pts',(0.601463815507247,44.2517749140429,15.4227810305552));
#66063=CARTESIAN_POINT('Ctrl Pts',(-1.29162186703593,44.4674365769801,15.1369988331886));
#66064=CARTESIAN_POINT('Ctrl Pts',(-2.16357425753909,44.6625228061157,13.6556127826875));
#66065=CARTESIAN_POINT('Ctrl Pts',(-1.87153826486548,44.8361904377402,12.2281811299447));
#66066=CARTESIAN_POINT('Ctrl Pts',(-1.124208757008,44.9620959723648,11.4873485185699));
#66067=CARTESIAN_POINT('Ctrl Pts',(-0.344208843748469,45.0640384861851,
11.2133990437453));
#66068=CARTESIAN_POINT('Ctrl Pts',(0.305542062754602,45.1443340519541,11.1837221225817));
#66069=CARTESIAN_POINT('Ctrl Pts',(0.965600074924294,45.2285945750684,11.3652955927471));
#66070=CARTESIAN_POINT('Ctrl Pts',(1.75770762590764,45.3464019646695,11.9033594103926));
#66071=CARTESIAN_POINT('Ctrl Pts',(2.34064770972088,45.4958733909137,13.0257905767835));
#66072=CARTESIAN_POINT('Ctrl Pts',(2.05691682344594,45.6789904927352,14.5511095312853));
#66073=CARTESIAN_POINT('Ctrl Pts',(0.871285117834535,45.8660473054438,15.6011188018465));
#66074=CARTESIAN_POINT('Ctrl Pts',(-0.744178145769051,46.0572040445543,
15.702809222116));
#66075=CARTESIAN_POINT('Ctrl Pts',(-2.11039561200266,46.2525955949688,14.7696884134947));
#66076=CARTESIAN_POINT('Ctrl Pts',(-2.62495996595091,46.4523253192325,13.1583436840268));
#66077=CARTESIAN_POINT('Ctrl Pts',(-2.22701969031422,46.5884211851561,12.0776096121419));
#66078=CARTESIAN_POINT('Ctrl Pts',(-1.87713189663534,46.657212827205,11.6515692922621));
#66079=CARTESIAN_POINT('Ctrl Pts',(-0.928524254695599,35.7529573111631,
10.4693566435768));
#66080=CARTESIAN_POINT('Ctrl Pts',(-0.302351448403887,35.8349249624316,
10.2712100694345));
#66081=CARTESIAN_POINT('Ctrl Pts',(1.07964142130674,35.9983042873203,10.3077443607092));
#66082=CARTESIAN_POINT('Ctrl Pts',(2.66892271900442,36.2414530879768,11.6170450699432));
#66083=CARTESIAN_POINT('Ctrl Pts',(3.1109355193755,36.4824792190626,13.6096159864436));
#66084=CARTESIAN_POINT('Ctrl Pts',(2.2412653402876,36.7211720735862,15.4341158566646));
#66085=CARTESIAN_POINT('Ctrl Pts',(0.452404820286235,36.9573452503665,16.3276102496121));
#66086=CARTESIAN_POINT('Ctrl Pts',(-1.48645903874779,37.1908337232594,15.9340132840584));
#66087=CARTESIAN_POINT('Ctrl Pts',(-2.75303462194856,37.4214809426201,14.4511194819745));
#66088=CARTESIAN_POINT('Ctrl Pts',(-2.85492986041186,37.6744542905615,12.3079979573691));
#66089=CARTESIAN_POINT('Ctrl Pts',(-1.24193668279672,37.9483231609776,10.5039796610413));
#66090=CARTESIAN_POINT('Ctrl Pts',(0.913112028660612,38.1925516538795,10.604645079803));
#66091=CARTESIAN_POINT('Ctrl Pts',(2.11300131054057,38.3850155279473,11.63525163892));
#66092=CARTESIAN_POINT('Ctrl Pts',(2.59791237230024,38.5278949222772,12.7033537235139));
#66093=CARTESIAN_POINT('Ctrl Pts',(2.57545282267576,38.6692982128313,13.8634999863281));
#66094=CARTESIAN_POINT('Ctrl Pts',(1.90093268976562,38.8558656519239,15.2433560739298));
#66095=CARTESIAN_POINT('Ctrl Pts',(0.0696743896235553,39.0853830840031,
16.1109546339611));
#66096=CARTESIAN_POINT('Ctrl Pts',(-1.90410487343739,39.3324996979054,15.1787107387759));
#66097=CARTESIAN_POINT('Ctrl Pts',(-2.55456593756854,39.5529976676009,13.4263717799337));
#66098=CARTESIAN_POINT('Ctrl Pts',(-2.06165747168906,39.748327985643,11.8495201010784));
#66099=CARTESIAN_POINT('Ctrl Pts',(-0.718798232809231,39.9406424887904,
10.9261681097463));
#66100=CARTESIAN_POINT('Ctrl Pts',(0.48085385964531,40.0827133731717,10.9984774691904));
#66101=CARTESIAN_POINT('Ctrl Pts',(1.15291310828357,40.1765676975719,11.3424147239867));
#66102=CARTESIAN_POINT('Ctrl Pts',(1.555680829885,40.2389142093674,11.6405819896993));
#66103=CARTESIAN_POINT('Ctrl Pts',(2.11498582008125,40.3474355071447,12.3232392027595));
#66104=CARTESIAN_POINT('Ctrl Pts',(2.35530702507243,40.5008571269339,13.5991552068882));
#66105=CARTESIAN_POINT('Ctrl Pts',(1.6475116476446,40.6825591967348,14.9664523143975));
#66106=CARTESIAN_POINT('Ctrl Pts',(0.266043325204939,40.8620650218924,15.6000893188088));
#66107=CARTESIAN_POINT('Ctrl Pts',(-1.19652997111221,41.0395781865116,15.2538100228942));
#66108=CARTESIAN_POINT('Ctrl Pts',(-2.1272252638981,41.2153253649343,14.0915006276765));
#66109=CARTESIAN_POINT('Ctrl Pts',(-2.14149232020009,41.360512507773,12.8631716507578));
#66110=CARTESIAN_POINT('Ctrl Pts',(-1.7577029360263,41.4615792510597,12.136583923261));
#66111=CARTESIAN_POINT('Ctrl Pts',(-1.44811693946317,41.519191370033,11.7921953718333));
#66112=CARTESIAN_POINT('Ctrl Pts',(-0.905905233845331,41.6054687313099,
11.358829834061));
#66113=CARTESIAN_POINT('Ctrl Pts',(0.148783283224247,41.7344084333373,11.080034544991));
#66114=CARTESIAN_POINT('Ctrl Pts',(1.48264268622566,41.905567866661,11.6498940810064));
#66115=CARTESIAN_POINT('Ctrl Pts',(2.17804706649762,42.0762312421305,12.9152113329992));
#66116=CARTESIAN_POINT('Ctrl Pts',(1.9281502881629,42.2656152135407,14.5019643907221));
#66117=CARTESIAN_POINT('Ctrl Pts',(0.454206047228391,42.4740014059576,15.6010773688966));
#66118=CARTESIAN_POINT('Ctrl Pts',(-1.50492058521437,42.7020851652482,15.1190889953041));
#66119=CARTESIAN_POINT('Ctrl Pts',(-2.37393678440876,42.9315346015318,13.2844054826429));
#66120=CARTESIAN_POINT('Ctrl Pts',(-1.51093073900629,43.1629797347666,11.4325359425679));
#66121=CARTESIAN_POINT('Ctrl Pts',(0.499870888212584,43.397023065096,10.9221304640026));
#66122=CARTESIAN_POINT('Ctrl Pts',(1.90249455419702,43.5946859167395,11.9584394585814));
#66123=CARTESIAN_POINT('Ctrl Pts',(2.24947803672872,43.7546603065521,13.226802610543));
#66124=CARTESIAN_POINT('Ctrl Pts',(2.03249683098778,43.9159410443849,14.5338782293896));
#66125=CARTESIAN_POINT('Ctrl Pts',(0.709081435241008,44.1201506791162,15.7540073459432));
#66126=CARTESIAN_POINT('Ctrl Pts',(-1.48517107917157,44.3698059824277,15.4441339572982));
#66127=CARTESIAN_POINT('Ctrl Pts',(-2.51179701745175,44.5961435788324,13.7348300181415));
#66128=CARTESIAN_POINT('Ctrl Pts',(-2.18702749691963,44.7976270138815,12.0762756711685));
#66129=CARTESIAN_POINT('Ctrl Pts',(-1.32803235969944,44.9435697167804,11.210705134577));
#66130=CARTESIAN_POINT('Ctrl Pts',(-0.427955672068899,45.0615747648806,
10.8863098737508));
#66131=CARTESIAN_POINT('Ctrl Pts',(0.322903160144552,45.1544230560825,10.8459404674635));
#66132=CARTESIAN_POINT('Ctrl Pts',(1.08654236719346,45.2517202654121,11.049522088885));
#66133=CARTESIAN_POINT('Ctrl Pts',(2.00430019963811,45.3875248410472,11.6625506339721));
#66134=CARTESIAN_POINT('Ctrl Pts',(2.68332056852154,45.5593334049225,12.9477790937394));
#66135=CARTESIAN_POINT('Ctrl Pts',(2.37029763305347,45.7688203617572,14.6946173751069));
#66136=CARTESIAN_POINT('Ctrl Pts',(1.02903008263469,45.9816339492315,15.8973953661167));
#66137=CARTESIAN_POINT('Ctrl Pts',(-0.79656024254013,46.1977617860478,16.0229620984205));
#66138=CARTESIAN_POINT('Ctrl Pts',(-2.33618804037084,46.4171691651988,14.9835519669358));
#66139=CARTESIAN_POINT('Ctrl Pts',(-2.91868728668747,46.6397983888878,13.190566256523));
#66140=CARTESIAN_POINT('Ctrl Pts',(-2.48421628078386,46.7903156144816,11.9933694045403));
#66141=CARTESIAN_POINT('Ctrl Pts',(-2.10165986920628,46.8660802928157,11.5219695835744));
#66142=CARTESIAN_POINT('Ctrl Pts',(-0.887428765782225,35.9808555724499,
10.7085387006856));
#66143=CARTESIAN_POINT('Ctrl Pts',(-0.311297298919368,36.0563139320087,
10.5251922734079));
#66144=CARTESIAN_POINT('Ctrl Pts',(0.956182722428914,36.2061571733015,10.5581995808197));
#66145=CARTESIAN_POINT('Ctrl Pts',(2.40393680295423,36.427598992995,11.7501494675763));
#66146=CARTESIAN_POINT('Ctrl Pts',(2.8042882130932,36.6456529674432,13.5526656681114));
#66147=CARTESIAN_POINT('Ctrl Pts',(2.02277348890814,36.8602678904659,15.1932783264235));
#66148=CARTESIAN_POINT('Ctrl Pts',(0.42364643856152,37.0714207111093,15.9924669294578));
#66149=CARTESIAN_POINT('Ctrl Pts',(-1.30101744941622,37.2791092270855,15.6427856641674));
#66150=CARTESIAN_POINT('Ctrl Pts',(-2.42300675911287,37.4833567115649,14.3299697480881));
#66151=CARTESIAN_POINT('Ctrl Pts',(-2.51342212709626,37.7065237363028,12.4393796979659));
#66152=CARTESIAN_POINT('Ctrl Pts',(-1.09575604550953,37.947264156854,10.8534571478067));
#66153=CARTESIAN_POINT('Ctrl Pts',(0.793438380159059,38.1613662113293,10.9410032864159));
#66154=CARTESIAN_POINT('Ctrl Pts',(1.84508075502765,38.3299484882543,11.8428360321102));
#66155=CARTESIAN_POINT('Ctrl Pts',(2.27051252845255,38.4550776559217,12.7778903029709));
#66156=CARTESIAN_POINT('Ctrl Pts',(2.251711703402,38.578944823334,13.7941656985855));
#66157=CARTESIAN_POINT('Ctrl Pts',(1.66162188783096,38.74248787994,15.0041593947542));
#66158=CARTESIAN_POINT('Ctrl Pts',(0.0549098890299007,38.9440237547044,
15.7685548802624));
#66159=CARTESIAN_POINT('Ctrl Pts',(-1.68683220346387,39.1618946783455,14.9503137729369));
#66160=CARTESIAN_POINT('Ctrl Pts',(-2.26649463487766,39.3573110536744,13.3985301578978));
#66161=CARTESIAN_POINT('Ctrl Pts',(-1.83046120726377,39.5313783241587,11.9924379207797));
#66162=CARTESIAN_POINT('Ctrl Pts',(-0.628228936488634,39.703882311947,11.1610210580248));
#66163=CARTESIAN_POINT('Ctrl Pts',(0.456148479941315,39.8322864458366,11.2231156498228));
#66164=CARTESIAN_POINT('Ctrl Pts',(1.06738829203189,39.9175621664208,11.5344308483598));
#66165=CARTESIAN_POINT('Ctrl Pts',(1.43466327027188,39.9743359019283,11.8052164137364));
#66166=CARTESIAN_POINT('Ctrl Pts',(1.94709560754598,40.0734894404267,12.4276203085341));
#66167=CARTESIAN_POINT('Ctrl Pts',(2.17262965646704,40.2146683998495,13.6007105553058));
#66168=CARTESIAN_POINT('Ctrl Pts',(1.52010117493962,40.3835969738312,14.8744970626542));
#66169=CARTESIAN_POINT('Ctrl Pts',(0.224417228438533,40.5523377080158,15.4760765369319));
#66170=CARTESIAN_POINT('Ctrl Pts',(-1.16799590396964,40.7211630067128,15.1538154772671));
#66171=CARTESIAN_POINT('Ctrl Pts',(-2.07002216923418,40.8903593799966,14.039923371144));
#66172=CARTESIAN_POINT('Ctrl Pts',(-2.09086888652449,41.0319056796453,12.8426283730148));
#66173=CARTESIAN_POINT('Ctrl Pts',(-1.71636714860424,41.131390501226,12.1256808138265));
#66174=CARTESIAN_POINT('Ctrl Pts',(-1.41161451667769,41.188376143123,11.7837848389202));
#66175=CARTESIAN_POINT('Ctrl Pts',(-0.875547016170588,41.2739913176985,
11.3514903673047));
#66176=CARTESIAN_POINT('Ctrl Pts',(0.177493804920967,41.4029809248012,11.0657718412948));
#66177=CARTESIAN_POINT('Ctrl Pts',(1.53285019780908,41.576431089139,11.633772368445));
#66178=CARTESIAN_POINT('Ctrl Pts',(2.25566746057696,41.751595249683,12.9271422052756));
#66179=CARTESIAN_POINT('Ctrl Pts',(2.00844273635235,41.9484000060053,14.5774458636001));
#66180=CARTESIAN_POINT('Ctrl Pts',(0.466126754257215,42.1679954635567,15.7492526689788));
#66181=CARTESIAN_POINT('Ctrl Pts',(-1.63328367615364,42.4119523769338,15.25323481247));
#66182=CARTESIAN_POINT('Ctrl Pts',(-2.5936841912799,42.6607365343597,13.2729081086898));
#66183=CARTESIAN_POINT('Ctrl Pts',(-1.66502625721867,42.9147444446644,11.2326505293673));
#66184=CARTESIAN_POINT('Ctrl Pts',(0.559643186070704,43.1743050227638,10.6469371223761));
#66185=CARTESIAN_POINT('Ctrl Pts',(2.13836514940656,43.3954441421182,11.7930301791872));
#66186=CARTESIAN_POINT('Ctrl Pts',(2.53867419119688,43.5753558848156,13.2166167625263));
#66187=CARTESIAN_POINT('Ctrl Pts',(2.30441801080858,43.7572872124519,14.6923828640066));
#66188=CARTESIAN_POINT('Ctrl Pts',(0.816699054974774,43.9885264441894,16.0852336613315));
#66189=CARTESIAN_POINT('Ctrl Pts',(-1.67872029130721,44.2721753878753,15.7512690814078));
#66190=CARTESIAN_POINT('Ctrl Pts',(-2.86001977736444,44.5297643515489,13.8140472535956));
#66191=CARTESIAN_POINT('Ctrl Pts',(-2.5025167289738,44.7590635900227,11.9243702123924));
#66192=CARTESIAN_POINT('Ctrl Pts',(-1.53185596239088,44.9250434611961,10.9340617505841));
#66193=CARTESIAN_POINT('Ctrl Pts',(-0.511702500389332,45.0591110435762,
10.5592207037563));
#66194=CARTESIAN_POINT('Ctrl Pts',(0.340264257534502,45.1645120602108,10.5081588123451));
#66195=CARTESIAN_POINT('Ctrl Pts',(1.20748465946262,45.2748459557558,10.733748585023));
#66196=CARTESIAN_POINT('Ctrl Pts',(2.25089277336859,45.428647717425,11.4217418575516));
#66197=CARTESIAN_POINT('Ctrl Pts',(3.02599342732222,45.6227934189313,12.8697676106951));
#66198=CARTESIAN_POINT('Ctrl Pts',(2.683678442661,45.8586502307792,14.8381252189284));
#66199=CARTESIAN_POINT('Ctrl Pts',(1.18677504743485,46.0972205930193,16.1936719303867));
#66200=CARTESIAN_POINT('Ctrl Pts',(-0.848942339311207,46.3383195275414,
16.3431149747252));
#66201=CARTESIAN_POINT('Ctrl Pts',(-2.56198046873903,46.5817427354286,15.197415520377));
#66202=CARTESIAN_POINT('Ctrl Pts',(-3.21241460742404,46.827271458543,13.2227888290192));
#66203=CARTESIAN_POINT('Ctrl Pts',(-2.74141287125351,46.992210043807,11.9091291969388));
#66204=CARTESIAN_POINT('Ctrl Pts',(-2.32618784177721,47.0749477584263,11.3923698748866));
#66205=CARTESIAN_POINT('Ctrl Pts',(-0.846333276868852,36.2087538337368,
10.9477207577944));
#66206=CARTESIAN_POINT('Ctrl Pts',(-0.32024314943485,36.2777029015855,10.7791744773813));
#66207=CARTESIAN_POINT('Ctrl Pts',(0.832724023551092,36.4140100592826,10.8086548009301));
#66208=CARTESIAN_POINT('Ctrl Pts',(2.13895088690405,36.6137448980134,11.8832538652094));
#66209=CARTESIAN_POINT('Ctrl Pts',(2.49764090681091,36.8088267158237,13.4957153497792));
#66210=CARTESIAN_POINT('Ctrl Pts',(1.80428163752868,36.9993637073457,14.9524407961822));
#66211=CARTESIAN_POINT('Ctrl Pts',(0.394888056836802,37.1854961718521,15.6573236093034));
#66212=CARTESIAN_POINT('Ctrl Pts',(-1.11557586008467,37.3673847309119,15.3515580442764));
#66213=CARTESIAN_POINT('Ctrl Pts',(-2.09297889627718,37.5452324805099,14.2088200142016));
#66214=CARTESIAN_POINT('Ctrl Pts',(-2.17191439378068,37.7385931820442,12.5707614385627));
#66215=CARTESIAN_POINT('Ctrl Pts',(-0.949575408222315,37.9462051527305,
11.202934634572));
#66216=CARTESIAN_POINT('Ctrl Pts',(0.673764731657505,38.1301807687792,11.2773614930289));
#66217=CARTESIAN_POINT('Ctrl Pts',(1.57716019951472,38.2748814485611,12.0504204253005));
#66218=CARTESIAN_POINT('Ctrl Pts',(1.94311268460486,38.382260389566,12.8524268824278));
#66219=CARTESIAN_POINT('Ctrl Pts',(1.92797058412824,38.4885914338368,13.724831410843));
#66220=CARTESIAN_POINT('Ctrl Pts',(1.42231108589628,38.6291101079561,14.7649627155785));
#66221=CARTESIAN_POINT('Ctrl Pts',(0.0401453884362414,38.8026644254056,
15.4261551265637));
#66222=CARTESIAN_POINT('Ctrl Pts',(-1.46955953349035,38.9912896587856,14.721916807098));
#66223=CARTESIAN_POINT('Ctrl Pts',(-1.97842333218679,39.161624439748,13.3706885358619));
#66224=CARTESIAN_POINT('Ctrl Pts',(-1.59926494283846,39.3144286626745,12.1353557404812));
#66225=CARTESIAN_POINT('Ctrl Pts',(-0.537659640168033,39.4671221351034,
11.3958740063034));
#66226=CARTESIAN_POINT('Ctrl Pts',(0.431443100237323,39.5818595185013,11.4477538304553));
#66227=CARTESIAN_POINT('Ctrl Pts',(0.981863475780215,39.6585566352696,11.7264469727329));
#66228=CARTESIAN_POINT('Ctrl Pts',(1.31364571065875,39.7097575944895,11.9698508377737));
#66229=CARTESIAN_POINT('Ctrl Pts',(1.77920539501069,39.7995433737088,12.5320014143087));
#66230=CARTESIAN_POINT('Ctrl Pts',(1.98995228786165,39.9284796727651,13.6022659037234));
#66231=CARTESIAN_POINT('Ctrl Pts',(1.39269070223466,40.0846347509277,14.782541810911));
#66232=CARTESIAN_POINT('Ctrl Pts',(0.182791131672126,40.2426103941391,15.3520637550552));
#66233=CARTESIAN_POINT('Ctrl Pts',(-1.13946183682706,40.402747826914,15.0538209316398));
#66234=CARTESIAN_POINT('Ctrl Pts',(-2.01281907457026,40.5653933950589,13.9883461146112));
#66235=CARTESIAN_POINT('Ctrl Pts',(-2.0402454528489,40.7032988515178,12.8220850952719));
#66236=CARTESIAN_POINT('Ctrl Pts',(-1.6750313611822,40.8012017513922,12.1147777043921));
#66237=CARTESIAN_POINT('Ctrl Pts',(-1.37511209389223,40.8575609162131,11.7753743060073));
#66238=CARTESIAN_POINT('Ctrl Pts',(-0.845188798495847,40.9425139040871,
11.3441509005482));
#66239=CARTESIAN_POINT('Ctrl Pts',(0.206204326617689,41.071553416265,11.0515091375987));
#66240=CARTESIAN_POINT('Ctrl Pts',(1.58305770939249,41.2472943116171,11.6176506558837));
#66241=CARTESIAN_POINT('Ctrl Pts',(2.33328785465628,41.4269592572355,12.9390730775521));
#66242=CARTESIAN_POINT('Ctrl Pts',(2.08873518454178,41.63118479847,14.652927336478));
#66243=CARTESIAN_POINT('Ctrl Pts',(0.478047461286037,41.8619895211559,15.8974279690608));
#66244=CARTESIAN_POINT('Ctrl Pts',(-1.76164676709294,42.1218195886195,15.3873806296362));
#66245=CARTESIAN_POINT('Ctrl Pts',(-2.81343159815104,42.3899384671876,13.2614107347368));
#66246=CARTESIAN_POINT('Ctrl Pts',(-1.81912177543106,42.6665091545622,11.0327651161668));
#66247=CARTESIAN_POINT('Ctrl Pts',(0.619415483928814,42.9515869804317,10.3717437807498));
#66248=CARTESIAN_POINT('Ctrl Pts',(2.37423574461608,43.196202367497,11.6276208997929));
#66249=CARTESIAN_POINT('Ctrl Pts',(2.82787034566504,43.3960514630793,13.2064309145094));
#66250=CARTESIAN_POINT('Ctrl Pts',(2.57633919062938,43.598633380519,14.8508874986237));
#66251=CARTESIAN_POINT('Ctrl Pts',(0.924316674708532,43.8569022092627,16.4164599767195));
#66252=CARTESIAN_POINT('Ctrl Pts',(-1.87226950344286,44.1745447933228,16.0584042055174));
#66253=CARTESIAN_POINT('Ctrl Pts',(-3.20824253727711,44.4633851242655,13.8932644890496));
#66254=CARTESIAN_POINT('Ctrl Pts',(-2.81800596102796,44.720500166164,11.7724647536162));
#66255=CARTESIAN_POINT('Ctrl Pts',(-1.73567956508233,44.9065172056118,10.6574183665911));
#66256=CARTESIAN_POINT('Ctrl Pts',(-0.595449328709767,45.0566473222717,
10.2321315337616));
#66257=CARTESIAN_POINT('Ctrl Pts',(0.357625354924448,45.1746010643391,10.1703771572269));
#66258=CARTESIAN_POINT('Ctrl Pts',(1.32842695173177,45.2979716460994,10.417975081161));
#66259=CARTESIAN_POINT('Ctrl Pts',(2.49748534709905,45.4697705938028,11.1809330811311));
#66260=CARTESIAN_POINT('Ctrl Pts',(3.36866628612287,45.68625343294,12.791756127651));
#66261=CARTESIAN_POINT('Ctrl Pts',(2.99705925226852,45.9484800998012,14.98163306275));
#66262=CARTESIAN_POINT('Ctrl Pts',(1.344520012235,46.2128072368071,16.4899484946569));
#66263=CARTESIAN_POINT('Ctrl Pts',(-0.901324436082288,46.4788772690349,
16.6632678510297));
#66264=CARTESIAN_POINT('Ctrl Pts',(-2.78777289710721,46.7463163056586,15.4112790738181));
#66265=CARTESIAN_POINT('Ctrl Pts',(-3.50614192816061,47.0147445281983,13.2550114015154));
#66266=CARTESIAN_POINT('Ctrl Pts',(-2.99860946172314,47.1941044731325,11.8248889893372));
#66267=CARTESIAN_POINT('Ctrl Pts',(-2.55071581434815,47.283815224037,11.2627701661989));
#66268=CARTESIAN_POINT('Ctrl Pts',(0.445846264208625,51.6658477063225,10.1121426167274));
#66269=CARTESIAN_POINT('Ctrl Pts',(1.16404206559057,51.7563468451642,10.2127508125863));
#66270=CARTESIAN_POINT('Ctrl Pts',(2.51084538435324,51.9352746543126,10.9131244582453));
#66271=CARTESIAN_POINT('Ctrl Pts',(3.43546172194773,52.2021181550985,12.9752067851171));
#66272=CARTESIAN_POINT('Ctrl Pts',(2.90016583811925,52.4660706907587,15.1448692652158));
#66273=CARTESIAN_POINT('Ctrl Pts',(1.15108978739344,52.7287973130357,16.5189201188617));
#66274=CARTESIAN_POINT('Ctrl Pts',(-1.05986975257263,52.9899432723208,16.5244632521564));
#66275=CARTESIAN_POINT('Ctrl Pts',(-2.79299924630602,53.2491804520227,15.1779379934512));
#66276=CARTESIAN_POINT('Ctrl Pts',(-3.32480009112557,53.5061795791808,13.0668764085995));
#66277=CARTESIAN_POINT('Ctrl Pts',(-2.48609575586124,53.7512036302333,11.1706159064391));
#66278=CARTESIAN_POINT('Ctrl Pts',(-0.797770401081796,53.9843201289036,
10.185651493995));
#66279=CARTESIAN_POINT('Ctrl Pts',(1.04695880052775,54.2056729305981,10.3005443775845));
#66280=CARTESIAN_POINT('Ctrl Pts',(2.75732496495255,54.4608671974974,11.5896407034103));
#66281=CARTESIAN_POINT('Ctrl Pts',(3.21092349295627,54.7478772279226,14.0799057085922));
#66282=CARTESIAN_POINT('Ctrl Pts',(1.40221873075584,55.0639890763963,16.2154026564162));
#66283=CARTESIAN_POINT('Ctrl Pts',(-1.32826248154208,55.3729279006118,16.1639039679761));
#66284=CARTESIAN_POINT('Ctrl Pts',(-2.46324596201939,55.5801574022457,14.7299387087418));
#66285=CARTESIAN_POINT('Ctrl Pts',(-2.6435839192479,55.6916462498041,13.8546566050136));
#66286=CARTESIAN_POINT('Ctrl Pts',(-2.67320101458777,55.7163812827006,13.6585635500232));
#66287=CARTESIAN_POINT('Ctrl Pts',(-2.68950031358046,55.7472242652351,13.4116438102883));
#66288=CARTESIAN_POINT('Ctrl Pts',(-2.67654859278463,55.7841138257671,13.1156583788531));
#66289=CARTESIAN_POINT('Ctrl Pts',(-2.58516892110096,55.8576484167926,12.5333589951533));
#66290=CARTESIAN_POINT('Ctrl Pts',(-2.04824134124429,56.015649313113,11.3456205112857));
#66291=CARTESIAN_POINT('Ctrl Pts',(-0.173069692310768,56.2537881248067,
10.397914739607));
#66292=CARTESIAN_POINT('Ctrl Pts',(1.88964734427024,56.5084479913319,11.2989850846241));
#66293=CARTESIAN_POINT('Ctrl Pts',(2.60142242705677,56.7341868214723,13.0778682424338));
#66294=CARTESIAN_POINT('Ctrl Pts',(2.14212645018905,56.9329559190759,14.6937475450074));
#66295=CARTESIAN_POINT('Ctrl Pts',(0.809504952860645,57.1274072773428,15.6643722638487));
#66296=CARTESIAN_POINT('Ctrl Pts',(-0.800286605823953,57.3176571401586,
15.6088479390479));
#66297=CARTESIAN_POINT('Ctrl Pts',(-2.00925065186011,57.5038425162973,14.5962951303551));
#66298=CARTESIAN_POINT('Ctrl Pts',(-2.33089364379664,57.6861283245531,13.0859315767866));
#66299=CARTESIAN_POINT('Ctrl Pts',(-1.66868325190088,57.8647115917552,11.7262435341493));
#66300=CARTESIAN_POINT('Ctrl Pts',(-0.335405361119072,58.0398094756416,
11.0746722341866));
#66301=CARTESIAN_POINT('Ctrl Pts',(1.08777266255173,58.2116592038884,11.3777316224606));
#66302=CARTESIAN_POINT('Ctrl Pts',(2.00844471935908,58.3805310808016,12.4732448226105));
#66303=CARTESIAN_POINT('Ctrl Pts',(2.04589361782153,58.505161388625,13.5272553458206));
#66304=CARTESIAN_POINT('Ctrl Pts',(1.80162355774204,58.5874976800848,14.1431016224888));
#66305=CARTESIAN_POINT('Ctrl Pts',(1.57462652991566,58.6421964556724,14.5194599162909));
#66306=CARTESIAN_POINT('Ctrl Pts',(0.921284375875408,58.7555706101121,15.1716196737154));
#66307=CARTESIAN_POINT('Ctrl Pts',(-0.559323486541137,58.9258795698348,
15.4251265913212));
#66308=CARTESIAN_POINT('Ctrl Pts',(-1.98161722775831,59.1381198537348,14.1989325529882));
#66309=CARTESIAN_POINT('Ctrl Pts',(-1.92830754970155,59.3482717047087,12.3391872739581));
#66310=CARTESIAN_POINT('Ctrl Pts',(-0.474337152083153,59.5571963003103,
11.2027925785685));
#66311=CARTESIAN_POINT('Ctrl Pts',(1.32802077288509,59.7657739417265,11.6099790789725));
#66312=CARTESIAN_POINT('Ctrl Pts',(2.15772795610831,59.9748521182681,13.2614463248672));
#66313=CARTESIAN_POINT('Ctrl Pts',(1.40689670059518,60.1852962987321,14.9632314121181));
#66314=CARTESIAN_POINT('Ctrl Pts',(-0.407278733503049,60.3979740857096,
15.468739419225));
#66315=CARTESIAN_POINT('Ctrl Pts',(-1.70421135728494,60.5777470442394,14.5561329060626));
#66316=CARTESIAN_POINT('Ctrl Pts',(-2.04852498716468,60.7234716717298,13.408246526714));
#66317=CARTESIAN_POINT('Ctrl Pts',(-1.90436246834392,60.8460742215266,12.412420236595));
#66318=CARTESIAN_POINT('Ctrl Pts',(-1.42619810349544,60.9391411294724,11.7972487198612));
#66319=CARTESIAN_POINT('Ctrl Pts',(-1.00545093965125,61.0017050399128,11.5236867403454));
#66320=CARTESIAN_POINT('Ctrl Pts',(-0.653343800533873,61.0518521649572,
11.329343969651));
#66321=CARTESIAN_POINT('Ctrl Pts',(0.099998629121662,61.146503828448,11.1375368016581));
#66322=CARTESIAN_POINT('Ctrl Pts',(1.28912570182539,61.2936681364074,11.4604593570168));
#66323=CARTESIAN_POINT('Ctrl Pts',(2.19138559292769,61.4630318554624,12.5750982685794));
#66324=CARTESIAN_POINT('Ctrl Pts',(2.21879758576631,61.642449074206,14.0945176467641));
#66325=CARTESIAN_POINT('Ctrl Pts',(1.28772112801874,61.8256164694219,15.3348576439151));
#66326=CARTESIAN_POINT('Ctrl Pts',(-0.241443755623096,62.0127224705213,
15.7495969807645));
#66327=CARTESIAN_POINT('Ctrl Pts',(-1.73425307349269,62.2039267452204,15.1230719503154));
#66328=CARTESIAN_POINT('Ctrl Pts',(-2.54423592511502,62.3993640676977,13.6800226513326));
#66329=CARTESIAN_POINT('Ctrl Pts',(-2.28296970228244,62.6043950170162,11.9633098075878));
#66330=CARTESIAN_POINT('Ctrl Pts',(-1.38591243097158,62.7460124560898,11.1534718409885));
#66331=CARTESIAN_POINT('Ctrl Pts',(-0.829611386823436,62.8203761132634,
10.9386484300407));
#66332=CARTESIAN_POINT('Ctrl Pts',(0.38002601593105,51.894132922063,10.3452258592843));
#66333=CARTESIAN_POINT('Ctrl Pts',(1.04561055735909,51.9779870683912,10.4375209418931));
#66334=CARTESIAN_POINT('Ctrl Pts',(2.28959663373971,52.1432373900973,11.0839834026683));
#66335=CARTESIAN_POINT('Ctrl Pts',(3.1389126194169,52.3882134746617,12.9768465067893));
#66336=CARTESIAN_POINT('Ctrl Pts',(2.65062121395832,52.6292008894566,14.9578142951044));
#66337=CARTESIAN_POINT('Ctrl Pts',(1.06206603561794,52.8678552946214,16.2062727884347));
#66338=CARTESIAN_POINT('Ctrl Pts',(-0.937078411997912,53.1039875153361,
16.2116698916617));
#66339=CARTESIAN_POINT('Ctrl Pts',(-2.49800482308679,53.3374328297761,14.9994365287431));
#66340=CARTESIAN_POINT('Ctrl Pts',(-2.97559942988575,53.568037876535,13.105315068351));
#66341=CARTESIAN_POINT('Ctrl Pts',(-2.22576011261648,53.7872381782223,11.4087407820391));
#66342=CARTESIAN_POINT('Ctrl Pts',(-0.719211151907584,53.9953106016391,
10.5290335875151));
#66343=CARTESIAN_POINT('Ctrl Pts',(0.924657178006765,54.1925572595333,10.6306634839183));
#66344=CARTESIAN_POINT('Ctrl Pts',(2.44751583241136,54.4197001537148,11.7773150632063));
#66345=CARTESIAN_POINT('Ctrl Pts',(2.85222472287848,54.6749694417843,13.9918788858764));
#66346=CARTESIAN_POINT('Ctrl Pts',(1.24466783780811,54.956241155142,15.8932578850828));
#66347=CARTESIAN_POINT('Ctrl Pts',(-1.18899616424661,55.2316068648696,15.8504376842965));
#66348=CARTESIAN_POINT('Ctrl Pts',(-2.20587709721319,55.4169082924069,14.5699720254287));
#66349=CARTESIAN_POINT('Ctrl Pts',(-2.36822651153772,55.516847918831,13.7855025636774));
#66350=CARTESIAN_POINT('Ctrl Pts',(-2.39493674542547,55.539027045757,13.6097011178693));
#66351=CARTESIAN_POINT('Ctrl Pts',(-2.40975768379484,55.5666954993779,13.3882119714191));
#66352=CARTESIAN_POINT('Ctrl Pts',(-2.39838198229458,55.5998097611757,13.122516874998));
#66353=CARTESIAN_POINT('Ctrl Pts',(-2.3167775359425,55.6658631764742,12.5993804450098));
#66354=CARTESIAN_POINT('Ctrl Pts',(-1.83523332892062,55.8080304714487,11.530273157802));
#66355=CARTESIAN_POINT('Ctrl Pts',(-0.142248222083035,56.0233232803886,
10.6689858858619));
#66356=CARTESIAN_POINT('Ctrl Pts',(1.73948903769928,56.2553659901608,11.4838300332593));
#66357=CARTESIAN_POINT('Ctrl Pts',(2.39836936022397,56.4627627807999,13.1161972427045));
#66358=CARTESIAN_POINT('Ctrl Pts',(1.9777870995906,56.64684408314,14.6138748628466));
#66359=CARTESIAN_POINT('Ctrl Pts',(0.736254230871711,56.8285256399016,15.5252124467261));
#66360=CARTESIAN_POINT('Ctrl Pts',(-0.782492003945809,57.008012802175,15.4791022171478));
#66361=CARTESIAN_POINT('Ctrl Pts',(-1.93927405337162,57.1855130743989,14.5192215493128));
#66362=CARTESIAN_POINT('Ctrl Pts',(-2.25669900564292,57.3612496887774,13.0649459223754));
#66363=CARTESIAN_POINT('Ctrl Pts',(-1.61818130107,57.5354648773718,11.7351894938078));
#66364=CARTESIAN_POINT('Ctrl Pts',(-0.305549112424641,57.7084045570741,
11.0837620750159));
#66365=CARTESIAN_POINT('Ctrl Pts',(1.11991210009554,57.8803206864588,11.3775497551447));
#66366=CARTESIAN_POINT('Ctrl Pts',(2.06072059219382,58.0514829670831,12.4810414041313));
#66367=CARTESIAN_POINT('Ctrl Pts',(2.10725865009378,58.1794875676566,13.5630161536499));
#66368=CARTESIAN_POINT('Ctrl Pts',(1.85801322786466,58.2647543577404,14.2021700051929));
#66369=CARTESIAN_POINT('Ctrl Pts',(1.62445737768668,58.3215872081488,14.5945059340594));
#66370=CARTESIAN_POINT('Ctrl Pts',(0.94710368745052,58.439968768518,15.2795932435486));
#66371=CARTESIAN_POINT('Ctrl Pts',(-0.614371771197201,58.6199556753514,
15.5629719319932));
#66372=CARTESIAN_POINT('Ctrl Pts',(-2.15600600757443,58.8480648658049,14.2620100689544));
#66373=CARTESIAN_POINT('Ctrl Pts',(-2.11995695792847,59.0775462281663,12.2311772197443));
#66374=CARTESIAN_POINT('Ctrl Pts',(-0.523423431696986,59.3090277093448,
10.9551827677584));
#66375=CARTESIAN_POINT('Ctrl Pts',(1.50367428801177,59.5431148830245,11.3898078095394));
#66376=CARTESIAN_POINT('Ctrl Pts',(2.46495145155469,59.780356498564,13.2530761359036));
#66377=CARTESIAN_POINT('Ctrl Pts',(1.62594816896165,60.0212828002207,15.2097164770404));
#66378=CARTESIAN_POINT('Ctrl Pts',(-0.458508601026925,60.2663874533731,
15.813091542949));
#66379=CARTESIAN_POINT('Ctrl Pts',(-1.96939148720944,60.4744806514749,14.7711547587735));
#66380=CARTESIAN_POINT('Ctrl Pts',(-2.3801743425067,60.6434428231889,13.4440484551771));
#66381=CARTESIAN_POINT('Ctrl Pts',(-2.22297758285063,60.7856732537224,12.2876999672974));
#66382=CARTESIAN_POINT('Ctrl Pts',(-1.67447145664554,60.8936360758271,11.5695545665826));
#66383=CARTESIAN_POINT('Ctrl Pts',(-1.18941724923096,60.9661799395199,11.2483368299688));
#66384=CARTESIAN_POINT('Ctrl Pts',(-0.783218346752186,61.024317361992,11.0196557639951));
#66385=CARTESIAN_POINT('Ctrl Pts',(0.0876819560510596,61.1339957656059,
10.7902562013244));
#66386=CARTESIAN_POINT('Ctrl Pts',(1.46612917475685,61.3042633158441,11.1529481660207));
#66387=CARTESIAN_POINT('Ctrl Pts',(2.51651255753311,61.4996775639743,12.4310524210908));
#66388=CARTESIAN_POINT('Ctrl Pts',(2.56024916794277,61.7058918118971,14.1768777154794));
#66389=CARTESIAN_POINT('Ctrl Pts',(1.50471339889892,61.915422008706,15.6025313116502));
#66390=CARTESIAN_POINT('Ctrl Pts',(-0.23171713912405,62.128277794586,16.085063349869));
#66391=CARTESIAN_POINT('Ctrl Pts',(-1.92331879578128,62.3444465989242,15.3866180607013));
#66392=CARTESIAN_POINT('Ctrl Pts',(-2.84145203577105,62.5638933635446,13.7713782437873));
#66393=CARTESIAN_POINT('Ctrl Pts',(-2.55987100019197,62.7924197557714,11.8567130657939));
#66394=CARTESIAN_POINT('Ctrl Pts',(-1.5721280846574,62.9489892365689,10.9569442928862));
#66395=CARTESIAN_POINT('Ctrl Pts',(-0.961374574518973,63.0308340001136,
10.7170354018271));
#66396=CARTESIAN_POINT('Ctrl Pts',(0.314205767653474,52.1224181378033,10.5783091018412));
#66397=CARTESIAN_POINT('Ctrl Pts',(0.927179049127616,52.1996272916182,10.6622910711999));
#66398=CARTESIAN_POINT('Ctrl Pts',(2.06834788312619,52.3512001258821,11.2548423470911));
#66399=CARTESIAN_POINT('Ctrl Pts',(2.84236351688607,52.574308794225,12.9784862284615));
#66400=CARTESIAN_POINT('Ctrl Pts',(2.40107658979739,52.7923310881545,14.770759324993));
#66401=CARTESIAN_POINT('Ctrl Pts',(0.973042283842452,53.0069132762071,15.8936254580078));
#66402=CARTESIAN_POINT('Ctrl Pts',(-0.814287071423194,53.2180317583515,
15.8988765311669));
#66403=CARTESIAN_POINT('Ctrl Pts',(-2.20301039986756,53.4256852075293,14.820935064035));
#66404=CARTESIAN_POINT('Ctrl Pts',(-2.62639876864594,53.6298961738894,13.1437537281026));
#66405=CARTESIAN_POINT('Ctrl Pts',(-1.96542446937171,53.8232727262112,11.6468656576391));
#66406=CARTESIAN_POINT('Ctrl Pts',(-0.640651902733371,54.0063010743747,
10.872415681035));
#66407=CARTESIAN_POINT('Ctrl Pts',(0.802355555485791,54.1794415884684,10.9607825902522));
#66408=CARTESIAN_POINT('Ctrl Pts',(2.13770669987019,54.3785331099324,11.9649894230023));
#66409=CARTESIAN_POINT('Ctrl Pts',(2.49352595280071,54.602061655646,13.9038520631604));
#66410=CARTESIAN_POINT('Ctrl Pts',(1.08711694486039,54.8484932338877,15.5711131137492));
#66411=CARTESIAN_POINT('Ctrl Pts',(-1.04972984695112,55.0902858291273,15.536971400617));
#66412=CARTESIAN_POINT('Ctrl Pts',(-1.94850823240697,55.2536591825681,14.4100053421157));
#66413=CARTESIAN_POINT('Ctrl Pts',(-2.09286910382753,55.3420495878578,13.7163485223411));
#66414=CARTESIAN_POINT('Ctrl Pts',(-2.11667247626317,55.3616728088132,13.5608386857155));
#66415=CARTESIAN_POINT('Ctrl Pts',(-2.13001505400921,55.3861667335208,13.36478013255));
#66416=CARTESIAN_POINT('Ctrl Pts',(-2.12021537180453,55.4155056965844,13.129375371143));
#66417=CARTESIAN_POINT('Ctrl Pts',(-2.04838615078405,55.4740779361559,12.6654018948664));
#66418=CARTESIAN_POINT('Ctrl Pts',(-1.62222531659694,55.6004116297843,11.7149258043184));
#66419=CARTESIAN_POINT('Ctrl Pts',(-0.111426751855292,55.7928584359703,
10.9400570321169));
#66420=CARTESIAN_POINT('Ctrl Pts',(1.58933073112833,56.0022839889897,11.6686749818947));
#66421=CARTESIAN_POINT('Ctrl Pts',(2.19531629339118,56.1913387401275,13.1545262429752));
#66422=CARTESIAN_POINT('Ctrl Pts',(1.81344774899216,56.3607322472041,14.5340021806857));
#66423=CARTESIAN_POINT('Ctrl Pts',(0.663003508882794,56.5296440024604,15.3860526296035));
#66424=CARTESIAN_POINT('Ctrl Pts',(-0.76469740206766,56.6983684641913,15.3493564952476));
#66425=CARTESIAN_POINT('Ctrl Pts',(-1.86929745488312,56.8671836325004,14.4421479682705));
#66426=CARTESIAN_POINT('Ctrl Pts',(-2.1825043674892,57.0363710530016,13.0439602679641));
#66427=CARTESIAN_POINT('Ctrl Pts',(-1.56767935023913,57.2062181629884,11.7441354534662));
#66428=CARTESIAN_POINT('Ctrl Pts',(-0.275692863730203,57.3769996385065,
11.0928519158453));
#66429=CARTESIAN_POINT('Ctrl Pts',(1.15205153763939,57.5489821690291,11.3773678878289));
#66430=CARTESIAN_POINT('Ctrl Pts',(2.11299646502858,57.7224348533646,12.4888379856522));
#66431=CARTESIAN_POINT('Ctrl Pts',(2.16862368236604,57.8538137466882,13.5987769614792));
#66432=CARTESIAN_POINT('Ctrl Pts',(1.91440289798728,57.9420110353959,14.2612383878969));
#66433=CARTESIAN_POINT('Ctrl Pts',(1.67428822545771,58.0009779606252,14.6695519518278));
#66434=CARTESIAN_POINT('Ctrl Pts',(0.972922999025649,58.1243669269237,15.3875668133818));
#66435=CARTESIAN_POINT('Ctrl Pts',(-0.669420055853256,58.314031780868,15.7008172726651));
#66436=CARTESIAN_POINT('Ctrl Pts',(-2.33039478739054,58.5580098778749,14.3250875849206));
#66437=CARTESIAN_POINT('Ctrl Pts',(-2.31160636615539,58.8068207516239,12.1231671655305));
#66438=CARTESIAN_POINT('Ctrl Pts',(-0.572509711310807,59.0608591183793,
10.7075729569483));
#66439=CARTESIAN_POINT('Ctrl Pts',(1.67932780313847,59.3204558243225,11.1696365401063));
#66440=CARTESIAN_POINT('Ctrl Pts',(2.77217494700108,59.5858608788598,13.2447059469399));
#66441=CARTESIAN_POINT('Ctrl Pts',(1.84499963732813,59.8572693017093,15.4562015419629));
#66442=CARTESIAN_POINT('Ctrl Pts',(-0.509738468550788,60.1348008210364,
16.1574436666731));
#66443=CARTESIAN_POINT('Ctrl Pts',(-2.23457161713394,60.3712142587102,14.9861766114844));
#66444=CARTESIAN_POINT('Ctrl Pts',(-2.71182369784871,60.563413974648,13.4798503836404));
#66445=CARTESIAN_POINT('Ctrl Pts',(-2.54159269735736,60.7252722859181,12.1629796979999));
#66446=CARTESIAN_POINT('Ctrl Pts',(-1.92274480979564,60.8481310221818,11.3418604133041));
#66447=CARTESIAN_POINT('Ctrl Pts',(-1.37338355881068,60.930654839127,10.9729869195923));
#66448=CARTESIAN_POINT('Ctrl Pts',(-0.913092892970496,60.9967825590269,
10.7099675583393));
#66449=CARTESIAN_POINT('Ctrl Pts',(0.0753652829804603,61.1214877027638,
10.4429756009906));
#66450=CARTESIAN_POINT('Ctrl Pts',(1.6431326476883,61.3148584952808,10.8454369750245));
#66451=CARTESIAN_POINT('Ctrl Pts',(2.84163952213855,61.5363232724862,12.2870065736023));
#66452=CARTESIAN_POINT('Ctrl Pts',(2.90170075011925,61.7693345495881,14.2592377841948));
#66453=CARTESIAN_POINT('Ctrl Pts',(1.72170566977911,62.0052275479901,15.8702049793853));
#66454=CARTESIAN_POINT('Ctrl Pts',(-0.221990522625003,62.2438331186507,
16.4205297189735));
#66455=CARTESIAN_POINT('Ctrl Pts',(-2.11238451806987,62.484966452628,15.6501641710872));
#66456=CARTESIAN_POINT('Ctrl Pts',(-3.13866814642708,62.7284226593914,13.8627338362421));
#66457=CARTESIAN_POINT('Ctrl Pts',(-2.83677229810149,62.9804444945266,11.7501163239999));
#66458=CARTESIAN_POINT('Ctrl Pts',(-1.75834373834323,63.1519660170479,10.7604167447839));
#66459=CARTESIAN_POINT('Ctrl Pts',(-1.09313776221452,63.2412918869638,10.4954223736136));
#66460=CARTESIAN_POINT('Ctrl Pts',(0.248385519375899,52.3507033535437,10.8113923443982));
#66461=CARTESIAN_POINT('Ctrl Pts',(0.80874754089614,52.4212675148452,10.8870612005067));
#66462=CARTESIAN_POINT('Ctrl Pts',(1.84709913251267,52.5591628616668,11.4257012915141));
#66463=CARTESIAN_POINT('Ctrl Pts',(2.54581441435525,52.7604041137883,12.9801259501337));
#66464=CARTESIAN_POINT('Ctrl Pts',(2.15153196563645,52.9554612868524,14.5837043548816));
#66465=CARTESIAN_POINT('Ctrl Pts',(0.884018532066958,53.1459712577928,15.5809781275808));
#66466=CARTESIAN_POINT('Ctrl Pts',(-0.69149573084848,53.3320760013669,15.5860831706721));
#66467=CARTESIAN_POINT('Ctrl Pts',(-1.90801597664832,53.5139375852825,14.642433599327));
#66468=CARTESIAN_POINT('Ctrl Pts',(-2.27719810740612,53.6917544712438,13.1821923878542));
#66469=CARTESIAN_POINT('Ctrl Pts',(-1.70508882612695,53.8593072742,11.8849905332391));
#66470=CARTESIAN_POINT('Ctrl Pts',(-0.562092653559157,54.0172915471103,
11.215797774555));
#66471=CARTESIAN_POINT('Ctrl Pts',(0.680053932964807,54.1663259174035,11.290901696586));
#66472=CARTESIAN_POINT('Ctrl Pts',(1.82789756732901,54.3373660661498,12.1526637827982));
#66473=CARTESIAN_POINT('Ctrl Pts',(2.13482718272291,54.5291538695076,13.8158252404444));
#66474=CARTESIAN_POINT('Ctrl Pts',(0.929566051912647,54.7407453126335,15.2489683424158));
#66475=CARTESIAN_POINT('Ctrl Pts',(-0.910463529655639,54.948964793385,15.2235051169375));
#66476=CARTESIAN_POINT('Ctrl Pts',(-1.69113936760076,55.0904100727293,14.2500386588026));
#66477=CARTESIAN_POINT('Ctrl Pts',(-1.81751169611734,55.1672512568847,13.6471944810048));
#66478=CARTESIAN_POINT('Ctrl Pts',(-1.83840820710088,55.1843185718696,13.5119762535616));
#66479=CARTESIAN_POINT('Ctrl Pts',(-1.85027242422358,55.2056379676637,13.3413482936807));
#66480=CARTESIAN_POINT('Ctrl Pts',(-1.84204876131448,55.231201631993,13.1362338672878));
#66481=CARTESIAN_POINT('Ctrl Pts',(-1.77999476562559,55.2822926958375,12.7314233447229));
#66482=CARTESIAN_POINT('Ctrl Pts',(-1.40921730427326,55.3927927881198,11.8995784508347));
#66483=CARTESIAN_POINT('Ctrl Pts',(-0.0806052816275569,55.5623935915521,
11.2111281783718));
#66484=CARTESIAN_POINT('Ctrl Pts',(1.43917242455737,55.7492019878187,11.8535199305299));
#66485=CARTESIAN_POINT('Ctrl Pts',(1.99226322655837,55.9199146994551,13.1928552432458));
#66486=CARTESIAN_POINT('Ctrl Pts',(1.64910839839372,56.0746204112681,14.4541294985246));
#66487=CARTESIAN_POINT('Ctrl Pts',(0.589752786893861,56.2307623650192,15.2468928124809));
#66488=CARTESIAN_POINT('Ctrl Pts',(-0.746902800189516,56.3887241262077,
15.2196107733473));
#66489=CARTESIAN_POINT('Ctrl Pts',(-1.79932085639463,56.548854190602,14.3650743872282));
#66490=CARTESIAN_POINT('Ctrl Pts',(-2.10830972933549,56.7114924172259,13.0229746135528));
#66491=CARTESIAN_POINT('Ctrl Pts',(-1.51717739940825,56.876971448605,11.7530814131246));
#66492=CARTESIAN_POINT('Ctrl Pts',(-0.245836615035774,57.0455947199389,
11.1019417566746));
#66493=CARTESIAN_POINT('Ctrl Pts',(1.18419097518321,57.2176436515995,11.377186020513));
#66494=CARTESIAN_POINT('Ctrl Pts',(2.16527233786333,57.393386739646,12.4966345671731));
#66495=CARTESIAN_POINT('Ctrl Pts',(2.22998871463829,57.5281399257198,13.6345377693084));
#66496=CARTESIAN_POINT('Ctrl Pts',(1.97079256810989,57.6192677130515,14.3203067706008));
#66497=CARTESIAN_POINT('Ctrl Pts',(1.72411907322871,57.6803687131016,14.7445979695963));
#66498=CARTESIAN_POINT('Ctrl Pts',(0.998742310600759,57.8087650853294,15.495540383215));
#66499=CARTESIAN_POINT('Ctrl Pts',(-0.724468340509324,58.0081078863845,
15.8386626133371));
#66500=CARTESIAN_POINT('Ctrl Pts',(-2.50478356720666,58.2679548899448,14.3881651008867));
#66501=CARTESIAN_POINT('Ctrl Pts',(-2.50325577438232,58.5360952750815,12.0151571113168));
#66502=CARTESIAN_POINT('Ctrl Pts',(-0.621595990924646,58.8126905274138,
10.4599631461383));
#66503=CARTESIAN_POINT('Ctrl Pts',(1.85498131826514,59.0977967656205,10.9494652706732));
#66504=CARTESIAN_POINT('Ctrl Pts',(3.07939844244746,59.3913652591555,13.2363357579762));
#66505=CARTESIAN_POINT('Ctrl Pts',(2.0640511056946,59.6932558031979,15.7026866068853));
#66506=CARTESIAN_POINT('Ctrl Pts',(-0.56096833607467,60.0032141886998,16.5017957903972));
#66507=CARTESIAN_POINT('Ctrl Pts',(-2.49975174705845,60.2679478659456,15.2011984641953));
#66508=CARTESIAN_POINT('Ctrl Pts',(-3.04347305319073,60.4833851261072,13.5156523121035));
#66509=CARTESIAN_POINT('Ctrl Pts',(-2.86020781186409,60.6648713181137,12.0382594287024));
#66510=CARTESIAN_POINT('Ctrl Pts',(-2.17101816294575,60.8026259685364,11.1141662600256));
#66511=CARTESIAN_POINT('Ctrl Pts',(-1.55734986839041,60.8951297387342,10.6976370092157));
#66512=CARTESIAN_POINT('Ctrl Pts',(-1.04296743918883,60.9692477560618,10.4002793526834));
#66513=CARTESIAN_POINT('Ctrl Pts',(0.0630486099098471,61.1089796399216,
10.0956950006568));
#66514=CARTESIAN_POINT('Ctrl Pts',(1.82013612061974,61.3254536747173,10.5379257840283));
#66515=CARTESIAN_POINT('Ctrl Pts',(3.16676648674395,61.572968980998,12.1429607261137));
#66516=CARTESIAN_POINT('Ctrl Pts',(3.24315233229571,61.8327772872792,14.3415978529102));
#66517=CARTESIAN_POINT('Ctrl Pts',(1.93869794065929,62.0950330872743,16.1378786471204));
#66518=CARTESIAN_POINT('Ctrl Pts',(-0.212263906125961,62.3593884427155,
16.7559960880779));
#66519=CARTESIAN_POINT('Ctrl Pts',(-2.30145024035847,62.6254863063319,15.9137102814732));
#66520=CARTESIAN_POINT('Ctrl Pts',(-3.43588425708311,62.8929519552382,13.9540894286967));
#66521=CARTESIAN_POINT('Ctrl Pts',(-3.11367359601103,63.1684692332818,11.643519582206));
#66522=CARTESIAN_POINT('Ctrl Pts',(-1.94455939202906,63.3549427975269,10.5638891966816));
#66523=CARTESIAN_POINT('Ctrl Pts',(-1.22490094991005,63.4517497738138,10.2738093454001));
#66524=CARTESIAN_POINT('Ctrl Pts',(1.85670933670314,67.8162814825949,10.6678728949504));
#66525=CARTESIAN_POINT('Ctrl Pts',(2.43602197966479,67.9048067130758,11.0772117886178));
#66526=CARTESIAN_POINT('Ctrl Pts',(3.31138477419987,68.0818237056135,12.2930394731503));
#66527=CARTESIAN_POINT('Ctrl Pts',(3.22470059147693,68.3468414640187,14.5358665053979));
#66528=CARTESIAN_POINT('Ctrl Pts',(1.78035101801571,68.6110053286756,16.2437005675216));
#66529=CARTESIAN_POINT('Ctrl Pts',(-0.398931224427797,68.87395706305,16.6986682402629));
#66530=CARTESIAN_POINT('Ctrl Pts',(-2.3843464145878,69.1353372445261,15.7211359742319));
#66531=CARTESIAN_POINT('Ctrl Pts',(-3.34029854038271,69.3948123372156,13.7432675526659));
#66532=CARTESIAN_POINT('Ctrl Pts',(-2.87920489104697,69.652058213363,11.6138171811909));
#66533=CARTESIAN_POINT('Ctrl Pts',(-1.28405859028018,69.8973232110643,10.2856759717977));
#66534=CARTESIAN_POINT('Ctrl Pts',(0.667327379030212,70.1306721384216,10.1534794027043));
#66535=CARTESIAN_POINT('Ctrl Pts',(2.27325538581328,70.3522534623988,11.0739567043829));
#66536=CARTESIAN_POINT('Ctrl Pts',(3.23327615711246,70.6077079139465,12.99126474038));
#66537=CARTESIAN_POINT('Ctrl Pts',(2.53340867575295,70.8950134973084,15.4265265382553));
#66538=CARTESIAN_POINT('Ctrl Pts',(-0.0387874535395751,71.2114494314392,
16.537589845118));
#66539=CARTESIAN_POINT('Ctrl Pts',(-2.46488681075965,71.5207018511086,15.2793708579856));
#66540=CARTESIAN_POINT('Ctrl Pts',(-3.0194423980344,71.822422717759,12.6713480466428));
#66541=CARTESIAN_POINT('Ctrl Pts',(-1.38798471805984,72.1163679385386,10.6399663599959));
#66542=CARTESIAN_POINT('Ctrl Pts',(0.502791661670317,72.3308848888959,10.6231415412111));
#66543=CARTESIAN_POINT('Ctrl Pts',(1.47389601290199,72.4714016735426,11.2093038867376));
#66544=CARTESIAN_POINT('Ctrl Pts',(1.88316787655009,72.5411621865908,11.5944131847211));
#66545=CARTESIAN_POINT('Ctrl Pts',(2.19405691725845,72.6104243783894,12.0586074280405));
#66546=CARTESIAN_POINT('Ctrl Pts',(2.53070804850737,72.7250336026109,12.9195308779709));
#66547=CARTESIAN_POINT('Ctrl Pts',(2.43170974236522,72.883170223474,14.2545730359041));
#66548=CARTESIAN_POINT('Ctrl Pts',(1.29763738145591,73.0820761708995,15.5011320023063));
#66549=CARTESIAN_POINT('Ctrl Pts',(-0.326434740095091,73.2766468129717,
15.7785554159035));
#66550=CARTESIAN_POINT('Ctrl Pts',(-1.7457431520839,73.466995830727,15.0140013277268));
#66551=CARTESIAN_POINT('Ctrl Pts',(-2.37915175472792,73.6532626901171,13.5691967259924));
#66552=CARTESIAN_POINT('Ctrl Pts',(-1.99682535493553,73.8356096858057,12.0728221880452));
#66553=CARTESIAN_POINT('Ctrl Pts',(-0.799077803009128,74.01423239441,11.1483727982448));
#66554=CARTESIAN_POINT('Ctrl Pts',(0.684242025495391,74.1893507431627,11.157075878773));
#66555=CARTESIAN_POINT('Ctrl Pts',(1.82618961641565,74.3612004242115,12.0600879660341));
#66556=CARTESIAN_POINT('Ctrl Pts',(2.16567416243771,74.5300528254682,13.4492130447806));
#66557=CARTESIAN_POINT('Ctrl Pts',(1.58618759125941,74.696183100623,14.73214214359));
#66558=CARTESIAN_POINT('Ctrl Pts',(0.357063385623933,74.8598981792545,15.3762725490012));
#66559=CARTESIAN_POINT('Ctrl Pts',(-0.986547124399861,75.0215158702681,
15.1328704254147));
#66560=CARTESIAN_POINT('Ctrl Pts',(-1.99665026629802,75.1991266012217,14.008047190742));
#66561=CARTESIAN_POINT('Ctrl Pts',(-1.93314910690999,75.3573224550387,12.6189681599128));
#66562=CARTESIAN_POINT('Ctrl Pts',(-1.08666427933318,75.5145655987107,11.63650588873));
#66563=CARTESIAN_POINT('Ctrl Pts',(0.0310153359284624,75.6538155156279,
11.2735856755919));
#66564=CARTESIAN_POINT('Ctrl Pts',(1.2767819779433,75.8101327231011,11.7298773561435));
#66565=CARTESIAN_POINT('Ctrl Pts',(1.97616391758332,75.9664765024184,12.8535243090815));
#66566=CARTESIAN_POINT('Ctrl Pts',(1.83728075366513,76.1232123129657,14.1740596869939));
#66567=CARTESIAN_POINT('Ctrl Pts',(0.911576562100944,76.2807155795881,15.1345764081083));
#66568=CARTESIAN_POINT('Ctrl Pts',(-0.419740331737157,76.4393345343032,
15.3238994606443));
#66569=CARTESIAN_POINT('Ctrl Pts',(-1.59340498562502,76.5994257148169,14.6502009434244));
#66570=CARTESIAN_POINT('Ctrl Pts',(-2.17724646289294,76.7793301999848,13.23842029717));
#66571=CARTESIAN_POINT('Ctrl Pts',(-1.51301420837496,76.9802742295743,11.5954783371621));
#66572=CARTESIAN_POINT('Ctrl Pts',(0.372263544000895,77.2040586660941,10.993031354742));
#66573=CARTESIAN_POINT('Ctrl Pts',(1.71371613042439,77.3853767161158,11.8693209754832));
#66574=CARTESIAN_POINT('Ctrl Pts',(2.07812199344447,77.5067673998192,12.787549358819));
#66575=CARTESIAN_POINT('Ctrl Pts',(2.14159723430654,77.5654598619418,13.254921766966));
#66576=CARTESIAN_POINT('Ctrl Pts',(2.12669180036108,77.6244463050604,13.7293760541241));
#66577=CARTESIAN_POINT('Ctrl Pts',(1.96007099854122,77.698728531597,14.3090748515968));
#66578=CARTESIAN_POINT('Ctrl Pts',(1.40225955808634,77.8188007585235,15.1102220024261));
#66579=CARTESIAN_POINT('Ctrl Pts',(0.250892231981857,77.9712350172198,15.6915466425755));
#66580=CARTESIAN_POINT('Ctrl Pts',(-1.30233550994055,78.1581011855988,15.3843152222005));
#66581=CARTESIAN_POINT('Ctrl Pts',(-2.36017044749241,78.3490726374534,14.1617211117542));
#66582=CARTESIAN_POINT('Ctrl Pts',(-2.44529326530541,78.5442859556217,12.5110277849349));
#66583=CARTESIAN_POINT('Ctrl Pts',(-1.47548070536812,78.7438463495833,11.1269582907925));
#66584=CARTESIAN_POINT('Ctrl Pts',(-0.375471582425882,78.8798352338376,
10.7894481836038));
#66585=CARTESIAN_POINT('Ctrl Pts',(0.175037137306408,78.9485750961381,10.8098385013603));
#66586=CARTESIAN_POINT('Ctrl Pts',(1.6908637574071,68.0447466494469,10.8458773711862));
#66587=CARTESIAN_POINT('Ctrl Pts',(2.22798671957131,68.1267463690719,11.2242837835917));
#66588=CARTESIAN_POINT('Ctrl Pts',(3.03658819127134,68.2901931069568,12.3466170372939));
#66589=CARTESIAN_POINT('Ctrl Pts',(2.95754503485996,68.5334493293176,14.4052783886444));
#66590=CARTESIAN_POINT('Ctrl Pts',(1.63946032851273,68.7745858162928,15.9644933705822));
#66591=CARTESIAN_POINT('Ctrl Pts',(-0.339666919821582,69.01339855444,16.3780848913055));
#66592=CARTESIAN_POINT('Ctrl Pts',(-2.13469030133651,69.2496953306187,15.494721729799));
#66593=CARTESIAN_POINT('Ctrl Pts',(-2.99571041460629,69.4833086246055,13.714185366764));
#66594=CARTESIAN_POINT('Ctrl Pts',(-2.58248382224423,69.7140871144928,11.80376017475));
#66595=CARTESIAN_POINT('Ctrl Pts',(-1.15610395069001,69.9334567944685,10.6154883664123));
#66596=CARTESIAN_POINT('Ctrl Pts',(0.585165556796055,70.1416931193554,10.496838092407));
#66597=CARTESIAN_POINT('Ctrl Pts',(2.01625356645349,70.3390990857319,11.3162524642622));
#66598=CARTESIAN_POINT('Ctrl Pts',(2.87134270658542,70.5664254649136,13.0219942174795));
#66599=CARTESIAN_POINT('Ctrl Pts',(2.25028856230078,70.821902835782,15.1877697105361));
#66600=CARTESIAN_POINT('Ctrl Pts',(-0.0368840815874874,71.1034026808018,
16.178102643529));
#66601=CARTESIAN_POINT('Ctrl Pts',(-2.20012627605475,71.3789882022379,15.0596346097378));
#66602=CARTESIAN_POINT('Ctrl Pts',(-2.6997469456442,71.6487263265457,12.7291745761339));
#66603=CARTESIAN_POINT('Ctrl Pts',(-1.23851386451774,71.9127606817029,10.9014114004134));
#66604=CARTESIAN_POINT('Ctrl Pts',(0.47036207186609,72.1066567862411,10.8817739166415));
#66605=CARTESIAN_POINT('Ctrl Pts',(1.35329158177082,72.2342881946177,11.4129403636492));
#66606=CARTESIAN_POINT('Ctrl Pts',(1.7262508293604,72.2977828683341,11.7629106708839));
#66607=CARTESIAN_POINT('Ctrl Pts',(2.01047124602242,72.3609591527076,12.1858815356422));
#66608=CARTESIAN_POINT('Ctrl Pts',(2.31945641328146,72.4657375867817,12.9723889777793));
#66609=CARTESIAN_POINT('Ctrl Pts',(2.23199454505765,72.6109978916266,14.1988498760847));
#66610=CARTESIAN_POINT('Ctrl Pts',(1.18579312871404,72.7951763476163,15.3563986803355));
#66611=CARTESIAN_POINT('Ctrl Pts',(-0.330275915687068,72.9769418543322,
15.621117764498));
#66612=CARTESIAN_POINT('Ctrl Pts',(-1.67189963570851,73.1564980205229,14.9055500254477));
#66613=CARTESIAN_POINT('Ctrl Pts',(-2.2819418968461,73.334056048206,13.5312995370621));
#66614=CARTESIAN_POINT('Ctrl Pts',(-1.92079877016408,73.509835767522,12.087200469746));
#66615=CARTESIAN_POINT('Ctrl Pts',(-0.757702727053409,73.6840781414891,
11.1790774296483));
#66616=CARTESIAN_POINT('Ctrl Pts',(0.706999028706615,73.8570324079774,11.1787549573379));
#66617=CARTESIAN_POINT('Ctrl Pts',(1.85507178555875,74.0289485500747,12.0743780146905));
#66618=CARTESIAN_POINT('Ctrl Pts',(2.20897506698,74.2000975019401,13.4795202611282));
#66619=CARTESIAN_POINT('Ctrl Pts',(1.6239403103936,74.3707393203612,14.8014365791305));
#66620=CARTESIAN_POINT('Ctrl Pts',(0.350151449131357,74.5411503549865,15.4820174971789));
#66621=CARTESIAN_POINT('Ctrl Pts',(-1.06847454630527,74.7116031039766,15.2371502021208));
#66622=CARTESIAN_POINT('Ctrl Pts',(-2.15809908045976,74.901341833707,14.0458318361661));
#66623=CARTESIAN_POINT('Ctrl Pts',(-2.10481117645329,75.0727931302178,12.5402712220382));
#66624=CARTESIAN_POINT('Ctrl Pts',(-1.18620856045404,75.2451808363801,11.4552688564583));
#66625=CARTESIAN_POINT('Ctrl Pts',(0.046045271720834,75.3992393285853,11.0423615123174));
#66626=CARTESIAN_POINT('Ctrl Pts',(1.44263668058336,75.573922910794,11.5384046732556));
#66627=CARTESIAN_POINT('Ctrl Pts',(2.24340518791338,75.750216614577,12.7973762745375));
#66628=CARTESIAN_POINT('Ctrl Pts',(2.10025705293841,75.9283527132405,14.2992105770565));
#66629=CARTESIAN_POINT('Ctrl Pts',(1.05214770800895,76.1085583193164,15.4081463814273));
#66630=CARTESIAN_POINT('Ctrl Pts',(-0.476886486902698,76.2910335636422,
15.6405602731496));
#66631=CARTESIAN_POINT('Ctrl Pts',(-1.8395781310858,76.4759732412606,14.875277590802));
#66632=CARTESIAN_POINT('Ctrl Pts',(-2.5309286729142,76.684398089858,13.2463448599704));
#66633=CARTESIAN_POINT('Ctrl Pts',(-1.77709762854491,76.9176501442953,11.3328365937584));
#66634=CARTESIAN_POINT('Ctrl Pts',(0.405025589060511,77.1774085192071,10.615426790541));
#66635=CARTESIAN_POINT('Ctrl Pts',(1.96644435451936,77.3874472951319,11.6184892768977));
#66636=CARTESIAN_POINT('Ctrl Pts',(2.3956515391194,77.52768729193,12.6756599141739));
#66637=CARTESIAN_POINT('Ctrl Pts',(2.47317674299433,77.5954091950267,13.2142138706979));
#66638=CARTESIAN_POINT('Ctrl Pts',(2.46030531838649,77.6634044766836,13.7611362800532));
#66639=CARTESIAN_POINT('Ctrl Pts',(2.27368042992308,77.7489112471484,14.4297292960393));
#66640=CARTESIAN_POINT('Ctrl Pts',(1.64001466463188,77.8868236335093,15.354563799779));
#66641=CARTESIAN_POINT('Ctrl Pts',(0.326891597429018,78.0612879022827,16.0285818285653));
#66642=CARTESIAN_POINT('Ctrl Pts',(-1.44289062624411,78.2739747921973,15.6899474839444));
#66643=CARTESIAN_POINT('Ctrl Pts',(-2.6472907269544,78.4899797904215,14.3142674428346));
#66644=CARTESIAN_POINT('Ctrl Pts',(-2.75296903649539,78.7092691128502,12.4607241288402));
#66645=CARTESIAN_POINT('Ctrl Pts',(-1.67950205787869,78.9317853940746,10.9121973695958));
#66646=CARTESIAN_POINT('Ctrl Pts',(-0.464434207018058,79.0822315596954,
10.5331333222611));
#66647=CARTESIAN_POINT('Ctrl Pts',(0.142094012249548,79.1579621925517,10.5520430852575));
#66648=CARTESIAN_POINT('Ctrl Pts',(1.52501817811105,68.2732118162988,11.0238818474219));
#66649=CARTESIAN_POINT('Ctrl Pts',(2.01995145947785,68.348686025068,11.3713557785656));
#66650=CARTESIAN_POINT('Ctrl Pts',(2.76179160834279,68.4985625083001,12.4001946014373));
#66651=CARTESIAN_POINT('Ctrl Pts',(2.69038947824299,68.7200571946162,14.2746902718909));
#66652=CARTESIAN_POINT('Ctrl Pts',(1.49856963900974,68.9381663039099,15.6852861736429));
#66653=CARTESIAN_POINT('Ctrl Pts',(-0.280402615215369,69.1528400458299,
16.0575015423482));
#66654=CARTESIAN_POINT('Ctrl Pts',(-1.88503418808523,69.3640534167114,15.2683074853659));
#66655=CARTESIAN_POINT('Ctrl Pts',(-2.6511222888299,69.5718049119957,13.6851031808621));
#66656=CARTESIAN_POINT('Ctrl Pts',(-2.28576275344152,69.7761160156225,11.9937031683093));
#66657=CARTESIAN_POINT('Ctrl Pts',(-1.02814931109985,69.969590377873,10.9453007610268));
#66658=CARTESIAN_POINT('Ctrl Pts',(0.50300373456189,70.152714100289,10.8401967821098));
#66659=CARTESIAN_POINT('Ctrl Pts',(1.7592517470937,70.3259447090649,11.5585482241415));
#66660=CARTESIAN_POINT('Ctrl Pts',(2.50940925605836,70.5251430158805,13.0527236945793));
#66661=CARTESIAN_POINT('Ctrl Pts',(1.9671684488486,70.7487921742557,14.9490128828172));
#66662=CARTESIAN_POINT('Ctrl Pts',(-0.0349807096354077,70.9953559301642,
15.8186154419401));
#66663=CARTESIAN_POINT('Ctrl Pts',(-1.93536574134987,71.237274553367,14.8398983614901));
#66664=CARTESIAN_POINT('Ctrl Pts',(-2.38005149325401,71.4750299353324,12.7870011056248));
#66665=CARTESIAN_POINT('Ctrl Pts',(-1.08904301097566,71.7091534248672,11.1628564408311));
#66666=CARTESIAN_POINT('Ctrl Pts',(0.437932482061858,71.8824286835865,11.1404062920719));
#66667=CARTESIAN_POINT('Ctrl Pts',(1.23268715063964,71.9971747156927,11.616576840561));
#66668=CARTESIAN_POINT('Ctrl Pts',(1.56933378217072,72.0544035500773,11.9314081570468));
#66669=CARTESIAN_POINT('Ctrl Pts',(1.82688557478638,72.1114939270255,12.3131556432439));
#66670=CARTESIAN_POINT('Ctrl Pts',(2.10820477805556,72.2064415709525,13.0252470775877));
#66671=CARTESIAN_POINT('Ctrl Pts',(2.0322793477501,72.3388255597791,14.1431267162651));
#66672=CARTESIAN_POINT('Ctrl Pts',(1.07394887597216,72.5082765243333,15.2116653583646));
#66673=CARTESIAN_POINT('Ctrl Pts',(-0.33411709127905,72.6772368956925,15.4636801130925));
#66674=CARTESIAN_POINT('Ctrl Pts',(-1.59805611933312,72.8460002103187,14.7970987231688));
#66675=CARTESIAN_POINT('Ctrl Pts',(-2.1847320389643,73.014849406295,13.4934023481318));
#66676=CARTESIAN_POINT('Ctrl Pts',(-1.84477218539263,73.1840618492383,12.1015787514466));
#66677=CARTESIAN_POINT('Ctrl Pts',(-0.716327651097694,73.3539238885679,
11.2097820610519));
#66678=CARTESIAN_POINT('Ctrl Pts',(0.729756031917838,73.524714072792,11.200434035903));
#66679=CARTESIAN_POINT('Ctrl Pts',(1.88395395470186,73.696696675938,12.0886680633468));
#66680=CARTESIAN_POINT('Ctrl Pts',(2.2522759715223,73.8701421784118,13.5098274774756));
#66681=CARTESIAN_POINT('Ctrl Pts',(1.66169302952779,74.0452955400992,14.8707310146709));
#66682=CARTESIAN_POINT('Ctrl Pts',(0.343239512638783,74.2224025307185,15.5877624453568));
#66683=CARTESIAN_POINT('Ctrl Pts',(-1.1504019682107,74.4016903376851,15.341429978827));
#66684=CARTESIAN_POINT('Ctrl Pts',(-2.3195478946215,74.6035570661924,14.0836164815903));
#66685=CARTESIAN_POINT('Ctrl Pts',(-2.2764732459966,74.7882638053972,12.4615742841636));
#66686=CARTESIAN_POINT('Ctrl Pts',(-1.2857528415749,74.9757960740495,11.2740318241866));
#66687=CARTESIAN_POINT('Ctrl Pts',(0.0610752075132027,75.1446631415427,
10.811137349043));
#66688=CARTESIAN_POINT('Ctrl Pts',(1.60849138322342,75.3377130984868,11.3469319903676));
#66689=CARTESIAN_POINT('Ctrl Pts',(2.51064645824345,75.5339567267357,12.7412282399934));
#66690=CARTESIAN_POINT('Ctrl Pts',(2.3632333522117,75.7334931135155,14.4243614671191));
#66691=CARTESIAN_POINT('Ctrl Pts',(1.19271885391695,75.9364010590447,15.6817163547461));
#66692=CARTESIAN_POINT('Ctrl Pts',(-0.534032642068244,76.1427325929813,
15.957221085655));
#66693=CARTESIAN_POINT('Ctrl Pts',(-2.08575127654658,76.3525207677044,15.1003542381797));
#66694=CARTESIAN_POINT('Ctrl Pts',(-2.88461088293549,76.5894659797311,13.2542694227708));
#66695=CARTESIAN_POINT('Ctrl Pts',(-2.04118104871486,76.8550260590165,11.0701948503547));
#66696=CARTESIAN_POINT('Ctrl Pts',(0.437787634120127,77.1507583723203,10.23782222634));
#66697=CARTESIAN_POINT('Ctrl Pts',(2.21917257861433,77.389517874148,11.3676575783123));
#66698=CARTESIAN_POINT('Ctrl Pts',(2.7131810847943,77.5486071840408,12.5637704695288));
#66699=CARTESIAN_POINT('Ctrl Pts',(2.80475625168213,77.6253585281116,13.1735059744297));
#66700=CARTESIAN_POINT('Ctrl Pts',(2.79391883641191,77.7023626483069,13.7928965059823));
#66701=CARTESIAN_POINT('Ctrl Pts',(2.58728986130495,77.7990939626997,14.5503837404819));
#66702=CARTESIAN_POINT('Ctrl Pts',(1.87776977117742,77.9548465084949,15.5989055971319));
#66703=CARTESIAN_POINT('Ctrl Pts',(0.402890962876184,78.1513407873456,16.3656170145551));
#66704=CARTESIAN_POINT('Ctrl Pts',(-1.58344574254767,78.389848398796,15.9955797456884));
#66705=CARTESIAN_POINT('Ctrl Pts',(-2.9344110064164,78.6308869433896,14.4668137739148));
#66706=CARTESIAN_POINT('Ctrl Pts',(-3.06064480768539,78.8742522700789,12.4104204727457));
#66707=CARTESIAN_POINT('Ctrl Pts',(-1.88352341038926,79.1197244385656,10.6974364483992));
#66708=CARTESIAN_POINT('Ctrl Pts',(-0.553396831610237,79.2846278855533,
10.2768184609184));
#66709=CARTESIAN_POINT('Ctrl Pts',(0.109150887192687,79.3673492889653,10.2942476691546));
#66710=CARTESIAN_POINT('Ctrl Pts',(1.35917259881499,68.5016769831508,11.2018863236575));
#66711=CARTESIAN_POINT('Ctrl Pts',(1.81191619938438,68.5706256810641,11.5184277735395));
#66712=CARTESIAN_POINT('Ctrl Pts',(2.48699502541424,68.7069319096434,12.4537721655809));
#66713=CARTESIAN_POINT('Ctrl Pts',(2.42323392162601,68.906665059915,14.1441021551374));
#66714=CARTESIAN_POINT('Ctrl Pts',(1.35767894950677,69.1017467915271,15.4060789767035));
#66715=CARTESIAN_POINT('Ctrl Pts',(-0.221138310609155,69.2922815372198,
15.7369181933908));
#66716=CARTESIAN_POINT('Ctrl Pts',(-1.63537807483394,69.4784115028039,15.0418932409329));
#66717=CARTESIAN_POINT('Ctrl Pts',(-2.3065341630535,69.6603011993856,13.6560209949601));
#66718=CARTESIAN_POINT('Ctrl Pts',(-1.98904168463877,69.8381449167524,12.1836461618684));
#66719=CARTESIAN_POINT('Ctrl Pts',(-0.900194671509688,70.0057239612773,
11.2751131556414));
#66720=CARTESIAN_POINT('Ctrl Pts',(0.420841912327732,70.1637350812228,11.1835554718125));
#66721=CARTESIAN_POINT('Ctrl Pts',(1.5022499277339,70.312790332398,11.8008439840208));
#66722=CARTESIAN_POINT('Ctrl Pts',(2.14747580553131,70.4838605668475,13.0834531716788));
#66723=CARTESIAN_POINT('Ctrl Pts',(1.68404833539643,70.6756815127292,14.7102560550982));
#66724=CARTESIAN_POINT('Ctrl Pts',(-0.0330773376833198,70.8873091795266,
15.4591282403512));
#66725=CARTESIAN_POINT('Ctrl Pts',(-1.67060520664496,71.0955609044962,14.6201621132424));
#66726=CARTESIAN_POINT('Ctrl Pts',(-2.0603560408638,71.3013335441192,12.8448276351158));
#66727=CARTESIAN_POINT('Ctrl Pts',(-0.93957215743358,71.5055461680315,11.4243014812485));
#66728=CARTESIAN_POINT('Ctrl Pts',(0.40550289225763,71.6582005809317,11.3990386675022));
#66729=CARTESIAN_POINT('Ctrl Pts',(1.11208271950847,71.7600612367677,11.8202133174726));
#66730=CARTESIAN_POINT('Ctrl Pts',(1.41241673498102,71.8110242318205,12.0999056432097));
#66731=CARTESIAN_POINT('Ctrl Pts',(1.64329990355035,71.8620287013435,12.4404297508457));
#66732=CARTESIAN_POINT('Ctrl Pts',(1.89695314282964,71.9471455551232,13.0781051773961));
#66733=CARTESIAN_POINT('Ctrl Pts',(1.83256415044253,72.0666532279316,14.0874035564457));
#66734=CARTESIAN_POINT('Ctrl Pts',(0.962104623230294,72.2213767010501,15.0669320363937));
#66735=CARTESIAN_POINT('Ctrl Pts',(-0.337958266871026,72.377531937053,15.3062424616871));
#66736=CARTESIAN_POINT('Ctrl Pts',(-1.52421260295774,72.5355024001146,14.6886474208897));
#66737=CARTESIAN_POINT('Ctrl Pts',(-2.08752218108247,72.6956427643839,13.4555051592014));
#66738=CARTESIAN_POINT('Ctrl Pts',(-1.76874560062118,72.8582879309545,12.1159570331473));
#66739=CARTESIAN_POINT('Ctrl Pts',(-0.674952575141974,73.0237696356469,
11.2404866924554));
#66740=CARTESIAN_POINT('Ctrl Pts',(0.752513035129063,73.1923957376067,11.2221131144679));
#66741=CARTESIAN_POINT('Ctrl Pts',(1.91283612384496,73.3644448018013,12.1029581120033));
#66742=CARTESIAN_POINT('Ctrl Pts',(2.29557687606458,73.5401868548836,13.540134693823));
#66743=CARTESIAN_POINT('Ctrl Pts',(1.69944574866197,73.7198517598374,14.9400254502113));
#66744=CARTESIAN_POINT('Ctrl Pts',(0.336327576146208,73.9036547064504,15.6935073935344));
#66745=CARTESIAN_POINT('Ctrl Pts',(-1.2323293901161,74.0917775713935,15.4457097555331));
#66746=CARTESIAN_POINT('Ctrl Pts',(-2.48099670878324,74.3057722986777,14.1214011270144));
#66747=CARTESIAN_POINT('Ctrl Pts',(-2.44813531553989,74.5037344805762,12.382877346289));
#66748=CARTESIAN_POINT('Ctrl Pts',(-1.38529712269576,74.7064113117189,11.0927947919148));
#66749=CARTESIAN_POINT('Ctrl Pts',(0.0761051433055752,74.8900869545002,
10.5799131857687));
#66750=CARTESIAN_POINT('Ctrl Pts',(1.77434608586349,75.1015032861798,11.1554593074796));
#66751=CARTESIAN_POINT('Ctrl Pts',(2.77788772857351,75.3176968388944,12.6850802054493));
#66752=CARTESIAN_POINT('Ctrl Pts',(2.62620965148495,75.5386335137904,14.5495123571817));
#66753=CARTESIAN_POINT('Ctrl Pts',(1.33328999982496,75.7642437987729,15.955286328065));
#66754=CARTESIAN_POINT('Ctrl Pts',(-0.591178797233786,75.9944316223205,
16.2738818981605));
#66755=CARTESIAN_POINT('Ctrl Pts',(-2.33192442200736,76.2290682941482,15.3254308855573));
#66756=CARTESIAN_POINT('Ctrl Pts',(-3.23829309295676,76.4945338696043,13.2621939855711));
#66757=CARTESIAN_POINT('Ctrl Pts',(-2.30526446888481,76.7924019737375,10.8075531069511));
#66758=CARTESIAN_POINT('Ctrl Pts',(0.470549679179745,77.1241082254333,9.86021766213912));
#66759=CARTESIAN_POINT('Ctrl Pts',(2.4719008027093,77.3915884531642,11.1168258797268));
#66760=CARTESIAN_POINT('Ctrl Pts',(3.03071063046922,77.5695270761517,12.4518810248836));
#66761=CARTESIAN_POINT('Ctrl Pts',(3.13633576036993,77.6553078611967,13.1327980781616));
#66762=CARTESIAN_POINT('Ctrl Pts',(3.12753235443733,77.74132081993,13.8246567319115));
#66763=CARTESIAN_POINT('Ctrl Pts',(2.90089929268681,77.8492766782512,14.6710381849245));
#66764=CARTESIAN_POINT('Ctrl Pts',(2.11552487772295,78.0228693834808,15.8432473944847));
#66765=CARTESIAN_POINT('Ctrl Pts',(0.478890328323348,78.2413936724085,16.7026522005448));
#66766=CARTESIAN_POINT('Ctrl Pts',(-1.72400085885123,78.5057220053945,16.3012120074322));
#66767=CARTESIAN_POINT('Ctrl Pts',(-3.22153128587838,78.7717940963577,14.6193601049952));
#66768=CARTESIAN_POINT('Ctrl Pts',(-3.36832057887537,79.0392354273075,12.360116816651));
#66769=CARTESIAN_POINT('Ctrl Pts',(-2.08754476289982,79.3076634830567,10.4826755272027));
#66770=CARTESIAN_POINT('Ctrl Pts',(-0.642359456202413,79.4870242114111,
10.0205035995757));
#66771=CARTESIAN_POINT('Ctrl Pts',(0.0762077621358257,79.576736385379,10.0364522530518));
#66772=CARTESIAN_POINT('Ctrl Pts',(2.81131480190565,83.9588917569221,11.7304854175133));
#66773=CARTESIAN_POINT('Ctrl Pts',(3.1634734059473,84.0490914904875,12.3617083701036));
#66774=CARTESIAN_POINT('Ctrl Pts',(3.41927311572191,84.2277460141943,13.8547319648058));
#66775=CARTESIAN_POINT('Ctrl Pts',(2.33912418555997,84.4943504633577,15.8372825840002));
#66776=CARTESIAN_POINT('Ctrl Pts',(0.287239187875634,84.7583831881601,16.7254887171579));
#66777=CARTESIAN_POINT('Ctrl Pts',(-1.86632053509874,85.0211986207285,16.1651191296993));
#66778=CARTESIAN_POINT('Ctrl Pts',(-3.21132830161042,85.2824397306322,14.4088646646408));
#66779=CARTESIAN_POINT('Ctrl Pts',(-3.18862357503074,85.5417678794362,12.2116117870217));
#66780=CARTESIAN_POINT('Ctrl Pts',(-1.83388297336382,85.7988641651152,10.5121773355353));
#66781=CARTESIAN_POINT('Ctrl Pts',(0.501237119890374,86.0816969064778,9.94806983576265));
#66782=CARTESIAN_POINT('Ctrl Pts',(2.3976931384394,86.3329225326326,11.0853724677802));
#66783=CARTESIAN_POINT('Ctrl Pts',(3.04292942468987,86.5533961798783,12.7795112871806));
#66784=CARTESIAN_POINT('Ctrl Pts',(2.92206733122934,86.7718730917204,14.5706524524003));
#66785=CARTESIAN_POINT('Ctrl Pts',(1.32567383401337,87.041052574509,16.3290287773339));
#66786=CARTESIAN_POINT('Ctrl Pts',(-1.47145643355607,87.3572972781939,16.1899578223516));
#66787=CARTESIAN_POINT('Ctrl Pts',(-3.08216932414845,87.6663565997973,13.9789898804522));
#66788=CARTESIAN_POINT('Ctrl Pts',(-2.47216016580187,87.942769012737,11.6185629897703));
#66789=CARTESIAN_POINT('Ctrl Pts',(-0.690694897967686,88.1883927916437,
10.5383284001373));
#66790=CARTESIAN_POINT('Ctrl Pts',(1.13002648557816,88.4050238387048,10.747872608232));
#66791=CARTESIAN_POINT('Ctrl Pts',(2.40770993731236,88.6171836897901,12.0115089895042));
#66792=CARTESIAN_POINT('Ctrl Pts',(2.63267941973996,88.8248658396074,13.7554790818738));
#66793=CARTESIAN_POINT('Ctrl Pts',(1.75537245676262,89.0280911225172,15.2362829583177));
#66794=CARTESIAN_POINT('Ctrl Pts',(0.186729728072551,89.2269139728645,15.8489582981416));
#66795=CARTESIAN_POINT('Ctrl Pts',(-1.39147934974809,89.4214132646649,15.3763700465788));
#66796=CARTESIAN_POINT('Ctrl Pts',(-2.32347814117571,89.6117006625855,14.0612378074417));
#66797=CARTESIAN_POINT('Ctrl Pts',(-2.24973188901709,89.7979186483429,12.4855872732891));
#66798=CARTESIAN_POINT('Ctrl Pts',(-1.24305608263045,89.9802295684301,11.3145613956799));
#66799=CARTESIAN_POINT('Ctrl Pts',(0.240233047129281,90.1588265301917,11.0178176751031));
#66800=CARTESIAN_POINT('Ctrl Pts',(1.56532538871952,90.3339330312789,11.6840101966434));
#66801=CARTESIAN_POINT('Ctrl Pts',(2.18729149046849,90.505783787506,12.9997555342965));
#66802=CARTESIAN_POINT('Ctrl Pts',(1.87494079047942,90.6746486932259,14.395446589982));
#66803=CARTESIAN_POINT('Ctrl Pts',(0.784888113405734,90.8408045247825,15.2867363064573));
#66804=CARTESIAN_POINT('Ctrl Pts',(-0.600743943724048,91.0045575052185,
15.3198072369973));
#66805=CARTESIAN_POINT('Ctrl Pts',(-1.70177211459418,91.1662251260324,14.5004567628948));
#66806=CARTESIAN_POINT('Ctrl Pts',(-2.01714312898682,91.3083684314537,13.3429961213115));
#66807=CARTESIAN_POINT('Ctrl Pts',(-1.65649172539696,91.467107854453,12.0840708518216));
#66808=CARTESIAN_POINT('Ctrl Pts',(-0.532550109112778,91.6246713686028,
11.2747192128877));
#66809=CARTESIAN_POINT('Ctrl Pts',(0.932547456212629,91.7988368784177,11.4993881399202));
#66810=CARTESIAN_POINT('Ctrl Pts',(1.84228482993564,91.9552567777171,12.4572187451289));
#66811=CARTESIAN_POINT('Ctrl Pts',(1.9721115764305,92.111714941055,13.7771894871907));
#66812=CARTESIAN_POINT('Ctrl Pts',(1.25989227087951,92.2685707605075,14.8984729993988));
#66813=CARTESIAN_POINT('Ctrl Pts',(0.00333932959659818,92.4262004921002,
15.348492069359));
#66814=CARTESIAN_POINT('Ctrl Pts',(-1.2749231585388,92.5849565243759,14.9263720564591));
#66815=CARTESIAN_POINT('Ctrl Pts',(-2.02797557135136,92.7451870109718,13.7999461577328));
#66816=CARTESIAN_POINT('Ctrl Pts',(-1.92439385153347,92.9252507192101,12.2749837865247));
#66817=CARTESIAN_POINT('Ctrl Pts',(-0.598169095806888,93.1263804160157,
11.0929087972298));
#66818=CARTESIAN_POINT('Ctrl Pts',(1.36056420078383,93.3503628519224,11.4015256735229));
#66819=CARTESIAN_POINT('Ctrl Pts',(2.30107078704159,93.560499426661,12.9987178470627));
#66820=CARTESIAN_POINT('Ctrl Pts',(1.90268123985577,93.7558063742613,14.6070907964034));
#66821=CARTESIAN_POINT('Ctrl Pts',(0.712823826060705,93.9351257409999,15.5472965779981));
#66822=CARTESIAN_POINT('Ctrl Pts',(-0.838406291108695,94.1181965624792,
15.5576480364145));
#66823=CARTESIAN_POINT('Ctrl Pts',(-2.09367889856679,94.3052082155816,14.5919591474277));
#66824=CARTESIAN_POINT('Ctrl Pts',(-2.49940843490071,94.4963211079793,13.0251281454885));
#66825=CARTESIAN_POINT('Ctrl Pts',(-1.84207682216284,94.6916699268768,11.5069054891674));
#66826=CARTESIAN_POINT('Ctrl Pts',(-0.324467363129059,94.8958280351608,
10.67837767433));
#66827=CARTESIAN_POINT('Ctrl Pts',(0.854984362619392,95.0365675621011,10.8955737776502));
#66828=CARTESIAN_POINT('Ctrl Pts',(1.35943926359463,95.1100701719084,11.2003610085549));
#66829=CARTESIAN_POINT('Ctrl Pts',(2.5854520276638,84.1873662167992,11.8188762531224));
#66830=CARTESIAN_POINT('Ctrl Pts',(2.91253206383163,84.2709353426817,12.4032348828803));
#66831=CARTESIAN_POINT('Ctrl Pts',(3.14915586599972,84.4359195989222,13.7819068115739));
#66832=CARTESIAN_POINT('Ctrl Pts',(2.15807315015206,84.6806566806843,15.6020916097792));
#66833=CARTESIAN_POINT('Ctrl Pts',(0.285068220968175,84.9216996807521,16.413348807361));
#66834=CARTESIAN_POINT('Ctrl Pts',(-1.67109844695777,85.160415163267,15.9047677567488));
#66835=CARTESIAN_POINT('Ctrl Pts',(-2.88744692882538,85.396612122941,14.3171209916001));
#66836=CARTESIAN_POINT('Ctrl Pts',(-2.86740715724632,85.6301207841428,12.3386894762662));
#66837=CARTESIAN_POINT('Ctrl Pts',(-1.65225590824352,85.860792556601,10.8136250694661));
#66838=CARTESIAN_POINT('Ctrl Pts',(0.436403417431028,86.1137925878981,10.3085700292359));
#66839=CARTESIAN_POINT('Ctrl Pts',(2.12820626833387,86.3378901386587,11.3228458190353));
#66840=CARTESIAN_POINT('Ctrl Pts',(2.70362696673639,86.5342434618883,12.8312527502471));
#66841=CARTESIAN_POINT('Ctrl Pts',(2.5969382753804,86.7286734444469,14.4252978231867));
#66842=CARTESIAN_POINT('Ctrl Pts',(1.17810109142946,86.9680636529594,15.9898183410281));
#66843=CARTESIAN_POINT('Ctrl Pts',(-1.31035803152768,87.2494235126238,15.8682322153034));
#66844=CARTESIAN_POINT('Ctrl Pts',(-2.74839274372567,87.5248733235881,13.899654818273));
#66845=CARTESIAN_POINT('Ctrl Pts',(-2.20647747994194,87.7720165816171,11.7883563528541));
#66846=CARTESIAN_POINT('Ctrl Pts',(-0.608731181166276,87.9925368752317,
10.8159473053283));
#66847=CARTESIAN_POINT('Ctrl Pts',(1.03336076441061,88.1878849652216,11.0018719634053));
#66848=CARTESIAN_POINT('Ctrl Pts',(2.19404375918698,88.3802174652576,12.1448397907251));
#66849=CARTESIAN_POINT('Ctrl Pts',(2.40320971567541,88.5696601920862,13.7349977865651));
#66850=CARTESIAN_POINT('Ctrl Pts',(1.60121716602805,88.756357255753,15.097533337494));
#66851=CARTESIAN_POINT('Ctrl Pts',(0.150600329632758,88.9404760425103,15.6695519202184));
#66852=CARTESIAN_POINT('Ctrl Pts',(-1.32532063886921,89.1221914699639,15.2334970850425));
#66853=CARTESIAN_POINT('Ctrl Pts',(-2.20954062082533,89.3017028467093,13.9966386823743));
#66854=CARTESIAN_POINT('Ctrl Pts',(-2.14615455673499,89.4792262135844,12.4944725429736));
#66855=CARTESIAN_POINT('Ctrl Pts',(-1.18159272372089,89.6549805577111,11.3608275948985));
#66856=CARTESIAN_POINT('Ctrl Pts',(0.263464546250137,89.8292040840662,11.0633309231916));
#66857=CARTESIAN_POINT('Ctrl Pts',(1.57592204643969,90.002150022639,11.7131990761825));
#66858=CARTESIAN_POINT('Ctrl Pts',(2.2066228743119,90.174067094111,13.0250484964761));
#66859=CARTESIAN_POINT('Ctrl Pts',(1.90011809253171,90.3452248620228,14.441461025335));
#66860=CARTESIAN_POINT('Ctrl Pts',(0.787690164230864,90.5158848987094,15.3651514375489));
#66861=CARTESIAN_POINT('Ctrl Pts',(-0.65374675169598,90.6863230737345,15.4110429139321));
#66862=CARTESIAN_POINT('Ctrl Pts',(-1.82192680704175,90.8568112840542,14.557063743915));
#66863=CARTESIAN_POINT('Ctrl Pts',(-2.16924526933698,91.0086416664991,13.3239025695316));
#66864=CARTESIAN_POINT('Ctrl Pts',(-1.79137319025143,91.1799469073033,11.9627293492403));
#66865=CARTESIAN_POINT('Ctrl Pts',(-0.573590439104622,91.3520233928302,
11.06642807203));
#66866=CARTESIAN_POINT('Ctrl Pts',(1.04905466587743,91.544670528724,11.2989185145622));
#66867=CARTESIAN_POINT('Ctrl Pts',(2.07539198860986,91.7194272837472,12.3590436946813));
#66868=CARTESIAN_POINT('Ctrl Pts',(2.23623694555617,91.8958025280184,13.8450315151429));
#66869=CARTESIAN_POINT('Ctrl Pts',(1.43969013104392,92.0740242729069,15.1265597720918));
#66870=CARTESIAN_POINT('Ctrl Pts',(0.00790787849180596,92.2543203617113,
15.6550412764804));
#66871=CARTESIAN_POINT('Ctrl Pts',(-1.4663543163428,92.4368930058903,15.183803995202));
#66872=CARTESIAN_POINT('Ctrl Pts',(-2.3478777074049,92.6219321531392,13.8915311332495));
#66873=CARTESIAN_POINT('Ctrl Pts',(-2.24421352307133,92.8304711337829,12.1247829321979));
#66874=CARTESIAN_POINT('Ctrl Pts',(-0.717840456061674,93.0638544450115,
10.7397389347576));
#66875=CARTESIAN_POINT('Ctrl Pts',(1.55753455888578,93.3237562683135,11.0790571099927));
#66876=CARTESIAN_POINT('Ctrl Pts',(2.66050638885144,93.5670930898916,12.9199648922052));
#66877=CARTESIAN_POINT('Ctrl Pts',(2.21453464333129,93.7924946455065,14.7791660858403));
#66878=CARTESIAN_POINT('Ctrl Pts',(0.85454209279392,93.998641329072,15.8694668344574));
#66879=CARTESIAN_POINT('Ctrl Pts',(-0.919977059355176,94.208104937822,15.8930508439885));
#66880=CARTESIAN_POINT('Ctrl Pts',(-2.35489039484447,94.420895720329,14.8032782782973));
#66881=CARTESIAN_POINT('Ctrl Pts',(-2.82392567654851,94.6370014294129,13.0344450229515));
#66882=CARTESIAN_POINT('Ctrl Pts',(-2.09501575230247,94.8563877686733,11.3256031638159));
#66883=CARTESIAN_POINT('Ctrl Pts',(-0.40807524298053,95.0839772241254,10.3935981604164));
#66884=CARTESIAN_POINT('Ctrl Pts',(0.897190420009427,95.2396054419005,10.6278613760455));
#66885=CARTESIAN_POINT('Ctrl Pts',(1.45434235785663,95.3205220683781,10.9601002251437));
#66886=CARTESIAN_POINT('Ctrl Pts',(2.35958925342194,84.4158406766762,11.9072670887315));
#66887=CARTESIAN_POINT('Ctrl Pts',(2.66159072171595,84.4927791948759,12.444761395657));
#66888=CARTESIAN_POINT('Ctrl Pts',(2.87903861627751,84.6440931836499,13.7090816583421));
#66889=CARTESIAN_POINT('Ctrl Pts',(1.97702211474414,84.866962898011,15.3669006355582));
#66890=CARTESIAN_POINT('Ctrl Pts',(0.282897254060713,85.0850161733442,16.1012088975638));
#66891=CARTESIAN_POINT('Ctrl Pts',(-1.47587635881681,85.2996317058054,15.6444163837983));
#66892=CARTESIAN_POINT('Ctrl Pts',(-2.56356555604033,85.5107845152498,14.2253773185593));
#66893=CARTESIAN_POINT('Ctrl Pts',(-2.5461907394619,85.7184736888495,12.4657671655105));
#66894=CARTESIAN_POINT('Ctrl Pts',(-1.47062884312324,85.9227209480869,11.1150728033969));
#66895=CARTESIAN_POINT('Ctrl Pts',(0.371569714971683,86.1458882693185,10.6690702227092));
#66896=CARTESIAN_POINT('Ctrl Pts',(1.85871939822834,86.3428577446849,11.5603191702903));
#66897=CARTESIAN_POINT('Ctrl Pts',(2.36432450878294,86.5150907438982,12.8829942133133));
#66898=CARTESIAN_POINT('Ctrl Pts',(2.27180921953146,86.6854737971734,14.2799431939731));
#66899=CARTESIAN_POINT('Ctrl Pts',(1.03052834884555,86.8950747314099,15.6506079047223));
#66900=CARTESIAN_POINT('Ctrl Pts',(-1.14925962949929,87.1415497470537,15.5465066082551));
#66901=CARTESIAN_POINT('Ctrl Pts',(-2.41461616330291,87.383390047379,13.8203197560938));
#66902=CARTESIAN_POINT('Ctrl Pts',(-1.94079479408201,87.6012641504972,11.9581497159379));
#66903=CARTESIAN_POINT('Ctrl Pts',(-0.526767464364877,87.7966809588198,
11.0935662105192));
#66904=CARTESIAN_POINT('Ctrl Pts',(0.936695043243057,87.9707460917385,11.2558713185787));
#66905=CARTESIAN_POINT('Ctrl Pts',(1.98037758106161,88.1432512407249,12.2781705919459));
#66906=CARTESIAN_POINT('Ctrl Pts',(2.17374001161086,88.3144545445653,13.7145164912566));
#66907=CARTESIAN_POINT('Ctrl Pts',(1.44706187529347,88.4846233889889,14.9587837166703));
#66908=CARTESIAN_POINT('Ctrl Pts',(0.114470931192956,88.654038112156,15.490145542295));
#66909=CARTESIAN_POINT('Ctrl Pts',(-1.25916192799034,88.822969675263,15.0906241235063));
#66910=CARTESIAN_POINT('Ctrl Pts',(-2.09560310047496,88.9917050308331,13.9320395573069));
#66911=CARTESIAN_POINT('Ctrl Pts',(-2.04257722445289,89.1605337788261,12.5033578126581));
#66912=CARTESIAN_POINT('Ctrl Pts',(-1.12012936481134,89.3297315469923,11.4070937941172));
#66913=CARTESIAN_POINT('Ctrl Pts',(0.286696045370998,89.4995816379407,11.1088441712803));
#66914=CARTESIAN_POINT('Ctrl Pts',(1.58651870415989,89.6703670139991,11.7423879557218));
#66915=CARTESIAN_POINT('Ctrl Pts',(2.22595425815534,89.842350400716,13.0503414586556));
#66916=CARTESIAN_POINT('Ctrl Pts',(1.92529539458401,90.0158010308196,14.4874754606883));
#66917=CARTESIAN_POINT('Ctrl Pts',(0.790492215056007,90.1909652726362,15.4435665686406));
#66918=CARTESIAN_POINT('Ctrl Pts',(-0.706749559667907,90.3680886422505,
15.5022785908669));
#66919=CARTESIAN_POINT('Ctrl Pts',(-1.94208149948933,90.5473974420758,14.6136707249352));
#66920=CARTESIAN_POINT('Ctrl Pts',(-2.32134740968715,90.7089149015442,13.3048090177519));
#66921=CARTESIAN_POINT('Ctrl Pts',(-1.92625465510593,90.8927859601538,11.8413878466589));
#66922=CARTESIAN_POINT('Ctrl Pts',(-0.614630769096463,91.0793754170575,
10.8581369311724));
#66923=CARTESIAN_POINT('Ctrl Pts',(1.16556187554226,91.2905041790304,11.0984488892043));
#66924=CARTESIAN_POINT('Ctrl Pts',(2.30849914728408,91.4835977897773,12.2608686442338));
#66925=CARTESIAN_POINT('Ctrl Pts',(2.50036231468186,91.6798901149816,13.9128735430949));
#66926=CARTESIAN_POINT('Ctrl Pts',(1.61948799120833,91.8794777853063,15.3546465447847));
#66927=CARTESIAN_POINT('Ctrl Pts',(0.0124764273870137,92.0824402313226,
15.9615904836018));
#66928=CARTESIAN_POINT('Ctrl Pts',(-1.65778547414679,92.2888294874047,15.4412359339448));
#66929=CARTESIAN_POINT('Ctrl Pts',(-2.66777984345844,92.4986772953065,13.9831161087662));
#66930=CARTESIAN_POINT('Ctrl Pts',(-2.56403319460919,92.7356915483555,11.9745820778711));
#66931=CARTESIAN_POINT('Ctrl Pts',(-0.83751181631646,93.0013284740074,10.3865690722854));
#66932=CARTESIAN_POINT('Ctrl Pts',(1.75450491698771,93.2971496847048,10.7565885464627));
#66933=CARTESIAN_POINT('Ctrl Pts',(3.01994199066127,93.5736867531223,12.8412119373476));
#66934=CARTESIAN_POINT('Ctrl Pts',(2.52638804680682,93.8291829167515,14.9512413752771));
#66935=CARTESIAN_POINT('Ctrl Pts',(0.996260359527135,94.0621569171439,16.1916370909168));
#66936=CARTESIAN_POINT('Ctrl Pts',(-1.00154782760166,94.298013313165,16.2284536515627));
#66937=CARTESIAN_POINT('Ctrl Pts',(-2.61610189112216,94.5365832250761,15.0145974091672));
#66938=CARTESIAN_POINT('Ctrl Pts',(-3.14844291819632,94.7776817508467,13.0437619004143));
#66939=CARTESIAN_POINT('Ctrl Pts',(-2.34795468244211,95.0211056104699,11.1443008384644));
#66940=CARTESIAN_POINT('Ctrl Pts',(-0.491683122832005,95.2721264130899,
10.1088186465028));
#66941=CARTESIAN_POINT('Ctrl Pts',(0.939396477399463,95.4426433216997,10.3601489744408));
#66942=CARTESIAN_POINT('Ctrl Pts',(1.54924545211863,95.5309739648478,10.7198394417325));
#66943=CARTESIAN_POINT('Ctrl Pts',(2.1337264791801,84.6443151365533,11.9956579243407));
#66944=CARTESIAN_POINT('Ctrl Pts',(2.41064937960028,84.7146230470702,12.4862879084337));
#66945=CARTESIAN_POINT('Ctrl Pts',(2.60892136655532,84.8522667683779,13.6362565051101));
#66946=CARTESIAN_POINT('Ctrl Pts',(1.79597107933622,85.0532691153375,15.1317096613373));
#66947=CARTESIAN_POINT('Ctrl Pts',(0.280726287153252,85.2483326659362,15.7890689877668));
#66948=CARTESIAN_POINT('Ctrl Pts',(-1.28065427067585,85.4388482483439,15.3840650108478));
#66949=CARTESIAN_POINT('Ctrl Pts',(-2.23968418325529,85.6249569075585,14.1336336455185));
#66950=CARTESIAN_POINT('Ctrl Pts',(-2.2249743216775,85.8068265935561,12.5928448547549));
#66951=CARTESIAN_POINT('Ctrl Pts',(-1.28900177800295,85.9846493395728,11.4165205373277));
#66952=CARTESIAN_POINT('Ctrl Pts',(0.306736012512332,86.1779839507388,11.0295704161824));
#66953=CARTESIAN_POINT('Ctrl Pts',(1.5892325281228,86.347825350711,11.7977925215452));
#66954=CARTESIAN_POINT('Ctrl Pts',(2.02502205082946,86.4959380259083,12.9347356763797));
#66955=CARTESIAN_POINT('Ctrl Pts',(1.94668016368254,86.6422741499,14.1345885647596));
#66956=CARTESIAN_POINT('Ctrl Pts',(0.882955606261628,86.8220858098603,15.3113974684164));
#66957=CARTESIAN_POINT('Ctrl Pts',(-0.988161227470902,87.0336759814836,
15.2247810012068));
#66958=CARTESIAN_POINT('Ctrl Pts',(-2.08083958288015,87.2419067711699,13.7409846939147));
#66959=CARTESIAN_POINT('Ctrl Pts',(-1.67511210822208,87.4305117193772,12.1279430790217));
#66960=CARTESIAN_POINT('Ctrl Pts',(-0.444803747563472,87.6008250424078,
11.3711851157103));
#66961=CARTESIAN_POINT('Ctrl Pts',(0.840029322075505,87.7536072182553,11.5098706737521));
#66962=CARTESIAN_POINT('Ctrl Pts',(1.76671140293624,87.9062850161924,12.4115013931666));
#66963=CARTESIAN_POINT('Ctrl Pts',(1.9442703075463,88.0592488970441,13.6940351959479));
#66964=CARTESIAN_POINT('Ctrl Pts',(1.2929065845589,88.2128895222246,14.8200340958466));
#66965=CARTESIAN_POINT('Ctrl Pts',(0.078341532753162,88.3676001818018,15.3107391643716));
#66966=CARTESIAN_POINT('Ctrl Pts',(-1.19300321711147,88.5237478805622,14.9477511619699));
#66967=CARTESIAN_POINT('Ctrl Pts',(-1.98166558012459,88.6817072149568,13.8674404322395));
#66968=CARTESIAN_POINT('Ctrl Pts',(-1.93899989217078,88.8418413440677,12.5122430823426));
#66969=CARTESIAN_POINT('Ctrl Pts',(-1.05866600590178,89.0044825362734,11.4533599933358));
#66970=CARTESIAN_POINT('Ctrl Pts',(0.309927544491852,89.1699591918152,11.1543574193689));
#66971=CARTESIAN_POINT('Ctrl Pts',(1.59711536188005,89.3385840053592,11.7715768352609));
#66972=CARTESIAN_POINT('Ctrl Pts',(2.24528564199875,89.5106337073209,13.0756344208351));
#66973=CARTESIAN_POINT('Ctrl Pts',(1.9504726966363,89.6863771996163,14.5334898960415));
#66974=CARTESIAN_POINT('Ctrl Pts',(0.793294265881137,89.866045646563,15.5219816997322));
#66975=CARTESIAN_POINT('Ctrl Pts',(-0.759752367639839,90.0498542107665,
15.5935142678018));
#66976=CARTESIAN_POINT('Ctrl Pts',(-2.0622361919369,90.2379836000976,14.6702777059554));
#66977=CARTESIAN_POINT('Ctrl Pts',(-2.4734495500373,90.4091881365894,13.2857154659721));
#66978=CARTESIAN_POINT('Ctrl Pts',(-2.06113611996042,90.6056250130043,11.7200463440775));
#66979=CARTESIAN_POINT('Ctrl Pts',(-0.655671099088308,90.8067274412847,
10.6498457903147));
#66980=CARTESIAN_POINT('Ctrl Pts',(1.28206908520706,91.0363378293367,10.8979792638463));
#66981=CARTESIAN_POINT('Ctrl Pts',(2.5416063059583,91.2477682958074,12.1626935937863));
#66982=CARTESIAN_POINT('Ctrl Pts',(2.76448768380754,91.4639777019449,13.9807155710471));
#66983=CARTESIAN_POINT('Ctrl Pts',(1.79928585137275,91.6849312977057,15.5827333174776));
#66984=CARTESIAN_POINT('Ctrl Pts',(0.0170449762822211,91.9105601009339,
16.2681396907231));
#66985=CARTESIAN_POINT('Ctrl Pts',(-1.84921663195079,92.1407659689192,15.6986678726876));
#66986=CARTESIAN_POINT('Ctrl Pts',(-2.98768197951198,92.3754224374738,14.0747010842829));
#66987=CARTESIAN_POINT('Ctrl Pts',(-2.88385286614705,92.640911962928,11.8243812235443));
#66988=CARTESIAN_POINT('Ctrl Pts',(-0.957183176571245,92.9388025030031,
10.0333992098132));
#66989=CARTESIAN_POINT('Ctrl Pts',(1.95147527508967,93.2705431010961,10.4341199829326));
#66990=CARTESIAN_POINT('Ctrl Pts',(3.3793775924711,93.5802804163528,12.7624589824902));
#66991=CARTESIAN_POINT('Ctrl Pts',(2.83824145028234,93.8658711879965,15.123316664714));
#66992=CARTESIAN_POINT('Ctrl Pts',(1.13797862626035,94.1256725052158,16.5138073473761));
#66993=CARTESIAN_POINT('Ctrl Pts',(-1.08311859584813,94.3879216885077,16.5638564591368));
#66994=CARTESIAN_POINT('Ctrl Pts',(-2.87731338739983,94.6522707298234,15.225916540037));
#66995=CARTESIAN_POINT('Ctrl Pts',(-3.47296015984411,94.9183620722804,13.0530787778772));
#66996=CARTESIAN_POINT('Ctrl Pts',(-2.60089361258174,95.1858234522663,10.9629985131129));
#66997=CARTESIAN_POINT('Ctrl Pts',(-0.575291002683476,95.4602756020544,
9.8240391325891));
#66998=CARTESIAN_POINT('Ctrl Pts',(0.981602534789498,95.645681201499,10.0924365728361));
#66999=CARTESIAN_POINT('Ctrl Pts',(1.64414854638063,95.7414258613175,10.4795786583213));
#67000=CARTESIAN_POINT('Ctrl Pts',(2.32926620539106,98.3820905511788,11.315870744573));
#67001=CARTESIAN_POINT('Ctrl Pts',(2.69493995777859,98.4541857528228,11.7630352306204));
#67002=CARTESIAN_POINT('Ctrl Pts',(3.15450211047238,98.5959918188983,12.8524682974727));
#67003=CARTESIAN_POINT('Ctrl Pts',(2.8728678713054,98.8053526764308,14.5732971974836));
#67004=CARTESIAN_POINT('Ctrl Pts',(1.7489436325344,99.0105003412595,15.8596457798458));
#67005=CARTESIAN_POINT('Ctrl Pts',(0.137401383018491,99.2128414252949,16.3532340115199));
#67006=CARTESIAN_POINT('Ctrl Pts',(-1.20008932127566,99.3790185028937,15.9985498101805));
#67007=CARTESIAN_POINT('Ctrl Pts',(-2.0298458980374,99.5104422645353,15.3341208557355));
#67008=CARTESIAN_POINT('Ctrl Pts',(-2.64371113418118,99.6408387621566,14.4754288465473));
#67009=CARTESIAN_POINT('Ctrl Pts',(-2.91077650132971,99.801879403758,13.1629053944612));
#67010=CARTESIAN_POINT('Ctrl Pts',(-2.30193793452482,100.013038207241,11.5098151807535));
#67011=CARTESIAN_POINT('Ctrl Pts',(-0.653860747579426,100.240650037961,
10.4643285577639));
#67012=CARTESIAN_POINT('Ctrl Pts',(1.39652630140739,100.483036430519,10.827076812383));
#67013=CARTESIAN_POINT('Ctrl Pts',(2.52533114927779,100.699746357258,12.3030925980515));
#67014=CARTESIAN_POINT('Ctrl Pts',(2.53500450171196,100.892395386792,13.9085733567948));
#67015=CARTESIAN_POINT('Ctrl Pts',(1.79773017141689,101.062432504713,15.1162732471124));
#67016=CARTESIAN_POINT('Ctrl Pts',(0.557534924579458,101.229155089766,15.7422279973987));
#67017=CARTESIAN_POINT('Ctrl Pts',(-0.571837703131487,101.365366721425,
15.6410180425175));
#67018=CARTESIAN_POINT('Ctrl Pts',(-1.33230934740187,101.47273570082,15.2210687872799));
#67019=CARTESIAN_POINT('Ctrl Pts',(-1.79058153699214,101.552468988986,14.7671787687757));
#67020=CARTESIAN_POINT('Ctrl Pts',(-2.10298870045688,101.631423318044,14.2100248929845));
#67021=CARTESIAN_POINT('Ctrl Pts',(-2.29941666157641,101.73566621192,13.3899123585956));
#67022=CARTESIAN_POINT('Ctrl Pts',(-2.10340034761895,101.864076701832,12.3374498456843));
#67023=CARTESIAN_POINT('Ctrl Pts',(-1.34801811984108,101.998445948856,11.5143857513643));
#67024=CARTESIAN_POINT('Ctrl Pts',(-0.214963331132888,102.147276247187,
11.07378096596));
#67025=CARTESIAN_POINT('Ctrl Pts',(1.0134066427486,102.29338793081,11.3094928437476));
#67026=CARTESIAN_POINT('Ctrl Pts',(1.898888574248,102.452466354268,12.2994347933101));
#67027=CARTESIAN_POINT('Ctrl Pts',(2.10849282477825,102.5932690289,13.4503728680158));
#67028=CARTESIAN_POINT('Ctrl Pts',(1.68169428198145,102.731883915474,14.5250971334327));
#67029=CARTESIAN_POINT('Ctrl Pts',(0.870570209303794,102.853302183626,15.1256434184298));
#67030=CARTESIAN_POINT('Ctrl Pts',(-0.21524462154583,102.988381671201,15.3203822425943));
#67031=CARTESIAN_POINT('Ctrl Pts',(-1.09816815381474,103.099539973989,14.9672230150072));
#67032=CARTESIAN_POINT('Ctrl Pts',(-1.62082829575769,103.202274108003,14.3196850878211));
#67033=CARTESIAN_POINT('Ctrl Pts',(-1.90109061114495,103.28989800875,13.6687113972404));
#67034=CARTESIAN_POINT('Ctrl Pts',(-1.89160665090365,103.376916014849,12.9440991525659));
#67035=CARTESIAN_POINT('Ctrl Pts',(-1.59953921394162,103.463444601711,12.3078190182658));
#67036=CARTESIAN_POINT('Ctrl Pts',(-1.14734301614179,103.549679693028,11.7763926106062));
#67037=CARTESIAN_POINT('Ctrl Pts',(-0.341801890305038,103.656998696664,
11.389519255861));
#67038=CARTESIAN_POINT('Ctrl Pts',(0.720330453089296,103.785246069805,11.5049339932187));
#67039=CARTESIAN_POINT('Ctrl Pts',(1.55977130459687,103.913188765162,12.1608445039213));
#67040=CARTESIAN_POINT('Ctrl Pts',(1.92756435851514,104.041056120166,13.1606287698491));
#67041=CARTESIAN_POINT('Ctrl Pts',(1.73609916594073,104.154858394614,14.0885033980296));
#67042=CARTESIAN_POINT('Ctrl Pts',(1.23283508114643,104.254681708604,14.7283130870023));
#67043=CARTESIAN_POINT('Ctrl Pts',(0.731674204292337,104.32618975619,15.0256034889539));
#67044=CARTESIAN_POINT('Ctrl Pts',(0.285162600187898,104.383544486588,15.1427637986439));
#67045=CARTESIAN_POINT('Ctrl Pts',(-0.176137074242099,104.441018582419,
15.1763120810118));
#67046=CARTESIAN_POINT('Ctrl Pts',(-0.751264634096996,104.51309058961,15.0567985842817));
#67047=CARTESIAN_POINT('Ctrl Pts',(-1.24688257511855,104.58553341317,14.7354388218607));
#67048=CARTESIAN_POINT('Ctrl Pts',(-1.55441023882616,104.643735615231,14.3823236486075));
#67049=CARTESIAN_POINT('Ctrl Pts',(-1.91377889489559,104.731316081866,13.7757375195179));
#67050=CARTESIAN_POINT('Ctrl Pts',(-1.99664443357858,104.863745532147,12.6438805035126));
#67051=CARTESIAN_POINT('Ctrl Pts',(-1.04309428332082,105.043102190833,11.4328977755217));
#67052=CARTESIAN_POINT('Ctrl Pts',(0.244197832177701,105.195270638501,11.2225120094968));
#67053=CARTESIAN_POINT('Ctrl Pts',(1.17430485409628,105.31885632517,11.6120647990092));
#67054=CARTESIAN_POINT('Ctrl Pts',(1.78711054085387,105.422926774664,12.1977614975811));
#67055=CARTESIAN_POINT('Ctrl Pts',(2.13921750944901,105.53887239286,13.0889544092712));
#67056=CARTESIAN_POINT('Ctrl Pts',(2.01431169320179,105.667297712427,14.1421503743038));
#67057=CARTESIAN_POINT('Ctrl Pts',(1.3711465398885,105.803211209963,15.0627365372946));
#67058=CARTESIAN_POINT('Ctrl Pts',(0.286102187432918,105.947032839628,15.5691851440355));
#67059=CARTESIAN_POINT('Ctrl Pts',(-0.973013580671568,106.099235761022,
15.4189649577865));
#67060=CARTESIAN_POINT('Ctrl Pts',(-1.98293771020574,106.25440520203,14.6132612144251));
#67061=CARTESIAN_POINT('Ctrl Pts',(-2.42540130933238,106.41264225971,13.3718877473894));
#67062=CARTESIAN_POINT('Ctrl Pts',(-2.14159152551099,106.574035260974,12.05824585642));
#67063=CARTESIAN_POINT('Ctrl Pts',(-1.18955423369878,106.738656846882,11.0719338039678));
#67064=CARTESIAN_POINT('Ctrl Pts',(0.219166308238618,106.913130725917,10.7155127352073));
#67065=CARTESIAN_POINT('Ctrl Pts',(1.17828412266602,107.03412190253,11.0517911283707));
#67066=CARTESIAN_POINT('Ctrl Pts',(1.58874560978865,107.098668256655,11.3669222244684));
#67067=CARTESIAN_POINT('Ctrl Pts',(2.16507776278379,98.4487062429102,11.4115576670062));
#67068=CARTESIAN_POINT('Ctrl Pts',(2.51172315852272,98.5164451800714,11.8291290167757));
#67069=CARTESIAN_POINT('Ctrl Pts',(2.9501904150609,98.6495211739876,12.8483188307114));
#67070=CARTESIAN_POINT('Ctrl Pts',(2.69810460566407,98.8455618367907,14.4613815118639));
#67071=CARTESIAN_POINT('Ctrl Pts',(1.65666157345432,99.0372836109927,15.671090461532));
#67072=CARTESIAN_POINT('Ctrl Pts',(0.156784680815158,99.2260577432743,16.1427198977121));
#67073=CARTESIAN_POINT('Ctrl Pts',(-1.09154198223851,99.3808653102375,15.8218016783094));
#67074=CARTESIAN_POINT('Ctrl Pts',(-1.86857646175828,99.5031875405753,15.2095054230858));
#67075=CARTESIAN_POINT('Ctrl Pts',(-2.44585043467083,99.6244894116808,14.4152909674852));
#67076=CARTESIAN_POINT('Ctrl Pts',(-2.70372853688371,99.77419436994,13.1972753456789));
#67077=CARTESIAN_POINT('Ctrl Pts',(-2.1505549898306,99.9703691734479,11.6571577300591));
#67078=CARTESIAN_POINT('Ctrl Pts',(-0.628257391422791,100.181757318978,
10.673676255501));
#67079=CARTESIAN_POINT('Ctrl Pts',(1.27892157899806,100.406914176573,10.9941873969971));
#67080=CARTESIAN_POINT('Ctrl Pts',(2.34048410598568,100.608394905306,12.3568259937458));
#67081=CARTESIAN_POINT('Ctrl Pts',(2.36315036799856,100.787749485407,13.851171738007));
#67082=CARTESIAN_POINT('Ctrl Pts',(1.68633892577243,100.946302723298,14.9835439965474));
#67083=CARTESIAN_POINT('Ctrl Pts',(0.533450727153234,101.102076850792,15.5794325826145));
#67084=CARTESIAN_POINT('Ctrl Pts',(-0.525066618352268,101.229653703928,
15.4951216475083));
#67085=CARTESIAN_POINT('Ctrl Pts',(-1.24261559725032,101.330433895234,15.1079982740459));
#67086=CARTESIAN_POINT('Ctrl Pts',(-1.67756889910168,101.405389363526,14.6856544196782));
#67087=CARTESIAN_POINT('Ctrl Pts',(-1.97695860024531,101.479737598154,14.1640433477083));
#67088=CARTESIAN_POINT('Ctrl Pts',(-2.17005146414342,101.57807228972,13.3924623469577));
#67089=CARTESIAN_POINT('Ctrl Pts',(-1.99538196912404,101.69955164982,12.3950488160063));
#67090=CARTESIAN_POINT('Ctrl Pts',(-1.28647863191238,101.827206737331,11.605377727602));
#67091=CARTESIAN_POINT('Ctrl Pts',(-0.210783711347632,101.969150612895,
11.1734303992142));
#67092=CARTESIAN_POINT('Ctrl Pts',(0.968980110784211,102.109197430349,11.3851065206294));
#67093=CARTESIAN_POINT('Ctrl Pts',(1.83449204726866,102.262652988264,12.329588887239));
#67094=CARTESIAN_POINT('Ctrl Pts',(2.05136790923078,102.399278256329,13.4435900836687));
#67095=CARTESIAN_POINT('Ctrl Pts',(1.6479272701096,102.534620253491,14.4978847248409));
#67096=CARTESIAN_POINT('Ctrl Pts',(0.858482367728352,102.653945955347,15.0980434272643));
#67097=CARTESIAN_POINT('Ctrl Pts',(-0.211879256810604,102.787446772081,
15.3038835430309));
#67098=CARTESIAN_POINT('Ctrl Pts',(-1.09508607595738,102.898069112918,14.9646832330691));
#67099=CARTESIAN_POINT('Ctrl Pts',(-1.6267785734138,103.000973018449,14.3228560151164));
#67100=CARTESIAN_POINT('Ctrl Pts',(-1.91674678972689,103.089055190921,13.6722937375774));
#67101=CARTESIAN_POINT('Ctrl Pts',(-1.91714874007563,103.177000200415,12.9400669685551));
#67102=CARTESIAN_POINT('Ctrl Pts',(-1.62887128498662,103.264921017815,12.2898310562481));
#67103=CARTESIAN_POINT('Ctrl Pts',(-1.17501187054071,103.352856902418,11.7420751853729));
#67104=CARTESIAN_POINT('Ctrl Pts',(-0.354999662671231,103.462876607181,
11.3341085134853));
#67105=CARTESIAN_POINT('Ctrl Pts',(0.742794669808538,103.595269319499,11.4378314328122));
#67106=CARTESIAN_POINT('Ctrl Pts',(1.6245574524756,103.728242056865,12.1070383547486));
#67107=CARTESIAN_POINT('Ctrl Pts',(2.0239406035163,103.862000653388,13.1471298237393));
#67108=CARTESIAN_POINT('Ctrl Pts',(1.83622631795286,103.981779730254,14.1262977461567));
#67109=CARTESIAN_POINT('Ctrl Pts',(1.3133416807573,104.087352933003,14.8100338655519));
#67110=CARTESIAN_POINT('Ctrl Pts',(0.785834080040622,104.163255187635,15.132724277827));
#67111=CARTESIAN_POINT('Ctrl Pts',(0.312439097394648,104.22429356955,15.2637142130627));
#67112=CARTESIAN_POINT('Ctrl Pts',(-0.178671074865471,104.285559869038,
15.3060159702618));
#67113=CARTESIAN_POINT('Ctrl Pts',(-0.794786296770833,104.362574759393,
15.1866477277048));
#67114=CARTESIAN_POINT('Ctrl Pts',(-1.330469273762,104.440218336155,14.8494644185806));
#67115=CARTESIAN_POINT('Ctrl Pts',(-1.66568812591068,104.502730747048,14.474658333133));
#67116=CARTESIAN_POINT('Ctrl Pts',(-2.06065477599685,104.596919873498,13.8276155705839));
#67117=CARTESIAN_POINT('Ctrl Pts',(-2.16697226106977,104.739796149952,12.6080465029953));
#67118=CARTESIAN_POINT('Ctrl Pts',(-1.15199041777266,104.934097470161,11.2824363581431));
#67119=CARTESIAN_POINT('Ctrl Pts',(0.243658765030482,105.099464035666,11.0354787111077));
#67120=CARTESIAN_POINT('Ctrl Pts',(1.26119383106488,105.233986560599,11.4466899111251));
#67121=CARTESIAN_POINT('Ctrl Pts',(1.9365604370268,105.347363371189,12.0763001234226));
#67122=CARTESIAN_POINT('Ctrl Pts',(2.33228516036666,105.473765523175,13.0429364538209));
#67123=CARTESIAN_POINT('Ctrl Pts',(2.20993278665595,105.613831408377,14.1929931475162));
#67124=CARTESIAN_POINT('Ctrl Pts',(1.52047758571895,105.762065900799,15.2051331481097));
#67125=CARTESIAN_POINT('Ctrl Pts',(0.344098514121134,105.91886873789,15.7708592678365));
#67126=CARTESIAN_POINT('Ctrl Pts',(-1.02912827537185,106.084671343671,15.6227001010336));
#67127=CARTESIAN_POINT('Ctrl Pts',(-2.13736931842044,106.253494995048,14.75831771187));
#67128=CARTESIAN_POINT('Ctrl Pts',(-2.63234926916575,106.42537687195,13.4152597750011));
#67129=CARTESIAN_POINT('Ctrl Pts',(-2.3395791441654,106.600340436149,11.9881676930327));
#67130=CARTESIAN_POINT('Ctrl Pts',(-1.32084832213294,106.778394314994,10.9110647073382));
#67131=CARTESIAN_POINT('Ctrl Pts',(0.194853311955219,106.966615675196,10.5115694226002));
#67132=CARTESIAN_POINT('Ctrl Pts',(1.22978840410585,107.096747140189,10.8633655039387));
#67133=CARTESIAN_POINT('Ctrl Pts',(1.67374240970349,107.166046927473,11.1972689795355));
#67134=CARTESIAN_POINT('Ctrl Pts',(2.00088932017653,98.5153219346416,11.5072445894395));
#67135=CARTESIAN_POINT('Ctrl Pts',(2.32850635926684,98.57870460732,11.8952228029309));
#67136=CARTESIAN_POINT('Ctrl Pts',(2.74587871964942,98.7030505290768,12.8441693639504));
#67137=CARTESIAN_POINT('Ctrl Pts',(2.52334134002275,98.8857709971507,14.3494658262441));
#67138=CARTESIAN_POINT('Ctrl Pts',(1.56437951437425,99.0640668807258,15.4825351432181));
#67139=CARTESIAN_POINT('Ctrl Pts',(0.176167978611816,99.2392740612538,15.9322057839043));
#67140=CARTESIAN_POINT('Ctrl Pts',(-0.982994643201375,99.3827121175813,
15.6450535464384));
#67141=CARTESIAN_POINT('Ctrl Pts',(-1.70730702547919,99.4959328166154,15.0848899904361));
#67142=CARTESIAN_POINT('Ctrl Pts',(-2.2479897351605,99.6081400612049,14.355153088423));
#67143=CARTESIAN_POINT('Ctrl Pts',(-2.49668057243772,99.7465093361221,13.2316452968967));
#67144=CARTESIAN_POINT('Ctrl Pts',(-1.99917204513637,99.9277001396536,11.8045002793647));
#67145=CARTESIAN_POINT('Ctrl Pts',(-0.602654035266162,100.122864599995,
10.883023953238));
#67146=CARTESIAN_POINT('Ctrl Pts',(1.16131685658873,100.330791922626,11.1612979816114));
#67147=CARTESIAN_POINT('Ctrl Pts',(2.15563706269356,100.517043453353,12.4105593894401));
#67148=CARTESIAN_POINT('Ctrl Pts',(2.19129623428519,100.683103584022,13.7937701192192));
#67149=CARTESIAN_POINT('Ctrl Pts',(1.57494768012797,100.830172941884,14.8508147459825));
#67150=CARTESIAN_POINT('Ctrl Pts',(0.509366529727014,100.974998611821,15.4166371678302));
#67151=CARTESIAN_POINT('Ctrl Pts',(-0.478295533573054,101.093940686429,
15.349225252499));
#67152=CARTESIAN_POINT('Ctrl Pts',(-1.15292184709877,101.188132089647,14.9949277608119));
#67153=CARTESIAN_POINT('Ctrl Pts',(-1.56455626121122,101.258309738068,14.6041300705805));
#67154=CARTESIAN_POINT('Ctrl Pts',(-1.85092850003376,101.328051878265,14.1180618024322));
#67155=CARTESIAN_POINT('Ctrl Pts',(-2.04068626671044,101.420478367521,13.39501233532));
#67156=CARTESIAN_POINT('Ctrl Pts',(-1.88736359062915,101.53502659781,12.4526477863286));
#67157=CARTESIAN_POINT('Ctrl Pts',(-1.22493914398367,101.655967525809,11.6963697038397));
#67158=CARTESIAN_POINT('Ctrl Pts',(-0.206604091562376,101.791024978605,
11.2730798324683));
#67159=CARTESIAN_POINT('Ctrl Pts',(0.924553578819829,101.925006929887,11.4607201975114));
#67160=CARTESIAN_POINT('Ctrl Pts',(1.77009552028933,102.072839622259,12.3597429811677));
#67161=CARTESIAN_POINT('Ctrl Pts',(1.99424299368331,102.205287483758,13.4368072993216));
#67162=CARTESIAN_POINT('Ctrl Pts',(1.61416025823776,102.337356591508,14.4706723162492));
#67163=CARTESIAN_POINT('Ctrl Pts',(0.846394526152918,102.454589727069,15.0704434360988));
#67164=CARTESIAN_POINT('Ctrl Pts',(-0.208513892075373,102.586511872962,
15.2873848434675));
#67165=CARTESIAN_POINT('Ctrl Pts',(-1.09200399810003,102.696598251846,14.9621434511312));
#67166=CARTESIAN_POINT('Ctrl Pts',(-1.63272885106989,102.799671928898,14.3260269424118));
#67167=CARTESIAN_POINT('Ctrl Pts',(-1.93240296830881,102.888212373092,13.6758760779144));
#67168=CARTESIAN_POINT('Ctrl Pts',(-1.94269082924761,102.977084385981,12.9360347845444));
#67169=CARTESIAN_POINT('Ctrl Pts',(-1.65820335603162,103.06639743392,12.2718430942304));
#67170=CARTESIAN_POINT('Ctrl Pts',(-1.20268072493963,103.156034111808,11.7077577601396));
#67171=CARTESIAN_POINT('Ctrl Pts',(-0.368197435037411,103.268754517698,
11.2786977711096));
#67172=CARTESIAN_POINT('Ctrl Pts',(0.765258886527789,103.405292569193,11.3707288724057));
#67173=CARTESIAN_POINT('Ctrl Pts',(1.68934360035434,103.543295348571,12.0532322055757));
#67174=CARTESIAN_POINT('Ctrl Pts',(2.12031684851748,103.682945186611,13.1336308776294));
#67175=CARTESIAN_POINT('Ctrl Pts',(1.93635346996498,103.808701065892,14.1640920942839));
#67176=CARTESIAN_POINT('Ctrl Pts',(1.39384828036816,103.920024157402,14.8917546441016));
#67177=CARTESIAN_POINT('Ctrl Pts',(0.839993955788918,104.000320619079,15.2398450667002));
#67178=CARTESIAN_POINT('Ctrl Pts',(0.339715594601406,104.065042652514,15.3846646274813));
#67179=CARTESIAN_POINT('Ctrl Pts',(-0.181205075488834,104.130101155658,
15.4357198595116));
#67180=CARTESIAN_POINT('Ctrl Pts',(-0.838307959444663,104.212058929177,
15.3164968711279));
#67181=CARTESIAN_POINT('Ctrl Pts',(-1.41405597240546,104.294903259141,14.9634900153004));
#67182=CARTESIAN_POINT('Ctrl Pts',(-1.77696601299519,104.361725878863,14.5669930176586));
#67183=CARTESIAN_POINT('Ctrl Pts',(-2.2075306570981,104.46252366513,13.8794936216499));
#67184=CARTESIAN_POINT('Ctrl Pts',(-2.33730008856093,104.615846767758,12.5722125024781));
#67185=CARTESIAN_POINT('Ctrl Pts',(-1.2608865522245,104.825092749488,11.1319749407646));
#67186=CARTESIAN_POINT('Ctrl Pts',(0.243119697883272,105.003657432829,10.8484454127187));
#67187=CARTESIAN_POINT('Ctrl Pts',(1.34808280803351,105.149116796028,11.2813150232408));
#67188=CARTESIAN_POINT('Ctrl Pts',(2.08601033319973,105.271799967715,11.9548387492641));
#67189=CARTESIAN_POINT('Ctrl Pts',(2.52535281128431,105.40865865349,12.9969184983707));
#67190=CARTESIAN_POINT('Ctrl Pts',(2.4055538801101,105.560365104324,14.2438359207287));
#67191=CARTESIAN_POINT('Ctrl Pts',(1.66980863154941,105.720920591636,15.3475297589247));
#67192=CARTESIAN_POINT('Ctrl Pts',(0.402094840809354,105.890704636152,15.9725333916377));
#67193=CARTESIAN_POINT('Ctrl Pts',(-1.08524297007214,106.070106926321,15.8264352442804));
#67194=CARTESIAN_POINT('Ctrl Pts',(-2.29180092663514,106.252584788068,14.9033742093148));
#67195=CARTESIAN_POINT('Ctrl Pts',(-2.83929722899912,106.438111484187,13.4586318026127));
#67196=CARTESIAN_POINT('Ctrl Pts',(-2.53756676281984,106.626645611325,11.9180895296454));
#67197=CARTESIAN_POINT('Ctrl Pts',(-1.45214241056707,106.818131783107,10.7501956107087));
#67198=CARTESIAN_POINT('Ctrl Pts',(0.170540315671819,107.020100624473,10.3076261099931));
#67199=CARTESIAN_POINT('Ctrl Pts',(1.28129268554569,107.159372377849,10.6749398795065));
#67200=CARTESIAN_POINT('Ctrl Pts',(1.75873920961835,107.233425598291,11.0276157346027));
#67201=CARTESIAN_POINT('Ctrl Pts',(1.83670087756925,98.5819376263729,11.6029315118727));
#67202=CARTESIAN_POINT('Ctrl Pts',(2.14528956001096,98.6409640345686,11.9613165890863));
#67203=CARTESIAN_POINT('Ctrl Pts',(2.54156702423794,98.7565798841661,12.8400198971892));
#67204=CARTESIAN_POINT('Ctrl Pts',(2.34857807438143,98.9259801575108,14.2375501406243));
#67205=CARTESIAN_POINT('Ctrl Pts',(1.47209745529416,99.0908501504588,15.2939798249042));
#67206=CARTESIAN_POINT('Ctrl Pts',(0.19555127640848,99.2524903792333,15.7216916700965));
#67207=CARTESIAN_POINT('Ctrl Pts',(-0.874447304164229,99.3845589249252,
15.4683054145673));
#67208=CARTESIAN_POINT('Ctrl Pts',(-1.54603758920007,99.4886780926552,14.9602745577865));
#67209=CARTESIAN_POINT('Ctrl Pts',(-2.05012903565016,99.591790710729,14.2950152093608));
#67210=CARTESIAN_POINT('Ctrl Pts',(-2.28963260799172,99.7188243023042,13.2660152481144));
#67211=CARTESIAN_POINT('Ctrl Pts',(-1.84778910044215,99.8850311058594,11.9518428286703));
#67212=CARTESIAN_POINT('Ctrl Pts',(-0.577050679109529,100.063971881012,
11.0923716509751));
#67213=CARTESIAN_POINT('Ctrl Pts',(1.04371213417939,100.25466966868,11.3284085662256));
#67214=CARTESIAN_POINT('Ctrl Pts',(1.97079001940144,100.425692001399,12.4642927851344));
#67215=CARTESIAN_POINT('Ctrl Pts',(2.01944210057179,100.578457682636,13.7363685004315));
#67216=CARTESIAN_POINT('Ctrl Pts',(1.46355643448351,100.71404316047,14.7180854954176));
#67217=CARTESIAN_POINT('Ctrl Pts',(0.485282332300793,100.847920372847,15.2538417530459));
#67218=CARTESIAN_POINT('Ctrl Pts',(-0.431524448793835,100.958227668931,
15.2033288574897));
#67219=CARTESIAN_POINT('Ctrl Pts',(-1.06322809694722,101.045830284061,14.8818572475778));
#67220=CARTESIAN_POINT('Ctrl Pts',(-1.45154362332076,101.111230112609,14.5226057214829));
#67221=CARTESIAN_POINT('Ctrl Pts',(-1.72489839982219,101.176366158375,14.072080257156));
#67222=CARTESIAN_POINT('Ctrl Pts',(-1.91132106927746,101.262884445321,13.3975623236822));
#67223=CARTESIAN_POINT('Ctrl Pts',(-1.77934521213425,101.370501545798,12.5102467566506));
#67224=CARTESIAN_POINT('Ctrl Pts',(-1.16339965605497,101.484728314285,11.7873616800774));
#67225=CARTESIAN_POINT('Ctrl Pts',(-0.202424471777119,101.612899344313,
11.3727292657226));
#67226=CARTESIAN_POINT('Ctrl Pts',(0.880127046855447,101.740816429424,11.5363338743933));
#67227=CARTESIAN_POINT('Ctrl Pts',(1.70569899331,101.883026256255,12.3898970750966));
#67228=CARTESIAN_POINT('Ctrl Pts',(1.93711807813584,102.011296711186,13.4300245149745));
#67229=CARTESIAN_POINT('Ctrl Pts',(1.58039324636591,102.140092929525,14.4434599076574));
#67230=CARTESIAN_POINT('Ctrl Pts',(0.834306684577478,102.25523349879,15.0428434449332));
#67231=CARTESIAN_POINT('Ctrl Pts',(-0.205148527340144,102.385576973841,
15.270886143904));
#67232=CARTESIAN_POINT('Ctrl Pts',(-1.08892192024266,102.495127390775,14.9596036691931));
#67233=CARTESIAN_POINT('Ctrl Pts',(-1.638679128726,102.598370839346,14.3291978697072));
#67234=CARTESIAN_POINT('Ctrl Pts',(-1.94805914689074,102.687369555263,13.6794584182514));
#67235=CARTESIAN_POINT('Ctrl Pts',(-1.9682329184196,102.777168571547,12.9320026005336));
#67236=CARTESIAN_POINT('Ctrl Pts',(-1.68753542707662,102.867873850023,12.2538551322126));
#67237=CARTESIAN_POINT('Ctrl Pts',(-1.23034957933855,102.959211321198,11.6734403349063));
#67238=CARTESIAN_POINT('Ctrl Pts',(-0.381395207403597,103.074632428216,
11.2232870287339));
#67239=CARTESIAN_POINT('Ctrl Pts',(0.787723103247037,103.215315818886,11.3036263119991));
#67240=CARTESIAN_POINT('Ctrl Pts',(1.75412974823307,103.358348640276,11.9994260564029));
#67241=CARTESIAN_POINT('Ctrl Pts',(2.21669309351866,103.503889719833,13.1201319315196));
#67242=CARTESIAN_POINT('Ctrl Pts',(2.03648062197711,103.635622401532,14.201886442411));
#67243=CARTESIAN_POINT('Ctrl Pts',(1.47435487997904,103.752695381801,14.9734754226512));
#67244=CARTESIAN_POINT('Ctrl Pts',(0.894153831537209,103.837386050524,15.3469658555734));
#67245=CARTESIAN_POINT('Ctrl Pts',(0.366992091808162,103.905791735478,15.5056150418999));
#67246=CARTESIAN_POINT('Ctrl Pts',(-0.183739076112201,103.974642442278,
15.5654237487616));
#67247=CARTESIAN_POINT('Ctrl Pts',(-0.881829622118494,104.06154309896,15.446346014551));
#67248=CARTESIAN_POINT('Ctrl Pts',(-1.49764267104891,104.149588182126,15.0775156120203));
#67249=CARTESIAN_POINT('Ctrl Pts',(-1.88824390007971,104.22072101068,14.6593277021841));
#67250=CARTESIAN_POINT('Ctrl Pts',(-2.35440653819935,104.328127456763,13.9313716727161));
#67251=CARTESIAN_POINT('Ctrl Pts',(-2.50762791605212,104.491897385563,12.5363785019609));
#67252=CARTESIAN_POINT('Ctrl Pts',(-1.36978268667635,104.716088028814,10.9815135233859));
#67253=CARTESIAN_POINT('Ctrl Pts',(0.242580630736055,104.907850829993,10.6614121143297));
#67254=CARTESIAN_POINT('Ctrl Pts',(1.43497178500211,105.064247031457,11.1159401353568));
#67255=CARTESIAN_POINT('Ctrl Pts',(2.23546022937266,105.196236564241,11.8333773751057));
#67256=CARTESIAN_POINT('Ctrl Pts',(2.71842046220195,105.343551783805,12.9509005429204));
#67257=CARTESIAN_POINT('Ctrl Pts',(2.60117497356426,105.506898800274,14.2946786939413));
#67258=CARTESIAN_POINT('Ctrl Pts',(1.81913967737985,105.679775282475,15.4899263697399));
#67259=CARTESIAN_POINT('Ctrl Pts',(0.460091167497574,105.862540534413,16.1742075154388));
#67260=CARTESIAN_POINT('Ctrl Pts',(-1.14135766477241,106.055542508971,16.0301703875275));
#67261=CARTESIAN_POINT('Ctrl Pts',(-2.44623253484984,106.251674581087,15.0484307067596));
#67262=CARTESIAN_POINT('Ctrl Pts',(-3.04624518883249,106.450846096425,13.5020038302243));
#67263=CARTESIAN_POINT('Ctrl Pts',(-2.73555438147426,106.6529507865,11.8480113662582));
#67264=CARTESIAN_POINT('Ctrl Pts',(-1.58343649900123,106.857869251219,10.589326514079));
#67265=CARTESIAN_POINT('Ctrl Pts',(0.14622731938842,107.073585573753,10.1036827973861));
#67266=CARTESIAN_POINT('Ctrl Pts',(1.33279696698552,107.221997615509,10.4865142550742));
#67267=CARTESIAN_POINT('Ctrl Pts',(1.8437360095332,107.300804269109,10.8579624896698));
#67268=CARTESIAN_POINT('Ctrl Pts',(2.49284186651808,100.7945130522,13.1110770588995));
#67269=CARTESIAN_POINT('Ctrl Pts',(2.51510269440366,100.863453425796,13.6629870657637));
#67270=CARTESIAN_POINT('Ctrl Pts',(2.17961349497895,100.999754830071,14.7663896380711));
#67271=CARTESIAN_POINT('Ctrl Pts',(0.795914331805827,101.1994864983,15.7392516655857));
#67272=CARTESIAN_POINT('Ctrl Pts',(-0.853766209202168,101.394579343051,
15.6554435518708));
#67273=CARTESIAN_POINT('Ctrl Pts',(-2.07338251428329,101.585126420958,14.5992895565228));
#67274=CARTESIAN_POINT('Ctrl Pts',(-2.3769033064482,101.771265881478,13.0525813475902));
#67275=CARTESIAN_POINT('Ctrl Pts',(-1.68070836712873,101.953168845295,11.6790615543513));
#67276=CARTESIAN_POINT('Ctrl Pts',(-0.316585819691275,102.131026046402,
11.0391790038355));
#67277=CARTESIAN_POINT('Ctrl Pts',(0.95913378208078,102.285723454486,11.3318051599028));
#67278=CARTESIAN_POINT('Ctrl Pts',(1.7385263897513,102.418771549116,12.0978996555273));
#67279=CARTESIAN_POINT('Ctrl Pts',(2.05900879000914,102.53130516533,12.9642472996834));
#67280=CARTESIAN_POINT('Ctrl Pts',(1.99140764775307,102.623895737268,13.7215605251988));
#67281=CARTESIAN_POINT('Ctrl Pts',(1.7505100490346,102.697301489324,14.2621652806589));
#67282=CARTESIAN_POINT('Ctrl Pts',(1.48692355688233,102.752034803086,14.6158543164599));
#67283=CARTESIAN_POINT('Ctrl Pts',(0.932904994664702,102.842734592139,15.0934843577826));
#67284=CARTESIAN_POINT('Ctrl Pts',(-0.0914144687160896,102.968333415228,
15.3762721980933));
#67285=CARTESIAN_POINT('Ctrl Pts',(-1.33485789371615,103.127446017604,14.853019541222));
#67286=CARTESIAN_POINT('Ctrl Pts',(-1.9848419465324,103.284558264171,13.6933545546193));
#67287=CARTESIAN_POINT('Ctrl Pts',(-1.7859198054212,103.440023723922,12.3916974239502));
#67288=CARTESIAN_POINT('Ctrl Pts',(-0.836554893827291,103.594221052691,
11.4959387949505));
#67289=CARTESIAN_POINT('Ctrl Pts',(0.456174919648817,103.747531635336,11.3738488107031));
#67290=CARTESIAN_POINT('Ctrl Pts',(1.3638147823984,103.874871679777,11.9549038831241));
#67291=CARTESIAN_POINT('Ctrl Pts',(1.76271423183761,103.976693557164,12.6795595279847));
#67292=CARTESIAN_POINT('Ctrl Pts',(1.90810598694439,104.078542102711,13.4945344024168));
#67293=CARTESIAN_POINT('Ctrl Pts',(1.65790918644532,104.17203697728,14.2442552014034));
#67294=CARTESIAN_POINT('Ctrl Pts',(1.18092989180617,104.257276104356,14.7396737469657));
#67295=CARTESIAN_POINT('Ctrl Pts',(0.836952047812147,104.308512974323,14.9680700673282));
#67296=CARTESIAN_POINT('Ctrl Pts',(0.450100297839354,104.359851063443,15.1155674993526));
#67297=CARTESIAN_POINT('Ctrl Pts',(0.0395872801241101,104.411306853854,
15.1750254409463));
#67298=CARTESIAN_POINT('Ctrl Pts',(-0.375108892402885,104.462898554674,
15.1429069972814));
#67299=CARTESIAN_POINT('Ctrl Pts',(-0.840313267844409,104.523254297577,
15.0001497606756));
#67300=CARTESIAN_POINT('Ctrl Pts',(-1.31270319649571,104.592502929932,14.6948548388226));
#67301=CARTESIAN_POINT('Ctrl Pts',(-1.70591154338413,104.670811240362,14.1946222164672));
#67302=CARTESIAN_POINT('Ctrl Pts',(-1.91536791775402,104.749572649424,13.5901594840855));
#67303=CARTESIAN_POINT('Ctrl Pts',(-1.92018868414222,104.85525116503,12.7322430362218));
#67304=CARTESIAN_POINT('Ctrl Pts',(-1.38717216919487,104.98870517941,11.7334940060542));
#67305=CARTESIAN_POINT('Ctrl Pts',(-0.270060311200083,105.13328337949,11.2421101980971));
#67306=CARTESIAN_POINT('Ctrl Pts',(1.07762575349443,105.29829144771,11.4226004121413));
#67307=CARTESIAN_POINT('Ctrl Pts',(1.94172923493356,105.438337213777,12.2957565076881));
#67308=CARTESIAN_POINT('Ctrl Pts',(2.11223738347851,105.571487979555,13.3693963868629));
#67309=CARTESIAN_POINT('Ctrl Pts',(1.96016494784412,105.686803188369,14.291952220544));
#67310=CARTESIAN_POINT('Ctrl Pts',(1.35126081272394,105.803960330811,15.0753078389932));
#67311=CARTESIAN_POINT('Ctrl Pts',(0.573346440079449,105.908193804669,15.4114252004776));
#67312=CARTESIAN_POINT('Ctrl Pts',(0.156498882992677,105.96074884795,15.4795852197261));
#67313=CARTESIAN_POINT('Ctrl Pts',(-0.0852434104585933,105.99090946777,
15.4884288797639));
#67314=CARTESIAN_POINT('Ctrl Pts',(-0.690982562143647,106.066524384947,
15.4613152548541));
#67315=CARTESIAN_POINT('Ctrl Pts',(-1.69935828633558,106.196714378299,15.0178602255304));
#67316=CARTESIAN_POINT('Ctrl Pts',(-2.45487748272796,106.384833620489,13.6157127030245));
#67317=CARTESIAN_POINT('Ctrl Pts',(-2.18187137791978,106.577424396135,12.0086256405781));
#67318=CARTESIAN_POINT('Ctrl Pts',(-0.948900392360805,106.774611627066,
10.8830013639477));
#67319=CARTESIAN_POINT('Ctrl Pts',(0.233539243349673,106.914804888263,10.7911776881976));
#67320=CARTESIAN_POINT('Ctrl Pts',(0.823185956938756,106.991473315452,10.9644105236304));
#67321=CARTESIAN_POINT('Ctrl Pts',(0.909520965425754,107.002848116697,10.9936163144232));
#67322=CARTESIAN_POINT('Ctrl Pts',(1.03788710524578,107.019926828246,11.0410609823112));
#67323=CARTESIAN_POINT('Ctrl Pts',(1.22456730925336,107.045442868801,11.1251201833512));
#67324=CARTESIAN_POINT('Ctrl Pts',(1.3818642775407,107.068192490325,11.2177754657732));
#67325=CARTESIAN_POINT('Ctrl Pts',(1.45735612640718,107.079506406801,11.2679629878995));
#67326=CARTESIAN_POINT('Ctrl Pts',(3.21941318832154,100.108785057528,13.1833163433551));
#67327=CARTESIAN_POINT('Ctrl Pts',(3.24455523314204,100.197321287997,13.8923045368011));
#67328=CARTESIAN_POINT('Ctrl Pts',(2.80713176742478,100.374361485089,15.3250956794238));
#67329=CARTESIAN_POINT('Ctrl Pts',(0.969614502742895,100.639422025843,16.6144421993269));
#67330=CARTESIAN_POINT('Ctrl Pts',(-1.26454957428976,100.903625125234,16.4990836728105));
#67331=CARTESIAN_POINT('Ctrl Pts',(-2.94684780441473,101.166617778622,15.0400296462461));
#67332=CARTESIAN_POINT('Ctrl Pts',(-3.37158210295618,101.428047309056,12.8672526496821));
#67333=CARTESIAN_POINT('Ctrl Pts',(-2.37673874171828,101.687566346648,10.9082910923444));
#67334=CARTESIAN_POINT('Ctrl Pts',(-0.402489017164984,101.944858172735,
9.98417551291717));
#67335=CARTESIAN_POINT('Ctrl Pts',(1.46456479582327,102.171301975291,10.4145590099485));
#67336=CARTESIAN_POINT('Ctrl Pts',(2.61231259502638,102.367597713274,11.5473339970204));
#67337=CARTESIAN_POINT('Ctrl Pts',(3.08497142042482,102.534508032253,12.8333323454061));
#67338=CARTESIAN_POINT('Ctrl Pts',(2.98184891257021,102.672415521047,13.961120190847));
#67339=CARTESIAN_POINT('Ctrl Pts',(2.62024973410492,102.781992635605,14.7672819481499));
#67340=CARTESIAN_POINT('Ctrl Pts',(2.22499652586286,102.86379154855,15.294913342711));
#67341=CARTESIAN_POINT('Ctrl Pts',(1.39445192806024,102.999473850705,16.0074493521681));
#67342=CARTESIAN_POINT('Ctrl Pts',(-0.140565850136767,103.187553708594,
16.4272206062621));
#67343=CARTESIAN_POINT('Ctrl Pts',(-1.9985595677167,103.425570942461,15.6387475870579));
#67344=CARTESIAN_POINT('Ctrl Pts',(-2.96048320986048,103.659593451464,13.9075444527093));
#67345=CARTESIAN_POINT('Ctrl Pts',(-2.65787738048873,103.889471146227,11.9838453444094));
#67346=CARTESIAN_POINT('Ctrl Pts',(-1.26176999230344,104.115073879095,10.6802078223776));
#67347=CARTESIAN_POINT('Ctrl Pts',(0.605124317383043,104.336304043699,10.5154870563486));
#67348=CARTESIAN_POINT('Ctrl Pts',(1.88707072683939,104.516961487962,11.3489400854149));
#67349=CARTESIAN_POINT('Ctrl Pts',(2.43904296713747,104.659246682307,12.3644427552886));
#67350=CARTESIAN_POINT('Ctrl Pts',(2.63371417310203,104.800036629377,13.4925391037022));
#67351=CARTESIAN_POINT('Ctrl Pts',(2.28458834892654,104.92703642919,14.5080554840302));
#67352=CARTESIAN_POINT('Ctrl Pts',(1.64371035343149,105.040835090016,15.165413844503));
#67353=CARTESIAN_POINT('Ctrl Pts',(1.18664880104888,105.108620123374,15.4647724792534));
#67354=CARTESIAN_POINT('Ctrl Pts',(0.678233264625506,105.17591182741,15.6547340548872));
#67355=CARTESIAN_POINT('Ctrl Pts',(0.144674432748567,105.242712965019,15.7282656905062));
#67356=CARTESIAN_POINT('Ctrl Pts',(-0.388137622843626,105.309026834882,
15.6831454939067));
#67357=CARTESIAN_POINT('Ctrl Pts',(-0.978854928122067,105.385826316907,
15.4970265683964));
#67358=CARTESIAN_POINT('Ctrl Pts',(-1.56896826791722,105.472795189938,15.1084644066728));
#67359=CARTESIAN_POINT('Ctrl Pts',(-2.04938088700793,105.569563993684,14.4857050331616));
#67360=CARTESIAN_POINT('Ctrl Pts',(-2.29698114254584,105.665276579509,13.7487193482343));
#67361=CARTESIAN_POINT('Ctrl Pts',(-2.29251479802894,105.79150776619,12.7231693556636));
#67362=CARTESIAN_POINT('Ctrl Pts',(-1.65421308374222,105.9467435063,11.5707423061279));
#67363=CARTESIAN_POINT('Ctrl Pts',(-0.392842510617309,106.108841018637,
11.0395975521201));
#67364=CARTESIAN_POINT('Ctrl Pts',(1.06923407512284,106.288091924768,11.2574218887874));
#67365=CARTESIAN_POINT('Ctrl Pts',(1.95337222561244,106.434482360356,12.1908952611499));
#67366=CARTESIAN_POINT('Ctrl Pts',(2.1082466558304,106.568779458601,13.2756411100311));
#67367=CARTESIAN_POINT('Ctrl Pts',(1.94421267177165,106.682846004844,14.1866454226411));
#67368=CARTESIAN_POINT('Ctrl Pts',(1.34330259058895,106.79540736939,14.9275804835321));
#67369=CARTESIAN_POINT('Ctrl Pts',(0.61200668180574,106.892712422958,15.2291155882341));
#67370=CARTESIAN_POINT('Ctrl Pts',(0.227225315900298,106.941080281224,15.2858774481804));
#67371=CARTESIAN_POINT('Ctrl Pts',(0.00613214032702904,106.968643257595,
15.2905083201661));
#67372=CARTESIAN_POINT('Ctrl Pts',(-0.54471342419038,107.037421791256,15.2571654833285));
#67373=CARTESIAN_POINT('Ctrl Pts',(-1.43438208415316,107.153376225102,14.8421645711519));
#67374=CARTESIAN_POINT('Ctrl Pts',(-2.05603692064065,107.314978655579,13.6223386293409));
#67375=CARTESIAN_POINT('Ctrl Pts',(-1.79818201528118,107.474811222724,12.2935478036575));
#67376=CARTESIAN_POINT('Ctrl Pts',(-0.786014398068314,107.6332147514,11.4126594286765));
#67377=CARTESIAN_POINT('Ctrl Pts',(0.137534125330372,107.742482326453,11.3631447251376));
#67378=CARTESIAN_POINT('Ctrl Pts',(0.587677173117342,107.801336393184,11.5049815654278));
#67379=CARTESIAN_POINT('Ctrl Pts',(0.653425842901073,107.810053434367,11.5286618432418));
#67380=CARTESIAN_POINT('Ctrl Pts',(0.75100760781322,107.823126728322,11.5669103329402));
#67381=CARTESIAN_POINT('Ctrl Pts',(0.956389857350736,107.851441476637,11.6642964257376));
#67382=CARTESIAN_POINT('Ctrl Pts',(1.35986455640331,107.912367400845,11.9449080491776));
#67383=CARTESIAN_POINT('Ctrl Pts',(1.78122114059743,107.999272471419,12.521010802963));
#67384=CARTESIAN_POINT('Ctrl Pts',(1.94192063122901,108.103466225824,13.3620056610018));
#67385=CARTESIAN_POINT('Ctrl Pts',(1.76390438783843,108.190300974208,14.0525436062148));
#67386=CARTESIAN_POINT('Ctrl Pts',(1.51226222511977,108.246795981566,14.4325824089464));
#67387=CARTESIAN_POINT('Ctrl Pts',(1.37402659897863,108.272882024984,14.5895751776131));
#67388=CARTESIAN_POINT('Ctrl Pts',(1.27618860602231,108.290276554284,14.6890093996381));
#67389=CARTESIAN_POINT('Ctrl Pts',(1.14383757110516,108.312027478503,14.8029233156905));
#67390=CARTESIAN_POINT('Ctrl Pts',(0.970805900348634,108.338144302769,14.9213825185975));
#67391=CARTESIAN_POINT('Ctrl Pts',(0.723945101066349,108.372989395592,15.0529453341035));
#67392=CARTESIAN_POINT('Ctrl Pts',(0.257373367219668,108.43402285334,15.2102168710372));
#67393=CARTESIAN_POINT('Ctrl Pts',(-0.460529247412758,108.521432115362,
15.2051861304357));
#67394=CARTESIAN_POINT('Ctrl Pts',(-1.24039994542318,108.626762875932,14.8304636360463));
#67395=CARTESIAN_POINT('Ctrl Pts',(-1.78791423789818,108.732648358347,14.1546113404499));
#67396=CARTESIAN_POINT('Ctrl Pts',(-1.99545953699991,108.839181926111,13.3045066713905));
#67397=CARTESIAN_POINT('Ctrl Pts',(-1.81861916546087,108.946473201078,12.4412539227986));
#67398=CARTESIAN_POINT('Ctrl Pts',(-1.2855418969239,109.054621381307,11.7304303379646));
#67399=CARTESIAN_POINT('Ctrl Pts',(-0.493259060560167,109.16372418882,11.3125997973087));
#67400=CARTESIAN_POINT('Ctrl Pts',(0.511368579472583,109.286110722847,11.2667175254659));
#67401=CARTESIAN_POINT('Ctrl Pts',(1.52783037367081,109.422363220256,11.7834151903454));
#67402=CARTESIAN_POINT('Ctrl Pts',(2.04447062716034,109.548086024133,12.7001566610426));
#67403=CARTESIAN_POINT('Ctrl Pts',(2.09991900669706,109.649879979524,13.5233406882324));
#67404=CARTESIAN_POINT('Ctrl Pts',(1.90500107311737,109.758925662751,14.3851318524273));
#67405=CARTESIAN_POINT('Ctrl Pts',(1.12516702783843,109.901988919277,15.311513234486));
#67406=CARTESIAN_POINT('Ctrl Pts',(-0.359505704859066,110.081107404553,
15.6254905457));
#67407=CARTESIAN_POINT('Ctrl Pts',(-1.75137860208549,110.2639827875,14.9469903243404));
#67408=CARTESIAN_POINT('Ctrl Pts',(-2.4471099510444,110.450802616763,13.5261006325578));
#67409=CARTESIAN_POINT('Ctrl Pts',(-2.11498461487842,110.641730113627,11.9439348554511));
#67410=CARTESIAN_POINT('Ctrl Pts',(-0.853141999308173,110.836900028849,
10.8768689052287));
#67411=CARTESIAN_POINT('Ctrl Pts',(0.866788744668601,111.040141111079,10.8090293100212));
#67412=CARTESIAN_POINT('Ctrl Pts',(1.82218329954828,111.179993228394,11.5191862896573));
#67413=CARTESIAN_POINT('Ctrl Pts',(2.13896789330312,111.252654201251,12.0080759845444));
#67414=CARTESIAN_POINT('Ctrl Pts',(2.97721912554466,100.337349853617,13.1591469020712));
#67415=CARTESIAN_POINT('Ctrl Pts',(3.0014225553287,100.41935795199,13.815805619725));
#67416=CARTESIAN_POINT('Ctrl Pts',(2.59798398913854,100.582822327766,15.138842769738));
#67417=CARTESIAN_POINT('Ctrl Pts',(0.911714445763874,100.826110183329,16.3227120214131));
#67418=CARTESIAN_POINT('Ctrl Pts',(-1.12762178592724,101.067276531172,16.2178702991639));
#67419=CARTESIAN_POINT('Ctrl Pts',(-2.65569270770424,101.306120659401,14.893116283005));
#67420=CARTESIAN_POINT('Ctrl Pts',(-3.04002250412019,101.542453499864,12.9290288823181));
#67421=CARTESIAN_POINT('Ctrl Pts',(-2.1447286168551,101.776100512864,11.16521457968));
#67422=CARTESIAN_POINT('Ctrl Pts',(-0.373854618007078,102.006914130624,
10.3358433432232));
#67423=CARTESIAN_POINT('Ctrl Pts',(1.29608779124244,102.209442468357,10.7203077266));
#67424=CARTESIAN_POINT('Ctrl Pts',(2.32105052660134,102.384655658554,11.7308558831893));
#67425=CARTESIAN_POINT('Ctrl Pts',(2.74298387695292,102.533440409946,12.8769706634986));
#67426=CARTESIAN_POINT('Ctrl Pts',(2.65170182429782,102.656242259788,13.8812669689642));
#67427=CARTESIAN_POINT('Ctrl Pts',(2.33033650574815,102.753762253511,14.598909725653));
#67428=CARTESIAN_POINT('Ctrl Pts',(1.97897220286934,102.826539300063,15.0685603339605));
#67429=CARTESIAN_POINT('Ctrl Pts',(1.24060295026172,102.947227431183,15.7027943540395));
#67430=CARTESIAN_POINT('Ctrl Pts',(-0.124182056329873,103.114480277472,
16.0769044702059));
#67431=CARTESIAN_POINT('Ctrl Pts',(-1.77732567638319,103.326195967508,15.3768382384458));
#67432=CARTESIAN_POINT('Ctrl Pts',(-2.63526945541779,103.534581722366,13.8361478200127));
#67433=CARTESIAN_POINT('Ctrl Pts',(-2.36722485546621,103.739655338792,12.1197960375897));
#67434=CARTESIAN_POINT('Ctrl Pts',(-1.12003162614473,103.941456270294,10.9521181465686));
#67435=CARTESIAN_POINT('Ctrl Pts',(0.555474518138305,104.140046574245,10.8016076411335));
#67436=CARTESIAN_POINT('Ctrl Pts',(1.71265207869239,104.3029315519,11.5509280179846));
#67437=CARTESIAN_POINT('Ctrl Pts',(2.21360005537086,104.431728973927,12.4694816795206));
#67438=CARTESIAN_POINT('Ctrl Pts',(2.39184477771615,104.559538453822,13.4932042032737));
#67439=CARTESIAN_POINT('Ctrl Pts',(2.07569529476612,104.675369945219,14.420122056488));
#67440=CARTESIAN_POINT('Ctrl Pts',(1.48945019955638,104.779648761463,15.0235004786572));
#67441=CARTESIAN_POINT('Ctrl Pts',(1.07008321663664,104.841917740357,15.2992050086116));
#67442=CARTESIAN_POINT('Ctrl Pts',(0.602188942363458,104.903891572755,15.475011869709));
#67443=CARTESIAN_POINT('Ctrl Pts',(0.109645381873752,104.965577594631,15.5438522739862));
#67444=CARTESIAN_POINT('Ctrl Pts',(-0.383794712696708,105.026984074812,
15.5030659950316));
#67445=CARTESIAN_POINT('Ctrl Pts',(-0.932674374696177,105.098302310464,
15.3314009658229));
#67446=CARTESIAN_POINT('Ctrl Pts',(-1.48354657744338,105.179364436602,14.9705945507227));
#67447=CARTESIAN_POINT('Ctrl Pts',(-1.93489110579998,105.269979742577,14.3886774275969));
#67448=CARTESIAN_POINT('Ctrl Pts',(-2.16977673428189,105.360041936148,13.6958660601848));
#67449=CARTESIAN_POINT('Ctrl Pts',(-2.16840609340003,105.47942223247,12.7261939158498));
#67450=CARTESIAN_POINT('Ctrl Pts',(-1.56519944555977,105.627397397336,11.62499287277));
#67451=CARTESIAN_POINT('Ctrl Pts',(-0.351915110811561,105.783655138921,
11.1071017674458));
#67452=CARTESIAN_POINT('Ctrl Pts',(1.07203130124671,105.958158432415,11.312481396572));
#67453=CARTESIAN_POINT('Ctrl Pts',(1.94949122871948,106.102433978162,12.225849009996));
#67454=CARTESIAN_POINT('Ctrl Pts',(2.10957689837978,106.236348965585,13.306892868975));
#67455=CARTESIAN_POINT('Ctrl Pts',(1.94953009712914,106.350831732687,14.2217476886087));
#67456=CARTESIAN_POINT('Ctrl Pts',(1.34595533130063,106.464925023196,14.9768229353525));
#67457=CARTESIAN_POINT('Ctrl Pts',(0.599119934563651,106.564539550196,15.289885458982));
#67458=CARTESIAN_POINT('Ctrl Pts',(0.203649838264434,106.614303136798,15.3504467053623));
#67459=CARTESIAN_POINT('Ctrl Pts',(-0.0243263766015025,106.64273199432,
15.356481840032));
#67460=CARTESIAN_POINT('Ctrl Pts',(-0.593469803508126,106.713789322486,
15.3252154071703));
#67461=CARTESIAN_POINT('Ctrl Pts',(-1.52270748488062,106.834488942835,14.9007297892781));
#67462=CARTESIAN_POINT('Ctrl Pts',(-2.18898377466974,107.004930310548,13.6201299872355));
#67463=CARTESIAN_POINT('Ctrl Pts',(-1.92607846949404,107.175682280527,12.1985737492977));
#67464=CARTESIAN_POINT('Ctrl Pts',(-0.840309729499128,107.347013709955,
11.2361067404336));
#67465=CARTESIAN_POINT('Ctrl Pts',(0.169535831336823,107.466589847056,11.1724890461576));
#67466=CARTESIAN_POINT('Ctrl Pts',(0.666180101057831,107.531382033941,11.324791218162));
#67467=CARTESIAN_POINT('Ctrl Pts',(0.738790883742652,107.540984995144,11.3503133336356));
#67468=CARTESIAN_POINT('Ctrl Pts',(0.846634106957426,107.555393428296,11.3916272160638));
#67469=CARTESIAN_POINT('Ctrl Pts',(1.07401648099589,107.586634405511,11.4972844068827));
#67470=CARTESIAN_POINT('Ctrl Pts',(1.52273373306752,107.654037196072,11.804042311152));
#67471=CARTESIAN_POINT('Ctrl Pts',(1.9967268298589,107.750680601562,12.4403935395825));
#67472=CARTESIAN_POINT('Ctrl Pts',(2.18490022917524,107.867299542099,13.3797933847505));
#67473=CARTESIAN_POINT('Ctrl Pts',(1.99148579757452,107.965076000406,14.1588828236315));
#67474=CARTESIAN_POINT('Ctrl Pts',(1.71074153044894,108.028951655748,14.590898884757));
#67475=CARTESIAN_POINT('Ctrl Pts',(1.55574190339104,108.058495319469,14.769973722537));
#67476=CARTESIAN_POINT('Ctrl Pts',(1.44585607606784,108.078208256583,14.8835704792628));
#67477=CARTESIAN_POINT('Ctrl Pts',(1.29687288352194,108.102881966276,15.0140356843413));
#67478=CARTESIAN_POINT('Ctrl Pts',(1.10156630049055,108.132544513271,15.1502224385089));
#67479=CARTESIAN_POINT('Ctrl Pts',(0.822227619337672,108.172167789794,15.3021958157975));
#67480=CARTESIAN_POINT('Ctrl Pts',(0.292462013639442,108.241697602338,15.4859538200435));
#67481=CARTESIAN_POINT('Ctrl Pts',(-0.527870899667793,108.341603780246,
15.4877029851746));
#67482=CARTESIAN_POINT('Ctrl Pts',(-1.42639530611788,108.462467618126,15.0660623239948));
#67483=CARTESIAN_POINT('Ctrl Pts',(-2.06365860953833,108.584372632003,14.2939479126033));
#67484=CARTESIAN_POINT('Ctrl Pts',(-2.31212380606438,108.707368925733,13.3149675711768));
#67485=CARTESIAN_POINT('Ctrl Pts',(-2.11658312055525,108.831513517464,12.3145741411436));
#67486=CARTESIAN_POINT('Ctrl Pts',(-1.50630007764062,108.956855261822,11.4854580477888));
#67487=CARTESIAN_POINT('Ctrl Pts',(-0.591603229966188,109.083440171806,
10.9926973044355));
#67488=CARTESIAN_POINT('Ctrl Pts',(0.573863165244347,109.225516128066,10.9292815651746));
#67489=CARTESIAN_POINT('Ctrl Pts',(1.75863530343156,109.383687562582,11.5189168345029));
#67490=CARTESIAN_POINT('Ctrl Pts',(2.36645968899241,109.529504991381,12.5769886842501));
#67491=CARTESIAN_POINT('Ctrl Pts',(2.43848095796253,109.647408968564,13.5296536457081));
#67492=CARTESIAN_POINT('Ctrl Pts',(2.22110617041835,109.773575853537,14.5283583099813));
#67493=CARTESIAN_POINT('Ctrl Pts',(1.32892436585788,109.93875195499,15.6044418360144));
#67494=CARTESIAN_POINT('Ctrl Pts',(-0.375735547519591,110.144754052652,
15.9775159621844));
#67495=CARTESIAN_POINT('Ctrl Pts',(-1.9737793652605,110.354075777694,15.2116037190409));
#67496=CARTESIAN_POINT('Ctrl Pts',(-2.77568014980066,110.566727843583,13.5994221513611));
#67497=CARTESIAN_POINT('Ctrl Pts',(-2.41047606829342,110.782699052213,11.8077710606813));
#67498=CARTESIAN_POINT('Ctrl Pts',(-0.999571941372368,111.001956153692,
10.6014571112487));
#67499=CARTESIAN_POINT('Ctrl Pts',(0.917719561938274,111.228591161885,10.5161593504357));
#67500=CARTESIAN_POINT('Ctrl Pts',(1.97805596779178,111.383286307474,11.2968351135459));
#67501=CARTESIAN_POINT('Ctrl Pts',(2.32997171279836,111.463304468483,11.833078989016));
#67502=CARTESIAN_POINT('Ctrl Pts',(2.7350250627678,100.565914649707,13.1349774607871));
#67503=CARTESIAN_POINT('Ctrl Pts',(2.75828987751536,100.641394615982,13.7393067026489));
#67504=CARTESIAN_POINT('Ctrl Pts',(2.38883621085233,100.791283170442,14.9525898600523));
#67505=CARTESIAN_POINT('Ctrl Pts',(0.853814388784849,101.012798340815,16.0309818434995));
#67506=CARTESIAN_POINT('Ctrl Pts',(-0.990693997564699,101.230927937112,
15.9366569255174));
#67507=CARTESIAN_POINT('Ctrl Pts',(-2.36453761099378,101.445623540179,14.7462029197638));
#67508=CARTESIAN_POINT('Ctrl Pts',(-2.70846290528419,101.656859690671,12.9908051149541));
#67509=CARTESIAN_POINT('Ctrl Pts',(-1.91271849199191,101.864634679079,11.4221380670157));
#67510=CARTESIAN_POINT('Ctrl Pts',(-0.345220218849182,102.068970088513,
10.6875111735294));
#67511=CARTESIAN_POINT('Ctrl Pts',(1.12761078666161,102.247582961421,11.0260564432514));
#67512=CARTESIAN_POINT('Ctrl Pts',(2.02978845817633,102.401713603836,11.9143777693584));
#67513=CARTESIAN_POINT('Ctrl Pts',(2.40099633348103,102.532372787637,12.9206089815911));
#67514=CARTESIAN_POINT('Ctrl Pts',(2.32155473602545,102.640068998527,13.8014137470815));
#67515=CARTESIAN_POINT('Ctrl Pts',(2.04042327739136,102.725531871417,14.4305375031559));
#67516=CARTESIAN_POINT('Ctrl Pts',(1.73294787987584,102.789287051574,14.8422073252102));
#67517=CARTESIAN_POINT('Ctrl Pts',(1.08675397246322,102.894981011661,15.3981393559111));
#67518=CARTESIAN_POINT('Ctrl Pts',(-0.107798262522985,103.041406846351,
15.7265883341495));
#67519=CARTESIAN_POINT('Ctrl Pts',(-1.55609178504967,103.226820992556,15.114928889834));
#67520=CARTESIAN_POINT('Ctrl Pts',(-2.3100557009751,103.409569993268,13.764751187316));
#67521=CARTESIAN_POINT('Ctrl Pts',(-2.07657233044371,103.589839531357,12.25574673077));
#67522=CARTESIAN_POINT('Ctrl Pts',(-0.978293259986012,103.767838661493,
11.2240284707595));
#67523=CARTESIAN_POINT('Ctrl Pts',(0.505824718893558,103.94378910479,11.0877282259183));
#67524=CARTESIAN_POINT('Ctrl Pts',(1.53823343054539,104.088901615839,11.7529159505543));
#67525=CARTESIAN_POINT('Ctrl Pts',(1.98815714360423,104.204211265545,12.5745206037526));
#67526=CARTESIAN_POINT('Ctrl Pts',(2.14997538233027,104.319040278266,13.4938693028453));
#67527=CARTESIAN_POINT('Ctrl Pts',(1.86680224060572,104.423703461249,14.3321886289457));
#67528=CARTESIAN_POINT('Ctrl Pts',(1.33519004568128,104.518462432909,14.8815871128114));
#67529=CARTESIAN_POINT('Ctrl Pts',(0.953517632224392,104.57521535734,15.1336375379699));
#67530=CARTESIAN_POINT('Ctrl Pts',(0.526144620101407,104.631871318099,15.2952896845308));
#67531=CARTESIAN_POINT('Ctrl Pts',(0.0746163309989309,104.688442224242,
15.3594388574662));
#67532=CARTESIAN_POINT('Ctrl Pts',(-0.379451802549797,104.744941314744,
15.3229864961564));
#67533=CARTESIAN_POINT('Ctrl Pts',(-0.886493821270294,104.81077830402,15.1657753632491));
#67534=CARTESIAN_POINT('Ctrl Pts',(-1.39812488696955,104.885933683268,14.8327246947727));
#67535=CARTESIAN_POINT('Ctrl Pts',(-1.82040132459206,104.97039549147,14.291649822032));
#67536=CARTESIAN_POINT('Ctrl Pts',(-2.04257232601797,105.054807292785,13.6430127721351));
#67537=CARTESIAN_POINT('Ctrl Pts',(-2.04429738877112,105.16733669875,12.7292184760357));
#67538=CARTESIAN_POINT('Ctrl Pts',(-1.47618580737732,105.308051288373,11.6792434394121));
#67539=CARTESIAN_POINT('Ctrl Pts',(-0.310987711005822,105.458469259206,
11.1746059827715));
#67540=CARTESIAN_POINT('Ctrl Pts',(1.07482852737057,105.628224940062,11.3675409043566));
#67541=CARTESIAN_POINT('Ctrl Pts',(1.94561023182653,105.77038559597,12.260802758842));
#67542=CARTESIAN_POINT('Ctrl Pts',(2.11090714092915,105.90391847257,13.338144627919));
#67543=CARTESIAN_POINT('Ctrl Pts',(1.95484752248664,106.018817460528,14.2568499545763));
#67544=CARTESIAN_POINT('Ctrl Pts',(1.34860807201228,106.134442677004,15.0260653871728));
#67545=CARTESIAN_POINT('Ctrl Pts',(0.586233187321556,106.236366677432,15.3506553297297));
#67546=CARTESIAN_POINT('Ctrl Pts',(0.18007436062856,106.287525992374,15.4150159625443));
#67547=CARTESIAN_POINT('Ctrl Pts',(-0.0547848935300436,106.316820731045,
15.4224553598979));
#67548=CARTESIAN_POINT('Ctrl Pts',(-0.642226182825883,106.390156853716,
15.3932653310122));
#67549=CARTESIAN_POINT('Ctrl Pts',(-1.6110328856081,106.515601660566,14.9592950074042));
#67550=CARTESIAN_POINT('Ctrl Pts',(-2.32193062869885,106.694881965519,13.6179213451299));
#67551=CARTESIAN_POINT('Ctrl Pts',(-2.0539749237069,106.876553338331,12.1035996949379));
#67552=CARTESIAN_POINT('Ctrl Pts',(-0.89460506092996,107.060812668511,11.0595540521907));
#67553=CARTESIAN_POINT('Ctrl Pts',(0.201537537343257,107.190697367659,10.9818333671775));
#67554=CARTESIAN_POINT('Ctrl Pts',(0.744683028998303,107.261427674696,11.1446008708961));
#67555=CARTESIAN_POINT('Ctrl Pts',(0.824155924584212,107.27191655592,11.1719648240295));
#67556=CARTESIAN_POINT('Ctrl Pts',(0.942260606101615,107.287660128272,11.2163440991875));
#67557=CARTESIAN_POINT('Ctrl Pts',(1.191643104641,107.321827334384,11.3302723880277));
#67558=CARTESIAN_POINT('Ctrl Pts',(1.68560290973175,107.395706991298,11.6631765731265));
#67559=CARTESIAN_POINT('Ctrl Pts',(2.21223251912034,107.502088731704,12.3597762762018));
#67560=CARTESIAN_POINT('Ctrl Pts',(2.42787982712146,107.631132858374,13.3975811084991));
#67561=CARTESIAN_POINT('Ctrl Pts',(2.2190672073106,107.739851026604,14.265222041048));
#67562=CARTESIAN_POINT('Ctrl Pts',(1.90922083577811,107.811107329933,14.7492153605674));
#67563=CARTESIAN_POINT('Ctrl Pts',(1.73745720780343,107.844108613953,14.9503722674611));
#67564=CARTESIAN_POINT('Ctrl Pts',(1.61552354611335,107.866139958883,15.0781315588876));
#67565=CARTESIAN_POINT('Ctrl Pts',(1.44990819593871,107.893736454049,15.225148052992));
#67566=CARTESIAN_POINT('Ctrl Pts',(1.23232670063248,107.926944723774,15.3790623584201));
#67567=CARTESIAN_POINT('Ctrl Pts',(0.920510137608981,107.971346183998,15.5514462974916));
#67568=CARTESIAN_POINT('Ctrl Pts',(0.327550660059198,108.049372351337,15.76169076905));
#67569=CARTESIAN_POINT('Ctrl Pts',(-0.595212551922845,108.161775445127,
15.7702198399133));
#67570=CARTESIAN_POINT('Ctrl Pts',(-1.61239066681261,108.298172360322,15.3016610119433));
#67571=CARTESIAN_POINT('Ctrl Pts',(-2.33940298117849,108.436096905661,14.4332844847565));
#67572=CARTESIAN_POINT('Ctrl Pts',(-2.62878807512887,108.575555925357,13.325428470963));
#67573=CARTESIAN_POINT('Ctrl Pts',(-2.41454707564966,108.716553833851,12.1878943594883));
#67574=CARTESIAN_POINT('Ctrl Pts',(-1.72705825835735,108.859089142338,11.2404857576132));
#67575=CARTESIAN_POINT('Ctrl Pts',(-0.689947399372223,109.003156154794,
10.6727948115623));
#67576=CARTESIAN_POINT('Ctrl Pts',(0.6363577510161,109.164921533284,10.5918456048832));
#67577=CARTESIAN_POINT('Ctrl Pts',(1.98944023319231,109.345011904906,11.2544184786604));
#67578=CARTESIAN_POINT('Ctrl Pts',(2.68844875082447,109.510923958626,12.4538207074574));
#67579=CARTESIAN_POINT('Ctrl Pts',(2.777042909228,109.644937957605,13.5359666031841));
#67580=CARTESIAN_POINT('Ctrl Pts',(2.5372112677193,109.788226044324,14.6715847675353));
#67581=CARTESIAN_POINT('Ctrl Pts',(1.53268170387733,109.975514990703,15.8973704375427));
#67582=CARTESIAN_POINT('Ctrl Pts',(-0.391965390180126,110.20840070075,16.3295413786689));
#67583=CARTESIAN_POINT('Ctrl Pts',(-2.19618012843552,110.444168767888,15.4762171137414));
#67584=CARTESIAN_POINT('Ctrl Pts',(-3.10425034855693,110.682653070405,13.6727436701643));
#67585=CARTESIAN_POINT('Ctrl Pts',(-2.70596752170842,110.9236679908,11.6716072659118));
#67586=CARTESIAN_POINT('Ctrl Pts',(-1.14600188343656,111.167012278533,10.3260453172688));
#67587=CARTESIAN_POINT('Ctrl Pts',(0.968650379207943,111.417041212691,10.2232893908503));
#67588=CARTESIAN_POINT('Ctrl Pts',(2.13392863603529,111.586579386555,11.0744839374344));
#67589=CARTESIAN_POINT('Ctrl Pts',(2.52097553229361,111.673954735715,11.6580819934878));
#67590=CARTESIAN_POINT('Ctrl Pts',(2.49283099999093,100.794479445797,13.1108080195032));
#67591=CARTESIAN_POINT('Ctrl Pts',(2.51515719970202,100.863431279975,13.6628077855728));
#67592=CARTESIAN_POINT('Ctrl Pts',(2.17968843256609,100.999744013118,14.7663369503664));
#67593=CARTESIAN_POINT('Ctrl Pts',(0.795914331805827,101.1994864983,15.7392516655857));
#67594=CARTESIAN_POINT('Ctrl Pts',(-0.853766209202168,101.394579343051,
15.6554435518708));
#67595=CARTESIAN_POINT('Ctrl Pts',(-2.07338251428329,101.585126420958,14.5992895565228));
#67596=CARTESIAN_POINT('Ctrl Pts',(-2.3769033064482,101.771265881478,13.0525813475902));
#67597=CARTESIAN_POINT('Ctrl Pts',(-1.68070836712873,101.953168845295,11.6790615543513));
#67598=CARTESIAN_POINT('Ctrl Pts',(-0.316585819691275,102.131026046402,
11.0391790038355));
#67599=CARTESIAN_POINT('Ctrl Pts',(0.95913378208078,102.285723454486,11.3318051599028));
#67600=CARTESIAN_POINT('Ctrl Pts',(1.7385263897513,102.418771549116,12.0978996555273));
#67601=CARTESIAN_POINT('Ctrl Pts',(2.05900879000914,102.53130516533,12.9642472996834));
#67602=CARTESIAN_POINT('Ctrl Pts',(1.99140764775307,102.623895737268,13.7215605251988));
#67603=CARTESIAN_POINT('Ctrl Pts',(1.7505100490346,102.697301489324,14.2621652806589));
#67604=CARTESIAN_POINT('Ctrl Pts',(1.48692355688233,102.752034803086,14.6158543164599));
#67605=CARTESIAN_POINT('Ctrl Pts',(0.932904994664702,102.842734592139,15.0934843577826));
#67606=CARTESIAN_POINT('Ctrl Pts',(-0.0914144687160896,102.968333415228,
15.3762721980933));
#67607=CARTESIAN_POINT('Ctrl Pts',(-1.33485789371615,103.127446017604,14.853019541222));
#67608=CARTESIAN_POINT('Ctrl Pts',(-1.9848419465324,103.284558264171,13.6933545546193));
#67609=CARTESIAN_POINT('Ctrl Pts',(-1.7859198054212,103.440023723922,12.3916974239502));
#67610=CARTESIAN_POINT('Ctrl Pts',(-0.836554893827291,103.594221052691,
11.4959387949505));
#67611=CARTESIAN_POINT('Ctrl Pts',(0.456174919648817,103.747531635336,11.3738488107031));
#67612=CARTESIAN_POINT('Ctrl Pts',(1.3638147823984,103.874871679777,11.9549038831241));
#67613=CARTESIAN_POINT('Ctrl Pts',(1.76271423183761,103.976693557164,12.6795595279847));
#67614=CARTESIAN_POINT('Ctrl Pts',(1.90810598694439,104.078542102711,13.4945344024168));
#67615=CARTESIAN_POINT('Ctrl Pts',(1.65790918644532,104.17203697728,14.2442552014034));
#67616=CARTESIAN_POINT('Ctrl Pts',(1.18092989180617,104.257276104356,14.7396737469657));
#67617=CARTESIAN_POINT('Ctrl Pts',(0.836952047812147,104.308512974323,14.9680700673282));
#67618=CARTESIAN_POINT('Ctrl Pts',(0.450100297839354,104.359851063443,15.1155674993526));
#67619=CARTESIAN_POINT('Ctrl Pts',(0.0395872801241101,104.411306853854,
15.1750254409463));
#67620=CARTESIAN_POINT('Ctrl Pts',(-0.375108892402885,104.462898554674,
15.1429069972814));
#67621=CARTESIAN_POINT('Ctrl Pts',(-0.840313267844409,104.523254297577,
15.0001497606756));
#67622=CARTESIAN_POINT('Ctrl Pts',(-1.31270319649571,104.592502929932,14.6948548388226));
#67623=CARTESIAN_POINT('Ctrl Pts',(-1.70591154338413,104.670811240362,14.1946222164672));
#67624=CARTESIAN_POINT('Ctrl Pts',(-1.91536791775402,104.749572649424,13.5901594840855));
#67625=CARTESIAN_POINT('Ctrl Pts',(-1.92018868414222,104.85525116503,12.7322430362218));
#67626=CARTESIAN_POINT('Ctrl Pts',(-1.38717216919487,104.98870517941,11.7334940060542));
#67627=CARTESIAN_POINT('Ctrl Pts',(-0.270060311200083,105.13328337949,11.2421101980971));
#67628=CARTESIAN_POINT('Ctrl Pts',(1.07762575349443,105.29829144771,11.4226004121413));
#67629=CARTESIAN_POINT('Ctrl Pts',(1.94172923493356,105.438337213777,12.2957565076881));
#67630=CARTESIAN_POINT('Ctrl Pts',(2.11223738347851,105.571487979555,13.3693963868629));
#67631=CARTESIAN_POINT('Ctrl Pts',(1.96016494784412,105.686803188369,14.291952220544));
#67632=CARTESIAN_POINT('Ctrl Pts',(1.35126081272394,105.803960330811,15.0753078389932));
#67633=CARTESIAN_POINT('Ctrl Pts',(0.573346440079449,105.908193804669,15.4114252004776));
#67634=CARTESIAN_POINT('Ctrl Pts',(0.156498882992677,105.96074884795,15.4795852197261));
#67635=CARTESIAN_POINT('Ctrl Pts',(-0.0852434104585933,105.99090946777,
15.4884288797639));
#67636=CARTESIAN_POINT('Ctrl Pts',(-0.690982562143647,106.066524384947,
15.4613152548541));
#67637=CARTESIAN_POINT('Ctrl Pts',(-1.69935828633558,106.196714378299,15.0178602255304));
#67638=CARTESIAN_POINT('Ctrl Pts',(-2.45487748272796,106.384833620489,13.6157127030245));
#67639=CARTESIAN_POINT('Ctrl Pts',(-2.18187137791978,106.577424396135,12.0086256405781));
#67640=CARTESIAN_POINT('Ctrl Pts',(-0.948900392360805,106.774611627066,
10.8830013639477));
#67641=CARTESIAN_POINT('Ctrl Pts',(0.233539243349673,106.914804888263,10.7911776881976));
#67642=CARTESIAN_POINT('Ctrl Pts',(0.823185956938756,106.991473315452,10.9644105236304));
#67643=CARTESIAN_POINT('Ctrl Pts',(0.909520965425754,107.002848116697,10.9936163144232));
#67644=CARTESIAN_POINT('Ctrl Pts',(1.03788710524578,107.019926828246,11.0410609823112));
#67645=CARTESIAN_POINT('Ctrl Pts',(1.30926972828611,107.057020263259,11.1632603691728));
#67646=CARTESIAN_POINT('Ctrl Pts',(1.84847208639594,107.137376786525,11.5223108351008));
#67647=CARTESIAN_POINT('Ctrl Pts',(2.42773820838176,107.253496861847,12.2791590128213));
#67648=CARTESIAN_POINT('Ctrl Pts',(2.67085942506765,107.394966174649,13.4153688322477));
#67649=CARTESIAN_POINT('Ctrl Pts',(2.44664861704666,107.514626052802,14.3715612584646));
#67650=CARTESIAN_POINT('Ctrl Pts',(2.10770014110726,107.593263004116,14.907531836378));
#67651=CARTESIAN_POINT('Ctrl Pts',(1.9191725122158,107.629721908436,15.1307708123851));
#67652=CARTESIAN_POINT('Ctrl Pts',(1.78519101615885,107.654071661183,15.2726926385123));
#67653=CARTESIAN_POINT('Ctrl Pts',(1.60294350835546,107.684590941821,15.4362604216428));
#67654=CARTESIAN_POINT('Ctrl Pts',(1.36308710077436,107.721344934276,15.6079022783315));
#67655=CARTESIAN_POINT('Ctrl Pts',(1.01879265588027,107.770524578201,15.8006967791856));
#67656=CARTESIAN_POINT('Ctrl Pts',(0.362639306478935,107.857047100334,16.0374277180563));
#67657=CARTESIAN_POINT('Ctrl Pts',(-0.662554204177914,107.981947110009,
16.052736694652));
#67658=CARTESIAN_POINT('Ctrl Pts',(-1.79838602750735,108.133877102516,15.5372596998919));
#67659=CARTESIAN_POINT('Ctrl Pts',(-2.61514735281868,108.287821179317,14.5726210569098));
#67660=CARTESIAN_POINT('Ctrl Pts',(-2.94545234419337,108.443742924981,13.3358893707492));
#67661=CARTESIAN_POINT('Ctrl Pts',(-2.71251103074408,108.601594150237,12.0612145778331));
#67662=CARTESIAN_POINT('Ctrl Pts',(-1.94781643907409,108.761323022852,10.9955134674375));
#67663=CARTESIAN_POINT('Ctrl Pts',(-0.788291568778272,108.922872137781,
10.3528923186892));
#67664=CARTESIAN_POINT('Ctrl Pts',(0.698852336787839,109.104326938504,10.2544096445917));
#67665=CARTESIAN_POINT('Ctrl Pts',(2.22024516295304,109.306336247231,10.9899201228179));
#67666=CARTESIAN_POINT('Ctrl Pts',(3.01043781265651,109.492342925873,12.3306527306649));
#67667=CARTESIAN_POINT('Ctrl Pts',(3.11560486049346,109.642466946645,13.5422795606599));
#67668=CARTESIAN_POINT('Ctrl Pts',(2.85331636502024,109.80287623511,14.8148112250893));
#67669=CARTESIAN_POINT('Ctrl Pts',(1.73643904189676,110.012278026417,16.190299039071));
#67670=CARTESIAN_POINT('Ctrl Pts',(-0.408195232840666,110.272047348849,
16.6815667951534));
#67671=CARTESIAN_POINT('Ctrl Pts',(-2.41858089161053,110.534261758082,15.7408305084419));
#67672=CARTESIAN_POINT('Ctrl Pts',(-3.43282054731318,110.798578297227,13.7460651889675));
#67673=CARTESIAN_POINT('Ctrl Pts',(-3.00145897512342,111.064636929387,11.5354434711421));
#67674=CARTESIAN_POINT('Ctrl Pts',(-1.29243182550077,111.332068403376,10.0506335232888));
#67675=CARTESIAN_POINT('Ctrl Pts',(1.01958119647761,111.605491263496,9.93041943126484));
#67676=CARTESIAN_POINT('Ctrl Pts',(2.2898013042788,111.789872465636,10.8521327613231));
#67677=CARTESIAN_POINT('Ctrl Pts',(2.71197935178886,111.884605002945,11.4830849979595));
#67678=CARTESIAN_POINT('Ctrl Pts',(2.31220144791066,104.895136985459,14.2499282950331));
#67679=CARTESIAN_POINT('Ctrl Pts',(2.27420039961476,104.906599180693,14.3345491847664));
#67680=CARTESIAN_POINT('Ctrl Pts',(2.23140315805251,104.917892748149,14.4168838347965));
#67681=CARTESIAN_POINT('Ctrl Pts',(2.18421017770141,104.92913510024,14.4964371151384));
#67682=CARTESIAN_POINT('Ctrl Pts',(2.15840306163429,104.935282893473,14.5399402108113));
#67683=CARTESIAN_POINT('Ctrl Pts',(2.13128235315898,104.941415302853,14.5826113449346));
#67684=CARTESIAN_POINT('Ctrl Pts',(2.1029200134062,104.947551014578,14.6243685072651));
#67685=CARTESIAN_POINT('Ctrl Pts',(2.07259601784244,104.954111097306,14.6690137663058));
#67686=CARTESIAN_POINT('Ctrl Pts',(2.04084876730712,104.9606764644,14.7126201487188));
#67687=CARTESIAN_POINT('Ctrl Pts',(2.00775362174451,104.967273385227,14.7551051400211));
#67688=CARTESIAN_POINT('Ctrl Pts',(1.92026468474914,104.984712728088,14.867416678892));
#67689=CARTESIAN_POINT('Ctrl Pts',(1.82334397601601,105.002375722057,14.9719076479643));
#67690=CARTESIAN_POINT('Ctrl Pts',(1.71867319953035,105.020116808472,15.0672745496425));
#67691=CARTESIAN_POINT('Ctrl Pts',(1.68902870082,105.025141378185,15.0942840368053));
#67692=CARTESIAN_POINT('Ctrl Pts',(1.65876324929722,105.030172047059,15.1205608831828));
#67693=CARTESIAN_POINT('Ctrl Pts',(1.62791693994719,105.035205272825,15.1460740158455));
#67694=CARTESIAN_POINT('Ctrl Pts',(1.52002140916941,105.052810703653,15.2353149347254));
#67695=CARTESIAN_POINT('Ctrl Pts',(1.40501478746162,105.070451758976,15.3152168018034));
#67696=CARTESIAN_POINT('Ctrl Pts',(1.28446866836278,105.088008386665,15.3845447744751));
#67697=CARTESIAN_POINT('Ctrl Pts',(1.24873987207963,105.093212014777,15.4050929682356));
#67698=CARTESIAN_POINT('Ctrl Pts',(1.2125249485834,105.098407899999,15.4247118951434));
#67699=CARTESIAN_POINT('Ctrl Pts',(1.17586637806379,105.103592191453,15.4433687062027));
#67700=CARTESIAN_POINT('Ctrl Pts',(1.12459789858549,105.110842630742,15.4694610038937));
#67701=CARTESIAN_POINT('Ctrl Pts',(1.07246073447628,105.118070378548,15.4936716081275));
#67702=CARTESIAN_POINT('Ctrl Pts',(1.01958922738601,105.125241585622,15.5159221619009));
#67703=CARTESIAN_POINT('Ctrl Pts',(1.01956424715919,105.125244973806,15.5159326746309));
#67704=CARTESIAN_POINT('Ctrl Pts',(1.01953926676833,105.125248361977,15.5159431869236));
#67705=CARTESIAN_POINT('Ctrl Pts',(1.01951428621352,105.125251750135,15.5159536987788));
#67706=CARTESIAN_POINT('Ctrl Pts',(0.937462525771387,105.136380581006,15.5504812036761));
#67707=CARTESIAN_POINT('Ctrl Pts',(0.853515168959687,105.147382834861,15.580345047422));
#67708=CARTESIAN_POINT('Ctrl Pts',(0.768280266695011,105.158332912142,15.6054595511352));
#67709=CARTESIAN_POINT('Ctrl Pts',(0.736515636026395,105.162413695381,15.6148190143795));
#67710=CARTESIAN_POINT('Ctrl Pts',(0.704572600040203,105.166487200638,15.6235191907505));
#67711=CARTESIAN_POINT('Ctrl Pts',(0.672484017712271,105.170557164629,15.6315568484486));
#67712=CARTESIAN_POINT('Ctrl Pts',(0.543653859675258,105.186897372456,15.6638266664454));
#67713=CARTESIAN_POINT('Ctrl Pts',(0.412461897545337,105.203187832181,15.6854181899435));
#67714=CARTESIAN_POINT('Ctrl Pts',(0.280754984522898,105.219568177955,15.6963245673514));
#67715=CARTESIAN_POINT('Ctrl Pts',(0.235205809239355,105.225233114015,15.7000964004683));
#67716=CARTESIAN_POINT('Ctrl Pts',(0.189594149019697,105.23090875347,15.7025904915425));
#67717=CARTESIAN_POINT('Ctrl Pts',(0.143993589047487,105.236600494221,15.7038067337658));
#67718=CARTESIAN_POINT('Ctrl Pts',(0.0214336593638503,105.251898099046,
15.7070756094429));
#67719=CARTESIAN_POINT('Ctrl Pts',(-0.101053045992834,105.26731534126,15.7011142175678));
#67720=CARTESIAN_POINT('Ctrl Pts',(-0.222054613535675,105.282761645719,
15.6860517097815));
#67721=CARTESIAN_POINT('Ctrl Pts',(-0.231879006231722,105.284015766338,
15.6848287504886));
#67722=CARTESIAN_POINT('Ctrl Pts',(-0.241693629493812,105.285270081524,
15.683545775842));
#67723=CARTESIAN_POINT('Ctrl Pts',(-0.251497738146157,105.286524544392,
15.6822028442612));
#67724=CARTESIAN_POINT('Ctrl Pts',(-0.295773122662273,105.292189702523,
15.6761381611544));
#67725=CARTESIAN_POINT('Ctrl Pts',(-0.339832900064291,105.297857415166,
15.6688511049375));
#67726=CARTESIAN_POINT('Ctrl Pts',(-0.383605439801159,105.303522213605,
15.6603482858131));
#67727=CARTESIAN_POINT('Ctrl Pts',(-0.474632834078136,105.31530247228,15.642666207653));
#67728=CARTESIAN_POINT('Ctrl Pts',(-0.564428333984754,105.327071019503,
15.6197226781248));
#67729=CARTESIAN_POINT('Ctrl Pts',(-0.652325899701623,105.338715235235,
15.5916425343705));
#67730=CARTESIAN_POINT('Ctrl Pts',(-0.683819847232622,105.342887390815,
15.581581339082));
#67731=CARTESIAN_POINT('Ctrl Pts',(-0.715070591587191,105.347043635564,
15.5708608561379));
#67732=CARTESIAN_POINT('Ctrl Pts',(-0.746049078785308,105.35117896166,15.5594872212166));
#67733=CARTESIAN_POINT('Ctrl Pts',(-0.746050762019458,105.351179186355,
15.5594866032235));
#67734=CARTESIAN_POINT('Ctrl Pts',(-0.746052445252847,105.35117941105,15.5594859852285));
#67735=CARTESIAN_POINT('Ctrl Pts',(-0.746054128485389,105.351179635746,
15.5594853672316));
#67736=CARTESIAN_POINT('Ctrl Pts',(-0.793086767511783,105.357458037176,
15.542217386672));
#67737=CARTESIAN_POINT('Ctrl Pts',(-0.839532451831011,105.36369197631,15.5234300496359));
#67738=CARTESIAN_POINT('Ctrl Pts',(-0.88529182882496,105.369902005009,15.503181560758));
#67739=CARTESIAN_POINT('Ctrl Pts',(-0.982641150680751,105.383113331785,
15.4601045612367));
#67740=CARTESIAN_POINT('Ctrl Pts',(-1.07687862515342,105.396215416679,15.4104165331654));
#67741=CARTESIAN_POINT('Ctrl Pts',(-1.16722703977509,105.409290524897,15.3547778569735));
#67742=CARTESIAN_POINT('Ctrl Pts',(-1.19234182397621,105.412925104681,15.3393115828651));
#67743=CARTESIAN_POINT('Ctrl Pts',(-1.21715597278025,105.416557568954,15.3233857783956));
#67744=CARTESIAN_POINT('Ctrl Pts',(-1.24165254843071,105.420189612386,15.3070152965456));
#67745=CARTESIAN_POINT('Ctrl Pts',(-1.33468628106446,105.433983481476,15.2448430544639));
#67746=CARTESIAN_POINT('Ctrl Pts',(-1.42314424358298,105.447773826133,15.1762536441637));
#67747=CARTESIAN_POINT('Ctrl Pts',(-1.50617387261965,105.461660206449,15.1020104225316));
#67748=CARTESIAN_POINT('Ctrl Pts',(-1.51634606224985,105.463361465331,15.0929146799881));
#67749=CARTESIAN_POINT('Ctrl Pts',(-1.52643671658802,105.465064157184,15.0837341006866));
#67750=CARTESIAN_POINT('Ctrl Pts',(-1.53644421913697,105.466768457951,15.0744701109921));
#67751=CARTESIAN_POINT('Ctrl Pts',(-1.61677973838047,105.480449782181,15.0001031629209));
#67752=CARTESIAN_POINT('Ctrl Pts',(-1.6917708061302,105.494237643618,14.9203492168783));
#67753=CARTESIAN_POINT('Ctrl Pts',(-1.76073527650109,105.508034423551,14.8360397261554));
#67754=CARTESIAN_POINT('Ctrl Pts',(-1.77675949669865,105.511240170488,14.8164500180518));
#67755=CARTESIAN_POINT('Ctrl Pts',(-1.79245844556267,105.514446426784,14.7966141639437));
#67756=CARTESIAN_POINT('Ctrl Pts',(-1.80782371518128,105.517652018906,14.7765422221908));
#67757=CARTESIAN_POINT('Ctrl Pts',(-1.86879426141414,105.530372049695,14.6968952467062));
#67758=CARTESIAN_POINT('Ctrl Pts',(-1.92450788267108,105.543079431336,14.6135337054796));
#67759=CARTESIAN_POINT('Ctrl Pts',(-1.97441075903152,105.555687562119,14.5271518064505));
#67760=CARTESIAN_POINT('Ctrl Pts',(-1.98624318030295,105.558677063441,14.5066698804758));
#67761=CARTESIAN_POINT('Ctrl Pts',(-1.99774912755194,105.561661009207,14.4860180562287));
#67762=CARTESIAN_POINT('Ctrl Pts',(-2.00892160078681,105.564638290794,14.4652053898462));
#67763=CARTESIAN_POINT('Ctrl Pts',(-2.01763154882185,105.566959349647,14.448980043958));
#67764=CARTESIAN_POINT('Ctrl Pts',(-2.02613860509512,105.569276332924,14.4326572761255));
#67765=CARTESIAN_POINT('Ctrl Pts',(-2.03444811357903,105.571579479006,14.4162461873535));
#67766=CARTESIAN_POINT('Ctrl Pts',(-2.03446150325956,105.571583190223,14.4162197430414));
#67767=CARTESIAN_POINT('Ctrl Pts',(-2.03447489240929,105.571586901433,14.4161932984712));
#67768=CARTESIAN_POINT('Ctrl Pts',(-2.03448828102828,105.571590612637,14.4161668536429));
#67769=CARTESIAN_POINT('Ctrl Pts',(-2.07648480457982,105.583231668721,14.3332164869913));
#67770=CARTESIAN_POINT('Ctrl Pts',(-2.1132550838095,105.594807933288,14.2477244678497));
#67771=CARTESIAN_POINT('Ctrl Pts',(-2.14472416620306,105.606305480878,14.1604491939523));
#67772=CARTESIAN_POINT('Ctrl Pts',(-2.1564212796263,105.610579139594,14.1280088207297));
#67773=CARTESIAN_POINT('Ctrl Pts',(-2.16738644906337,105.614841927265,14.0953222879995));
#67774=CARTESIAN_POINT('Ctrl Pts',(-2.17761752864817,105.619093145075,14.0624291555584));
#67775=CARTESIAN_POINT('Ctrl Pts',(-2.20744654807204,105.631487698118,13.9665282412546));
#67776=CARTESIAN_POINT('Ctrl Pts',(-2.23099406701571,105.643826754511,13.8688475741174));
#67777=CARTESIAN_POINT('Ctrl Pts',(-2.24813593865129,105.656199546234,13.7702733671563));
#67778=CARTESIAN_POINT('Ctrl Pts',(-2.249751117528,105.657365362445,13.7609852928867));
#67779=CARTESIAN_POINT('Ctrl Pts',(-2.2513094271258,105.658531473181,13.7516893235597));
#67780=CARTESIAN_POINT('Ctrl Pts',(-2.25281076541762,105.659697949965,13.7423862242467));
#67781=CARTESIAN_POINT('Ctrl Pts',(-2.27308663248914,105.675451446922,13.6167460497098));
#67782=CARTESIAN_POINT('Ctrl Pts',(-2.28297344172099,105.691275271019,13.4897921642673));
#67783=CARTESIAN_POINT('Ctrl Pts',(-2.28243769111326,105.707173664902,13.3633101936904));
#67784=CARTESIAN_POINT('Ctrl Pts',(-2.28204297258892,105.718886933132,13.2701235951838));
#67785=CARTESIAN_POINT('Ctrl Pts',(-2.27598992932626,105.73064025116,13.177196942669));
#67786=CARTESIAN_POINT('Ctrl Pts',(-2.2643692664422,105.742346446779,13.0852252627368));
#67787=CARTESIAN_POINT('Ctrl Pts',(-2.26025649785685,105.746489486988,13.0526747757515));
#67788=CARTESIAN_POINT('Ctrl Pts',(-2.255446294118,105.750626683126,13.02024343671));
#67789=CARTESIAN_POINT('Ctrl Pts',(-2.24994239248223,105.754754364393,12.9879605246861));
#67790=CARTESIAN_POINT('Ctrl Pts',(-2.23586841052012,105.765309224481,12.9054101537717));
#67791=CARTESIAN_POINT('Ctrl Pts',(-2.21733181160476,105.77574347324,12.8238073247741));
#67792=CARTESIAN_POINT('Ctrl Pts',(-2.1941782950671,105.786163606793,12.7436717166253));
#67793=CARTESIAN_POINT('Ctrl Pts',(-2.19415222754999,105.786175338359,12.7435814954991));
#67794=CARTESIAN_POINT('Ctrl Pts',(-2.19412615413402,105.786187069927,12.7434912760791));
#67795=CARTESIAN_POINT('Ctrl Pts',(-2.19410007481906,105.786198801498,12.7434010583658));
#67796=CARTESIAN_POINT('Ctrl Pts',(-2.17084996842585,105.796657675197,12.6629705932076));
#67797=CARTESIAN_POINT('Ctrl Pts',(-2.14290692946814,105.807118255861,12.5838976670209));
#67798=CARTESIAN_POINT('Ctrl Pts',(-2.11062188922789,105.817566777419,12.5066962471183));
#67799=CARTESIAN_POINT('Ctrl Pts',(-2.09218205364603,105.823534526511,12.4626020945604));
#67800=CARTESIAN_POINT('Ctrl Pts',(-2.07232676388679,105.82949834534,12.419118288576));
#67801=CARTESIAN_POINT('Ctrl Pts',(-2.05112860949134,105.835455698038,12.3763382896272));
#67802=CARTESIAN_POINT('Ctrl Pts',(-2.01005570878195,105.846998483854,12.2934490618013));
#67803=CARTESIAN_POINT('Ctrl Pts',(-1.96394352830422,105.858516221837,12.2132085252751));
#67804=CARTESIAN_POINT('Ctrl Pts',(-1.91337228647697,105.869950662046,12.1361612675599));
#67805=CARTESIAN_POINT('Ctrl Pts',(-1.88610183507187,105.876116663409,12.0946136720985));
#67806=CARTESIAN_POINT('Ctrl Pts',(-1.85753493633608,105.882258518483,12.0539937768536));
#67807=CARTESIAN_POINT('Ctrl Pts',(-1.82776294759618,105.88836763039,12.0143806935106));
#67808=CARTESIAN_POINT('Ctrl Pts',(-1.77363839518428,105.899473806416,11.9423653362456));
#67809=CARTESIAN_POINT('Ctrl Pts',(-1.71541761572262,105.91056647888,11.8737411495443));
#67810=CARTESIAN_POINT('Ctrl Pts',(-1.65346856418764,105.921727293805,11.8090617901708));
#67811=CARTESIAN_POINT('Ctrl Pts',(-1.62305798741109,105.927206099546,11.7773109146473));
#67812=CARTESIAN_POINT('Ctrl Pts',(-1.59174923650817,105.932701220555,11.7465114045834));
#67813=CARTESIAN_POINT('Ctrl Pts',(-1.55958800014773,105.938221698182,11.7167327888761));
#67814=CARTESIAN_POINT('Ctrl Pts',(-1.5543975039448,105.939112647082,11.7119268233956));
#67815=CARTESIAN_POINT('Ctrl Pts',(-1.54918476732884,105.940004254391,11.7071473973373));
#67816=CARTESIAN_POINT('Ctrl Pts',(-1.54394998157397,105.940896547551,11.7023947818719));
#67817=CARTESIAN_POINT('Ctrl Pts',(-1.47945933338536,105.951889273317,11.6438442955078));
#67818=CARTESIAN_POINT('Ctrl Pts',(-1.41180652123641,105.962801288623,11.5891520869799));
#67819=CARTESIAN_POINT('Ctrl Pts',(-1.34129713765614,105.973662939573,11.5387351859745));
#67820=CARTESIAN_POINT('Ctrl Pts',(-1.30255702088344,105.979630678968,11.5110345235507));
#67821=CARTESIAN_POINT('Ctrl Pts',(-1.26295418549131,105.985583188231,11.4846252713274));
#67822=CARTESIAN_POINT('Ctrl Pts',(-1.22253722997851,105.99152530639,11.459583012843));
#67823=CARTESIAN_POINT('Ctrl Pts',(-1.21331913596365,105.992880554531,11.4538715016685));
#67824=CARTESIAN_POINT('Ctrl Pts',(-1.20405865225382,105.99423566561,11.4482319331064));
#67825=CARTESIAN_POINT('Ctrl Pts',(-1.19475662808346,105.995590629736,11.4426653275844));
#67826=CARTESIAN_POINT('Ctrl Pts',(-1.19467046260739,105.995603180889,11.4426137636231));
#67827=CARTESIAN_POINT('Ctrl Pts',(-1.19458429352618,105.995615732036,11.4425622058978));
#67828=CARTESIAN_POINT('Ctrl Pts',(-1.19449812084045,105.995628283176,11.4425106544095));
#67829=CARTESIAN_POINT('Ctrl Pts',(-1.11827078254639,106.006730872859,11.3969088177554));
#67830=CARTESIAN_POINT('Ctrl Pts',(-1.03922131389124,106.017828090831,11.3561914637407));
#67831=CARTESIAN_POINT('Ctrl Pts',(-0.958079564117482,106.02889315763,11.320463658687));
#67832=CARTESIAN_POINT('Ctrl Pts',(-0.87496204969569,106.040227653765,11.2838658978538));
#67833=CARTESIAN_POINT('Ctrl Pts',(-0.789650234395092,106.051528405288,
11.25250371516));
#67834=CARTESIAN_POINT('Ctrl Pts',(-0.702939310861689,106.062768405711,
11.226437420213));
#67835=CARTESIAN_POINT('Ctrl Pts',(-0.691972596945212,106.064189978265,
11.2231407006315));
#67836=CARTESIAN_POINT('Ctrl Pts',(-0.680983503790746,106.065610581433,
11.2199286246592));
#67837=CARTESIAN_POINT('Ctrl Pts',(-0.669973637772597,106.067030162643,
11.2168012554285));
#67838=CARTESIAN_POINT('Ctrl Pts',(-0.596242281793452,106.076536876656,
11.1958577513349));
#67839=CARTESIAN_POINT('Ctrl Pts',(-0.521594012127566,106.0859592265,11.1786470542945));
#67840=CARTESIAN_POINT('Ctrl Pts',(-0.446378319094508,106.095374568071,
11.1653006883884));
#67841=CARTESIAN_POINT('Ctrl Pts',(-0.373298020979768,106.104522605417,
11.1523332296064));
#67842=CARTESIAN_POINT('Ctrl Pts',(-0.299681807214974,106.113664005035,
11.1430146279782));
#67843=CARTESIAN_POINT('Ctrl Pts',(-0.225891105797696,106.122863974629,
11.1374884678137));
#67844=CARTESIAN_POINT('Ctrl Pts',(-0.14339479848619,106.133149329076,11.131310347828));
#67845=CARTESIAN_POINT('Ctrl Pts',(-0.0606540173709518,106.143508255438,
11.129867656258));
#67846=CARTESIAN_POINT('Ctrl Pts',(0.0217462257417332,106.153870595193,
11.1331027964363));
#67847=CARTESIAN_POINT('Ctrl Pts',(0.0996101080729353,106.163662459547,
11.1361598332199));
#67848=CARTESIAN_POINT('Ctrl Pts',(0.177170135376786,106.173457417067,11.143392939204));
#67849=CARTESIAN_POINT('Ctrl Pts',(0.253974465255779,106.18320170211,11.1547455584407));
#67850=CARTESIAN_POINT('Ctrl Pts',(0.290109610774734,106.187786224344,11.1600867748641));
#67851=CARTESIAN_POINT('Ctrl Pts',(0.326074151320781,106.192359440177,11.1663399787423));
#67852=CARTESIAN_POINT('Ctrl Pts',(0.361817298262778,106.19691615701,11.1734987980242));
#67853=CARTESIAN_POINT('Ctrl Pts',(0.369752224482258,106.197927741467,11.1750880454095));
#67854=CARTESIAN_POINT('Ctrl Pts',(0.377676219185207,106.19893845325,11.1767218047798));
#67855=CARTESIAN_POINT('Ctrl Pts',(0.385589320558754,106.199948416309,11.1784003272889));
#67856=CARTESIAN_POINT('Ctrl Pts',(0.399726235083881,106.201752735597,11.1813990414618));
#67857=CARTESIAN_POINT('Ctrl Pts',(0.413828388402745,106.203554665579,11.1845406098083));
#67858=CARTESIAN_POINT('Ctrl Pts',(0.427896328510184,106.205354908042,11.1878248239191));
#67859=CARTESIAN_POINT('Ctrl Pts',(0.496011645924629,106.21407147108,11.2037266037749));
#67860=CARTESIAN_POINT('Ctrl Pts',(0.563283685263166,106.22274484046,11.2229683911427));
#67861=CARTESIAN_POINT('Ctrl Pts',(0.629330603489222,106.231430431946,11.2454761241329));
#67862=CARTESIAN_POINT('Ctrl Pts',(0.658079077638241,106.235211039868,11.2552731441514));
#67863=CARTESIAN_POINT('Ctrl Pts',(0.686594926239551,106.238993888204,11.265688514558));
#67864=CARTESIAN_POINT('Ctrl Pts',(0.71484446174108,106.24278319748,11.2767139852148));
#67865=CARTESIAN_POINT('Ctrl Pts',(0.781986129750496,106.25178938257,11.302918610436));
#67866=CARTESIAN_POINT('Ctrl Pts',(0.847631645539037,106.260835618038,11.3325764984433));
#67867=CARTESIAN_POINT('Ctrl Pts',(0.911534058805369,106.26986322064,11.3653742253422));
#67868=CARTESIAN_POINT('Ctrl Pts',(0.935902949783958,106.273305855313,11.3778814874359));
#67869=CARTESIAN_POINT('Ctrl Pts',(0.960018798076461,106.276745844659,11.390845656331));
#67870=CARTESIAN_POINT('Ctrl Pts',(0.983869475843969,106.280180173273,11.40425056808));
#67871=CARTESIAN_POINT('Ctrl Pts',(1.03153578423814,106.287043783961,11.4310406938641));
#67872=CARTESIAN_POINT('Ctrl Pts',(1.07817034688009,106.293853057527,11.4595298036398));
#67873=CARTESIAN_POINT('Ctrl Pts',(1.12360386288074,106.300656487286,11.489727866128));
#67874=CARTESIAN_POINT('Ctrl Pts',(1.12365926278775,106.30066478313,11.4897646885005));
#67875=CARTESIAN_POINT('Ctrl Pts',(1.12371466089045,106.300673078963,11.489801513403));
#67876=CARTESIAN_POINT('Ctrl Pts',(1.12377005718842,106.300681374784,11.4898383408353));
#67877=CARTESIAN_POINT('Ctrl Pts',(1.21883652868225,106.314917966604,11.5530384852764));
#67878=CARTESIAN_POINT('Ctrl Pts',(1.30859016660072,106.329121033484,11.6236870039346));
#67879=CARTESIAN_POINT('Ctrl Pts',(1.39204457833629,106.343297376238,11.7008037116028));
#67880=CARTESIAN_POINT('Ctrl Pts',(1.46712375098319,106.356051022965,11.7701812135056));
#67881=CARTESIAN_POINT('Ctrl Pts',(1.53710150328638,106.368782762367,11.8447941298811));
#67882=CARTESIAN_POINT('Ctrl Pts',(1.60122042459052,106.381492453046,11.9239052235944));
#67883=CARTESIAN_POINT('Ctrl Pts',(1.63008654138185,106.387214311868,11.9595207645948));
#67884=CARTESIAN_POINT('Ctrl Pts',(1.65776174908389,106.392931095069,11.9960444184693));
#67885=CARTESIAN_POINT('Ctrl Pts',(1.68433499070737,106.398561331456,12.0332820906798));
#67886=CARTESIAN_POINT('Ctrl Pts',(1.68656466909823,106.399033747151,12.0364065884069));
#67887=CARTESIAN_POINT('Ctrl Pts',(1.68878661000094,106.399505557261,12.0395361349704));
#67888=CARTESIAN_POINT('Ctrl Pts',(1.6910008771225,106.399976715713,12.0426706279985));
#67889=CARTESIAN_POINT('Ctrl Pts',(1.69101435879028,106.399979584383,12.0426897125043));
#67890=CARTESIAN_POINT('Ctrl Pts',(1.69102784015037,106.399982453044,12.0427087972224));
#67891=CARTESIAN_POINT('Ctrl Pts',(1.69104132120274,106.399985321697,12.0427278821528));
#67892=CARTESIAN_POINT('Ctrl Pts',(1.7281760628828,106.407887277476,12.0952989975656));
#67893=CARTESIAN_POINT('Ctrl Pts',(1.76297760691431,106.41572430273,12.1494850633351));
#67894=CARTESIAN_POINT('Ctrl Pts',(1.79522323258318,106.423548761793,12.2050923605098));
#67895=CARTESIAN_POINT('Ctrl Pts',(1.8086376653189,106.426803798022,12.2282254314952));
#67896=CARTESIAN_POINT('Ctrl Pts',(1.82160954051176,106.430056585454,12.2516038884278));
#67897=CARTESIAN_POINT('Ctrl Pts',(1.83412204242246,106.433310576039,12.2752112597003));
#67898=CARTESIAN_POINT('Ctrl Pts',(1.8673563186388,106.441953453592,12.337914458726));
#67899=CARTESIAN_POINT('Ctrl Pts',(1.89734992033821,106.450606035702,12.4022367996933));
#67900=CARTESIAN_POINT('Ctrl Pts',(1.92385711591667,106.459314064612,12.4678661360404));
#67901=CARTESIAN_POINT('Ctrl Pts',(1.93077581557633,106.461586965813,12.4849961891124));
#67902=CARTESIAN_POINT('Ctrl Pts',(1.93745688799951,106.463863609922,12.5022150326731));
#67903=CARTESIAN_POINT('Ctrl Pts',(1.94389576434339,106.466144737025,12.5195165694771));
#67904=CARTESIAN_POINT('Ctrl Pts',(1.95278245464122,106.469293061205,12.543395487326));
#67905=CARTESIAN_POINT('Ctrl Pts',(1.9612083840792,106.472449947364,12.5674327080015));
#67906=CARTESIAN_POINT('Ctrl Pts',(1.9691626354976,106.475617239892,12.5916133493029));
#67907=CARTESIAN_POINT('Ctrl Pts',(1.98702336922665,106.482729181105,12.6459093443581));
#67908=CARTESIAN_POINT('Ctrl Pts',(2.00250551225335,106.48989358909,12.7009289184984));
#67909=CARTESIAN_POINT('Ctrl Pts',(2.01563081321039,106.497072068049,12.756432926117));
#67910=CARTESIAN_POINT('Ctrl Pts',(2.01566999108625,106.497093495181,12.7565986007273));
#67911=CARTESIAN_POINT('Ctrl Pts',(2.01570914797441,106.497114922442,12.7567642796745));
#67912=CARTESIAN_POINT('Ctrl Pts',(2.01574828387691,106.497136349829,12.7569299629524));
#67913=CARTESIAN_POINT('Ctrl Pts',(2.03315128913704,106.506664709131,12.8306062236724));
#67914=CARTESIAN_POINT('Ctrl Pts',(2.04640392038463,106.516212173606,12.9051065380258));
#67915=CARTESIAN_POINT('Ctrl Pts',(2.05560223298109,106.52573997703,12.9799745305667));
#67916=CARTESIAN_POINT('Ctrl Pts',(2.05720372334514,106.527398834045,12.9930095701321));
#67917=CARTESIAN_POINT('Ctrl Pts',(2.05868231642198,106.529057110534,13.0060558820584));
#67918=CARTESIAN_POINT('Ctrl Pts',(2.0600385150921,106.530714621495,13.0191112181));
#67919=CARTESIAN_POINT('Ctrl Pts',(2.06827633959412,106.540782677678,13.0984119647347));
#67920=CARTESIAN_POINT('Ctrl Pts',(2.07199787975471,106.550821575886,13.1780405372738));
#67921=CARTESIAN_POINT('Ctrl Pts',(2.07128305867051,106.560796196022,13.2574603773354));
#67922=CARTESIAN_POINT('Ctrl Pts',(2.07123384373994,106.561482941627,13.2629283776508));
#67923=CARTESIAN_POINT('Ctrl Pts',(2.07116360377587,106.562169384997,13.2683954084505));
#67924=CARTESIAN_POINT('Ctrl Pts',(2.07107236646904,106.562855515764,13.2738613035474));
#67925=CARTESIAN_POINT('Ctrl Pts',(2.06962589105825,106.573733426536,13.3605175533834));
#67926=CARTESIAN_POINT('Ctrl Pts',(2.06290110218543,106.584533555568,13.4468827845573));
#67927=CARTESIAN_POINT('Ctrl Pts',(2.05089935882075,106.595255300884,13.5324077362176));
#67928=CARTESIAN_POINT('Ctrl Pts',(2.050892248048,106.595261653286,13.5324584078973));
#67929=CARTESIAN_POINT('Ctrl Pts',(2.05088513542134,106.59526800566,13.5325090792829));
#67930=CARTESIAN_POINT('Ctrl Pts',(2.05087802094089,106.595274358007,13.532559750374));
#67931=CARTESIAN_POINT('Ctrl Pts',(2.04173028718651,106.603442147344,13.5977121748083));
#67932=CARTESIAN_POINT('Ctrl Pts',(2.02952069130434,106.61156211999,13.66236009784));
#67933=CARTESIAN_POINT('Ctrl Pts',(2.01426416762495,106.61967394276,13.7262096654756));
#67934=CARTESIAN_POINT('Ctrl Pts',(2.00512022408077,106.624535735067,13.7644776781664));
#67935=CARTESIAN_POINT('Ctrl Pts',(1.99488198236352,106.629394475103,13.8024579322979));
#67936=CARTESIAN_POINT('Ctrl Pts',(1.98355572954919,106.634257578248,13.8400787879328));
#67937=CARTESIAN_POINT('Ctrl Pts',(1.97289374012445,106.638835469556,13.8754932512601));
#67938=CARTESIAN_POINT('Ctrl Pts',(1.96126697018555,106.64341757991,13.9105922964225));
#67939=CARTESIAN_POINT('Ctrl Pts',(1.94868017937678,106.64801030961,13.9453213261371));
#67940=CARTESIAN_POINT('Ctrl Pts',(1.92112627961522,106.65806431112,14.0213470755208));
#67941=CARTESIAN_POINT('Ctrl Pts',(1.88896804748103,106.66817039956,14.0956017957832));
#67942=CARTESIAN_POINT('Ctrl Pts',(1.85259474927175,106.678296263071,14.1676207893657));
#67943=CARTESIAN_POINT('Ctrl Pts',(1.84190082487254,106.681273315585,14.1887947194352));
#67944=CARTESIAN_POINT('Ctrl Pts',(1.83084237860993,106.68425212139,14.2097756887979));
#67945=CARTESIAN_POINT('Ctrl Pts',(1.81942881751468,106.687231969321,14.2305525822634));
#67946=CARTESIAN_POINT('Ctrl Pts',(1.78237298048731,106.696906492321,14.298007881426));
#67947=CARTESIAN_POINT('Ctrl Pts',(1.74157631895577,106.706591081943,14.3633098133132));
#67948=CARTESIAN_POINT('Ctrl Pts',(1.69739482677731,106.716253628718,14.4260586078122));
#67949=CARTESIAN_POINT('Ctrl Pts',(1.68101580228434,106.719835741556,14.4493209285561));
#67950=CARTESIAN_POINT('Ctrl Pts',(1.66417143699621,106.723414890053,14.4722328507827));
#67951=CARTESIAN_POINT('Ctrl Pts',(1.64687919716595,106.726989669104,14.4947756854846));
#67952=CARTESIAN_POINT('Ctrl Pts',(1.59212670309234,106.73830850754,14.5661531609034));
#67953=CARTESIAN_POINT('Ctrl Pts',(1.53295032325131,106.749564422212,14.6338678838562));
#67954=CARTESIAN_POINT('Ctrl Pts',(1.46981441294025,106.760746735467,14.6972127195225));
#67955=CARTESIAN_POINT('Ctrl Pts',(1.45922353259919,106.762622538652,14.707838646534));
#67956=CARTESIAN_POINT('Ctrl Pts',(1.44852128540073,106.764496274647,14.7183417158395));
#67957=CARTESIAN_POINT('Ctrl Pts',(1.43770991924172,106.766367897714,14.7287187245816));
#67958=CARTESIAN_POINT('Ctrl Pts',(1.43768550379726,106.766372124424,14.7287421591112));
#67959=CARTESIAN_POINT('Ctrl Pts',(1.43766108779333,106.766376351121,14.7287655930306));
#67960=CARTESIAN_POINT('Ctrl Pts',(1.43763667123001,106.766380577807,14.7287890263397));
#67961=CARTESIAN_POINT('Ctrl Pts',(1.39173214752141,106.774326986706,14.772844976286));
#67962=CARTESIAN_POINT('Ctrl Pts',(1.3438467780252,106.782231140677,14.8147462663298));
#67963=CARTESIAN_POINT('Ctrl Pts',(1.29414526465123,106.790120931987,14.8542823463259));
#67964=CARTESIAN_POINT('Ctrl Pts',(1.24453721148936,106.797995887098,14.8937440814948));
#67965=CARTESIAN_POINT('Ctrl Pts',(1.19311947451598,106.805856534675,14.930848854179));
#67966=CARTESIAN_POINT('Ctrl Pts',(1.14010096732926,106.813724233105,14.9653624716543));
#67967=CARTESIAN_POINT('Ctrl Pts',(1.13168593824299,106.814972984053,14.9708404285101));
#67968=CARTESIAN_POINT('Ctrl Pts',(1.12323068167995,106.816221899543,14.9762530709656));
#67969=CARTESIAN_POINT('Ctrl Pts',(1.11473614598593,106.817471050163,14.9815994224094));
#67970=CARTESIAN_POINT('Ctrl Pts',(1.0403589062157,106.828408478475,15.0284114999091));
#67971=CARTESIAN_POINT('Ctrl Pts',(0.96293079169232,106.839370468413,15.0701586979578));
#67972=CARTESIAN_POINT('Ctrl Pts',(0.883215959514714,106.850336159934,15.1066484684882));
#67973=CARTESIAN_POINT('Ctrl Pts',(0.842924095903791,106.855878768945,15.1250922237749));
#67974=CARTESIAN_POINT('Ctrl Pts',(0.802047275557933,106.861422426754,15.1421931927125));
#67975=CARTESIAN_POINT('Ctrl Pts',(0.760679432527574,106.866965072867,15.1579281494837));
#67976=CARTESIAN_POINT('Ctrl Pts',(0.702198564405304,106.874800597579,15.1801723339623));
#67977=CARTESIAN_POINT('Ctrl Pts',(0.642742727877497,106.882633065654,15.1996849416091));
#67978=CARTESIAN_POINT('Ctrl Pts',(0.582623353521924,106.890440017239,15.2164953412303));
#67979=CARTESIAN_POINT('Ctrl Pts',(0.555253859136353,106.893994151324,15.2241483173796));
#67980=CARTESIAN_POINT('Ctrl Pts',(0.527746220400075,106.897543084433,15.2312415876166));
#67981=CARTESIAN_POINT('Ctrl Pts',(0.500126557908841,106.901085136587,15.2377793389447));
#67982=CARTESIAN_POINT('Ctrl Pts',(0.413926382623553,106.912139779874,15.2581834735218));
#67983=CARTESIAN_POINT('Ctrl Pts',(0.3265326132082,106.923170028877,15.2729182309128));
#67984=CARTESIAN_POINT('Ctrl Pts',(0.238655941651049,106.934183156336,15.2816536572493));
#67985=CARTESIAN_POINT('Ctrl Pts',(0.238567491824711,106.934194241294,15.2816624496504));
#67986=CARTESIAN_POINT('Ctrl Pts',(0.238479041466734,106.93420532624,15.2816712359778));
#67987=CARTESIAN_POINT('Ctrl Pts',(0.238390590577828,106.934216411174,15.2816800162313));
#67988=CARTESIAN_POINT('Ctrl Pts',(0.16178467325091,106.943816897281,15.2892844550426));
#67989=CARTESIAN_POINT('Ctrl Pts',(0.0847827294383409,106.953408057825,
15.2923311531031));
#67990=CARTESIAN_POINT('Ctrl Pts',(0.00793992072725377,106.962985676773,
15.2909356875329));
#67991=CARTESIAN_POINT('Ctrl Pts',(-0.0439573489995137,106.969454106055,
15.289993233004));
#67992=CARTESIAN_POINT('Ctrl Pts',(-0.0957784160519001,106.975915923052,
15.2870246406397));
#67993=CARTESIAN_POINT('Ctrl Pts',(-0.147337536445514,106.982367944768,
15.2820732147274));
#67994=CARTESIAN_POINT('Ctrl Pts',(-0.219145308937171,106.991353848794,
15.2751772308025));
#67995=CARTESIAN_POINT('Ctrl Pts',(-0.290452604006382,107.000321661448,
15.2644381955568));
#67996=CARTESIAN_POINT('Ctrl Pts',(-0.360897333028724,107.009280080517,
15.2499534424375));
#67997=CARTESIAN_POINT('Ctrl Pts',(-0.424928366238981,107.017422873269,
15.2367874650691));
#67998=CARTESIAN_POINT('Ctrl Pts',(-0.488246064484556,107.025557783316,
15.2205264383419));
#67999=CARTESIAN_POINT('Ctrl Pts',(-0.550570205952548,107.033690822623,
15.2012250032835));
#68000=CARTESIAN_POINT('Ctrl Pts',(-0.634697004798602,107.044669017359,
15.1751714082183));
#68001=CARTESIAN_POINT('Ctrl Pts',(-0.71700725972373,107.055643099448,15.1435756551976));
#68002=CARTESIAN_POINT('Ctrl Pts',(-0.796660794646603,107.066609435735,
15.1066058385688));
#68003=CARTESIAN_POINT('Ctrl Pts',(-0.842119199686749,107.072867942118,
15.085507102647));
#68004=CARTESIAN_POINT('Ctrl Pts',(-0.886715293108071,107.079124367692,
15.0626565498559));
#68005=CARTESIAN_POINT('Ctrl Pts',(-0.930281051229547,107.085376307396,
15.0380949762599));
#68006=CARTESIAN_POINT('Ctrl Pts',(-0.963052477241712,107.090079197654,
15.0196190486839));
#68007=CARTESIAN_POINT('Ctrl Pts',(-0.995239509619407,107.094779353001,
15.000175776424));
#68008=CARTESIAN_POINT('Ctrl Pts',(-1.02676916585278,107.099475324812,14.9797868477451));
#68009=CARTESIAN_POINT('Ctrl Pts',(-1.02693329067948,107.099499769276,14.9796807149867));
#68010=CARTESIAN_POINT('Ctrl Pts',(-1.02709739887614,107.099524213803,14.9795745558479));
#68011=CARTESIAN_POINT('Ctrl Pts',(-1.02726149043209,107.099548658391,14.9794683703343));
#68012=CARTESIAN_POINT('Ctrl Pts',(-1.07822398336964,107.107140500326,14.9464899610819));
#68013=CARTESIAN_POINT('Ctrl Pts',(-1.12757710569181,107.114737912216,14.9109662585429));
#68014=CARTESIAN_POINT('Ctrl Pts',(-1.17516702871453,107.122326054767,14.8732558902454));
#68015=CARTESIAN_POINT('Ctrl Pts',(-1.20436144204537,107.126981060617,14.8501221676208));
#68016=CARTESIAN_POINT('Ctrl Pts',(-1.23289331627348,107.131632666299,14.8261658916509));
#68017=CARTESIAN_POINT('Ctrl Pts',(-1.26073663596602,107.136278282374,14.8014714572102));
#68018=CARTESIAN_POINT('Ctrl Pts',(-1.28430373824257,107.140210417996,14.780569629822));
#68019=CARTESIAN_POINT('Ctrl Pts',(-1.30751037372541,107.144131041719,14.759331799902));
#68020=CARTESIAN_POINT('Ctrl Pts',(-1.33017835559884,107.14805176292,14.7375275760134));
#68021=CARTESIAN_POINT('Ctrl Pts',(-1.39939450961625,107.160023593676,14.670948886859));
#68022=CARTESIAN_POINT('Ctrl Pts',(-1.46355113224768,107.171991306496,14.5991087040727));
#68023=CARTESIAN_POINT('Ctrl Pts',(-1.52211657808587,107.183947453271,14.5229809858679));
#68024=CARTESIAN_POINT('Ctrl Pts',(-1.58262960160205,107.196301198395,14.4443216614826));
#68025=CARTESIAN_POINT('Ctrl Pts',(-1.6371726339279,107.208642419216,14.3610858047828));
#68026=CARTESIAN_POINT('Ctrl Pts',(-1.68519607156579,107.220962124354,14.2743884519512));
#68027=CARTESIAN_POINT('Ctrl Pts',(-1.7329289728637,107.233207296676,14.1882156082513));
#68028=CARTESIAN_POINT('Ctrl Pts',(-1.77422038552428,107.245431073975,14.0986242296114));
#68029=CARTESIAN_POINT('Ctrl Pts',(-1.80857598691776,107.257626277559,14.0067323324837));
#68030=CARTESIAN_POINT('Ctrl Pts',(-1.84162758138612,107.269358597965,13.9183282994992));
#68031=CARTESIAN_POINT('Ctrl Pts',(-1.86825969015914,107.28106441381,13.8277961289283));
#68032=CARTESIAN_POINT('Ctrl Pts',(-1.88807920419422,107.292740261752,13.7361361881972));
#68033=CARTESIAN_POINT('Ctrl Pts',(-1.89639863050633,107.297641308084,13.6976610711315));
#68034=CARTESIAN_POINT('Ctrl Pts',(-1.90351700382206,107.302536603697,13.6589911103909));
#68035=CARTESIAN_POINT('Ctrl Pts',(-1.90961068327992,107.307438130595,13.6202521027464));
#68036=CARTESIAN_POINT('Ctrl Pts',(-1.91045184120514,107.308114726439,13.614904656508));
#68037=CARTESIAN_POINT('Ctrl Pts',(-1.91127349823806,107.308791451028,13.6095558177041));
#68038=CARTESIAN_POINT('Ctrl Pts',(-1.91207613960894,107.309468345496,13.6042058428203));
#68039=CARTESIAN_POINT('Ctrl Pts',(-1.92274394036054,107.31846486072,13.5331000312374));
#68040=CARTESIAN_POINT('Ctrl Pts',(-1.92945891623361,107.32746221094,13.4615841732368));
#68041=CARTESIAN_POINT('Ctrl Pts',(-1.93189267743231,107.336451252017,13.3900567083924));
#68042=CARTESIAN_POINT('Ctrl Pts',(-1.93252994110109,107.338804970738,13.3713277325629));
#68043=CARTESIAN_POINT('Ctrl Pts',(-1.93287369565044,107.341158084246,13.3525982357956));
#68044=CARTESIAN_POINT('Ctrl Pts',(-1.93291812964871,107.34351035279,13.3338759519325));
#68045=CARTESIAN_POINT('Ctrl Pts',(-1.93291846211627,107.343527953119,13.3337358665865));
#68046=CARTESIAN_POINT('Ctrl Pts',(-1.93291877782965,107.343545553549,13.3335957804611));
#68047=CARTESIAN_POINT('Ctrl Pts',(-1.93291907678648,107.34356315408,13.3334556935608));
#68048=CARTESIAN_POINT('Ctrl Pts',(-1.93305037040335,107.351292823189,13.2719333813634));
#68049=CARTESIAN_POINT('Ctrl Pts',(-1.92994528317225,107.359041997369,13.2102611881824));
#68050=CARTESIAN_POINT('Ctrl Pts',(-1.92371562688559,107.366795633922,13.1488127563905));
#68051=CARTESIAN_POINT('Ctrl Pts',(-1.92038329339603,107.370943166556,13.1159430991063));
#68052=CARTESIAN_POINT('Ctrl Pts',(-1.91615784140607,107.375091977645,13.0831375621709));
#68053=CARTESIAN_POINT('Ctrl Pts',(-1.91106244729389,107.379239775609,13.050453402942));
#68054=CARTESIAN_POINT('Ctrl Pts',(-1.90307811136313,107.385739255647,12.999238266065));
#68055=CARTESIAN_POINT('Ctrl Pts',(-1.893292919909,107.392265624772,12.9483253686079));
#68056=CARTESIAN_POINT('Ctrl Pts',(-1.88163058522903,107.398805824831,12.8978460125036));
#68057=CARTESIAN_POINT('Ctrl Pts',(-1.87123302293243,107.404636744576,12.8528411087524));
#68058=CARTESIAN_POINT('Ctrl Pts',(-1.85934308089877,107.410478566673,12.8081815907255));
#68059=CARTESIAN_POINT('Ctrl Pts',(-1.84591326539498,107.416317549966,12.7639945706258));
#68060=CARTESIAN_POINT('Ctrl Pts',(-1.82674217848543,107.424652709607,12.7009175162639));
#68061=CARTESIAN_POINT('Ctrl Pts',(-1.80438503606112,107.432976658583,12.6388114571308));
#68062=CARTESIAN_POINT('Ctrl Pts',(-1.77891111747281,107.441269651585,12.5780305378066));
#68063=CARTESIAN_POINT('Ctrl Pts',(-1.76555453484415,107.44561786546,12.5461616532302));
#68064=CARTESIAN_POINT('Ctrl Pts',(-1.75134133701015,107.449957452586,12.5146579041327));
#68065=CARTESIAN_POINT('Ctrl Pts',(-1.73628373074468,107.454284801398,12.4835755667181));
#68066=CARTESIAN_POINT('Ctrl Pts',(-1.71707431732516,107.459805322448,12.4439229513611));
#68067=CARTESIAN_POINT('Ctrl Pts',(-1.69648973490362,107.465306489921,12.4049524071892));
#68068=CARTESIAN_POINT('Ctrl Pts',(-1.67455499375723,107.470782377846,12.3667726720596));
#68069=CARTESIAN_POINT('Ctrl Pts',(-1.64128786324746,107.479087334675,12.308867715584));
#68070=CARTESIAN_POINT('Ctrl Pts',(-1.60490998011633,107.487334292046,12.2527786019574));
#68071=CARTESIAN_POINT('Ctrl Pts',(-1.56572551425112,107.495541702607,12.1987701848449));
#68072=CARTESIAN_POINT('Ctrl Pts',(-1.54602678476878,107.4996677142,12.1716191908227));
#68073=CARTESIAN_POINT('Ctrl Pts',(-1.52561823215195,107.50378383509,12.1449933966371));
#68074=CARTESIAN_POINT('Ctrl Pts',(-1.50453495600743,107.507893035257,12.1189230461787));
#68075=CARTESIAN_POINT('Ctrl Pts',(-1.46636396394904,107.515332687704,12.071723022165));
#68076=CARTESIAN_POINT('Ctrl Pts',(-1.42598401004741,107.522749727454,12.0263448236212));
#68077=CARTESIAN_POINT('Ctrl Pts',(-1.38366043994489,107.530166144122,11.9829630156392));
#68078=CARTESIAN_POINT('Ctrl Pts',(-1.35422042767174,107.535324957455,11.9527868996754));
#68079=CARTESIAN_POINT('Ctrl Pts',(-1.32383955943577,107.540483607884,11.9235757200112));
#68080=CARTESIAN_POINT('Ctrl Pts',(-1.29259847812592,107.545651394958,11.8953762726244));
#68081=CARTESIAN_POINT('Ctrl Pts',(-1.25244841288815,107.552292874044,11.8591352206258));
#68082=CARTESIAN_POINT('Ctrl Pts',(-1.21101867279548,107.558981745805,11.8244489763536));
#68083=CARTESIAN_POINT('Ctrl Pts',(-1.16828471652994,107.565690386974,11.7915833615631));
#68084=CARTESIAN_POINT('Ctrl Pts',(-1.13463751899251,107.57097253247,11.7657061451834));
#68085=CARTESIAN_POINT('Ctrl Pts',(-1.10018238305018,107.576266803463,11.7409585249536));
#68086=CARTESIAN_POINT('Ctrl Pts',(-1.0649253297805,107.581556823008,11.7174838721533));
#68087=CARTESIAN_POINT('Ctrl Pts',(-1.05993500493425,107.582305578605,11.7141612421471));
#68088=CARTESIAN_POINT('Ctrl Pts',(-1.05492874948117,107.583054228879,11.7108642014886));
#68089=CARTESIAN_POINT('Ctrl Pts',(-1.0499066660986,107.583802780861,11.7075929425082));
#68090=CARTESIAN_POINT('Ctrl Pts',(-0.991219818328679,107.592550177683,
11.6693658038541));
#68091=CARTESIAN_POINT('Ctrl Pts',(-0.930228297682015,107.601305122401,
11.6345713200927));
#68092=CARTESIAN_POINT('Ctrl Pts',(-0.867464676749782,107.61005406824,11.603355212156));
#68093=CARTESIAN_POINT('Ctrl Pts',(-0.830320208917726,107.615231827783,
11.5848810435234));
#68094=CARTESIAN_POINT('Ctrl Pts',(-0.792558630281349,107.62040709212,11.5676605321247));
#68095=CARTESIAN_POINT('Ctrl Pts',(-0.754283093784006,107.625578556984,
11.5517120295663));
#68096=CARTESIAN_POINT('Ctrl Pts',(-0.668001388472514,107.637236206968,
11.5157605021986));
#68097=CARTESIAN_POINT('Ctrl Pts',(-0.579101139665477,107.648875775813,
11.486264133236));
#68098=CARTESIAN_POINT('Ctrl Pts',(-0.488564333837079,107.660508081308,
11.4633640719517));
#68099=CARTESIAN_POINT('Ctrl Pts',(-0.40313283342547,107.671484449455,11.4417553286662));
#68100=CARTESIAN_POINT('Ctrl Pts',(-0.316235351384715,107.682455293058,
11.4260209618426));
#68101=CARTESIAN_POINT('Ctrl Pts',(-0.228746918708682,107.693422325914,
11.4163187295061));
#68102=CARTESIAN_POINT('Ctrl Pts',(-0.203667267928375,107.696566162713,
11.4135374635565));
#68103=CARTESIAN_POINT('Ctrl Pts',(-0.178539198357052,107.699709669414,
11.4112519413924));
#68104=CARTESIAN_POINT('Ctrl Pts',(-0.153383473816096,107.70285287079,11.4094659507271));
#68105=CARTESIAN_POINT('Ctrl Pts',(-0.153323789078853,107.702860328383,
11.4094617132669));
#68106=CARTESIAN_POINT('Ctrl Pts',(-0.153264104180559,107.702867785979,
11.4094574786036));
#68107=CARTESIAN_POINT('Ctrl Pts',(-0.153204419121579,107.702875243578,
11.4094532467374));
#68108=CARTESIAN_POINT('Ctrl Pts',(-0.0503082794465152,107.7157320319,11.4021575733437));
#68109=CARTESIAN_POINT('Ctrl Pts',(0.0530647704723847,107.728598333694,
11.4031794466173));
#68110=CARTESIAN_POINT('Ctrl Pts',(0.155564843474227,107.741471740227,11.4123192936204));
#68111=CARTESIAN_POINT('Ctrl Pts',(0.195744104762457,107.746518019216,11.4159020452236));
#68112=CARTESIAN_POINT('Ctrl Pts',(0.235789349262896,107.751565405274,11.4207316333851));
#68113=CARTESIAN_POINT('Ctrl Pts',(0.275620013322703,107.756613811943,11.4267939874474));
#68114=CARTESIAN_POINT('Ctrl Pts',(0.353137764528065,107.766438933904,11.4385924363313));
#68115=CARTESIAN_POINT('Ctrl Pts',(0.429860535829397,107.776236805584,11.4551752460502));
#68116=CARTESIAN_POINT('Ctrl Pts',(0.505205833897759,107.785978354576,11.4765543596553));
#68117=CARTESIAN_POINT('Ctrl Pts',(0.53888822020398,107.790333219773,11.4861116854845));
#68118=CARTESIAN_POINT('Ctrl Pts',(0.572295512101532,107.794676919606,11.4966276750502));
#68119=CARTESIAN_POINT('Ctrl Pts',(0.605387977521011,107.799028791502,11.5080363533329));
#68120=CARTESIAN_POINT('Ctrl Pts',(0.6219342621262,107.801204734275,11.5137407103652));
#68121=CARTESIAN_POINT('Ctrl Pts',(0.638401807431331,107.803382708495,11.5196682310407));
#68122=CARTESIAN_POINT('Ctrl Pts',(0.654782616705315,107.805560803768,11.5258234700986));
#68123=CARTESIAN_POINT('Ctrl Pts',(0.671163226945381,107.807738872576,11.5319786343677));
#68124=CARTESIAN_POINT('Ctrl Pts',(0.68745698972609,107.809917050831,11.538361487542));
#68125=CARTESIAN_POINT('Ctrl Pts',(0.703660466053377,107.812100528228,11.5449548006635));
#68126=CARTESIAN_POINT('Ctrl Pts',(0.726758869241025,107.815213122109,11.554353709993));
#68127=CARTESIAN_POINT('Ctrl Pts',(0.749668765831185,107.818327248075,11.5642092253437));
#68128=CARTESIAN_POINT('Ctrl Pts',(0.772370087930443,107.821440878198,11.5745244080491));
#68129=CARTESIAN_POINT('Ctrl Pts',(0.77240211744071,107.821445271248,11.574538961838));
#68130=CARTESIAN_POINT('Ctrl Pts',(0.772434146546288,107.821449664299,11.5745535165468));
#68131=CARTESIAN_POINT('Ctrl Pts',(0.772466175247419,107.82145405735,11.5745680721755));
#68132=CARTESIAN_POINT('Ctrl Pts',(0.813409826174717,107.827069881514,11.5931751514367));
#68133=CARTESIAN_POINT('Ctrl Pts',(0.853691310046216,107.832686373679,11.6132853975448));
#68134=CARTESIAN_POINT('Ctrl Pts',(0.893223189291165,107.838316104378,11.6347820257333));
#68135=CARTESIAN_POINT('Ctrl Pts',(0.963932215868106,107.848385769298,11.6732321496062));
#68136=CARTESIAN_POINT('Ctrl Pts',(1.03222649571,107.858477387079,11.7161771247585));
#68137=CARTESIAN_POINT('Ctrl Pts',(1.09753010505694,107.86855227438,11.7632718359109));
#68138=CARTESIAN_POINT('Ctrl Pts',(1.12048666829478,107.872093958978,11.7798273176912));
#68139=CARTESIAN_POINT('Ctrl Pts',(1.14307328065565,107.875633516843,11.7968953253573));
#68140=CARTESIAN_POINT('Ctrl Pts',(1.16526381138637,107.879169075699,11.8144598343174));
#68141=CARTESIAN_POINT('Ctrl Pts',(1.18956780137538,107.883041366457,11.8336972133196));
#68142=CARTESIAN_POINT('Ctrl Pts',(1.21339758945319,107.886909049586,11.8535306653475));
#68143=CARTESIAN_POINT('Ctrl Pts',(1.2367205136842,107.890770253688,11.8739392041113));
#68144=CARTESIAN_POINT('Ctrl Pts',(1.29270144708995,107.900038122827,11.9229248732377));
#68145=CARTESIAN_POINT('Ctrl Pts',(1.34576573083898,107.909268748033,11.9752294206335));
#68146=CARTESIAN_POINT('Ctrl Pts',(1.39556867414692,107.918505973281,12.030421414051));
#68147=CARTESIAN_POINT('Ctrl Pts',(1.41884597613203,107.922823342242,12.0562174938127));
#68148=CARTESIAN_POINT('Ctrl Pts',(1.44141140271464,107.927142246835,12.0826448212329));
#68149=CARTESIAN_POINT('Ctrl Pts',(1.4632323950436,107.931467654987,12.109662182857));
#68150=CARTESIAN_POINT('Ctrl Pts',(1.47718970054447,107.934234304738,12.1269432287567));
#68151=CARTESIAN_POINT('Ctrl Pts',(1.49084195922481,107.937003551222,12.1444649320569));
#68152=CARTESIAN_POINT('Ctrl Pts',(1.50418026134739,107.939776614462,12.1622156871461));
#68153=CARTESIAN_POINT('Ctrl Pts',(1.50419212819256,107.939779081606,12.1622314796706));
#68154=CARTESIAN_POINT('Ctrl Pts',(1.50420399479058,107.939781548754,12.1622472723778));
#68155=CARTESIAN_POINT('Ctrl Pts',(1.50421586114142,107.939784015905,12.1622630652677));
#68156=CARTESIAN_POINT('Ctrl Pts',(1.5489167875955,107.949077852235,12.2217553910282));
#68157=CARTESIAN_POINT('Ctrl Pts',(1.59011255430665,107.958419810004,12.2838443321159));
#68158=CARTESIAN_POINT('Ctrl Pts',(1.62752645131653,107.96776315549,12.3481295844515));
#68159=CARTESIAN_POINT('Ctrl Pts',(1.66449871912309,107.976996213233,12.4116560212923));
#68160=CARTESIAN_POINT('Ctrl Pts',(1.69777693953788,107.986230607277,12.4773274505966));
#68161=CARTESIAN_POINT('Ctrl Pts',(1.72707490853383,107.995415020297,12.5447116847064));
#68162=CARTESIAN_POINT('Ctrl Pts',(1.7585214679531,108.005272979729,12.6170375965179));
#68163=CARTESIAN_POINT('Ctrl Pts',(1.78539617584054,108.015077634329,12.6913676067518));
#68164=CARTESIAN_POINT('Ctrl Pts',(1.8075555410359,108.024873771686,12.76706296488));
#68165=CARTESIAN_POINT('Ctrl Pts',(1.82900486110536,108.03435601469,12.8403328419703));
#68166=CARTESIAN_POINT('Ctrl Pts',(1.84603718829411,108.043830316501,12.9148818596889));
#68167=CARTESIAN_POINT('Ctrl Pts',(1.85854169112516,108.053343116012,12.9901727679075));
#68168=CARTESIAN_POINT('Ctrl Pts',(1.86057427055602,108.054889400648,13.0024111394321));
#68169=CARTESIAN_POINT('Ctrl Pts',(1.86248710821986,108.056436628437,13.0146687422829));
#68170=CARTESIAN_POINT('Ctrl Pts',(1.86427970516388,108.057984960076,13.0269431330409));
#68171=CARTESIAN_POINT('Ctrl Pts',(1.86428039852866,108.05798555896,13.026947880695));
#68172=CARTESIAN_POINT('Ctrl Pts',(1.86428109187545,108.057986157845,13.0269526283516));
#68173=CARTESIAN_POINT('Ctrl Pts',(1.86428178520429,108.05798675673,13.0269573760111));
#68174=CARTESIAN_POINT('Ctrl Pts',(1.87524500381698,108.067456586847,13.1020294419768));
#68175=CARTESIAN_POINT('Ctrl Pts',(1.88171525716222,108.076972609446,13.1777724884613));
#68176=CARTESIAN_POINT('Ctrl Pts',(1.88361208860195,108.08648032582,13.2536471959942));
#68177=CARTESIAN_POINT('Ctrl Pts',(1.88450005735865,108.090931198424,13.2891666250286));
#68178=CARTESIAN_POINT('Ctrl Pts',(1.88438573730388,108.095380157836,13.3247141603359));
#68179=CARTESIAN_POINT('Ctrl Pts',(1.88326117130547,108.099821126105,13.3602305922588));
#68180=CARTESIAN_POINT('Ctrl Pts',(1.88179566098341,108.105608500832,13.4065148456144));
#68181=CARTESIAN_POINT('Ctrl Pts',(1.87861456796639,108.111382822336,13.452750260111));
#68182=CARTESIAN_POINT('Ctrl Pts',(1.87374192211305,108.117154216983,13.4988132921293));
#68183=CARTESIAN_POINT('Ctrl Pts',(1.87374121925935,108.117155049476,13.498819936481));
#68184=CARTESIAN_POINT('Ctrl Pts',(1.87374051637044,108.11715588197,13.4988265808292));
#68185=CARTESIAN_POINT('Ctrl Pts',(1.87373981344633,108.117156714463,13.4988332251737));
#68186=CARTESIAN_POINT('Ctrl Pts',(1.86375552053862,108.128981402164,13.5932091071049));
#68187=CARTESIAN_POINT('Ctrl Pts',(1.84667352779593,108.140789842786,13.6868306513806));
#68188=CARTESIAN_POINT('Ctrl Pts',(1.82273984890812,108.152631737893,13.7786480261527));
#68189=CARTESIAN_POINT('Ctrl Pts',(1.81189394076528,108.157998071551,13.8202564565725));
#68190=CARTESIAN_POINT('Ctrl Pts',(1.79964082232468,108.16337136398,13.8614950815876));
#68191=CARTESIAN_POINT('Ctrl Pts',(1.78600211636631,108.168756676845,13.902269462313));
#68192=CARTESIAN_POINT('Ctrl Pts',(1.77969626305583,108.171246575304,13.9211214900981));
#68193=CARTESIAN_POINT('Ctrl Pts',(1.77309559706695,108.17373968257,13.9398740648559));
#68194=CARTESIAN_POINT('Ctrl Pts',(1.76619994546931,108.176235268159,13.958517662311));
#68195=CARTESIAN_POINT('Ctrl Pts',(1.75527788476314,108.180188039978,13.9880473594402));
#68196=CARTESIAN_POINT('Ctrl Pts',(1.74361576800181,108.184147036455,14.0173037180304));
#68197=CARTESIAN_POINT('Ctrl Pts',(1.73122901172699,108.188109234452,14.0462548285743));
#68198=CARTESIAN_POINT('Ctrl Pts',(1.71413999127076,108.193575563255,14.086196368501));
#68199=CARTESIAN_POINT('Ctrl Pts',(1.6956690756824,108.199045451061,14.1255533276468));
#68200=CARTESIAN_POINT('Ctrl Pts',(1.67584846591692,108.204503272049,14.1642316908938));
#68201=CARTESIAN_POINT('Ctrl Pts',(1.62818322275471,108.217628416411,14.2572466692973));
#68202=CARTESIAN_POINT('Ctrl Pts',(1.57270897662728,108.230685549007,14.3463428601481));
#68203=CARTESIAN_POINT('Ctrl Pts',(1.51031547041863,108.243711872239,14.4303274257314));
#68204=CARTESIAN_POINT('Ctrl Pts',(1.48941061563552,108.248076323159,14.4584663339965));
#68205=CARTESIAN_POINT('Ctrl Pts',(1.46772898050822,108.252437365451,14.486031857037));
#68206=CARTESIAN_POINT('Ctrl Pts',(1.44530377793378,108.256796548177,14.5129803988635));
#68207=CARTESIAN_POINT('Ctrl Pts',(1.42296634031131,108.26113867048,14.5398234728589));
#68208=CARTESIAN_POINT('Ctrl Pts',(1.3998915975729,108.265478636989,14.5660535371844));
#68209=CARTESIAN_POINT('Ctrl Pts',(1.37610597632969,108.269816897345,14.5916302585667));
#68210=CARTESIAN_POINT('Ctrl Pts',(1.35231945319316,108.274155322197,14.6172079497565));
#68211=CARTESIAN_POINT('Ctrl Pts',(1.32782193232556,108.27849211975,14.6421322449387));
#68212=CARTESIAN_POINT('Ctrl Pts',(1.30265205719123,108.282831974951,14.6663616227905));
#68213=CARTESIAN_POINT('Ctrl Pts',(1.27998541948397,108.286740215458,14.6881812991579));
#68214=CARTESIAN_POINT('Ctrl Pts',(1.25677702100915,108.290653156273,14.7094391604563));
#68215=CARTESIAN_POINT('Ctrl Pts',(1.23304717436089,108.294570971721,14.7301047171995));
#68216=CARTESIAN_POINT('Ctrl Pts',(1.20407315493938,108.29935460402,14.7553372545736));
#68217=CARTESIAN_POINT('Ctrl Pts',(1.1743217523591,108.304145503826,14.7796867837824));
#68218=CARTESIAN_POINT('Ctrl Pts',(1.14385301557154,108.308943972914,14.8031180912194));
#68219=CARTESIAN_POINT('Ctrl Pts',(1.08843558416345,108.317671569118,14.8457356398806));
#68220=CARTESIAN_POINT('Ctrl Pts',(1.03063671059079,108.326414274237,14.8853033104582));
#68221=CARTESIAN_POINT('Ctrl Pts',(0.97081961488415,108.335150275283,14.9215703550054));
#68222=CARTESIAN_POINT('Ctrl Pts',(0.928186359654004,108.341376658525,14.9474188544745));
#68223=CARTESIAN_POINT('Ctrl Pts',(0.884526485399702,108.347600678116,14.9715929539637));
#68224=CARTESIAN_POINT('Ctrl Pts',(0.839979531862484,108.353827252736,14.9940174782538));
#68225=CARTESIAN_POINT('Ctrl Pts',(0.822017863373078,108.356337854702,15.0030592160012));
#68226=CARTESIAN_POINT('Ctrl Pts',(0.803911953720946,108.35884887504,15.011816520812));
#68227=CARTESIAN_POINT('Ctrl Pts',(0.7856708619492,108.361360648253,15.0202863087384));
#68228=CARTESIAN_POINT('Ctrl Pts',(0.702703679152465,108.372785115053,15.0588100140042));
#68229=CARTESIAN_POINT('Ctrl Pts',(0.616939738427914,108.384218522087,15.0913759547903));
#68230=CARTESIAN_POINT('Ctrl Pts',(0.529219838814109,108.395639467232,15.1176260166494));
#68231=CARTESIAN_POINT('Ctrl Pts',(0.484383276888817,108.401477092634,15.1310432974405));
#68232=CARTESIAN_POINT('Ctrl Pts',(0.439035184854932,108.407311285814,15.1428104264786));
#68233=CARTESIAN_POINT('Ctrl Pts',(0.393286543835379,108.413137886914,15.1528779590084));
#68234=CARTESIAN_POINT('Ctrl Pts',(0.391555418960531,108.413358365028,15.1532589136248));
#68235=CARTESIAN_POINT('Ctrl Pts',(0.3898237207389,108.413578832247,15.1536374345775));
#68236=CARTESIAN_POINT('Ctrl Pts',(0.388091457000056,108.413799288348,15.1540135197612));
#68237=CARTESIAN_POINT('Ctrl Pts',(0.324523358755103,108.421889266079,15.1678145474989));
#68238=CARTESIAN_POINT('Ctrl Pts',(0.26019742050251,108.429961888862,15.1783321900859));
#68239=CARTESIAN_POINT('Ctrl Pts',(0.195517808938001,108.438053322813,15.1855237469954));
#68240=CARTESIAN_POINT('Ctrl Pts',(0.183082805712587,108.439608944513,15.1869063624936));
#68241=CARTESIAN_POINT('Ctrl Pts',(0.170634865978392,108.441165588903,15.1881664611473));
#68242=CARTESIAN_POINT('Ctrl Pts',(0.158176642001111,108.442723116671,15.1893032368294));
#68243=CARTESIAN_POINT('Ctrl Pts',(0.126371161183714,108.446699439429,15.1922053918412));
#68244=CARTESIAN_POINT('Ctrl Pts',(0.0944986060005764,108.4506815256,15.1943037817774));
#68245=CARTESIAN_POINT('Ctrl Pts',(0.0625846769082255,108.454666905654,
15.195607396074));
#68246=CARTESIAN_POINT('Ctrl Pts',(0.0152080268535606,108.460583255081,
15.1975426287481));
#68247=CARTESIAN_POINT('Ctrl Pts',(-0.032258804083024,108.466505164633,
15.1977244485999));
#68248=CARTESIAN_POINT('Ctrl Pts',(-0.079733805609635,108.472412900431,
15.1961669242321));
#68249=CARTESIAN_POINT('Ctrl Pts',(-0.0797457843910396,108.472414391057,
15.1961665312412));
#68250=CARTESIAN_POINT('Ctrl Pts',(-0.0797577631728505,108.472415881682,
15.1961661381395));
#68251=CARTESIAN_POINT('Ctrl Pts',(-0.0797697419552132,108.472417372307,
15.1961657449271));
#68252=CARTESIAN_POINT('Ctrl Pts',(-0.152296998582491,108.481442570844,
15.1937849840778));
#68253=CARTESIAN_POINT('Ctrl Pts',(-0.224813819289416,108.490440401394,
15.1873581350595));
#68254=CARTESIAN_POINT('Ctrl Pts',(-0.296746304465991,108.499444664769,
15.1768154422734));
#68255=CARTESIAN_POINT('Ctrl Pts',(-0.347536648869933,108.505802427007,
15.1693714203376));
#68256=CARTESIAN_POINT('Ctrl Pts',(-0.398034968456748,108.512163966197,
15.1598757348434));
#68257=CARTESIAN_POINT('Ctrl Pts',(-0.448029752902181,108.518547390497,
15.1483127290138));
#68258=CARTESIAN_POINT('Ctrl Pts',(-0.482363440440263,108.522931177681,
15.1403718881128));
#68259=CARTESIAN_POINT('Ctrl Pts',(-0.516459656282199,108.527325447624,
15.1314561566781));
#68260=CARTESIAN_POINT('Ctrl Pts',(-0.550247651254368,108.531747944161,
15.1215771816121));
#68261=CARTESIAN_POINT('Ctrl Pts',(-0.550248083214224,108.531748000701,
15.1215770553152));
#68262=CARTESIAN_POINT('Ctrl Pts',(-0.550248515174057,108.53174805724,15.1215769290181));
#68263=CARTESIAN_POINT('Ctrl Pts',(-0.550248947133812,108.531748113779,
15.1215768027208));
#68264=CARTESIAN_POINT('Ctrl Pts',(-0.618316268900948,108.540657420602,
15.1016751421431));
#68265=CARTESIAN_POINT('Ctrl Pts',(-0.685276377078738,108.549720929029,
15.0778455464417));
#68266=CARTESIAN_POINT('Ctrl Pts',(-0.750740232549232,108.558866557164,
15.0503067853443));
#68267=CARTESIAN_POINT('Ctrl Pts',(-0.816138006644147,108.568002953401,
15.022795822781));
#68268=CARTESIAN_POINT('Ctrl Pts',(-0.880041776071536,108.577221298021,
14.9915831209971));
#68269=CARTESIAN_POINT('Ctrl Pts',(-0.942045786141081,108.586445406733,
14.9569354411003));
#68270=CARTESIAN_POINT('Ctrl Pts',(-1.01109530809121,108.596717650356,14.9183507474511));
#68271=CARTESIAN_POINT('Ctrl Pts',(-1.07780018936664,108.606993481739,14.8754981788652));
#68272=CARTESIAN_POINT('Ctrl Pts',(-1.14169435252236,108.617166231207,14.8286943605301));
#68273=CARTESIAN_POINT('Ctrl Pts',(-1.1623256668463,108.620450994344,14.8135814888695));
#68274=CARTESIAN_POINT('Ctrl Pts',(-1.18266355547137,108.623724954356,14.7980568093125));
#68275=CARTESIAN_POINT('Ctrl Pts',(-1.20269131967569,108.626984363034,14.7821315275056));
#68276=CARTESIAN_POINT('Ctrl Pts',(-1.27896116548536,108.639396861744,14.7214847785473));
#68277=CARTESIAN_POINT('Ctrl Pts',(-1.35075853641657,108.651601151534,14.6550100057487));
#68278=CARTESIAN_POINT('Ctrl Pts',(-1.41733223837496,108.663665506402,14.5835154665705));
#68279=CARTESIAN_POINT('Ctrl Pts',(-1.44916094053487,108.669433440985,14.5493341257914));
#68280=CARTESIAN_POINT('Ctrl Pts',(-1.47979587266395,108.675169475196,14.5140046271308));
#68281=CARTESIAN_POINT('Ctrl Pts',(-1.50915546850041,108.680881530702,14.4776111778369));
#68282=CARTESIAN_POINT('Ctrl Pts',(-1.57562356625245,108.693813229961,14.3952189215307));
#68283=CARTESIAN_POINT('Ctrl Pts',(-1.63555150521017,108.706623910656,14.3073783843346));
#68284=CARTESIAN_POINT('Ctrl Pts',(-1.68793735961649,108.719397688634,14.2151411815396));
#68285=CARTESIAN_POINT('Ctrl Pts',(-1.70429293358189,108.723385835299,14.1863434763237));
#68286=CARTESIAN_POINT('Ctrl Pts',(-1.71991364783203,108.727370439896,14.1571169868998));
#68287=CARTESIAN_POINT('Ctrl Pts',(-1.73476979970958,108.731354210771,14.1274930723761));
#68288=CARTESIAN_POINT('Ctrl Pts',(-1.76521444237875,108.739518133822,14.0667849226769));
#68289=CARTESIAN_POINT('Ctrl Pts',(-1.79245154811977,108.747681757492,14.0043990366965));
#68290=CARTESIAN_POINT('Ctrl Pts',(-1.8162652288592,108.755931073961,13.9407080569616));
#68291=CARTESIAN_POINT('Ctrl Pts',(-1.83105790375132,108.761055416474,13.9011442462643));
#68292=CARTESIAN_POINT('Ctrl Pts',(-1.84453056491651,108.766212918018,13.8610765079872));
#68293=CARTESIAN_POINT('Ctrl Pts',(-1.85664051206695,108.77142507718,13.8205896755338));
#68294=CARTESIAN_POINT('Ctrl Pts',(-1.85664298319636,108.771426140762,13.8205814138791));
#68295=CARTESIAN_POINT('Ctrl Pts',(-1.85664545426903,108.771427204345,13.8205731522046));
#68296=CARTESIAN_POINT('Ctrl Pts',(-1.85664792528492,108.771428267931,13.8205648905105));
#68297=CARTESIAN_POINT('Ctrl Pts',(-1.87611417489621,108.779807015837,13.7554806471141));
#68298=CARTESIAN_POINT('Ctrl Pts',(-1.89205583967587,108.788296679808,13.6891770610977));
#68299=CARTESIAN_POINT('Ctrl Pts',(-1.90444564021192,108.7968262807,13.6221275369253));
#68300=CARTESIAN_POINT('Ctrl Pts',(-1.91679911494914,108.805330873556,13.5552745960247));
#68301=CARTESIAN_POINT('Ctrl Pts',(-1.92562303307632,108.813874603247,13.4876802910133));
#68302=CARTESIAN_POINT('Ctrl Pts',(-1.93091198941321,108.822405534247,13.4197745662474));
#68303=CARTESIAN_POINT('Ctrl Pts',(-1.9328938959672,108.825602291222,13.3943285628406));
#68304=CARTESIAN_POINT('Ctrl Pts',(-1.93437952954262,108.828797478379,13.3688384235775));
#68305=CARTESIAN_POINT('Ctrl Pts',(-1.93536875477021,108.831989255394,13.3433253517718));
#68306=CARTESIAN_POINT('Ctrl Pts',(-1.93536888315373,108.831989669629,13.3433220406371));
#68307=CARTESIAN_POINT('Ctrl Pts',(-1.93536901152889,108.831990083864,13.343318729502));
#68308=CARTESIAN_POINT('Ctrl Pts',(-1.93536913989568,108.831990498099,13.3433154183666));
#68309=CARTESIAN_POINT('Ctrl Pts',(-1.93589688961357,108.833693526245,13.3297024681694));
#68310=CARTESIAN_POINT('Ctrl Pts',(-1.93628326895919,108.835395388104,13.3160849175915));
#68311=CARTESIAN_POINT('Ctrl Pts',(-1.93652779389579,108.837095796902,13.3024650858162));
#68312=CARTESIAN_POINT('Ctrl Pts',(-1.93786738009383,108.846411182846,13.2278512696566));
#68313=CARTESIAN_POINT('Ctrl Pts',(-1.93495108223821,108.855684228379,13.1531655757965));
#68314=CARTESIAN_POINT('Ctrl Pts',(-1.92777629531796,108.864964810249,13.0788321969946));
#68315=CARTESIAN_POINT('Ctrl Pts',(-1.92068525514588,108.874137065759,13.005366464692));
#68316=CARTESIAN_POINT('Ctrl Pts',(-1.90943317625142,108.883317050789,12.9322452604249));
#68317=CARTESIAN_POINT('Ctrl Pts',(-1.89401259176596,108.892534598748,12.8599152995615));
#68318=CARTESIAN_POINT('Ctrl Pts',(-1.89401126364815,108.892535392621,12.8599090700499));
#68319=CARTESIAN_POINT('Ctrl Pts',(-1.89400993549962,108.892536186495,12.8599028405442));
#68320=CARTESIAN_POINT('Ctrl Pts',(-1.89400860732034,108.892536980369,12.8598966110442));
#68321=CARTESIAN_POINT('Ctrl Pts',(-1.87503209950633,108.903879546833,12.7708919439851));
#68322=CARTESIAN_POINT('Ctrl Pts',(-1.84977984652267,108.915329006507,12.6830647589565));
#68323=CARTESIAN_POINT('Ctrl Pts',(-1.81850801035019,108.926765430093,12.5972872809673));
#68324=CARTESIAN_POINT('Ctrl Pts',(-1.81553173600613,108.92785388342,12.5891234716653));
#68325=CARTESIAN_POINT('Ctrl Pts',(-1.81250094854636,108.928942213636,12.5809782651924));
#68326=CARTESIAN_POINT('Ctrl Pts',(-1.8094158780891,108.930030314201,12.5728524357855));
#68327=CARTESIAN_POINT('Ctrl Pts',(-1.79554110192141,108.934923930729,12.5363073825172));
#68328=CARTESIAN_POINT('Ctrl Pts',(-1.78056790567763,108.939813294932,12.5001524243863));
#68329=CARTESIAN_POINT('Ctrl Pts',(-1.76451512912029,108.944690359364,12.4644529204725));
#68330=CARTESIAN_POINT('Ctrl Pts',(-1.72367364891042,108.957098588542,12.3736262290656));
#68331=CARTESIAN_POINT('Ctrl Pts',(-1.67583869639274,108.969427642048,12.2857384594742));
#68332=CARTESIAN_POINT('Ctrl Pts',(-1.62153010177169,108.981793910678,12.2018922735153));
#68333=CARTESIAN_POINT('Ctrl Pts',(-1.57377007371127,108.992669046388,12.1281563165807));
#68334=CARTESIAN_POINT('Ctrl Pts',(-1.52100199589187,109.003574081424,12.0575494940714));
#68335=CARTESIAN_POINT('Ctrl Pts',(-1.46364032579349,109.014577888671,11.9908697307493));
#68336=CARTESIAN_POINT('Ctrl Pts',(-1.46363051150188,109.014579771367,11.9908583221791));
#68337=CARTESIAN_POINT('Ctrl Pts',(-1.46362069707465,109.014581654067,11.9908469137213));
#68338=CARTESIAN_POINT('Ctrl Pts',(-1.46361088251184,109.014583536771,11.990835505376));
#68339=CARTESIAN_POINT('Ctrl Pts',(-1.4089382030819,109.025071265528,11.9272845540605));
#68340=CARTESIAN_POINT('Ctrl Pts',(-1.35005376806083,109.035687412997,11.8672224646944));
#68341=CARTESIAN_POINT('Ctrl Pts',(-1.28748464177007,109.046295375921,11.8110940219998));
#68342=CARTESIAN_POINT('Ctrl Pts',(-1.27388731706961,109.048600664884,11.7988963662949));
#68343=CARTESIAN_POINT('Ctrl Pts',(-1.26011615904058,109.050905544747,11.786884552742));
#68344=CARTESIAN_POINT('Ctrl Pts',(-1.24617688277292,109.053208576314,11.7750632427495));
#68345=CARTESIAN_POINT('Ctrl Pts',(-1.14591915656587,109.06977304522,11.6900389102171));
#68346=CARTESIAN_POINT('Ctrl Pts',(-1.03692821812283,109.086244866285,11.6148358074028));
#68347=CARTESIAN_POINT('Ctrl Pts',(-0.921408887350246,109.102683591447,
11.5508140451168));
#68348=CARTESIAN_POINT('Ctrl Pts',(-0.807228492933731,109.118931782205,
11.4875343323607));
#68349=CARTESIAN_POINT('Ctrl Pts',(-0.686667685469148,109.135149189964,
11.4351822760625));
#68350=CARTESIAN_POINT('Ctrl Pts',(-0.561923213141406,109.151403428664,
11.3951093109741));
#68351=CARTESIAN_POINT('Ctrl Pts',(-0.533602355987048,109.15509364406,11.3860115072892));
#68352=CARTESIAN_POINT('Ctrl Pts',(-0.505066213971739,109.158785746996,
11.3775466115163));
#68353=CARTESIAN_POINT('Ctrl Pts',(-0.476341145705833,109.162480477521,
11.3697303378323));
#68354=CARTESIAN_POINT('Ctrl Pts',(-0.432229202362458,109.168154328043,
11.3577271976233));
#68355=CARTESIAN_POINT('Ctrl Pts',(-0.387670939531217,109.173834579638,
11.3472537403331));
#68356=CARTESIAN_POINT('Ctrl Pts',(-0.342778193468239,109.179540904526,
11.3383573875759));
#68357=CARTESIAN_POINT('Ctrl Pts',(-0.342773072460125,109.179541555458,
11.3383563727506));
#68358=CARTESIAN_POINT('Ctrl Pts',(-0.342767951447331,109.179542206391,
11.3383553579457));
#68359=CARTESIAN_POINT('Ctrl Pts',(-0.342762830429772,109.179542857324,
11.3383543431613));
#68360=CARTESIAN_POINT('Ctrl Pts',(-0.253722983770747,109.190860722285,
11.3207101439316));
#68361=CARTESIAN_POINT('Ctrl Pts',(-0.163252302171303,109.202310914098,
11.3092405498241));
#68362=CARTESIAN_POINT('Ctrl Pts',(-0.0722659009461916,109.213799137132,
11.3039408459732));
#68363=CARTESIAN_POINT('Ctrl Pts',(-0.0536508068134595,109.216149536205,
11.3028565687106));
#68364=CARTESIAN_POINT('Ctrl Pts',(-0.0350142409579838,109.218501515008,
11.3020304193361));
#68365=CARTESIAN_POINT('Ctrl Pts',(-0.0163642026663661,109.220854247431,
11.3014621481135));
#68366=CARTESIAN_POINT('Ctrl Pts',(0.0945107911799775,109.234841306805,
11.2980837599663));
#68367=CARTESIAN_POINT('Ctrl Pts',(0.205867162649476,109.248853458614,11.3038180654636));
#68368=CARTESIAN_POINT('Ctrl Pts',(0.316203639275899,109.262743079122,11.3186132619521));
#68369=CARTESIAN_POINT('Ctrl Pts',(0.344610819783086,109.266319094679,11.322422426701));
#68370=CARTESIAN_POINT('Ctrl Pts',(0.372951158686283,109.269887196702,11.3268323794333));
#68371=CARTESIAN_POINT('Ctrl Pts',(0.40120053760262,109.273445370479,11.3318428876719));
#68372=CARTESIAN_POINT('Ctrl Pts',(0.504283837842697,109.286429312423,11.3501264657517));
#68373=CARTESIAN_POINT('Ctrl Pts',(0.606178065701835,109.299282835421,11.3764115366991));
#68374=CARTESIAN_POINT('Ctrl Pts',(0.705579404323949,109.312191801006,11.4105266508771));
#68375=CARTESIAN_POINT('Ctrl Pts',(0.711582751676879,109.312971438438,11.4125870344014));
#68376=CARTESIAN_POINT('Ctrl Pts',(0.71757702088544,109.313751280418,11.4146759831112));
#68377=CARTESIAN_POINT('Ctrl Pts',(0.723561930260544,109.314531368777,11.4167934613312));
#68378=CARTESIAN_POINT('Ctrl Pts',(0.797385807564586,109.324153761308,11.4429125623083));
#68379=CARTESIAN_POINT('Ctrl Pts',(0.869777372373823,109.333813896558,11.4733732610354));
#68380=CARTESIAN_POINT('Ctrl Pts',(0.940120873681946,109.343572377364,11.508052956718));
#68381=CARTESIAN_POINT('Ctrl Pts',(0.947088368344305,109.344538950845,11.5114879662081));
#68382=CARTESIAN_POINT('Ctrl Pts',(0.954035798632474,109.345506490686,11.5149643365429));
#68383=CARTESIAN_POINT('Ctrl Pts',(0.96096258594782,109.346475056762,11.5184819285432));
#68384=CARTESIAN_POINT('Ctrl Pts',(0.960979521509151,109.346477424845,11.5184905288354));
#68385=CARTESIAN_POINT('Ctrl Pts',(0.960996456953629,109.346479792936,11.5184991293772));
#68386=CARTESIAN_POINT('Ctrl Pts',(0.961013392281206,109.346482161034,11.5185077301684));
#68387=CARTESIAN_POINT('Ctrl Pts',(1.03876129819005,109.357353795348,11.5579928538976));
#68388=CARTESIAN_POINT('Ctrl Pts',(1.11404612503515,109.368383165716,11.6027406483499));
#68389=CARTESIAN_POINT('Ctrl Pts',(1.18625174548857,109.379455654256,11.6522472692857));
#68390=CARTESIAN_POINT('Ctrl Pts',(1.20861419916872,109.382884861159,11.6675797255486));
#68391=CARTESIAN_POINT('Ctrl Pts',(1.23068129245706,109.386318178422,11.6833682556536));
#68392=CARTESIAN_POINT('Ctrl Pts',(1.25243477358313,109.389752134003,11.6995968924701));
#68393=CARTESIAN_POINT('Ctrl Pts',(1.32179139372386,109.400700613991,11.7513386524469));
#68394=CARTESIAN_POINT('Ctrl Pts',(1.38797012139924,109.411655731262,11.8075590966998));
#68395=CARTESIAN_POINT('Ctrl Pts',(1.45048149457184,109.422526164979,11.8678281572102));
#68396=CARTESIAN_POINT('Ctrl Pts',(1.53309961114421,109.436893066784,11.9474827226795));
#68397=CARTESIAN_POINT('Ctrl Pts',(1.60933543245218,109.451116239369,12.0342334673502));
#68398=CARTESIAN_POINT('Ctrl Pts',(1.67803652371654,109.465353016301,12.1269321145783));
#68399=CARTESIAN_POINT('Ctrl Pts',(1.7320388580821,109.476543801978,12.1997976724716));
#68400=CARTESIAN_POINT('Ctrl Pts',(1.78138165387847,109.487744706282,12.2763416981877));
#68401=CARTESIAN_POINT('Ctrl Pts',(1.82544946795883,109.499017374168,12.3559056472522));
#68402=CARTESIAN_POINT('Ctrl Pts',(1.8369529107494,109.501959986431,12.376674985495));
#68403=CARTESIAN_POINT('Ctrl Pts',(1.84809716987093,109.504907498156,12.3976500241351));
#68404=CARTESIAN_POINT('Ctrl Pts',(1.85887186978288,109.507861025223,12.4188189068126));
#68405=CARTESIAN_POINT('Ctrl Pts',(1.86940297836426,109.510747779796,12.4395092094517));
#68406=CARTESIAN_POINT('Ctrl Pts',(1.87958062550558,109.513640095786,12.460383958756));
#68407=CARTESIAN_POINT('Ctrl Pts',(1.88939488094984,109.516538702891,12.4814308649676));
#68408=CARTESIAN_POINT('Ctrl Pts',(1.88940003301704,109.516540224537,12.4814419136993));
#68409=CARTESIAN_POINT('Ctrl Pts',(1.88940518498505,109.516541746184,12.4814529624812));
#68410=CARTESIAN_POINT('Ctrl Pts',(1.8894103368539,109.516543267832,12.4814640113134));
#68411=CARTESIAN_POINT('Ctrl Pts',(1.92307171724716,109.526485441465,12.5536550852641));
#68412=CARTESIAN_POINT('Ctrl Pts',(1.95249726178874,109.536480542927,12.62799404341));
#68413=CARTESIAN_POINT('Ctrl Pts',(1.97753897570652,109.546486591178,12.703907048022));
#68414=CARTESIAN_POINT('Ctrl Pts',(2.00001983487993,109.555469385341,12.7720569187423));
#68415=CARTESIAN_POINT('Ctrl Pts',(2.0189701699992,109.564460801653,12.8414756753979));
#68416=CARTESIAN_POINT('Ctrl Pts',(2.03430731340211,109.573438968279,12.911800097432));
#68417=CARTESIAN_POINT('Ctrl Pts',(2.05096107398141,109.583187865678,12.9881615199386));
#68418=CARTESIAN_POINT('Ctrl Pts',(2.06335606598736,109.592922388582,13.0655990543191));
#68419=CARTESIAN_POINT('Ctrl Pts',(2.07140518948593,109.602706524858,13.143617414013));
#68420=CARTESIAN_POINT('Ctrl Pts',(2.07140601901899,109.602707533199,13.143625454492));
#68421=CARTESIAN_POINT('Ctrl Pts',(2.07140684850574,109.602708541541,13.1436334949769));
#68422=CARTESIAN_POINT('Ctrl Pts',(2.07140767794618,109.602709549882,13.1436415354678));
#68423=CARTESIAN_POINT('Ctrl Pts',(2.08102833810477,109.61440528097,13.2369029998119));
#68424=CARTESIAN_POINT('Ctrl Pts',(2.08442071776682,109.626117496683,13.3309604660696));
#68425=CARTESIAN_POINT('Ctrl Pts',(2.08148699424942,109.637856538144,13.4249853359634));
#68426=CARTESIAN_POINT('Ctrl Pts',(2.08047818792699,109.641893189578,13.4573172454469));
#68427=CARTESIAN_POINT('Ctrl Pts',(2.07872114074448,109.645932962924,13.4896448314478));
#68428=CARTESIAN_POINT('Ctrl Pts',(2.07621144714014,109.649976082837,13.5219328815354));
#68429=CARTESIAN_POINT('Ctrl Pts',(2.06893545016503,109.661697724157,13.6155410233275));
#68430=CARTESIAN_POINT('Ctrl Pts',(2.05533102326315,109.673448715969,13.7088219604897));
#68431=CARTESIAN_POINT('Ctrl Pts',(2.03530678847665,109.685235629954,13.8008634064405));
#68432=CARTESIAN_POINT('Ctrl Pts',(2.03280776174858,109.68670663813,13.8123501891302));
#68433=CARTESIAN_POINT('Ctrl Pts',(2.03020879341823,109.688178184181,13.8238175846766));
#68434=CARTESIAN_POINT('Ctrl Pts',(2.02750975357541,109.689650261466,13.8352637537059));
#68435=CARTESIAN_POINT('Ctrl Pts',(2.02750691238552,109.689651811073,13.8352758027091));
#68436=CARTESIAN_POINT('Ctrl Pts',(2.02750407108507,109.689653360682,13.8352878516887));
#68437=CARTESIAN_POINT('Ctrl Pts',(2.02750122967404,109.689654910292,13.8352999006448));
#68438=CARTESIAN_POINT('Ctrl Pts',(2.00450040737611,109.702198787307,13.9328345040158));
#68439=CARTESIAN_POINT('Ctrl Pts',(1.97425423397393,109.714849273242,14.0288264559821));
#68440=CARTESIAN_POINT('Ctrl Pts',(1.93724533476024,109.727468592401,14.1223759642247));
#68441=CARTESIAN_POINT('Ctrl Pts',(1.89512619194701,109.741830405835,14.2288429270768));
#68442=CARTESIAN_POINT('Ctrl Pts',(1.8442349654792,109.75615667757,14.3321889440122));
#68443=CARTESIAN_POINT('Ctrl Pts',(1.78528329627254,109.770497721719,14.4311299418159));
#68444=CARTESIAN_POINT('Ctrl Pts',(1.77340675816491,109.773386901273,14.4510628215229));
#68445=CARTESIAN_POINT('Ctrl Pts',(1.76120291576132,109.776276684223,14.4708168462382));
#68446=CARTESIAN_POINT('Ctrl Pts',(1.74867736162986,109.779167487636,14.4903813935025));
#68447=CARTESIAN_POINT('Ctrl Pts',(1.6843329681792,109.79401768829,14.5908854441533));
#68448=CARTESIAN_POINT('Ctrl Pts',(1.61149537262497,109.808896191927,14.6863869329));
#68449=CARTESIAN_POINT('Ctrl Pts',(1.53103586007233,109.823840129088,14.7753075840577));
#68450=CARTESIAN_POINT('Ctrl Pts',(1.51740666653029,109.82637151171,14.7903700263478));
#68451=CARTESIAN_POINT('Ctrl Pts',(1.50355887156844,109.82890477356,14.8052437100646));
#68452=CARTESIAN_POINT('Ctrl Pts',(1.48949682534355,109.831440097097,14.8199210570519));
#68453=CARTESIAN_POINT('Ctrl Pts',(1.42564669235199,109.842951988212,14.8865650249433));
#68454=CARTESIAN_POINT('Ctrl Pts',(1.35738064405652,109.854505653173,14.9491533697211));
#68455=CARTESIAN_POINT('Ctrl Pts',(1.28516978592211,109.86610476067,15.0069531561418));
#68456=CARTESIAN_POINT('Ctrl Pts',(1.28515132482487,109.866107726045,15.0069679329705));
#68457=CARTESIAN_POINT('Ctrl Pts',(1.28513286346812,109.866110691424,15.006982709488));
#68458=CARTESIAN_POINT('Ctrl Pts',(1.2851144018518,109.866113656806,15.0069974856946));
#68459=CARTESIAN_POINT('Ctrl Pts',(1.20743211661619,109.878591312462,15.069172404177));
#68460=CARTESIAN_POINT('Ctrl Pts',(1.12515570427157,109.891138404837,15.1258417777281));
#68461=CARTESIAN_POINT('Ctrl Pts',(1.03914322942434,109.90365553316,15.1766500823808));
#68462=CARTESIAN_POINT('Ctrl Pts',(0.937625917716596,109.918429032235,15.2366172267971));
#68463=CARTESIAN_POINT('Ctrl Pts',(0.830857999498407,109.933167531805,15.2884484472141));
#68464=CARTESIAN_POINT('Ctrl Pts',(0.720252908317178,109.947923312942,15.3315176108421));
#68465=CARTESIAN_POINT('Ctrl Pts',(0.690590419332554,109.951880573777,15.3430680609891));
#68466=CARTESIAN_POINT('Ctrl Pts',(0.660651839016121,109.955839082895,15.3539880557953));
#68467=CARTESIAN_POINT('Ctrl Pts',(0.630464239915361,109.959799860039,15.3642649019636));
#68468=CARTESIAN_POINT('Ctrl Pts',(0.526021692407841,109.973503290169,15.3998205614443));
#68469=CARTESIAN_POINT('Ctrl Pts',(0.418598095206419,109.987234664124,15.4276730546173));
#68470=CARTESIAN_POINT('Ctrl Pts',(0.309471377177917,110.001015880522,15.4472650485884));
#68471=CARTESIAN_POINT('Ctrl Pts',(0.271024458714651,110.005871202049,15.4541675909571));
#68472=CARTESIAN_POINT('Ctrl Pts',(0.232366308112867,110.010732711996,15.4600452356261));
#68473=CARTESIAN_POINT('Ctrl Pts',(0.193553207676388,110.015601372545,15.4648751047488));
#68474=CARTESIAN_POINT('Ctrl Pts',(0.11364529300297,110.025624908602,15.4748187775139));
#68475=CARTESIAN_POINT('Ctrl Pts',(0.0330870109350791,110.03567774002,15.4803178638995));
#68476=CARTESIAN_POINT('Ctrl Pts',(-0.047587460874768,110.045760037852,
15.4811903732368));
#68477=CARTESIAN_POINT('Ctrl Pts',(-0.0476041706067929,110.045762126152,
15.4811905539557));
#68478=CARTESIAN_POINT('Ctrl Pts',(-0.0476208803467128,110.045764214453,
15.4811907344762));
#68479=CARTESIAN_POINT('Ctrl Pts',(-0.0476375900947904,110.045766302757,
15.4811909147984));
#68480=CARTESIAN_POINT('Ctrl Pts',(-0.146456125117576,110.058116163592,
15.4822573087886));
#68481=CARTESIAN_POINT('Ctrl Pts',(-0.245555396409884,110.070523073124,
15.476388413267));
#68482=CARTESIAN_POINT('Ctrl Pts',(-0.344037521982087,110.082932043234,
15.4637870451847));
#68483=CARTESIAN_POINT('Ctrl Pts',(-0.463325542175896,110.097962603027,
15.448523440327));
#68484=CARTESIAN_POINT('Ctrl Pts',(-0.581754791070992,110.113002077922,
15.4233778358814));
#68485=CARTESIAN_POINT('Ctrl Pts',(-0.697729150556525,110.12808094041,15.3886750338168));
#68486=CARTESIAN_POINT('Ctrl Pts',(-0.797186004854783,110.141012214497,
15.3589147355579));
#68487=CARTESIAN_POINT('Ctrl Pts',(-0.894835413450012,110.153972851852,
15.322119651773));
#68488=CARTESIAN_POINT('Ctrl Pts',(-0.989551672779695,110.166966655232,
15.2785458398567));
#68489=CARTESIAN_POINT('Ctrl Pts',(-1.00574172623382,110.169187713926,15.271097674683));
#68490=CARTESIAN_POINT('Ctrl Pts',(-1.02184612180391,110.171409741364,15.2634515657377));
#68491=CARTESIAN_POINT('Ctrl Pts',(-1.03785929845104,110.173632756148,15.2556089330049));
#68492=CARTESIAN_POINT('Ctrl Pts',(-1.06048518812931,110.176773774845,15.2445276499522));
#68493=CARTESIAN_POINT('Ctrl Pts',(-1.08292833471847,110.179916666637,15.2330543039541));
#68494=CARTESIAN_POINT('Ctrl Pts',(-1.10517223570307,110.183061325066,15.2211936368503));
#68495=CARTESIAN_POINT('Ctrl Pts',(-1.10518397338107,110.183062984442,15.2211873782048));
#68496=CARTESIAN_POINT('Ctrl Pts',(-1.10519571100572,110.183064643818,15.2211811194503));
#68497=CARTESIAN_POINT('Ctrl Pts',(-1.10520744857709,110.183066303196,15.2211748605868));
#68498=CARTESIAN_POINT('Ctrl Pts',(-1.19925586538353,110.196362222771,15.1710251161729));
#68499=CARTESIAN_POINT('Ctrl Pts',(-1.28987922969665,110.209709506862,15.1138739398531));
#68500=CARTESIAN_POINT('Ctrl Pts',(-1.37612755368538,110.223084635313,15.0504439106069));
#68501=CARTESIAN_POINT('Ctrl Pts',(-1.38880111623854,110.225050012949,15.0411233301454));
#68502=CARTESIAN_POINT('Ctrl Pts',(-1.40138025994434,110.227015991325,15.0316672540107));
#68503=CARTESIAN_POINT('Ctrl Pts',(-1.41386202424372,110.22898249533,15.0220780525104));
#68504=CARTESIAN_POINT('Ctrl Pts',(-1.49237304676439,110.241351919761,14.9617614180278));
#68505=CARTESIAN_POINT('Ctrl Pts',(-1.56703798599791,110.253742879956,14.896176250949));
#68506=CARTESIAN_POINT('Ctrl Pts',(-1.63721950063078,110.266154511041,14.8258150679101));
#68507=CARTESIAN_POINT('Ctrl Pts',(-1.72392691560699,110.281488754718,14.7388856773451));
#68508=CARTESIAN_POINT('Ctrl Pts',(-1.80382090971275,110.296861122966,14.6446231324412));
#68509=CARTESIAN_POINT('Ctrl Pts',(-1.87552555125901,110.312277975576,14.5440909255201));
#68510=CARTESIAN_POINT('Ctrl Pts',(-1.89151977978687,110.315716813823,14.5216665042102));
#68511=CARTESIAN_POINT('Ctrl Pts',(-1.90710568589463,110.319157644916,14.4989316743978));
#68512=CARTESIAN_POINT('Ctrl Pts',(-1.92226692633959,110.322600156949,14.4759011327845));
#68513=CARTESIAN_POINT('Ctrl Pts',(-1.92227108889527,110.322601102099,14.475894809693));
#68514=CARTESIAN_POINT('Ctrl Pts',(-1.92227525141932,110.322602047249,14.4758884865785));
#68515=CARTESIAN_POINT('Ctrl Pts',(-1.92227941391178,110.3226029924,14.4758821634412));
#68516=CARTESIAN_POINT('Ctrl Pts',(-1.98371355793695,110.336552448123,14.3825591039405));
#68517=CARTESIAN_POINT('Ctrl Pts',(-2.0382585472013,110.350531220208,14.2842470159127));
#68518=CARTESIAN_POINT('Ctrl Pts',(-2.085372516468,110.364537239114,14.1821958687918));
#68519=CARTESIAN_POINT('Ctrl Pts',(-2.10194678452092,110.369464429824,14.1462951986972));
#68520=CARTESIAN_POINT('Ctrl Pts',(-2.11760181028108,110.374394990735,14.1099320549485));
#68521=CARTESIAN_POINT('Ctrl Pts',(-2.13231535993761,110.379328825668,14.0731615550672));
#68522=CARTESIAN_POINT('Ctrl Pts',(-2.18231562772883,110.396095212681,13.9482063346211));
#68523=CARTESIAN_POINT('Ctrl Pts',(-2.22144860440119,110.412899907065,13.8185482593629));
#68524=CARTESIAN_POINT('Ctrl Pts',(-2.24891684882211,110.429768454545,13.6861326704635));
#68525=CARTESIAN_POINT('Ctrl Pts',(-2.25313778887605,110.432360579714,13.6657848734078));
#68526=CARTESIAN_POINT('Ctrl Pts',(-2.25708319521983,110.434954212933,13.6453719205305));
#68527=CARTESIAN_POINT('Ctrl Pts',(-2.26075007217476,110.437549447166,13.6249008325395));
#68528=CARTESIAN_POINT('Ctrl Pts',(-2.26815586153436,110.44279089876,13.5835565039769));
#68529=CARTESIAN_POINT('Ctrl Pts',(-2.27442596979226,110.44803909271,13.5419732460962));
#68530=CARTESIAN_POINT('Ctrl Pts',(-2.27953531506399,110.453295211892,13.5002048223747));
#68531=CARTESIAN_POINT('Ctrl Pts',(-2.28308796134232,110.456949913475,13.4711622685457));
#68532=CARTESIAN_POINT('Ctrl Pts',(-2.286079380829,110.460608471516,13.4420299700733));
#68533=CARTESIAN_POINT('Ctrl Pts',(-2.28850068218742,110.464270298831,13.4128278836824));
#68534=CARTESIAN_POINT('Ctrl Pts',(-2.28850195542795,110.464272224401,13.4128125277749));
#68535=CARTESIAN_POINT('Ctrl Pts',(-2.28850322851069,110.464274149973,13.4127971718496));
#68536=CARTESIAN_POINT('Ctrl Pts',(-2.28850450143566,110.464276075545,13.4127818159066));
#68537=CARTESIAN_POINT('Ctrl Pts',(-2.2991622457932,110.480398200416,13.2842120107848));
#68538=CARTESIAN_POINT('Ctrl Pts',(-2.29876151461231,110.496569795702,13.1544009523245));
#68539=CARTESIAN_POINT('Ctrl Pts',(-2.2875131865112,110.512782139525,13.025148513299));
#68540=CARTESIAN_POINT('Ctrl Pts',(-2.27611672148484,110.529207994791,12.894193860511));
#68541=CARTESIAN_POINT('Ctrl Pts',(-2.25358266164367,110.545675397593,12.7638131799088));
#68542=CARTESIAN_POINT('Ctrl Pts',(-2.22012284844778,110.562172038801,12.6359232236228));
#68543=CARTESIAN_POINT('Ctrl Pts',(-2.18891553345408,110.57755813422,12.5166427564252));
#68544=CARTESIAN_POINT('Ctrl Pts',(-2.14820301977644,110.592969364365,12.3995305454992));
#68545=CARTESIAN_POINT('Ctrl Pts',(-2.09817411773941,110.608397046164,12.2861639713865));
#68546=CARTESIAN_POINT('Ctrl Pts',(-2.09817273107111,110.608397473778,12.2861608291662));
#68547=CARTESIAN_POINT('Ctrl Pts',(-2.09817134439567,110.608397901392,12.2861576869487));
#68548=CARTESIAN_POINT('Ctrl Pts',(-2.09816995771305,110.608398329007,12.2861545447341));
#68549=CARTESIAN_POINT('Ctrl Pts',(-2.05908247704408,110.62045182211,12.1975825444839));
#68550=CARTESIAN_POINT('Ctrl Pts',(-2.01430181816575,110.632535849416,12.1112862642052));
#68551=CARTESIAN_POINT('Ctrl Pts',(-1.96422019338439,110.644693528793,12.02794157505));
#68552=CARTESIAN_POINT('Ctrl Pts',(-1.91397081635425,110.656891931251,11.944317716457));
#68553=CARTESIAN_POINT('Ctrl Pts',(-1.85837309022311,110.669166915175,11.8636481585629));
#68554=CARTESIAN_POINT('Ctrl Pts',(-1.79784476165745,110.681487677843,11.7866307540655));
#68555=CARTESIAN_POINT('Ctrl Pts',(-1.79783778251977,110.681489098472,11.7866218736771));
#68556=CARTESIAN_POINT('Ctrl Pts',(-1.79783080331657,110.681490519101,11.7866129933372));
#68557=CARTESIAN_POINT('Ctrl Pts',(-1.79782382404781,110.681491939732,11.7866041130458));
#68558=CARTESIAN_POINT('Ctrl Pts',(-1.7358533973767,110.694106020649,11.7077540982695));
#68559=CARTESIAN_POINT('Ctrl Pts',(-1.66871801896252,110.706756334567,11.6327293597556));
#68560=CARTESIAN_POINT('Ctrl Pts',(-1.59693074248384,110.719401143423,11.562124819429));
#68561=CARTESIAN_POINT('Ctrl Pts',(-1.52872908249229,110.731414371902,11.4950468205215));
#68562=CARTESIAN_POINT('Ctrl Pts',(-1.45632803878547,110.743422408375,11.4319598983437));
#68563=CARTESIAN_POINT('Ctrl Pts',(-1.38018946334844,110.755388637441,11.3733977294143));
#68564=CARTESIAN_POINT('Ctrl Pts',(-1.38016583383902,110.755392351145,11.3733795547202));
#68565=CARTESIAN_POINT('Ctrl Pts',(-1.38014220396964,110.755396064845,11.3733613804617));
#68566=CARTESIAN_POINT('Ctrl Pts',(-1.38011857374031,110.75539977854,11.3733432066391));
#68567=CARTESIAN_POINT('Ctrl Pts',(-1.30196435758779,110.767682392561,11.313235416559));
#68568=CARTESIAN_POINT('Ctrl Pts',(-1.21984993539952,110.779927172049,11.2578792232138));
#68569=CARTESIAN_POINT('Ctrl Pts',(-1.13445157810722,110.792197271441,11.2077439862546));
#68570=CARTESIAN_POINT('Ctrl Pts',(-1.04906646440958,110.804465467984,11.1576165242781));
#68571=CARTESIAN_POINT('Ctrl Pts',(-0.960399632900019,110.816759314713,
11.1127059378167));
#68572=CARTESIAN_POINT('Ctrl Pts',(-0.86907193265452,110.829148517403,11.0734487355745));
#68573=CARTESIAN_POINT('Ctrl Pts',(-0.869057767339681,110.829150439021,
11.0734426466154));
#68574=CARTESIAN_POINT('Ctrl Pts',(-0.869043601960864,110.829152360641,
11.0734365577924));
#68575=CARTESIAN_POINT('Ctrl Pts',(-0.869029436517997,110.829154282264,
11.0734304691054));
#68576=CARTESIAN_POINT('Ctrl Pts',(-0.841101772249262,110.832942828244,
11.0614264105134));
#68577=CARTESIAN_POINT('Ctrl Pts',(-0.812930052409786,110.836742231314,
11.0499537942301));
#68578=CARTESIAN_POINT('Ctrl Pts',(-0.784532884087689,110.840553326691,
11.0390191405254));
#68579=CARTESIAN_POINT('Ctrl Pts',(-0.695612383247482,110.852487069725,
11.004779286998));
#68580=CARTESIAN_POINT('Ctrl Pts',(-0.60447439323736,110.864536520627,10.9758112663676));
#68581=CARTESIAN_POINT('Ctrl Pts',(-0.511741795115254,110.876623330507,
10.9523249234607));
#68582=CARTESIAN_POINT('Ctrl Pts',(-0.440408054463211,110.885921003372,
10.9342582594427));
#68583=CARTESIAN_POINT('Ctrl Pts',(-0.368132052889044,110.895240438188,
10.9194367423256));
#68584=CARTESIAN_POINT('Ctrl Pts',(-0.29522758730732,110.904542379711,10.9079600696815));
#68585=CARTESIAN_POINT('Ctrl Pts',(-0.295187514083616,110.904547492687,
10.9079537613262));
#68586=CARTESIAN_POINT('Ctrl Pts',(-0.295147440669938,110.904552605657,
10.9079474539813));
#68587=CARTESIAN_POINT('Ctrl Pts',(-0.295107367066453,110.904557718623,
10.9079411476467));
#68588=CARTESIAN_POINT('Ctrl Pts',(-0.19616115143769,110.917182203022,10.89237010119));
#68589=CARTESIAN_POINT('Ctrl Pts',(-0.0960277085892771,110.929773050324,
10.8829525041896));
#68590=CARTESIAN_POINT('Ctrl Pts',(0.0045203639492899,110.942329915504,
10.8797700252342));
#68591=CARTESIAN_POINT('Ctrl Pts',(0.00456871948157908,110.942335954346,
10.8797684947179));
#68592=CARTESIAN_POINT('Ctrl Pts',(0.004617075109645,110.94234199318,10.8797669656437));
#68593=CARTESIAN_POINT('Ctrl Pts',(0.00466543083367732,110.942348032006,
10.8797654380116));
#68594=CARTESIAN_POINT('Ctrl Pts',(0.105219794853847,110.95490560042,10.8765887701901));
#68595=CARTESIAN_POINT('Ctrl Pts',(0.20618849603257,110.967429568142,10.8796480880734));
#68596=CARTESIAN_POINT('Ctrl Pts',(0.306777259267146,110.979927951317,10.8890214945142));
#68597=CARTESIAN_POINT('Ctrl Pts',(0.306819736736933,110.979933229239,10.8890254527952));
#68598=CARTESIAN_POINT('Ctrl Pts',(0.306862214139012,110.979938507157,10.8890294122022));
#68599=CARTESIAN_POINT('Ctrl Pts',(0.30690469147322,110.97994378507,10.8890333727351));
#68600=CARTESIAN_POINT('Ctrl Pts',(0.404730243812092,110.992098850771,10.8981545036191));
#68601=CARTESIAN_POINT('Ctrl Pts',(0.502216743195765,111.004240432774,10.913253758302));
#68602=CARTESIAN_POINT('Ctrl Pts',(0.598599075847304,111.016457344285,10.9342321298295));
#68603=CARTESIAN_POINT('Ctrl Pts',(0.662418877813026,111.024546802713,10.9481230108615));
#68604=CARTESIAN_POINT('Ctrl Pts',(0.725756424234182,111.032669579998,10.9645909835171));
#68605=CARTESIAN_POINT('Ctrl Pts',(0.788409092860007,111.040853078828,10.9836101491186));
#68606=CARTESIAN_POINT('Ctrl Pts',(0.825776009236343,111.045733830488,10.994953442009));
#68607=CARTESIAN_POINT('Ctrl Pts',(0.862899977419791,111.050636232305,11.0072045053116));
#68608=CARTESIAN_POINT('Ctrl Pts',(0.899737380831095,111.055557395671,11.0203552379715));
#68609=CARTESIAN_POINT('Ctrl Pts',(0.899763975116234,111.055560948441,11.0203647319722));
#68610=CARTESIAN_POINT('Ctrl Pts',(0.89979056925204,111.055564501221,11.0203742264418));
#68611=CARTESIAN_POINT('Ctrl Pts',(0.899817163238463,111.055568054011,11.0203837213803));
#68612=CARTESIAN_POINT('Ctrl Pts',(0.995769942590633,111.068386742687,11.0546420580142));
#68613=CARTESIAN_POINT('Ctrl Pts',(1.08975364505154,111.081297354889,11.0949830330797));
#68614=CARTESIAN_POINT('Ctrl Pts',(1.18105978369377,111.094208322136,11.1411116544715));
#68615=CARTESIAN_POINT('Ctrl Pts',(1.27231753550347,111.107112447338,11.1872158304327));
#68616=CARTESIAN_POINT('Ctrl Pts',(1.36089921071295,111.120016402732,11.239104209367));
#68617=CARTESIAN_POINT('Ctrl Pts',(1.44603641190564,111.132819799862,11.2964523654609));
#68618=CARTESIAN_POINT('Ctrl Pts',(1.44608155348979,111.1328265885,11.2964827726927));
#68619=CARTESIAN_POINT('Ctrl Pts',(1.44612669410611,111.13283337711,11.2965131814593));
#68620=CARTESIAN_POINT('Ctrl Pts',(1.44617183375462,111.132840165691,11.2965435917605));
#68621=CARTESIAN_POINT('Ctrl Pts',(1.51563559984642,111.14328686715,11.3433409001863));
#68622=CARTESIAN_POINT('Ctrl Pts',(1.58282234530331,111.153668629732,11.393782710617));
#68623=CARTESIAN_POINT('Ctrl Pts',(1.64746239050899,111.1640970458,11.4475182852451));
#68624=CARTESIAN_POINT('Ctrl Pts',(1.66204961579713,111.166450411336,11.459644714467));
#68625=CARTESIAN_POINT('Ctrl Pts',(1.676507349584,111.168806202672,11.4719390412158));
#68626=CARTESIAN_POINT('Ctrl Pts',(1.69083281828931,111.171165781603,11.4843975467765));
#68627=CARTESIAN_POINT('Ctrl Pts',(1.69086858377381,111.171171672614,11.4844286511331));
#68628=CARTESIAN_POINT('Ctrl Pts',(1.69090434843375,111.171177563648,11.484459756513));
#68629=CARTESIAN_POINT('Ctrl Pts',(1.6909401122692,111.171183454705,11.4844908629163));
#68630=CARTESIAN_POINT('Ctrl Pts',(1.74635565641906,111.180311562881,11.5326897836048));
#68631=CARTESIAN_POINT('Ctrl Pts',(1.79978000550124,111.18949556541,11.5833355296906));
#68632=CARTESIAN_POINT('Ctrl Pts',(1.85083037852574,111.198601923597,11.6364041098969));
#68633=CARTESIAN_POINT('Ctrl Pts',(1.87146057282596,111.202281934685,11.6578498909173));
#68634=CARTESIAN_POINT('Ctrl Pts',(1.89170248915674,111.205949118275,11.679690867053));
#68635=CARTESIAN_POINT('Ctrl Pts',(1.9115288023957,111.209594155977,11.7019231056942));
#68636=CARTESIAN_POINT('Ctrl Pts',(1.91155359787195,111.209598714588,11.7019509101044));
#68637=CARTESIAN_POINT('Ctrl Pts',(1.9115783926982,111.209603273164,11.7019787151265));
#68638=CARTESIAN_POINT('Ctrl Pts',(1.91160318687453,111.209607831706,11.7020065207606));
#68639=CARTESIAN_POINT('Ctrl Pts',(1.95919582421182,111.218357991857,11.7553796774532));
#68640=CARTESIAN_POINT('Ctrl Pts',(2.00440512406786,111.22698198537,11.81102038669));
#68641=CARTESIAN_POINT('Ctrl Pts',(2.04710225378665,111.235599353169,11.8686802785851));
#68642=CARTESIAN_POINT('Ctrl Pts',(2.06145000751985,111.23849509515,11.8880560524285));
#68643=CARTESIAN_POINT('Ctrl Pts',(2.07551435835042,111.241390157184,11.9076601534837));
#68644=CARTESIAN_POINT('Ctrl Pts',(2.08929110769117,111.244289249369,11.9274842264238));
#68645=CARTESIAN_POINT('Ctrl Pts',(2.90681173597704,103.854552771039,14.4175227442231));
#68646=CARTESIAN_POINT('Ctrl Pts',(2.63264798485741,103.95385495439,15.1646348490477));
#68647=CARTESIAN_POINT('Ctrl Pts',(1.49083056653157,104.151063919667,16.4244092746339));
#68648=CARTESIAN_POINT('Ctrl Pts',(-1.05817372960175,104.448274315067,16.6201105460967));
#68649=CARTESIAN_POINT('Ctrl Pts',(-3.05249466751713,104.745106921702,15.0266860645816));
#68650=CARTESIAN_POINT('Ctrl Pts',(-3.42901662081578,105.043546951771,12.4890643696838));
#68651=CARTESIAN_POINT('Ctrl Pts',(-1.96751718769065,105.343083663407,10.3654093854579));
#68652=CARTESIAN_POINT('Ctrl Pts',(0.130224879799022,105.593176463126,9.90337622186573));
#68653=CARTESIAN_POINT('Ctrl Pts',(1.66609337331968,105.793269206908,10.4586464905891));
#68654=CARTESIAN_POINT('Ctrl Pts',(2.58745819416953,105.943284758349,11.2626524023438));
#68655=CARTESIAN_POINT('Ctrl Pts',(3.1477791609849,106.093175311736,12.349176213815));
#68656=CARTESIAN_POINT('Ctrl Pts',(3.30881198513969,106.281690758094,13.8782839209593));
#68657=CARTESIAN_POINT('Ctrl Pts',(2.52885555445624,106.508484576144,15.6360413544147));
#68658=CARTESIAN_POINT('Ctrl Pts',(0.552586543155371,106.772829197388,16.6810916807751));
#68659=CARTESIAN_POINT('Ctrl Pts',(-2.01179905013733,107.079459120307,16.2278473478844));
#68660=CARTESIAN_POINT('Ctrl Pts',(-3.68191758413864,107.426772062514,13.5565035374946));
#68661=CARTESIAN_POINT('Ctrl Pts',(-2.42805946625477,107.747949405601,10.9257775430486));
#68662=CARTESIAN_POINT('Ctrl Pts',(-0.46995553826754,108.001722082342,10.1586505583125));
#68663=CARTESIAN_POINT('Ctrl Pts',(1.07508180875167,108.190346887958,10.3385354236562));
#68664=CARTESIAN_POINT('Ctrl Pts',(2.33593740943957,108.377152545808,11.2353671016102));
#68665=CARTESIAN_POINT('Ctrl Pts',(2.8928771135283,108.53122080733,12.3796729815658));
#68666=CARTESIAN_POINT('Ctrl Pts',(2.97090758485472,108.653462194652,13.3640168289253));
#68667=CARTESIAN_POINT('Ctrl Pts',(2.80613213962208,108.775015492972,14.3320426466057));
#68668=CARTESIAN_POINT('Ctrl Pts',(2.28979959784192,108.895510736219,15.1834259478592));
#68669=CARTESIAN_POINT('Ctrl Pts',(1.52256885958377,109.014906219318,15.7681537405536));
#68670=CARTESIAN_POINT('Ctrl Pts',(0.971903944637074,109.089062781808,16.0028169166292));
#68671=CARTESIAN_POINT('Ctrl Pts',(0.508529708149316,109.148105042691,16.1043440298024));
#68672=CARTESIAN_POINT('Ctrl Pts',(0.0385556231530761,109.206954544851,
16.1465900629988));
#68673=CARTESIAN_POINT('Ctrl Pts',(-1.26134894552435,109.368002063753,16.0269418470898));
#68674=CARTESIAN_POINT('Ctrl Pts',(-2.42146781906107,109.540766094044,14.9954976241844));
#68675=CARTESIAN_POINT('Ctrl Pts',(-2.72256324956282,109.710470239931,13.6548996602733));
#68676=CARTESIAN_POINT('Ctrl Pts',(-2.70272022843698,109.822784912802,12.7494026467838));
#68677=CARTESIAN_POINT('Ctrl Pts',(-2.19786584670101,109.98014059768,11.5475342367803));
#68678=CARTESIAN_POINT('Ctrl Pts',(-0.787693309640737,110.180194811126,
10.6109538898846));
#68679=CARTESIAN_POINT('Ctrl Pts',(1.01870577211658,110.393928793874,10.7498948506012));
#68680=CARTESIAN_POINT('Ctrl Pts',(2.10419463547849,110.568274228434,11.7517884366777));
#68681=CARTESIAN_POINT('Ctrl Pts',(2.46316648785379,110.705500429676,12.8070638438925));
#68682=CARTESIAN_POINT('Ctrl Pts',(2.46375808236071,110.841235052451,13.9109031113142));
#68683=CARTESIAN_POINT('Ctrl Pts',(1.77979820499809,111.008121570367,15.1476579499127));
#68684=CARTESIAN_POINT('Ctrl Pts',(0.380213540866219,111.187691809938,15.7426116475981));
#68685=CARTESIAN_POINT('Ctrl Pts',(-0.923082425093289,111.347830969033,
15.503160237289));
#68686=CARTESIAN_POINT('Ctrl Pts',(-1.83584649687992,111.489617699394,14.768741531006));
#68687=CARTESIAN_POINT('Ctrl Pts',(-2.27775706335791,111.629132182632,13.7020687273194));
#68688=CARTESIAN_POINT('Ctrl Pts',(-2.17729566802582,111.743561512123,12.7616840700015));
#68689=CARTESIAN_POINT('Ctrl Pts',(-1.83989547207112,111.834049994605,12.1130192209344));
#68690=CARTESIAN_POINT('Ctrl Pts',(-1.47795183257781,111.901395372625,11.7069533144105));
#68691=CARTESIAN_POINT('Ctrl Pts',(-1.03001366334317,111.968239986844,11.4052174233104));
#68692=CARTESIAN_POINT('Ctrl Pts',(-0.609463651730633,112.023527612806,
11.2548334453014));
#68693=CARTESIAN_POINT('Ctrl Pts',(-0.260452763356783,112.067519905567,
11.199801986779));
#68694=CARTESIAN_POINT('Ctrl Pts',(0.0914627850391553,112.111354672102,
11.1885457737289));
#68695=CARTESIAN_POINT('Ctrl Pts',(0.5262964590746,112.165851041506,11.25685877975));
#68696=CARTESIAN_POINT('Ctrl Pts',(0.928356282889431,112.219973850279,11.4290887639811));
#68697=CARTESIAN_POINT('Ctrl Pts',(1.21506878098601,112.263049928539,11.622452038207));
#68698=CARTESIAN_POINT('Ctrl Pts',(1.8673642460961,112.37037650421,12.1870800767796));
#68699=CARTESIAN_POINT('Ctrl Pts',(2.32564333624236,112.550119454129,13.7487515890008));
#68700=CARTESIAN_POINT('Ctrl Pts',(0.857942820871301,112.798018163271,15.4593287880594));
#68701=CARTESIAN_POINT('Ctrl Pts',(-1.33588576058301,113.041155186133,15.1515921963496));
#68702=CARTESIAN_POINT('Ctrl Pts',(-2.14355161351861,113.254060359302,13.4006149978819));
#68703=CARTESIAN_POINT('Ctrl Pts',(-1.53367476616883,113.438784209471,11.9546519400679));
#68704=CARTESIAN_POINT('Ctrl Pts',(-0.369804341368539,113.596407856987,
11.3032888791665));
#68705=CARTESIAN_POINT('Ctrl Pts',(0.838022111309818,113.740581086973,11.4927043608578));
#68706=CARTESIAN_POINT('Ctrl Pts',(1.63927578177115,113.871676899798,12.2235980999995));
#68707=CARTESIAN_POINT('Ctrl Pts',(1.95948343014593,113.989837235801,13.1464677838519));
#68708=CARTESIAN_POINT('Ctrl Pts',(1.79717931737704,114.108329735318,14.1132911901071));
#68709=CARTESIAN_POINT('Ctrl Pts',(1.18918375849656,114.227310414659,14.8871680207432));
#68710=CARTESIAN_POINT('Ctrl Pts',(0.279975681687718,114.346930556551,15.2773039793232));
#68711=CARTESIAN_POINT('Ctrl Pts',(-0.712306032734786,114.467345568773,
15.1836650206917));
#68712=CARTESIAN_POINT('Ctrl Pts',(-1.40463281222753,114.568468484755,14.7149792157192));
#68713=CARTESIAN_POINT('Ctrl Pts',(-1.73026114226455,114.639733774504,14.23957264692));
#68714=CARTESIAN_POINT('Ctrl Pts',(-1.86164459924767,114.680598472528,13.9390965480409));
#68715=CARTESIAN_POINT('Ctrl Pts',(-2.09935034112274,114.783008522088,13.1499718822202));
#68716=CARTESIAN_POINT('Ctrl Pts',(-1.76503529547132,114.917638441435,11.9842552755218));
#68717=CARTESIAN_POINT('Ctrl Pts',(-0.567487175863522,115.086316822326,
11.2599496856478));
#68718=CARTESIAN_POINT('Ctrl Pts',(0.665519304553295,115.235790922527,11.1971637803623));
#68719=CARTESIAN_POINT('Ctrl Pts',(1.92016243365841,115.409510586213,12.0066278758882));
#68720=CARTESIAN_POINT('Ctrl Pts',(2.33861956090724,115.609211184837,13.6750014934849));
#68721=CARTESIAN_POINT('Ctrl Pts',(1.6301418363172,115.779470559898,14.9552947116152));
#68722=CARTESIAN_POINT('Ctrl Pts',(0.635494893866887,115.918122660083,15.4956801563099));
#68723=CARTESIAN_POINT('Ctrl Pts',(-0.499791186913486,116.058458118718,
15.643431048584));
#68724=CARTESIAN_POINT('Ctrl Pts',(-1.89423469946485,116.23707880032,15.0005349982472));
#68725=CARTESIAN_POINT('Ctrl Pts',(-2.60953214547825,116.456826834462,13.2493627101195));
#68726=CARTESIAN_POINT('Ctrl Pts',(-1.90299736565981,116.688139689368,11.3891119411448));
#68727=CARTESIAN_POINT('Ctrl Pts',(-0.637255827920347,116.848579631347,
10.8064219699136));
#68728=CARTESIAN_POINT('Ctrl Pts',(0.0392219119147239,116.932968917921,
10.7964020467747));
#68729=CARTESIAN_POINT('Ctrl Pts',(2.71505794088331,104.1994437308,14.3468610267603));
#68730=CARTESIAN_POINT('Ctrl Pts',(2.44854735935264,104.292313447051,15.0416272092801));
#68731=CARTESIAN_POINT('Ctrl Pts',(1.36756482302596,104.475801927177,16.1958735715385));
#68732=CARTESIAN_POINT('Ctrl Pts',(-0.983662767649807,104.749721435673,
16.3386992894006));
#68733=CARTESIAN_POINT('Ctrl Pts',(-2.78217366894562,105.020910301127,14.8550186522848));
#68734=CARTESIAN_POINT('Ctrl Pts',(-3.08800545020851,105.291383777472,12.5508031196169));
#68735=CARTESIAN_POINT('Ctrl Pts',(-1.74472357217229,105.56087112011,10.6608062718286));
#68736=CARTESIAN_POINT('Ctrl Pts',(0.135625608828576,105.784400237312,10.2757794639132));
#68737=CARTESIAN_POINT('Ctrl Pts',(1.49502657686255,105.962468409704,10.7887768814312));
#68738=CARTESIAN_POINT('Ctrl Pts',(2.30264041650804,106.095612653712,11.5134951068175));
#68739=CARTESIAN_POINT('Ctrl Pts',(2.78524563770895,106.228317938575,12.4819913514941));
#68740=CARTESIAN_POINT('Ctrl Pts',(2.90874630672134,106.394841463325,13.8343063389686));
#68741=CARTESIAN_POINT('Ctrl Pts',(2.20004500026988,106.594606461261,15.3723449650755));
#68742=CARTESIAN_POINT('Ctrl Pts',(0.451984644705152,106.826764135065,16.2654245396575));
#68743=CARTESIAN_POINT('Ctrl Pts',(-1.78882197927717,107.095458932795,15.8367470047943));
#68744=CARTESIAN_POINT('Ctrl Pts',(-3.21619776564414,107.399246079781,13.4802679274698));
#68745=CARTESIAN_POINT('Ctrl Pts',(-2.0882346499087,107.680042569535,11.1962729879085));
#68746=CARTESIAN_POINT('Ctrl Pts',(-0.365742139369948,107.902133889693,
10.549148540978));
#68747=CARTESIAN_POINT('Ctrl Pts',(0.985322022483406,108.067401390196,10.7259094226531));
#68748=CARTESIAN_POINT('Ctrl Pts',(2.08025913738351,108.231343450877,11.5284561491254));
#68749=CARTESIAN_POINT('Ctrl Pts',(2.5554633745237,108.366841980157,12.5415462205961));
#68750=CARTESIAN_POINT('Ctrl Pts',(2.61143887944914,108.474561818227,13.409667832991));
#68751=CARTESIAN_POINT('Ctrl Pts',(2.45344216292041,108.581827780697,14.2614262617206));
#68752=CARTESIAN_POINT('Ctrl Pts',(1.98585296195543,108.688410614965,15.0075574214225));
#68753=CARTESIAN_POINT('Ctrl Pts',(1.29777849423895,108.794308983379,15.5157261953399));
#68754=CARTESIAN_POINT('Ctrl Pts',(0.805428609191861,108.860210108581,15.7167319489964));
#68755=CARTESIAN_POINT('Ctrl Pts',(0.391781166622539,108.912760257788,15.8007187722551));
#68756=CARTESIAN_POINT('Ctrl Pts',(-0.0274075049062522,108.965196661223,
15.8318584187781));
#68757=CARTESIAN_POINT('Ctrl Pts',(-1.18527549088678,109.108927758844,15.7073432711166));
#68758=CARTESIAN_POINT('Ctrl Pts',(-2.21381540198591,109.264023600951,14.7672557840495));
#68759=CARTESIAN_POINT('Ctrl Pts',(-2.4666221194252,109.417455916768,13.5512181994124));
#68760=CARTESIAN_POINT('Ctrl Pts',(-2.43525232684139,109.519304698459,12.7307790999533));
#68761=CARTESIAN_POINT('Ctrl Pts',(-1.95826944884497,109.662664632789,11.6435908816576));
#68762=CARTESIAN_POINT('Ctrl Pts',(-0.650482528322692,109.846363248703,
10.8039310880342));
#68763=CARTESIAN_POINT('Ctrl Pts',(1.02182660581755,110.044567718633,10.9591201241675));
#68764=CARTESIAN_POINT('Ctrl Pts',(2.02377124064189,110.207984441163,11.9142507291509));
#68765=CARTESIAN_POINT('Ctrl Pts',(2.34515085280631,110.337721417545,12.9176288954705));
#68766=CARTESIAN_POINT('Ctrl Pts',(2.32669728841621,110.466814757994,13.9667344923216));
#68767=CARTESIAN_POINT('Ctrl Pts',(1.65024421515736,110.627010942262,15.1422811214735));
#68768=CARTESIAN_POINT('Ctrl Pts',(0.279841231730215,110.801635822459,15.6967579505581));
#68769=CARTESIAN_POINT('Ctrl Pts',(-0.997723993787982,110.959225644215,
15.437098270253));
#68770=CARTESIAN_POINT('Ctrl Pts',(-1.89073077452904,111.100228398427,14.689633673013));
#68771=CARTESIAN_POINT('Ctrl Pts',(-2.31361461167824,111.240471817201,13.6092790523088));
#68772=CARTESIAN_POINT('Ctrl Pts',(-2.19227242180266,111.356767594283,12.6561660152691));
#68773=CARTESIAN_POINT('Ctrl Pts',(-1.83243226651477,111.449499794301,11.9992928382035));
#68774=CARTESIAN_POINT('Ctrl Pts',(-1.45059332214956,111.518902314342,11.5892585743851));
#68775=CARTESIAN_POINT('Ctrl Pts',(-0.979851457299495,111.588174909696,
11.2869954931243));
#68776=CARTESIAN_POINT('Ctrl Pts',(-0.538407219059272,111.645794817927,
11.140130616902));
#68777=CARTESIAN_POINT('Ctrl Pts',(-0.172120535377108,111.691835651858,
11.0908611006565));
#68778=CARTESIAN_POINT('Ctrl Pts',(0.19719169622667,111.73784065953,11.0874665918825));
#68779=CARTESIAN_POINT('Ctrl Pts',(0.65349947446874,111.795278306845,11.1698210577316));
#68780=CARTESIAN_POINT('Ctrl Pts',(1.07509744453089,111.852641265216,11.3619597323698));
#68781=CARTESIAN_POINT('Ctrl Pts',(1.37521290996629,111.898488472078,11.5747499552319));
#68782=CARTESIAN_POINT('Ctrl Pts',(2.05657697613875,112.013038804026,12.1930111133316));
#68783=CARTESIAN_POINT('Ctrl Pts',(2.5198426174308,112.207309807241,13.8895055813126));
#68784=CARTESIAN_POINT('Ctrl Pts',(0.863358025389426,112.4810590135,15.7453375640381));
#68785=CARTESIAN_POINT('Ctrl Pts',(-1.60009927363686,112.754983055442,15.3477610936586));
#68786=CARTESIAN_POINT('Ctrl Pts',(-2.48158913313704,112.999225065672,13.3196393176612));
#68787=CARTESIAN_POINT('Ctrl Pts',(-1.73154951128389,113.213913880982,11.6578741429386));
#68788=CARTESIAN_POINT('Ctrl Pts',(-0.348206397242804,113.398792298062,
10.9293842108788));
#68789=CARTESIAN_POINT('Ctrl Pts',(1.07234040692998,113.569220429567,11.1898313111311));
#68790=CARTESIAN_POINT('Ctrl Pts',(2.00084073465665,113.725049090902,12.0830127970274));
#68791=CARTESIAN_POINT('Ctrl Pts',(2.35323487848361,113.866053623984,13.193307214017));
#68792=CARTESIAN_POINT('Ctrl Pts',(2.12830650217169,114.007886824867,14.3442064957623));
#68793=CARTESIAN_POINT('Ctrl Pts',(1.37491864048594,114.150614707706,15.2521168057112));
#68794=CARTESIAN_POINT('Ctrl Pts',(0.271426623166744,114.294299038404,15.6911251296496));
#68795=CARTESIAN_POINT('Ctrl Pts',(-0.916803365805068,114.439000041518,
15.5469928482248));
#68796=CARTESIAN_POINT('Ctrl Pts',(-1.73268742066223,114.560474348342,14.962515710009));
#68797=CARTESIAN_POINT('Ctrl Pts',(-2.10810420031903,114.645998554686,14.3822819218351));
#68798=CARTESIAN_POINT('Ctrl Pts',(-2.25611753397905,114.695011815457,14.0181352682096));
#68799=CARTESIAN_POINT('Ctrl Pts',(-2.51617452672619,114.817785799399,13.0655010803562));
#68800=CARTESIAN_POINT('Ctrl Pts',(-2.07923546760282,114.97881806575,11.6838635643743));
#68801=CARTESIAN_POINT('Ctrl Pts',(-0.633626624243302,115.17950681556,10.8596907877631));
#68802=CARTESIAN_POINT('Ctrl Pts',(0.827782894109682,115.356601837116,10.8224739007951));
#68803=CARTESIAN_POINT('Ctrl Pts',(2.27930210313871,115.561175716011,11.8129702385169));
#68804=CARTESIAN_POINT('Ctrl Pts',(2.71753295138253,115.794337474248,13.7715057220754));
#68805=CARTESIAN_POINT('Ctrl Pts',(1.86214478959958,115.991188085206,15.2298020769417));
#68806=CARTESIAN_POINT('Ctrl Pts',(0.708060464255386,116.150212355569,15.8225350252024));
#68807=CARTESIAN_POINT('Ctrl Pts',(-0.589859124811868,116.310255772754,
15.9613469133736));
#68808=CARTESIAN_POINT('Ctrl Pts',(-2.14762077271569,116.512258718969,15.1970536166379));
#68809=CARTESIAN_POINT('Ctrl Pts',(-2.90049964340585,116.757632216301,13.2238631994602));
#68810=CARTESIAN_POINT('Ctrl Pts',(-2.07350245045037,117.012892421133,11.1917174196688));
#68811=CARTESIAN_POINT('Ctrl Pts',(-0.685204826526019,117.187183007416,
10.5894830032886));
#68812=CARTESIAN_POINT('Ctrl Pts',(0.0464586395786999,117.278479420639,
10.5932235447126));
#68813=CARTESIAN_POINT('Ctrl Pts',(2.52330414578958,104.544334690561,14.2761993092975));
#68814=CARTESIAN_POINT('Ctrl Pts',(2.26444673384787,104.630771939713,14.9186195695124));
#68815=CARTESIAN_POINT('Ctrl Pts',(1.24429907952034,104.800539934689,15.9673378684431));
#68816=CARTESIAN_POINT('Ctrl Pts',(-0.909151805697865,105.051168556281,
16.0572880327045));
#68817=CARTESIAN_POINT('Ctrl Pts',(-2.51185267037412,105.296713680551,14.6833512399881));
#68818=CARTESIAN_POINT('Ctrl Pts',(-2.74699427960123,105.539220603172,12.61254186955));
#68819=CARTESIAN_POINT('Ctrl Pts',(-1.52192995665394,105.778658576813,10.9562031581992));
#68820=CARTESIAN_POINT('Ctrl Pts',(0.141026337858125,105.975624011497,10.6481827059608));
#68821=CARTESIAN_POINT('Ctrl Pts',(1.32395978040542,106.131667612499,11.1189072722733));
#68822=CARTESIAN_POINT('Ctrl Pts',(2.01782263884653,106.247940549075,11.7643378112914));
#68823=CARTESIAN_POINT('Ctrl Pts',(2.42271211443298,106.363460565413,12.6148064891733));
#68824=CARTESIAN_POINT('Ctrl Pts',(2.50868062830299,106.507992168557,13.7903287569779));
#68825=CARTESIAN_POINT('Ctrl Pts',(1.87123444608351,106.68072834638,15.1086485757361));
#68826=CARTESIAN_POINT('Ctrl Pts',(0.35138274625492,106.880699072743,15.8497573985399));
#68827=CARTESIAN_POINT('Ctrl Pts',(-1.56584490841702,107.111458745282,15.4456466617042));
#68828=CARTESIAN_POINT('Ctrl Pts',(-2.75047794714966,107.371720097048,13.4040323174451));
#68829=CARTESIAN_POINT('Ctrl Pts',(-1.74840983356265,107.61213573347,11.4667684327686));
#68830=CARTESIAN_POINT('Ctrl Pts',(-0.261528740472371,107.802545697043,
10.9396465236436));
#68831=CARTESIAN_POINT('Ctrl Pts',(0.895562236215122,107.944455892434,11.11328342165));
#68832=CARTESIAN_POINT('Ctrl Pts',(1.82458086532744,108.085534355947,11.8215451966406));
#68833=CARTESIAN_POINT('Ctrl Pts',(2.21804963551908,108.202463152983,12.7034194596264));
#68834=CARTESIAN_POINT('Ctrl Pts',(2.25197017404353,108.295661441802,13.4553188370568));
#68835=CARTESIAN_POINT('Ctrl Pts',(2.10075218621871,108.388640068422,14.1908098768355));
#68836=CARTESIAN_POINT('Ctrl Pts',(1.6819063260689,108.481310493711,14.8316888949858));
#68837=CARTESIAN_POINT('Ctrl Pts',(1.07298812889412,108.573711747439,15.263298650126));
#68838=CARTESIAN_POINT('Ctrl Pts',(0.638953273746623,108.631357435354,15.4306469813635));
#68839=CARTESIAN_POINT('Ctrl Pts',(0.275032625095737,108.677415472885,15.4970935147077));
#68840=CARTESIAN_POINT('Ctrl Pts',(-0.0933706329656045,108.723438777596,
15.5171267745574));
#68841=CARTESIAN_POINT('Ctrl Pts',(-1.10920203624921,108.849853453934,15.3877446951435));
#68842=CARTESIAN_POINT('Ctrl Pts',(-2.00616298491076,108.987281107858,14.5390139439145));
#68843=CARTESIAN_POINT('Ctrl Pts',(-2.21068098928759,109.124441593605,13.4475367385515));
#68844=CARTESIAN_POINT('Ctrl Pts',(-2.16778442524582,109.215824484117,12.7121555531227));
#68845=CARTESIAN_POINT('Ctrl Pts',(-1.71867305098895,109.345188667898,11.7396475265348));
#68846=CARTESIAN_POINT('Ctrl Pts',(-0.513271747004666,109.51253168628,10.9969082861839));
#68847=CARTESIAN_POINT('Ctrl Pts',(1.02494743951852,109.695206643391,11.1683453977339));
#68848=CARTESIAN_POINT('Ctrl Pts',(1.94334784580527,109.847694653892,12.0767130216241));
#68849=CARTESIAN_POINT('Ctrl Pts',(2.22713521775881,109.969942405414,13.0281939470486));
#68850=CARTESIAN_POINT('Ctrl Pts',(2.18963649447169,110.092394463537,14.022565873329));
#68851=CARTESIAN_POINT('Ctrl Pts',(1.52069022531662,110.245900314157,15.1369042930342));
#68852=CARTESIAN_POINT('Ctrl Pts',(0.179468922594197,110.41557983498,15.6509042535181));
#68853=CARTESIAN_POINT('Ctrl Pts',(-1.07236556248268,110.570620319398,15.371036303217));
#68854=CARTESIAN_POINT('Ctrl Pts',(-1.94561505217817,110.710839097462,14.6105258150201));
#68855=CARTESIAN_POINT('Ctrl Pts',(-2.34947215999859,110.851811451771,13.5164893772982));
#68856=CARTESIAN_POINT('Ctrl Pts',(-2.20724917557952,110.969973676442,12.5506479605367));
#68857=CARTESIAN_POINT('Ctrl Pts',(-1.82496906095844,111.064949593997,11.8855664554727));
#68858=CARTESIAN_POINT('Ctrl Pts',(-1.42323481172131,111.136409256059,11.4715638343598));
#68859=CARTESIAN_POINT('Ctrl Pts',(-0.929689251255833,111.208109832547,
11.1687735629382));
#68860=CARTESIAN_POINT('Ctrl Pts',(-0.467350786387917,111.268062023047,
11.0254277885027));
#68861=CARTESIAN_POINT('Ctrl Pts',(-0.0837883073974405,111.316151398149,
10.9819202145342));
#68862=CARTESIAN_POINT('Ctrl Pts',(0.302920607414179,111.364326646958,10.9863874100361));
#68863=CARTESIAN_POINT('Ctrl Pts',(0.780702489862876,111.424705572184,11.0827833357131));
#68864=CARTESIAN_POINT('Ctrl Pts',(1.22183860617235,111.485308680154,11.2948307007585));
#68865=CARTESIAN_POINT('Ctrl Pts',(1.53535703894656,111.533927015618,11.5270478722568));
#68866=CARTESIAN_POINT('Ctrl Pts',(2.24578970618141,111.655701103841,12.1989421498836));
#68867=CARTESIAN_POINT('Ctrl Pts',(2.71404189861924,111.864500160352,14.0302595736244));
#68868=CARTESIAN_POINT('Ctrl Pts',(0.868773229907559,112.164099863729,16.0313463400168));
#68869=CARTESIAN_POINT('Ctrl Pts',(-1.86431278669073,112.468810924751,15.5439299909674));
#68870=CARTESIAN_POINT('Ctrl Pts',(-2.81962665275547,112.744389772042,13.2386636374405));
#68871=CARTESIAN_POINT('Ctrl Pts',(-1.92942425639895,112.989043552493,11.3610963458093));
#68872=CARTESIAN_POINT('Ctrl Pts',(-0.32660845311707,113.201176739136,10.5554795425911));
#68873=CARTESIAN_POINT('Ctrl Pts',(1.30665870255015,113.397859772161,10.8869582614042));
#68874=CARTESIAN_POINT('Ctrl Pts',(2.36240568754215,113.578421282006,11.9424274940553));
#68875=CARTESIAN_POINT('Ctrl Pts',(2.74698632682127,113.742270012166,13.2401466441822));
#68876=CARTESIAN_POINT('Ctrl Pts',(2.45943368696635,113.907443914416,14.5751218014176));
#68877=CARTESIAN_POINT('Ctrl Pts',(1.56065352247533,114.073919000753,15.6170655906792));
#68878=CARTESIAN_POINT('Ctrl Pts',(0.262877564645767,114.241667520256,16.104946279976));
#68879=CARTESIAN_POINT('Ctrl Pts',(-1.12130069887536,114.410654514264,15.910320675758));
#68880=CARTESIAN_POINT('Ctrl Pts',(-2.06074202909693,114.552480211929,15.2100522042989));
#68881=CARTESIAN_POINT('Ctrl Pts',(-2.48594725837351,114.652263334868,14.5249911967502));
#68882=CARTESIAN_POINT('Ctrl Pts',(-2.65059046871045,114.709425158385,14.0971739883781));
#68883=CARTESIAN_POINT('Ctrl Pts',(-2.93299871232966,114.852563076709,12.9810302784921));
#68884=CARTESIAN_POINT('Ctrl Pts',(-2.39343563973433,115.039997690066,11.3834718532269));
#68885=CARTESIAN_POINT('Ctrl Pts',(-0.699766072623095,115.272696808793,
10.4594318898784));
#68886=CARTESIAN_POINT('Ctrl Pts',(0.990046483666062,115.477412751704,10.447784021228));
#68887=CARTESIAN_POINT('Ctrl Pts',(2.638441772619,115.712840845808,11.6193126011455));
#68888=CARTESIAN_POINT('Ctrl Pts',(3.09644634185781,115.979463763659,13.868009950666));
#68889=CARTESIAN_POINT('Ctrl Pts',(2.09414774288195,116.202905610514,15.5043094422683));
#68890=CARTESIAN_POINT('Ctrl Pts',(0.780626034643881,116.382302051056,16.1493898940948));
#68891=CARTESIAN_POINT('Ctrl Pts',(-0.679927062710262,116.56205342679,16.2792627781633));
#68892=CARTESIAN_POINT('Ctrl Pts',(-2.40100684596654,116.787438637619,15.3935722350285));
#68893=CARTESIAN_POINT('Ctrl Pts',(-3.19146714133348,117.058437598141,13.1983636888011));
#68894=CARTESIAN_POINT('Ctrl Pts',(-2.24400753524095,117.337645152896,10.994322898193));
#68895=CARTESIAN_POINT('Ctrl Pts',(-0.733153825131694,117.525786383484,
10.3725440366635));
#68896=CARTESIAN_POINT('Ctrl Pts',(0.0536953672426754,117.623989923356,
10.3900450426506));
#68897=CARTESIAN_POINT('Ctrl Pts',(2.33155035069585,104.889225650322,14.2055375918348));
#68898=CARTESIAN_POINT('Ctrl Pts',(2.08034610834311,104.969230432376,14.7956119297448));
#68899=CARTESIAN_POINT('Ctrl Pts',(1.12103333601473,105.125277942201,15.7388021653477));
#68900=CARTESIAN_POINT('Ctrl Pts',(-0.834640843745923,105.352615676887,
15.7758767760086));
#68901=CARTESIAN_POINT('Ctrl Pts',(-2.24153167180261,105.572517059975,14.5116838276913));
#68902=CARTESIAN_POINT('Ctrl Pts',(-2.40598310899397,105.787057428874,12.6742806194831));
#68903=CARTESIAN_POINT('Ctrl Pts',(-1.29913634113558,105.996446033516,11.2516000445698));
#68904=CARTESIAN_POINT('Ctrl Pts',(0.146427066887681,106.166847785682,11.0205859480082));
#68905=CARTESIAN_POINT('Ctrl Pts',(1.15289298394829,106.300866815296,11.4490376631154));
#68906=CARTESIAN_POINT('Ctrl Pts',(1.73300486118504,106.400268444437,12.0151805157652));
#68907=CARTESIAN_POINT('Ctrl Pts',(2.06017859115705,106.498603192252,12.7476216268525));
#68908=CARTESIAN_POINT('Ctrl Pts',(2.10861494988465,106.621142873788,13.7463511749871));
#68909=CARTESIAN_POINT('Ctrl Pts',(1.54242389189715,106.766850231498,14.8449521863969));
#68910=CARTESIAN_POINT('Ctrl Pts',(0.250780847804702,106.934634010421,15.4340902574224));
#68911=CARTESIAN_POINT('Ctrl Pts',(-1.34286783755684,107.127458557769,15.0545463186142));
#68912=CARTESIAN_POINT('Ctrl Pts',(-2.28475812865515,107.344194114315,13.3277967074203));
#68913=CARTESIAN_POINT('Ctrl Pts',(-1.40858501721658,107.544228897403,11.7372638776285));
#68914=CARTESIAN_POINT('Ctrl Pts',(-0.157315341574774,107.702957504394,
11.3301445063092));
#68915=CARTESIAN_POINT('Ctrl Pts',(0.805802449946862,107.821510394672,11.500657420647));
#68916=CARTESIAN_POINT('Ctrl Pts',(1.56890259327139,107.939725261016,12.1146342441558));
#68917=CARTESIAN_POINT('Ctrl Pts',(1.88063589651449,108.03808432581,12.8652926986567));
#68918=CARTESIAN_POINT('Ctrl Pts',(1.89250146863796,108.116761065377,13.5009698411227));
#68919=CARTESIAN_POINT('Ctrl Pts',(1.74806220951704,108.195452356148,14.1201934919506));
#68920=CARTESIAN_POINT('Ctrl Pts',(1.3779596901824,108.274210372457,14.6558203685491));
#68921=CARTESIAN_POINT('Ctrl Pts',(0.848197763549307,108.3531145115,15.0108711049122));
#68922=CARTESIAN_POINT('Ctrl Pts',(0.472477938301414,108.402504762127,15.1445620137306));
#68923=CARTESIAN_POINT('Ctrl Pts',(0.158284083568963,108.442070687982,15.1934682571603));
#68924=CARTESIAN_POINT('Ctrl Pts',(-0.159333761024929,108.481680893968,
15.2023951303368));
#68925=CARTESIAN_POINT('Ctrl Pts',(-1.03312858161163,108.590779149026,15.0681461191704));
#68926=CARTESIAN_POINT('Ctrl Pts',(-1.79851056783559,108.710538614764,14.3107721037796));
#68927=CARTESIAN_POINT('Ctrl Pts',(-1.95473985914995,108.831427270441,13.3438552776906));
#68928=CARTESIAN_POINT('Ctrl Pts',(-1.90031652365022,108.912344269774,12.6935320062921));
#68929=CARTESIAN_POINT('Ctrl Pts',(-1.47907665313292,109.027712703007,11.8357041714121));
#68930=CARTESIAN_POINT('Ctrl Pts',(-0.376060965686619,109.178700123857,
11.1898854843336));
#68931=CARTESIAN_POINT('Ctrl Pts',(1.0280682732195,109.345845568149,11.3775706713003));
#68932=CARTESIAN_POINT('Ctrl Pts',(1.86292445096866,109.487404866621,12.2391753140972));
#68933=CARTESIAN_POINT('Ctrl Pts',(2.10911958271135,109.602163393282,13.1387589986266));
#68934=CARTESIAN_POINT('Ctrl Pts',(2.05257570052719,109.71797416908,14.0783972543364));
#68935=CARTESIAN_POINT('Ctrl Pts',(1.39113623547589,109.864789686052,15.131527464595));
#68936=CARTESIAN_POINT('Ctrl Pts',(0.0790966134581977,110.029523847502,
15.6050505564782));
#68937=CARTESIAN_POINT('Ctrl Pts',(-1.14700713117737,110.18201499458,15.304974336181));
#68938=CARTESIAN_POINT('Ctrl Pts',(-2.00049932982729,110.321449796495,14.5314179570271));
#68939=CARTESIAN_POINT('Ctrl Pts',(-2.38532970831892,110.46315108634,13.4236997022875));
#68940=CARTESIAN_POINT('Ctrl Pts',(-2.22222592935636,110.583179758602,12.4451299058044));
#68941=CARTESIAN_POINT('Ctrl Pts',(-1.81750585540209,110.680399393693,11.7718400727418));
#68942=CARTESIAN_POINT('Ctrl Pts',(-1.39587630129307,110.753916197775,11.3538690943344));
#68943=CARTESIAN_POINT('Ctrl Pts',(-0.879527045212157,110.828044755399,
11.0505516327519));
#68944=CARTESIAN_POINT('Ctrl Pts',(-0.39629435371655,110.890329228167,10.9107249601033));
#68945=CARTESIAN_POINT('Ctrl Pts',(0.00454392058224056,110.94046714444,
10.8729793284117));
#68946=CARTESIAN_POINT('Ctrl Pts',(0.408649518601699,110.990812634386,10.8853082281896));
#68947=CARTESIAN_POINT('Ctrl Pts',(0.907905505257022,111.054132837524,10.9957456136948));
#68948=CARTESIAN_POINT('Ctrl Pts',(1.36857976781383,111.117976095091,11.2277016691471));
#68949=CARTESIAN_POINT('Ctrl Pts',(1.69550116792685,111.169365559157,11.4793457892818));
#68950=CARTESIAN_POINT('Ctrl Pts',(2.43500243622407,111.298363403658,12.2048731864356));
#68951=CARTESIAN_POINT('Ctrl Pts',(2.90824117980769,111.521690513464,14.1710135659361));
#68952=CARTESIAN_POINT('Ctrl Pts',(0.87418843442569,111.84714071396,16.3173551159956));
#68953=CARTESIAN_POINT('Ctrl Pts',(-2.12852629974458,112.18263879406,15.7400988882763));
#68954=CARTESIAN_POINT('Ctrl Pts',(-3.15766417237389,112.489554478412,13.1576879572197));
#68955=CARTESIAN_POINT('Ctrl Pts',(-2.12729900151401,112.764173224004,11.0643185486799));
#68956=CARTESIAN_POINT('Ctrl Pts',(-0.305010508991329,113.003561180212,
10.1815748743034));
#68957=CARTESIAN_POINT('Ctrl Pts',(1.54097699817032,113.226499114754,10.5840852116775));
#68958=CARTESIAN_POINT('Ctrl Pts',(2.72397064042765,113.431793473111,11.8018421910831));
#68959=CARTESIAN_POINT('Ctrl Pts',(3.14073777515895,113.618486400348,13.2869860743474));
#68960=CARTESIAN_POINT('Ctrl Pts',(2.79056087176101,113.807001003966,14.8060371070729));
#68961=CARTESIAN_POINT('Ctrl Pts',(1.74638840446472,113.9972232938,15.9820143756473));
#68962=CARTESIAN_POINT('Ctrl Pts',(0.254328506124801,114.189036002109,16.5187674303024));
#68963=CARTESIAN_POINT('Ctrl Pts',(-1.32579803194563,114.382308987009,16.2736485032911));
#68964=CARTESIAN_POINT('Ctrl Pts',(-2.38879663753162,114.544486075516,15.4575886985887));
#68965=CARTESIAN_POINT('Ctrl Pts',(-2.86379031642799,114.658528115049,14.6677004716653));
#68966=CARTESIAN_POINT('Ctrl Pts',(-3.04506340344182,114.723838501314,14.1762127085468));
#68967=CARTESIAN_POINT('Ctrl Pts',(-3.34982289793312,114.88734035402,12.8965594766281));
#68968=CARTESIAN_POINT('Ctrl Pts',(-2.70763581186582,115.101177314382,11.0830801420794));
#68969=CARTESIAN_POINT('Ctrl Pts',(-0.765905521002873,115.365886802026,
10.0591729919936));
#68970=CARTESIAN_POINT('Ctrl Pts',(1.15231007322245,115.598223666293,10.0730941416609));
#68971=CARTESIAN_POINT('Ctrl Pts',(2.9975814420993,115.864505975606,11.4256549637742));
#68972=CARTESIAN_POINT('Ctrl Pts',(3.4753597323331,116.164590053071,13.9645141792565));
#68973=CARTESIAN_POINT('Ctrl Pts',(2.32615069616434,116.414623135822,15.7788168075948));
#68974=CARTESIAN_POINT('Ctrl Pts',(0.853191605032384,116.614391746542,16.4762447629873));
#68975=CARTESIAN_POINT('Ctrl Pts',(-0.769995000608643,116.813851080826,
16.5971786429528));
#68976=CARTESIAN_POINT('Ctrl Pts',(-2.65439291921737,117.062618556269,15.5900908534192));
#68977=CARTESIAN_POINT('Ctrl Pts',(-3.4824346392611,117.359242979981,13.1728641781418));
#68978=CARTESIAN_POINT('Ctrl Pts',(-2.41451262003151,117.662397884661,10.796928376717));
#68979=CARTESIAN_POINT('Ctrl Pts',(-0.781102823737367,117.864389759553,
10.1556050700385));
#68980=CARTESIAN_POINT('Ctrl Pts',(0.0609320949066517,117.969500426075,
10.1868665405886));
#68981=CARTESIAN_POINT('Origin',(2.375,22.1,13.3));
#68982=CARTESIAN_POINT('Origin',(1.7,145.,13.3));
#68983=CARTESIAN_POINT('',(-1.7,145.,13.3));
#68984=CARTESIAN_POINT('Origin',(0.,145.,13.3));
#68985=CARTESIAN_POINT('Origin',(0.,144.85,13.3));
#68986=CARTESIAN_POINT('',(-2.,144.7,13.3));
#68987=CARTESIAN_POINT('Origin',(0.,144.7,13.3));
#68988=CARTESIAN_POINT('',(-1.85,144.85,13.3));
#68989=CARTESIAN_POINT('Origin',(0.,132.35,13.3));
#68990=CARTESIAN_POINT('',(-2.,120.,13.3));
#68991=CARTESIAN_POINT('Origin',(0.,120.,13.3));
#68992=CARTESIAN_POINT('',(-2.,132.35,13.3));
#68993=CARTESIAN_POINT('Origin',(2.5,120.,13.3));
#68994=CARTESIAN_POINT('Origin',(0.,20.25,13.3));
#68995=CARTESIAN_POINT('',(-2.2,20.1,13.3));
#68996=CARTESIAN_POINT('',(-2.35,20.25,13.3));
#68997=CARTESIAN_POINT('Origin',(0.,20.1,13.3));
#68998=CARTESIAN_POINT('Origin',(2.,20.1,13.3));
#68999=CARTESIAN_POINT('',(-2.,20.1,13.3));
#69000=CARTESIAN_POINT('Origin',(0.,20.1,13.3));
#69001=CARTESIAN_POINT('Origin',(0.,15.45,13.3));
#69002=CARTESIAN_POINT('',(-2.,10.8,13.3));
#69003=CARTESIAN_POINT('Origin',(0.,10.8,13.3));
#69004=CARTESIAN_POINT('',(-2.,15.45,13.3));
#69005=CARTESIAN_POINT('Origin',(0.,10.65,13.3));
#69006=CARTESIAN_POINT('',(-1.7,10.5,13.3));
#69007=CARTESIAN_POINT('',(-1.85,10.65,13.3));
#69008=CARTESIAN_POINT('Origin',(0.,10.5,13.3));
#69009=CARTESIAN_POINT('Origin',(0.,10.5,13.3));
#135257=UNCERTAINTY_MEASURE_WITH_UNIT(LENGTH_MEASURE(0.01),#135283,
'DISTANCE_ACCURACY_VALUE',
'Maximum model space distance between geometric entities at asserted c
onnectivities');
#135267=UNCERTAINTY_MEASURE_WITH_UNIT(LENGTH_MEASURE(0.01),#135283,
'DISTANCE_ACCURACY_VALUE',
'Maximum model space distance between geometric entities at asserted c
onnectivities');
#135272=(
GEOMETRIC_REPRESENTATION_CONTEXT(3)
GLOBAL_UNCERTAINTY_ASSIGNED_CONTEXT((#135257))
GLOBAL_UNIT_ASSIGNED_CONTEXT((#135283,#135285,#135286))
REPRESENTATION_CONTEXT('','3D')
);
#135282=(
GEOMETRIC_REPRESENTATION_CONTEXT(3)
GLOBAL_UNCERTAINTY_ASSIGNED_CONTEXT((#135267))
GLOBAL_UNIT_ASSIGNED_CONTEXT((#135283,#135285,#135286))
REPRESENTATION_CONTEXT('','3D')
);
#135283=(
LENGTH_UNIT()
NAMED_UNIT(*)
SI_UNIT(.MILLI.,.METRE.)
);
#135285=(
NAMED_UNIT(*)
PLANE_ANGLE_UNIT()
SI_UNIT($,.RADIAN.)
);
#135286=(
NAMED_UNIT(*)
SI_UNIT($,.STERADIAN.)
SOLID_ANGLE_UNIT()
);
#135291=SHAPE_DEFINITION_REPRESENTATION(#135305,#135340);
#135305=PRODUCT_DEFINITION_SHAPE('',$,#135355);
#135340=SHAPE_REPRESENTATION('',(#32403),#135272);
#135350=PRODUCT_DEFINITION_CONTEXT('part definition',#135394,'design');
#135355=PRODUCT_DEFINITION('2026-10-15-19-09-11-258',
'Precision Feed Screw D5 Lead 2',#135369,#135350);
#135369=PRODUCT_DEFINITION_FORMATION('',$,#135400);
#135394=APPLICATION_CONTEXT(
'Core Data for Automotive Mechanical Design Process');
#135395=PRODUCT_CONTEXT('part definition',#135394,'mechanical');
#135400=PRODUCT('2026-10-15-19-09-11-258',
'Precision Feed Screw D5 Lead 2',$,(#135395));
#135414=PRESENTATION_STYLE_ASSIGNMENT((#135428));
#135428=SURFACE_STYLE_USAGE(.BOTH.,#135442);
#135442=SURFACE_SIDE_STYLE('',(#135456));
#135456=SURFACE_STYLE_FILL_AREA(#135470);
#135470=FILL_AREA_STYLE('Opaque(234,236,239)',(#135484));
#135484=FILL_AREA_STYLE_COLOUR('Opaque(234,236,239)',#135498);
#135498=COLOUR_RGB('Opaque(234,236,239)', 0.40784314, 0.44705882, 0.49803922);
ENDSEC;
END-ISO-10303-21;
